ISO-10303-21;
HEADER;
/* Generated by software containing ST-Developer
 * from STEP Tools, Inc. (www.steptools.com) 
 */

FILE_DESCRIPTION(
/* description */ (''),
/* implementation_level */ '2;1');

FILE_NAME(
/* name */ 'Screw.step',
/* time_stamp */ '2026-10-04T16:36:43-07:00',
/* author */ (''),
/* organization */ (''),
/* preprocessor_version */ 'ST-DEVELOPER v20.2',
/* originating_system */ 'Autodesk Translation Framework v15.15.0.0',
/* authorisation */ '');

FILE_SCHEMA (('AUTOMOTIVE_DESIGN { 1 0 10303 214 3 1 1 }'));
ENDSEC;

DATA;
#10=MECHANICAL_DESIGN_GEOMETRIC_PRESENTATION_REPRESENTATION('',(#67),#33474);
#57=SHAPE_REPRESENTATION_RELATIONSHIP('SRR','None',#33497,#62);
#62=ADVANCED_BREP_SHAPE_REPRESENTATION('',(#72),#33469);
#67=STYLED_ITEM('',(#33531),#72);
#72=MANIFOLD_SOLID_BREP('Body1',#2807);
#77=TOROIDAL_SURFACE('',#3082,4.5,1.);
#84=B_SPLINE_SURFACE_WITH_KNOTS('',3,3,((#27469,#27470,#27471,#27472,#27473,
#27474,#27475,#27476,#27477,#27478,#27479,#27480,#27481,#27482,#27483,#27484,
#27485,#27486,#27487,#27488,#27489,#27490,#27491,#27492,#27493,#27494,#27495,
#27496,#27497,#27498,#27499,#27500,#27501,#27502,#27503,#27504,#27505,#27506,
#27507,#27508,#27509,#27510,#27511,#27512,#27513,#27514,#27515,#27516,#27517,
#27518,#27519,#27520,#27521,#27522,#27523,#27524,#27525,#27526,#27527,#27528,
#27529,#27530,#27531,#27532,#27533,#27534,#27535,#27536,#27537,#27538,#27539,
#27540,#27541,#27542,#27543,#27544,#27545,#27546,#27547,#27548,#27549,#27550,
#27551,#27552,#27553,#27554,#27555,#27556,#27557,#27558,#27559,#27560,#27561,
#27562,#27563,#27564,#27565,#27566,#27567,#27568,#27569,#27570,#27571,#27572,
#27573,#27574,#27575,#27576,#27577,#27578,#27579,#27580,#27581,#27582,#27583,
#27584,#27585,#27586,#27587,#27588,#27589,#27590,#27591,#27592,#27593,#27594,
#27595,#27596,#27597,#27598,#27599,#27600,#27601,#27602,#27603,#27604,#27605,
#27606,#27607,#27608,#27609,#27610,#27611,#27612,#27613,#27614,#27615,#27616,
#27617,#27618,#27619,#27620,#27621,#27622,#27623,#27624,#27625,#27626,#27627,
#27628,#27629,#27630,#27631,#27632,#27633,#27634,#27635,#27636,#27637,#27638,
#27639,#27640,#27641,#27642,#27643,#27644,#27645,#27646,#27647,#27648,#27649,
#27650,#27651,#27652,#27653,#27654,#27655,#27656,#27657,#27658,#27659,#27660,
#27661,#27662,#27663,#27664,#27665,#27666,#27667,#27668,#27669,#27670,#27671,
#27672,#27673,#27674,#27675,#27676,#27677,#27678,#27679,#27680,#27681,#27682,
#27683,#27684,#27685,#27686,#27687,#27688,#27689,#27690,#27691,#27692,#27693,
#27694,#27695,#27696,#27697,#27698,#27699,#27700,#27701,#27702,#27703,#27704,
#27705,#27706,#27707,#27708,#27709),(#27710,#27711,#27712,#27713,#27714,
#27715,#27716,#27717,#27718,#27719,#27720,#27721,#27722,#27723,#27724,#27725,
#27726,#27727,#27728,#27729,#27730,#27731,#27732,#27733,#27734,#27735,#27736,
#27737,#27738,#27739,#27740,#27741,#27742,#27743,#27744,#27745,#27746,#27747,
#27748,#27749,#27750,#27751,#27752,#27753,#27754,#27755,#27756,#27757,#27758,
#27759,#27760,#27761,#27762,#27763,#27764,#27765,#27766,#27767,#27768,#27769,
#27770,#27771,#27772,#27773,#27774,#27775,#27776,#27777,#27778,#27779,#27780,
#27781,#27782,#27783,#27784,#27785,#27786,#27787,#27788,#27789,#27790,#27791,
#27792,#27793,#27794,#27795,#27796,#27797,#27798,#27799,#27800,#27801,#27802,
#27803,#27804,#27805,#27806,#27807,#27808,#27809,#27810,#27811,#27812,#27813,
#27814,#27815,#27816,#27817,#27818,#27819,#27820,#27821,#27822,#27823,#27824,
#27825,#27826,#27827,#27828,#27829,#27830,#27831,#27832,#27833,#27834,#27835,
#27836,#27837,#27838,#27839,#27840,#27841,#27842,#27843,#27844,#27845,#27846,
#27847,#27848,#27849,#27850,#27851,#27852,#27853,#27854,#27855,#27856,#27857,
#27858,#27859,#27860,#27861,#27862,#27863,#27864,#27865,#27866,#27867,#27868,
#27869,#27870,#27871,#27872,#27873,#27874,#27875,#27876,#27877,#27878,#27879,
#27880,#27881,#27882,#27883,#27884,#27885,#27886,#27887,#27888,#27889,#27890,
#27891,#27892,#27893,#27894,#27895,#27896,#27897,#27898,#27899,#27900,#27901,
#27902,#27903,#27904,#27905,#27906,#27907,#27908,#27909,#27910,#27911,#27912,
#27913,#27914,#27915,#27916,#27917,#27918,#27919,#27920,#27921,#27922,#27923,
#27924,#27925,#27926,#27927,#27928,#27929,#27930,#27931,#27932,#27933,#27934,
#27935,#27936,#27937,#27938,#27939,#27940,#27941,#27942,#27943,#27944,#27945,
#27946,#27947,#27948,#27949,#27950),(#27951,#27952,#27953,#27954,#27955,
#27956,#27957,#27958,#27959,#27960,#27961,#27962,#27963,#27964,#27965,#27966,
#27967,#27968,#27969,#27970,#27971,#27972,#27973,#27974,#27975,#27976,#27977,
#27978,#27979,#27980,#27981,#27982,#27983,#27984,#27985,#27986,#27987,#27988,
#27989,#27990,#27991,#27992,#27993,#27994,#27995,#27996,#27997,#27998,#27999,
#28000,#28001,#28002,#28003,#28004,#28005,#28006,#28007,#28008,#28009,#28010,
#28011,#28012,#28013,#28014,#28015,#28016,#28017,#28018,#28019,#28020,#28021,
#28022,#28023,#28024,#28025,#28026,#28027,#28028,#28029,#28030,#28031,#28032,
#28033,#28034,#28035,#28036,#28037,#28038,#28039,#28040,#28041,#28042,#28043,
#28044,#28045,#28046,#28047,#28048,#28049,#28050,#28051,#28052,#28053,#28054,
#28055,#28056,#28057,#28058,#28059,#28060,#28061,#28062,#28063,#28064,#28065,
#28066,#28067,#28068,#28069,#28070,#28071,#28072,#28073,#28074,#28075,#28076,
#28077,#28078,#28079,#28080,#28081,#28082,#28083,#28084,#28085,#28086,#28087,
#28088,#28089,#28090,#28091,#28092,#28093,#28094,#28095,#28096,#28097,#28098,
#28099,#28100,#28101,#28102,#28103,#28104,#28105,#28106,#28107,#28108,#28109,
#28110,#28111,#28112,#28113,#28114,#28115,#28116,#28117,#28118,#28119,#28120,
#28121,#28122,#28123,#28124,#28125,#28126,#28127,#28128,#28129,#28130,#28131,
#28132,#28133,#28134,#28135,#28136,#28137,#28138,#28139,#28140,#28141,#28142,
#28143,#28144,#28145,#28146,#28147,#28148,#28149,#28150,#28151,#28152,#28153,
#28154,#28155,#28156,#28157,#28158,#28159,#28160,#28161,#28162,#28163,#28164,
#28165,#28166,#28167,#28168,#28169,#28170,#28171,#28172,#28173,#28174,#28175,
#28176,#28177,#28178,#28179,#28180,#28181,#28182,#28183,#28184,#28185,#28186,
#28187,#28188,#28189,#28190,#28191),(#28192,#28193,#28194,#28195,#28196,
#28197,#28198,#28199,#28200,#28201,#28202,#28203,#28204,#28205,#28206,#28207,
#28208,#28209,#28210,#28211,#28212,#28213,#28214,#28215,#28216,#28217,#28218,
#28219,#28220,#28221,#28222,#28223,#28224,#28225,#28226,#28227,#28228,#28229,
#28230,#28231,#28232,#28233,#28234,#28235,#28236,#28237,#28238,#28239,#28240,
#28241,#28242,#28243,#28244,#28245,#28246,#28247,#28248,#28249,#28250,#28251,
#28252,#28253,#28254,#28255,#28256,#28257,#28258,#28259,#28260,#28261,#28262,
#28263,#28264,#28265,#28266,#28267,#28268,#28269,#28270,#28271,#28272,#28273,
#28274,#28275,#28276,#28277,#28278,#28279,#28280,#28281,#28282,#28283,#28284,
#28285,#28286,#28287,#28288,#28289,#28290,#28291,#28292,#28293,#28294,#28295,
#28296,#28297,#28298,#28299,#28300,#28301,#28302,#28303,#28304,#28305,#28306,
#28307,#28308,#28309,#28310,#28311,#28312,#28313,#28314,#28315,#28316,#28317,
#28318,#28319,#28320,#28321,#28322,#28323,#28324,#28325,#28326,#28327,#28328,
#28329,#28330,#28331,#28332,#28333,#28334,#28335,#28336,#28337,#28338,#28339,
#28340,#28341,#28342,#28343,#28344,#28345,#28346,#28347,#28348,#28349,#28350,
#28351,#28352,#28353,#28354,#28355,#28356,#28357,#28358,#28359,#28360,#28361,
#28362,#28363,#28364,#28365,#28366,#28367,#28368,#28369,#28370,#28371,#28372,
#28373,#28374,#28375,#28376,#28377,#28378,#28379,#28380,#28381,#28382,#28383,
#28384,#28385,#28386,#28387,#28388,#28389,#28390,#28391,#28392,#28393,#28394,
#28395,#28396,#28397,#28398,#28399,#28400,#28401,#28402,#28403,#28404,#28405,
#28406,#28407,#28408,#28409,#28410,#28411,#28412,#28413,#28414,#28415,#28416,
#28417,#28418,#28419,#28420,#28421,#28422,#28423,#28424,#28425,#28426,#28427,
#28428,#28429,#28430,#28431,#28432)),.UNSPECIFIED.,.F.,.F.,.F.,(4,4),(4,
1,1,1,1,1,1,1,1,1,1,1,1,1,1,1,1,1,1,1,1,1,1,1,1,1,1,1,1,1,1,1,1,1,1,1,1,
1,1,1,1,1,1,1,1,1,1,1,1,1,1,1,1,1,1,1,1,1,1,1,1,1,1,1,1,1,1,1,1,1,1,1,1,
1,1,1,1,1,1,1,1,1,1,1,1,1,1,1,1,1,1,1,1,1,1,1,1,1,1,1,1,1,1,1,1,1,1,1,1,
1,1,1,1,1,1,1,1,1,1,1,1,1,1,1,1,1,1,1,1,1,1,1,1,1,1,1,1,1,1,1,1,1,1,1,1,
1,1,1,1,1,1,1,1,1,1,1,1,1,1,1,1,1,1,1,1,1,1,1,1,1,1,1,1,1,1,1,1,1,1,1,1,
1,1,1,1,1,1,1,1,1,1,1,1,1,1,1,1,1,1,1,1,1,1,1,1,1,1,1,1,1,1,1,1,1,1,1,1,
1,1,1,1,1,1,1,1,1,1,1,1,1,1,1,1,1,1,1,1,1,4),(-0.000412226121642421,0.0529946871768046),
(8.30797483681352,9.30683859552365,10.3055194638844,11.3042003322452,12.3028812006059,
13.3015620689667,14.3002429373274,15.2989238056882,16.2976046740489,17.2962855424097,
18.2949664107704,19.2936472791312,20.2923281474919,21.2910090158527,22.2896898842134,
23.2883707525742,24.2870516209349,25.2857324892957,26.2844133576564,27.2830942260172,
28.2817750943779,29.2804559627387,30.2791368310994,31.2778176994602,32.2764985678209,
33.2751794361817,34.2738603045424,35.2725411729032,36.2712220412639,37.2699029096247,
38.2685837779855,39.2672646463462,40.265945514707,41.2646263830677,42.2633072514285,
43.2619881197892,44.26066898815,45.2593498565107,46.2580307248715,47.2567115932322,
48.255392461593,49.2540733299537,50.2527541983145,51.2514350666752,52.250115935036,
53.2487968033967,54.2474776717575,55.2461585401182,56.244839408479,57.2435202768397,
58.2422011452005,59.2408820135612,60.239562881922,61.2382437502827,62.2369246186435,
63.2356054870042,64.234286355365,65.2329672237257,66.2316480920865,67.2303289604472,
68.229009828808,69.2276906971688,70.2263715655295,71.2250524338903,72.223733302251,
73.2224141706118,74.2210950389725,75.2197759073333,76.218456775694,77.2171376440548,
78.2158185124155,79.2144993807763,80.213180249137,81.2118611174978,82.2105419858585,
83.2092228542193,84.20790372258,85.2065845909408,86.2052654593015,87.2039463276623,
88.202627196023,89.2013080643838,90.1999889327445,91.1986698011053,92.197350669466,
93.1960315378268,94.1947124061875,95.1933932745483,96.192074142909,97.1907550112698,
98.1894358796306,99.1881167479913,100.186797616352,101.185478484713,102.184159353074,
103.182840221434,104.181521089795,105.180201958156,106.178882826517,107.177563694877,
108.176244563238,109.174925431599,110.17360629996,111.17228716832,112.170968036681,
113.169648905042,114.168329773403,115.167010641763,116.165691510124,117.164372378485,
118.163053246846,119.161734115206,120.160414983567,121.159095851928,122.157776720289,
123.156457588649,124.15513845701,125.153819325371,126.152500193732,127.151181062092,
128.149861930453,129.148542798814,130.147223667175,131.145904535535,132.144585403896,
133.143266272257,134.141947140618,135.140628008978,136.139308877339,137.1379897457,
138.136670614061,139.135351482421,140.134032350782,141.132713219143,142.131394087504,
143.130074955864,144.128755824225,145.127436692586,146.126117560947,147.124798429307,
148.123479297668,149.122160166029,150.12084103439,151.11952190275,152.118202771111,
153.116883639472,154.115564507833,155.114245376193,156.112926244554,157.111607112915,
158.110287981276,159.108968849636,160.107649717997,161.106330586358,162.105011454719,
163.103692323079,164.10237319144,165.101054059801,166.099734928162,167.098415796522,
168.097096664883,169.095777533244,170.094458401605,171.093139269965,172.091820138326,
173.090501006687,174.089181875048,175.087862743408,176.086543611769,177.08522448013,
178.083905348491,179.082586216851,180.081267085212,181.079947953573,182.078628821934,
183.077309690294,184.075990558655,185.074671427016,186.073352295377,187.072033163737,
188.070714032098,189.069394900459,190.06807576882,191.06675663718,192.065437505541,
193.064118373902,194.062799242263,195.061480110623,196.060160978984,197.058841847345,
198.057522715706,199.056203584066,200.054884452427,201.053565320788,202.052246189149,
203.050927057509,204.04960792587,205.048288794231,206.046969662592,207.045650530952,
208.044331399313,209.043012267674,210.041693136035,211.040374004395,212.039054872756,
213.037735741117,214.036416609478,215.035097477838,216.033778346199,217.03245921456,
218.031140082921,219.029820951281,220.028501819642,221.027182688003,222.025863556364,
223.024544424724,224.023225293085,225.021906161446,226.020587029807,227.019267898167,
228.017948766528,229.016629634889,230.01531050325,231.01399137161,232.012672239971,
233.011353108332,234.010033976693,235.008714845054,236.007395713414,237.006076581775,
238.004757450136,239.003438318497,240.002119186857,241.000800055218,241.999480923579,
242.99816179194,243.9968426603,244.995523528661,245.994616623144),
 .UNSPECIFIED.);
#85=B_SPLINE_SURFACE_WITH_KNOTS('',3,3,((#28611,#28612,#28613,#28614,#28615,
#28616,#28617,#28618,#28619,#28620,#28621,#28622,#28623,#28624,#28625,#28626,
#28627,#28628,#28629,#28630,#28631,#28632,#28633,#28634,#28635,#28636,#28637,
#28638,#28639,#28640,#28641,#28642,#28643,#28644,#28645,#28646,#28647,#28648,
#28649,#28650,#28651,#28652,#28653,#28654,#28655,#28656,#28657,#28658,#28659,
#28660,#28661,#28662,#28663,#28664,#28665,#28666,#28667,#28668,#28669,#28670,
#28671,#28672,#28673,#28674,#28675,#28676,#28677,#28678,#28679,#28680,#28681,
#28682,#28683,#28684,#28685,#28686,#28687,#28688,#28689,#28690,#28691,#28692,
#28693,#28694,#28695,#28696,#28697,#28698,#28699,#28700,#28701,#28702,#28703,
#28704,#28705,#28706,#28707,#28708,#28709,#28710,#28711,#28712,#28713,#28714,
#28715,#28716,#28717,#28718,#28719,#28720,#28721,#28722,#28723,#28724,#28725,
#28726,#28727,#28728,#28729,#28730,#28731,#28732,#28733,#28734,#28735,#28736,
#28737,#28738,#28739,#28740,#28741,#28742,#28743,#28744,#28745,#28746,#28747,
#28748,#28749,#28750,#28751,#28752,#28753,#28754,#28755,#28756,#28757,#28758,
#28759,#28760,#28761,#28762,#28763,#28764,#28765,#28766,#28767,#28768,#28769,
#28770,#28771,#28772,#28773,#28774,#28775,#28776,#28777,#28778,#28779,#28780,
#28781,#28782,#28783,#28784,#28785,#28786,#28787,#28788,#28789,#28790,#28791,
#28792,#28793,#28794,#28795,#28796,#28797,#28798,#28799,#28800,#28801,#28802,
#28803,#28804,#28805,#28806,#28807,#28808,#28809,#28810,#28811,#28812,#28813,
#28814,#28815,#28816,#28817,#28818,#28819,#28820,#28821,#28822,#28823,#28824,
#28825,#28826,#28827,#28828,#28829,#28830,#28831,#28832,#28833,#28834,#28835,
#28836,#28837,#28838,#28839,#28840,#28841,#28842,#28843,#28844,#28845,#28846,
#28847,#28848,#28849,#28850,#28851),(#28852,#28853,#28854,#28855,#28856,
#28857,#28858,#28859,#28860,#28861,#28862,#28863,#28864,#28865,#28866,#28867,
#28868,#28869,#28870,#28871,#28872,#28873,#28874,#28875,#28876,#28877,#28878,
#28879,#28880,#28881,#28882,#28883,#28884,#28885,#28886,#28887,#28888,#28889,
#28890,#28891,#28892,#28893,#28894,#28895,#28896,#28897,#28898,#28899,#28900,
#28901,#28902,#28903,#28904,#28905,#28906,#28907,#28908,#28909,#28910,#28911,
#28912,#28913,#28914,#28915,#28916,#28917,#28918,#28919,#28920,#28921,#28922,
#28923,#28924,#28925,#28926,#28927,#28928,#28929,#28930,#28931,#28932,#28933,
#28934,#28935,#28936,#28937,#28938,#28939,#28940,#28941,#28942,#28943,#28944,
#28945,#28946,#28947,#28948,#28949,#28950,#28951,#28952,#28953,#28954,#28955,
#28956,#28957,#28958,#28959,#28960,#28961,#28962,#28963,#28964,#28965,#28966,
#28967,#28968,#28969,#28970,#28971,#28972,#28973,#28974,#28975,#28976,#28977,
#28978,#28979,#28980,#28981,#28982,#28983,#28984,#28985,#28986,#28987,#28988,
#28989,#28990,#28991,#28992,#28993,#28994,#28995,#28996,#28997,#28998,#28999,
#29000,#29001,#29002,#29003,#29004,#29005,#29006,#29007,#29008,#29009,#29010,
#29011,#29012,#29013,#29014,#29015,#29016,#29017,#29018,#29019,#29020,#29021,
#29022,#29023,#29024,#29025,#29026,#29027,#29028,#29029,#29030,#29031,#29032,
#29033,#29034,#29035,#29036,#29037,#29038,#29039,#29040,#29041,#29042,#29043,
#29044,#29045,#29046,#29047,#29048,#29049,#29050,#29051,#29052,#29053,#29054,
#29055,#29056,#29057,#29058,#29059,#29060,#29061,#29062,#29063,#29064,#29065,
#29066,#29067,#29068,#29069,#29070,#29071,#29072,#29073,#29074,#29075,#29076,
#29077,#29078,#29079,#29080,#29081,#29082,#29083,#29084,#29085,#29086,#29087,
#29088,#29089,#29090,#29091,#29092),(#29093,#29094,#29095,#29096,#29097,
#29098,#29099,#29100,#29101,#29102,#29103,#29104,#29105,#29106,#29107,#29108,
#29109,#29110,#29111,#29112,#29113,#29114,#29115,#29116,#29117,#29118,#29119,
#29120,#29121,#29122,#29123,#29124,#29125,#29126,#29127,#29128,#29129,#29130,
#29131,#29132,#29133,#29134,#29135,#29136,#29137,#29138,#29139,#29140,#29141,
#29142,#29143,#29144,#29145,#29146,#29147,#29148,#29149,#29150,#29151,#29152,
#29153,#29154,#29155,#29156,#29157,#29158,#29159,#29160,#29161,#29162,#29163,
#29164,#29165,#29166,#29167,#29168,#29169,#29170,#29171,#29172,#29173,#29174,
#29175,#29176,#29177,#29178,#29179,#29180,#29181,#29182,#29183,#29184,#29185,
#29186,#29187,#29188,#29189,#29190,#29191,#29192,#29193,#29194,#29195,#29196,
#29197,#29198,#29199,#29200,#29201,#29202,#29203,#29204,#29205,#29206,#29207,
#29208,#29209,#29210,#29211,#29212,#29213,#29214,#29215,#29216,#29217,#29218,
#29219,#29220,#29221,#29222,#29223,#29224,#29225,#29226,#29227,#29228,#29229,
#29230,#29231,#29232,#29233,#29234,#29235,#29236,#29237,#29238,#29239,#29240,
#29241,#29242,#29243,#29244,#29245,#29246,#29247,#29248,#29249,#29250,#29251,
#29252,#29253,#29254,#29255,#29256,#29257,#29258,#29259,#29260,#29261,#29262,
#29263,#29264,#29265,#29266,#29267,#29268,#29269,#29270,#29271,#29272,#29273,
#29274,#29275,#29276,#29277,#29278,#29279,#29280,#29281,#29282,#29283,#29284,
#29285,#29286,#29287,#29288,#29289,#29290,#29291,#29292,#29293,#29294,#29295,
#29296,#29297,#29298,#29299,#29300,#29301,#29302,#29303,#29304,#29305,#29306,
#29307,#29308,#29309,#29310,#29311,#29312,#29313,#29314,#29315,#29316,#29317,
#29318,#29319,#29320,#29321,#29322,#29323,#29324,#29325,#29326,#29327,#29328,
#29329,#29330,#29331,#29332,#29333),(#29334,#29335,#29336,#29337,#29338,
#29339,#29340,#29341,#29342,#29343,#29344,#29345,#29346,#29347,#29348,#29349,
#29350,#29351,#29352,#29353,#29354,#29355,#29356,#29357,#29358,#29359,#29360,
#29361,#29362,#29363,#29364,#29365,#29366,#29367,#29368,#29369,#29370,#29371,
#29372,#29373,#29374,#29375,#29376,#29377,#29378,#29379,#29380,#29381,#29382,
#29383,#29384,#29385,#29386,#29387,#29388,#29389,#29390,#29391,#29392,#29393,
#29394,#29395,#29396,#29397,#29398,#29399,#29400,#29401,#29402,#29403,#29404,
#29405,#29406,#29407,#29408,#29409,#29410,#29411,#29412,#29413,#29414,#29415,
#29416,#29417,#29418,#29419,#29420,#29421,#29422,#29423,#29424,#29425,#29426,
#29427,#29428,#29429,#29430,#29431,#29432,#29433,#29434,#29435,#29436,#29437,
#29438,#29439,#29440,#29441,#29442,#29443,#29444,#29445,#29446,#29447,#29448,
#29449,#29450,#29451,#29452,#29453,#29454,#29455,#29456,#29457,#29458,#29459,
#29460,#29461,#29462,#29463,#29464,#29465,#29466,#29467,#29468,#29469,#29470,
#29471,#29472,#29473,#29474,#29475,#29476,#29477,#29478,#29479,#29480,#29481,
#29482,#29483,#29484,#29485,#29486,#29487,#29488,#29489,#29490,#29491,#29492,
#29493,#29494,#29495,#29496,#29497,#29498,#29499,#29500,#29501,#29502,#29503,
#29504,#29505,#29506,#29507,#29508,#29509,#29510,#29511,#29512,#29513,#29514,
#29515,#29516,#29517,#29518,#29519,#29520,#29521,#29522,#29523,#29524,#29525,
#29526,#29527,#29528,#29529,#29530,#29531,#29532,#29533,#29534,#29535,#29536,
#29537,#29538,#29539,#29540,#29541,#29542,#29543,#29544,#29545,#29546,#29547,
#29548,#29549,#29550,#29551,#29552,#29553,#29554,#29555,#29556,#29557,#29558,
#29559,#29560,#29561,#29562,#29563,#29564,#29565,#29566,#29567,#29568,#29569,
#29570,#29571,#29572,#29573,#29574)),.UNSPECIFIED.,.F.,.F.,.F.,(4,4),(4,
1,1,1,1,1,1,1,1,1,1,1,1,1,1,1,1,1,1,1,1,1,1,1,1,1,1,1,1,1,1,1,1,1,1,1,1,
1,1,1,1,1,1,1,1,1,1,1,1,1,1,1,1,1,1,1,1,1,1,1,1,1,1,1,1,1,1,1,1,1,1,1,1,
1,1,1,1,1,1,1,1,1,1,1,1,1,1,1,1,1,1,1,1,1,1,1,1,1,1,1,1,1,1,1,1,1,1,1,1,
1,1,1,1,1,1,1,1,1,1,1,1,1,1,1,1,1,1,1,1,1,1,1,1,1,1,1,1,1,1,1,1,1,1,1,1,
1,1,1,1,1,1,1,1,1,1,1,1,1,1,1,1,1,1,1,1,1,1,1,1,1,1,1,1,1,1,1,1,1,1,1,1,
1,1,1,1,1,1,1,1,1,1,1,1,1,1,1,1,1,1,1,1,1,1,1,1,1,1,1,1,1,1,1,1,1,1,1,1,
1,1,1,1,1,1,1,1,1,1,1,1,1,1,1,1,1,1,1,1,1,4),(-0.000369208222476486,0.0530376906591354),
(11.6159809837193,12.6150740657025,13.6137549340633,14.612435802424,15.6111166707848,
16.6097975391455,17.6084784075063,18.607159275867,19.6058401442278,20.6045210125885,
21.6032018809493,22.60188274931,23.6005636176708,24.5992444860315,25.5979253543923,
26.596606222753,27.5952870911138,28.5939679594746,29.5926488278353,30.5913296961961,
31.5900105645568,32.5886914329176,33.5873723012783,34.5860531696391,35.5847340379998,
36.5834149063606,37.5820957747213,38.5807766430821,39.5794575114428,40.5781383798036,
41.5768192481643,42.5755001165251,43.5741809848858,44.5728618532466,45.5715427216073,
46.5702235899681,47.5689044583288,48.5675853266896,49.5662661950503,50.5649470634111,
51.5636279317718,52.5623088001326,53.5609896684933,54.5596705368541,55.5583514052148,
56.5570322735756,57.5557131419363,58.5543940102971,59.5530748786578,60.5517557470186,
61.5504366153793,62.5491174837401,63.5477983521008,64.5464792204616,65.5451600888223,
66.5438409571831,67.5425218255438,68.5412026939046,69.5398835622653,70.5385644306261,
71.5372452989868,72.5359261673476,73.5346070357083,74.5332879040691,75.5319687724298,
76.5306496407906,77.5293305091514,78.5280113775121,79.5266922458729,80.5253731142336,
81.5240539825944,82.5227348509551,83.5214157193159,84.5200965876766,85.5187774560374,
86.5174583243981,87.5161391927589,88.5148200611196,89.5135009294804,90.5121817978411,
91.5108626662019,92.5095435345626,93.5082244029234,94.5069052712841,95.5055861396449,
96.5042670080056,97.5029478763664,98.5016287447271,99.5003096130879,100.498990481449,
101.497671349809,102.49635221817,103.495033086531,104.493713954892,105.492394823252,
106.491075691613,107.489756559974,108.488437428335,109.487118296695,110.485799165056,
111.484480033417,112.483160901778,113.481841770138,114.480522638499,115.47920350686,
116.477884375221,117.476565243581,118.475246111942,119.473926980303,120.472607848664,
121.471288717024,122.469969585385,123.468650453746,124.467331322107,125.466012190467,
126.464693058828,127.463373927189,128.46205479555,129.46073566391,130.459416532271,
131.458097400632,132.456778268993,133.455459137353,134.454140005714,135.452820874075,
136.451501742436,137.450182610796,138.448863479157,139.447544347518,140.446225215879,
141.444906084239,142.4435869526,143.442267820961,144.440948689322,145.439629557682,
146.438310426043,147.436991294404,148.435672162765,149.434353031125,150.433033899486,
151.431714767847,152.430395636208,153.429076504568,154.427757372929,155.42643824129,
156.425119109651,157.423799978011,158.422480846372,159.421161714733,160.419842583094,
161.418523451454,162.417204319815,163.415885188176,164.414566056537,165.413246924897,
166.411927793258,167.410608661619,168.40928952998,169.40797039834,170.406651266701,
171.405332135062,172.404013003423,173.402693871783,174.401374740144,175.400055608505,
176.398736476866,177.397417345226,178.396098213587,179.394779081948,180.393459950309,
181.392140818669,182.39082168703,183.389502555391,184.388183423752,185.386864292112,
186.385545160473,187.384226028834,188.382906897195,189.381587765555,190.380268633916,
191.378949502277,192.377630370638,193.376311238999,194.374992107359,195.37367297572,
196.372353844081,197.371034712442,198.369715580802,199.368396449163,200.367077317524,
201.365758185885,202.364439054245,203.363119922606,204.361800790967,205.360481659328,
206.359162527688,207.357843396049,208.35652426441,209.355205132771,210.353886001131,
211.352566869492,212.351247737853,213.349928606214,214.348609474574,215.347290342935,
216.345971211296,217.344652079657,218.343332948017,219.342013816378,220.340694684739,
221.3393755531,222.33805642146,223.336737289821,224.335418158182,225.334099026543,
226.332779894903,227.331460763264,228.330141631625,229.328822499986,230.327503368346,
231.326184236707,232.324865105068,233.323545973429,234.322226841789,235.32090771015,
236.319588578511,237.318269446872,238.316950315232,239.315631183593,240.314312051954,
241.312992920315,242.311673788675,243.310354657036,244.309035525397,245.307716393758,
246.306397262118,247.305078130479,248.30375899884,249.302622768849),
 .UNSPECIFIED.);
#87=FACE_BOUND('',#425,.T.);
#88=FACE_BOUND('',#511,.T.);
#91=PLANE('',#2883);
#92=PLANE('',#2962);
#93=PLANE('',#3087);
#94=PLANE('',#3088);
#105=LINE('',#27458,#202);
#106=LINE('',#27464,#203);
#107=LINE('',#29795,#204);
#108=LINE('',#29798,#205);
#109=LINE('',#29837,#206);
#110=LINE('',#29840,#207);
#111=LINE('',#29879,#208);
#112=LINE('',#29882,#209);
#113=LINE('',#29921,#210);
#114=LINE('',#29924,#211);
#115=LINE('',#29963,#212);
#116=LINE('',#29966,#213);
#117=LINE('',#30005,#214);
#118=LINE('',#30008,#215);
#119=LINE('',#30047,#216);
#120=LINE('',#30050,#217);
#121=LINE('',#30089,#218);
#122=LINE('',#30092,#219);
#123=LINE('',#30131,#220);
#124=LINE('',#30134,#221);
#125=LINE('',#30159,#222);
#126=LINE('',#30163,#223);
#127=LINE('',#30220,#224);
#128=LINE('',#30223,#225);
#129=LINE('',#30262,#226);
#130=LINE('',#30265,#227);
#131=LINE('',#30304,#228);
#132=LINE('',#30307,#229);
#133=LINE('',#30346,#230);
#134=LINE('',#30349,#231);
#135=LINE('',#30388,#232);
#136=LINE('',#30391,#233);
#137=LINE('',#30430,#234);
#138=LINE('',#30433,#235);
#139=LINE('',#30472,#236);
#140=LINE('',#30475,#237);
#141=LINE('',#30514,#238);
#142=LINE('',#30517,#239);
#143=LINE('',#30556,#240);
#144=LINE('',#30559,#241);
#145=LINE('',#30598,#242);
#146=LINE('',#30601,#243);
#147=LINE('',#30640,#244);
#148=LINE('',#30643,#245);
#149=LINE('',#30682,#246);
#150=LINE('',#30685,#247);
#151=LINE('',#30724,#248);
#152=LINE('',#30727,#249);
#153=LINE('',#30766,#250);
#154=LINE('',#30769,#251);
#155=LINE('',#30808,#252);
#156=LINE('',#30811,#253);
#157=LINE('',#30850,#254);
#158=LINE('',#30853,#255);
#159=LINE('',#30892,#256);
#160=LINE('',#30895,#257);
#161=LINE('',#30934,#258);
#162=LINE('',#30937,#259);
#163=LINE('',#30976,#260);
#164=LINE('',#30979,#261);
#165=LINE('',#31018,#262);
#166=LINE('',#31021,#263);
#167=LINE('',#31060,#264);
#168=LINE('',#31063,#265);
#169=LINE('',#31102,#266);
#170=LINE('',#31105,#267);
#171=LINE('',#31144,#268);
#172=LINE('',#31147,#269);
#173=LINE('',#31186,#270);
#174=LINE('',#31189,#271);
#175=LINE('',#31228,#272);
#176=LINE('',#31231,#273);
#177=LINE('',#31270,#274);
#178=LINE('',#31273,#275);
#179=LINE('',#31312,#276);
#180=LINE('',#31315,#277);
#181=LINE('',#31354,#278);
#182=LINE('',#31357,#279);
#183=LINE('',#31396,#280);
#184=LINE('',#31399,#281);
#185=LINE('',#31447,#282);
#186=LINE('',#31563,#283);
#202=VECTOR('',#3169,4.);
#203=VECTOR('',#3176,4.5);
#204=VECTOR('',#3185,10.);
#205=VECTOR('',#3188,10.);
#206=VECTOR('',#3191,10.);
#207=VECTOR('',#3194,10.);
#208=VECTOR('',#3197,10.);
#209=VECTOR('',#3200,10.);
#210=VECTOR('',#3203,10.);
#211=VECTOR('',#3206,10.);
#212=VECTOR('',#3209,10.);
#213=VECTOR('',#3212,10.);
#214=VECTOR('',#3215,10.);
#215=VECTOR('',#3218,10.);
#216=VECTOR('',#3221,10.);
#217=VECTOR('',#3224,10.);
#218=VECTOR('',#3227,10.);
#219=VECTOR('',#3230,10.);
#220=VECTOR('',#3233,10.);
#221=VECTOR('',#3236,10.);
#222=VECTOR('',#3239,10.);
#223=VECTOR('',#3242,10.);
#224=VECTOR('',#3245,10.);
#225=VECTOR('',#3248,10.);
#226=VECTOR('',#3251,10.);
#227=VECTOR('',#3254,10.);
#228=VECTOR('',#3257,10.);
#229=VECTOR('',#3260,10.);
#230=VECTOR('',#3263,10.);
#231=VECTOR('',#3266,10.);
#232=VECTOR('',#3269,10.);
#233=VECTOR('',#3272,10.);
#234=VECTOR('',#3275,10.);
#235=VECTOR('',#3278,10.);
#236=VECTOR('',#3281,10.);
#237=VECTOR('',#3284,10.);
#238=VECTOR('',#3287,10.);
#239=VECTOR('',#3290,10.);
#240=VECTOR('',#3293,10.);
#241=VECTOR('',#3296,10.);
#242=VECTOR('',#3299,10.);
#243=VECTOR('',#3302,10.);
#244=VECTOR('',#3305,10.);
#245=VECTOR('',#3308,10.);
#246=VECTOR('',#3311,10.);
#247=VECTOR('',#3314,10.);
#248=VECTOR('',#3317,10.);
#249=VECTOR('',#3320,10.);
#250=VECTOR('',#3323,10.);
#251=VECTOR('',#3326,10.);
#252=VECTOR('',#3329,10.);
#253=VECTOR('',#3332,10.);
#254=VECTOR('',#3335,10.);
#255=VECTOR('',#3338,10.);
#256=VECTOR('',#3341,10.);
#257=VECTOR('',#3344,10.);
#258=VECTOR('',#3347,10.);
#259=VECTOR('',#3350,10.);
#260=VECTOR('',#3353,10.);
#261=VECTOR('',#3356,10.);
#262=VECTOR('',#3359,10.);
#263=VECTOR('',#3362,10.);
#264=VECTOR('',#3365,10.);
#265=VECTOR('',#3368,10.);
#266=VECTOR('',#3371,10.);
#267=VECTOR('',#3374,10.);
#268=VECTOR('',#3377,10.);
#269=VECTOR('',#3380,10.);
#270=VECTOR('',#3383,10.);
#271=VECTOR('',#3386,10.);
#272=VECTOR('',#3389,10.);
#273=VECTOR('',#3392,10.);
#274=VECTOR('',#3395,10.);
#275=VECTOR('',#3398,10.);
#276=VECTOR('',#3401,10.);
#277=VECTOR('',#3404,10.);
#278=VECTOR('',#3407,10.);
#279=VECTOR('',#3410,10.);
#280=VECTOR('',#3413,10.);
#281=VECTOR('',#3416,10.);
#282=VECTOR('',#3505,10.);
#283=VECTOR('',#3666,10.);
#299=FACE_OUTER_BOUND('',#420,.T.);
#300=FACE_OUTER_BOUND('',#421,.T.);
#301=FACE_OUTER_BOUND('',#422,.T.);
#302=FACE_OUTER_BOUND('',#423,.T.);
#303=FACE_OUTER_BOUND('',#424,.T.);
#304=FACE_OUTER_BOUND('',#426,.T.);
#305=FACE_OUTER_BOUND('',#427,.T.);
#306=FACE_OUTER_BOUND('',#428,.T.);
#307=FACE_OUTER_BOUND('',#429,.T.);
#308=FACE_OUTER_BOUND('',#430,.T.);
#309=FACE_OUTER_BOUND('',#431,.T.);
#310=FACE_OUTER_BOUND('',#432,.T.);
#311=FACE_OUTER_BOUND('',#433,.T.);
#312=FACE_OUTER_BOUND('',#434,.T.);
#313=FACE_OUTER_BOUND('',#435,.T.);
#314=FACE_OUTER_BOUND('',#436,.T.);
#315=FACE_OUTER_BOUND('',#437,.T.);
#316=FACE_OUTER_BOUND('',#438,.T.);
#317=FACE_OUTER_BOUND('',#439,.T.);
#318=FACE_OUTER_BOUND('',#440,.T.);
#319=FACE_OUTER_BOUND('',#441,.T.);
#320=FACE_OUTER_BOUND('',#442,.T.);
#321=FACE_OUTER_BOUND('',#443,.T.);
#322=FACE_OUTER_BOUND('',#444,.T.);
#323=FACE_OUTER_BOUND('',#445,.T.);
#324=FACE_OUTER_BOUND('',#446,.T.);
#325=FACE_OUTER_BOUND('',#447,.T.);
#326=FACE_OUTER_BOUND('',#448,.T.);
#327=FACE_OUTER_BOUND('',#449,.T.);
#328=FACE_OUTER_BOUND('',#450,.T.);
#329=FACE_OUTER_BOUND('',#451,.T.);
#330=FACE_OUTER_BOUND('',#452,.T.);
#331=FACE_OUTER_BOUND('',#453,.T.);
#332=FACE_OUTER_BOUND('',#454,.T.);
#333=FACE_OUTER_BOUND('',#455,.T.);
#334=FACE_OUTER_BOUND('',#456,.T.);
#335=FACE_OUTER_BOUND('',#457,.T.);
#336=FACE_OUTER_BOUND('',#458,.T.);
#337=FACE_OUTER_BOUND('',#459,.T.);
#338=FACE_OUTER_BOUND('',#460,.T.);
#339=FACE_OUTER_BOUND('',#461,.T.);
#340=FACE_OUTER_BOUND('',#462,.T.);
#341=FACE_OUTER_BOUND('',#463,.T.);
#342=FACE_OUTER_BOUND('',#464,.T.);
#343=FACE_OUTER_BOUND('',#465,.T.);
#344=FACE_OUTER_BOUND('',#466,.T.);
#345=FACE_OUTER_BOUND('',#467,.T.);
#346=FACE_OUTER_BOUND('',#468,.T.);
#347=FACE_OUTER_BOUND('',#469,.T.);
#348=FACE_OUTER_BOUND('',#470,.T.);
#349=FACE_OUTER_BOUND('',#471,.T.);
#350=FACE_OUTER_BOUND('',#472,.T.);
#351=FACE_OUTER_BOUND('',#473,.T.);
#352=FACE_OUTER_BOUND('',#474,.T.);
#353=FACE_OUTER_BOUND('',#475,.T.);
#354=FACE_OUTER_BOUND('',#476,.T.);
#355=FACE_OUTER_BOUND('',#477,.T.);
#356=FACE_OUTER_BOUND('',#478,.T.);
#357=FACE_OUTER_BOUND('',#479,.T.);
#358=FACE_OUTER_BOUND('',#480,.T.);
#359=FACE_OUTER_BOUND('',#481,.T.);
#360=FACE_OUTER_BOUND('',#482,.T.);
#361=FACE_OUTER_BOUND('',#483,.T.);
#362=FACE_OUTER_BOUND('',#484,.T.);
#363=FACE_OUTER_BOUND('',#485,.T.);
#364=FACE_OUTER_BOUND('',#486,.T.);
#365=FACE_OUTER_BOUND('',#487,.T.);
#366=FACE_OUTER_BOUND('',#488,.T.);
#367=FACE_OUTER_BOUND('',#489,.T.);
#368=FACE_OUTER_BOUND('',#490,.T.);
#369=FACE_OUTER_BOUND('',#491,.T.);
#370=FACE_OUTER_BOUND('',#492,.T.);
#371=FACE_OUTER_BOUND('',#493,.T.);
#372=FACE_OUTER_BOUND('',#494,.T.);
#373=FACE_OUTER_BOUND('',#495,.T.);
#374=FACE_OUTER_BOUND('',#496,.T.);
#375=FACE_OUTER_BOUND('',#497,.T.);
#376=FACE_OUTER_BOUND('',#498,.T.);
#377=FACE_OUTER_BOUND('',#499,.T.);
#378=FACE_OUTER_BOUND('',#500,.T.);
#379=FACE_OUTER_BOUND('',#501,.T.);
#380=FACE_OUTER_BOUND('',#502,.T.);
#381=FACE_OUTER_BOUND('',#503,.T.);
#382=FACE_OUTER_BOUND('',#504,.T.);
#383=FACE_OUTER_BOUND('',#505,.T.);
#384=FACE_OUTER_BOUND('',#506,.T.);
#385=FACE_OUTER_BOUND('',#507,.T.);
#386=FACE_OUTER_BOUND('',#508,.T.);
#387=FACE_OUTER_BOUND('',#509,.T.);
#388=FACE_OUTER_BOUND('',#510,.T.);
#389=FACE_OUTER_BOUND('',#512,.T.);
#420=EDGE_LOOP('',(#1687,#1688,#1689,#1690,#1691,#1692,#1693,#1694,#1695,
#1696,#1697,#1698,#1699,#1700,#1701,#1702,#1703,#1704,#1705,#1706,#1707,
#1708,#1709,#1710,#1711,#1712,#1713,#1714,#1715,#1716,#1717,#1718,#1719,
#1720,#1721,#1722,#1723,#1724,#1725,#1726,#1727,#1728,#1729,#1730,#1731,
#1732,#1733,#1734,#1735,#1736,#1737,#1738,#1739,#1740,#1741,#1742,#1743,
#1744,#1745,#1746,#1747,#1748,#1749,#1750,#1751,#1752,#1753,#1754,#1755,
#1756,#1757,#1758,#1759,#1760,#1761,#1762,#1763,#1764,#1765,#1766));
#421=EDGE_LOOP('',(#1767,#1768,#1769,#1770,#1771,#1772,#1773,#1774,#1775,
#1776,#1777,#1778,#1779,#1780,#1781,#1782,#1783,#1784,#1785,#1786,#1787,
#1788,#1789,#1790,#1791,#1792,#1793,#1794,#1795,#1796,#1797,#1798,#1799,
#1800,#1801,#1802,#1803,#1804,#1805,#1806,#1807,#1808,#1809,#1810,#1811,
#1812,#1813,#1814,#1815,#1816,#1817,#1818));
#422=EDGE_LOOP('',(#1819,#1820,#1821,#1822));
#423=EDGE_LOOP('',(#1823,#1824,#1825,#1826,#1827));
#424=EDGE_LOOP('',(#1828));
#425=EDGE_LOOP('',(#1829));
#426=EDGE_LOOP('',(#1830,#1831,#1832,#1833,#1834,#1835,#1836,#1837,#1838,
#1839,#1840,#1841,#1842,#1843,#1844,#1845,#1846,#1847,#1848,#1849,#1850,
#1851,#1852,#1853,#1854,#1855,#1856,#1857,#1858,#1859,#1860,#1861,#1862,
#1863,#1864,#1865,#1866,#1867,#1868,#1869,#1870,#1871,#1872,#1873,#1874,
#1875,#1876,#1877,#1878,#1879,#1880,#1881,#1882,#1883,#1884,#1885,#1886,
#1887,#1888,#1889,#1890,#1891,#1892,#1893,#1894,#1895,#1896));
#427=EDGE_LOOP('',(#1897,#1898,#1899,#1900,#1901,#1902,#1903,#1904,#1905,
#1906,#1907,#1908,#1909,#1910,#1911,#1912,#1913,#1914,#1915,#1916,#1917,
#1918,#1919,#1920,#1921,#1922,#1923,#1924,#1925,#1926,#1927,#1928,#1929,
#1930,#1931,#1932,#1933,#1934,#1935,#1936,#1937,#1938,#1939,#1940,#1941,
#1942,#1943,#1944,#1945,#1946,#1947,#1948,#1949,#1950,#1951,#1952,#1953,
#1954,#1955,#1956,#1957,#1958,#1959,#1960,#1961,#1962));
#428=EDGE_LOOP('',(#1963,#1964,#1965,#1966));
#429=EDGE_LOOP('',(#1967,#1968,#1969,#1970));
#430=EDGE_LOOP('',(#1971,#1972,#1973,#1974));
#431=EDGE_LOOP('',(#1975,#1976,#1977,#1978));
#432=EDGE_LOOP('',(#1979,#1980,#1981,#1982));
#433=EDGE_LOOP('',(#1983,#1984,#1985,#1986));
#434=EDGE_LOOP('',(#1987,#1988,#1989,#1990));
#435=EDGE_LOOP('',(#1991,#1992,#1993,#1994));
#436=EDGE_LOOP('',(#1995,#1996,#1997,#1998));
#437=EDGE_LOOP('',(#1999,#2000,#2001,#2002,#2003));
#438=EDGE_LOOP('',(#2004,#2005,#2006,#2007));
#439=EDGE_LOOP('',(#2008,#2009,#2010,#2011));
#440=EDGE_LOOP('',(#2012,#2013,#2014,#2015));
#441=EDGE_LOOP('',(#2016,#2017,#2018,#2019));
#442=EDGE_LOOP('',(#2020,#2021,#2022,#2023));
#443=EDGE_LOOP('',(#2024,#2025,#2026,#2027));
#444=EDGE_LOOP('',(#2028,#2029,#2030,#2031));
#445=EDGE_LOOP('',(#2032,#2033,#2034,#2035));
#446=EDGE_LOOP('',(#2036,#2037,#2038,#2039));
#447=EDGE_LOOP('',(#2040,#2041,#2042,#2043));
#448=EDGE_LOOP('',(#2044,#2045,#2046,#2047));
#449=EDGE_LOOP('',(#2048,#2049,#2050,#2051));
#450=EDGE_LOOP('',(#2052,#2053,#2054,#2055));
#451=EDGE_LOOP('',(#2056,#2057,#2058,#2059));
#452=EDGE_LOOP('',(#2060,#2061,#2062,#2063));
#453=EDGE_LOOP('',(#2064,#2065,#2066,#2067));
#454=EDGE_LOOP('',(#2068,#2069,#2070,#2071));
#455=EDGE_LOOP('',(#2072,#2073,#2074,#2075));
#456=EDGE_LOOP('',(#2076,#2077,#2078,#2079));
#457=EDGE_LOOP('',(#2080,#2081,#2082,#2083));
#458=EDGE_LOOP('',(#2084,#2085,#2086,#2087));
#459=EDGE_LOOP('',(#2088,#2089,#2090,#2091));
#460=EDGE_LOOP('',(#2092,#2093,#2094,#2095));
#461=EDGE_LOOP('',(#2096,#2097,#2098,#2099));
#462=EDGE_LOOP('',(#2100,#2101,#2102,#2103));
#463=EDGE_LOOP('',(#2104,#2105,#2106,#2107));
#464=EDGE_LOOP('',(#2108,#2109,#2110,#2111));
#465=EDGE_LOOP('',(#2112,#2113,#2114,#2115));
#466=EDGE_LOOP('',(#2116,#2117,#2118,#2119));
#467=EDGE_LOOP('',(#2120,#2121,#2122,#2123,#2124,#2125,#2126,#2127,#2128,
#2129,#2130,#2131,#2132,#2133,#2134,#2135,#2136,#2137,#2138,#2139,#2140,
#2141,#2142,#2143,#2144,#2145,#2146,#2147,#2148,#2149,#2150,#2151,#2152,
#2153,#2154,#2155,#2156,#2157,#2158,#2159,#2160,#2161,#2162,#2163,#2164,
#2165,#2166,#2167,#2168,#2169,#2170,#2171,#2172,#2173,#2174,#2175,#2176,
#2177,#2178,#2179,#2180,#2181,#2182,#2183,#2184,#2185,#2186,#2187,#2188,
#2189,#2190,#2191,#2192,#2193,#2194,#2195,#2196,#2197,#2198,#2199));
#468=EDGE_LOOP('',(#2200,#2201,#2202,#2203));
#469=EDGE_LOOP('',(#2204,#2205,#2206,#2207));
#470=EDGE_LOOP('',(#2208,#2209,#2210,#2211));
#471=EDGE_LOOP('',(#2212,#2213,#2214,#2215));
#472=EDGE_LOOP('',(#2216,#2217,#2218,#2219));
#473=EDGE_LOOP('',(#2220,#2221,#2222,#2223));
#474=EDGE_LOOP('',(#2224,#2225,#2226,#2227));
#475=EDGE_LOOP('',(#2228,#2229,#2230,#2231));
#476=EDGE_LOOP('',(#2232,#2233,#2234,#2235));
#477=EDGE_LOOP('',(#2236,#2237,#2238,#2239));
#478=EDGE_LOOP('',(#2240,#2241,#2242,#2243));
#479=EDGE_LOOP('',(#2244,#2245,#2246,#2247));
#480=EDGE_LOOP('',(#2248,#2249,#2250,#2251));
#481=EDGE_LOOP('',(#2252,#2253,#2254,#2255));
#482=EDGE_LOOP('',(#2256,#2257,#2258,#2259));
#483=EDGE_LOOP('',(#2260,#2261,#2262,#2263));
#484=EDGE_LOOP('',(#2264,#2265,#2266,#2267));
#485=EDGE_LOOP('',(#2268,#2269,#2270,#2271));
#486=EDGE_LOOP('',(#2272,#2273,#2274,#2275));
#487=EDGE_LOOP('',(#2276,#2277,#2278,#2279));
#488=EDGE_LOOP('',(#2280,#2281,#2282,#2283));
#489=EDGE_LOOP('',(#2284,#2285,#2286,#2287));
#490=EDGE_LOOP('',(#2288,#2289,#2290,#2291));
#491=EDGE_LOOP('',(#2292,#2293,#2294,#2295));
#492=EDGE_LOOP('',(#2296,#2297,#2298,#2299));
#493=EDGE_LOOP('',(#2300,#2301,#2302,#2303));
#494=EDGE_LOOP('',(#2304,#2305,#2306,#2307));
#495=EDGE_LOOP('',(#2308,#2309,#2310,#2311));
#496=EDGE_LOOP('',(#2312,#2313,#2314,#2315));
#497=EDGE_LOOP('',(#2316,#2317,#2318,#2319));
#498=EDGE_LOOP('',(#2320,#2321,#2322,#2323));
#499=EDGE_LOOP('',(#2324,#2325,#2326,#2327));
#500=EDGE_LOOP('',(#2328,#2329,#2330,#2331));
#501=EDGE_LOOP('',(#2332,#2333,#2334,#2335));
#502=EDGE_LOOP('',(#2336,#2337,#2338,#2339));
#503=EDGE_LOOP('',(#2340,#2341,#2342,#2343));
#504=EDGE_LOOP('',(#2344,#2345,#2346,#2347));
#505=EDGE_LOOP('',(#2348,#2349,#2350,#2351));
#506=EDGE_LOOP('',(#2352,#2353,#2354,#2355));
#507=EDGE_LOOP('',(#2356,#2357,#2358,#2359,#2360,#2361,#2362,#2363,#2364,
#2365,#2366,#2367,#2368,#2369,#2370,#2371,#2372,#2373,#2374,#2375,#2376,
#2377,#2378,#2379,#2380,#2381,#2382,#2383,#2384,#2385,#2386,#2387,#2388,
#2389,#2390,#2391,#2392,#2393,#2394,#2395,#2396,#2397,#2398,#2399,#2400,
#2401,#2402,#2403,#2404,#2405,#2406,#2407,#2408,#2409,#2410,#2411,#2412,
#2413,#2414,#2415,#2416,#2417,#2418,#2419,#2420,#2421,#2422,#2423,#2424,
#2425,#2426,#2427,#2428,#2429,#2430,#2431,#2432,#2433,#2434,#2435,#2436,
#2437,#2438,#2439,#2440));
#508=EDGE_LOOP('',(#2441,#2442,#2443,#2444));
#509=EDGE_LOOP('',(#2445,#2446,#2447,#2448));
#510=EDGE_LOOP('',(#2449));
#511=EDGE_LOOP('',(#2450,#2451,#2452,#2453,#2454));
#512=EDGE_LOOP('',(#2455,#2456,#2457,#2458));
#545=CIRCLE('',#2871,2.4505);
#546=CIRCLE('',#2872,2.4505);
#547=CIRCLE('',#2874,1.99475);
#548=CIRCLE('',#2875,1.99475);
#549=CIRCLE('',#2877,4.);
#550=CIRCLE('',#2878,4.);
#551=CIRCLE('',#2880,4.5);
#552=CIRCLE('',#2881,4.5);
#553=CIRCLE('',#2882,4.5);
#554=CIRCLE('',#2885,0.25);
#555=CIRCLE('',#2887,0.25);
#556=CIRCLE('',#2889,0.25);
#557=CIRCLE('',#2891,0.25);
#558=CIRCLE('',#2893,0.25);
#559=CIRCLE('',#2895,0.25);
#560=CIRCLE('',#2897,0.25);
#561=CIRCLE('',#2899,0.25);
#562=CIRCLE('',#2901,0.25);
#563=CIRCLE('',#2903,0.25);
#564=CIRCLE('',#2905,0.25);
#565=CIRCLE('',#2907,0.25);
#566=CIRCLE('',#2909,0.25);
#567=CIRCLE('',#2911,0.25);
#568=CIRCLE('',#2913,0.25);
#569=CIRCLE('',#2915,0.25);
#570=CIRCLE('',#2917,0.25);
#571=CIRCLE('',#2919,0.25);
#572=CIRCLE('',#2921,0.25);
#573=CIRCLE('',#2923,0.25);
#574=CIRCLE('',#2925,0.25);
#575=CIRCLE('',#2927,0.25);
#576=CIRCLE('',#2929,0.25);
#577=CIRCLE('',#2931,0.25);
#578=CIRCLE('',#2933,0.25);
#579=CIRCLE('',#2935,0.25);
#580=CIRCLE('',#2937,0.25);
#581=CIRCLE('',#2939,0.25);
#582=CIRCLE('',#2941,0.25);
#583=CIRCLE('',#2943,0.25);
#584=CIRCLE('',#2945,0.25);
#585=CIRCLE('',#2947,0.25);
#586=CIRCLE('',#2949,0.25);
#587=CIRCLE('',#2951,0.25);
#588=CIRCLE('',#2953,0.25);
#589=CIRCLE('',#2955,0.25);
#590=CIRCLE('',#2957,0.25);
#591=CIRCLE('',#2959,0.25);
#592=CIRCLE('',#2961,0.25);
#593=CIRCLE('',#2963,5.5);
#594=CIRCLE('',#2964,5.5);
#595=CIRCLE('',#2965,5.5);
#596=CIRCLE('',#2966,5.5);
#597=CIRCLE('',#2967,5.5);
#598=CIRCLE('',#2968,5.5);
#599=CIRCLE('',#2969,5.5);
#600=CIRCLE('',#2970,5.5);
#601=CIRCLE('',#2971,5.5);
#602=CIRCLE('',#2972,5.5);
#603=CIRCLE('',#2973,5.5);
#604=CIRCLE('',#2974,5.5);
#605=CIRCLE('',#2975,5.5);
#606=CIRCLE('',#2976,5.5);
#607=CIRCLE('',#2977,5.5);
#608=CIRCLE('',#2978,5.5);
#609=CIRCLE('',#2979,5.5);
#610=CIRCLE('',#2980,5.5);
#611=CIRCLE('',#2981,5.5);
#612=CIRCLE('',#2982,5.5);
#613=CIRCLE('',#2983,5.5);
#614=CIRCLE('',#2984,5.5);
#615=CIRCLE('',#2985,5.5);
#616=CIRCLE('',#2986,5.5);
#617=CIRCLE('',#2987,5.5);
#618=CIRCLE('',#2988,5.5);
#619=CIRCLE('',#2989,5.5);
#620=CIRCLE('',#2990,5.5);
#621=CIRCLE('',#2991,5.5);
#622=CIRCLE('',#2992,5.5);
#623=CIRCLE('',#2993,5.5);
#624=CIRCLE('',#2994,5.5);
#625=CIRCLE('',#2995,5.5);
#626=CIRCLE('',#2996,5.5);
#627=CIRCLE('',#2997,5.5);
#628=CIRCLE('',#2998,5.5);
#629=CIRCLE('',#2999,5.5);
#630=CIRCLE('',#3000,5.5);
#631=CIRCLE('',#3001,5.5);
#632=CIRCLE('',#3002,0.25);
#633=CIRCLE('',#3003,5.5);
#634=CIRCLE('',#3005,5.5);
#635=CIRCLE('',#3007,5.5);
#636=CIRCLE('',#3009,5.5);
#637=CIRCLE('',#3011,5.5);
#638=CIRCLE('',#3013,5.5);
#639=CIRCLE('',#3015,5.5);
#640=CIRCLE('',#3017,5.5);
#641=CIRCLE('',#3019,5.5);
#642=CIRCLE('',#3021,5.5);
#643=CIRCLE('',#3023,5.5);
#644=CIRCLE('',#3025,5.5);
#645=CIRCLE('',#3027,5.5);
#646=CIRCLE('',#3029,5.5);
#647=CIRCLE('',#3031,5.5);
#648=CIRCLE('',#3033,5.5);
#649=CIRCLE('',#3035,5.5);
#650=CIRCLE('',#3037,5.5);
#651=CIRCLE('',#3039,5.5);
#652=CIRCLE('',#3041,5.5);
#653=CIRCLE('',#3043,5.5);
#654=CIRCLE('',#3045,5.5);
#655=CIRCLE('',#3047,5.5);
#656=CIRCLE('',#3049,5.5);
#657=CIRCLE('',#3051,5.5);
#658=CIRCLE('',#3053,5.5);
#659=CIRCLE('',#3055,5.5);
#660=CIRCLE('',#3057,5.5);
#661=CIRCLE('',#3059,5.5);
#662=CIRCLE('',#3061,5.5);
#663=CIRCLE('',#3063,5.5);
#664=CIRCLE('',#3065,5.5);
#665=CIRCLE('',#3067,5.5);
#666=CIRCLE('',#3069,5.5);
#667=CIRCLE('',#3071,5.5);
#668=CIRCLE('',#3073,5.5);
#669=CIRCLE('',#3075,5.5);
#670=CIRCLE('',#3077,5.5);
#671=CIRCLE('',#3079,5.5);
#672=CIRCLE('',#3081,5.5);
#673=CIRCLE('',#3083,1.);
#674=CIRCLE('',#3084,5.5);
#701=B_SPLINE_CURVE_WITH_KNOTS('',3,(#3813,#3814,#3815,#3816,#3817,#3818),
 .UNSPECIFIED.,.F.,.F.,(4,1,1,4),(-4.09157007060746,-3.994723473443,-2.99604260508226,
-2.0669567652117),.UNSPECIFIED.);
#702=B_SPLINE_CURVE_WITH_KNOTS('',3,(#3822,#3823,#3824,#3825,#3826,#3827,
#3828,#3829,#3830,#3831,#3832,#3833,#3834,#3835,#3836,#3837,#3838,#3839,
#3840,#3841,#3842,#3843,#3844,#3845,#3846,#3847,#3848,#3849,#3850,#3851,
#3852,#3853,#3854,#3855),.UNSPECIFIED.,.F.,.F.,(4,3,3,3,3,3,3,3,3,3,3,4),
(0.,0.102023156236483,0.203984576046395,0.30593583891409,0.407884768424913,
0.50985600275984,0.611874198231225,0.714044517939152,0.816293156139123,
0.918743873970227,0.998680868360744,1.11662023360707),.UNSPECIFIED.);
#703=B_SPLINE_CURVE_WITH_KNOTS('',3,(#3857,#3858,#3859,#3860,#3861,#3862,
#3863,#3864,#3865,#3866,#3867,#3868,#3869,#3870,#3871,#3872,#3873,#3874,
#3875,#3876,#3877,#3878,#3879,#3880,#3881,#3882,#3883,#3884,#3885,#3886,
#3887,#3888,#3889,#3890,#3891,#3892,#3893,#3894,#3895,#3896,#3897,#3898,
#3899,#3900,#3901,#3902,#3903,#3904,#3905,#3906,#3907,#3908,#3909,#3910,
#3911,#3912,#3913,#3914,#3915,#3916,#3917,#3918,#3919,#3920,#3921,#3922,
#3923,#3924,#3925,#3926,#3927,#3928,#3929,#3930,#3931,#3932,#3933,#3934,
#3935,#3936,#3937,#3938,#3939,#3940,#3941,#3942,#3943,#3944,#3945,#3946,
#3947,#3948,#3949,#3950,#3951,#3952,#3953,#3954,#3955,#3956,#3957,#3958,
#3959,#3960,#3961,#3962,#3963,#3964,#3965,#3966,#3967,#3968,#3969,#3970,
#3971,#3972,#3973,#3974,#3975,#3976,#3977,#3978,#3979,#3980,#3981,#3982,
#3983,#3984,#3985,#3986,#3987,#3988,#3989,#3990,#3991,#3992,#3993,#3994,
#3995,#3996,#3997,#3998,#3999,#4000,#4001,#4002,#4003,#4004,#4005,#4006,
#4007,#4008,#4009,#4010,#4011,#4012,#4013,#4014,#4015,#4016,#4017,#4018,
#4019,#4020,#4021,#4022,#4023,#4024,#4025,#4026,#4027,#4028,#4029,#4030,
#4031,#4032,#4033,#4034,#4035,#4036,#4037,#4038,#4039,#4040,#4041,#4042,
#4043,#4044,#4045,#4046),.UNSPECIFIED.,.F.,.F.,(4,3,3,3,3,3,3,3,3,3,3,3,
3,3,3,3,3,3,3,3,3,3,3,3,3,3,3,3,3,3,3,3,3,3,3,3,3,3,3,3,3,3,3,3,3,3,3,3,
3,3,3,3,3,3,3,3,3,3,3,3,3,3,3,4),(1.11662023381331,1.21393749512102,1.31186552532108,
1.40895568848407,1.50599774867716,1.60302436386015,1.70160870707549,1.79876006485995,
1.89806090079072,1.9973617367215,2.0971951147542,2.19688541258594,2.29678006164798,
2.39628986921115,2.49576606614439,2.59523889921085,2.6954398256787,2.79505356449904,
2.89554808479064,2.99604260508225,3.09590085771483,3.19561947633777,3.29550747597593,
3.39505385307093,3.4945696602538,3.59408510451255,3.69424469674516,3.79390804450808,
3.89431575897554,3.994723473443,4.09427171410558,4.19367485294064,4.29364103904853,
4.39286092752618,4.49204682472469,4.59122937758233,4.69177311863769,4.79109962130981,
4.89225198155678,4.99340434180375,5.09311693288323,5.19268643289398,5.29261128005279,
5.39200122521914,5.49135819719149,5.59071261738691,5.6910557655813,5.7905543529646,
5.89131978156455,5.9920852101645,6.0917896034481,6.19135123448222,6.2912780899876,
6.39066103446566,6.49001135007882,6.58935946901391,6.68971112139174,6.78920435337002,
6.88998521594764,6.99076607852525,7.10075815164408,7.21042743348155,7.31954741556262,
7.3998051206394),.UNSPECIFIED.);
#704=B_SPLINE_CURVE_WITH_KNOTS('',3,(#4048,#4049,#4050,#4051,#4052,#4053,
#4054,#4055,#4056,#4057),.UNSPECIFIED.,.F.,.F.,(4,1,1,1,1,1,1,4),(7.39980554078666,
7.98944694688601,8.98812781524676,9.98680868360752,10.9854895519683,11.984170420329,
12.9828512886898,13.6829908479662),.UNSPECIFIED.);
#705=B_SPLINE_CURVE_WITH_KNOTS('',3,(#4059,#4060,#4061,#4062,#4063,#4064,
#4065,#4066,#4067,#4068,#4069,#4070,#4071,#4072,#4073,#4074,#4075,#4076,
#4077,#4078,#4079,#4080,#4081,#4082,#4083,#4084,#4085,#4086,#4087,#4088,
#4089,#4090,#4091,#4092,#4093,#4094,#4095,#4096,#4097,#4098,#4099,#4100,
#4101,#4102,#4103,#4104,#4105,#4106,#4107,#4108,#4109,#4110,#4111,#4112,
#4113,#4114,#4115,#4116,#4117,#4118,#4119,#4120,#4121,#4122,#4123,#4124,
#4125,#4126,#4127,#4128,#4129,#4130,#4131,#4132,#4133,#4134,#4135,#4136,
#4137,#4138,#4139,#4140,#4141,#4142,#4143,#4144,#4145,#4146,#4147,#4148,
#4149,#4150,#4151,#4152,#4153,#4154,#4155,#4156,#4157,#4158,#4159,#4160,
#4161,#4162,#4163,#4164,#4165,#4166,#4167,#4168,#4169,#4170,#4171,#4172,
#4173,#4174,#4175,#4176,#4177,#4178,#4179,#4180,#4181,#4182,#4183,#4184,
#4185,#4186,#4187,#4188,#4189,#4190,#4191,#4192,#4193,#4194,#4195,#4196,
#4197,#4198,#4199,#4200,#4201,#4202,#4203,#4204,#4205,#4206,#4207,#4208,
#4209,#4210,#4211,#4212,#4213,#4214,#4215,#4216,#4217,#4218,#4219,#4220,
#4221,#4222,#4223,#4224,#4225,#4226,#4227,#4228,#4229,#4230,#4231,#4232,
#4233,#4234,#4235,#4236,#4237,#4238,#4239,#4240,#4241,#4242,#4243,#4244,
#4245,#4246,#4247,#4248),.UNSPECIFIED.,.F.,.F.,(4,3,3,3,3,3,3,3,3,3,3,3,
3,3,3,3,3,3,3,3,3,3,3,3,3,3,3,3,3,3,3,3,3,3,3,3,3,3,3,3,3,3,3,3,3,3,3,3,
3,3,3,3,3,3,3,3,3,3,3,3,3,3,3,4),(13.6829910273321,13.8027886851572,13.9242775395078,
13.9815321570505,14.0812158855861,14.1807563980189,14.2806884764429,14.3800493486247,
14.4793772813362,14.5787027361138,14.6790803084382,14.7785504119759,14.8793817186936,
14.9802130254113,15.0798966080951,15.1794369736886,15.279369088699,15.3787298127342,
15.4780575971396,15.5773829036542,15.6777606511837,15.7772306080887,15.8780622509303,
15.978893893772,16.0785774056108,16.1781176986771,16.2780498316091,16.3774104795357,
16.4767381866505,16.5760634147927,16.6764412516277,16.7759111282822,16.8767429452075,
16.9775747621328,17.0772583543262,17.176798728974,17.2767308416639,17.3760915735656,
17.4754193653706,17.5747446788055,17.6751224167275,17.7745923792929,17.8754240048932,
17.9762556304935,18.07593919654,18.1754795448068,18.2754116640627,18.3747723692092,
18.4741001341781,18.5734254207322,18.6738031902627,18.7732731261129,18.8741048124836,
18.9749364988543,19.0744883959638,19.1738971727394,19.2731905896819,19.3724208663801,
19.471618683102,19.570814680118,19.6701088383941,19.7694498169088,19.8689715645658,
19.9661761551458),.UNSPECIFIED.);
#706=B_SPLINE_CURVE_WITH_KNOTS('',3,(#4250,#4251,#4252,#4253,#4254,#4255,
#4256,#4257,#4258,#4259,#4260,#4261),.UNSPECIFIED.,.F.,.F.,(4,2,1,1,1,1,
1,1,4),(19.9661761551458,19.973617367215,20.9722982355758,21.9709791039365,
22.9696599722973,23.968340840658,24.9670217090188,25.9657025773795,26.2493568946854),
 .UNSPECIFIED.);
#707=B_SPLINE_CURVE_WITH_KNOTS('',3,(#4263,#4264,#4265,#4266,#4267,#4268,
#4269,#4270,#4271,#4272,#4273,#4274,#4275,#4276,#4277,#4278,#4279,#4280,
#4281,#4282,#4283,#4284,#4285,#4286,#4287,#4288,#4289,#4290,#4291,#4292,
#4293,#4294,#4295,#4296,#4297,#4298,#4299,#4300,#4301,#4302,#4303,#4304,
#4305,#4306,#4307,#4308,#4309,#4310,#4311,#4312,#4313,#4314,#4315,#4316,
#4317,#4318,#4319,#4320,#4321,#4322,#4323,#4324,#4325,#4326,#4327,#4328,
#4329,#4330,#4331,#4332,#4333,#4334,#4335,#4336,#4337,#4338,#4339,#4340,
#4341,#4342,#4343,#4344,#4345,#4346,#4347,#4348,#4349,#4350,#4351,#4352,
#4353,#4354,#4355,#4356,#4357,#4358,#4359,#4360,#4361,#4362,#4363,#4364,
#4365,#4366,#4367,#4368,#4369,#4370,#4371,#4372,#4373,#4374,#4375,#4376,
#4377,#4378,#4379,#4380,#4381,#4382,#4383,#4384,#4385,#4386,#4387,#4388,
#4389,#4390,#4391,#4392,#4393,#4394,#4395,#4396,#4397,#4398,#4399,#4400,
#4401,#4402,#4403,#4404,#4405,#4406,#4407,#4408,#4409,#4410,#4411,#4412,
#4413,#4414,#4415,#4416,#4417,#4418,#4419,#4420,#4421,#4422,#4423,#4424,
#4425,#4426,#4427,#4428,#4429,#4430,#4431,#4432,#4433,#4434,#4435,#4436,
#4437,#4438,#4439,#4440,#4441,#4442,#4443,#4444,#4445,#4446,#4447,#4448,
#4449,#4450,#4451,#4452,#4453,#4454,#4455),.UNSPECIFIED.,.F.,.F.,(4,3,3,
3,3,3,3,3,3,3,3,3,3,3,3,3,3,3,3,3,3,3,3,3,3,3,3,3,3,3,3,3,3,3,3,3,3,3,3,
3,3,3,3,3,3,3,3,3,3,3,3,3,3,3,3,3,3,3,3,3,3,3,3,3,4),(26.2493614623254,
26.3479492131184,26.4464925326639,26.545022844986,26.6435715522213,26.7422307023355,
26.8409562100383,26.9398413203745,26.9643834457403,27.0640670117324,27.1636073598688,
27.2635394791478,27.3629001839775,27.4622279485599,27.5615532346581,27.6619310045188,
27.7614009397454,27.8622326269232,27.963064314101,28.0627478801,28.162288228243,
28.2622203475203,28.3615810523563,28.4609088169447,28.5602341030488,28.6606118729021,
28.7600818081338,28.8609134952978,28.9617451824618,29.061428748488,29.1609690966589,
29.2609012159294,29.3602619207941,29.4595896854117,29.5589149715449,29.6592927413643,
29.7587626766259,29.8595943637242,29.9604260508225,30.0601096168314,30.1596499649844,
30.2595820842593,30.3589427891061,30.4582705537053,30.5575958398202,30.657973609661,
30.7574435449042,30.8582752320438,30.9591069191833,31.0587904851944,31.1583308333497,
31.258262952624,31.357623657473,31.4569514220748,31.5562767081925,31.6566544780304,
31.7561244132758,31.8569561004099,31.957787787544,32.0596638740538,32.1613737804538,
32.2629105875756,32.3643455803479,32.4656954588227,32.532546769505),
 .UNSPECIFIED.);
#708=B_SPLINE_CURVE_WITH_KNOTS('',3,(#4457,#4458,#4459,#4460,#4461,#4462,
#4463,#4464,#4465,#4466),.UNSPECIFIED.,.F.,.F.,(4,1,1,1,1,1,1,4),(32.5325523549555,
32.9564686559048,33.9551495242656,34.9538303926263,35.9525112609871,36.9511921293478,
37.9498729977086,38.8157320766846),.UNSPECIFIED.);
#709=B_SPLINE_CURVE_WITH_KNOTS('',3,(#4468,#4469,#4470,#4471,#4472,#4473,
#4474,#4475,#4476,#4477,#4478),.UNSPECIFIED.,.F.,.F.,(4,1,1,1,1,1,1,1,4),
(38.8157320766846,38.9485538660693,39.9472347344301,40.9459156027908,41.9445964711516,
42.9432773395123,43.9419582078731,44.9406390762338,45.0989173838642),
 .UNSPECIFIED.);
#710=B_SPLINE_CURVE_WITH_KNOTS('',3,(#4480,#4481,#4482,#4483,#4484,#4485,
#4486,#4487,#4488,#4489),.UNSPECIFIED.,.F.,.F.,(4,1,1,1,1,1,1,4),(45.0989173838642,
45.9393199445946,46.9380008129553,47.9366816813161,48.9353625496768,49.9340434180376,
50.9327242863983,51.3821026910438),.UNSPECIFIED.);
#711=B_SPLINE_CURVE_WITH_KNOTS('',3,(#4491,#4492,#4493,#4494,#4495,#4496,
#4497,#4498,#4499,#4500),.UNSPECIFIED.,.F.,.F.,(4,1,1,1,1,1,1,4),(51.3821026910438,
51.9314051547591,52.9300860231198,53.9287668914806,54.9274477598413,55.9261286282021,
56.9248094965628,57.6652879982234),.UNSPECIFIED.);
#712=B_SPLINE_CURVE_WITH_KNOTS('',3,(#4502,#4503,#4504,#4505,#4506,#4507,
#4508,#4509,#4510,#4511,#4512,#4513,#4514,#4515,#4516,#4517,#4518,#4519,
#4520,#4521,#4522,#4523,#4524,#4525,#4526,#4527,#4528,#4529,#4530,#4531,
#4532,#4533,#4534,#4535,#4536,#4537,#4538,#4539,#4540,#4541,#4542,#4543,
#4544,#4545,#4546,#4547,#4548,#4549,#4550,#4551,#4552,#4553,#4554,#4555,
#4556,#4557,#4558,#4559,#4560,#4561,#4562,#4563,#4564,#4565,#4566,#4567,
#4568,#4569,#4570,#4571,#4572,#4573,#4574,#4575,#4576,#4577,#4578,#4579,
#4580,#4581,#4582,#4583,#4584,#4585,#4586,#4587,#4588,#4589,#4590,#4591,
#4592,#4593,#4594,#4595,#4596,#4597,#4598,#4599,#4600,#4601,#4602,#4603,
#4604,#4605,#4606,#4607,#4608,#4609,#4610,#4611,#4612,#4613,#4614,#4615,
#4616,#4617,#4618,#4619,#4620,#4621,#4622,#4623,#4624,#4625,#4626,#4627,
#4628,#4629,#4630,#4631,#4632,#4633,#4634,#4635,#4636,#4637,#4638,#4639,
#4640,#4641,#4642,#4643,#4644,#4645,#4646,#4647,#4648,#4649,#4650,#4651,
#4652,#4653,#4654,#4655,#4656,#4657,#4658,#4659,#4660,#4661,#4662,#4663,
#4664,#4665,#4666,#4667,#4668,#4669,#4670,#4671,#4672,#4673,#4674,#4675,
#4676,#4677,#4678,#4679,#4680,#4681,#4682,#4683,#4684,#4685,#4686,#4687,
#4688,#4689,#4690,#4691),.UNSPECIFIED.,.F.,.F.,(4,3,3,3,3,3,3,3,3,3,3,3,
3,3,3,3,3,3,3,3,3,3,3,3,3,3,3,3,3,3,3,3,3,3,3,3,3,3,3,3,3,3,3,3,3,3,3,3,
3,3,3,3,3,3,3,3,3,3,3,3,3,3,3,4),(57.6652881545519,57.7943892597378,57.9234903649236,
58.0231739309364,58.1227142790933,58.2226463983672,58.3220071032179,58.4213348678212,
58.5206601539402,58.6210379237762,58.7205078590233,58.8213395461538,58.9221712332843,
59.0218547992971,59.1213951474542,59.221327266728,59.3206879715787,59.420015736182,
59.5193410223011,59.6197187921371,59.7191887273842,59.8200204145147,59.9208521016451,
60.0205356676579,60.1200760158151,60.2200081350889,60.3193688399396,60.418696604543,
60.5180218906621,60.618399660498,60.7178695957452,60.8187012828756,60.9195329700059,
61.0192165360187,61.1187568841757,61.2186890034496,61.3180497083003,61.4173774729035,
61.5167027590226,61.6170805288586,61.7165504641057,61.8173821512361,61.9182138383666,
62.0178974043794,62.1174377525365,62.2173698718104,62.316730576661,62.4160583412643,
62.5153836273834,62.6157613972194,62.7152313324666,62.816063019597,62.9168947067274,
63.0165782727402,63.1161186208972,63.2160507401711,63.3154114450218,63.4147392096251,
63.5140644957442,63.6144422655802,63.7139122008273,63.8147438879577,63.9155755750881,
63.948473305403),.UNSPECIFIED.);
#713=B_SPLINE_CURVE_WITH_KNOTS('',3,(#4693,#4694,#4695,#4696,#4697,#4698,
#4699,#4700,#4701,#4702),.UNSPECIFIED.,.F.,.F.,(4,1,1,1,1,1,1,4),(63.9484777838044,
64.9142564434489,65.9129373118096,66.9116181801704,67.9102990485311,68.9089799168918,
69.9076607852526,70.2316517155),.UNSPECIFIED.);
#714=B_SPLINE_CURVE_WITH_KNOTS('',3,(#4704,#4705,#4706,#4707,#4708,#4709,
#4710,#4711,#4712,#4713,#4714,#4715,#4716,#4717,#4718,#4719,#4720,#4721,
#4722,#4723,#4724,#4725,#4726,#4727,#4728,#4729,#4730,#4731,#4732,#4733,
#4734,#4735,#4736,#4737,#4738,#4739,#4740,#4741,#4742,#4743,#4744,#4745,
#4746,#4747,#4748,#4749,#4750,#4751,#4752,#4753,#4754,#4755,#4756,#4757,
#4758,#4759,#4760,#4761,#4762,#4763,#4764,#4765,#4766,#4767,#4768,#4769,
#4770,#4771,#4772,#4773,#4774,#4775,#4776,#4777,#4778,#4779,#4780,#4781,
#4782,#4783,#4784,#4785,#4786,#4787,#4788,#4789,#4790,#4791,#4792,#4793,
#4794,#4795,#4796,#4797,#4798,#4799,#4800,#4801,#4802,#4803,#4804,#4805,
#4806,#4807,#4808,#4809,#4810,#4811,#4812,#4813,#4814,#4815,#4816,#4817,
#4818,#4819,#4820,#4821,#4822,#4823,#4824,#4825,#4826,#4827,#4828,#4829,
#4830,#4831,#4832,#4833,#4834,#4835,#4836,#4837,#4838,#4839,#4840,#4841,
#4842,#4843,#4844,#4845,#4846,#4847,#4848,#4849,#4850,#4851,#4852,#4853,
#4854,#4855,#4856,#4857,#4858,#4859,#4860,#4861,#4862,#4863,#4864,#4865,
#4866,#4867,#4868,#4869,#4870,#4871,#4872,#4873,#4874,#4875,#4876,#4877,
#4878,#4879,#4880,#4881,#4882,#4883,#4884,#4885,#4886,#4887,#4888,#4889,
#4890,#4891,#4892,#4893),.UNSPECIFIED.,.F.,.F.,(4,3,3,3,3,3,3,3,3,3,3,3,
3,3,3,3,3,3,3,3,3,3,3,3,3,3,3,3,3,3,3,3,3,3,3,3,3,3,3,3,3,3,3,3,3,3,3,3,
3,3,3,3,3,3,3,3,3,3,3,3,3,3,3,4),(70.2316586125826,70.3307800166858,70.4298793745695,
70.5289873506871,70.6282047037803,70.7274781134284,70.8269336412923,70.9063416536133,
71.0060252196261,71.1055655677834,71.2054976870572,71.3048583919079,71.4041861565112,
71.5035114426302,71.6038892124662,71.7033591477134,71.8041908348438,71.9050225219741,
72.0047060879869,72.1042464361441,72.2041785554179,72.3035392602686,72.402867024872,
72.5021923109908,72.6025700808268,72.702040016074,72.8028717032045,72.9037033903349,
73.0033869563477,73.1029273045047,73.2028594237785,73.3022201286292,73.4015478932325,
73.5008731793516,73.6012509491876,73.7007208844348,73.8015525715652,73.9023842586956,
74.0020678247084,74.1016081728656,74.2015402921394,74.3009009969901,74.4002287615935,
74.4995540477125,74.5999318175485,74.6994017527956,74.800233439926,74.9010651270564,
75.0007486930691,75.1002890412263,75.2002211605002,75.299581865351,75.3989096299542,
75.4982349160732,75.5986126859092,75.6980826211565,75.7989143082868,75.8997459954171,
76.000471352571,76.1010449027966,76.204494657038,76.3048389751224,76.4098414474423,
76.5148439197622),.UNSPECIFIED.);
#715=B_SPLINE_CURVE_WITH_KNOTS('',3,(#4895,#4896,#4897,#4898,#4899,#4900,
#4901,#4902,#4903,#4904),.UNSPECIFIED.,.F.,.F.,(4,1,1,1,1,1,1,4),(76.5148513200435,
76.8984268637779,77.8971077321387,78.8957886004994,79.8944694688601,80.8931503372209,
81.8918312055816,82.7980204291147),.UNSPECIFIED.);
#716=B_SPLINE_CURVE_WITH_KNOTS('',3,(#4906,#4907,#4908,#4909,#4910,#4911,
#4912,#4913,#4914,#4915,#4916,#4917,#4918,#4919,#4920,#4921,#4922,#4923,
#4924,#4925,#4926,#4927,#4928,#4929,#4930,#4931,#4932,#4933,#4934,#4935,
#4936,#4937,#4938,#4939,#4940,#4941,#4942,#4943,#4944,#4945,#4946,#4947,
#4948,#4949,#4950,#4951,#4952,#4953,#4954,#4955,#4956,#4957,#4958,#4959,
#4960,#4961,#4962,#4963,#4964,#4965,#4966,#4967,#4968,#4969,#4970,#4971,
#4972,#4973,#4974,#4975,#4976,#4977,#4978,#4979,#4980,#4981,#4982,#4983,
#4984,#4985,#4986,#4987,#4988,#4989,#4990,#4991,#4992,#4993,#4994,#4995,
#4996,#4997,#4998,#4999,#5000,#5001,#5002,#5003,#5004,#5005,#5006,#5007,
#5008,#5009,#5010,#5011,#5012,#5013,#5014,#5015,#5016,#5017,#5018,#5019,
#5020,#5021,#5022,#5023,#5024,#5025,#5026,#5027,#5028,#5029,#5030,#5031,
#5032,#5033,#5034,#5035,#5036,#5037,#5038,#5039,#5040,#5041,#5042,#5043,
#5044,#5045,#5046,#5047,#5048,#5049,#5050,#5051,#5052,#5053,#5054,#5055,
#5056,#5057,#5058,#5059,#5060,#5061,#5062,#5063,#5064,#5065,#5066,#5067,
#5068,#5069,#5070,#5071,#5072,#5073,#5074,#5075,#5076,#5077,#5078,#5079,
#5080,#5081,#5082,#5083,#5084,#5085,#5086,#5087,#5088,#5089,#5090,#5091,
#5092,#5093,#5094,#5095),.UNSPECIFIED.,.F.,.F.,(4,3,3,3,3,3,3,3,3,3,3,3,
3,3,3,3,3,3,3,3,3,3,3,3,3,3,3,3,3,3,3,3,3,3,3,3,3,3,3,3,3,3,3,3,3,3,3,3,
3,3,3,3,3,3,3,3,3,3,3,3,3,3,3,4),(82.7980292269418,82.8905120739424,82.9901956399552,
83.0897359881124,83.1896681073862,83.2890288122369,83.3883565768402,83.4876818629593,
83.5880596327953,83.6875295680425,83.7883612551728,83.8891929423031,83.9888765083159,
84.088416856473,84.1883489757469,84.2877096805976,84.3870374452009,84.48636273132,
84.586740501156,84.6862104364031,84.7870421235335,84.8878738106639,84.9875573766767,
85.0870977248337,85.1870298441076,85.2863905489582,85.3857183135615,85.4850435996806,
85.5854213695166,85.6848913047637,85.7857229918941,85.8865546790246,85.9862382450374,
86.0857785931945,86.1857107124683,86.285071417319,86.3843991819223,86.4837244680414,
86.5841022378774,86.6835721731245,86.784403860255,86.8852355473854,86.9849191133982,
87.0844594615553,87.1843915808292,87.2837522856799,87.3830800502832,87.4824053364024,
87.5827831062383,87.6822530414855,87.7830847286158,87.8839164157462,87.983599981759,
88.083140329916,88.1830724491899,88.2824331540406,88.3817609186438,88.4810862047629,
88.5814639745989,88.680933909846,88.7817655969764,88.8825972841069,89.0259343107751,
89.0812145341213),.UNSPECIFIED.);
#717=B_SPLINE_CURVE_WITH_KNOTS('',3,(#5097,#5098,#5099,#5100,#5101,#5102,
#5103,#5104,#5105,#5106,#5107,#5108,#5109,#5110,#5111,#5112,#5113,#5114,
#5115,#5116,#5117,#5118,#5119,#5120,#5121,#5122,#5123,#5124,#5125,#5126,
#5127,#5128,#5129,#5130,#5131,#5132,#5133,#5134,#5135,#5136,#5137,#5138,
#5139,#5140,#5141,#5142,#5143,#5144,#5145,#5146,#5147,#5148,#5149,#5150,
#5151,#5152,#5153,#5154,#5155,#5156,#5157,#5158,#5159,#5160,#5161,#5162,
#5163,#5164,#5165,#5166,#5167,#5168,#5169,#5170,#5171,#5172,#5173,#5174,
#5175,#5176,#5177,#5178,#5179,#5180,#5181,#5182,#5183,#5184,#5185,#5186,
#5187,#5188,#5189,#5190,#5191,#5192,#5193,#5194,#5195,#5196,#5197,#5198,
#5199,#5200,#5201,#5202,#5203,#5204,#5205,#5206,#5207,#5208,#5209,#5210,
#5211,#5212,#5213,#5214,#5215,#5216,#5217,#5218,#5219,#5220,#5221,#5222,
#5223,#5224,#5225,#5226,#5227,#5228,#5229,#5230,#5231,#5232,#5233,#5234,
#5235,#5236,#5237,#5238,#5239,#5240,#5241,#5242,#5243,#5244,#5245,#5246,
#5247,#5248,#5249,#5250,#5251,#5252,#5253,#5254,#5255,#5256,#5257,#5258,
#5259,#5260,#5261,#5262,#5263,#5264,#5265,#5266,#5267,#5268,#5269,#5270,
#5271,#5272,#5273,#5274,#5275,#5276,#5277,#5278,#5279,#5280,#5281,#5282,
#5283,#5284,#5285,#5286,#5287,#5288,#5289),.UNSPECIFIED.,.F.,.F.,(4,3,3,
3,3,3,3,3,3,3,3,3,3,3,3,3,3,3,3,3,3,3,3,3,3,3,3,3,3,3,3,3,3,3,3,3,3,3,3,
3,3,3,3,3,3,3,3,3,3,3,3,3,3,3,3,3,3,3,3,3,3,3,3,3,4),(89.0812145344659,
89.1812224867161,89.2791888648667,89.3771066451239,89.4750078977673,89.5765754614424,
89.6745991542258,89.7726889754984,89.8709299133438,89.8812781524677,89.9809617184804,
90.0805020666376,90.1804341859115,90.2797948907621,90.3791226553653,90.4784479414842,
90.5788257113202,90.6782956465674,90.7791273336979,90.8799590208284,90.9796425868411,
91.0791829349983,91.1791150542722,91.2784757591229,91.3778035237263,91.4771288098453,
91.5775065796813,91.6769765149286,91.7778082020589,91.8786398891892,91.978323455202,
92.0778638033592,92.1777959226331,92.2771566274838,92.376484392087,92.4758096782061,
92.5761874480421,92.6756573832893,92.7764890704196,92.8773207575499,92.9770043235627,
93.07654467172,93.1764767909939,93.2758374958446,93.3751652604479,93.4744905465672,
93.574868316403,93.6743382516501,93.7751699387804,93.8760016259107,93.9756851919234,
94.0752255400803,94.1751576593542,94.274518364205,94.3738461288083,94.4731714149275,
94.5735491847635,94.6730191200106,94.773850807141,94.8746824942714,94.9799562416788,
95.0849191111029,95.1896943939098,95.2942224671571,95.3643998410932),
 .UNSPECIFIED.);
#718=B_SPLINE_CURVE_WITH_KNOTS('',3,(#5291,#5292,#5293,#5294,#5295,#5296,
#5297,#5298,#5299,#5300,#5301,#5302,#5303,#5304,#5305,#5306,#5307,#5308,
#5309,#5310,#5311,#5312,#5313,#5314,#5315,#5316,#5317,#5318,#5319,#5320,
#5321,#5322,#5323,#5324,#5325,#5326,#5327,#5328,#5329,#5330,#5331,#5332,
#5333,#5334,#5335,#5336,#5337,#5338,#5339,#5340,#5341,#5342,#5343,#5344,
#5345,#5346,#5347,#5348,#5349,#5350,#5351,#5352,#5353,#5354,#5355,#5356,
#5357,#5358,#5359,#5360,#5361,#5362,#5363,#5364,#5365,#5366,#5367,#5368,
#5369,#5370,#5371,#5372,#5373,#5374,#5375,#5376,#5377,#5378,#5379,#5380,
#5381,#5382,#5383,#5384,#5385,#5386,#5387,#5388,#5389,#5390,#5391,#5392,
#5393,#5394,#5395,#5396,#5397,#5398,#5399,#5400,#5401,#5402,#5403,#5404,
#5405,#5406,#5407,#5408,#5409,#5410,#5411,#5412,#5413,#5414,#5415,#5416,
#5417,#5418,#5419,#5420,#5421,#5422,#5423,#5424,#5425,#5426,#5427,#5428,
#5429,#5430,#5431,#5432,#5433,#5434,#5435,#5436,#5437,#5438,#5439,#5440,
#5441,#5442,#5443,#5444,#5445,#5446,#5447,#5448,#5449,#5450,#5451,#5452,
#5453,#5454,#5455,#5456,#5457,#5458,#5459,#5460,#5461,#5462,#5463,#5464,
#5465,#5466,#5467,#5468,#5469,#5470,#5471,#5472,#5473,#5474,#5475,#5476,
#5477,#5478,#5479,#5480),.UNSPECIFIED.,.F.,.F.,(4,3,3,3,3,3,3,3,3,3,3,3,
3,3,3,3,3,3,3,3,3,3,3,3,3,3,3,3,3,3,3,3,3,3,3,3,3,3,3,3,3,3,3,3,3,3,3,3,
3,3,3,3,3,3,3,3,3,3,3,3,3,3,3,4),(95.3643998413009,95.4680336789824,95.5719312818759,
95.6759621223708,95.7802739763669,95.8733633626321,95.9730469286449,96.072587276802,
96.1725193960759,96.2718801009265,96.3712078655298,96.4705331516489,96.5709109214849,
96.670380856732,96.7712125438624,96.8720442309929,96.9717277970057,97.0712681451628,
97.1712002644367,97.2705609692874,97.3698887338907,97.4692140200096,97.5695917898456,
97.6690617250928,97.7698934122232,97.8707250993537,97.9704086653665,98.069949013524,
98.1698811327978,98.2692418376485,98.3685696022517,98.4678948883709,98.5682726582068,
98.667742593454,98.7685742805842,98.8694059677144,98.9690895337272,99.0686298818843,
99.1685620011582,99.2679227060087,99.3672504706121,99.4665757567313,99.5669535265673,
99.6664234618143,99.7672551489447,99.8680868360752,99.9677704020879,100.067310750245,
100.167242869519,100.26660357437,100.365931338973,100.465256625092,100.565634394928,
100.665104330175,100.765936017306,100.866767704436,100.965052680092,101.063210571496,
101.16127360859,101.259273897761,101.357280728377,101.455284337592,101.55338873245,
101.647585148481),.UNSPECIFIED.);
#719=B_SPLINE_CURVE_WITH_KNOTS('',3,(#5482,#5483,#5484,#5485,#5486,#5487,
#5488,#5489,#5490,#5491,#5492),.UNSPECIFIED.,.F.,.F.,(4,1,1,1,1,1,1,1,4),
(101.647585148481,101.865448572797,102.864129441157,103.862810309518,104.861491177879,
105.86017204624,106.8588529146,107.857533782961,107.93077045566),
 .UNSPECIFIED.);
#720=B_SPLINE_CURVE_WITH_KNOTS('',3,(#5494,#5495,#5496,#5497,#5498,#5499,
#5500,#5501,#5502,#5503,#5504,#5505,#5506,#5507,#5508,#5509,#5510,#5511,
#5512,#5513,#5514,#5515,#5516,#5517,#5518,#5519,#5520,#5521,#5522,#5523,
#5524,#5525,#5526,#5527,#5528,#5529,#5530,#5531,#5532,#5533,#5534,#5535,
#5536,#5537,#5538,#5539,#5540,#5541,#5542,#5543,#5544,#5545,#5546,#5547,
#5548,#5549,#5550,#5551,#5552,#5553,#5554,#5555,#5556,#5557,#5558,#5559,
#5560,#5561,#5562,#5563,#5564,#5565,#5566,#5567,#5568,#5569,#5570,#5571,
#5572,#5573,#5574,#5575,#5576,#5577,#5578,#5579,#5580,#5581,#5582,#5583,
#5584,#5585,#5586,#5587,#5588,#5589,#5590,#5591,#5592,#5593,#5594,#5595,
#5596,#5597,#5598,#5599,#5600,#5601,#5602,#5603,#5604,#5605,#5606,#5607,
#5608,#5609,#5610,#5611,#5612,#5613,#5614,#5615,#5616,#5617,#5618,#5619,
#5620,#5621,#5622,#5623,#5624,#5625,#5626,#5627,#5628,#5629,#5630,#5631,
#5632,#5633,#5634,#5635,#5636,#5637,#5638,#5639,#5640,#5641,#5642,#5643,
#5644,#5645,#5646,#5647,#5648,#5649,#5650,#5651,#5652,#5653,#5654,#5655,
#5656,#5657,#5658,#5659,#5660,#5661,#5662,#5663,#5664,#5665,#5666,#5667,
#5668,#5669,#5670,#5671,#5672,#5673,#5674,#5675,#5676,#5677,#5678,#5679,
#5680,#5681,#5682,#5683,#5684,#5685,#5686),.UNSPECIFIED.,.F.,.F.,(4,3,3,
3,3,3,3,3,3,3,3,3,3,3,3,3,3,3,3,3,3,3,3,3,3,3,3,3,3,3,3,3,3,3,3,3,3,3,3,
3,3,3,3,3,3,3,3,3,3,3,3,3,3,3,3,3,3,3,3,3,3,3,3,3,4),(107.93077045566,108.029399639198,
108.132751515713,108.231141282269,108.329479409736,108.42779758391,108.526127461288,
108.624561429513,108.723056288678,108.821710387347,108.856214651322,108.955898217335,
109.055438565492,109.155370684766,109.254731389617,109.35405915422,109.453384440339,
109.553762210175,109.653232145423,109.754063832553,109.854895519683,109.954579085695,
110.054119433852,110.154051553126,110.253412257977,110.35274002258,110.452065308699,
110.552443078535,110.651913013782,110.752744700912,110.853576388043,110.953259954056,
111.052800302213,111.152732421487,111.252093126338,111.351420890941,111.45074617706,
111.551123946896,111.650593882143,111.751425569273,111.852257256404,111.951940822417,
112.051481170574,112.151413289848,112.250773994699,112.350101759302,112.449427045422,
112.549804815257,112.649274750505,112.750106437635,112.850938124765,112.950621690778,
113.050162038935,113.150094158209,113.249454863059,113.348782627663,113.448107913782,
113.548485683618,113.647955618865,113.748787305995,113.849618993126,113.963410379371,
114.076729763095,114.189250107695,114.213955762605),.UNSPECIFIED.);
#721=B_SPLINE_CURVE_WITH_KNOTS('',3,(#5688,#5689,#5690,#5691,#5692,#5693,
#5694,#5695,#5696,#5697,#5698,#5699,#5700,#5701,#5702,#5703,#5704,#5705,
#5706,#5707,#5708,#5709,#5710,#5711,#5712,#5713,#5714,#5715,#5716,#5717,
#5718,#5719,#5720,#5721,#5722,#5723,#5724,#5725,#5726,#5727,#5728,#5729,
#5730,#5731,#5732,#5733,#5734,#5735,#5736,#5737,#5738,#5739,#5740,#5741,
#5742,#5743,#5744,#5745,#5746,#5747,#5748,#5749,#5750,#5751,#5752,#5753,
#5754,#5755,#5756,#5757,#5758,#5759,#5760,#5761,#5762,#5763,#5764,#5765,
#5766,#5767,#5768,#5769,#5770,#5771,#5772,#5773,#5774,#5775,#5776,#5777,
#5778,#5779,#5780,#5781,#5782,#5783,#5784,#5785,#5786,#5787,#5788,#5789,
#5790,#5791,#5792,#5793,#5794,#5795,#5796,#5797,#5798,#5799,#5800,#5801,
#5802,#5803,#5804,#5805,#5806,#5807,#5808,#5809,#5810,#5811,#5812,#5813,
#5814,#5815,#5816,#5817,#5818,#5819,#5820,#5821,#5822,#5823,#5824,#5825,
#5826,#5827,#5828,#5829,#5830,#5831,#5832,#5833,#5834,#5835,#5836,#5837,
#5838,#5839,#5840,#5841,#5842,#5843,#5844,#5845,#5846,#5847,#5848,#5849,
#5850,#5851,#5852,#5853,#5854,#5855,#5856,#5857,#5858,#5859,#5860,#5861,
#5862,#5863,#5864,#5865,#5866,#5867,#5868,#5869,#5870,#5871,#5872,#5873,
#5874,#5875,#5876,#5877,#5878,#5879,#5880),.UNSPECIFIED.,.F.,.F.,(4,3,3,
3,3,3,3,3,3,3,3,3,3,3,3,3,3,3,3,3,3,3,3,3,3,3,3,3,3,3,3,3,3,3,3,3,3,3,3,
3,3,3,3,3,3,3,3,3,3,3,3,3,3,3,3,3,3,3,3,3,3,3,3,3,4),(114.21395576284,114.31380774229,
114.413664648862,114.513555872153,114.613578633856,114.713677918333,114.813953963102,
114.848299861486,114.947983427499,115.047523775657,115.14745589493,115.246816599781,
115.346144364385,115.445469650504,115.54584742034,115.645317355587,115.746149042717,
115.846980729847,115.94666429586,116.046204644017,116.146136763291,116.245497468142,
116.344825232745,116.444150518864,116.5445282887,116.643998223947,116.744829911078,
116.845661598208,116.945345164221,117.044885512378,117.144817631652,117.244178336503,
117.343506101106,117.442831387225,117.543209157061,117.642679092308,117.743510779439,
117.844342466569,117.944026032582,118.043566380739,118.143498500012,118.242859204863,
118.342186969466,118.441512255585,118.541890025421,118.641359960668,118.742191647798,
118.843023334929,118.942706900942,119.042247249099,119.142179368373,119.241540073224,
119.340867837827,119.440193123946,119.540570893782,119.640040829029,119.74087251616,
119.84170420329,119.941520374619,120.041194654516,120.140757472728,120.240240659712,
120.339676519161,120.439118953947,120.497141070019),.UNSPECIFIED.);
#722=B_SPLINE_CURVE_WITH_KNOTS('',3,(#5882,#5883,#5884,#5885,#5886,#5887,
#5888,#5889,#5890,#5891,#5892,#5893,#5894,#5895,#5896,#5897,#5898,#5899,
#5900,#5901,#5902,#5903,#5904,#5905,#5906,#5907,#5908,#5909,#5910,#5911,
#5912,#5913,#5914,#5915,#5916,#5917,#5918,#5919,#5920,#5921,#5922,#5923,
#5924,#5925,#5926,#5927,#5928,#5929,#5930,#5931,#5932,#5933,#5934,#5935,
#5936,#5937,#5938,#5939,#5940,#5941,#5942,#5943,#5944,#5945,#5946,#5947,
#5948,#5949,#5950,#5951,#5952,#5953,#5954,#5955,#5956,#5957,#5958,#5959,
#5960,#5961,#5962,#5963,#5964,#5965,#5966,#5967,#5968,#5969,#5970,#5971,
#5972,#5973,#5974,#5975,#5976,#5977,#5978,#5979,#5980,#5981,#5982,#5983,
#5984,#5985,#5986,#5987,#5988,#5989,#5990,#5991,#5992,#5993,#5994,#5995,
#5996,#5997,#5998,#5999,#6000,#6001,#6002,#6003,#6004,#6005,#6006,#6007,
#6008,#6009,#6010,#6011,#6012,#6013,#6014,#6015,#6016,#6017,#6018,#6019,
#6020,#6021,#6022,#6023,#6024,#6025,#6026,#6027,#6028,#6029,#6030,#6031,
#6032,#6033,#6034,#6035,#6036,#6037,#6038,#6039,#6040,#6041,#6042,#6043,
#6044,#6045,#6046,#6047,#6048,#6049,#6050,#6051,#6052,#6053,#6054,#6055,
#6056,#6057,#6058,#6059,#6060,#6061,#6062,#6063,#6064,#6065,#6066,#6067,
#6068,#6069,#6070,#6071),.UNSPECIFIED.,.F.,.F.,(4,3,3,3,3,3,3,3,3,3,3,3,
3,3,3,3,3,3,3,3,3,3,3,3,3,3,3,3,3,3,3,3,3,3,3,3,3,3,3,3,3,3,3,3,3,3,3,3,
3,3,3,3,3,3,3,3,3,3,3,3,3,3,3,4),(120.497141070246,120.611799468103,120.727559034228,
120.840385071651,120.940068637664,121.039608985821,121.139541105095,121.238901809945,
121.338229574549,121.437554860668,121.537932630504,121.637402565751,121.738234252881,
121.839065940012,121.938749506025,122.038289854181,122.138221973455,122.237582678306,
122.336910442909,122.436235729027,122.536613498864,122.63608343411,122.736915121241,
122.837746808372,122.937430374385,123.036970722542,123.136902841816,123.236263546666,
123.33559131127,123.434916597389,123.535294367225,123.634764302472,123.735595989603,
123.836427676733,123.936111242746,124.035651590903,124.135583710177,124.234944415028,
124.334272179631,124.433597465751,124.533975235586,124.633445170834,124.734276857964,
124.835108545094,124.934792111107,125.034332459264,125.134264578538,125.233625283389,
125.332953047992,125.432278334111,125.532656103947,125.632126039194,125.732957726325,
125.833789413455,125.932685008728,126.031438152,126.130077732587,126.228656280004,
126.327205255562,126.425756081762,126.5244022177,126.623100091491,126.721959841375,
126.780326377199),.UNSPECIFIED.);
#723=B_SPLINE_CURVE_WITH_KNOTS('',3,(#6073,#6074,#6075,#6076,#6077,#6078,
#6079,#6080,#6081,#6082,#6083,#6084),.UNSPECIFIED.,.F.,.F.,(4,2,1,1,1,1,
1,1,4),(126.780326377199,126.832470281815,127.831151150176,128.829832018537,
129.828512886898,130.827193755258,131.825874623619,132.82455549198,133.063511684379),
 .UNSPECIFIED.);
#724=B_SPLINE_CURVE_WITH_KNOTS('',3,(#6086,#6087,#6088,#6089,#6090,#6091,
#6092,#6093,#6094,#6095),.UNSPECIFIED.,.F.,.F.,(4,1,1,1,1,1,1,4),(133.063511684379,
133.823236360341,134.821917228701,135.820598097062,136.819278965423,137.817959833784,
138.816640702144,139.346696991558),.UNSPECIFIED.);
#725=B_SPLINE_CURVE_WITH_KNOTS('',3,(#6097,#6098,#6099,#6100,#6101,#6102,
#6103,#6104,#6105,#6106,#6107,#6108,#6109,#6110,#6111,#6112,#6113,#6114,
#6115,#6116,#6117,#6118,#6119,#6120,#6121,#6122,#6123,#6124,#6125,#6126,
#6127,#6128,#6129,#6130,#6131,#6132,#6133,#6134,#6135,#6136,#6137,#6138,
#6139,#6140,#6141,#6142,#6143,#6144,#6145,#6146,#6147,#6148,#6149,#6150,
#6151,#6152,#6153,#6154,#6155,#6156,#6157,#6158,#6159,#6160,#6161,#6162,
#6163,#6164,#6165,#6166,#6167,#6168,#6169,#6170,#6171,#6172,#6173,#6174,
#6175,#6176,#6177,#6178,#6179,#6180,#6181,#6182,#6183,#6184,#6185,#6186,
#6187,#6188,#6189,#6190,#6191,#6192,#6193,#6194,#6195,#6196,#6197,#6198,
#6199,#6200,#6201,#6202,#6203,#6204,#6205,#6206,#6207,#6208,#6209,#6210,
#6211,#6212,#6213,#6214,#6215,#6216,#6217,#6218,#6219,#6220,#6221,#6222,
#6223,#6224,#6225,#6226,#6227,#6228,#6229,#6230,#6231,#6232,#6233,#6234,
#6235,#6236,#6237,#6238,#6239,#6240,#6241,#6242,#6243,#6244,#6245,#6246,
#6247,#6248,#6249,#6250,#6251,#6252,#6253,#6254,#6255,#6256,#6257,#6258,
#6259,#6260,#6261,#6262,#6263,#6264,#6265,#6266,#6267,#6268,#6269,#6270,
#6271,#6272,#6273,#6274,#6275,#6276,#6277,#6278,#6279,#6280,#6281,#6282,
#6283,#6284,#6285,#6286,#6287,#6288,#6289),.UNSPECIFIED.,.F.,.F.,(4,3,3,
3,3,3,3,3,3,3,3,3,3,3,3,3,3,3,3,3,3,3,3,3,3,3,3,3,3,3,3,3,3,3,3,3,3,3,3,
3,3,3,3,3,3,3,3,3,3,3,3,3,3,3,3,3,3,3,3,3,3,3,3,3,4),(139.34669715841,139.452165000516,
139.557994919341,139.6640172491,139.770348389444,139.815321570505,139.915005136518,
140.014545484675,140.114477603949,140.2138383088,140.313166073403,140.412491359522,
140.512869129358,140.612339064606,140.713170751736,140.814002438866,140.913686004879,
141.013226353036,141.11315847231,141.212519177161,141.311846941764,141.411172227884,
141.511549997719,141.611019932967,141.711851620097,141.812683307227,141.91236687324,
142.011907221396,142.11183934067,142.211200045521,142.310527810124,142.409853096242,
142.510230866079,142.609700801325,142.710532488456,142.811364175587,142.9110477416,
143.010588089757,143.110520209031,143.209880913881,143.309208678485,143.408533964604,
143.50891173444,143.608381669687,143.709213356817,143.810045043948,143.909728609961,
144.009268958118,144.109201077392,144.208561782243,144.307889546846,144.407214832966,
144.507592602801,144.607062538049,144.707894225179,144.808725912309,144.911370460613,
145.009401903958,145.107341864103,145.205222543426,145.303076064612,145.400976998535,
145.49890612746,145.596947071887,145.629882298738),.UNSPECIFIED.);
#726=B_SPLINE_CURVE_WITH_KNOTS('',3,(#6291,#6292,#6293,#6294,#6295,#6296,
#6297,#6298,#6299,#6300,#6301),.UNSPECIFIED.,.F.,.F.,(4,1,1,1,1,1,1,1,4),
(145.629882298738,145.80740678067,146.80608764903,147.804768517391,148.803449385752,
149.802130254113,150.800811122473,151.799491990834,151.913067605917),
 .UNSPECIFIED.);
#727=B_SPLINE_CURVE_WITH_KNOTS('',3,(#6303,#6304,#6305,#6306,#6307,#6308,
#6309,#6310,#6311,#6312,#6313,#6314,#6315,#6316,#6317,#6318,#6319,#6320,
#6321,#6322,#6323,#6324,#6325,#6326,#6327,#6328,#6329,#6330,#6331,#6332,
#6333,#6334,#6335,#6336,#6337,#6338,#6339,#6340,#6341,#6342,#6343,#6344,
#6345,#6346,#6347,#6348,#6349,#6350,#6351,#6352,#6353,#6354,#6355,#6356,
#6357,#6358,#6359,#6360,#6361,#6362,#6363,#6364,#6365,#6366,#6367,#6368,
#6369,#6370,#6371,#6372,#6373,#6374,#6375,#6376,#6377,#6378,#6379,#6380,
#6381,#6382,#6383,#6384,#6385,#6386,#6387,#6388,#6389,#6390,#6391,#6392,
#6393,#6394,#6395,#6396,#6397,#6398,#6399,#6400,#6401,#6402,#6403,#6404,
#6405,#6406,#6407,#6408,#6409,#6410,#6411,#6412,#6413,#6414,#6415,#6416,
#6417,#6418,#6419,#6420,#6421,#6422,#6423,#6424,#6425,#6426,#6427,#6428,
#6429,#6430,#6431,#6432,#6433,#6434,#6435,#6436,#6437,#6438,#6439,#6440,
#6441,#6442,#6443,#6444,#6445,#6446,#6447,#6448,#6449,#6450,#6451,#6452,
#6453,#6454,#6455,#6456,#6457,#6458,#6459,#6460,#6461,#6462,#6463,#6464,
#6465,#6466,#6467,#6468,#6469,#6470,#6471,#6472,#6473,#6474,#6475,#6476,
#6477,#6478,#6479,#6480,#6481,#6482,#6483,#6484,#6485,#6486,#6487,#6488,
#6489,#6490,#6491,#6492),.UNSPECIFIED.,.F.,.F.,(4,3,3,3,3,3,3,3,3,3,3,3,
3,3,3,3,3,3,3,3,3,3,3,3,3,3,3,3,3,3,3,3,3,3,3,3,3,3,3,3,3,3,3,3,3,3,3,3,
3,3,3,3,3,3,3,3,3,3,3,3,3,3,3,4),(151.913067605917,152.011345432823,152.10969886112,
152.207764087066,152.305785655644,152.403795535228,152.502389866219,152.600528477886,
152.69935066854,152.798172859195,152.897856425208,152.997396773365,153.097328892639,
153.19668959749,153.296017362093,153.395342648212,153.495720418048,153.595190353295,
153.696022040426,153.796853727556,153.896537293569,153.996077641725,154.096009760999,
154.19537046585,154.294698230453,154.394023516572,154.494401286408,154.593871221655,
154.694702908785,154.795534595916,154.895218161929,154.994758510086,155.09469062936,
155.19405133421,155.293379098814,155.392704384933,155.493082154769,155.592552090016,
155.693383777146,155.794215464277,155.89389903029,155.993439378447,156.093371497721,
156.192732202572,156.292059967175,156.391385253294,156.49176302313,156.591232958377,
156.692064645508,156.792896332638,156.892579898651,156.992120246808,157.092052366082,
157.191413070933,157.290740835536,157.390066121655,157.490443891491,157.589913826738,
157.690745513869,157.791577200999,157.901929993823,158.011949532061,158.121400059036,
158.196252481728),.UNSPECIFIED.);
#728=B_SPLINE_CURVE_WITH_KNOTS('',3,(#6494,#6495,#6496,#6497,#6498,#6499,
#6500,#6501,#6502,#6503),.UNSPECIFIED.,.F.,.F.,(4,1,1,1,1,1,1,4),(158.196252913097,
158.790258069359,159.78893893772,160.787619806081,161.786300674442,162.784981542803,
163.783662411163,164.479438220276),.UNSPECIFIED.);
#729=B_SPLINE_CURVE_WITH_KNOTS('',3,(#6505,#6506,#6507,#6508,#6509,#6510,
#6511,#6512,#6513,#6514,#6515,#6516,#6517,#6518,#6519,#6520,#6521,#6522,
#6523,#6524,#6525,#6526,#6527,#6528,#6529,#6530,#6531,#6532,#6533,#6534,
#6535,#6536,#6537,#6538,#6539,#6540,#6541,#6542,#6543,#6544,#6545,#6546,
#6547,#6548,#6549,#6550,#6551,#6552,#6553,#6554,#6555,#6556,#6557,#6558,
#6559,#6560,#6561,#6562,#6563,#6564,#6565,#6566,#6567,#6568,#6569,#6570,
#6571,#6572,#6573,#6574,#6575,#6576,#6577,#6578,#6579,#6580,#6581,#6582,
#6583,#6584,#6585,#6586,#6587,#6588,#6589,#6590,#6591,#6592,#6593,#6594,
#6595,#6596,#6597,#6598,#6599,#6600,#6601,#6602,#6603,#6604,#6605,#6606,
#6607,#6608,#6609,#6610,#6611,#6612,#6613,#6614,#6615,#6616,#6617,#6618,
#6619,#6620,#6621,#6622,#6623,#6624,#6625,#6626,#6627,#6628,#6629,#6630,
#6631,#6632,#6633,#6634,#6635,#6636,#6637,#6638,#6639,#6640,#6641,#6642,
#6643,#6644,#6645,#6646,#6647,#6648,#6649,#6650,#6651,#6652,#6653,#6654,
#6655,#6656,#6657,#6658,#6659,#6660,#6661,#6662,#6663,#6664,#6665,#6666,
#6667,#6668,#6669,#6670,#6671,#6672,#6673,#6674,#6675,#6676,#6677,#6678,
#6679,#6680,#6681,#6682,#6683,#6684,#6685,#6686,#6687,#6688,#6689,#6690,
#6691,#6692,#6693,#6694),.UNSPECIFIED.,.F.,.F.,(4,3,3,3,3,3,3,3,3,3,3,3,
3,3,3,3,3,3,3,3,3,3,3,3,3,3,3,3,3,3,3,3,3,3,3,3,3,3,3,3,3,3,3,3,3,3,3,3,
3,3,3,3,3,3,3,3,3,3,3,3,3,3,3,4),(164.479438408164,164.598666659614,164.719510400896,
164.782343279524,164.882026845537,164.981567193694,165.081499312967,165.180860017818,
165.280187782421,165.37951306854,165.479890838376,165.579360773623,165.680192460754,
165.781024147885,165.880707713898,165.980248062055,166.080180181329,166.17954088618,
166.278868650783,166.378193936903,166.478571706738,166.578041641986,166.678873329116,
166.779705016246,166.879388582259,166.978928930415,167.078861049689,167.17822175454,
167.277549519143,167.376874805262,167.477252575098,167.576722510345,167.677554197475,
167.778385884606,167.878069450619,167.977609798776,168.07754191805,168.1769026229,
168.276230387504,168.375555673623,168.475933443459,168.575403378706,168.676235065836,
168.777066752967,168.87675031898,168.976290667137,169.076222786411,169.175583491262,
169.274911255866,169.374236541985,169.474614311821,169.574084247068,169.674915934198,
169.775747621328,169.87522536163,169.974560042941,170.073779603311,170.172936277215,
170.272060841864,170.371184034681,170.470405346651,170.569674070912,170.669121992281,
170.762623527456),.UNSPECIFIED.);
#730=B_SPLINE_CURVE_WITH_KNOTS('',3,(#6696,#6697,#6698,#6699,#6700,#6701,
#6702,#6703,#6704,#6705,#6706,#6707),.UNSPECIFIED.,.F.,.F.,(4,2,1,1,1,1,
1,1,4),(170.762623527456,170.774428489689,171.773109358049,172.77179022641,
173.770471094771,174.769151963132,175.767832831492,176.766513699853,177.045804600382),
 .UNSPECIFIED.);
#731=B_SPLINE_CURVE_WITH_KNOTS('',3,(#6709,#6710,#6711,#6712,#6713,#6714,
#6715,#6716,#6717,#6718,#6719,#6720,#6721,#6722,#6723,#6724,#6725,#6726,
#6727,#6728,#6729,#6730,#6731,#6732,#6733,#6734,#6735,#6736,#6737,#6738,
#6739,#6740,#6741,#6742,#6743,#6744,#6745,#6746,#6747,#6748,#6749,#6750,
#6751,#6752,#6753,#6754,#6755,#6756,#6757,#6758,#6759,#6760,#6761,#6762,
#6763,#6764,#6765,#6766,#6767,#6768,#6769,#6770,#6771,#6772,#6773,#6774,
#6775,#6776,#6777,#6778,#6779,#6780,#6781,#6782,#6783,#6784,#6785,#6786,
#6787,#6788,#6789,#6790,#6791,#6792,#6793,#6794,#6795,#6796,#6797,#6798,
#6799,#6800,#6801,#6802,#6803,#6804,#6805,#6806,#6807,#6808,#6809,#6810,
#6811,#6812,#6813,#6814,#6815,#6816,#6817,#6818,#6819,#6820,#6821,#6822,
#6823,#6824,#6825,#6826,#6827,#6828,#6829,#6830,#6831,#6832,#6833,#6834,
#6835,#6836,#6837,#6838,#6839,#6840,#6841,#6842,#6843,#6844,#6845,#6846,
#6847,#6848,#6849,#6850,#6851,#6852,#6853,#6854,#6855,#6856,#6857,#6858,
#6859,#6860,#6861,#6862,#6863,#6864,#6865,#6866,#6867,#6868,#6869,#6870,
#6871,#6872,#6873,#6874,#6875,#6876,#6877,#6878,#6879,#6880,#6881,#6882,
#6883,#6884,#6885,#6886,#6887,#6888,#6889,#6890,#6891,#6892,#6893,#6894,
#6895,#6896,#6897,#6898,#6899,#6900,#6901),.UNSPECIFIED.,.F.,.F.,(4,3,3,
3,3,3,3,3,3,3,3,3,3,3,3,3,3,3,3,3,3,3,3,3,3,3,3,3,3,3,3,3,3,3,3,3,3,3,3,
3,3,3,3,3,3,3,3,3,3,3,3,3,3,3,3,3,3,3,3,3,3,3,3,3,4),(177.045808834635,
177.144350017315,177.242844566572,177.341323967424,177.439819680818,177.538424273858,
177.637093471072,177.735923162666,177.765194568214,177.864878134227,177.964418482384,
178.064350601658,178.163711306509,178.263039071112,178.362364357231,178.462742127067,
178.562212062314,178.663043749445,178.763875436575,178.863559002587,178.963099350744,
179.063031470018,179.162392174869,179.261719939472,179.361045225591,179.461422995427,
179.560892930674,179.661724617804,179.762556304935,179.862239870948,179.961780219105,
180.061712338379,180.161073043229,180.260400807833,180.359726093952,180.460103863788,
180.559573799035,180.660405486165,180.761237173296,180.860920739309,180.960461087466,
181.06039320674,181.159753911591,181.259081676194,181.358406962314,181.458784732149,
181.558254667397,181.659086354527,181.759918041657,181.85960160767,181.959141955827,
182.059074075101,182.158434779952,182.257762544555,182.357087830674,182.45746560051,
182.556935535757,182.657767222888,182.758598910018,182.860615373313,182.962463753037,
183.064135186073,183.165702513586,183.267179688219,183.328994141815),
 .UNSPECIFIED.);
#732=B_SPLINE_CURVE_WITH_KNOTS('',3,(#6903,#6904,#6905,#6906,#6907,#6908,
#6909,#6910,#6911,#6912),.UNSPECIFIED.,.F.,.F.,(4,1,1,1,1,1,1,4),(183.328999479296,
183.757279778378,184.755960646739,185.7546415151,186.753322383461,187.752003251821,
188.750684120182,189.612179448995),.UNSPECIFIED.);
#733=B_SPLINE_CURVE_WITH_KNOTS('',3,(#6914,#6915,#6916,#6917,#6918,#6919,
#6920,#6921,#6922,#6923,#6924),.UNSPECIFIED.,.F.,.F.,(4,1,1,1,1,1,1,1,4),
(189.612179448995,189.749364988543,190.748045856904,191.746726725264,192.745407593625,
193.744088461986,194.742769330347,195.741450198707,195.895364756174),
 .UNSPECIFIED.);
#734=B_SPLINE_CURVE_WITH_KNOTS('',3,(#6926,#6927,#6928,#6929,#6930,#6931,
#6932,#6933,#6934,#6935),.UNSPECIFIED.,.F.,.F.,(4,1,1,1,1,1,1,4),(195.895364756174,
196.740131067068,197.738811935429,198.73749280379,199.73617367215,200.734854540511,
201.733535408872,202.178550063354),.UNSPECIFIED.);
#735=B_SPLINE_CURVE_WITH_KNOTS('',3,(#6937,#6938,#6939,#6940,#6941,#6942,
#6943,#6944,#6945,#6946),.UNSPECIFIED.,.F.,.F.,(4,1,1,1,1,1,1,4),(202.178550063354,
202.732216277233,203.730897145593,204.729578013954,205.728258882315,206.726939750676,
207.725620619036,208.461735370533),.UNSPECIFIED.);
#736=B_SPLINE_CURVE_WITH_KNOTS('',3,(#6948,#6949,#6950,#6951,#6952,#6953,
#6954,#6955,#6956,#6957,#6958,#6959,#6960,#6961,#6962,#6963,#6964,#6965,
#6966,#6967,#6968,#6969,#6970,#6971,#6972,#6973,#6974,#6975,#6976,#6977,
#6978,#6979,#6980,#6981,#6982,#6983,#6984,#6985,#6986,#6987,#6988,#6989,
#6990,#6991,#6992,#6993,#6994,#6995,#6996,#6997,#6998,#6999,#7000,#7001,
#7002,#7003,#7004,#7005,#7006,#7007,#7008,#7009,#7010,#7011,#7012,#7013,
#7014,#7015,#7016,#7017,#7018,#7019,#7020,#7021,#7022,#7023,#7024,#7025,
#7026,#7027,#7028,#7029,#7030,#7031,#7032,#7033,#7034,#7035,#7036,#7037,
#7038,#7039,#7040,#7041,#7042,#7043,#7044,#7045,#7046,#7047,#7048,#7049,
#7050,#7051,#7052,#7053,#7054,#7055,#7056,#7057,#7058,#7059,#7060,#7061,
#7062,#7063,#7064,#7065,#7066,#7067,#7068,#7069,#7070,#7071,#7072,#7073,
#7074,#7075,#7076,#7077,#7078,#7079,#7080,#7081,#7082,#7083,#7084,#7085,
#7086,#7087,#7088,#7089,#7090,#7091,#7092,#7093,#7094,#7095,#7096,#7097,
#7098,#7099,#7100,#7101,#7102,#7103,#7104,#7105,#7106,#7107,#7108,#7109,
#7110,#7111,#7112,#7113,#7114,#7115,#7116,#7117,#7118,#7119,#7120,#7121,
#7122,#7123,#7124,#7125,#7126,#7127,#7128,#7129,#7130,#7131,#7132,#7133,
#7134,#7135,#7136,#7137),.UNSPECIFIED.,.F.,.F.,(4,3,3,3,3,3,3,3,3,3,3,3,
3,3,3,3,3,3,3,3,3,3,3,3,3,3,3,3,3,3,3,3,3,3,3,3,3,3,3,3,3,3,3,3,3,3,3,3,
3,3,3,3,3,3,3,3,3,3,3,3,3,3,3,4),(208.461735551838,208.593018519617,208.724301487397,
208.823985053394,208.923525401536,209.023457520813,209.122818225649,209.222145990237,
209.321471276341,209.421849046195,209.521318981428,209.622150668593,209.722982355758,
209.822665921751,209.922206269888,210.022138389167,210.121499093997,210.22082685858,
210.320152144678,210.420529914538,210.519999849765,210.620831536942,210.721663224119,
210.821346790229,210.920887138484,211.020819257734,211.120179962682,211.219507727383,
211.318833013599,211.419210783319,211.518680718661,211.61951240557,211.720344092479,
211.820027658363,211.919568006391,212.019500125697,212.118860830421,212.218188594898,
212.317513880893,212.417891650879,212.517361586006,212.618193273423,212.71902496084,
212.818708526764,212.91824887483,213.018180994127,213.117541698884,213.216869463392,
213.316194749415,213.416572519362,213.516042454512,213.616874141857,213.717705829201,
213.817389395867,213.916929744679,214.01686186379,214.116222569296,214.215550334553,
214.314875621323,214.415253390383,214.514723326269,214.615555011916,214.716386697562,
214.744920677713),.UNSPECIFIED.);
#737=B_SPLINE_CURVE_WITH_KNOTS('',3,(#7139,#7140,#7141,#7142,#7143,#7144,
#7145,#7146,#7147,#7148,#7149,#7150,#7151,#7152,#7153,#7154,#7155,#7156,
#7157,#7158,#7159,#7160,#7161,#7162,#7163,#7164,#7165,#7166,#7167,#7168,
#7169,#7170,#7171,#7172,#7173,#7174,#7175,#7176,#7177,#7178,#7179,#7180,
#7181,#7182,#7183,#7184,#7185,#7186,#7187,#7188,#7189,#7190,#7191,#7192,
#7193,#7194,#7195,#7196,#7197,#7198,#7199,#7200,#7201,#7202,#7203,#7204,
#7205,#7206,#7207,#7208,#7209,#7210,#7211,#7212,#7213,#7214,#7215,#7216,
#7217,#7218,#7219,#7220,#7221,#7222,#7223,#7224,#7225,#7226,#7227,#7228,
#7229,#7230,#7231,#7232,#7233,#7234,#7235,#7236,#7237,#7238,#7239,#7240,
#7241,#7242,#7243,#7244,#7245,#7246,#7247,#7248,#7249,#7250,#7251,#7252,
#7253,#7254,#7255,#7256,#7257,#7258,#7259,#7260,#7261,#7262,#7263,#7264,
#7265,#7266,#7267,#7268,#7269,#7270,#7271,#7272,#7273,#7274,#7275,#7276,
#7277,#7278,#7279,#7280,#7281,#7282,#7283,#7284,#7285,#7286,#7287,#7288,
#7289,#7290,#7291,#7292,#7293,#7294,#7295,#7296,#7297,#7298,#7299,#7300,
#7301,#7302,#7303,#7304,#7305,#7306,#7307,#7308,#7309,#7310,#7311,#7312,
#7313,#7314,#7315,#7316,#7317,#7318,#7319,#7320,#7321,#7322,#7323,#7324,
#7325,#7326,#7327,#7328),.UNSPECIFIED.,.F.,.F.,(4,3,3,3,3,3,3,3,3,3,3,3,
3,3,3,3,3,3,3,3,3,3,3,3,3,3,3,3,3,3,3,3,3,3,3,3,3,3,3,3,3,3,3,3,3,3,3,3,
3,3,3,3,3,3,3,3,3,3,3,3,3,3,3,4),(214.744920678121,214.844128676269,214.943195171378,
215.042149305934,215.141042635403,215.239906261421,215.338771247639,215.437735542156,
215.536750313415,215.635939296236,215.715067565922,215.814751131676,215.914291479564,
216.014223598904,216.11358430346,216.21291206776,216.312237353568,216.412615123747,
216.512085058666,216.612916746474,216.713748434283,216.813432004555,216.912972356988,
217.012904475195,217.112265184329,217.211592953209,217.310918243593,217.411296008356,
217.510765947794,217.611597625219,217.712429302644,217.812112860803,217.911653201114,
218.011585322351,218.110946019429,218.210273776305,218.309599054752,218.409976833815,
218.509446761601,218.610278466303,218.711110171005,218.810793737748,218.910334086561,
219.010266205662,219.109626910987,219.208954675997,219.308279962453,219.408657731681,
219.508127667096,219.60895935323,219.709791039365,219.809474632422,219.909015007748,
220.008947120245,220.108307852369,220.207635644225,220.306960957539,220.407338695086,
220.506808657111,220.607640282419,220.708471907726,220.827206194457,220.944620333216,
221.028105769477),.UNSPECIFIED.);
#738=B_SPLINE_CURVE_WITH_KNOTS('',3,(#7330,#7331,#7332,#7333,#7334,#7335,
#7336,#7337,#7338,#7339),.UNSPECIFIED.,.F.,.F.,(4,1,1,1,1,1,1,4),(221.028105984892,
221.707152776087,222.705833644448,223.704514512808,224.703195381169,225.70187624953,
226.700557117891,227.311291292072),.UNSPECIFIED.);
#739=B_SPLINE_CURVE_WITH_KNOTS('',3,(#7341,#7342,#7343,#7344,#7345,#7346,
#7347,#7348,#7349,#7350),.UNSPECIFIED.,.F.,.F.,(4,1,1,1,1,1,1,4),(227.311291292072,
227.699237986251,228.697918854612,229.696599722973,230.695280591334,231.693961459694,
232.692642328055,233.594476599252),.UNSPECIFIED.);
#740=B_SPLINE_CURVE_WITH_KNOTS('',3,(#7352,#7353,#7354,#7355,#7356,#7357),
 .UNSPECIFIED.,.F.,.F.,(4,1,1,4),(233.594476599252,233.691323196416,234.690004064777,
235.619089830444),.UNSPECIFIED.);
#741=B_SPLINE_CURVE_WITH_KNOTS('',3,(#7361,#7362,#7363,#7364,#7365,#7366,
#7367,#7368,#7369,#7370,#7371,#7372,#7373,#7374,#7375,#7376,#7377,#7378,
#7379,#7380,#7381,#7382,#7383,#7384,#7385,#7386,#7387,#7388,#7389,#7390,
#7391,#7392,#7393,#7394),.UNSPECIFIED.,.F.,.F.,(4,3,3,3,3,3,3,3,3,3,3,4),
(-237.686046669859,-237.58402334176,-237.482061745961,-237.380110302383,
-237.27816118961,-237.176189769977,-237.074171387682,-236.972000880612,
-236.869752054663,-236.767301150916,-236.687365801498,-236.569426436252),
 .UNSPECIFIED.);
#742=B_SPLINE_CURVE_WITH_KNOTS('',3,(#7396,#7397,#7398,#7399,#7400,#7401,
#7402,#7403,#7404,#7405,#7406,#7407,#7408,#7409,#7410,#7411,#7412,#7413,
#7414,#7415,#7416,#7417,#7418,#7419,#7420,#7421,#7422,#7423,#7424,#7425,
#7426,#7427,#7428,#7429,#7430,#7431,#7432,#7433,#7434,#7435,#7436,#7437,
#7438,#7439,#7440,#7441,#7442,#7443,#7444,#7445,#7446,#7447,#7448,#7449,
#7450,#7451,#7452,#7453,#7454,#7455,#7456,#7457,#7458,#7459,#7460,#7461,
#7462,#7463,#7464,#7465,#7466,#7467,#7468,#7469,#7470,#7471,#7472,#7473,
#7474,#7475,#7476,#7477,#7478,#7479,#7480,#7481,#7482,#7483,#7484,#7485,
#7486,#7487,#7488,#7489,#7490,#7491,#7492,#7493,#7494,#7495,#7496,#7497,
#7498,#7499,#7500,#7501,#7502,#7503,#7504,#7505,#7506,#7507,#7508,#7509,
#7510,#7511,#7512,#7513,#7514,#7515,#7516,#7517,#7518,#7519,#7520,#7521,
#7522,#7523,#7524,#7525,#7526,#7527,#7528,#7529,#7530,#7531,#7532,#7533,
#7534,#7535,#7536,#7537,#7538,#7539,#7540,#7541,#7542,#7543,#7544,#7545,
#7546,#7547,#7548,#7549,#7550,#7551,#7552,#7553,#7554,#7555,#7556,#7557,
#7558,#7559,#7560,#7561,#7562,#7563,#7564,#7565,#7566,#7567,#7568,#7569,
#7570,#7571,#7572,#7573,#7574,#7575,#7576,#7577,#7578,#7579,#7580,#7581,
#7582,#7583,#7584,#7585),.UNSPECIFIED.,.F.,.F.,(4,3,3,3,3,3,3,3,3,3,3,3,
3,3,3,3,3,3,3,3,3,3,3,3,3,3,3,3,3,3,3,3,3,3,3,3,3,3,3,3,3,3,3,3,3,3,3,3,
3,3,3,3,3,3,3,3,3,3,3,3,3,3,3,4),(-236.569426436046,-236.47210942377,-236.374181362441,
-236.277091450807,-236.180049642806,-236.083023280348,-235.984438693545,
-235.887287588253,-235.787986260695,-235.688684933137,-235.588851429478,
-235.489161004665,-235.389266387179,-235.289756450306,-235.190280123486,
-235.090807160138,-234.990606386298,-234.890992517576,-234.790498291177,
-234.690004064777,-234.590145789274,-234.490427147139,-234.390539153298,
-234.290992751295,-234.191476918733,-234.091961448655,-233.991801885595,
-233.892138511189,-233.791730853802,-233.691323196416,-233.591775013876,
-233.492371933963,-233.392405733225,-233.293185905218,-233.194000068945,
-233.094817577393,-232.994273765058,-232.894947324027,-232.793794826041,
-232.692642328055,-232.592929711517,-232.493360185805,-232.393435345041,
-232.294045373771,-232.194688375603,-232.095333929155,-231.994990811789,
-231.89549219828,-231.794726828987,-231.693961459694,-231.594257060298,
-231.494695422986,-231.39476856903,-231.295385617913,-231.196035295539,
-231.09668716973,-230.996335525131,-230.896842286067,-230.796061438701,
-230.695280591334,-230.585288532613,-230.475619265595,-230.366499298658,
-230.286241549226),.UNSPECIFIED.);
#743=B_SPLINE_CURVE_WITH_KNOTS('',3,(#7587,#7588,#7589,#7590,#7591,#7592,
#7593,#7594,#7595,#7596),.UNSPECIFIED.,.F.,.F.,(4,1,1,1,1,1,1,4),(-230.286241129072,
-229.696599722973,-228.697918854612,-227.699237986251,-226.700557117891,
-225.70187624953,-224.703195381169,-224.003055821893),.UNSPECIFIED.);
#744=B_SPLINE_CURVE_WITH_KNOTS('',3,(#7598,#7599,#7600,#7601,#7602,#7603,
#7604,#7605,#7606,#7607,#7608,#7609,#7610,#7611,#7612,#7613,#7614,#7615,
#7616,#7617,#7618,#7619,#7620,#7621,#7622,#7623,#7624,#7625,#7626,#7627,
#7628,#7629,#7630,#7631,#7632,#7633,#7634,#7635,#7636,#7637,#7638,#7639,
#7640,#7641,#7642,#7643,#7644,#7645,#7646,#7647,#7648,#7649,#7650,#7651,
#7652,#7653,#7654,#7655,#7656,#7657,#7658,#7659,#7660,#7661,#7662,#7663,
#7664,#7665,#7666,#7667,#7668,#7669,#7670,#7671,#7672,#7673,#7674,#7675,
#7676,#7677,#7678,#7679,#7680,#7681,#7682,#7683,#7684,#7685,#7686,#7687,
#7688,#7689,#7690,#7691,#7692,#7693,#7694,#7695,#7696,#7697,#7698,#7699,
#7700,#7701,#7702,#7703,#7704,#7705,#7706,#7707,#7708,#7709,#7710,#7711,
#7712,#7713,#7714,#7715,#7716,#7717,#7718,#7719,#7720,#7721,#7722,#7723,
#7724,#7725,#7726,#7727,#7728,#7729,#7730,#7731,#7732,#7733,#7734,#7735,
#7736,#7737,#7738,#7739,#7740,#7741,#7742,#7743,#7744,#7745,#7746,#7747,
#7748,#7749,#7750,#7751,#7752,#7753,#7754,#7755,#7756,#7757,#7758,#7759,
#7760,#7761,#7762,#7763,#7764,#7765,#7766,#7767,#7768,#7769,#7770,#7771,
#7772,#7773,#7774,#7775,#7776,#7777,#7778,#7779,#7780,#7781,#7782,#7783,
#7784,#7785,#7786,#7787),.UNSPECIFIED.,.F.,.F.,(4,3,3,3,3,3,3,3,3,3,3,3,
3,3,3,3,3,3,3,3,3,3,3,3,3,3,3,3,3,3,3,3,3,3,3,3,3,3,3,3,3,3,3,3,3,3,3,3,
3,3,3,3,3,3,3,3,3,3,3,3,3,3,3,4),(-224.003055642521,-223.88325798579,-223.761769132628,
-223.704514512808,-223.604830784056,-223.505290271404,-223.405358193035,
-223.30599732063,-223.206669387694,-223.107343932691,-223.00696636063,-222.907496256868,
-222.806664950658,-222.705833644448,-222.606150061763,-222.506609696167,
-222.406677581157,-222.307316857118,-222.207989072708,-222.108663766188,
-222.008286018663,-221.908816061752,-221.807984418919,-221.707152776087,
-221.607469264316,-221.507928971319,-221.40799683837,-221.308636190515,
-221.209308483473,-221.109983255403,-221.009605418484,-220.910135541903,
-220.809303724815,-220.708471907726,-220.608788315492,-220.509247940804,
-220.409315828124,-220.309955096181,-220.210627304334,-220.111301990857,
-220.010924252984,-219.911454290377,-219.810622664871,-219.709791039365,
-219.610107473322,-219.510567125058,-219.410635005801,-219.311274300658,
-219.211946535692,-219.11262124914,-219.012243479606,-218.912773543759,
-218.811941857382,-218.711110171005,-218.611558273906,-218.512149497141,
-218.412856080209,-218.313625803522,-218.214427986811,-218.115231989806,
-218.015937831542,-217.916596853038,-217.817075105393,-217.719870514713),
 .UNSPECIFIED.);
#745=B_SPLINE_CURVE_WITH_KNOTS('',3,(#7789,#7790,#7791,#7792,#7793,#7794,
#7795,#7796,#7797,#7798,#7799,#7800),.UNSPECIFIED.,.F.,.F.,(4,2,1,1,1,1,
1,1,4),(-217.719870514713,-217.712429302644,-216.713748434283,-215.715067565922,
-214.716386697562,-213.717705829201,-212.71902496084,-211.720344092479,
-211.436689775384),.UNSPECIFIED.);
#746=B_SPLINE_CURVE_WITH_KNOTS('',3,(#7802,#7803,#7804,#7805,#7806,#7807,
#7808,#7809,#7810,#7811,#7812,#7813,#7814,#7815,#7816,#7817,#7818,#7819,
#7820,#7821,#7822,#7823,#7824,#7825,#7826,#7827,#7828,#7829,#7830,#7831,
#7832,#7833,#7834,#7835,#7836,#7837,#7838,#7839,#7840,#7841,#7842,#7843,
#7844,#7845,#7846,#7847,#7848,#7849,#7850,#7851,#7852,#7853,#7854,#7855,
#7856,#7857,#7858,#7859,#7860,#7861,#7862,#7863,#7864,#7865,#7866,#7867,
#7868,#7869,#7870,#7871,#7872,#7873,#7874,#7875,#7876,#7877,#7878,#7879,
#7880,#7881,#7882,#7883,#7884,#7885,#7886,#7887,#7888,#7889,#7890,#7891,
#7892,#7893,#7894,#7895,#7896,#7897,#7898,#7899,#7900,#7901,#7902,#7903,
#7904,#7905,#7906,#7907,#7908,#7909,#7910,#7911,#7912,#7913,#7914,#7915,
#7916,#7917,#7918,#7919,#7920,#7921,#7922,#7923,#7924,#7925,#7926,#7927,
#7928,#7929,#7930,#7931,#7932,#7933,#7934,#7935,#7936,#7937,#7938,#7939,
#7940,#7941,#7942,#7943,#7944,#7945,#7946,#7947,#7948,#7949,#7950,#7951,
#7952,#7953,#7954,#7955,#7956,#7957,#7958,#7959,#7960,#7961,#7962,#7963,
#7964,#7965,#7966,#7967,#7968,#7969,#7970,#7971,#7972,#7973,#7974,#7975,
#7976,#7977,#7978,#7979,#7980,#7981,#7982,#7983,#7984,#7985,#7986,#7987,
#7988,#7989,#7990,#7991,#7992,#7993,#7994),.UNSPECIFIED.,.F.,.F.,(4,3,3,
3,3,3,3,3,3,3,3,3,3,3,3,3,3,3,3,3,3,3,3,3,3,3,3,3,3,3,3,3,3,3,3,3,3,3,3,
3,3,3,3,3,3,3,3,3,3,3,3,3,3,3,3,3,3,3,3,3,3,3,3,3,4),(-211.436685207534,
-211.338097456741,-211.239554137195,-211.141023824873,-211.042475117638,
-210.943815967523,-210.845090459821,-210.746205349484,-210.721663224119,
-210.621979658127,-210.522439309991,-210.422507190712,-210.323146485882,
-210.223818721299,-210.124493435201,-210.02411566534,-209.924645730114,
-209.823814042936,-209.722982355758,-209.623298789759,-209.523758441616,
-209.423826322339,-209.324465617503,-209.225137852914,-209.12581256681,
-209.025434796957,-208.925964861725,-208.825133174561,-208.724301487397,
-208.624617921371,-208.5250775732,-208.425145453929,-208.325784749064,-208.226456984446,
-208.127131698313,-208.026753928494,-207.927283993232,-207.826452306134,
-207.725620619036,-207.625937053027,-207.526396704874,-207.426464585599,
-207.327103880753,-207.227776116154,-207.128450830039,-207.028073060198,
-206.928603124955,-206.827771437816,-206.726939750676,-206.627256184665,
-206.527715836509,-206.427783717235,-206.328423012386,-206.229095247784,
-206.129769961667,-206.029392191829,-205.929922256584,-205.829090569449,
-205.728258882315,-205.626382795805,-205.524672889404,-205.423136082282,
-205.32170108951,-205.220351211035,-205.153499900354),.UNSPECIFIED.);
#747=B_SPLINE_CURVE_WITH_KNOTS('',3,(#7996,#7997,#7998,#7999,#8000,#8001,
#8002,#8003,#8004,#8005),.UNSPECIFIED.,.F.,.F.,(4,1,1,1,1,1,1,4),(-205.153494314817,
-204.729578013954,-203.730897145593,-202.732216277232,-201.733535408872,
-200.734854540511,-199.73617367215,-198.870314593174),.UNSPECIFIED.);
#748=B_SPLINE_CURVE_WITH_KNOTS('',3,(#8007,#8008,#8009,#8010,#8011,#8012,
#8013,#8014,#8015,#8016,#8017),.UNSPECIFIED.,.F.,.F.,(4,1,1,1,1,1,1,1,4),
(-198.870314593174,-198.737492803789,-197.738811935429,-196.740131067068,
-195.741450198707,-194.742769330346,-193.744088461986,-192.745407593625,
-192.587129285995),.UNSPECIFIED.);
#749=B_SPLINE_CURVE_WITH_KNOTS('',3,(#8019,#8020,#8021,#8022,#8023,#8024,
#8025,#8026,#8027,#8028),.UNSPECIFIED.,.F.,.F.,(4,1,1,1,1,1,1,4),(-192.587129285995,
-191.746726725264,-190.748045856903,-189.749364988543,-188.750684120182,
-187.752003251821,-186.75332238346,-186.303943978815),.UNSPECIFIED.);
#750=B_SPLINE_CURVE_WITH_KNOTS('',3,(#8030,#8031,#8032,#8033,#8034,#8035,
#8036,#8037,#8038,#8039),.UNSPECIFIED.,.F.,.F.,(4,1,1,1,1,1,1,4),(-186.303943978815,
-185.7546415151,-184.755960646739,-183.757279778378,-182.758598910017,-181.759918041657,
-180.761237173296,-180.020758671636),.UNSPECIFIED.);
#751=B_SPLINE_CURVE_WITH_KNOTS('',3,(#8041,#8042,#8043,#8044,#8045,#8046,
#8047,#8048,#8049,#8050,#8051,#8052,#8053,#8054,#8055,#8056,#8057,#8058,
#8059,#8060,#8061,#8062,#8063,#8064,#8065,#8066,#8067,#8068,#8069,#8070,
#8071,#8072,#8073,#8074,#8075,#8076,#8077,#8078,#8079,#8080,#8081,#8082,
#8083,#8084,#8085,#8086,#8087,#8088,#8089,#8090,#8091,#8092,#8093,#8094,
#8095,#8096,#8097,#8098,#8099,#8100,#8101,#8102,#8103,#8104,#8105,#8106,
#8107,#8108,#8109,#8110,#8111,#8112,#8113,#8114,#8115,#8116,#8117,#8118,
#8119,#8120,#8121,#8122,#8123,#8124,#8125,#8126,#8127,#8128,#8129,#8130,
#8131,#8132,#8133,#8134,#8135,#8136,#8137,#8138,#8139,#8140,#8141,#8142,
#8143,#8144,#8145,#8146,#8147,#8148,#8149,#8150,#8151,#8152,#8153,#8154,
#8155,#8156,#8157,#8158,#8159,#8160,#8161,#8162,#8163,#8164,#8165,#8166,
#8167,#8168,#8169,#8170,#8171,#8172,#8173,#8174,#8175,#8176,#8177,#8178,
#8179,#8180,#8181,#8182,#8183,#8184,#8185,#8186,#8187,#8188,#8189,#8190,
#8191,#8192,#8193,#8194,#8195,#8196,#8197,#8198,#8199,#8200,#8201,#8202,
#8203,#8204,#8205,#8206,#8207,#8208,#8209,#8210,#8211,#8212,#8213,#8214,
#8215,#8216,#8217,#8218,#8219,#8220,#8221,#8222,#8223,#8224,#8225,#8226,
#8227,#8228,#8229,#8230),.UNSPECIFIED.,.F.,.F.,(4,3,3,3,3,3,3,3,3,3,3,3,
3,3,3,3,3,3,3,3,3,3,3,3,3,3,3,3,3,3,3,3,3,3,3,3,3,3,3,3,3,3,3,3,3,3,3,3,
3,3,3,3,3,3,3,3,3,3,3,3,3,3,3,4),(-180.020758515293,-179.891657410114,-179.762556304935,
-179.662872738923,-179.563332390766,-179.463400271492,-179.364039566642,
-179.264711802039,-179.16538651592,-179.065008746084,-178.965538810837,
-178.864707123705,-178.763875436574,-178.664191870561,-178.564651522405,
-178.464719403131,-178.36535869828,-178.266030933677,-178.166705647558,
-178.066327877722,-177.966857942475,-177.866026255345,-177.765194568214,
-177.665511002201,-177.565970654044,-177.46603853477,-177.366677829919,
-177.267350065316,-177.168024779197,-177.067647009361,-176.968177074114,
-176.867345386983,-176.766513699853,-176.66683013384,-176.567289785683,
-176.467357666409,-176.367996961558,-176.268669196955,-176.169343910836,
-176.068966141,-175.969496205752,-175.868664518622,-175.767832831492,-175.668149265479,
-175.568608917322,-175.468676798048,-175.369316093197,-175.269988328594,
-175.170663042475,-175.070285272639,-174.970815337392,-174.869983650261,
-174.769151963131,-174.669468397118,-174.569928048962,-174.469995929688,
-174.370635224837,-174.271307460234,-174.171982174115,-174.071604404279,
-173.972134469032,-173.871302781902,-173.770471094771,-173.737573364456),
 .UNSPECIFIED.);
#752=B_SPLINE_CURVE_WITH_KNOTS('',3,(#8232,#8233,#8234,#8235,#8236,#8237,
#8238,#8239,#8240,#8241),.UNSPECIFIED.,.F.,.F.,(4,1,1,1,1,1,1,4),(-173.737568886119,
-172.77179022641,-171.773109358049,-170.774428489688,-169.775747621328,
-168.777066752967,-167.778385884606,-167.454394954544),.UNSPECIFIED.);
#753=B_SPLINE_CURVE_WITH_KNOTS('',3,(#8243,#8244,#8245,#8246,#8247,#8248,
#8249,#8250,#8251,#8252,#8253,#8254,#8255,#8256,#8257,#8258,#8259,#8260,
#8261,#8262,#8263,#8264,#8265,#8266,#8267,#8268,#8269,#8270,#8271,#8272,
#8273,#8274,#8275,#8276,#8277,#8278,#8279,#8280,#8281,#8282,#8283,#8284,
#8285,#8286,#8287,#8288,#8289,#8290,#8291,#8292,#8293,#8294,#8295,#8296,
#8297,#8298,#8299,#8300,#8301,#8302,#8303,#8304,#8305,#8306,#8307,#8308,
#8309,#8310,#8311,#8312,#8313,#8314,#8315,#8316,#8317,#8318,#8319,#8320,
#8321,#8322,#8323,#8324,#8325,#8326,#8327,#8328,#8329,#8330,#8331,#8332,
#8333,#8334,#8335,#8336,#8337,#8338,#8339,#8340,#8341,#8342,#8343,#8344,
#8345,#8346,#8347,#8348,#8349,#8350,#8351,#8352,#8353,#8354,#8355,#8356,
#8357,#8358,#8359,#8360,#8361,#8362,#8363,#8364,#8365,#8366,#8367,#8368,
#8369,#8370,#8371,#8372,#8373,#8374,#8375,#8376,#8377,#8378,#8379,#8380,
#8381,#8382,#8383,#8384,#8385,#8386,#8387,#8388,#8389,#8390,#8391,#8392,
#8393,#8394,#8395,#8396,#8397,#8398,#8399,#8400,#8401,#8402,#8403,#8404,
#8405,#8406,#8407,#8408,#8409,#8410,#8411,#8412,#8413,#8414,#8415,#8416,
#8417,#8418,#8419,#8420,#8421,#8422,#8423,#8424,#8425,#8426,#8427,#8428,
#8429,#8430,#8431,#8432),.UNSPECIFIED.,.F.,.F.,(4,3,3,3,3,3,3,3,3,3,3,3,
3,3,3,3,3,3,3,3,3,3,3,3,3,3,3,3,3,3,3,3,3,3,3,3,3,3,3,3,3,3,3,3,3,3,3,3,
3,3,3,3,3,3,3,3,3,3,3,3,3,3,3,4),(-167.454388057277,-167.355266653173,-167.256167295289,
-167.157059319171,-167.057841966077,-166.958568556428,-166.859113028564,
-166.779705016245,-166.680021450233,-166.580481102076,-166.480548982802,
-166.381188277952,-166.281860513349,-166.18253522723,-166.082157457394,
-165.982687522147,-165.881855835016,-165.781024147885,-165.681340581872,
-165.581800233715,-165.481868114441,-165.382507409591,-165.283179644987,
-165.183854358868,-165.083476589032,-164.984006653785,-164.883174966655,
-164.782343279524,-164.682659713511,-164.583119365354,-164.48318724608,
-164.383826541229,-164.284498776625,-164.185173490506,-164.08479572067,
-163.985325785423,-163.884494098293,-163.783662411163,-163.68397884515,
-163.584438496993,-163.484506377719,-163.385145672868,-163.285817908265,
-163.186492622146,-163.08611485231,-162.986644917063,-162.885813229932,
-162.784981542802,-162.685297976789,-162.585757628632,-162.485825509358,
-162.386464804508,-162.287137039905,-162.187811753786,-162.08743398395,
-161.987964048704,-161.887132361573,-161.786300674442,-161.685575317288,
-161.585001767063,-161.481552012821,-161.381207694737,-161.276205222417,
-161.171202750097),.UNSPECIFIED.);
#754=B_SPLINE_CURVE_WITH_KNOTS('',3,(#8434,#8435,#8436,#8437,#8438,#8439,
#8440,#8441,#8442,#8443),.UNSPECIFIED.,.F.,.F.,(4,1,1,1,1,1,1,4),(-161.171195349684,
-160.787619806081,-159.78893893772,-158.790258069359,-157.791577200999,
-156.792896332638,-155.794215464277,-154.888026240588),.UNSPECIFIED.);
#755=B_SPLINE_CURVE_WITH_KNOTS('',3,(#8445,#8446,#8447,#8448,#8449,#8450,
#8451,#8452,#8453,#8454,#8455,#8456,#8457,#8458,#8459,#8460,#8461,#8462,
#8463,#8464,#8465,#8466,#8467,#8468,#8469,#8470,#8471,#8472,#8473,#8474,
#8475,#8476,#8477,#8478,#8479,#8480,#8481,#8482,#8483,#8484,#8485,#8486,
#8487,#8488,#8489,#8490,#8491,#8492,#8493,#8494,#8495,#8496,#8497,#8498,
#8499,#8500,#8501,#8502,#8503,#8504,#8505,#8506,#8507,#8508,#8509,#8510,
#8511,#8512,#8513,#8514,#8515,#8516,#8517,#8518,#8519,#8520,#8521,#8522,
#8523,#8524,#8525,#8526,#8527,#8528,#8529,#8530,#8531,#8532,#8533,#8534,
#8535,#8536,#8537,#8538,#8539,#8540,#8541,#8542,#8543,#8544,#8545,#8546,
#8547,#8548,#8549,#8550,#8551,#8552,#8553,#8554,#8555,#8556,#8557,#8558,
#8559,#8560,#8561,#8562,#8563,#8564,#8565,#8566,#8567,#8568,#8569,#8570,
#8571,#8572,#8573,#8574,#8575,#8576,#8577,#8578,#8579,#8580,#8581,#8582,
#8583,#8584,#8585,#8586,#8587,#8588,#8589,#8590,#8591,#8592,#8593,#8594,
#8595,#8596,#8597,#8598,#8599,#8600,#8601,#8602,#8603,#8604,#8605,#8606,
#8607,#8608,#8609,#8610,#8611,#8612,#8613,#8614,#8615,#8616,#8617,#8618,
#8619,#8620,#8621,#8622,#8623,#8624,#8625,#8626,#8627,#8628,#8629,#8630,
#8631,#8632,#8633,#8634),.UNSPECIFIED.,.F.,.F.,(4,3,3,3,3,3,3,3,3,3,3,3,
3,3,3,3,3,3,3,3,3,3,3,3,3,3,3,3,3,3,3,3,3,3,3,3,3,3,3,3,3,3,3,3,3,3,3,3,
3,3,3,3,3,3,3,3,3,3,3,3,3,3,3,4),(-154.888017442918,-154.795534595916,-154.695851029908,
-154.596310681755,-154.49637856248,-154.397017857634,-154.297690093035,
-154.198364806921,-154.09798703708,-153.998517101837,-153.897685414697,
-153.796853727556,-153.697170161542,-153.597629813385,-153.497697694111,
-153.398336989259,-153.299009224655,-153.199683938535,-153.0993061687,-152.999836233452,
-152.899004546324,-152.798172859195,-152.698489293182,-152.598948945024,
-152.49901682575,-152.399656120899,-152.300328356295,-152.201003070175,
-152.10062530034,-152.001155365092,-151.900323677963,-151.799491990834,
-151.699808424822,-151.600268076665,-151.500335957391,-151.400975252541,
-151.301647487938,-151.202322201819,-151.101944431982,-151.002474496736,
-150.901642809604,-150.800811122473,-150.70112755646,-150.601587208303,
-150.501655089029,-150.402294384179,-150.302966619576,-150.203641333457,
-150.103263563621,-150.003793628374,-149.902961941243,-149.802130254113,
-149.7024466881,-149.602906339943,-149.502974220669,-149.403613515819,-149.304285751215,
-149.204960465096,-149.10458269526,-149.005112760013,-148.904281072882,
-148.803449385752,-148.660112359079,-148.604832135738),.UNSPECIFIED.);
#756=B_SPLINE_CURVE_WITH_KNOTS('',3,(#8636,#8637,#8638,#8639,#8640,#8641,
#8642,#8643,#8644,#8645,#8646,#8647,#8648,#8649,#8650,#8651,#8652,#8653,
#8654,#8655,#8656,#8657,#8658,#8659,#8660,#8661,#8662,#8663,#8664,#8665,
#8666,#8667,#8668,#8669,#8670,#8671,#8672,#8673,#8674,#8675,#8676,#8677,
#8678,#8679,#8680,#8681,#8682,#8683,#8684,#8685,#8686,#8687,#8688,#8689,
#8690,#8691,#8692,#8693,#8694,#8695,#8696,#8697,#8698,#8699,#8700,#8701,
#8702,#8703,#8704,#8705,#8706,#8707,#8708,#8709,#8710,#8711,#8712,#8713,
#8714,#8715,#8716,#8717,#8718,#8719,#8720,#8721,#8722,#8723,#8724,#8725,
#8726,#8727,#8728,#8729,#8730,#8731,#8732,#8733,#8734,#8735,#8736,#8737,
#8738,#8739,#8740,#8741,#8742,#8743,#8744,#8745,#8746,#8747,#8748,#8749,
#8750,#8751,#8752,#8753,#8754,#8755,#8756,#8757,#8758,#8759,#8760,#8761,
#8762,#8763,#8764,#8765,#8766,#8767,#8768,#8769,#8770,#8771,#8772,#8773,
#8774,#8775,#8776,#8777,#8778,#8779,#8780,#8781,#8782,#8783,#8784,#8785,
#8786,#8787,#8788,#8789,#8790,#8791,#8792,#8793,#8794,#8795,#8796,#8797,
#8798,#8799,#8800,#8801,#8802,#8803,#8804,#8805,#8806,#8807,#8808,#8809,
#8810,#8811,#8812,#8813,#8814,#8815,#8816,#8817,#8818,#8819,#8820,#8821,
#8822,#8823,#8824,#8825,#8826,#8827,#8828),.UNSPECIFIED.,.F.,.F.,(4,3,3,
3,3,3,3,3,3,3,3,3,3,3,3,3,3,3,3,3,3,3,3,3,3,3,3,3,3,3,3,3,3,3,3,3,3,3,3,
3,3,3,3,3,3,3,3,3,3,3,3,3,3,3,3,3,3,3,3,3,3,3,3,3,4),(-148.604832135393,
-148.504824183143,-148.406857804993,-148.308940024735,-148.211038772092,
-148.109471208417,-148.011447515633,-147.913357694361,-147.815116756516,
-147.804768517391,-147.705084951378,-147.605544603221,-147.505612483947,
-147.406251779096,-147.306924014493,-147.207598728373,-147.107220958538,
-147.00775102329,-146.90691933616,-146.80608764903,-146.706404083018,-146.606863734861,
-146.506931615587,-146.407570910736,-146.308243146133,-146.208917860014,
-146.108540090178,-146.009070154931,-145.908238467801,-145.80740678067,
-145.707723214657,-145.6081828665,-145.508250747226,-145.408890042376,-145.309562277772,
-145.210236991653,-145.109859221817,-145.01038928657,-144.90955759944,-144.808725912309,
-144.709042346296,-144.609501998139,-144.509569878865,-144.410209174014,
-144.310881409411,-144.211556123291,-144.111178353456,-144.011708418208,
-143.910876731078,-143.810045043948,-143.710361477935,-143.610821129778,
-143.510889010504,-143.411528305654,-143.31220054105,-143.212875254932,
-143.112497485096,-143.013027549848,-142.912195862718,-142.811364175587,
-142.70609042818,-142.601127558756,-142.496352275949,-142.391824202702,
-142.321646828766),.UNSPECIFIED.);
#757=B_SPLINE_CURVE_WITH_KNOTS('',3,(#8830,#8831,#8832,#8833,#8834,#8835,
#8836,#8837,#8838,#8839,#8840,#8841,#8842,#8843,#8844,#8845,#8846,#8847,
#8848,#8849,#8850,#8851,#8852,#8853,#8854,#8855,#8856,#8857,#8858,#8859,
#8860,#8861,#8862,#8863,#8864,#8865,#8866,#8867,#8868,#8869,#8870,#8871,
#8872,#8873,#8874,#8875,#8876,#8877,#8878,#8879,#8880,#8881,#8882,#8883,
#8884,#8885,#8886,#8887,#8888,#8889,#8890,#8891,#8892,#8893,#8894,#8895,
#8896,#8897,#8898,#8899,#8900,#8901,#8902,#8903,#8904,#8905,#8906,#8907,
#8908,#8909,#8910,#8911,#8912,#8913,#8914,#8915,#8916,#8917,#8918,#8919,
#8920,#8921,#8922,#8923,#8924,#8925,#8926,#8927,#8928,#8929,#8930,#8931,
#8932,#8933,#8934,#8935,#8936,#8937,#8938,#8939,#8940,#8941,#8942,#8943,
#8944,#8945,#8946,#8947,#8948,#8949,#8950,#8951,#8952,#8953,#8954,#8955,
#8956,#8957,#8958,#8959,#8960,#8961,#8962,#8963,#8964,#8965,#8966,#8967,
#8968,#8969,#8970,#8971,#8972,#8973,#8974,#8975,#8976,#8977,#8978,#8979,
#8980,#8981,#8982,#8983,#8984,#8985,#8986,#8987,#8988,#8989,#8990,#8991,
#8992,#8993,#8994,#8995,#8996,#8997,#8998,#8999,#9000,#9001,#9002,#9003,
#9004,#9005,#9006,#9007,#9008,#9009,#9010,#9011,#9012,#9013,#9014,#9015,
#9016,#9017,#9018,#9019),.UNSPECIFIED.,.F.,.F.,(4,3,3,3,3,3,3,3,3,3,3,3,
3,3,3,3,3,3,3,3,3,3,3,3,3,3,3,3,3,3,3,3,3,3,3,3,3,3,3,3,3,3,3,3,3,3,3,3,
3,3,3,3,3,3,3,3,3,3,3,3,3,3,3,4),(-142.321646828558,-142.218012990877,-142.114115387984,
-142.01008454749,-141.905772693495,-141.812683307227,-141.712999741214,
-141.613459393057,-141.513527273783,-141.414166568932,-141.314838804328,
-141.215513518209,-141.115135748373,-141.015665813125,-140.914834125996,
-140.814002438866,-140.714318872853,-140.614778524696,-140.514846405422,
-140.415485700571,-140.316157935968,-140.216832649849,-140.116454880013,
-140.016984944766,-139.916153257635,-139.815321570505,-139.715638004492,
-139.616097656335,-139.516165537061,-139.41680483221,-139.317477067607,
-139.218151781488,-139.117774011652,-139.018304076405,-138.917472389274,
-138.816640702144,-138.716957136131,-138.617416787974,-138.517484668701,
-138.41812396385,-138.318796199247,-138.219470913128,-138.119093143292,
-138.019623208045,-137.918791520915,-137.817959833784,-137.718276267771,
-137.618735919614,-137.51880380034,-137.419443095489,-137.320115330886,
-137.220790044767,-137.120412274931,-137.020942339684,-136.920110652553,
-136.819278965423,-136.720993989767,-136.622836098362,-136.524773061268,
-136.426772772098,-136.328765941481,-136.230762332266,-136.132657937408,
-136.038461521379),.UNSPECIFIED.);
#758=B_SPLINE_CURVE_WITH_KNOTS('',3,(#9021,#9022,#9023,#9024,#9025,#9026,
#9027,#9028,#9029,#9030,#9031),.UNSPECIFIED.,.F.,.F.,(4,1,1,1,1,1,1,1,4),
(-136.038461521379,-135.820598097062,-134.821917228701,-133.823236360341,
-132.82455549198,-131.825874623619,-130.827193755258,-129.828512886898,
-129.755276214199),.UNSPECIFIED.);
#759=B_SPLINE_CURVE_WITH_KNOTS('',3,(#9033,#9034,#9035,#9036,#9037,#9038,
#9039,#9040,#9041,#9042,#9043,#9044,#9045,#9046,#9047,#9048,#9049,#9050,
#9051,#9052,#9053,#9054,#9055,#9056,#9057,#9058,#9059,#9060,#9061,#9062,
#9063,#9064,#9065,#9066,#9067,#9068,#9069,#9070,#9071,#9072,#9073,#9074,
#9075,#9076,#9077,#9078,#9079,#9080,#9081,#9082,#9083,#9084,#9085,#9086,
#9087,#9088,#9089,#9090,#9091,#9092,#9093,#9094,#9095,#9096,#9097,#9098,
#9099,#9100,#9101,#9102,#9103,#9104,#9105,#9106,#9107,#9108,#9109,#9110,
#9111,#9112,#9113,#9114,#9115,#9116,#9117,#9118,#9119,#9120,#9121,#9122,
#9123,#9124,#9125,#9126,#9127,#9128,#9129,#9130,#9131,#9132,#9133,#9134,
#9135,#9136,#9137,#9138,#9139,#9140,#9141,#9142,#9143,#9144,#9145,#9146,
#9147,#9148,#9149,#9150,#9151,#9152,#9153,#9154,#9155,#9156,#9157,#9158,
#9159,#9160,#9161,#9162,#9163,#9164,#9165,#9166,#9167,#9168,#9169,#9170,
#9171,#9172,#9173,#9174,#9175,#9176,#9177,#9178,#9179,#9180,#9181,#9182,
#9183,#9184,#9185,#9186,#9187,#9188,#9189,#9190,#9191,#9192,#9193,#9194,
#9195,#9196,#9197,#9198,#9199,#9200,#9201,#9202,#9203,#9204,#9205,#9206,
#9207,#9208,#9209,#9210,#9211,#9212,#9213,#9214,#9215,#9216,#9217,#9218,
#9219,#9220,#9221,#9222,#9223,#9224,#9225),.UNSPECIFIED.,.F.,.F.,(4,3,3,
3,3,3,3,3,3,3,3,3,3,3,3,3,3,3,3,3,3,3,3,3,3,3,3,3,3,3,3,3,3,3,3,3,3,3,3,
3,3,3,3,3,3,3,3,3,3,3,3,3,3,3,3,3,3,3,3,3,3,3,3,3,4),(-129.755276214199,
-129.656647030661,-129.553295154146,-129.45490538759,-129.356567260123,
-129.25824908595,-129.159919208572,-129.061485240347,-128.962990381182,
-128.864336282513,-128.829832018537,-128.730148452524,-128.630608104367,
-128.530675985093,-128.431315280243,-128.331987515639,-128.23266222952,
-128.132284459684,-128.032814524437,-127.931982837306,-127.831151150176,
-127.731467584163,-127.631927236006,-127.531995116732,-127.432634411881,
-127.333306647277,-127.233981361158,-127.133603591322,-127.034133656075,
-126.933301968945,-126.832470281815,-126.732786715803,-126.633246367646,
-126.533314248372,-126.433953543522,-126.334625778918,-126.2353004928,-126.134922722964,
-126.035452787717,-125.934621100586,-125.833789413455,-125.734105847442,
-125.634565499285,-125.534633380011,-125.43527267516,-125.335944910557,
-125.236619624438,-125.136241854602,-125.036771919355,-124.935940232224,
-124.835108545094,-124.735424979081,-124.635884630923,-124.53595251165,
-124.436591806799,-124.337264042195,-124.237938756076,-124.13756098624,
-124.038091050993,-123.937259363863,-123.836427676733,-123.722636290486,
-123.609316906763,-123.496796562164,-123.472090907255),.UNSPECIFIED.);
#760=B_SPLINE_CURVE_WITH_KNOTS('',3,(#9227,#9228,#9229,#9230,#9231,#9232,
#9233,#9234,#9235,#9236,#9237,#9238,#9239,#9240,#9241,#9242,#9243,#9244,
#9245,#9246,#9247,#9248,#9249,#9250,#9251,#9252,#9253,#9254,#9255,#9256,
#9257,#9258,#9259,#9260,#9261,#9262,#9263,#9264,#9265,#9266,#9267,#9268,
#9269,#9270,#9271,#9272,#9273,#9274,#9275,#9276,#9277,#9278,#9279,#9280,
#9281,#9282,#9283,#9284,#9285,#9286,#9287,#9288,#9289,#9290,#9291,#9292,
#9293,#9294,#9295,#9296,#9297,#9298,#9299,#9300,#9301,#9302,#9303,#9304,
#9305,#9306,#9307,#9308,#9309,#9310,#9311,#9312,#9313,#9314,#9315,#9316,
#9317,#9318,#9319,#9320,#9321,#9322,#9323,#9324,#9325,#9326,#9327,#9328,
#9329,#9330,#9331,#9332,#9333,#9334,#9335,#9336,#9337,#9338,#9339,#9340,
#9341,#9342,#9343,#9344,#9345,#9346,#9347,#9348,#9349,#9350,#9351,#9352,
#9353,#9354,#9355,#9356,#9357,#9358,#9359,#9360,#9361,#9362,#9363,#9364,
#9365,#9366,#9367,#9368,#9369,#9370,#9371,#9372,#9373,#9374,#9375,#9376,
#9377,#9378,#9379,#9380,#9381,#9382,#9383,#9384,#9385,#9386,#9387,#9388,
#9389,#9390,#9391,#9392,#9393,#9394,#9395,#9396,#9397,#9398,#9399,#9400,
#9401,#9402,#9403,#9404,#9405,#9406,#9407,#9408,#9409,#9410,#9411,#9412,
#9413,#9414,#9415,#9416,#9417,#9418,#9419),.UNSPECIFIED.,.F.,.F.,(4,3,3,
3,3,3,3,3,3,3,3,3,3,3,3,3,3,3,3,3,3,3,3,3,3,3,3,3,3,3,3,3,3,3,3,3,3,3,3,
3,3,3,3,3,3,3,3,3,3,3,3,3,3,3,3,3,3,3,3,3,3,3,3,3,4),(-123.47209090702,
-123.372238927569,-123.272382020996,-123.172490797704,-123.072468036,-122.972368751522,
-122.872092706752,-122.837746808372,-122.73806324236,-122.638522894203,
-122.538590774929,-122.439230070079,-122.339902305476,-122.240577019357,
-122.140199249521,-122.040729314274,-121.939897627143,-121.839065940012,
-121.739382373999,-121.639842025842,-121.539909906568,-121.440549201717,
-121.341221437114,-121.241896150995,-121.141518381159,-121.042048445912,
-120.941216758782,-120.840385071651,-120.740701505638,-120.641161157481,
-120.541229038207,-120.441868333356,-120.342540568752,-120.243215282633,
-120.142837512797,-120.04336757755,-119.94253589042,-119.84170420329,-119.742020637277,
-119.64248028912,-119.542548169846,-119.443187464996,-119.343859700392,
-119.244534414273,-119.144156644437,-119.04468670919,-118.943855022059,
-118.843023334929,-118.743339768917,-118.64379942076,-118.543867301486,
-118.444506596635,-118.345178832032,-118.245853545913,-118.145475776077,
-118.04600584083,-117.9451741537,-117.844342466569,-117.744526295241,-117.644852015344,
-117.545289197132,-117.445806010149,-117.3463701507,-117.246927715914,-117.18890559984),
 .UNSPECIFIED.);
#761=B_SPLINE_CURVE_WITH_KNOTS('',3,(#9421,#9422,#9423,#9424,#9425,#9426,
#9427,#9428,#9429,#9430,#9431,#9432,#9433,#9434,#9435,#9436,#9437,#9438,
#9439,#9440,#9441,#9442,#9443,#9444,#9445,#9446,#9447,#9448,#9449,#9450,
#9451,#9452,#9453,#9454,#9455,#9456,#9457,#9458,#9459,#9460,#9461,#9462,
#9463,#9464,#9465,#9466,#9467,#9468,#9469,#9470,#9471,#9472,#9473,#9474,
#9475,#9476,#9477,#9478,#9479,#9480,#9481,#9482,#9483,#9484,#9485,#9486,
#9487,#9488,#9489,#9490,#9491,#9492,#9493,#9494,#9495,#9496,#9497,#9498,
#9499,#9500,#9501,#9502,#9503,#9504,#9505,#9506,#9507,#9508,#9509,#9510,
#9511,#9512,#9513,#9514,#9515,#9516,#9517,#9518,#9519,#9520,#9521,#9522,
#9523,#9524,#9525,#9526,#9527,#9528,#9529,#9530,#9531,#9532,#9533,#9534,
#9535,#9536,#9537,#9538,#9539,#9540,#9541,#9542,#9543,#9544,#9545,#9546,
#9547,#9548,#9549,#9550,#9551,#9552,#9553,#9554,#9555,#9556,#9557,#9558,
#9559,#9560,#9561,#9562,#9563,#9564,#9565,#9566,#9567,#9568,#9569,#9570,
#9571,#9572,#9573,#9574,#9575,#9576,#9577,#9578,#9579,#9580,#9581,#9582,
#9583,#9584,#9585,#9586,#9587,#9588,#9589,#9590,#9591,#9592,#9593,#9594,
#9595,#9596,#9597,#9598,#9599,#9600,#9601,#9602,#9603,#9604,#9605,#9606,
#9607,#9608,#9609,#9610),.UNSPECIFIED.,.F.,.F.,(4,3,3,3,3,3,3,3,3,3,3,3,
3,3,3,3,3,3,3,3,3,3,3,3,3,3,3,3,3,3,3,3,3,3,3,3,3,3,3,3,3,3,3,3,3,3,3,3,
3,3,3,3,3,3,3,3,3,3,3,3,3,3,3,4),(-117.188905599613,-117.074247201759,-116.958487635636,
-116.845661598208,-116.745978032195,-116.646437684038,-116.546505564764,
-116.447144859913,-116.347817095309,-116.24849180919,-116.148114039354,
-116.048644104107,-115.947812416977,-115.846980729847,-115.747297163834,
-115.647756815677,-115.547824696403,-115.448463991552,-115.349136226949,
-115.24981094083,-115.149433170994,-115.049963235746,-114.949131548616,
-114.848299861486,-114.748616295473,-114.649075947317,-114.549143828043,
-114.449783123192,-114.350455358589,-114.251130072471,-114.150752302634,
-114.051282367388,-113.950450680257,-113.849618993126,-113.749935427113,
-113.650395078956,-113.550462959682,-113.451102254832,-113.351774490228,
-113.252449204109,-113.152071434273,-113.052601499026,-112.951769811895,
-112.850938124765,-112.751254558752,-112.651714210595,-112.551782091321,
-112.45242138647,-112.353093621866,-112.253768335747,-112.153390565911,
-112.053920630664,-111.953088943534,-111.852257256404,-111.753361661131,
-111.654608517859,-111.555968937272,-111.457390389855,-111.358841414297,
-111.260290588098,-111.16164445216,-111.062946578368,-110.964086828485,
-110.905720292661),.UNSPECIFIED.);
#762=B_SPLINE_CURVE_WITH_KNOTS('',3,(#9612,#9613,#9614,#9615,#9616,#9617,
#9618,#9619,#9620,#9621,#9622,#9623),.UNSPECIFIED.,.F.,.F.,(4,2,1,1,1,1,
1,1,4),(-110.905720292661,-110.853576388043,-109.854895519683,-108.856214651322,
-107.857533782961,-106.8588529146,-105.86017204624,-104.861491177879,-104.622534985481),
 .UNSPECIFIED.);
#763=B_SPLINE_CURVE_WITH_KNOTS('',3,(#9625,#9626,#9627,#9628,#9629,#9630,
#9631,#9632,#9633,#9634),.UNSPECIFIED.,.F.,.F.,(4,1,1,1,1,1,1,4),(-104.622534985481,
-103.862810309518,-102.864129441157,-101.865448572797,-100.866767704436,
-99.8680868360751,-98.8694059677144,-98.3393496783013),.UNSPECIFIED.);
#764=B_SPLINE_CURVE_WITH_KNOTS('',3,(#9636,#9637,#9638,#9639,#9640,#9641,
#9642,#9643,#9644,#9645,#9646,#9647,#9648,#9649,#9650,#9651,#9652,#9653,
#9654,#9655,#9656,#9657,#9658,#9659,#9660,#9661,#9662,#9663,#9664,#9665,
#9666,#9667,#9668,#9669,#9670,#9671,#9672,#9673,#9674,#9675,#9676,#9677,
#9678,#9679,#9680,#9681,#9682,#9683,#9684,#9685,#9686,#9687,#9688,#9689,
#9690,#9691,#9692,#9693,#9694,#9695,#9696,#9697,#9698,#9699,#9700,#9701,
#9702,#9703,#9704,#9705,#9706,#9707,#9708,#9709,#9710,#9711,#9712,#9713,
#9714,#9715,#9716,#9717,#9718,#9719,#9720,#9721,#9722,#9723,#9724,#9725,
#9726,#9727,#9728,#9729,#9730,#9731,#9732,#9733,#9734,#9735,#9736,#9737,
#9738,#9739,#9740,#9741,#9742,#9743,#9744,#9745,#9746,#9747,#9748,#9749,
#9750,#9751,#9752,#9753,#9754,#9755,#9756,#9757,#9758,#9759,#9760,#9761,
#9762,#9763,#9764,#9765,#9766,#9767,#9768,#9769,#9770,#9771,#9772,#9773,
#9774,#9775,#9776,#9777,#9778,#9779,#9780,#9781,#9782,#9783,#9784,#9785,
#9786,#9787,#9788,#9789,#9790,#9791,#9792,#9793,#9794,#9795,#9796,#9797,
#9798,#9799,#9800,#9801,#9802,#9803,#9804,#9805,#9806,#9807,#9808,#9809,
#9810,#9811,#9812,#9813,#9814,#9815,#9816,#9817,#9818,#9819,#9820,#9821,
#9822,#9823,#9824,#9825,#9826,#9827,#9828),.UNSPECIFIED.,.F.,.F.,(4,3,3,
3,3,3,3,3,3,3,3,3,3,3,3,3,3,3,3,3,3,3,3,3,3,3,3,3,3,3,3,3,3,3,3,3,3,3,3,
3,3,3,3,3,3,3,3,3,3,3,3,3,3,3,3,3,3,3,3,3,3,3,3,3,4),(-98.3393495114471,
-98.233881669341,-98.1280517505152,-98.0220294207556,-97.9156982804113,
-97.8707250993536,-97.7710415333408,-97.6715011851837,-97.5715690659099,
-97.4722083610592,-97.3728805964559,-97.2735553103369,-97.1731775405009,
-97.0737076052538,-96.9728759181233,-96.8720442309929,-96.7723606649801,
-96.6728203168229,-96.5728881975491,-96.4735274926984,-96.374199728095,
-96.2748744419759,-96.17449667214,-96.0750267368928,-95.9741950497625,-95.8733633626321,
-95.7736797966193,-95.6741394484622,-95.5742073291884,-95.4748466243377,
-95.3755188597344,-95.2761935736154,-95.1758158037794,-95.0763458685322,
-94.9755141814018,-94.8746824942714,-94.7749989282586,-94.6754585801015,
-94.5755264608276,-94.476165755977,-94.3768379913736,-94.2775127052546,
-94.1771349354186,-94.0776650001714,-93.976833313041,-93.8760016259106,
-93.7763180598978,-93.6767777117407,-93.5768455924669,-93.4774848876162,
-93.3781571230129,-93.2788318368939,-93.1784540670579,-93.0789841318107,
-92.9781524446803,-92.8773207575499,-92.7746762092464,-92.6766447659007,
-92.5787048057558,-92.4808241264331,-92.3829706052476,-92.2850696713238,
-92.1871405423995,-92.0890995979721,-92.0561643711217),.UNSPECIFIED.);
#765=B_SPLINE_CURVE_WITH_KNOTS('',3,(#9830,#9831,#9832,#9833,#9834,#9835,
#9836,#9837,#9838,#9839,#9840),.UNSPECIFIED.,.F.,.F.,(4,1,1,1,1,1,1,1,4),
(-92.0561643711217,-91.8786398891891,-90.8799590208284,-89.8812781524676,
-88.8825972841069,-87.8839164157461,-86.8852355473853,-85.8865546790246,
-85.7729790639421),.UNSPECIFIED.);
#766=B_SPLINE_CURVE_WITH_KNOTS('',3,(#9842,#9843,#9844,#9845,#9846,#9847,
#9848,#9849,#9850,#9851,#9852,#9853,#9854,#9855,#9856,#9857,#9858,#9859,
#9860,#9861,#9862,#9863,#9864,#9865,#9866,#9867,#9868,#9869,#9870,#9871,
#9872,#9873,#9874,#9875,#9876,#9877,#9878,#9879,#9880,#9881,#9882,#9883,
#9884,#9885,#9886,#9887,#9888,#9889,#9890,#9891,#9892,#9893,#9894,#9895,
#9896,#9897,#9898,#9899,#9900,#9901,#9902,#9903,#9904,#9905,#9906,#9907,
#9908,#9909,#9910,#9911,#9912,#9913,#9914,#9915,#9916,#9917,#9918,#9919,
#9920,#9921,#9922,#9923,#9924,#9925,#9926,#9927,#9928,#9929,#9930,#9931,
#9932,#9933,#9934,#9935,#9936,#9937,#9938,#9939,#9940,#9941,#9942,#9943,
#9944,#9945,#9946,#9947,#9948,#9949,#9950,#9951,#9952,#9953,#9954,#9955,
#9956,#9957,#9958,#9959,#9960,#9961,#9962,#9963,#9964,#9965,#9966,#9967,
#9968,#9969,#9970,#9971,#9972,#9973,#9974,#9975,#9976,#9977,#9978,#9979,
#9980,#9981,#9982,#9983,#9984,#9985,#9986,#9987,#9988,#9989,#9990,#9991,
#9992,#9993,#9994,#9995,#9996,#9997,#9998,#9999,#10000,#10001,#10002,#10003,
#10004,#10005,#10006,#10007,#10008,#10009,#10010,#10011,#10012,#10013,#10014,
#10015,#10016,#10017,#10018,#10019,#10020,#10021,#10022,#10023,#10024,#10025,
#10026,#10027,#10028,#10029,#10030,#10031),.UNSPECIFIED.,.F.,.F.,(4,3,3,
3,3,3,3,3,3,3,3,3,3,3,3,3,3,3,3,3,3,3,3,3,3,3,3,3,3,3,3,3,3,3,3,3,3,3,3,
3,3,3,3,3,3,3,3,3,3,3,3,3,3,3,3,3,3,3,3,3,3,3,3,4),(-85.7729790639421,-85.6747012370361,
-85.5763478087396,-85.4782825827934,-85.3802610142147,-85.2822511346314,
-85.1836568036395,-85.0855181919729,-84.9866960013183,-84.8878738106638,
-84.788190244651,-84.6886498964939,-84.5887177772201,-84.4893570723695,
-84.3900293077662,-84.2907040216472,-84.1903262518112,-84.090856316564,
-83.9900246294335,-83.8891929423031,-83.7895093762904,-83.6899690281336,
-83.5900369088597,-83.4906762040089,-83.3913484394057,-83.2920231532865,
-83.1916453834505,-83.0921754482033,-82.9913437610728,-82.8905120739423,
-82.7908285079295,-82.6912881597726,-82.5913560404987,-82.491995335648,
-82.3926675710447,-82.2933422849257,-82.1929645150897,-82.0934945798426,
-81.9926628927121,-81.8918312055816,-81.7921476395688,-81.6926072914119,
-81.592675172138,-81.4933144672874,-81.393986702684,-81.2946614165649,-81.1942836467289,
-81.0948137114817,-80.9939820243513,-80.8931503372209,-80.7934667712081,
-80.6939264230509,-80.5939943037771,-80.4946335989264,-80.3953058343231,
-80.2959805482041,-80.1956027783681,-80.096132843121,-79.9953011559905,
-79.8944694688601,-79.7841166760362,-79.6740971377985,-79.5646466108232,
-79.4897941881386),.UNSPECIFIED.);
#767=B_SPLINE_CURVE_WITH_KNOTS('',3,(#10033,#10034,#10035,#10036,#10037,
#10038,#10039,#10040,#10041,#10042),.UNSPECIFIED.,.F.,.F.,(4,1,1,1,1,1,
1,4),(-79.4897937567626,-78.8957886004994,-77.8971077321386,-76.8984268637779,
-75.8997459954171,-74.9010651270563,-73.9023842586956,-73.2066084495829),
 .UNSPECIFIED.);
#768=B_SPLINE_CURVE_WITH_KNOTS('',3,(#10044,#10045,#10046,#10047,#10048,
#10049,#10050,#10051,#10052,#10053,#10054,#10055,#10056,#10057,#10058,#10059,
#10060,#10061,#10062,#10063,#10064,#10065,#10066,#10067,#10068,#10069,#10070,
#10071,#10072,#10073,#10074,#10075,#10076,#10077,#10078,#10079,#10080,#10081,
#10082,#10083,#10084,#10085,#10086,#10087,#10088,#10089,#10090,#10091,#10092,
#10093,#10094,#10095,#10096,#10097,#10098,#10099,#10100,#10101,#10102,#10103,
#10104,#10105,#10106,#10107,#10108,#10109,#10110,#10111,#10112,#10113,#10114,
#10115,#10116,#10117,#10118,#10119,#10120,#10121,#10122,#10123,#10124,#10125,
#10126,#10127,#10128,#10129,#10130,#10131,#10132,#10133,#10134,#10135,#10136,
#10137,#10138,#10139,#10140,#10141,#10142,#10143,#10144,#10145,#10146,#10147,
#10148,#10149,#10150,#10151,#10152,#10153,#10154,#10155,#10156,#10157,#10158,
#10159,#10160,#10161,#10162,#10163,#10164,#10165,#10166,#10167,#10168,#10169,
#10170,#10171,#10172,#10173,#10174,#10175,#10176,#10177,#10178,#10179,#10180,
#10181,#10182,#10183,#10184,#10185,#10186,#10187,#10188,#10189,#10190,#10191,
#10192,#10193,#10194,#10195,#10196,#10197,#10198,#10199,#10200,#10201,#10202,
#10203,#10204,#10205,#10206,#10207,#10208,#10209,#10210,#10211,#10212,#10213,
#10214,#10215,#10216,#10217,#10218,#10219,#10220,#10221,#10222,#10223,#10224,
#10225,#10226,#10227,#10228,#10229,#10230,#10231,#10232,#10233),
 .UNSPECIFIED.,.F.,.F.,(4,3,3,3,3,3,3,3,3,3,3,3,3,3,3,3,3,3,3,3,3,3,3,3,
3,3,3,3,3,3,3,3,3,3,3,3,3,3,3,3,3,3,3,3,3,3,3,3,3,3,3,3,3,3,3,3,3,3,3,3,
3,3,3,4),(-73.2066082616887,-73.0873800102398,-72.9665362689588,-72.9037033903348,
-72.804019824322,-72.7044794761649,-72.6045473568911,-72.5051866520404,
-72.4058588874371,-72.306533601318,-72.2061558314821,-72.1066858962349,
-72.0058542091045,-71.9050225219741,-71.8053389559613,-71.7057986078042,
-71.6058664885303,-71.5065057836796,-71.4071780190763,-71.3078527329571,
-71.2074749631212,-71.108005027874,-71.0071733407436,-70.9063416536133,
-70.8066580876005,-70.7071177394434,-70.6071856201696,-70.5078249153189,
-70.4084971507156,-70.3091718645965,-70.2087940947605,-70.1093241595134,
-70.008492472383,-69.9076607852526,-69.8079772192398,-69.7084368710827,
-69.6085047518089,-69.5091440469582,-69.4098162823549,-69.3104909962358,
-69.2101132263998,-69.1106432911527,-69.0098116040222,-68.9089799168918,
-68.809296350879,-68.7097560027219,-68.609823883448,-68.5104631785974,-68.4111354139941,
-68.311810127875,-68.211432358039,-68.1119624227919,-68.0111307356615,-67.9102990485311,
-67.8108213082292,-67.7114866269179,-67.6122670665479,-67.5131103926434,
-67.4139858279942,-67.314862635178,-67.2156413232076,-67.116372598946,-67.0169246775773,
-66.9234231424034),.UNSPECIFIED.);
#769=B_SPLINE_CURVE_WITH_KNOTS('',3,(#10235,#10236,#10237,#10238,#10239,
#10240,#10241,#10242,#10243,#10244,#10245,#10246),.UNSPECIFIED.,.F.,.F.,
(4,2,1,1,1,1,1,1,4),(-66.9234231424034,-66.9116181801703,-65.9129373118096,
-64.9142564434488,-63.9155755750881,-62.9168947067273,-61.9182138383666,
-60.9195329700058,-60.6402420696886),.UNSPECIFIED.);
#770=B_SPLINE_CURVE_WITH_KNOTS('',3,(#10248,#10249,#10250,#10251,#10252,
#10253,#10254,#10255,#10256,#10257,#10258,#10259,#10260,#10261,#10262,#10263,
#10264,#10265,#10266,#10267,#10268,#10269,#10270,#10271,#10272,#10273,#10274,
#10275,#10276,#10277,#10278,#10279,#10280,#10281,#10282,#10283,#10284,#10285,
#10286,#10287,#10288,#10289,#10290,#10291,#10292,#10293,#10294,#10295,#10296,
#10297,#10298,#10299,#10300,#10301,#10302,#10303,#10304,#10305,#10306,#10307,
#10308,#10309,#10310,#10311,#10312,#10313,#10314,#10315,#10316,#10317,#10318,
#10319,#10320,#10321,#10322,#10323,#10324,#10325,#10326,#10327,#10328,#10329,
#10330,#10331,#10332,#10333,#10334,#10335,#10336,#10337,#10338,#10339,#10340,
#10341,#10342,#10343,#10344,#10345,#10346,#10347,#10348,#10349,#10350,#10351,
#10352,#10353,#10354,#10355,#10356,#10357,#10358,#10359,#10360,#10361,#10362,
#10363,#10364,#10365,#10366,#10367,#10368,#10369,#10370,#10371,#10372,#10373,
#10374,#10375,#10376,#10377,#10378,#10379,#10380,#10381,#10382,#10383,#10384,
#10385,#10386,#10387,#10388,#10389,#10390,#10391,#10392,#10393,#10394,#10395,
#10396,#10397,#10398,#10399,#10400,#10401,#10402,#10403,#10404,#10405,#10406,
#10407,#10408,#10409,#10410,#10411,#10412,#10413,#10414,#10415,#10416,#10417,
#10418,#10419,#10420,#10421,#10422,#10423,#10424,#10425,#10426,#10427,#10428,
#10429,#10430,#10431,#10432,#10433,#10434,#10435,#10436,#10437,#10438,#10439,
#10440),.UNSPECIFIED.,.F.,.F.,(4,3,3,3,3,3,3,3,3,3,3,3,3,3,3,3,3,3,3,3,
3,3,3,3,3,3,3,3,3,3,3,3,3,3,3,3,3,3,3,3,3,3,3,3,3,3,3,3,3,3,3,3,3,3,3,3,
3,3,3,3,3,3,3,3,4),(-60.6402378352238,-60.541696652544,-60.4432021032873,
-60.3447227024354,-60.2462269890419,-60.1476223960021,-60.0489531987877,
-59.9501235071943,-59.9208521016451,-59.8211685356324,-59.7216281874753,
-59.6216960682015,-59.5223353633507,-59.4230075987475,-59.3236823126283,
-59.2233045427923,-59.1238346075451,-59.0230029204147,-58.9221712332843,
-58.8224876672716,-58.7229473191144,-58.6230151998405,-58.5236544949899,
-58.4243267303866,-58.3250014442675,-58.2246236744316,-58.1251537391845,
-58.024322052054,-57.9234903649236,-57.8238067989108,-57.7242664507537,
-57.6243343314799,-57.5249736266291,-57.4256458620259,-57.3263205759069,
-57.2259428060708,-57.1264728708238,-57.0256411836933,-56.9248094965628,
-56.8251259305499,-56.7255855823927,-56.6256534631189,-56.5262927582682,
-56.4269649936648,-56.3276397075457,-56.2272619377098,-56.1277920024627,
-56.0269603153324,-55.9261286282021,-55.8264450621894,-55.7269047140322,
-55.6269725947583,-55.5276118899076,-55.4282841253044,-55.3289588391855,
-55.2285810693494,-55.1291111341022,-55.0282794469718,-54.9274477598413,
-54.8254312965464,-54.7235829168215,-54.6219114837855,-54.5203441562718,
-54.4188669816396,-54.3570525280442),.UNSPECIFIED.);
#771=B_SPLINE_CURVE_WITH_KNOTS('',3,(#10442,#10443,#10444,#10445,#10446,
#10447,#10448,#10449,#10450,#10451),.UNSPECIFIED.,.F.,.F.,(4,1,1,1,1,1,
1,4),(-54.3570471904822,-53.9287668914806,-52.9300860231198,-51.9314051547591,
-50.9327242863983,-49.9340434180376,-48.9353625496768,-48.0738672208646),
 .UNSPECIFIED.);
#772=B_SPLINE_CURVE_WITH_KNOTS('',3,(#10453,#10454,#10455,#10456,#10457,
#10458,#10459,#10460,#10461,#10462,#10463),.UNSPECIFIED.,.F.,.F.,(4,1,1,
1,1,1,1,1,4),(-48.0738672208646,-47.9366816813161,-46.9380008129553,-45.9393199445946,
-44.9406390762338,-43.941958207873,-42.9432773395123,-41.9445964711515,
-41.790681913685),.UNSPECIFIED.);
#773=B_SPLINE_CURVE_WITH_KNOTS('',3,(#10465,#10466,#10467,#10468,#10469,
#10470,#10471,#10472,#10473,#10474),.UNSPECIFIED.,.F.,.F.,(4,1,1,1,1,1,
1,4),(-41.790681913685,-40.9459156027908,-39.94723473443,-38.9485538660693,
-37.9498729977085,-36.9511921293478,-35.952511260987,-35.5074966065054),
 .UNSPECIFIED.);
#774=B_SPLINE_CURVE_WITH_KNOTS('',3,(#10476,#10477,#10478,#10479,#10480,
#10481,#10482,#10483,#10484,#10485),.UNSPECIFIED.,.F.,.F.,(4,1,1,1,1,1,
1,4),(-35.5074966065054,-34.9538303926263,-33.9551495242656,-32.9564686559048,
-31.957787787544,-30.9591069191833,-29.9604260508225,-29.2243112993258),
 .UNSPECIFIED.);
#775=B_SPLINE_CURVE_WITH_KNOTS('',3,(#10487,#10488,#10489,#10490,#10491,
#10492,#10493,#10494,#10495,#10496,#10497,#10498,#10499,#10500,#10501,#10502,
#10503,#10504,#10505,#10506,#10507,#10508,#10509,#10510,#10511,#10512,#10513,
#10514,#10515,#10516,#10517,#10518,#10519,#10520,#10521,#10522,#10523,#10524,
#10525,#10526,#10527,#10528,#10529,#10530,#10531,#10532,#10533,#10534,#10535,
#10536,#10537,#10538,#10539,#10540,#10541,#10542,#10543,#10544,#10545,#10546,
#10547,#10548,#10549,#10550,#10551,#10552,#10553,#10554,#10555,#10556,#10557,
#10558,#10559,#10560,#10561,#10562,#10563,#10564,#10565,#10566,#10567,#10568,
#10569,#10570,#10571,#10572,#10573,#10574,#10575,#10576,#10577,#10578,#10579,
#10580,#10581,#10582,#10583,#10584,#10585,#10586,#10587,#10588,#10589,#10590,
#10591,#10592,#10593,#10594,#10595,#10596,#10597,#10598,#10599,#10600,#10601,
#10602,#10603,#10604,#10605,#10606,#10607,#10608,#10609,#10610,#10611,#10612,
#10613,#10614,#10615,#10616,#10617,#10618,#10619,#10620,#10621,#10622,#10623,
#10624,#10625,#10626,#10627,#10628,#10629,#10630,#10631,#10632,#10633,#10634,
#10635,#10636,#10637,#10638,#10639,#10640,#10641,#10642,#10643,#10644,#10645,
#10646,#10647,#10648,#10649,#10650,#10651,#10652,#10653,#10654,#10655,#10656,
#10657,#10658,#10659,#10660,#10661,#10662,#10663,#10664,#10665,#10666,#10667,
#10668,#10669,#10670,#10671,#10672,#10673,#10674,#10675,#10676),
 .UNSPECIFIED.,.F.,.F.,(4,3,3,3,3,3,3,3,3,3,3,3,3,3,3,3,3,3,3,3,3,3,3,3,
3,3,3,3,3,3,3,3,3,3,3,3,3,3,3,3,3,3,3,3,3,3,3,3,3,3,3,3,3,3,3,3,3,3,3,3,
3,3,3,4),(-29.2243111180069,-29.0930281502344,-28.9617451824618,-28.8620616164645,
-28.7625212683228,-28.6625891490451,-28.5632284442096,-28.4639006796212,
-28.364575393517,-28.264197623663,-28.1647276884302,-28.0638960012656,-27.963064314101,
-27.8633807481083,-27.7638403999717,-27.6639082806927,-27.5645475758629,
-27.4652198112804,-27.3658945251824,-27.2655167553219,-27.1660468200957,
-27.065215132918,-26.9643834457403,-26.8646998796295,-26.7651595313741,
-26.6652274121248,-26.565866707176,-26.4665389424749,-26.3672136562584,
-26.2668358865386,-26.167365951196,-26.0665342642878,-25.9657025773795,
-25.8660190114961,-25.7664786634679,-25.6665465441617,-25.5671858394381,
-25.4678580749609,-25.3685327889668,-25.2681550189798,-25.1686850838535,
-25.0678533964362,-24.9670217090188,-24.8673381430953,-24.7677977950291,
-24.6678656757327,-24.5685049709762,-24.4691772064682,-24.3698519204453,
-24.2694741504985,-24.1700042153487,-24.0691725280033,-23.968340840658,
-23.8686572739908,-23.7691169251773,-23.6691848060673,-23.5698241005602,
-23.4704963353019,-23.3711710485301,-23.2707932794719,-23.1713233435843,
-23.0704916579408,-22.9696599722973,-22.9411259921462),.UNSPECIFIED.);
#776=B_SPLINE_CURVE_WITH_KNOTS('',3,(#10678,#10679,#10680,#10681,#10682,
#10683,#10684,#10685,#10686,#10687,#10688,#10689,#10690,#10691,#10692,#10693,
#10694,#10695,#10696,#10697,#10698,#10699,#10700,#10701,#10702,#10703,#10704,
#10705,#10706,#10707,#10708,#10709,#10710,#10711,#10712,#10713,#10714,#10715,
#10716,#10717,#10718,#10719,#10720,#10721,#10722,#10723,#10724,#10725,#10726,
#10727,#10728,#10729,#10730,#10731,#10732,#10733,#10734,#10735,#10736,#10737,
#10738,#10739,#10740,#10741,#10742,#10743,#10744,#10745,#10746,#10747,#10748,
#10749,#10750,#10751,#10752,#10753,#10754,#10755,#10756,#10757,#10758,#10759,
#10760,#10761,#10762,#10763,#10764,#10765,#10766,#10767,#10768,#10769,#10770,
#10771,#10772,#10773,#10774,#10775,#10776,#10777,#10778,#10779,#10780,#10781,
#10782,#10783,#10784,#10785,#10786,#10787,#10788,#10789,#10790,#10791,#10792,
#10793,#10794,#10795,#10796,#10797,#10798,#10799,#10800,#10801,#10802,#10803,
#10804,#10805,#10806,#10807,#10808,#10809,#10810,#10811,#10812,#10813,#10814,
#10815,#10816,#10817,#10818,#10819,#10820,#10821,#10822,#10823,#10824,#10825,
#10826,#10827,#10828,#10829,#10830,#10831,#10832,#10833,#10834,#10835,#10836,
#10837,#10838,#10839,#10840,#10841,#10842,#10843,#10844,#10845,#10846,#10847,
#10848,#10849,#10850,#10851,#10852,#10853,#10854,#10855,#10856,#10857,#10858,
#10859,#10860,#10861,#10862,#10863,#10864,#10865,#10866,#10867),
 .UNSPECIFIED.,.F.,.F.,(4,3,3,3,3,3,3,3,3,3,3,3,3,3,3,3,3,3,3,3,3,3,3,3,
3,3,3,3,3,3,3,3,3,3,3,3,3,3,3,3,3,3,3,3,3,3,3,3,3,3,3,3,3,3,3,3,3,3,3,3,
3,3,3,4),(-22.9411259917379,-22.8419179935918,-22.7428514984844,-22.6438973639292,
-22.5450040344622,-22.4461404084451,-22.3472754222286,-22.2483111277133,
-22.1492963564552,-22.0501073736359,-21.9709791039365,-21.8712955381832,
-21.7717551902968,-21.6718230709567,-21.5724623664015,-21.4731346021024,
-21.3738093162956,-21.2734315461156,-21.1739616111974,-21.0731299233866,
-20.9722982355758,-20.8726146652961,-20.7730743128561,-20.6731421946509,
-20.5737814855096,-20.4744537166221,-20.3751284262311,-20.2747506614771,
-20.1752807220312,-20.0744490446231,-19.973617367215,-19.8739338090674,
-19.7743934687681,-19.6744613475288,-19.5751006504616,-19.4757728935969,
-19.3764476151617,-19.2760698360849,-19.17659990831,-19.0757682035822,-18.9749364988543,
-18.8752529321135,-18.7757125833021,-18.6757804642011,-18.5764197588777,
-18.4770919938704,-18.3777667074162,-18.2773889381855,-18.1779190027736,
-18.0770873166336,-17.9762556304935,-17.8765720373954,-17.777031662028,
-17.6770995495411,-17.5777388173754,-17.4784110254777,-17.3790857121216,
-17.2787079746244,-17.1792380125578,-17.0784063873453,-16.9775747621328,
-16.8588404756105,-16.7414263370442,-16.6579409003871),.UNSPECIFIED.);
#777=B_SPLINE_CURVE_WITH_KNOTS('',3,(#10869,#10870,#10871,#10872,#10873,
#10874,#10875,#10876,#10877,#10878),.UNSPECIFIED.,.F.,.F.,(4,1,1,1,1,1,
1,4),(-16.6579406849666,-15.978893893772,-14.9802130254113,-13.9815321570505,
-12.9828512886898,-11.984170420329,-10.9854895519683,-10.3747553777871),
 .UNSPECIFIED.);
#778=B_SPLINE_CURVE_WITH_KNOTS('',3,(#10879,#10880,#10881,#10882,#10883,
#10884,#10885,#10886,#10887,#10888),.UNSPECIFIED.,.F.,.F.,(4,1,1,1,1,1,
1,4),(-10.3747553777871,-9.98680868360752,-8.98812781524676,-7.98944694688601,
-6.99076607852526,-5.99208521016451,-4.99340434180376,-4.09157007060746),
 .UNSPECIFIED.);
#779=B_SPLINE_CURVE_WITH_KNOTS('',3,(#10892,#10893,#10894,#10895,#10896,
#10897,#10898,#10899,#10900,#10901,#10902,#10903,#10904,#10905,#10906,#10907,
#10908,#10909,#10910,#10911,#10912,#10913,#10914,#10915,#10916,#10917,#10918,
#10919,#10920,#10921,#10922,#10923,#10924,#10925,#10926,#10927,#10928,#10929,
#10930,#10931,#10932,#10933,#10934,#10935,#10936,#10937,#10938,#10939,#10940,
#10941,#10942,#10943,#10944,#10945,#10946,#10947,#10948,#10949,#10950,#10951,
#10952,#10953,#10954,#10955,#10956,#10957,#10958,#10959,#10960,#10961,#10962,
#10963,#10964,#10965,#10966,#10967,#10968,#10969,#10970,#10971,#10972,#10973,
#10974,#10975,#10976,#10977,#10978,#10979,#10980,#10981,#10982,#10983,#10984,
#10985,#10986,#10987,#10988,#10989,#10990,#10991,#10992,#10993,#10994,#10995,
#10996,#10997,#10998,#10999,#11000,#11001,#11002,#11003,#11004,#11005,#11006,
#11007,#11008,#11009,#11010,#11011,#11012,#11013,#11014,#11015,#11016,#11017,
#11018,#11019,#11020,#11021,#11022,#11023,#11024,#11025,#11026,#11027,#11028,
#11029,#11030,#11031,#11032,#11033,#11034,#11035,#11036,#11037,#11038,#11039,
#11040,#11041,#11042,#11043,#11044,#11045,#11046,#11047,#11048,#11049,#11050,
#11051,#11052,#11053,#11054,#11055,#11056,#11057,#11058,#11059,#11060,#11061,
#11062,#11063,#11064,#11065,#11066,#11067,#11068,#11069,#11070,#11071,#11072,
#11073,#11074,#11075,#11076,#11077,#11078,#11079,#11080,#11081,#11082,#11083,
#11084,#11085,#11086,#11087,#11088,#11089,#11090,#11091,#11092,#11093,#11094,
#11095,#11096,#11097,#11098,#11099,#11100,#11101,#11102,#11103,#11104,#11105,
#11106,#11107,#11108,#11109,#11110,#11111,#11112,#11113,#11114,#11115,#11116,
#11117,#11118,#11119,#11120,#11121,#11122,#11123,#11124,#11125,#11126,#11127,
#11128,#11129,#11130,#11131,#11132,#11133,#11134,#11135,#11136,#11137,#11138,
#11139,#11140,#11141,#11142,#11143,#11144,#11145,#11146,#11147,#11148,#11149,
#11150,#11151,#11152,#11153,#11154,#11155,#11156,#11157,#11158,#11159,#11160,
#11161,#11162,#11163,#11164,#11165,#11166,#11167,#11168,#11169,#11170,#11171,
#11172,#11173,#11174,#11175,#11176,#11177,#11178,#11179,#11180,#11181,#11182,
#11183,#11184,#11185,#11186,#11187,#11188,#11189,#11190,#11191,#11192,#11193,
#11194,#11195,#11196,#11197,#11198,#11199,#11200,#11201,#11202,#11203,#11204,
#11205,#11206,#11207,#11208,#11209,#11210,#11211,#11212,#11213,#11214,#11215,
#11216,#11217,#11218,#11219,#11220,#11221,#11222,#11223,#11224,#11225,#11226,
#11227,#11228,#11229,#11230,#11231,#11232,#11233,#11234,#11235,#11236,#11237,
#11238,#11239,#11240,#11241,#11242,#11243,#11244,#11245,#11246,#11247,#11248,
#11249,#11250,#11251,#11252,#11253,#11254,#11255,#11256,#11257,#11258,#11259,
#11260,#11261,#11262,#11263,#11264,#11265,#11266,#11267,#11268,#11269,#11270,
#11271,#11272,#11273,#11274,#11275,#11276,#11277,#11278,#11279,#11280,#11281,
#11282,#11283,#11284,#11285,#11286,#11287,#11288,#11289,#11290,#11291,#11292,
#11293,#11294,#11295,#11296,#11297,#11298,#11299,#11300,#11301,#11302,#11303,
#11304,#11305,#11306,#11307,#11308,#11309,#11310,#11311,#11312,#11313,#11314,
#11315,#11316,#11317,#11318,#11319,#11320,#11321,#11322,#11323,#11324,#11325,
#11326,#11327,#11328,#11329,#11330,#11331,#11332,#11333,#11334,#11335,#11336,
#11337,#11338,#11339,#11340,#11341,#11342,#11343,#11344,#11345,#11346,#11347,
#11348,#11349,#11350,#11351,#11352,#11353,#11354,#11355,#11356,#11357,#11358,
#11359,#11360,#11361,#11362,#11363,#11364,#11365,#11366,#11367,#11368,#11369,
#11370,#11371,#11372,#11373,#11374,#11375,#11376,#11377,#11378,#11379,#11380,
#11381,#11382,#11383,#11384,#11385,#11386,#11387,#11388,#11389,#11390,#11391,
#11392,#11393,#11394,#11395,#11396,#11397,#11398,#11399,#11400,#11401,#11402,
#11403,#11404,#11405,#11406,#11407,#11408,#11409,#11410,#11411,#11412,#11413,
#11414,#11415,#11416,#11417,#11418,#11419,#11420,#11421,#11422,#11423,#11424,
#11425,#11426,#11427,#11428,#11429,#11430,#11431,#11432,#11433,#11434,#11435,
#11436,#11437,#11438,#11439,#11440,#11441,#11442,#11443,#11444,#11445,#11446,
#11447,#11448,#11449,#11450,#11451,#11452,#11453,#11454,#11455,#11456,#11457,
#11458,#11459,#11460,#11461,#11462,#11463,#11464,#11465,#11466,#11467,#11468,
#11469,#11470,#11471,#11472,#11473,#11474,#11475,#11476,#11477,#11478,#11479,
#11480,#11481,#11482,#11483,#11484,#11485,#11486,#11487,#11488,#11489),
 .UNSPECIFIED.,.F.,.F.,(4,2,2,2,2,2,2,2,2,2,2,2,2,2,2,2,2,2,2,2,2,2,2,2,
2,2,2,2,2,2,2,2,2,2,2,2,2,2,2,2,2,2,2,2,2,2,2,2,2,2,2,2,2,2,2,2,2,2,2,2,
2,2,2,2,2,2,2,2,2,2,2,2,2,2,2,2,2,2,2,2,2,2,2,2,2,2,2,2,2,2,2,2,2,2,2,2,
2,2,2,2,2,2,2,2,2,2,2,2,2,2,2,2,2,2,2,2,2,2,2,2,2,2,2,2,2,2,2,2,2,2,2,2,
2,2,2,2,2,2,2,2,2,2,2,2,2,2,2,2,2,2,2,2,2,2,2,2,2,2,2,2,2,2,2,2,2,2,2,2,
2,2,2,2,2,2,2,2,2,2,2,2,2,2,2,2,2,2,2,2,2,2,2,2,2,2,2,2,2,2,2,2,2,2,2,2,
2,2,2,2,2,2,2,2,2,2,2,2,2,2,2,2,2,2,2,2,2,2,2,2,2,2,2,2,2,2,2,2,2,2,2,2,
2,2,2,2,2,2,2,2,2,2,2,2,2,2,2,2,2,2,2,2,2,2,2,2,2,2,2,2,2,2,2,2,2,2,2,2,
2,2,2,2,2,2,2,2,2,2,2,2,2,2,2,2,2,2,2,2,2,2,4),(-2.32112203948973,-2.29034393663197,
-2.28647054352913,-2.28422159465382,-2.28264621329015,-2.28129251248404,
-2.2798401725342,-2.27797922378873,-2.27414412793826,-2.24389445016459,
-2.23036041817568,-2.21877297144587,-2.19059563289267,-2.18397206757087,
-2.18236890586133,-2.1814446293015,-2.18063469572578,-2.17959657842402,
-2.17745231764752,-2.16249553676311,-2.15720436896209,-2.13409044791361,
-2.10492105159793,-2.09324393439829,-2.08578149162186,-2.08336647075221,
-2.08200977518731,-2.08056223814677,-2.07874568768348,-2.07591690870325,
-2.06216288475466,-2.02167619677099,-1.99885813177772,-1.98966470636612,
-1.98435750324089,-1.98287944902174,-1.98198299658212,-1.98116654411944,
-1.98009601980632,-1.97781022307268,-1.9556209163649,-1.91250819660216,
-1.896322988853,-1.89003867888934,-1.88686054005509,-1.88420936482288,-1.88260958474796,
-1.88260750957859,-1.88260542812914,-1.88260334034155,-1.88260124622188,
-1.88259914573118,-1.88259703882885,-1.88259492552241,-1.88259280579806,
-1.88259067960941,-1.8825885469179,-1.88258640773099,-1.8825842620395,-1.88258210978222,
-1.88257995095738,-1.88257778553047,-1.88257561345168,-1.88257343471771,
-1.88257124931054,-1.88256905720309,-1.88256685835465,-1.88256465277214,
-1.88256244040908,-1.88256022124152,-1.88255799524241,-1.88255576240921,
-1.88255352269834,-1.88255127607508,-1.88254902253767,-1.88254676205236,
-1.88254449456044,-1.88254222008303,-1.88253993858481,-1.88253765002649,
-1.88253535437622,-1.88253305162833,-1.88253074174567,-1.88252842470268,
-1.8825261004789,-1.88252376903928,-1.88252143034712,-1.88251908436322,
-1.88251673110272,-1.88251437051583,-1.88251200258282,-1.88105849206935,
-1.87918855363602,-1.8753079328154,-1.84199111305543,-1.79289445508601,
-1.78526898762658,-1.78360264016469,-1.7826643572385,-1.78185621304291,
-1.78083847894255,-1.77886097613549,-1.76734971010007,-1.7421072132408,
-1.71187800519132,-1.69648907289517,-1.68729952727244,-1.68468700078164,
-1.68308575675656,-1.68163242979374,-1.67976308839528,-1.67588502211101,
-1.64275767203379,-1.59111607184786,-1.58552423136097,-1.58401893418032,
-1.58311639154152,-1.5823017367306,-1.58124330229314,-1.57893522530068,
-1.54421524856088,-1.51343883794952,-1.49735558552034,-1.48786705057944,
-1.4852245842756,-1.48361635959058,-1.48216407750241,-1.48030633016285,
-1.47648896168293,-1.44724726348877,-1.40472291912577,-1.39264370799567,
-1.38620522537503,-1.38462601371873,-1.38370677564465,-1.38289522322511,
-1.38184718680793,-1.37965554971408,-1.36331899094411,-1.31299151126481,
-1.29758514579751,-1.28838707638612,-1.2857725086439,-1.28417007496942,
-1.28271570394366,-1.28084506438132,-1.27696444119723,-1.24380312066774,
-1.19210564194618,-1.18657044295578,-1.18507006555024,-1.18416839465968,
-1.18335385406514,-1.18229405005337,-1.18051753815884,-1.16955082681112,
-1.16583493137157,-1.16119078516264,-1.12867971029247,-1.09103808395885,
-1.08713451033408,-1.08526088670644,-1.08380779044098,-1.08221039590717,
-1.0796122544168,-1.07055542696725,-1.0554665161363,-1.02544862332573,-0.988354041188919,
-0.986085814933734,-0.985035302940362,-0.984222042823835,-0.983315609292496,
-0.981793092288234,-0.976014536868777,-0.965662526197371,-0.938251863044715,
-0.891241316006559,-0.887469346613765,-0.88561996084362,-0.884167945054924,
-0.882553556857021,-0.879886048342114,-0.870145871165747,-0.853463515559964,
-0.822174880962791,-0.799484854265853,-0.788392709688315,-0.786607075987028,
-0.785543216418512,-0.784725907054903,-0.783820717399649,-0.782315814134777,
-0.776777517662026,-0.724753861172956,-0.692328027221089,-0.688454517676588,
-0.686582758152494,-0.685125452621556,-0.683517674783842,-0.680889565624703,
-0.671593688673812,-0.655974978735857,-0.625550588075654,-0.589616689867446,
-0.587553822922564,-0.586514065174554,-0.585753705255509,-0.584927288654787,
-0.583758069847875,-0.580851625180863,-0.544798429028698,-0.495932938030075,
-0.48963617077389,-0.487299944797091,-0.485920229628196,-0.484472590203036,
-0.482581777065521,-0.478551708701874,-0.443076827043676,-0.392367432511269,
-0.38822006290789,-0.386851881929456,-0.385988065153033,-0.385186070114668,
-0.384116666053907,-0.381743325347215,-0.378556751791188,-0.343450692637509,
-0.296015116137967,-0.289630282076299,-0.287261995042367,-0.28586407449693,
-0.284397794165779,-0.282483310422913,-0.27840477818196,-0.242398704891009,
-0.216755431214847,-0.190185124254524,-0.187866684088788,-0.186779718505182,
-0.185960650056648,-0.185955646327147,-0.185950774289003,-0.185946029927201,
-0.185941409397797,-0.185936908958964,-0.185932525012532,-0.185928254131056,
-0.185924092969507,-0.185920038301805,-0.185916087018049,-0.185912236117139,
-0.185908482706886,-0.185904823974739,-0.185901257224124,-0.185897779842561,
-0.18589490738148,-0.185892056307941,-0.185889222382127,-0.18588640542643,
-0.185883605320891,-0.185880821922682,-0.185878055068841,-0.18587530461481,
-0.185872570404359,-0.185869852291084,-0.18586715016686,-0.185864463892584,
-0.185861793324586,-0.185859138304044,-0.185856498723685,-0.185853874448655,
-0.185851265330031,-0.185848671268029,-0.185846092112797,-0.185843527743315,
-0.185840978034615,-0.18583844285917,-0.185835922097251,-0.18583341562781,
-0.185830918207774,-0.185828424477525,-0.185825944384559,-0.185823477799486,
-0.184885653291375,-0.1832401140909,-0.176379272645583,-0.16322878190832,
-0.12481775085509,-0.0955331156990872,-0.0916842850318327,-0.0897999504486535,
-0.0883215131433462,-0.0866786520257004,-0.0839658324994265,-0.0740714962628944,
-0.0571530413364035,-0.0033609016908596),.UNSPECIFIED.);
#780=B_SPLINE_CURVE_WITH_KNOTS('',3,(#11493,#11494,#11495,#11496,#11497,
#11498,#11499,#11500,#11501,#11502,#11503,#11504,#11505,#11506,#11507,#11508,
#11509,#11510,#11511,#11512,#11513,#11514,#11515,#11516,#11517,#11518,#11519,
#11520,#11521,#11522,#11523,#11524,#11525,#11526,#11527,#11528,#11529,#11530,
#11531,#11532,#11533,#11534,#11535,#11536,#11537,#11538,#11539,#11540,#11541,
#11542,#11543,#11544,#11545,#11546,#11547,#11548,#11549,#11550,#11551,#11552,
#11553,#11554,#11555,#11556,#11557,#11558,#11559,#11560,#11561,#11562,#11563,
#11564,#11565,#11566,#11567,#11568,#11569,#11570,#11571,#11572,#11573,#11574,
#11575,#11576,#11577,#11578,#11579,#11580,#11581,#11582,#11583,#11584,#11585,
#11586,#11587,#11588,#11589,#11590,#11591,#11592,#11593,#11594,#11595,#11596,
#11597,#11598,#11599,#11600,#11601,#11602,#11603,#11604,#11605,#11606,#11607,
#11608,#11609,#11610,#11611,#11612,#11613,#11614,#11615,#11616),
 .UNSPECIFIED.,.F.,.F.,(4,3,3,3,3,3,3,3,3,3,3,3,3,3,3,3,3,3,3,3,3,3,3,3,
3,3,3,3,3,3,3,3,3,3,3,3,3,3,3,3,3,4),(11.6163931973419,11.7238022892394,
11.8352112612973,11.942542704643,12.0498762579441,12.1572406721673,12.2646647271014,
12.3722554126795,12.4799425122239,12.5878292808977,12.6150740657025,12.7189450740463,
12.8226420757906,12.9261962507554,13.0296728657244,13.1331089565476,13.2365415004203,
13.3400790736674,13.4436725429885,13.5474529273096,13.6137549340633,13.7188586017124,
13.8238046664922,13.9286265972958,14.0333820339704,14.1381063103255,14.2428347153535,
14.3476713207162,14.4525677883591,14.5576434493371,14.612435802424,14.7175655496114,
14.8225415113328,14.9273988904908,15.0321931999677,15.1369597244014,15.241733707136,
15.3466206723545,15.4515702920288,15.5567029266591,15.6111166707848,15.7079632679492),
 .UNSPECIFIED.);
#781=B_SPLINE_CURVE_WITH_KNOTS('',3,(#11618,#11619,#11620,#11621,#11622,
#11623,#11624,#11625,#11626,#11627,#11628,#11629,#11630,#11631,#11632,#11633,
#11634,#11635,#11636,#11637,#11638,#11639,#11640,#11641,#11642,#11643,#11644,
#11645,#11646,#11647,#11648,#11649,#11650,#11651,#11652,#11653,#11654,#11655,
#11656,#11657,#11658,#11659,#11660,#11661,#11662,#11663,#11664,#11665,#11666,
#11667,#11668,#11669,#11670,#11671,#11672,#11673,#11674,#11675,#11676,#11677,
#11678,#11679,#11680,#11681,#11682,#11683,#11684,#11685,#11686,#11687,#11688,
#11689,#11690,#11691,#11692,#11693,#11694,#11695,#11696,#11697,#11698,#11699,
#11700,#11701,#11702,#11703,#11704,#11705,#11706,#11707,#11708,#11709,#11710,
#11711,#11712,#11713,#11714,#11715,#11716,#11717,#11718,#11719,#11720,#11721,
#11722,#11723,#11724,#11725,#11726,#11727,#11728,#11729,#11730,#11731,#11732,
#11733,#11734,#11735,#11736,#11737,#11738,#11739,#11740,#11741,#11742,#11743,
#11744,#11745,#11746,#11747,#11748,#11749,#11750,#11751,#11752,#11753,#11754,
#11755,#11756,#11757,#11758,#11759,#11760,#11761,#11762,#11763,#11764,#11765,
#11766,#11767,#11768,#11769,#11770,#11771,#11772,#11773,#11774,#11775,#11776,
#11777,#11778,#11779,#11780,#11781,#11782,#11783,#11784,#11785,#11786,#11787,
#11788,#11789,#11790,#11791,#11792,#11793,#11794,#11795,#11796,#11797,#11798,
#11799,#11800,#11801,#11802,#11803,#11804,#11805,#11806,#11807),
 .UNSPECIFIED.,.F.,.F.,(4,3,3,3,3,3,3,3,3,3,3,3,3,3,3,3,3,3,3,3,3,3,3,3,
3,3,3,3,3,3,3,3,3,3,3,3,3,3,3,3,3,3,3,3,3,3,3,3,3,3,3,3,3,3,3,3,3,3,3,3,
3,3,3,4),(15.7079632682185,15.811428089593,15.914735438257,16.0179561585831,
16.1211276382724,16.2242871927754,16.3275428620763,16.4308476158766,16.5343372072669,
16.6097975391455,16.7147739380985,16.8195927266471,16.9242880341238,17.0289173338591,
17.1335161631907,17.2381200152761,17.3428343171023,17.4476095828744,17.5525670804081,
17.6084784075063,17.7134461555384,17.818256657873,17.9229442656087,18.0275662339299,
18.1321581124525,18.2367554070047,18.3414637991167,18.4462335142689,18.5511860860768,
18.607159275867,18.712084244627,18.8168511407928,18.9214941268238,19.0260708692261,
19.1306169849403,19.2351680465238,19.3398298056802,19.4445525908897,19.5494582685097,
19.6058401442278,19.7107917719691,19.8155856953168,19.9202561227395,20.0248605477511,
20.1294345458482,20.2340136483747,20.3387034974021,20.4434544424511,20.5483880880719,
20.6045210125885,20.7094692639051,20.8142598285881,20.9189269407677,21.0235280793812,
21.1280988250196,21.2326747141547,21.3373614318861,21.4421092875596,21.547039942974,
21.6032018809493,21.720775965361,21.8379258085655,21.9543756998941,21.9911485747582),
 .UNSPECIFIED.);
#782=B_SPLINE_CURVE_WITH_KNOTS('',3,(#11809,#11810,#11811,#11812,#11813,
#11814,#11815,#11816,#11817,#11818,#11819,#11820,#11821,#11822,#11823,#11824,
#11825,#11826,#11827,#11828,#11829,#11830,#11831,#11832,#11833,#11834,#11835,
#11836,#11837,#11838,#11839,#11840,#11841,#11842,#11843,#11844,#11845,#11846,
#11847,#11848,#11849,#11850,#11851,#11852,#11853,#11854,#11855,#11856,#11857,
#11858,#11859,#11860,#11861,#11862,#11863,#11864,#11865,#11866,#11867,#11868,
#11869,#11870,#11871,#11872,#11873,#11874,#11875,#11876,#11877,#11878,#11879,
#11880,#11881,#11882,#11883,#11884,#11885,#11886,#11887,#11888,#11889,#11890,
#11891,#11892,#11893,#11894,#11895,#11896,#11897,#11898,#11899,#11900,#11901,
#11902,#11903,#11904,#11905,#11906,#11907,#11908,#11909,#11910,#11911,#11912,
#11913,#11914,#11915,#11916,#11917,#11918,#11919,#11920,#11921,#11922,#11923,
#11924,#11925,#11926,#11927,#11928,#11929,#11930,#11931,#11932,#11933,#11934,
#11935,#11936,#11937,#11938,#11939,#11940,#11941,#11942,#11943,#11944,#11945,
#11946,#11947,#11948,#11949,#11950,#11951,#11952,#11953,#11954,#11955,#11956,
#11957,#11958,#11959,#11960,#11961,#11962,#11963,#11964,#11965,#11966,#11967,
#11968,#11969,#11970,#11971,#11972,#11973,#11974,#11975,#11976,#11977,#11978,
#11979,#11980,#11981,#11982,#11983,#11984,#11985,#11986,#11987,#11988,#11989,
#11990,#11991,#11992,#11993,#11994,#11995,#11996,#11997,#11998,#11999,#12000,
#12001,#12002,#12003,#12004,#12005,#12006,#12007,#12008,#12009,#12010,#12011,
#12012,#12013,#12014,#12015,#12016,#12017,#12018,#12019,#12020,#12021,#12022,
#12023,#12024,#12025,#12026,#12027,#12028,#12029,#12030,#12031,#12032,#12033,
#12034,#12035,#12036,#12037,#12038,#12039,#12040,#12041,#12042,#12043,#12044,
#12045,#12046,#12047,#12048,#12049,#12050,#12051,#12052,#12053,#12054,#12055,
#12056,#12057,#12058,#12059,#12060,#12061,#12062,#12063,#12064,#12065,#12066,
#12067,#12068,#12069,#12070,#12071,#12072,#12073,#12074,#12075,#12076,#12077,
#12078,#12079,#12080,#12081,#12082,#12083,#12084,#12085,#12086,#12087,#12088,
#12089,#12090,#12091,#12092,#12093,#12094,#12095,#12096,#12097,#12098,#12099,
#12100,#12101,#12102,#12103,#12104,#12105,#12106,#12107,#12108,#12109,#12110,
#12111,#12112,#12113,#12114,#12115,#12116,#12117,#12118,#12119,#12120,#12121,
#12122,#12123,#12124,#12125,#12126,#12127,#12128,#12129,#12130,#12131,#12132,
#12133,#12134,#12135,#12136,#12137,#12138,#12139,#12140,#12141,#12142,#12143,
#12144,#12145,#12146,#12147,#12148,#12149,#12150,#12151,#12152,#12153,#12154,
#12155,#12156,#12157,#12158,#12159,#12160,#12161,#12162,#12163,#12164,#12165,
#12166,#12167,#12168,#12169,#12170,#12171,#12172,#12173,#12174,#12175,#12176,
#12177,#12178,#12179,#12180,#12181,#12182,#12183,#12184,#12185,#12186,#12187,
#12188,#12189,#12190,#12191,#12192,#12193,#12194,#12195,#12196,#12197,#12198,
#12199,#12200,#12201,#12202,#12203,#12204,#12205,#12206,#12207,#12208,#12209,
#12210,#12211,#12212,#12213,#12214,#12215,#12216,#12217,#12218,#12219,#12220,
#12221,#12222,#12223,#12224,#12225,#12226,#12227,#12228,#12229,#12230,#12231,
#12232,#12233,#12234,#12235,#12236,#12237,#12238,#12239,#12240,#12241,#12242,
#12243,#12244,#12245,#12246,#12247,#12248,#12249,#12250,#12251,#12252,#12253,
#12254,#12255,#12256,#12257,#12258,#12259,#12260,#12261,#12262,#12263,#12264,
#12265,#12266,#12267,#12268,#12269,#12270,#12271,#12272,#12273,#12274,#12275,
#12276,#12277,#12278,#12279,#12280,#12281,#12282,#12283,#12284,#12285,#12286,
#12287,#12288,#12289,#12290,#12291,#12292,#12293,#12294,#12295,#12296,#12297,
#12298,#12299,#12300,#12301,#12302,#12303,#12304,#12305,#12306,#12307,#12308,
#12309,#12310,#12311,#12312,#12313,#12314,#12315,#12316,#12317,#12318,#12319,
#12320,#12321,#12322,#12323,#12324,#12325,#12326,#12327,#12328,#12329,#12330,
#12331,#12332,#12333,#12334,#12335,#12336,#12337,#12338,#12339,#12340,#12341,
#12342,#12343,#12344,#12345,#12346,#12347,#12348,#12349,#12350,#12351,#12352,
#12353,#12354,#12355,#12356,#12357,#12358,#12359,#12360,#12361,#12362,#12363,
#12364,#12365,#12366,#12367,#12368,#12369,#12370,#12371,#12372,#12373,#12374,
#12375,#12376,#12377,#12378,#12379,#12380,#12381,#12382,#12383,#12384,#12385,
#12386,#12387,#12388,#12389,#12390,#12391,#12392,#12393,#12394,#12395,#12396,
#12397,#12398,#12399,#12400,#12401,#12402,#12403,#12404,#12405,#12406,#12407,
#12408,#12409,#12410,#12411,#12412,#12413,#12414,#12415,#12416),
 .UNSPECIFIED.,.F.,.F.,(4,2,2,2,2,2,2,2,2,2,2,2,2,2,2,2,2,2,2,2,2,2,2,2,
2,2,2,2,2,2,2,2,2,2,2,2,2,2,2,2,2,2,2,2,2,2,2,2,2,2,2,2,2,2,2,2,2,2,2,2,
2,2,2,2,2,2,2,2,2,2,2,2,2,2,2,2,2,2,2,2,2,2,2,2,2,2,2,2,2,2,2,2,2,2,2,2,
2,2,2,2,2,2,2,2,2,2,2,2,2,2,2,2,2,2,2,2,2,2,2,2,2,2,2,2,2,2,2,2,2,2,2,2,
2,2,2,2,2,2,2,2,2,2,2,2,2,2,2,2,2,2,2,2,2,2,2,2,2,2,2,2,2,2,2,2,2,2,2,2,
2,2,2,2,2,2,2,2,2,2,2,2,2,2,2,2,2,2,2,2,2,2,2,2,2,2,2,2,2,2,2,2,2,2,2,2,
2,2,2,2,2,2,2,2,2,2,2,2,2,2,2,2,2,2,2,2,2,2,2,2,2,2,2,2,2,2,2,2,2,2,2,2,
2,2,2,2,2,2,2,2,2,2,2,2,2,2,2,2,2,2,2,2,2,2,2,2,2,2,2,2,2,2,2,2,2,2,2,2,
2,2,2,2,2,2,2,2,2,2,2,2,2,2,2,2,2,2,2,2,2,2,2,2,2,2,2,4),(-2.50805337380735,
-2.49230273170689,-2.48969515725638,-2.4879721309386,-2.48659029377073,
-2.48515126546709,-2.48348737884313,-2.48066032034544,-2.47014031804258,
-2.46131255950347,-2.40889689640937,-2.38973858595966,-2.38765995750145,
-2.38663577510663,-2.3859045573641,-2.38511438624379,-2.38371722160485,
-2.37960653916059,-2.37860162748433,-2.3222694492425,-2.30245221453362,
-2.29522363888922,-2.29170703733424,-2.28960480204464,-2.28770806645155,
-2.28627238891754,-2.28490219428901,-2.28264369422874,-2.27689552789189,
-2.22137667587684,-2.1916881195377,-2.18880591033304,-2.18763568819163,
-2.18680623008844,-2.1860455866488,-2.18500117444484,-2.18291596846972,
-2.14876053791525,-2.1178653742566,-2.10159810517336,-2.09529398652869,
-2.09210979879743,-2.08945125019766,-2.08785303254331,-2.08785093934229,
-2.0878488397909,-2.08784673385193,-2.08784462155868,-2.0878425028829,-2.0878403777653,
-2.08783824622176,-2.08783610820019,-2.08783396366588,-2.08783181260181,
-2.08782965498483,-2.08782749082695,-2.08782532007492,-2.08782314271334,
-2.08782095871419,-2.08781876805332,-2.08781657070027,-2.08781436666209,
-2.08781215587453,-2.08780993835682,-2.08780771406652,-2.08780548298024,
-2.08780324506971,-2.08780100030342,-2.08779874865347,-2.08779649013827,
-2.0877942246835,-2.08779195229483,-2.08778967297212,-2.08634066469234,
-2.08449390550047,-2.08072308135107,-2.03402038592985,-2.00653898731637,
-1.9961716280542,-1.9903904965275,-1.98886923505029,-1.98796392091759,-1.98715148560001,
-1.98610210483188,-1.98383736749652,-1.94695335185385,-1.91696677325285,
-1.90185087497643,-1.89278335120487,-1.89018523071595,-1.88858848222102,
-1.8871363836171,-1.88526461484418,-1.88136693562351,-1.84296374730564,
-1.79657849051826,-1.79115166780097,-1.78966324424563,-1.78876520308745,
-1.78795067234804,-1.78688713195961,-1.78509707432152,-1.77383818049552,
-1.74838851190093,-1.71819206758287,-1.70281662861806,-1.69363585299979,
-1.69102610016798,-1.68942661162368,-1.68797491332695,-1.68610771508234,
-1.6822342631551,-1.64915564899741,-1.5975695252565,-1.59198976269645,-1.5904866869202,
-1.58958526941551,-1.5887715230805,-1.58771408496146,-1.58540738824961,
-1.5508353436415,-1.52006751265106,-1.4981887322564,-1.49323177999542,-1.49116794194978,
-1.48968436913414,-1.48833729828806,-1.48654141881142,-1.48216442033558,
-1.44993549698197,-1.39834760789211,-1.39275742684445,-1.39125326555121,
-1.39035154043785,-1.38953774776987,-1.38848056358157,-1.38617565771471,
-1.35145634724781,-1.32073184702012,-1.30469208490277,-1.2952253147138,
-1.29258696752626,-1.29098084839678,-1.2895302075669,-1.28767419944753,
-1.28385912536044,-1.25453762319655,-1.1967637902322,-1.19312165145767,
-1.19179344163707,-1.19101672620502,-1.19019756487045,-1.18908724020945,
-1.18655667564878,-1.15717917947136,-1.1339161099299,-1.09807467424259,
-1.094175968587,-1.09230333233862,-1.09085039390555,-1.08925255355955,-1.08665227837795,
-1.07757348969028,-1.06243290354129,-1.03238989762332,-0.995502802853251,
-0.993236619013654,-0.992186568320054,-0.991373618131902,-0.990467727025134,
-0.988945494002023,-0.983160557136287,-0.97278766769267,-0.945274881694213,
-0.898600441098291,-0.894828999092631,-0.892981442106069,-0.891531580964151,
-0.889920331307093,-0.887259734936026,-0.877563991373871,-0.86098076644573,
-0.82980243985953,-0.808407164941538,-0.805752070845725,-0.795700104316496,
-0.79396993004971,-0.792923752278704,-0.792111359758195,-0.791203402432694,
-0.789671768476562,-0.783780927678264,-0.773138525470895,-0.744491827041945,
-0.741424236279186,-0.699520288687299,-0.695648557225166,-0.693781254131466,
-0.692329057180731,-0.690728596884312,-0.688116304638167,-0.678916926780116,
-0.663498563055043,-0.633233954902853,-0.597017005719636,-0.594963104977835,
-0.593926315465913,-0.5931673840357,-0.592335664456485,-0.591155058594924,
-0.588210865063239,-0.584013178187592,-0.572202787995784,-0.542638995593051,
-0.500258447646521,-0.496391265845604,-0.494524840414645,-0.493072738267317,
-0.491471786913485,-0.488857345596995,-0.479636611977521,-0.464168956172589,
-0.433864913736107,-0.397771946191372,-0.395711701123519,-0.394673302083384,
-0.393913951394184,-0.393100322575271,-0.391957752399258,-0.390661291750234,
-0.388385686170942,-0.370466231470168,-0.332351007882784,-0.300982830065597,
-0.297131949164991,-0.29526870170595,-0.293816971609142,-0.292214297166831,
-0.289592201290835,-0.280294570895473,-0.264648719319465,-0.232866047653858,
-0.198560638514461,-0.196276962117871,-0.195207397497434,-0.194414312381531,
-0.194411525380222,-0.194408761899535,-0.194406018888907,-0.194403296127436,
-0.19440059339051,-0.194397910449151,-0.194395247063212,-0.194392603040179,
-0.194389978160289,-0.194387372207587,-0.194384784989408,-0.194382216307084,
-0.194379665966285,-0.194377133762692,-0.194374619504514,-0.194372122989017,
-0.19436964403352,-0.194367182443886,-0.194364738048061,-0.194362310675196,
-0.194359900137987,-0.194357506291771,-0.19435512892716,-0.194352767874405,
-0.194350422980133,-0.194348094073647,-0.194345780996807,-0.194343483581033,
-0.194341201674791,-0.194338935147501,-0.194336683807319,-0.194334447512859,
-0.194332226142063,-0.194330019516081,-0.194327827484882,-0.194325649918364,
-0.19432348668219,-0.194321331401382,-0.19431917752624,-0.194317037259404,
-0.193412541854142,-0.19245195608457,-0.190997705163816,-0.188322135206659,
-0.163703582311514,-0.130284239582554,-0.127728967988652,-0.116358897600143,
-0.100614438954047,-0.0976565302774177,-0.0957990029368107,-0.0943452047780524,
-0.0927335711596283,-0.0900815323075606,-0.0805162837021464,-0.0642572066088759,
-0.035656491744088,-0.000592665341133465),.UNSPECIFIED.);
#783=B_SPLINE_CURVE_WITH_KNOTS('',3,(#12418,#12419,#12420,#12421,#12422,
#12423,#12424,#12425,#12426,#12427,#12428,#12429,#12430,#12431,#12432,#12433,
#12434,#12435,#12436,#12437,#12438,#12439,#12440,#12441,#12442,#12443,#12444,
#12445,#12446,#12447,#12448,#12449,#12450,#12451,#12452,#12453,#12454,#12455,
#12456,#12457,#12458,#12459,#12460,#12461,#12462,#12463,#12464,#12465,#12466,
#12467,#12468,#12469,#12470,#12471,#12472,#12473,#12474,#12475,#12476,#12477,
#12478,#12479,#12480,#12481,#12482,#12483,#12484,#12485,#12486,#12487,#12488,
#12489,#12490,#12491,#12492,#12493,#12494,#12495,#12496,#12497,#12498,#12499,
#12500,#12501,#12502,#12503,#12504,#12505,#12506,#12507,#12508,#12509,#12510,
#12511,#12512,#12513,#12514,#12515,#12516,#12517,#12518,#12519,#12520,#12521,
#12522,#12523,#12524,#12525,#12526,#12527,#12528,#12529,#12530,#12531,#12532,
#12533,#12534,#12535,#12536,#12537,#12538,#12539,#12540,#12541,#12542,#12543,
#12544,#12545,#12546,#12547,#12548,#12549,#12550,#12551,#12552,#12553,#12554,
#12555,#12556,#12557,#12558,#12559,#12560,#12561,#12562,#12563,#12564,#12565,
#12566,#12567,#12568,#12569,#12570,#12571,#12572,#12573,#12574,#12575,#12576,
#12577,#12578,#12579,#12580,#12581,#12582,#12583,#12584,#12585,#12586,#12587,
#12588,#12589,#12590,#12591,#12592,#12593,#12594,#12595,#12596,#12597,#12598,
#12599,#12600,#12601,#12602,#12603,#12604,#12605,#12606,#12607,#12608,#12609,
#12610,#12611,#12612,#12613,#12614,#12615,#12616,#12617,#12618,#12619,#12620,
#12621,#12622,#12623,#12624,#12625,#12626,#12627,#12628,#12629,#12630,#12631,
#12632,#12633,#12634,#12635,#12636,#12637,#12638,#12639,#12640,#12641,#12642,
#12643,#12644,#12645,#12646,#12647,#12648,#12649,#12650,#12651,#12652,#12653,
#12654,#12655,#12656,#12657,#12658,#12659,#12660,#12661,#12662,#12663,#12664,
#12665,#12666,#12667,#12668,#12669,#12670,#12671,#12672,#12673,#12674,#12675,
#12676,#12677,#12678,#12679,#12680,#12681,#12682,#12683,#12684,#12685,#12686,
#12687,#12688,#12689,#12690,#12691,#12692,#12693,#12694,#12695,#12696,#12697,
#12698,#12699,#12700,#12701,#12702,#12703,#12704,#12705,#12706,#12707,#12708,
#12709,#12710,#12711,#12712,#12713,#12714,#12715,#12716,#12717,#12718,#12719,
#12720,#12721,#12722,#12723,#12724,#12725,#12726,#12727,#12728,#12729,#12730,
#12731,#12732,#12733,#12734,#12735,#12736,#12737,#12738,#12739,#12740,#12741,
#12742,#12743,#12744,#12745,#12746,#12747,#12748,#12749,#12750,#12751,#12752,
#12753,#12754,#12755,#12756,#12757,#12758,#12759,#12760,#12761,#12762,#12763,
#12764,#12765,#12766,#12767,#12768,#12769,#12770,#12771,#12772,#12773,#12774,
#12775,#12776,#12777,#12778,#12779,#12780,#12781,#12782,#12783,#12784,#12785,
#12786,#12787,#12788,#12789,#12790,#12791,#12792,#12793,#12794,#12795,#12796,
#12797,#12798,#12799,#12800,#12801,#12802,#12803,#12804,#12805,#12806,#12807,
#12808,#12809,#12810,#12811,#12812,#12813,#12814,#12815,#12816,#12817,#12818,
#12819,#12820,#12821,#12822,#12823,#12824,#12825,#12826,#12827,#12828,#12829,
#12830,#12831,#12832,#12833,#12834,#12835,#12836,#12837,#12838,#12839,#12840,
#12841,#12842,#12843,#12844,#12845,#12846,#12847,#12848,#12849,#12850,#12851,
#12852,#12853,#12854,#12855,#12856,#12857,#12858,#12859,#12860,#12861,#12862,
#12863,#12864,#12865,#12866,#12867,#12868,#12869,#12870,#12871,#12872,#12873,
#12874,#12875,#12876,#12877,#12878,#12879,#12880,#12881,#12882,#12883,#12884,
#12885,#12886,#12887,#12888,#12889,#12890,#12891,#12892,#12893,#12894,#12895,
#12896,#12897,#12898,#12899,#12900,#12901,#12902,#12903,#12904,#12905,#12906,
#12907,#12908,#12909),.UNSPECIFIED.,.F.,.F.,(4,2,2,2,2,2,2,2,2,2,2,2,2,
2,2,2,2,2,2,2,2,2,2,2,2,2,2,2,2,2,2,2,2,2,2,2,2,2,2,2,2,2,2,2,2,2,2,2,2,
2,2,2,2,2,2,2,2,2,2,2,2,2,2,2,2,2,2,2,2,2,2,2,2,2,2,2,2,2,2,2,2,2,2,2,2,
2,2,2,2,2,2,2,2,2,2,2,2,2,2,2,2,2,2,2,2,2,2,2,2,2,2,2,2,2,2,2,2,2,2,2,2,
2,2,2,2,2,2,2,2,2,2,2,2,2,2,2,2,2,2,2,2,2,2,2,2,2,2,2,2,2,2,2,2,2,2,2,2,
2,2,2,2,2,2,2,2,2,2,2,2,2,2,2,2,2,2,2,2,2,2,2,2,2,2,2,2,2,2,2,2,2,2,2,2,
2,2,2,2,2,2,2,2,2,2,2,2,2,2,2,2,2,2,2,2,2,2,2,2,2,2,2,2,2,2,2,2,2,2,2,2,
2,2,2,2,2,2,2,2,2,2,2,2,2,2,2,2,4),(-2.51449948729211,-2.51245742096797,
-2.51061254852901,-2.50973662496859,-2.50897977983815,-2.50817611630024,
-2.50709184495005,-2.50464863086608,-2.49736079827815,-2.43600423275735,
-2.42198602286685,-2.41630664148812,-2.41202729179934,-2.41007973372854,
-2.408613371016,-2.40723399121773,-2.40494158741794,-2.39900458656281,-2.39759431139554,
-2.39608371647185,-2.33741201082973,-2.3201346327642,-2.31470662092676,
-2.31228686925975,-2.31093234574058,-2.31001298729218,-2.30913822866073,
-2.30834546992963,-2.30728046796092,-2.30494243833302,-2.27214770724904,
-2.2489473218388,-2.2409053178807,-2.22380423309859,-2.21388477089582,-2.21119889511119,
-2.20957950714353,-2.20812690054294,-2.20628210177226,-2.20336656711075,
-2.188303011828,-2.17682904014002,-2.14042730567403,-2.11553578670406,-2.11284518726927,
-2.11138506192809,-2.11042195172882,-2.10951632865074,-2.10872779131837,
-2.1076988358432,-2.10560607879394,-2.09209250198751,-2.04168953094803,
-2.02422138514964,-2.01415081277562,-2.01145108418384,-2.00982864728293,
-2.0083766715546,-2.00653724843925,-2.0029411636405,-1.98014760140986,-1.9623937442954,
-1.93217889705929,-1.91910968361099,-1.91230943946295,-1.91070047704902,
-1.90977394375718,-1.90896273309397,-1.90792389918225,-1.90578131939415,
-1.8909466574496,-1.88653169529326,-1.87007017003166,-1.83949140380663,
-1.82369833128006,-1.81433011517413,-1.81169688981154,-1.81008923901227,
-1.80863419047183,-1.80676833972365,-1.80291801865423,-1.77211249823417,
-1.73153198660517,-1.719117960203,-1.71255380938743,-1.71096315804416,-1.710040646829,
-1.70922871323626,-1.70818333293725,-1.70600772096888,-1.69023348051677,
-1.66959046461123,-1.63926779094241,-1.62380050377503,-1.61457250995358,
-1.61195305120826,-1.61034839914475,-1.60889252872627,-1.60702068407316,
-1.60314019668699,-1.56069512871391,-1.53108282145904,-1.5135959027296,
-1.51154519055792,-1.51052466477915,-1.50979201583859,-1.50899628348168,
-1.5075792224838,-1.50332150287926,-1.46624854650443,-1.4418704551102,-1.42483125028608,
-1.4149372029657,-1.41225354892351,-1.41063457481892,-1.40918174892876,
-1.40733586555799,-1.40441702975491,-1.38930231686929,-1.38794839531444,
-1.33062653857943,-1.3137654998109,-1.31172855433181,-1.31071072927696,
-1.30997832829005,-1.30918115719914,-1.30775731001858,-1.30344929266811,
-1.25785937239113,-1.2171369254388,-1.21323985352464,-1.21136463739186,
-1.20990820256701,-1.20830500822037,-1.20569262227685,-1.19653728443282,
-1.18123583028555,-1.15101685625293,-1.11432620337532,-1.1120473787042,
-1.11099331972636,-1.11017807622191,-1.10927051609357,-1.10774742299906,
-1.10198181890987,-1.09166875381194,-1.0643494610083,-1.01714225872614,
-1.01337196742147,-1.01152177631739,-1.01006838412468,-1.00845169892891,
-1.00577862394998,-0.995998920906617,-0.979232241927195,-0.947863776094077,
-0.924854128346121,-0.914056222225798,-0.912284831191914,-0.911225110715698,
-0.910409112867163,-0.909504661201476,-0.907995351107947,-0.90237923585557,
-0.850674115830689,-0.817525165090444,-0.813640757158348,-0.811768131788582,
-0.810312148537813,-0.808707872523479,-0.806090159442023,-0.796879927679856,
-0.781451411650063,-0.751132685824435,-0.72554856158458,-0.714307045544392,
-0.712514089626195,-0.71144809666393,-0.710631244395518,-0.70973014661502,
-0.708235640511882,-0.702775601862105,-0.655910395233093,-0.617792579854328,
-0.613882657375662,-0.612005119749211,-0.610548593944236,-0.608947025640125,
-0.606341171811046,-0.597247804078683,-0.582087632069768,-0.551985319982088,
-0.514967259461071,-0.512695679389054,-0.511643092190335,-0.510828161925047,
-0.509920045737665,-0.508394035767894,-0.502594301901003,-0.492194384507113,
-0.464603828324921,-0.417833286691694,-0.4140496236272,-0.412196956943016,
-0.410781845014496,-0.409212536105932,-0.40757390901953,-0.405173753278498,
-0.400927596133162,-0.366829982625952,-0.325468660259128,-0.314706051457623,
-0.31293654470393,-0.311877435620106,-0.311061596313918,-0.310156980416095,
-0.308646661181059,-0.30301854278585,-0.251322733646518,-0.218195080654549,
-0.214306874924167,-0.212433626118568,-0.211016648592563,-0.209458885398998,
-0.207835875541873,-0.20547345865871,-0.201321565531384,-0.192246616068802,
-0.164335151817066,-0.118213310571157,-0.113931715412101,-0.112511519595434,
-0.111715177432494,-0.110982729485826,-0.109963633725146,-0.107919864809402,
-0.0907426186945712,-0.0254247461540436,-0.0166005131250681,-0.0137791143661076,
-0.0121133850868176,-0.0106716918028777,-0.00928465068694093,-0.00755312402976869,
-0.00448544524035413,-0.000592059025150225),.UNSPECIFIED.);
#784=B_SPLINE_CURVE_WITH_KNOTS('',3,(#12911,#12912,#12913,#12914,#12915,
#12916,#12917,#12918,#12919,#12920,#12921,#12922,#12923,#12924,#12925,#12926,
#12927,#12928,#12929,#12930,#12931,#12932,#12933,#12934,#12935,#12936,#12937,
#12938,#12939,#12940,#12941,#12942,#12943,#12944,#12945,#12946,#12947,#12948,
#12949,#12950,#12951,#12952,#12953,#12954,#12955,#12956,#12957,#12958,#12959,
#12960,#12961,#12962,#12963,#12964,#12965,#12966,#12967,#12968,#12969,#12970,
#12971,#12972,#12973,#12974,#12975,#12976,#12977,#12978,#12979,#12980,#12981,
#12982,#12983,#12984,#12985,#12986,#12987,#12988,#12989,#12990,#12991,#12992,
#12993,#12994,#12995,#12996,#12997,#12998,#12999,#13000,#13001,#13002,#13003,
#13004,#13005,#13006,#13007,#13008,#13009,#13010,#13011,#13012,#13013,#13014,
#13015,#13016,#13017,#13018,#13019,#13020,#13021,#13022,#13023,#13024,#13025,
#13026,#13027,#13028,#13029,#13030,#13031,#13032,#13033,#13034,#13035,#13036,
#13037,#13038,#13039,#13040,#13041,#13042,#13043,#13044,#13045,#13046,#13047,
#13048,#13049,#13050,#13051,#13052,#13053,#13054,#13055,#13056,#13057,#13058,
#13059,#13060,#13061,#13062,#13063,#13064,#13065,#13066,#13067,#13068,#13069,
#13070,#13071,#13072,#13073,#13074,#13075,#13076,#13077,#13078,#13079,#13080,
#13081,#13082,#13083,#13084,#13085,#13086,#13087,#13088,#13089,#13090,#13091,
#13092,#13093,#13094,#13095,#13096,#13097,#13098,#13099,#13100,#13101,#13102,
#13103,#13104,#13105,#13106,#13107,#13108,#13109,#13110,#13111,#13112,#13113,
#13114,#13115,#13116,#13117,#13118,#13119,#13120,#13121,#13122,#13123,#13124,
#13125,#13126,#13127,#13128,#13129,#13130,#13131,#13132,#13133,#13134,#13135,
#13136,#13137,#13138,#13139,#13140,#13141,#13142,#13143,#13144,#13145,#13146,
#13147,#13148,#13149,#13150,#13151,#13152,#13153,#13154,#13155,#13156,#13157,
#13158,#13159,#13160,#13161,#13162,#13163,#13164,#13165,#13166,#13167,#13168,
#13169,#13170,#13171,#13172,#13173,#13174,#13175,#13176,#13177,#13178,#13179,
#13180,#13181,#13182,#13183,#13184,#13185,#13186,#13187,#13188,#13189,#13190,
#13191,#13192,#13193,#13194,#13195,#13196,#13197,#13198,#13199,#13200,#13201,
#13202,#13203,#13204,#13205,#13206,#13207,#13208,#13209,#13210,#13211,#13212,
#13213,#13214,#13215,#13216,#13217,#13218,#13219,#13220,#13221,#13222,#13223,
#13224,#13225,#13226,#13227,#13228,#13229,#13230,#13231,#13232,#13233,#13234,
#13235,#13236,#13237,#13238,#13239,#13240,#13241,#13242,#13243,#13244,#13245,
#13246,#13247,#13248,#13249,#13250,#13251,#13252,#13253,#13254,#13255,#13256,
#13257,#13258,#13259,#13260,#13261,#13262,#13263,#13264,#13265,#13266,#13267,
#13268,#13269,#13270,#13271,#13272,#13273,#13274,#13275,#13276,#13277,#13278,
#13279,#13280,#13281,#13282,#13283,#13284,#13285,#13286,#13287,#13288,#13289,
#13290,#13291,#13292,#13293,#13294,#13295,#13296,#13297,#13298,#13299,#13300,
#13301,#13302,#13303,#13304,#13305,#13306,#13307,#13308,#13309,#13310,#13311,
#13312,#13313,#13314,#13315,#13316,#13317,#13318,#13319,#13320,#13321,#13322,
#13323,#13324,#13325,#13326,#13327,#13328,#13329,#13330,#13331,#13332,#13333,
#13334,#13335,#13336,#13337,#13338,#13339,#13340,#13341,#13342,#13343,#13344,
#13345,#13346,#13347,#13348,#13349,#13350,#13351,#13352,#13353,#13354,#13355,
#13356,#13357,#13358,#13359,#13360,#13361,#13362,#13363,#13364,#13365,#13366,
#13367,#13368,#13369,#13370,#13371,#13372,#13373,#13374,#13375,#13376,#13377,
#13378,#13379,#13380,#13381,#13382,#13383,#13384,#13385,#13386,#13387,#13388,
#13389,#13390,#13391,#13392,#13393,#13394,#13395,#13396,#13397,#13398,#13399,
#13400,#13401,#13402,#13403,#13404,#13405,#13406,#13407,#13408,#13409,#13410,
#13411,#13412,#13413,#13414,#13415,#13416,#13417,#13418,#13419,#13420,#13421,
#13422,#13423,#13424,#13425,#13426,#13427,#13428,#13429,#13430,#13431,#13432,
#13433,#13434,#13435,#13436,#13437,#13438,#13439,#13440,#13441,#13442,#13443,
#13444,#13445,#13446,#13447,#13448,#13449,#13450,#13451,#13452,#13453,#13454,
#13455,#13456,#13457,#13458,#13459,#13460,#13461,#13462,#13463,#13464,#13465,
#13466,#13467,#13468,#13469,#13470),.UNSPECIFIED.,.F.,.F.,(4,2,2,2,2,2,
2,2,2,2,2,2,2,2,2,2,2,2,2,2,2,2,2,2,2,2,2,2,2,2,2,2,2,2,2,2,2,2,2,2,2,2,
2,2,2,2,2,2,2,2,2,2,2,2,2,2,2,2,2,2,2,2,2,2,2,2,2,2,2,2,2,2,2,2,2,2,2,2,
2,2,2,2,2,2,2,2,2,2,2,2,2,2,2,2,2,2,2,2,2,2,2,2,2,2,2,2,2,2,2,2,2,2,2,2,
2,2,2,2,2,2,2,2,2,2,2,2,2,2,2,2,2,2,2,2,2,2,2,2,2,2,2,2,2,2,2,2,2,2,2,2,
2,2,2,2,2,2,2,2,2,2,2,2,2,2,2,2,2,2,2,2,2,2,2,2,2,2,2,2,2,2,2,2,2,2,2,2,
2,2,2,2,2,2,2,2,2,2,2,2,2,2,2,2,2,2,2,2,2,2,2,2,2,2,2,2,2,2,2,2,2,2,2,2,
2,2,2,2,2,2,2,2,2,2,2,2,2,2,2,2,2,2,2,2,2,2,2,2,2,2,2,2,2,2,2,2,2,2,2,2,
2,2,2,2,2,2,2,2,2,2,2,2,2,2,2,2,2,2,2,2,2,4),(-2.5133074761937,-2.441555832099,
-2.43219700810938,-2.42681902880013,-2.42533266847067,-2.42443353536165,
-2.42361637074292,-2.42254718197082,-2.42018595794761,-2.39121580926245,
-2.34792394817552,-2.33617687934896,-2.3311727316177,-2.32847494043576,
-2.32671218564173,-2.32505389769471,-2.32504508548084,-2.32503600427534,
-2.32502664341511,-2.32501699170266,-2.32500703733442,-2.32499676787873,
-2.3249861702373,-2.32497523060133,-2.32496393437945,-2.32495226617438,
-2.32494020970075,-2.32492774773434,-2.32491486204446,-2.32490153330995,
-2.32488774103758,-2.32487346348351,-2.32485867755953,-2.32484335869554,
-2.32482748076776,-2.32481101594265,-2.32479393454356,-2.32477620491566,
-2.32475896654083,-2.32333589174628,-2.321460035164,-2.31755605394049,-2.27869596130949,
-2.24834868319983,-2.23447723940278,-2.22739641827667,-2.22576694247466,
-2.22483610999621,-2.22402591651849,-2.22299462874836,-2.22095770062709,
-2.20816111595958,-2.18700987266577,-2.17038681340108,-2.13515370387584,
-2.13083729755746,-2.12840938402946,-2.12675951424038,-2.12518127770065,
-2.12517870958474,-2.12517613590436,-2.12517355664914,-2.12517097178146,
-2.12516838128418,-2.12516578513021,-2.12516318329547,-2.12516057573989,
-2.12515796242268,-2.12515534335618,-2.12515271849187,-2.12515008778882,
-2.12514745123588,-2.1251448088156,-2.12514216049822,-2.12513950625008,
-2.12513684606595,-2.12371424003327,-2.12184859059502,-2.11799683870704,
-2.08741769049248,-2.04658044022541,-2.02847933353453,-2.02641649909527,
-2.02539381855083,-2.0246611862245,-2.02386704362522,-2.02245666682299,
-2.01824590338492,-1.97106640892096,-1.93225028719694,-1.92810637194275,
-1.92618446828063,-1.92472236551103,-1.92333580465476,-1.92100471279583,
-1.91482168646161,-1.86403239719211,-1.84401870749798,-1.83362464717951,
-1.82782852516163,-1.82630326547405,-1.82539556127737,-1.82458097320294,
-1.82352880023793,-1.82125799240373,-1.78426364310036,-1.7542030781551,
-1.73905350948089,-1.7299647701368,-1.7273600580679,-1.72575914844842,-1.72430319306596,
-1.7224263505851,-1.71851773239354,-1.68192145721908,-1.64834601727162,
-1.63516495038078,-1.62832568720609,-1.62671412288149,-1.62578720681989,
-1.62497637810595,-1.62393897560121,-1.6218025756197,-1.60712290464845,
-1.60029621715297,-1.56825310490145,-1.53276288128461,-1.52870911967694,
-1.5268042307376,-1.52534447490756,-1.52395216063469,-1.52159195091537,
-1.5152769185501,-1.46739197314248,-1.44466705664436,-1.43427444242065,
-1.42847876548993,-1.42695347049625,-1.42604571575525,-1.42523106202492,
-1.42417877761964,-1.42190762795816,-1.38498712089924,-1.35489793428018,
-1.33971446878164,-1.33061074931315,-1.32800439622865,-1.32640304449159,
-1.32494705989569,-1.3230707040528,-1.3191650099287,-1.28364898803709,-1.25677039865494,
-1.23018470300706,-1.22782787358406,-1.22675957218805,-1.2259426227575,
-1.22504321998997,-1.22355535097764,-1.21816054715107,-1.20876178144355,
-1.18509721528406,-1.13669402191702,-1.13312494064002,-1.12923221778222,
-1.127358446439,-1.12590284564956,-1.12430027831388,-1.12168825787642,-1.11252755743439,
-1.09721068951628,-1.06698895462862,-1.03037327834174,-1.02809531007372,
-1.02704174612925,-1.02622692881707,-1.02531989058121,-1.02379777713794,
-1.01803708377352,-1.0077341395947,-0.980443641753844,-0.933239695903948,
-0.929472018027414,-0.927622934675346,-0.926170332624233,-0.924554443662548,
-0.921882493388162,-0.912104790489056,-0.895339347707471,-0.863981650724361,
-0.840940515189588,-0.830204597071183,-0.828436943297607,-0.827378608380033,
-0.826563162586575,-0.825658762094295,-0.824148324395362,-0.818514387620214,
-0.808528388329783,-0.78239582334916,-0.737475832326166,-0.733044440688509,
-0.729953077599993,-0.728075807321763,-0.726615502143086,-0.725030305574051,
-0.722496127661981,-0.714079186548939,-0.700433685809388,-0.643888818912175,
-0.630666927842235,-0.62858656435679,-0.627560284633167,-0.626750416700883,
-0.625815883886836,-0.624170057721989,-0.616864155793498,-0.602337381510688,
-0.554123147982252,-0.551429760952961,-0.547762815398685,-0.532944965303936,
-0.530045318924305,-0.528205702807971,-0.526754093300621,-0.525132606144415,
-0.522435727593154,-0.51239039311322,-0.494978813004558,-0.445074893535946,
-0.442579302647778,-0.430843063091563,-0.428851742265716,-0.42783011462256,
-0.4270205994022,-0.426101552224707,-0.424502668789999,-0.422533668695574,
-0.418452908497334,-0.407126561129945,-0.364998365998589,-0.334249169226604,
-0.330400864980992,-0.328535712729009,-0.3270810829575,-0.325473766543612,
-0.322840797388725,-0.313470518026063,-0.297668595149222,-0.243952725511428,
-0.231176502133581,-0.22913996781967,-0.228108593270446,-0.227298187809366,
-0.226535598454271,-0.225123886017466,-0.220432093983249,-0.212635786302988,
-0.186615885237806,-0.138120559031465,-0.134904660180586,-0.130784213489283,
-0.128887130089909,-0.127423562048058,-0.12584687539658,-0.123352090594298,
-0.115292947584701,-0.102424886580751,-0.0586127148397013,-0.0515117662900704,
-0.04696108305432,-0.0316015194634914,-0.0294403804906191,-0.0283979769820426,
-0.0275865104888005,-0.026825222637773,-0.0259135837775704,-0.0245776869027071,
-0.0192352251262995,-0.000591822641302136),.UNSPECIFIED.);
#785=B_SPLINE_CURVE_WITH_KNOTS('',3,(#13472,#13473,#13474,#13475,#13476,
#13477,#13478,#13479,#13480,#13481,#13482,#13483,#13484,#13485,#13486,#13487,
#13488,#13489,#13490,#13491,#13492,#13493,#13494,#13495,#13496,#13497,#13498,
#13499,#13500,#13501,#13502,#13503,#13504,#13505,#13506,#13507,#13508,#13509,
#13510,#13511,#13512,#13513,#13514,#13515,#13516,#13517,#13518,#13519,#13520,
#13521,#13522,#13523,#13524,#13525,#13526,#13527,#13528,#13529,#13530,#13531,
#13532,#13533,#13534,#13535,#13536,#13537,#13538,#13539,#13540,#13541,#13542,
#13543,#13544,#13545,#13546,#13547,#13548,#13549,#13550,#13551,#13552,#13553,
#13554,#13555,#13556,#13557,#13558,#13559,#13560,#13561,#13562,#13563,#13564,
#13565,#13566,#13567,#13568,#13569,#13570,#13571,#13572,#13573,#13574,#13575,
#13576,#13577,#13578,#13579,#13580,#13581,#13582,#13583,#13584,#13585,#13586,
#13587,#13588,#13589,#13590,#13591,#13592,#13593,#13594,#13595,#13596,#13597,
#13598,#13599,#13600,#13601,#13602,#13603,#13604,#13605,#13606,#13607,#13608,
#13609,#13610,#13611,#13612,#13613,#13614,#13615,#13616,#13617,#13618,#13619,
#13620,#13621,#13622,#13623,#13624,#13625,#13626,#13627,#13628,#13629,#13630,
#13631,#13632,#13633,#13634,#13635,#13636,#13637,#13638,#13639,#13640,#13641,
#13642,#13643,#13644,#13645,#13646,#13647,#13648,#13649,#13650,#13651,#13652,
#13653,#13654,#13655,#13656,#13657,#13658,#13659,#13660,#13661),
 .UNSPECIFIED.,.F.,.F.,(4,3,3,3,3,3,3,3,3,3,3,3,3,3,3,3,3,3,3,3,3,3,3,3,
3,3,3,3,3,3,3,3,3,3,3,3,3,3,3,3,3,3,3,3,3,3,3,3,3,3,3,3,3,3,3,3,3,3,3,3,
3,3,3,4),(59.6902604186975,59.7979473347376,59.9011330896705,60.0042464287171,
60.1073248025605,60.2104056071731,60.31359111605,60.4168388149509,60.5202570165798,
60.5517557470186,60.6567015618828,60.7614896268816,60.8661541575229,60.9707526653145,
61.0753207347265,61.1798939060593,61.2845778611266,61.3893229245271,61.4942507709874,
61.5504366153793,61.6553824302435,61.7601704952422,61.8648350258835,61.9694335336753,
62.0740016030872,62.1785747744198,62.283258729487,62.3880037928878,62.4929316393481,
62.5491174837401,62.6540632986043,62.7588513636033,62.8635158942446,62.9681144020364,
63.0726824714484,63.1772556427811,63.2819395978483,63.3866846612489,63.4916125077092,
63.5477983521008,63.6527441669649,63.7575322319637,63.862196762605,63.9667952703968,
64.0713633398087,64.1759365111414,64.2806204662085,64.3853655296093,64.4902933760696,
64.5464792204616,64.6514250353258,64.7562131003246,64.8608776309659,64.9654761387577,
65.0700442081696,65.1746173795019,65.2793013345691,65.3840463979698,65.4889742444302,
65.5451600888223,65.6595690390446,65.7736658819306,65.8872569368679,65.9734457253859),
 .UNSPECIFIED.);
#786=B_SPLINE_CURVE_WITH_KNOTS('',3,(#13663,#13664,#13665,#13666,#13667,
#13668,#13669,#13670,#13671,#13672),.UNSPECIFIED.,.F.,.F.,(4,1,1,1,1,1,
1,4),(65.9734457253859,66.5438409571831,67.5425218255438,68.5412026939046,
69.5398835622653,70.5385644306261,71.5372452989868,72.2566310325655),
 .UNSPECIFIED.);
#787=B_SPLINE_CURVE_WITH_KNOTS('',3,(#13674,#13675,#13676,#13677,#13678,
#13679,#13680,#13681,#13682,#13683,#13684,#13685,#13686,#13687,#13688,#13689,
#13690,#13691,#13692,#13693,#13694,#13695,#13696,#13697,#13698,#13699,#13700,
#13701,#13702,#13703,#13704,#13705,#13706,#13707,#13708,#13709,#13710,#13711,
#13712,#13713,#13714,#13715,#13716,#13717,#13718,#13719,#13720,#13721,#13722,
#13723,#13724,#13725,#13726,#13727,#13728,#13729,#13730,#13731,#13732,#13733,
#13734,#13735,#13736,#13737,#13738,#13739,#13740,#13741,#13742,#13743,#13744,
#13745,#13746,#13747,#13748,#13749,#13750,#13751,#13752,#13753,#13754,#13755,
#13756,#13757,#13758,#13759,#13760,#13761,#13762,#13763,#13764,#13765,#13766,
#13767,#13768,#13769,#13770,#13771,#13772,#13773,#13774,#13775,#13776,#13777,
#13778,#13779,#13780,#13781,#13782,#13783,#13784,#13785,#13786,#13787,#13788,
#13789,#13790,#13791,#13792,#13793,#13794,#13795,#13796,#13797,#13798,#13799,
#13800,#13801,#13802,#13803,#13804,#13805,#13806,#13807,#13808,#13809,#13810,
#13811,#13812,#13813,#13814,#13815,#13816,#13817,#13818,#13819,#13820,#13821,
#13822,#13823,#13824,#13825,#13826,#13827,#13828,#13829,#13830,#13831,#13832,
#13833,#13834,#13835,#13836,#13837,#13838,#13839,#13840,#13841,#13842,#13843,
#13844,#13845,#13846,#13847,#13848,#13849,#13850,#13851,#13852,#13853,#13854,
#13855,#13856,#13857,#13858,#13859,#13860,#13861,#13862,#13863,#13864,#13865,
#13866,#13867,#13868,#13869,#13870,#13871,#13872,#13873,#13874,#13875,#13876,
#13877,#13878,#13879,#13880,#13881,#13882,#13883,#13884,#13885,#13886,#13887,
#13888,#13889,#13890,#13891,#13892,#13893,#13894,#13895,#13896,#13897,#13898,
#13899,#13900,#13901,#13902,#13903,#13904,#13905,#13906,#13907,#13908,#13909,
#13910,#13911,#13912,#13913,#13914,#13915,#13916,#13917,#13918,#13919,#13920,
#13921,#13922,#13923,#13924,#13925,#13926,#13927,#13928,#13929,#13930,#13931,
#13932,#13933,#13934,#13935,#13936,#13937,#13938,#13939,#13940,#13941,#13942,
#13943,#13944,#13945,#13946,#13947,#13948,#13949,#13950,#13951,#13952,#13953,
#13954,#13955,#13956,#13957,#13958,#13959,#13960,#13961,#13962,#13963,#13964,
#13965,#13966,#13967,#13968,#13969,#13970,#13971,#13972,#13973,#13974,#13975,
#13976,#13977,#13978,#13979,#13980,#13981,#13982,#13983,#13984,#13985,#13986,
#13987,#13988,#13989,#13990,#13991,#13992,#13993,#13994,#13995,#13996,#13997,
#13998,#13999,#14000,#14001,#14002,#14003,#14004,#14005,#14006,#14007,#14008,
#14009,#14010,#14011,#14012,#14013,#14014,#14015,#14016,#14017,#14018,#14019,
#14020,#14021,#14022,#14023,#14024,#14025,#14026,#14027,#14028,#14029,#14030,
#14031,#14032,#14033,#14034,#14035,#14036,#14037,#14038,#14039,#14040,#14041,
#14042,#14043,#14044,#14045,#14046,#14047,#14048,#14049,#14050,#14051,#14052,
#14053,#14054,#14055,#14056,#14057,#14058,#14059,#14060,#14061,#14062,#14063,
#14064,#14065,#14066,#14067,#14068,#14069,#14070,#14071,#14072,#14073,#14074,
#14075,#14076,#14077,#14078,#14079,#14080,#14081,#14082,#14083,#14084,#14085,
#14086,#14087,#14088,#14089,#14090,#14091,#14092,#14093,#14094,#14095,#14096,
#14097,#14098,#14099,#14100,#14101,#14102,#14103,#14104,#14105,#14106,#14107,
#14108,#14109,#14110,#14111,#14112,#14113,#14114,#14115,#14116,#14117,#14118,
#14119,#14120,#14121,#14122,#14123,#14124,#14125,#14126,#14127,#14128,#14129,
#14130,#14131,#14132,#14133,#14134,#14135,#14136,#14137,#14138,#14139,#14140,
#14141,#14142,#14143,#14144,#14145,#14146,#14147,#14148,#14149,#14150,#14151,
#14152,#14153,#14154,#14155,#14156,#14157,#14158,#14159,#14160,#14161,#14162,
#14163,#14164,#14165,#14166,#14167,#14168,#14169,#14170,#14171,#14172,#14173),
 .UNSPECIFIED.,.F.,.F.,(4,2,2,2,2,2,2,2,2,2,2,2,2,2,2,2,2,2,2,2,2,2,2,2,
2,2,2,2,2,2,2,2,2,2,2,2,2,2,2,2,2,2,2,2,2,2,2,2,2,2,2,2,2,2,2,2,2,2,2,2,
2,2,2,2,2,2,2,2,2,2,2,2,2,2,2,2,2,2,2,2,2,2,2,2,2,2,2,2,2,2,2,2,2,2,2,2,
2,2,2,2,2,2,2,2,2,2,2,2,2,2,2,2,2,2,2,2,2,2,2,2,2,2,2,2,2,2,2,2,2,2,2,2,
2,2,2,2,2,2,2,2,2,2,2,2,2,2,2,2,2,2,2,2,2,2,2,2,2,2,2,2,2,2,2,2,2,2,2,2,
2,2,2,2,2,2,2,2,2,2,2,2,2,2,2,2,2,2,2,2,2,2,2,2,2,2,2,2,2,2,2,2,2,2,2,2,
2,2,2,2,2,2,2,2,2,2,2,2,2,2,2,2,2,2,2,2,2,2,2,2,2,2,2,2,2,2,2,2,2,2,2,2,
2,2,2,2,2,2,2,2,2,4),(-2.51331156719081,-2.46641556758931,-2.46237904032085,
-2.46042563756789,-2.45881987310794,-2.45789427341653,-2.45708329463419,
-2.45604398670242,-2.45389777857934,-2.43894518859822,-2.43352847324749,
-2.40708343247289,-2.38941412313501,-2.36694790405523,-2.36151719932127,
-2.3598606942312,-2.3582531174483,-2.35679876334723,-2.35493467563917,-2.35109111486464,
-2.32060805612252,-2.27621475136901,-2.26622847779929,-2.26061502890027,
-2.259093966513,-2.25818716021471,-2.25737227547749,-2.2563182702099,-2.25456545830247,
-2.24412581558946,-2.22170834771183,-2.18266364631991,-2.1703023514551,
-2.16511165265753,-2.16117080919431,-2.15928890521519,-2.15782689483504,
-2.15643955241997,-2.15410504959083,-2.1479043734363,-2.0973997782872,-2.07514456769658,
-2.06171459215125,-2.05973469102586,-2.05872883105891,-2.05792039886308,
-2.05697057770122,-2.05530112896679,-2.04852835706711,-1.98860779668247,
-1.97253934036405,-1.96305446153229,-1.96041051487245,-1.95880087305802,
-1.95734697669968,-1.95548670100387,-1.95166249094168,-1.90665504440521,
-1.88103280253598,-1.86807569803831,-1.86131617571103,-1.85971069830028,
-1.85878512771997,-1.8579740864549,-1.8569345825541,-1.85478757081168,-1.83981538124798,
-1.83423455787463,-1.79045309802062,-1.77336333953354,-1.76344968537372,
-1.76076504418596,-1.75914633356407,-1.75769429182097,-1.75585015212371,
-1.75210725958851,-1.74816788493183,-1.70361448423478,-1.67718542300212,
-1.66712468931043,-1.66146121594546,-1.6599479994821,-1.65904295524339,
-1.65822763355114,-1.65717039836451,-1.65540657665882,-1.64474824866497,
-1.64145682681466,-1.63635839707221,-1.61395774454113,-1.59706509127848,
-1.566707906706,-1.5622468266814,-1.56026627455423,-1.55879476935091,-1.55742473853623,
-1.55518060537167,-1.54953867289628,-1.48717258645446,-1.47016765452698,
-1.46206009734913,-1.46036069633657,-1.45941433883957,-1.4586055462611,
-1.45759504801634,-1.45602339207198,-1.44858983195532,-1.38694716935676,
-1.37249569056866,-1.36371452712017,-1.36114128062148,-1.35954726872352,
-1.35808930585529,-1.35622942257207,-1.35230491859648,-1.34864462726753,
-1.30464428965609,-1.26674506242754,-1.26344460977994,-1.26100486489638,
-1.25990954822187,-1.25909129735208,-1.25830725721525,-1.25694784501452,
-1.2527386236874,-1.22546839577746,-1.20378342813574,-1.16630248360066,
-1.16239257677004,-1.16051530777154,-1.15905910603019,-1.15745801060603,
-1.15485318803356,-1.14576604436613,-1.13061877894284,-1.10053114181583,
-1.06350040417531,-1.06122923517285,-1.06017687411129,-1.05936213459069,
-1.0584542481412,-1.05692866193142,-1.05113097885456,-1.04073523124816,
-1.01316179138208,-0.966384573395418,-0.962604821082921,-0.960753193482881,
-0.959300138148154,-0.957685338947238,-0.955018881811901,-0.94530178524887,
-0.928682041508377,-0.897435031373139,-0.875992205806229,-0.873337140315538,
-0.863258113587079,-0.861523868269612,-0.860475308793578,-0.859661116116092,
-0.858751201284992,-0.857216385170257,-0.851314738889617,-0.840654444771424,
-0.811961187897934,-0.810530397832079,-0.76681330059254,-0.762963629376737,
-0.761098224977234,-0.759643582918983,-0.75803644063079,-0.755404184086842,
-0.746040895799794,-0.730255183249775,-0.699660104992737,-0.664157430385115,
-0.661857069063419,-0.660799254031398,-0.65998380233488,-0.659078952266976,
-0.657566803858033,-0.651915658727571,-0.641887329398766,-0.615587649109692,
-0.570886879362118,-0.566401999564037,-0.56333936565416,-0.561470504887896,
-0.560011284694438,-0.558421756403332,-0.555868620949217,-0.547277624767821,
-0.533248568793334,-0.475369572012022,-0.463930956043464,-0.461954964218194,
-0.460936588064829,-0.460127248860624,-0.459186826604164,-0.457514570786302,
-0.449826126491585,-0.400411181547559,-0.367378126123984,-0.363496445871771,
-0.361624667035728,-0.360169133106218,-0.360166511435948,-0.360163895769302,
-0.360161286085973,-0.360158682405084,-0.360156084702595,-0.360153492950245,
-0.360150907113693,-0.360148327164743,-0.360145753099508,-0.358566835811915,
-0.356035654034639,-0.353017304955375,-0.347168365265727,-0.33255593713871,
-0.296581038777048,-0.276043764867396,-0.264233067965491,-0.262237716374046,
-0.261215184427658,-0.260405553475419,-0.259468210527326,-0.257809873516144,
-0.250326147616493,-0.23526871741068,-0.191584259048881,-0.182915678781613,
-0.166765508304984,-0.16378394871383,-0.161919233093932,-0.160464576525571,
-0.159108843420455,-0.157531528050288,-0.152933698999367,-0.132262473361209,
-0.11452803702179,-0.0677013431936985,-0.0634452588229367,-0.0620286008629612,
-0.061233060217987,-0.0605005625719637,-0.0594802164029013,-0.0574297403832107,
-0.0399344391945697,-0.000592787767141576),.UNSPECIFIED.);
#788=B_SPLINE_CURVE_WITH_KNOTS('',3,(#14175,#14176,#14177,#14178,#14179,
#14180,#14181,#14182,#14183,#14184,#14185,#14186,#14187,#14188,#14189,#14190,
#14191,#14192,#14193,#14194,#14195,#14196,#14197,#14198,#14199,#14200,#14201,
#14202,#14203,#14204,#14205,#14206,#14207,#14208,#14209,#14210,#14211,#14212,
#14213,#14214,#14215,#14216,#14217,#14218,#14219,#14220,#14221,#14222,#14223,
#14224,#14225,#14226,#14227,#14228,#14229,#14230,#14231,#14232,#14233,#14234,
#14235,#14236,#14237,#14238,#14239,#14240,#14241,#14242,#14243,#14244,#14245,
#14246,#14247,#14248,#14249,#14250,#14251,#14252,#14253,#14254,#14255,#14256,
#14257,#14258,#14259,#14260,#14261,#14262,#14263,#14264,#14265,#14266,#14267,
#14268,#14269,#14270,#14271,#14272,#14273,#14274,#14275,#14276,#14277,#14278,
#14279,#14280,#14281,#14282,#14283,#14284,#14285,#14286,#14287,#14288,#14289,
#14290,#14291,#14292,#14293,#14294,#14295,#14296,#14297,#14298,#14299,#14300,
#14301,#14302,#14303,#14304,#14305,#14306,#14307,#14308,#14309,#14310,#14311,
#14312,#14313,#14314,#14315,#14316,#14317,#14318,#14319,#14320,#14321,#14322,
#14323,#14324,#14325,#14326,#14327,#14328,#14329,#14330,#14331,#14332,#14333,
#14334,#14335,#14336,#14337,#14338,#14339,#14340,#14341,#14342,#14343,#14344,
#14345,#14346,#14347,#14348,#14349,#14350,#14351,#14352,#14353,#14354,#14355,
#14356,#14357,#14358,#14359,#14360,#14361,#14362,#14363,#14364),
 .UNSPECIFIED.,.F.,.F.,(4,3,3,3,3,3,3,3,3,3,3,3,3,3,3,3,3,3,3,3,3,3,3,3,
3,3,3,3,3,3,3,3,3,3,3,3,3,3,3,3,3,3,3,3,3,3,3,3,3,3,3,3,3,3,3,3,3,3,3,3,
3,3,3,4),(84.8230016469247,84.9270370546266,85.0310354285839,85.135033069763,
85.2391393980532,85.3433028849637,85.4476570100154,85.5187774560374,85.6237232709015,
85.7285113359001,85.8331758665414,85.9377743743331,86.0423424437451,86.1469156150778,
86.251599570145,86.3563446335458,86.4612724800061,86.5174583243981,86.6224041392623,
86.7271922042609,86.8318567349023,86.936455242694,87.0410233121059,87.1455964834384,
87.2502804385056,87.3550255019063,87.4599533483666,87.5161391927589,87.6210850076231,
87.725873072622,87.8305376032632,87.9351361110549,88.0397041804669,88.1442773517997,
88.2489613068668,88.3537063702675,88.4586342167277,88.5148200611196,88.6197658759839,
88.7245539409826,88.8292184716239,88.9338169794156,89.0383850488277,89.1429582201606,
89.2476421752278,89.3523872386285,89.4573150850887,89.5135009294804,89.6184467443445,
89.7232348093431,89.8278993399843,89.9324978477761,90.037065917188,90.1416390885208,
90.246323043588,90.3510681069884,90.4559959534485,90.5121817978411,90.6188240101089,
90.7252911795686,90.831589163945,90.9377877569733,91.0439192365143,91.1061869541043),
 .UNSPECIFIED.);
#789=B_SPLINE_CURVE_WITH_KNOTS('',3,(#14366,#14367,#14368,#14369,#14370,
#14371,#14372,#14373,#14374,#14375),.UNSPECIFIED.,.F.,.F.,(4,1,1,1,1,1,
1,4),(91.1061934734467,91.5108626662019,92.5095435345626,93.5082244029234,
94.5069052712841,95.5055861396449,96.5042670080056,97.3893634456),
 .UNSPECIFIED.);
#790=B_SPLINE_CURVE_WITH_KNOTS('',3,(#14377,#14378,#14379,#14380,#14381,
#14382,#14383,#14384,#14385,#14386,#14387,#14388,#14389,#14390,#14391,#14392,
#14393,#14394,#14395,#14396,#14397,#14398,#14399,#14400,#14401,#14402,#14403,
#14404,#14405,#14406,#14407,#14408,#14409,#14410,#14411,#14412,#14413,#14414,
#14415,#14416,#14417,#14418,#14419,#14420,#14421,#14422,#14423,#14424,#14425,
#14426,#14427,#14428,#14429,#14430,#14431,#14432,#14433,#14434,#14435,#14436,
#14437,#14438,#14439,#14440,#14441,#14442,#14443,#14444,#14445,#14446,#14447,
#14448,#14449,#14450,#14451,#14452,#14453,#14454,#14455,#14456,#14457,#14458,
#14459,#14460,#14461,#14462,#14463,#14464,#14465,#14466,#14467,#14468,#14469,
#14470,#14471,#14472,#14473,#14474,#14475,#14476,#14477,#14478,#14479,#14480,
#14481,#14482,#14483,#14484,#14485,#14486,#14487,#14488,#14489,#14490,#14491,
#14492,#14493,#14494,#14495,#14496,#14497,#14498,#14499,#14500,#14501,#14502,
#14503,#14504,#14505,#14506,#14507,#14508,#14509,#14510,#14511,#14512,#14513,
#14514,#14515,#14516,#14517,#14518,#14519,#14520,#14521,#14522,#14523,#14524,
#14525,#14526,#14527,#14528,#14529,#14530,#14531,#14532,#14533,#14534,#14535,
#14536,#14537,#14538,#14539,#14540,#14541,#14542,#14543,#14544,#14545,#14546,
#14547,#14548,#14549,#14550,#14551,#14552,#14553,#14554,#14555,#14556,#14557,
#14558,#14559,#14560,#14561,#14562,#14563,#14564,#14565,#14566),
 .UNSPECIFIED.,.F.,.F.,(4,3,3,3,3,3,3,3,3,3,3,3,3,3,3,3,3,3,3,3,3,3,3,3,
3,3,3,3,3,3,3,3,3,3,3,3,3,3,3,3,3,3,3,3,3,3,3,3,3,3,3,3,3,3,3,3,3,3,3,3,
3,3,3,4),(97.3893722612839,97.5029478763664,97.6078936912306,97.7126817562294,
97.8173462868706,97.9219447946623,98.0265128640743,98.131086035407,98.2357699904742,
98.3405150538749,98.4454429003351,98.5016287447271,98.6065745595913,98.7113626245902,
98.8160271552315,98.9206256630233,99.0251937324353,99.129766903768,99.2344508588353,
99.339195922236,99.4441237686963,99.5003096130879,99.6052554279521,99.7100434929509,
99.8147080235921,99.9193065313838,100.023874600796,100.128447772128,100.233131727196,
100.337876790596,100.442804637057,100.498990481449,100.603936296313,100.708724361312,
100.813388891953,100.917987399745,101.022555469157,101.127128640489,101.231812595557,
101.336557658957,101.441485505417,101.497671349809,101.602617164673,101.707405229672,
101.812069760313,101.916668268105,102.021236337517,102.12580950885,102.230493463917,
102.335238527318,102.440166373778,102.49635221817,102.601298033034,102.706086098033,
102.810750628674,102.915349136466,103.019917205878,103.124490377211,103.229174332278,
103.333919395679,103.438847242139,103.495033086531,103.655360446659,103.672557568463),
 .UNSPECIFIED.);
#791=B_SPLINE_CURVE_WITH_KNOTS('',3,(#14568,#14569,#14570,#14571,#14572,
#14573,#14574,#14575,#14576,#14577,#14578,#14579,#14580,#14581,#14582,#14583,
#14584,#14585,#14586,#14587,#14588,#14589,#14590,#14591,#14592,#14593,#14594,
#14595,#14596,#14597,#14598,#14599,#14600,#14601,#14602,#14603,#14604,#14605,
#14606,#14607,#14608,#14609,#14610,#14611,#14612,#14613,#14614,#14615,#14616,
#14617,#14618,#14619,#14620,#14621,#14622,#14623,#14624,#14625,#14626,#14627,
#14628,#14629,#14630,#14631,#14632,#14633,#14634,#14635,#14636,#14637,#14638,
#14639,#14640,#14641,#14642,#14643,#14644,#14645,#14646,#14647,#14648,#14649,
#14650,#14651,#14652,#14653,#14654,#14655,#14656,#14657,#14658,#14659,#14660,
#14661,#14662,#14663,#14664,#14665,#14666,#14667,#14668,#14669,#14670,#14671,
#14672,#14673,#14674,#14675,#14676,#14677,#14678,#14679,#14680,#14681,#14682,
#14683,#14684,#14685,#14686,#14687,#14688,#14689,#14690,#14691,#14692,#14693,
#14694,#14695,#14696,#14697,#14698,#14699,#14700,#14701,#14702,#14703,#14704,
#14705,#14706,#14707,#14708,#14709,#14710,#14711,#14712,#14713,#14714,#14715,
#14716,#14717,#14718,#14719,#14720,#14721,#14722,#14723,#14724,#14725,#14726,
#14727,#14728,#14729,#14730,#14731,#14732,#14733,#14734,#14735,#14736,#14737,
#14738,#14739,#14740,#14741,#14742,#14743,#14744,#14745,#14746,#14747,#14748,
#14749,#14750,#14751,#14752,#14753,#14754,#14755,#14756,#14757,#14758,#14759,
#14760,#14761,#14762,#14763,#14764,#14765,#14766,#14767,#14768,#14769,#14770,
#14771,#14772,#14773,#14774,#14775,#14776,#14777,#14778,#14779,#14780,#14781,
#14782,#14783,#14784,#14785,#14786,#14787,#14788,#14789,#14790,#14791,#14792,
#14793,#14794,#14795,#14796,#14797,#14798,#14799,#14800,#14801,#14802,#14803,
#14804,#14805,#14806,#14807,#14808,#14809,#14810,#14811,#14812,#14813,#14814,
#14815,#14816,#14817,#14818,#14819,#14820,#14821,#14822,#14823,#14824,#14825,
#14826,#14827,#14828,#14829,#14830,#14831,#14832,#14833,#14834,#14835,#14836,
#14837,#14838,#14839,#14840,#14841,#14842,#14843,#14844,#14845,#14846,#14847,
#14848,#14849,#14850,#14851,#14852,#14853,#14854,#14855,#14856,#14857,#14858,
#14859,#14860,#14861,#14862,#14863,#14864,#14865,#14866,#14867,#14868,#14869,
#14870,#14871,#14872,#14873,#14874,#14875,#14876,#14877,#14878,#14879,#14880,
#14881,#14882,#14883,#14884,#14885,#14886,#14887,#14888,#14889,#14890,#14891,
#14892,#14893,#14894,#14895,#14896,#14897,#14898,#14899,#14900,#14901,#14902,
#14903,#14904,#14905,#14906,#14907,#14908,#14909,#14910,#14911,#14912,#14913,
#14914,#14915,#14916,#14917,#14918,#14919,#14920,#14921,#14922,#14923,#14924,
#14925,#14926,#14927,#14928,#14929,#14930,#14931,#14932,#14933,#14934,#14935,
#14936,#14937,#14938,#14939,#14940,#14941,#14942,#14943,#14944,#14945,#14946,
#14947,#14948,#14949,#14950,#14951,#14952,#14953,#14954,#14955,#14956,#14957,
#14958,#14959,#14960,#14961,#14962,#14963,#14964,#14965,#14966,#14967,#14968,
#14969,#14970,#14971,#14972,#14973,#14974,#14975,#14976,#14977,#14978,#14979,
#14980,#14981,#14982,#14983,#14984,#14985,#14986,#14987,#14988,#14989,#14990,
#14991,#14992,#14993,#14994,#14995,#14996,#14997,#14998,#14999,#15000,#15001,
#15002,#15003,#15004,#15005,#15006,#15007,#15008,#15009,#15010,#15011,#15012,
#15013,#15014,#15015,#15016,#15017,#15018,#15019,#15020,#15021,#15022,#15023,
#15024,#15025,#15026,#15027,#15028,#15029,#15030,#15031,#15032,#15033,#15034,
#15035,#15036,#15037,#15038,#15039),.UNSPECIFIED.,.F.,.F.,(4,2,2,2,2,2,
2,2,2,2,2,2,2,2,2,2,2,2,2,2,2,2,2,2,2,2,2,2,2,2,2,2,2,2,2,2,2,2,2,2,2,2,
2,2,2,2,2,2,2,2,2,2,2,2,2,2,2,2,2,2,2,2,2,2,2,2,2,2,2,2,2,2,2,2,2,2,2,2,
2,2,2,2,2,2,2,2,2,2,2,2,2,2,2,2,2,2,2,2,2,2,2,2,2,2,2,2,2,2,2,2,2,2,2,2,
2,2,2,2,2,2,2,2,2,2,2,2,2,2,2,2,2,2,2,2,2,2,2,2,2,2,2,2,2,2,2,2,2,2,2,2,
2,2,2,2,2,2,2,2,2,2,2,2,2,2,2,2,2,2,2,2,2,2,2,2,2,2,2,2,2,2,2,2,2,2,2,2,
2,2,2,2,2,2,2,2,2,2,2,2,2,2,2,2,2,2,2,2,2,2,2,2,2,2,2,2,2,2,2,2,2,2,2,2,
2,2,2,2,2,2,2,2,2,2,2,2,2,4),(-2.51381709144448,-2.4616943203403,-2.45636384935998,
-2.45229589263989,-2.4503884266314,-2.44892844628467,-2.44753723688448,
-2.44518212638536,-2.43883933923972,-2.39132865758641,-2.37432821273789,
-2.35422184584957,-2.35137005240454,-2.35045549044507,-2.3496938177306,
-2.34888308507486,-2.34784610220737,-2.3461874676665,-2.33745085149639,
-2.33318433166976,-2.32140295634083,-2.27597377532883,-2.26242688882561,
-2.25423253663617,-2.25161330702175,-2.25000925115995,-2.24855422004964,
-2.24668387186621,-2.24280799441645,-2.21017357382959,-2.17511733595217,
-2.15544239993991,-2.15305391245716,-2.15120094119025,-2.15021742027139,
-2.14948708218152,-2.14856556988473,-2.14697815647314,-2.14128080460466,
-2.0786233247721,-2.06353115175816,-2.05449563222558,-2.05187977319521,
-2.05027659292584,-2.04882157731506,-2.04695015901558,-2.04306812236764,
-2.00993617628532,-1.95824262510073,-1.95261989831584,-1.95111057341721,
-1.95020646723168,-1.94939102389445,-1.94833235332837,-1.9460267589751,
-1.91093287082707,-1.88024170872365,-1.8642950648383,-1.85486229851676,
-1.85222353402949,-1.85061511344793,-1.84916106513199,-1.84729885398925,
-1.844324736508,-1.83979389570394,-1.79155652170574,-1.7677523338987,-1.75832095640315,
-1.75291336925023,-1.7514243542899,-1.75052475162212,-1.74970796570809,
-1.74864034809405,-1.74628687915129,-1.72030802225369,-1.66873734036535,
-1.65570126133217,-1.65276682486339,-1.65109287021838,-1.64979326604914,
-1.64809239473104,-1.64511736847035,-1.64007469943735,-1.59192421493179,
-1.56806020222045,-1.55861480556869,-1.55320146741699,-1.55171191212857,
-1.55081219715275,-1.54999546090758,-1.54892811062603,-1.5465760358642,
-1.5208410503503,-1.49123725349215,-1.4605957813531,-1.45461987527319,-1.45239345271687,
-1.45087501438962,-1.44939727919356,-1.44762597562196,-1.44323349537697,
-1.44043071158282,-1.39183512808602,-1.3682776509208,-1.3589042029825,-1.35352043875533,
-1.35203368159175,-1.35113455630874,-1.35031757477421,-1.34924886078076,
-1.34688962417538,-1.31959140073318,-1.28267592549371,-1.25727990435006,
-1.25414782900595,-1.25225846264476,-1.25079626412085,-1.24921650240911,
-1.24670712555776,-1.2385161053402,-1.22536323324388,-1.1723454382188,-1.15505810065911,
-1.15305818353829,-1.15203399145868,-1.15127715654279,-1.15043984266644,
-1.14923748612129,-1.14616640606154,-1.13105297241606,-1.1010401044924,
-1.05816980319124,-1.05430246779117,-1.05243357103647,-1.05097847409879,
-1.04937313329847,-1.04674905873934,-1.03746901763568,-1.02187697914105,
-0.991434506836916,-0.972462001061123,-0.95536988070217,-0.953155426613753,
-0.952113905239302,-0.951300636924812,-0.950386719699435,-0.948833886215519,
-0.942724788106874,-0.931528276223083,-0.90168752149348,-0.858485925908308,
-0.854624189957158,-0.852756443087467,-0.851301544566228,-0.849695714900161,
-0.847069234922686,-0.837764107485972,-0.822113578063696,-0.791625637597253,
-0.755804495926459,-0.753510002657553,-0.752453304321176,-0.751638026076871,
-0.750732618418351,-0.749217909705027,-0.743538729456008,-0.733440390370134,
-0.706868042805538,-0.662549361485804,-0.65838064817793,-0.6551423391341,
-0.653221783663702,-0.651754588679456,-0.650188099119181,-0.647738950432579,
-0.64007190767818,-0.585135754711058,-0.556159379838001,-0.553797991958006,
-0.552728794028803,-0.551911653521997,-0.551012572867447,-0.549526363686655,
-0.544149547156414,-0.534794645763726,-0.511317516205744,-0.462636722700139,
-0.460428687641927,-0.455728777501401,-0.45385742087868,-0.452489216080156,
-0.451016400848921,-0.449028351186105,-0.444627824642235,-0.438690332297171,
-0.423764170729645,-0.373584920335847,-0.356206710964582,-0.35420447156368,
-0.353179651521646,-0.352422626435502,-0.351585406504917,-0.350383719761933,
-0.347467231191857,-0.312517085664562,-0.27794077061886,-0.27243982345828,
-0.258198609356565,-0.255335165775178,-0.253506514879707,-0.252055870905966,
-0.250427386356295,-0.24787127424443,-0.238625657250771,-0.223047353278985,
-0.190779561646613,-0.185490330609927,-0.15672656894149,-0.154364801672018,
-0.153295508070814,-0.152478326607812,-0.15157923551403,-0.150645997651498,
-0.147597906892484,-0.113426603515479,-0.100055212277475,-0.0874973804172144,
-0.0595262308992935,-0.0557308961226528,-0.0538760873696228,-0.0524225632821771,
-0.050809329075979,-0.0491448252879598,-0.0466820881505009,-0.0373021931558657,
-0.00059233830958253),.UNSPECIFIED.);
#792=B_SPLINE_CURVE_WITH_KNOTS('',3,(#15041,#15042,#15043,#15044,#15045,
#15046,#15047,#15048,#15049,#15050,#15051,#15052,#15053,#15054,#15055,#15056,
#15057,#15058,#15059,#15060,#15061,#15062,#15063,#15064,#15065,#15066,#15067,
#15068,#15069,#15070,#15071,#15072,#15073,#15074,#15075,#15076,#15077,#15078,
#15079,#15080,#15081,#15082,#15083,#15084,#15085,#15086,#15087,#15088,#15089,
#15090,#15091,#15092,#15093,#15094,#15095,#15096,#15097,#15098,#15099,#15100,
#15101,#15102,#15103,#15104,#15105,#15106,#15107,#15108,#15109,#15110,#15111,
#15112,#15113,#15114,#15115,#15116,#15117,#15118,#15119,#15120,#15121,#15122,
#15123,#15124,#15125,#15126,#15127,#15128,#15129,#15130,#15131,#15132,#15133,
#15134,#15135,#15136,#15137,#15138,#15139,#15140,#15141,#15142,#15143,#15144,
#15145,#15146,#15147,#15148,#15149,#15150,#15151,#15152,#15153,#15154,#15155,
#15156,#15157,#15158,#15159,#15160,#15161,#15162,#15163,#15164,#15165,#15166,
#15167,#15168,#15169,#15170,#15171,#15172,#15173,#15174,#15175,#15176,#15177,
#15178,#15179,#15180,#15181,#15182,#15183,#15184,#15185,#15186,#15187,#15188,
#15189,#15190,#15191,#15192,#15193,#15194,#15195,#15196,#15197,#15198,#15199,
#15200,#15201,#15202,#15203,#15204,#15205,#15206,#15207,#15208,#15209,#15210,
#15211,#15212,#15213,#15214,#15215,#15216,#15217,#15218,#15219,#15220,#15221,
#15222,#15223,#15224,#15225,#15226,#15227,#15228,#15229,#15230,#15231,#15232,
#15233,#15234,#15235,#15236,#15237,#15238,#15239,#15240,#15241,#15242,#15243,
#15244,#15245,#15246,#15247,#15248,#15249,#15250,#15251,#15252,#15253,#15254,
#15255,#15256,#15257,#15258,#15259,#15260,#15261,#15262,#15263,#15264,#15265,
#15266,#15267,#15268,#15269,#15270,#15271,#15272,#15273,#15274,#15275,#15276,
#15277,#15278,#15279,#15280,#15281,#15282,#15283,#15284,#15285,#15286,#15287,
#15288,#15289,#15290,#15291,#15292,#15293,#15294,#15295,#15296,#15297,#15298,
#15299,#15300,#15301,#15302,#15303,#15304,#15305,#15306,#15307,#15308,#15309,
#15310,#15311,#15312,#15313,#15314,#15315,#15316,#15317,#15318,#15319,#15320,
#15321,#15322,#15323,#15324,#15325,#15326,#15327,#15328,#15329,#15330,#15331,
#15332,#15333,#15334,#15335,#15336,#15337,#15338,#15339,#15340,#15341,#15342,
#15343,#15344,#15345,#15346,#15347,#15348,#15349,#15350,#15351,#15352,#15353,
#15354,#15355,#15356,#15357,#15358,#15359,#15360,#15361,#15362,#15363,#15364,
#15365,#15366,#15367,#15368,#15369,#15370,#15371,#15372,#15373,#15374,#15375,
#15376,#15377,#15378,#15379,#15380,#15381,#15382,#15383,#15384,#15385,#15386,
#15387,#15388,#15389,#15390,#15391,#15392,#15393,#15394,#15395,#15396,#15397,
#15398,#15399,#15400,#15401,#15402,#15403,#15404,#15405,#15406,#15407,#15408,
#15409,#15410,#15411,#15412,#15413,#15414,#15415,#15416,#15417,#15418,#15419,
#15420,#15421,#15422,#15423,#15424,#15425,#15426,#15427,#15428,#15429,#15430,
#15431,#15432,#15433,#15434,#15435,#15436,#15437,#15438,#15439,#15440,#15441,
#15442,#15443,#15444,#15445,#15446,#15447,#15448,#15449,#15450,#15451,#15452,
#15453,#15454,#15455,#15456,#15457,#15458,#15459,#15460,#15461,#15462,#15463,
#15464,#15465,#15466,#15467,#15468,#15469,#15470,#15471,#15472,#15473,#15474,
#15475,#15476,#15477,#15478,#15479,#15480,#15481,#15482,#15483,#15484,#15485,
#15486,#15487,#15488,#15489,#15490,#15491,#15492,#15493,#15494,#15495,#15496,
#15497,#15498,#15499,#15500,#15501,#15502,#15503,#15504,#15505,#15506,#15507,
#15508,#15509,#15510,#15511,#15512,#15513,#15514,#15515,#15516,#15517,#15518,
#15519,#15520,#15521,#15522,#15523,#15524),.UNSPECIFIED.,.F.,.F.,(4,2,2,
2,2,2,2,2,2,2,2,2,2,2,2,2,2,2,2,2,2,2,2,2,2,2,2,2,2,2,2,2,2,2,2,2,2,2,2,
2,2,2,2,2,2,2,2,2,2,2,2,2,2,2,2,2,2,2,2,2,2,2,2,2,2,2,2,2,2,2,2,2,2,2,2,
2,2,2,2,2,2,2,2,2,2,2,2,2,2,2,2,2,2,2,2,2,2,2,2,2,2,2,2,2,2,2,2,2,2,2,2,
2,2,2,2,2,2,2,2,2,2,2,2,2,2,2,2,2,2,2,2,2,2,2,2,2,2,2,2,2,2,2,2,2,2,2,2,
2,2,2,2,2,2,2,2,2,2,2,2,2,2,2,2,2,2,2,2,2,2,2,2,2,2,2,2,2,2,2,2,2,2,2,2,
2,2,2,2,2,2,2,2,2,2,2,2,2,2,2,2,2,2,2,2,2,2,2,2,2,2,2,2,2,2,2,2,2,2,2,2,
2,2,2,2,2,2,2,2,2,2,2,2,2,2,2,2,2,2,2,2,2,2,4),(-2.51387412169946,-2.47424051490727,
-2.47065529924497,-2.46886192572763,-2.46776045391495,-2.46674226431793,
-2.46601006212805,-2.46521357297149,-2.46379209649113,-2.45949943594632,
-2.42157509791276,-2.40265965364949,-2.37539707095867,-2.37006884777345,
-2.36842151295062,-2.36682021689027,-2.36536394954583,-2.3634867604667,
-2.3595776229956,-2.32316829797097,-2.28933548144493,-2.27619027760965,
-2.27166976445615,-2.26857687944786,-2.26764352786978,-2.26674436395602,
-2.26592716231359,-2.26485791302871,-2.26249650716216,-2.23448538417367,
-2.19399620985139,-2.17368780881667,-2.16974318254306,-2.1678290092893,
-2.16636767872935,-2.1649780229331,-2.16263245539582,-2.15635958599902,
-2.10691533695347,-2.07386515890655,-2.07077106158281,-2.06847499590965,
-2.06739387202363,-2.06657758679952,-2.06578838518536,-2.06440346976183,
-2.0603827891444,-2.05953942291496,-1.99611070678133,-1.98069450149456,
-1.97148937085782,-1.96887268915347,-1.96726895304265,-1.96581339911095,
-1.96394124103311,-1.9600574982783,-1.92689114075823,-1.87516991124119,
-1.86957187906321,-1.86806449333192,-1.86716061328382,-1.86634472155771,
-1.86528460557971,-1.86297250963142,-1.82826008456372,-1.79742618884047,
-1.78130531693621,-1.77179734699623,-1.76915064622207,-1.76754008538151,
-1.76608584957558,-1.76422581888903,-1.7604045258413,-1.7567183920104,-1.70831024876051,
-1.68460410373265,-1.6751944056072,-1.66979519786641,-1.6683066382996,-1.66740692978507,
-1.66658977771468,-1.66552132079175,-1.66316456551867,-1.63693672993607,
-1.58411719571013,-1.5723709882152,-1.56953029564355,-1.56787665283292,
-1.56642925993887,-1.56463823011855,-1.56189673040706,-1.5569125799063,
-1.50873421855757,-1.48486905510172,-1.4754220134025,-1.47000745112446,
-1.46851743071336,-1.46761740846391,-1.466800374639,-1.46573261057816,-1.46337952504495,
-1.43202708577063,-1.42677918752818,-1.39878364824676,-1.3820739368407,
-1.37231749372118,-1.36964695848821,-1.36803103750096,-1.36657783713793,
-1.36472721109611,-1.36095366066974,-1.31387223358467,-1.27518070365034,
-1.27184819960044,-1.26938965048138,-1.26829072386411,-1.26747175599771,
-1.26657748447456,-1.26511344090479,-1.26049015981145,-1.25730645828561,
-1.24235705005221,-1.19358789874244,-1.17398311092688,-1.17082998796573,
-1.16893409288588,-1.1674704923256,-1.16589283176416,-1.16339450754561,
-1.155306688426,-1.1423778782493,-1.09191565227756,-1.08659026653516,-1.07159020794651,
-1.06944149118093,-1.06840139167889,-1.06758999541161,-1.06666413621532,
-1.06505844069888,-1.05830190392628,-1.04535759819697,-1.02041660586387,
-0.974694866000277,-0.97088203294331,-0.969023546622891,-0.967569351476187,
-0.965957640192113,-0.96330630598602,-0.953752506466787,-0.937521908538539,
-0.906572610798441,-0.872091955684922,-0.869804100260906,-0.868732178535826,
-0.867914452795685,-0.867016335720977,-0.865535107965709,-0.860211962752534,
-0.850987452791029,-0.828065225811737,-0.778558549755146,-0.772301188735705,
-0.769957841512482,-0.768568486050967,-0.767106725081874,-0.765190752233494,
-0.761080879115719,-0.723613825523667,-0.68347320988439,-0.671828506745652,
-0.669841573602604,-0.668820726486177,-0.668011067774648,-0.667072144789106,
-0.665407190718475,-0.657830321581256,-0.608940431929072,-0.602873487396412,
-0.575103641001259,-0.571314960979271,-0.569461300428425,-0.568007717182066,
-0.566393430508175,-0.563730359592587,-0.554053285731037,-0.537530408990782,
-0.506354302789171,-0.487705740959814,-0.472319635423436,-0.470157320112599,
-0.469114591644733,-0.46830298489631,-0.467378923017734,-0.465781120450227,
-0.459125185032049,-0.44646004502937,-0.407521753046994,-0.375509390967726,
-0.371640989158788,-0.369771635651691,-0.3683162093041,-0.368313609442767,
-0.368311015553016,-0.368308427658644,-0.368305845741099,-0.368303269768205,
-0.368300699725793,-0.368298135594457,-0.366719163677803,-0.36417883826322,
-0.3611541885163,-0.355288692253156,-0.340618821769142,-0.30495590249967,
-0.283209842175027,-0.272292827981774,-0.27051577878822,-0.269454494549948,
-0.268638391572769,-0.267735017431447,-0.266230078767635,-0.26065888634933,
-0.208943721982646,-0.175765854701592,-0.171883523432426,-0.170011502656316,
-0.168555812686019,-0.167200259220575,-0.164974753350029,-0.158580383062122,
-0.149035158608648,-0.127500668087479,-0.0983596711902327,-0.0731308752864359,
-0.070779654450056,-0.0697122656681324,-0.0688953227586978,-0.0679951814165042,
-0.066504507876579,-0.0610826223315877,-0.0149734459364435,-0.000592883991003962),
 .UNSPECIFIED.);
#793=B_SPLINE_CURVE_WITH_KNOTS('',3,(#15526,#15527,#15528,#15529,#15530,
#15531,#15532,#15533,#15534,#15535,#15536,#15537,#15538,#15539,#15540,#15541,
#15542,#15543,#15544,#15545,#15546,#15547,#15548,#15549,#15550,#15551,#15552,
#15553,#15554,#15555,#15556,#15557,#15558,#15559,#15560,#15561,#15562,#15563,
#15564,#15565,#15566,#15567,#15568,#15569,#15570,#15571,#15572,#15573,#15574,
#15575,#15576,#15577,#15578,#15579,#15580,#15581,#15582,#15583,#15584,#15585,
#15586,#15587,#15588,#15589,#15590,#15591,#15592,#15593,#15594,#15595,#15596,
#15597,#15598,#15599,#15600,#15601,#15602,#15603,#15604,#15605,#15606,#15607,
#15608,#15609,#15610,#15611,#15612,#15613,#15614,#15615,#15616,#15617,#15618,
#15619,#15620,#15621,#15622,#15623,#15624,#15625,#15626,#15627,#15628,#15629,
#15630,#15631,#15632,#15633,#15634,#15635,#15636,#15637,#15638,#15639,#15640,
#15641,#15642,#15643,#15644,#15645,#15646,#15647,#15648,#15649,#15650,#15651,
#15652,#15653,#15654,#15655,#15656,#15657,#15658,#15659,#15660,#15661,#15662,
#15663,#15664,#15665,#15666,#15667,#15668,#15669,#15670,#15671,#15672,#15673,
#15674,#15675,#15676,#15677,#15678,#15679,#15680,#15681,#15682,#15683,#15684,
#15685,#15686,#15687,#15688,#15689,#15690,#15691,#15692,#15693,#15694,#15695,
#15696,#15697,#15698,#15699,#15700,#15701,#15702,#15703,#15704,#15705,#15706,
#15707,#15708,#15709,#15710,#15711,#15712,#15713,#15714,#15715,#15716,#15717,
#15718,#15719,#15720,#15721,#15722,#15723,#15724,#15725,#15726,#15727,#15728,
#15729,#15730,#15731,#15732,#15733,#15734,#15735,#15736,#15737,#15738,#15739,
#15740,#15741,#15742,#15743,#15744,#15745,#15746,#15747,#15748,#15749,#15750,
#15751,#15752,#15753,#15754,#15755,#15756,#15757,#15758,#15759,#15760,#15761,
#15762,#15763,#15764,#15765,#15766,#15767,#15768,#15769,#15770,#15771,#15772,
#15773,#15774,#15775,#15776,#15777,#15778,#15779,#15780,#15781,#15782,#15783,
#15784,#15785,#15786,#15787,#15788,#15789,#15790,#15791,#15792,#15793,#15794,
#15795,#15796,#15797,#15798,#15799,#15800,#15801,#15802,#15803,#15804,#15805,
#15806,#15807,#15808,#15809,#15810,#15811,#15812,#15813,#15814,#15815,#15816,
#15817,#15818,#15819,#15820,#15821,#15822,#15823,#15824,#15825,#15826,#15827,
#15828,#15829,#15830,#15831,#15832,#15833,#15834,#15835,#15836,#15837,#15838,
#15839,#15840,#15841,#15842,#15843,#15844,#15845,#15846,#15847,#15848,#15849,
#15850,#15851,#15852,#15853,#15854,#15855,#15856,#15857,#15858,#15859,#15860,
#15861,#15862,#15863,#15864,#15865,#15866,#15867,#15868,#15869,#15870,#15871,
#15872,#15873,#15874,#15875,#15876,#15877,#15878,#15879,#15880,#15881,#15882,
#15883,#15884,#15885,#15886,#15887,#15888,#15889,#15890,#15891,#15892,#15893,
#15894,#15895,#15896,#15897,#15898,#15899,#15900,#15901,#15902,#15903,#15904,
#15905,#15906,#15907,#15908,#15909,#15910,#15911,#15912,#15913,#15914,#15915,
#15916,#15917,#15918,#15919,#15920,#15921,#15922,#15923,#15924,#15925,#15926,
#15927,#15928,#15929,#15930,#15931,#15932,#15933,#15934,#15935,#15936,#15937,
#15938,#15939,#15940,#15941,#15942,#15943,#15944,#15945,#15946,#15947,#15948,
#15949,#15950,#15951,#15952,#15953,#15954,#15955,#15956,#15957,#15958,#15959,
#15960,#15961,#15962,#15963,#15964,#15965,#15966,#15967,#15968,#15969,#15970,
#15971,#15972,#15973,#15974,#15975,#15976,#15977,#15978,#15979,#15980,#15981,
#15982,#15983,#15984,#15985,#15986,#15987,#15988,#15989,#15990,#15991,#15992,
#15993,#15994,#15995,#15996,#15997,#15998,#15999,#16000,#16001,#16002,#16003,
#16004,#16005,#16006,#16007,#16008,#16009,#16010,#16011,#16012,#16013,#16014,
#16015,#16016,#16017),.UNSPECIFIED.,.F.,.F.,(4,2,2,2,2,2,2,2,2,2,2,2,2,
2,2,2,2,2,2,2,2,2,2,2,2,2,2,2,2,2,2,2,2,2,2,2,2,2,2,2,2,2,2,2,2,2,2,2,2,
2,2,2,2,2,2,2,2,2,2,2,2,2,2,2,2,2,2,2,2,2,2,2,2,2,2,2,2,2,2,2,2,2,2,2,2,
2,2,2,2,2,2,2,2,2,2,2,2,2,2,2,2,2,2,2,2,2,2,2,2,2,2,2,2,2,2,2,2,2,2,2,2,
2,2,2,2,2,2,2,2,2,2,2,2,2,2,2,2,2,2,2,2,2,2,2,2,2,2,2,2,2,2,2,2,2,2,2,2,
2,2,2,2,2,2,2,2,2,2,2,2,2,2,2,2,2,2,2,2,2,2,2,2,2,2,2,2,2,2,2,2,2,2,2,2,
2,2,2,2,2,2,2,2,2,2,2,2,2,2,2,2,2,2,2,2,2,2,2,2,2,2,2,2,2,2,2,2,2,2,2,2,
2,2,2,2,2,2,2,2,2,2,2,2,2,2,2,2,4),(-2.51333060447836,-2.49512983230018,
-2.48739716911243,-2.48522350706903,-2.48367799139685,-2.48232491170383,
-2.480862333055,-2.47896655172281,-2.47581096820282,-2.45610152696639,-2.45367957048176,
-2.44115764410605,-2.39258688301428,-2.38509332619115,-2.38343500197589,
-2.38249801260629,-2.38168889958435,-2.3806673002386,-2.37867459955377,
-2.36689794538597,-2.31562663635226,-2.29753853462042,-2.29074574367014,
-2.28738240505075,-2.28460723191478,-2.28297760776761,-2.28296984974125,
-2.2829619921872,-2.28295403358371,-2.28294597238488,-2.28293780702015,
-2.28292953589554,-2.28292115751315,-2.2814738439416,-2.27967050619776,
-2.27688682678902,-2.263793784105,-2.20345593376292,-2.18607702469524,-2.18403008716689,
-2.18301084009084,-2.18227886593025,-2.18148362130747,-2.18006682497597,
-2.17580565351732,-2.12913863406614,-2.09159276277847,-2.08799192750396,
-2.08585361230794,-2.08392971250419,-2.08248742401021,-2.08112037096703,
-2.07925161613137,-2.07456360181829,-2.07234178796808,-2.02366918642796,
-2.00018797528709,-1.99083407297192,-1.98545900047289,-1.9839734796391,
-1.98307486181455,-1.98225817079891,-1.98118960877375,-1.97882979714319,
-1.95091812639709,-1.89922297759728,-1.88803115452106,-1.88523600312759,
-1.88359318742138,-1.88214572230551,-1.88034212786995,-1.87755792403532,
-1.87255623832035,-1.82760452779704,-1.80148334203757,-1.79150175612692,
-1.78587079925225,-1.78436103358559,-1.783457014399,-1.78264189379707,-1.78158396503917,
-1.77928123694008,-1.74400931283244,-1.71339177420336,-1.69753153112137,
-1.6881365625347,-1.6855020529409,-1.68389491383127,-1.68244117114537,-1.68057816657373,
-1.67673790970057,-1.64637045593677,-1.60525906039829,-1.59295101130457,
-1.58642719358636,-1.58484058313001,-1.58391941224498,-1.58310800220936,
-1.58206242507518,-1.57988335043724,-1.56396213145341,-1.56035862718075,
-1.55531910366999,-1.51549578637999,-1.49850570343895,-1.48863439058073,
-1.48595432231957,-1.48433699802903,-1.48288532492683,-1.4810404586082,
-1.47812234922137,-1.46299243308917,-1.45911671122481,-1.40503623496431,
-1.39314669652792,-1.3867772291463,-1.38520296730797,-1.38428447375514,
-1.38347246111477,-1.38242215810779,-1.38021925465062,-1.36351367357653,
-1.31618168607164,-1.29895897895577,-1.28899117544015,-1.28630201567029,
-1.28468258338822,-1.28323116895794,-1.2813895624857,-1.27848237003607,
-1.2635324900243,-1.25959153704919,-1.25710657351285,-1.19821909763059,
-1.18773087683868,-1.18597578920766,-1.18492120771139,-1.18410635896853,
-1.18320011223132,-1.18168113203052,-1.17595311458867,-1.16573166023608,
-1.13870760724108,-1.09504822815608,-1.09144095134786,-1.08748379232594,
-1.08561791707192,-1.08415939141838,-1.08256896156834,-1.08001073900125,
-1.0713685148452,-1.05722444819886,-0.99761407634702,-0.987934035231894,
-0.986221350273743,-0.985179225793872,-0.984365926159305,-0.983452461527025,
-0.981901493133867,-0.975813396348231,-0.964671379336478,-0.934923235539195,
-0.891546167579989,-0.887690814054384,-0.885824394156436,-0.884369740014561,
-0.882763377619921,-0.880134202681171,-0.870800632583476,-0.855083584867605,
-0.824544298368596,-0.78888418118745,-0.786587924644967,-0.785530936827555,
-0.784715662306423,-0.783810506513335,-0.782296757155216,-0.77662728337384,
-0.766552901756687,-0.740071841816019,-0.695635521922242,-0.691794992877175,
-0.687989627370943,-0.686133080748478,-0.684679631758147,-0.683067955995739,
-0.680414861002306,-0.670835218872872,-0.654540932222524,-0.623549652583773,
-0.621229064560786,-0.589292506369531,-0.586947072784163,-0.585880929203905,
-0.58506435168189,-0.584163978393464,-0.58267157115461,-0.577228877233172,
-0.530685940186298,-0.492272965017269,-0.488360815026363,-0.486503477252888,
-0.485046052813652,-0.483451142820358,-0.48087315215765,-0.472044112075408,
-0.457482027055751,-0.394962607227355,-0.388412649716335,-0.386762655115358,
-0.385817286049692,-0.385028361912028,-0.384046630407367,-0.382977225585352,
-0.381261318831078,-0.377889443708013,-0.338178026259798,-0.292306479083492,
-0.288500533607447,-0.286643742969465,-0.285190120619366,-0.283578270758942,
-0.280924930870097,-0.271344852143821,-0.255050277372561,-0.225564576575613,
-0.214817149280862,-0.189807967755032,-0.187458270636641,-0.186391277191671,
-0.185590505211471,-0.184713395261896,-0.183312272936186,-0.181628829054493,
-0.178345268818256,-0.170034772719444,-0.135978374418879,-0.0927087360612524,
-0.0888492938507777,-0.0869820119315153,-0.0855271867967861,-0.0839211446664105,
-0.0812936506670929,-0.0719780352331019,-0.056303059782647,-0.000592941019645857),
 .UNSPECIFIED.);
#794=B_SPLINE_CURVE_WITH_KNOTS('',3,(#16019,#16020,#16021,#16022,#16023,
#16024,#16025,#16026,#16027,#16028,#16029,#16030,#16031,#16032,#16033,#16034,
#16035,#16036,#16037,#16038,#16039,#16040,#16041,#16042,#16043,#16044,#16045,
#16046,#16047,#16048,#16049,#16050,#16051,#16052,#16053,#16054,#16055,#16056,
#16057,#16058,#16059,#16060,#16061,#16062,#16063,#16064,#16065,#16066,#16067,
#16068,#16069,#16070,#16071,#16072,#16073,#16074,#16075,#16076,#16077,#16078,
#16079,#16080,#16081,#16082,#16083,#16084,#16085,#16086,#16087,#16088,#16089,
#16090,#16091,#16092,#16093,#16094,#16095,#16096,#16097,#16098,#16099,#16100,
#16101,#16102,#16103,#16104,#16105,#16106,#16107,#16108,#16109,#16110,#16111,
#16112,#16113,#16114,#16115,#16116,#16117,#16118,#16119,#16120,#16121,#16122,
#16123,#16124,#16125,#16126,#16127,#16128,#16129,#16130,#16131,#16132,#16133,
#16134,#16135,#16136,#16137,#16138,#16139,#16140,#16141,#16142,#16143,#16144,
#16145,#16146,#16147,#16148,#16149,#16150,#16151,#16152,#16153,#16154,#16155,
#16156,#16157,#16158,#16159,#16160,#16161,#16162,#16163,#16164,#16165,#16166,
#16167,#16168,#16169,#16170,#16171,#16172,#16173,#16174,#16175,#16176,#16177,
#16178,#16179,#16180,#16181,#16182,#16183,#16184,#16185,#16186,#16187,#16188,
#16189,#16190,#16191,#16192,#16193,#16194,#16195,#16196,#16197,#16198,#16199,
#16200,#16201,#16202,#16203,#16204,#16205,#16206,#16207,#16208),
 .UNSPECIFIED.,.F.,.F.,(4,3,3,3,3,3,3,3,3,3,3,3,3,3,3,3,3,3,3,3,3,3,3,3,
3,3,3,3,3,3,3,3,3,3,3,3,3,3,3,3,3,3,3,3,3,3,3,3,3,3,3,3,3,3,3,3,3,3,3,3,
3,3,3,4),(141.371669411541,141.444906084239,141.549851899103,141.654639964102,
141.759304494743,141.863903002535,141.968471071947,142.07304424328,142.177728198347,
142.282473261748,142.387401108208,142.4435869526,142.548532767464,142.653320832463,
142.757985363105,142.862583870896,142.967151940308,143.071725111641,143.176409066708,
143.281154130109,143.38608197657,143.442267820961,143.547213635825,143.652001700824,
143.756666231465,143.861264739257,143.965832808669,144.070405980001,144.175089935069,
144.279834998469,144.38476284493,144.440948689322,144.545894504186,144.650682569185,
144.755347099826,144.859945607618,144.96451367703,145.069086848362,145.173770803429,
145.27851586683,145.38344371329,145.439629557682,145.544575372546,145.649363437545,
145.754027968186,145.858626475978,145.96319454539,146.067767716722,146.172451671789,
146.27719673519,146.38212458165,146.438310426043,146.543256240907,146.648044305906,
146.752708836547,146.857307344339,146.961875413751,147.066448585084,147.171132540151,
147.275877603552,147.380805450012,147.436991294404,147.581269901374,147.654854718721),
 .UNSPECIFIED.);
#795=B_SPLINE_CURVE_WITH_KNOTS('',3,(#16210,#16211,#16212,#16213,#16214,
#16215,#16216,#16217,#16218,#16219,#16220,#16221,#16222,#16223,#16224,#16225,
#16226,#16227,#16228,#16229,#16230,#16231,#16232,#16233,#16234,#16235,#16236,
#16237,#16238,#16239,#16240,#16241,#16242,#16243,#16244,#16245,#16246,#16247,
#16248,#16249,#16250,#16251,#16252,#16253,#16254,#16255,#16256,#16257,#16258,
#16259,#16260,#16261,#16262,#16263,#16264,#16265,#16266,#16267,#16268,#16269,
#16270,#16271,#16272,#16273,#16274,#16275,#16276,#16277,#16278,#16279,#16280,
#16281,#16282,#16283,#16284,#16285,#16286,#16287,#16288,#16289,#16290,#16291,
#16292,#16293,#16294,#16295,#16296,#16297,#16298,#16299,#16300,#16301,#16302,
#16303,#16304,#16305,#16306,#16307,#16308,#16309,#16310,#16311,#16312,#16313,
#16314,#16315,#16316,#16317,#16318,#16319,#16320,#16321,#16322,#16323,#16324,
#16325,#16326,#16327,#16328,#16329,#16330,#16331,#16332,#16333,#16334,#16335,
#16336,#16337,#16338,#16339,#16340,#16341,#16342,#16343,#16344,#16345,#16346,
#16347,#16348,#16349,#16350,#16351,#16352,#16353,#16354,#16355,#16356,#16357,
#16358,#16359,#16360,#16361,#16362,#16363,#16364,#16365,#16366,#16367,#16368,
#16369,#16370,#16371,#16372,#16373,#16374,#16375,#16376,#16377,#16378,#16379,
#16380,#16381,#16382,#16383,#16384,#16385,#16386,#16387,#16388,#16389,#16390,
#16391,#16392,#16393,#16394,#16395,#16396,#16397,#16398,#16399,#16400,#16401,
#16402,#16403,#16404,#16405,#16406,#16407,#16408,#16409,#16410,#16411,#16412,
#16413,#16414,#16415,#16416,#16417,#16418,#16419,#16420,#16421,#16422,#16423,
#16424,#16425,#16426,#16427,#16428,#16429,#16430,#16431,#16432,#16433,#16434,
#16435,#16436,#16437,#16438,#16439,#16440,#16441,#16442,#16443,#16444,#16445,
#16446,#16447,#16448,#16449,#16450,#16451,#16452,#16453,#16454,#16455,#16456,
#16457,#16458,#16459,#16460,#16461,#16462,#16463,#16464,#16465,#16466,#16467,
#16468,#16469,#16470,#16471,#16472,#16473,#16474,#16475,#16476,#16477,#16478,
#16479,#16480,#16481,#16482,#16483,#16484,#16485,#16486,#16487,#16488,#16489,
#16490,#16491,#16492,#16493,#16494,#16495,#16496,#16497,#16498,#16499,#16500,
#16501,#16502,#16503,#16504,#16505,#16506,#16507,#16508,#16509,#16510,#16511,
#16512,#16513,#16514,#16515,#16516,#16517,#16518,#16519,#16520,#16521,#16522,
#16523,#16524,#16525,#16526,#16527,#16528,#16529,#16530,#16531,#16532,#16533,
#16534,#16535,#16536,#16537,#16538,#16539,#16540,#16541,#16542,#16543,#16544,
#16545,#16546,#16547,#16548,#16549,#16550,#16551,#16552,#16553,#16554,#16555,
#16556,#16557,#16558,#16559,#16560,#16561,#16562,#16563,#16564,#16565,#16566,
#16567,#16568,#16569,#16570,#16571,#16572,#16573,#16574,#16575,#16576,#16577,
#16578,#16579,#16580,#16581,#16582,#16583,#16584,#16585,#16586,#16587,#16588,
#16589,#16590,#16591,#16592,#16593,#16594,#16595,#16596,#16597,#16598,#16599,
#16600,#16601,#16602,#16603,#16604,#16605,#16606,#16607,#16608,#16609,#16610,
#16611,#16612,#16613,#16614,#16615,#16616,#16617,#16618,#16619,#16620,#16621,
#16622,#16623,#16624,#16625,#16626,#16627,#16628,#16629,#16630,#16631,#16632,
#16633,#16634,#16635,#16636,#16637,#16638,#16639,#16640,#16641,#16642,#16643,
#16644,#16645,#16646,#16647,#16648,#16649,#16650,#16651,#16652,#16653,#16654,
#16655,#16656,#16657,#16658,#16659,#16660,#16661,#16662,#16663,#16664,#16665,
#16666,#16667,#16668,#16669),.UNSPECIFIED.,.F.,.F.,(4,2,2,2,2,2,2,2,2,2,
2,2,2,2,2,2,2,2,2,2,2,2,2,2,2,2,2,2,2,2,2,2,2,2,2,2,2,2,2,2,2,2,2,2,2,2,
2,2,2,2,2,2,2,2,2,2,2,2,2,2,2,2,2,2,2,2,2,2,2,2,2,2,2,2,2,2,2,2,2,2,2,2,
2,2,2,2,2,2,2,2,2,2,2,2,2,2,2,2,2,2,2,2,2,2,2,2,2,2,2,2,2,2,2,2,2,2,2,2,
2,2,2,2,2,2,2,2,2,2,2,2,2,2,2,2,2,2,2,2,2,2,2,2,2,2,2,2,2,2,2,2,2,2,2,2,
2,2,2,2,2,2,2,2,2,2,2,2,2,2,2,2,2,2,2,2,2,2,2,2,2,2,2,2,2,2,2,2,2,2,2,2,
2,2,2,2,2,2,2,2,2,2,2,2,2,2,2,2,2,2,2,2,2,2,2,2,2,2,2,2,2,2,2,2,2,2,2,2,
2,2,2,4),(-2.51385606234959,-2.47289550666998,-2.46356794956306,-2.46111353504795,
-2.45945278962572,-2.45784236606457,-2.45638908982159,-2.45453144208573,
-2.45071914265189,-2.40504735754676,-2.38668764753374,-2.3626464817215,
-2.35959888299152,-2.3586659586041,-2.35776720741894,-2.35695038458105,
-2.35588163587887,-2.35352135528082,-2.32459325832703,-2.29654340663641,
-2.27463527058973,-2.26689177004872,-2.26146409540678,-2.25981102992099,
-2.25820593673958,-2.25675135916563,-2.25488354117365,-2.2510199230131,
-2.21923394508305,-2.17925802622926,-2.16716200873673,-2.16073636769438,
-2.15915933173981,-2.15823299936577,-2.15742225151546,-2.15638438753919,
-2.15424510202596,-2.13947833821309,-2.08573634478856,-2.07138609772281,
-2.06267867958504,-2.06018950617599,-2.05857215376388,-2.05712027059102,
-2.0552748847606,-2.0523554559506,-2.04772243049398,-1.99953752651721,-1.97570503865045,
-1.96626763202286,-1.96085781200313,-1.95936874075576,-1.95846921877153,
-1.95765258734327,-1.95658528009643,-1.95478665688354,-1.94340978003152,
-1.91799123012333,-1.88772698119719,-1.87231931385273,-1.86311869212441,
-1.86050300448751,-1.85889981677321,-1.85744472068075,-1.85557309562895,
-1.8516902564788,-1.81850816048406,-1.76677209309934,-1.76122514784952,
-1.75972286504623,-1.75882030654831,-1.75800439130672,-1.75694263174336,
-1.75516325271525,-1.74418860798185,-1.7213700173946,-1.69006124486661,
-1.6733213756367,-1.66355332823,-1.66088233559437,-1.6592666840574,-1.65781407615172,
-1.65596468476574,-1.65219533122811,-1.60502624999197,-1.57768488428766,
-1.56736687116784,-1.56160080505959,-1.56007822315026,-1.5591710950712,
-1.55835632361331,-1.55730299370152,-1.55502618203653,-1.51836063908331,
-1.48818819115999,-1.47290008543883,-1.46375087704527,-1.46114000320452,
-1.4595376828324,-1.45808200624963,-1.45620771633176,-1.45231239056028,
-1.41813895341619,-1.3696200900882,-1.36214515817374,-1.36048749067014,
-1.35955033309762,-1.35874073987037,-1.35771810242628,-1.35572208412949,
-1.34386197823689,-1.3234183275915,-1.30132873804255,-1.26646890964632,
-1.26243309055215,-1.26053148516619,-1.25907203090686,-1.25748285564766,
-1.25493161807489,-1.24635940399886,-1.23237234035762,-1.1737477686684,
-1.16292590825433,-1.16115360223897,-1.16009373147221,-1.15927785796119,
-1.15837380527384,-1.15686572494401,-1.15126049497782,-1.09956355010413,
-1.0664137758482,-1.06253011394748,-1.06065787825693,-1.05920221136876,
-1.05759829748458,-1.05498120590484,-1.04577347292208,-1.03034944725737,
-1.00003824854281,-0.974444453268759,-0.963217081629322,-0.961425080661047,
-0.960359485519636,-0.959542836383574,-0.958641852747923,-0.957147301611772,
-0.951684564572241,-0.904750413416738,-0.866727949660168,-0.862816791798437,
-0.860939257541546,-0.859482998580386,-0.857881989878447,-0.855277644510307,
-0.846195533357814,-0.831059900270178,-0.800981318644419,-0.76392248464805,
-0.761650983747574,-0.76059854805586,-0.759783785527602,-0.758875911574715,
-0.757350430041585,-0.751554121543871,-0.741161930845878,-0.713611615629383,
-0.666803003257231,-0.663023986710399,-0.661172484336627,-0.65971941981336,
-0.658104499610478,-0.655437586305811,-0.645716022975051,-0.62908574926352,
-0.597830214320749,-0.576207056548242,-0.57539762546806,-0.563810642904664,
-0.561827083870032,-0.560807127637897,-0.559997738146478,-0.559058629711448,
-0.557392114679074,-0.549787528579539,-0.500782834838224,-0.46726483750101,
-0.463377037633508,-0.461504163055148,-0.460048603246971,-0.458445418112704,
-0.455830894810249,-0.446813098092226,-0.43176098598118,-0.374633903527819,
-0.36395183998955,-0.36218657607293,-0.361128814582881,-0.360313290673357,
-0.359408236747614,-0.357925866044045,-0.352588346756007,-0.301099518212894,
-0.267469031499313,-0.263579584304299,-0.261706300654746,-0.260250594069233,
-0.258647420319844,-0.256033306141193,-0.247877597067883,-0.234418582662184,
-0.192651244087699,-0.164825145006643,-0.16246394362629,-0.161394755778702,
-0.160577591547324,-0.159678450950414,-0.158745141000032,-0.155696274999276,
-0.133638589593711,-0.116108185495929,-0.0714612337013633,-0.0674036936796014,
-0.0637812838962045,-0.0619364316131628,-0.0604840974397912,-0.0588653394882416,
-0.0561812706654817,-0.0530006397652199,-0.0467126239847654,-0.000592616177282767),
 .UNSPECIFIED.);
#796=B_SPLINE_CURVE_WITH_KNOTS('',3,(#16671,#16672,#16673,#16674,#16675,
#16676,#16677,#16678,#16679,#16680,#16681,#16682,#16683,#16684,#16685,#16686,
#16687,#16688,#16689,#16690,#16691,#16692,#16693,#16694,#16695,#16696,#16697,
#16698,#16699,#16700,#16701,#16702,#16703,#16704,#16705,#16706,#16707,#16708,
#16709,#16710,#16711,#16712,#16713,#16714,#16715,#16716,#16717,#16718,#16719,
#16720,#16721,#16722,#16723,#16724,#16725,#16726,#16727,#16728,#16729,#16730,
#16731,#16732,#16733,#16734,#16735,#16736,#16737,#16738,#16739,#16740,#16741,
#16742,#16743,#16744,#16745,#16746,#16747,#16748,#16749,#16750,#16751,#16752,
#16753,#16754,#16755,#16756,#16757,#16758,#16759,#16760,#16761,#16762,#16763,
#16764,#16765,#16766,#16767,#16768,#16769,#16770,#16771,#16772,#16773,#16774,
#16775,#16776,#16777,#16778,#16779,#16780,#16781,#16782,#16783,#16784,#16785,
#16786,#16787,#16788,#16789,#16790,#16791,#16792,#16793,#16794,#16795,#16796,
#16797,#16798,#16799,#16800,#16801,#16802,#16803,#16804,#16805,#16806,#16807,
#16808,#16809,#16810,#16811,#16812,#16813,#16814,#16815,#16816,#16817,#16818,
#16819,#16820,#16821,#16822,#16823,#16824,#16825,#16826,#16827,#16828,#16829,
#16830,#16831,#16832,#16833,#16834,#16835,#16836,#16837,#16838,#16839,#16840,
#16841,#16842,#16843,#16844,#16845,#16846,#16847,#16848,#16849,#16850,#16851,
#16852,#16853,#16854,#16855,#16856,#16857,#16858,#16859,#16860,#16861,#16862,
#16863,#16864,#16865,#16866,#16867,#16868,#16869,#16870,#16871,#16872,#16873,
#16874,#16875,#16876,#16877,#16878,#16879,#16880,#16881,#16882,#16883,#16884,
#16885,#16886,#16887,#16888,#16889,#16890,#16891,#16892,#16893,#16894,#16895,
#16896,#16897,#16898,#16899,#16900,#16901,#16902,#16903,#16904,#16905,#16906,
#16907,#16908,#16909,#16910,#16911,#16912,#16913,#16914,#16915,#16916,#16917,
#16918,#16919,#16920,#16921,#16922,#16923,#16924,#16925,#16926,#16927,#16928,
#16929,#16930,#16931,#16932,#16933,#16934,#16935,#16936,#16937,#16938,#16939,
#16940,#16941,#16942,#16943,#16944,#16945,#16946,#16947,#16948,#16949,#16950,
#16951,#16952,#16953,#16954,#16955,#16956,#16957,#16958,#16959,#16960,#16961,
#16962,#16963,#16964,#16965,#16966,#16967,#16968,#16969,#16970,#16971,#16972,
#16973,#16974,#16975,#16976,#16977,#16978,#16979,#16980,#16981,#16982,#16983,
#16984,#16985,#16986,#16987,#16988,#16989,#16990,#16991,#16992,#16993,#16994,
#16995,#16996,#16997,#16998,#16999,#17000,#17001,#17002,#17003,#17004,#17005,
#17006,#17007,#17008,#17009,#17010,#17011,#17012,#17013,#17014,#17015,#17016,
#17017,#17018,#17019,#17020,#17021,#17022,#17023,#17024,#17025,#17026,#17027,
#17028,#17029,#17030,#17031,#17032,#17033,#17034,#17035,#17036,#17037,#17038,
#17039,#17040,#17041,#17042,#17043,#17044,#17045,#17046,#17047,#17048,#17049,
#17050,#17051,#17052,#17053,#17054,#17055,#17056,#17057,#17058,#17059,#17060,
#17061,#17062,#17063,#17064,#17065,#17066,#17067,#17068,#17069,#17070,#17071,
#17072,#17073,#17074,#17075,#17076,#17077,#17078,#17079,#17080,#17081,#17082,
#17083,#17084,#17085,#17086,#17087,#17088,#17089,#17090,#17091,#17092,#17093,
#17094,#17095,#17096,#17097,#17098,#17099,#17100,#17101,#17102,#17103,#17104,
#17105,#17106,#17107,#17108,#17109,#17110,#17111,#17112,#17113,#17114,#17115,
#17116,#17117,#17118,#17119,#17120,#17121,#17122,#17123,#17124,#17125,#17126,
#17127,#17128,#17129,#17130,#17131,#17132,#17133,#17134,#17135,#17136,#17137,
#17138,#17139,#17140,#17141,#17142,#17143,#17144,#17145,#17146,#17147,#17148,
#17149,#17150,#17151,#17152,#17153,#17154,#17155,#17156,#17157,#17158,#17159,
#17160,#17161,#17162,#17163,#17164,#17165,#17166,#17167,#17168,#17169,#17170,
#17171,#17172,#17173,#17174,#17175,#17176,#17177,#17178,#17179,#17180),
 .UNSPECIFIED.,.F.,.F.,(4,2,2,2,2,2,2,2,2,2,2,2,2,2,2,2,2,2,2,2,2,2,2,2,
2,2,2,2,2,2,2,2,2,2,2,2,2,2,2,2,2,2,2,2,2,2,2,2,2,2,2,2,2,2,2,2,2,2,2,2,
2,2,2,2,2,2,2,2,2,2,2,2,2,2,2,2,2,2,2,2,2,2,2,2,2,2,2,2,2,2,2,2,2,2,2,2,
2,2,2,2,2,2,2,2,2,2,2,2,2,2,2,2,2,2,2,2,2,2,2,2,2,2,2,2,2,2,2,2,2,2,2,2,
2,2,2,2,2,2,2,2,2,2,2,2,2,2,2,2,2,2,2,2,2,2,2,2,2,2,2,2,2,2,2,2,2,2,2,2,
2,2,2,2,2,2,2,2,2,2,2,2,2,2,2,2,2,2,2,2,2,2,2,2,2,2,2,2,2,2,2,2,2,2,2,2,
2,2,2,2,2,2,2,2,2,2,2,2,2,2,2,2,2,2,2,2,2,2,2,2,2,2,2,2,2,2,2,2,2,2,2,2,
2,2,2,2,2,2,2,2,2,2,2,2,2,2,4),(-2.51290263866645,-2.47973011981934,-2.47687838336318,
-2.4754543019939,-2.47450637763105,-2.47359717657777,-2.47278313890905,
-2.47173415476316,-2.46999790889112,-2.45987326217793,-2.43689520006323,
-2.42523894652728,-2.41513819529139,-2.38741498789146,-2.37825479294101,
-2.37562306929992,-2.37401630677287,-2.37256204358753,-2.37069717403871,
-2.36684878503042,-2.32278899666483,-2.2907434005837,-2.28159864658033,
-2.27633001841743,-2.27485682249618,-2.27395406575148,-2.27313829126578,
-2.27207713911402,-2.27029968474887,-2.25936226367964,-2.24654594397127,
-2.20142200124546,-2.18715731591929,-2.17860961507587,-2.17596952937816,
-2.17436088760221,-2.17290701841427,-2.17104556262997,-2.16807370470927,
-2.15208061106345,-2.14310410972149,-2.09637996204847,-2.08358561876969,
-2.07690028803354,-2.07530564152039,-2.07437529290822,-2.07356505117363,
-2.07253308948188,-2.07049294734063,-2.05761840199576,-2.05179205883425,
-2.01952404619975,-1.98145347040855,-1.97732896905583,-1.97541074887351,
-1.9739492038865,-1.97256149495135,-1.97022442220972,-1.96400845617728,
-1.91379525965114,-1.89325566706623,-1.88286096088637,-1.87706461298844,
-1.87553935050035,-1.87463165560911,-1.87381708342562,-1.87276494088064,
-1.87049423633264,-1.83336638788513,-1.80335267529129,-1.78062290291438,
-1.77722326985005,-1.77544932620379,-1.77414240546558,-1.77272761853201,
-1.77025329768429,-1.76410827515316,-1.71785869438524,-1.67957896568547,
-1.67664367443911,-1.67546301316162,-1.6746300030873,-1.67386895169163,
-1.67282797682456,-1.67076186678387,-1.63497006790056,-1.60450569083791,
-1.58885034863243,-1.5795421742219,-1.5769154276754,-1.57530955561765,-1.57385469711829,
-1.57198711109074,-1.56812610418335,-1.52486297318037,-1.49501981977373,
-1.48383720702256,-1.47773407080385,-1.47618175485276,-1.47526796178253,
-1.47445467905634,-1.47341298503938,-1.4717018526904,-1.46205089338169,
-1.45888748788825,-1.40401280454187,-1.38885755828111,-1.37976632101085,
-1.37716134329457,-1.37556036666545,-1.37410441372813,-1.37222766355903,
-1.36831956269003,-1.33201740601209,-1.29816353075714,-1.28497028464304,
-1.27812668621169,-1.27651478412686,-1.2755877887263,-1.27477696442944,
-1.27373966454656,-1.27160380759659,-1.25693941156251,-1.23050542730217,
-1.18600250189791,-1.18209614667404,-1.17833294029778,-1.17648475236689,
-1.17503225814045,-1.17341587345087,-1.17074167409172,-1.16093994983232,
-1.14411690791391,-1.11271461474076,-1.08943789072646,-1.07903767343225,
-1.07728693542252,-1.07623357895926,-1.07541882888513,-1.07451176338701,
-1.07298938074197,-1.06722507935204,-1.05691280156251,-1.0295934499279,
-0.982439373647723,-0.978670629694255,-0.976821397650103,-0.97536885029814,
-0.973753199333288,-0.971082053494814,-0.961311822767727,-0.944563885643717,
-0.913220829775399,-0.890278788010786,-0.879419393404867,-0.877645695181092,
-0.876585617404193,-0.875769962364344,-0.874866562534489,-0.873360457273545,
-0.867772451398172,-0.816088873812106,-0.782939753848354,-0.779057389371201,
-0.777185822610964,-0.775730695191473,-0.774127395324874,-0.771511349941322,
-0.762307749492934,-0.746891087061412,-0.716592481286442,-0.69099289446969,
-0.679780396665591,-0.677989579009808,-0.676924531926145,-0.676108209665247,
-0.675207485965857,-0.673713151295325,-0.668248881839877,-0.621259459467422,
-0.583328322254114,-0.579418498201252,-0.577541640178106,-0.576085921637413,
-0.574485523106977,-0.571882206311651,-0.562804042799036,-0.547675335952938,
-0.517609013257925,-0.480561084133031,-0.478290396652119,-0.477238347288493,
-0.476423887995528,-0.475516356485675,-0.473991460344343,-0.468197492753957,
-0.457809629451998,-0.430272445371526,-0.383480207330429,-0.379701074965947,
-0.377849960450568,-0.376397403387119,-0.374920448077874,-0.37246596139373,
-0.369568108065626,-0.3640392875826,-0.350536032217847,-0.294888758217795,
-0.292140623241821,-0.280461447916172,-0.278473422570434,-0.27745264000543,
-0.276643356604188,-0.275705237214562,-0.274042618433334,-0.266491524910349,
-0.217715711568212,-0.183932697841923,-0.180044256181476,-0.178171513528571,
-0.176716252580075,-0.176698987716623,-0.176682356260034,-0.176666329637557,
-0.176650880787118,-0.176635984134886,-0.176621615491089,-0.176607751969285,
-0.176594371908458,-0.176581454781815,-0.176568981136048,-0.176556932521543,
-0.176545291430695,-0.176534041245863,-0.176523166174698,-0.17651265120998,
-0.176502482077711,-0.17649264519348,-0.176483127621512,-0.176473917056579,
-0.176465001764495,-0.174809102909438,-0.171925927210577,-0.168397887116606,
-0.161144032794144,-0.141248451103759,-0.0830076872079403,-0.0794405920852786,
-0.0781220096349165,-0.0773459935269317,-0.076523549719491,-0.0754022315016852,
-0.0728184844714701,-0.0409558825915921,-0.000592896245600241),
 .UNSPECIFIED.);
#797=B_SPLINE_CURVE_WITH_KNOTS('',3,(#17182,#17183,#17184,#17185,#17186,
#17187,#17188,#17189,#17190,#17191,#17192,#17193,#17194,#17195,#17196,#17197,
#17198,#17199,#17200,#17201,#17202,#17203,#17204,#17205,#17206,#17207,#17208,
#17209,#17210,#17211,#17212,#17213,#17214,#17215,#17216,#17217,#17218,#17219,
#17220,#17221,#17222,#17223,#17224,#17225,#17226,#17227,#17228,#17229,#17230,
#17231,#17232,#17233,#17234,#17235,#17236,#17237,#17238,#17239,#17240,#17241,
#17242,#17243,#17244,#17245,#17246,#17247,#17248,#17249,#17250,#17251,#17252,
#17253,#17254,#17255,#17256,#17257,#17258,#17259,#17260,#17261,#17262,#17263,
#17264,#17265,#17266,#17267,#17268,#17269,#17270,#17271,#17272,#17273,#17274,
#17275,#17276,#17277,#17278,#17279,#17280,#17281,#17282,#17283,#17284,#17285,
#17286,#17287,#17288,#17289,#17290,#17291,#17292,#17293,#17294,#17295,#17296,
#17297,#17298,#17299,#17300,#17301,#17302,#17303,#17304,#17305,#17306,#17307,
#17308,#17309,#17310,#17311,#17312,#17313,#17314,#17315,#17316,#17317,#17318,
#17319,#17320,#17321,#17322,#17323,#17324,#17325,#17326,#17327,#17328,#17329,
#17330,#17331,#17332,#17333,#17334,#17335,#17336,#17337,#17338,#17339,#17340,
#17341,#17342,#17343,#17344,#17345,#17346,#17347,#17348,#17349,#17350,#17351,
#17352,#17353,#17354,#17355,#17356,#17357,#17358,#17359,#17360,#17361,#17362,
#17363,#17364,#17365,#17366,#17367,#17368,#17369,#17370,#17371,#17372,#17373,
#17374,#17375,#17376,#17377,#17378,#17379,#17380,#17381,#17382,#17383,#17384,
#17385,#17386,#17387,#17388,#17389,#17390,#17391,#17392,#17393,#17394,#17395,
#17396,#17397,#17398,#17399,#17400,#17401,#17402,#17403,#17404,#17405,#17406,
#17407,#17408,#17409,#17410,#17411,#17412,#17413,#17414,#17415,#17416,#17417,
#17418,#17419,#17420,#17421,#17422,#17423,#17424,#17425,#17426,#17427,#17428,
#17429,#17430,#17431,#17432,#17433,#17434,#17435,#17436,#17437,#17438,#17439,
#17440,#17441,#17442,#17443,#17444,#17445,#17446,#17447,#17448,#17449,#17450,
#17451,#17452,#17453,#17454,#17455,#17456,#17457,#17458,#17459,#17460,#17461,
#17462,#17463,#17464,#17465,#17466,#17467,#17468,#17469,#17470,#17471,#17472,
#17473,#17474,#17475,#17476,#17477,#17478,#17479,#17480,#17481,#17482,#17483,
#17484,#17485,#17486,#17487,#17488,#17489,#17490,#17491,#17492,#17493,#17494,
#17495,#17496,#17497,#17498,#17499,#17500,#17501,#17502,#17503,#17504,#17505,
#17506,#17507,#17508,#17509,#17510,#17511,#17512,#17513,#17514,#17515,#17516,
#17517,#17518,#17519,#17520,#17521,#17522,#17523,#17524,#17525,#17526,#17527,
#17528,#17529,#17530,#17531,#17532,#17533,#17534,#17535,#17536,#17537,#17538,
#17539,#17540,#17541,#17542,#17543,#17544,#17545,#17546,#17547,#17548,#17549,
#17550,#17551,#17552,#17553,#17554,#17555,#17556,#17557,#17558,#17559,#17560,
#17561,#17562,#17563,#17564,#17565,#17566,#17567,#17568,#17569,#17570,#17571,
#17572,#17573,#17574,#17575,#17576,#17577,#17578,#17579,#17580,#17581,#17582,
#17583,#17584,#17585,#17586,#17587,#17588,#17589,#17590,#17591,#17592,#17593,
#17594,#17595,#17596,#17597,#17598,#17599,#17600,#17601,#17602,#17603,#17604,
#17605,#17606,#17607,#17608,#17609,#17610,#17611,#17612,#17613,#17614,#17615,
#17616,#17617,#17618,#17619,#17620,#17621,#17622,#17623,#17624,#17625,#17626,
#17627,#17628,#17629,#17630,#17631,#17632,#17633,#17634,#17635,#17636,#17637,
#17638,#17639,#17640,#17641,#17642,#17643,#17644,#17645,#17646,#17647,#17648,
#17649,#17650,#17651,#17652,#17653,#17654,#17655,#17656,#17657,#17658,#17659,
#17660,#17661,#17662,#17663,#17664,#17665,#17666,#17667,#17668,#17669,#17670,
#17671,#17672,#17673,#17674,#17675,#17676,#17677,#17678,#17679,#17680,#17681,
#17682,#17683,#17684,#17685,#17686,#17687,#17688,#17689,#17690,#17691,#17692,
#17693,#17694,#17695,#17696,#17697,#17698,#17699,#17700,#17701,#17702,#17703,
#17704,#17705,#17706,#17707,#17708,#17709,#17710,#17711,#17712,#17713,#17714,
#17715,#17716,#17717,#17718,#17719,#17720,#17721,#17722,#17723,#17724,#17725,
#17726,#17727,#17728,#17729,#17730,#17731,#17732,#17733,#17734,#17735,#17736,
#17737,#17738,#17739,#17740,#17741,#17742,#17743,#17744,#17745,#17746,#17747,
#17748,#17749,#17750,#17751,#17752,#17753,#17754,#17755,#17756,#17757,#17758,
#17759,#17760,#17761,#17762,#17763,#17764,#17765,#17766,#17767,#17768,#17769,
#17770,#17771),.UNSPECIFIED.,.F.,.F.,(4,2,2,2,2,2,2,2,2,2,2,2,2,2,2,2,2,
2,2,2,2,2,2,2,2,2,2,2,2,2,2,2,2,2,2,2,2,2,2,2,2,2,2,2,2,2,2,2,2,2,2,2,2,
2,2,2,2,2,2,2,2,2,2,2,2,2,2,2,2,2,2,2,2,2,2,2,2,2,2,2,2,2,2,2,2,2,2,2,2,
2,2,2,2,2,2,2,2,2,2,2,2,2,2,2,2,2,2,2,2,2,2,2,2,2,2,2,2,2,2,2,2,2,2,2,2,
2,2,2,2,2,2,2,2,2,2,2,2,2,2,2,2,2,2,2,2,2,2,2,2,2,2,2,2,2,2,2,2,2,2,2,2,
2,2,2,2,2,2,2,2,2,2,2,2,2,2,2,2,2,2,2,2,2,2,2,2,2,2,2,2,2,2,2,2,2,2,2,2,
2,2,2,2,2,2,2,2,2,2,2,2,2,2,2,2,2,2,2,2,2,2,2,2,2,2,2,2,2,2,2,2,2,2,2,2,
2,2,2,2,2,2,2,2,2,2,2,2,2,2,2,2,2,2,2,2,2,2,2,2,2,2,2,2,2,2,2,2,2,2,2,2,
2,2,2,2,2,2,2,2,2,2,2,2,2,2,2,2,2,2,2,2,2,2,2,2,2,4),(-2.5085577871456,
-2.49262769230154,-2.48973435213939,-2.48789106392997,-2.48647124813858,
-2.48508379812839,-2.48370772053238,-2.48142077175534,-2.47549771094919,
-2.47408501189765,-2.47255980809686,-2.46873366496435,-2.45991519426738,
-2.40424748579275,-2.39404164677233,-2.38832358910043,-2.3868074239447,
-2.38590289490233,-2.38508961313634,-2.38403709775285,-2.38228553318593,
-2.3718202117363,-2.36966228132628,-2.31948581048527,-2.30125336278384,
-2.2944264626496,-2.29105236712866,-2.28826698358676,-2.28663851850139,
-2.28663067064916,-2.28662272345487,-2.28661467543457,-2.28660652510974,
-2.28659827095719,-2.28658991144072,-2.2865814450022,-2.28657287005424,
-2.28656418497052,-2.28655538811812,-2.2865464778247,-2.28653745239372,
-2.28652830984985,-2.28651955427403,-2.28651030289548,-2.28650052715088,
-2.28649019680124,-2.28647927996775,-2.28502880740622,-2.28317527238802,
-2.2793732862155,-2.25099595887576,-2.21419312138386,-2.19740890154388,
-2.18937661615718,-2.18768474224462,-2.18674137401547,-2.18593440908957,
-2.18492527086308,-2.18335403892253,-2.17589274737912,-2.1144368056051,
-2.10002498690207,-2.09423685596148,-2.0912431577006,-2.08871494933066,
-2.08714624463599,-2.08569445045336,-2.08382894116673,-2.07996553795128,
-2.04779673602627,-2.01097855770539,-1.99705169007737,-1.98995668162642,
-1.98832857206545,-1.98739927327844,-1.98659089164357,-1.9855625315347,
-1.98353329134673,-1.97084294733751,-1.94685960502824,-1.91667531680973,
-1.90132215607051,-1.8921502882157,-1.88954092074849,-1.88794121408498,
-1.88648902004258,-1.88462076714932,-1.88074361809504,-1.8477928275812,
-1.8448442168733,-1.8107340838666,-1.79755487682282,-1.7907210379829,-1.78911228750673,
-1.78818724783696,-1.78737822616853,-1.78634335323482,-1.78421290661734,
-1.76959990887754,-1.76504705565105,-1.74816118623124,-1.71780408648842,
-1.70223399560629,-1.69296821139032,-1.69034942535417,-1.6887475801415,
-1.68729582134265,-1.68543144899528,-1.68157433216095,-1.6387494611109,
-1.60879460180205,-1.59752778361971,-1.59139651382713,-1.58984407923392,
-1.58893151444945,-1.58812019598414,-1.5870821456267,-1.58537931282474,
-1.57583137057058,-1.51628502899276,-1.5021563696958,-1.49644926850228,
-1.49215545041037,-1.49020807995149,-1.48874461413679,-1.4873699741117,
-1.48509017609615,-1.47921265445488,-1.44838403368757,-1.39977699740586,
-1.3922634976555,-1.39060578928645,-1.3896699260512,-1.38886226783422,-1.38784312635858,
-1.38585707514599,-1.37416145435572,-1.32286906489092,-1.30484185569655,
-1.29455155839888,-1.29183658750595,-1.29021337524731,-1.28876598453411,
-1.28693949272978,-1.28407564608855,-1.2697554438151,-1.26572524824921,
-1.25459880813904,-1.20236843252919,-1.1933193812704,-1.19164438808857,
-1.19060353149748,-1.18979384092836,-1.18887246850041,-1.18728050255747,
-1.18066543079516,-1.16809914869998,-1.12891292499655,-1.09722064982594,
-1.09336508253521,-1.09150096717359,-1.09004918758919,-1.08844709507886,
-1.08582739633415,-1.07655320042075,-1.06096150002224,-1.0305595962796,
-1.02818175359588,-1.00602709186288,-0.994340258008126,-0.992354643852799,
-0.99133558839003,-0.990527927343633,-0.989591976100997,-0.987933909679917,
-0.980415261503741,-0.93180549014593,-0.89800988569456,-0.89412669165631,
-0.892257242704192,-0.89080488210923,-0.889205763314542,-0.886599095726911,
-0.877454453400216,-0.862161797096055,-0.831999139486753,-0.825847376604896,
-0.795619172790457,-0.793265844149407,-0.792199620432507,-0.791384467530498,
-0.790487266337861,-0.789003513181577,-0.783628672569723,-0.77426996911521,
-0.75073873339369,-0.702330226388538,-0.699258405472533,-0.695058802223551,
-0.693149760888062,-0.691687092373907,-0.690121278343756,-0.687664512576643,
-0.679902703535731,-0.625203211144041,-0.605903288709666,-0.595665610335983,
-0.593925828127673,-0.592876851229636,-0.592064133232738,-0.59115784240309,
-0.589633493580023,-0.583823599192919,-0.573386973941746,-0.545516872100343,
-0.499325996353757,-0.495542031327326,-0.493692126837332,-0.492242149017347,
-0.490632545348288,-0.487978766637682,-0.478352458886552,-0.461933656358038,
-0.430885367087165,-0.397031003067011,-0.394942095644275,-0.393896536196289,
-0.393135388384886,-0.392323563413582,-0.391189530092257,-0.389905135173534,
-0.387659660595867,-0.370202075436377,-0.335835335094181,-0.300276883913584,
-0.296379715526992,-0.29450752219128,-0.293054796427331,-0.291457057932786,
-0.288856651701757,-0.279774425148854,-0.264625233629228,-0.232496029252278,
-0.197782587315697,-0.195475885596427,-0.19441830401704,-0.193626902941515,
-0.193624263440276,-0.193621647425824,-0.193619050614331,-0.193616472797433,
-0.193613913790316,-0.193611373374273,-0.19360885134042,-0.193606347546237,
-0.19360386179843,-0.193601393895626,-0.193598943609693,-0.193596510792769,
-0.193594095275384,-0.193591696867853,-0.193589315413587,-0.19358695071515,
-0.193584602616196,-0.193582270959006,-0.193579955568018,-0.193577656292972,
-0.193575372969015,-0.193573105428499,-0.193570853517458,-0.193568617102638,
-0.193566395995654,-0.193564190067784,-0.193561999162903,-0.193559823161396,
-0.19355766189653,-0.193555515215056,-0.193553376672008,-0.193551239611196,
-0.193549116423135,-0.19264500912432,-0.191684908487208,-0.190231650513649,
-0.187558430343268,-0.162977944106383,-0.130155513385122,-0.100730850391224,
-0.0969068410978159,-0.0950466372798334,-0.0935927848156704,-0.0919831789769273,
-0.0893392632049909,-0.0798542638730792,-0.0637828867096131,-0.000620331519808279),
 .UNSPECIFIED.);
#798=B_SPLINE_CURVE_WITH_KNOTS('',3,(#17773,#17774,#17775,#17776,#17777,
#17778,#17779,#17780,#17781,#17782,#17783),.UNSPECIFIED.,.F.,.F.,(4,1,1,
1,1,1,1,1,4),(185.353966561798,185.386864292112,186.385545160473,187.384226028834,
188.382906897195,189.381587765555,190.380268633916,191.378949502277,191.637149496705),
 .UNSPECIFIED.);
#799=B_SPLINE_CURVE_WITH_KNOTS('',3,(#17785,#17786,#17787,#17788,#17789,
#17790,#17791,#17792,#17793,#17794,#17795,#17796,#17797,#17798,#17799,#17800,
#17801,#17802,#17803,#17804,#17805,#17806,#17807,#17808,#17809,#17810,#17811,
#17812,#17813,#17814,#17815,#17816,#17817,#17818,#17819,#17820,#17821,#17822,
#17823,#17824,#17825,#17826,#17827,#17828,#17829,#17830,#17831,#17832,#17833,
#17834,#17835,#17836,#17837,#17838,#17839,#17840,#17841,#17842,#17843,#17844,
#17845,#17846,#17847,#17848,#17849,#17850,#17851,#17852,#17853,#17854,#17855,
#17856,#17857,#17858,#17859,#17860,#17861,#17862,#17863,#17864,#17865,#17866,
#17867,#17868,#17869,#17870,#17871,#17872,#17873,#17874,#17875,#17876,#17877,
#17878,#17879,#17880,#17881,#17882,#17883,#17884,#17885,#17886,#17887,#17888,
#17889,#17890,#17891,#17892,#17893,#17894,#17895,#17896,#17897,#17898,#17899,
#17900,#17901,#17902,#17903,#17904,#17905,#17906,#17907,#17908,#17909,#17910,
#17911,#17912,#17913,#17914,#17915,#17916,#17917,#17918,#17919,#17920,#17921,
#17922,#17923,#17924,#17925,#17926,#17927,#17928,#17929,#17930,#17931,#17932,
#17933,#17934,#17935,#17936,#17937,#17938,#17939,#17940,#17941,#17942,#17943,
#17944,#17945,#17946,#17947,#17948,#17949,#17950,#17951,#17952,#17953,#17954,
#17955,#17956,#17957,#17958,#17959,#17960,#17961,#17962,#17963,#17964,#17965,
#17966,#17967,#17968,#17969,#17970,#17971,#17972,#17973,#17974,#17975,#17976,
#17977,#17978,#17979,#17980,#17981,#17982,#17983,#17984,#17985,#17986,#17987,
#17988,#17989,#17990,#17991,#17992,#17993,#17994,#17995,#17996,#17997,#17998,
#17999,#18000,#18001,#18002,#18003,#18004,#18005,#18006,#18007,#18008,#18009,
#18010,#18011,#18012,#18013,#18014,#18015,#18016,#18017,#18018,#18019,#18020,
#18021,#18022,#18023,#18024,#18025,#18026,#18027,#18028,#18029,#18030,#18031,
#18032,#18033,#18034,#18035,#18036,#18037,#18038,#18039,#18040,#18041,#18042,
#18043,#18044,#18045,#18046,#18047,#18048,#18049,#18050,#18051,#18052,#18053,
#18054,#18055,#18056,#18057,#18058,#18059,#18060,#18061,#18062,#18063,#18064,
#18065,#18066,#18067,#18068,#18069,#18070,#18071,#18072,#18073,#18074,#18075,
#18076,#18077,#18078,#18079,#18080,#18081,#18082,#18083,#18084,#18085,#18086,
#18087,#18088,#18089,#18090,#18091,#18092,#18093,#18094,#18095,#18096,#18097,
#18098,#18099,#18100,#18101,#18102,#18103,#18104,#18105,#18106,#18107,#18108,
#18109,#18110,#18111,#18112,#18113,#18114,#18115,#18116,#18117,#18118,#18119,
#18120,#18121,#18122,#18123,#18124,#18125,#18126,#18127,#18128,#18129,#18130,
#18131,#18132,#18133,#18134,#18135,#18136,#18137,#18138,#18139,#18140,#18141,
#18142,#18143,#18144,#18145,#18146,#18147,#18148,#18149,#18150,#18151,#18152,
#18153,#18154,#18155,#18156,#18157,#18158,#18159,#18160,#18161,#18162,#18163,
#18164,#18165,#18166,#18167,#18168,#18169,#18170,#18171,#18172,#18173,#18174,
#18175,#18176,#18177,#18178,#18179,#18180,#18181,#18182,#18183,#18184,#18185,
#18186,#18187,#18188,#18189,#18190,#18191,#18192,#18193,#18194,#18195,#18196,
#18197,#18198,#18199,#18200,#18201,#18202,#18203,#18204,#18205,#18206,#18207,
#18208,#18209,#18210,#18211,#18212,#18213,#18214,#18215,#18216,#18217,#18218,
#18219,#18220,#18221,#18222,#18223,#18224,#18225,#18226,#18227,#18228,#18229,
#18230,#18231,#18232,#18233,#18234,#18235,#18236,#18237,#18238,#18239,#18240,
#18241,#18242,#18243,#18244,#18245,#18246,#18247,#18248,#18249,#18250,#18251,
#18252,#18253,#18254,#18255,#18256,#18257,#18258,#18259,#18260,#18261,#18262,
#18263,#18264,#18265,#18266,#18267,#18268,#18269,#18270,#18271,#18272,#18273,
#18274,#18275,#18276,#18277,#18278,#18279,#18280,#18281,#18282,#18283,#18284,
#18285,#18286,#18287,#18288,#18289,#18290,#18291,#18292,#18293,#18294,#18295,
#18296,#18297,#18298,#18299,#18300,#18301,#18302),.UNSPECIFIED.,.F.,.F.,
(4,2,2,2,2,2,2,2,2,2,2,2,2,2,2,2,2,2,2,2,2,2,2,2,2,2,2,2,2,2,2,2,2,2,2,
2,2,2,2,2,2,2,2,2,2,2,2,2,2,2,2,2,2,2,2,2,2,2,2,2,2,2,2,2,2,2,2,2,2,2,2,
2,2,2,2,2,2,2,2,2,2,2,2,2,2,2,2,2,2,2,2,2,2,2,2,2,2,2,2,2,2,2,2,2,2,2,2,
2,2,2,2,2,2,2,2,2,2,2,2,2,2,2,2,2,2,2,2,2,2,2,2,2,2,2,2,2,2,2,2,2,2,2,2,
2,2,2,2,2,2,2,2,2,2,2,2,2,2,2,2,2,2,2,2,2,2,2,2,2,2,2,2,2,2,2,2,2,2,2,2,
2,2,2,2,2,2,2,2,2,2,2,2,2,2,2,2,2,2,2,2,2,2,2,2,2,2,2,2,2,2,2,2,2,2,2,2,
2,2,2,2,2,2,2,2,2,2,2,2,2,2,2,2,2,2,2,2,2,2,2,2,2,2,2,2,2,2,2,2,2,2,2,2,
2,2,2,2,2,2,2,4),(-2.51398133414389,-2.48094175545532,-2.47168106510804,
-2.46926076959548,-2.467614212309,-2.46601368312452,-2.46455814540407,-2.46268194213675,
-2.45877502270415,-2.41991617881569,-2.39953857607119,-2.37417890363605,
-2.36845741052523,-2.366928696018,-2.36602036660579,-2.36520619840469,-2.36415585310862,
-2.36189386455443,-2.32460157946666,-2.2938197608203,-2.27934229752528,
-2.27057952874916,-2.26802678361449,-2.26642148068764,-2.26496706728765,
-2.26309995428477,-2.25923957173121,-2.22765804283565,-2.17406261966766,
-2.16893403212184,-2.16732994053434,-2.16640475970811,-2.16559379572614,
-2.16455404267801,-2.16240531666918,-2.14737899368109,-2.14144762068344,
-2.09292531544002,-2.07922365938938,-2.0708087943132,-2.06831946276363,
-2.06671666613336,-2.06526147818122,-2.0633891089575,-2.05950245858449,
-2.02601915280448,-1.97696899466405,-1.96935716017211,-1.96769038473055,
-1.96675133922251,-1.96594213101539,-1.96492257083077,-1.96294027819942,
-1.95137205100061,-1.94888585697622,-1.9262629161582,-1.89595926110847,
-1.88050481778762,-1.87128362186004,-1.86866567160033,-1.86706185467856,
-1.86560668372267,-1.86373565688326,-1.85985657030819,-1.81812693396771,
-1.78941751686676,-1.77639289024704,-1.76960934477522,-1.7680020702245,
-1.76707612572484,-1.76626518367929,-1.7652263688428,-1.76308271238347,
-1.74820159192034,-1.74181643349194,-1.72637341381769,-1.69615454481816,
-1.68080770437188,-1.6716330405734,-1.66901965959808,-1.66741680992759,
-1.66596131494738,-1.66408818780691,-1.66019864878989,-1.62630758762357,
-1.57756865760962,-1.57003235489076,-1.56837050933725,-1.56743244860871,
-1.56662297952755,-1.56560166318075,-1.56361170249996,-1.55190054996639,
-1.54932817092889,-1.52694207947948,-1.49663256533507,-1.48117464996275,
-1.47195151558511,-1.46933307986235,-1.46772897923454,-1.4662735598391,
-1.46440222611581,-1.46052254867567,-1.41878494906313,-1.38988249714859,
-1.37105324413692,-1.36897575595239,-1.36795002564225,-1.36721689675486,
-1.36642390835619,-1.36501970276723,-1.36085863534669,-1.3198402164215,
-1.27489197203946,-1.27067773545672,-1.26874244409121,-1.26727813992438,
-1.26589540141608,-1.26358485885676,-1.25753004970178,-1.22496965591972,
-1.19146752549143,-1.18668171931917,-1.17145572812837,-1.16929948115566,
-1.16825810725949,-1.16744682266727,-1.16652231652083,-1.16492184549236,
-1.15822808596142,-1.14545663805007,-1.13275059197035,-1.07758429324634,
-1.0717714755534,-1.0694988870727,-1.06812350832289,-1.06665540160461,-1.06469523726938,
-1.06034602757736,-1.05454923706921,-1.04011897833516,-0.978592954777521,
-0.971000621473652,-0.969417613263893,-0.968403624918487,-0.967594614630355,
-0.966650955466922,-0.964963866846999,-0.957049131125499,-0.940661775149694,
-0.886519352839538,-0.873540572419314,-0.870763856863685,-0.868962034808591,
-0.867513975470122,-0.865868306229021,-0.863062938440502,-0.851758961183308,
-0.799746916106645,-0.772186862548338,-0.769826244760251,-0.768757155317357,
-0.767939996180307,-0.767040785690155,-0.765554130552059,-0.760173246858827,
-0.750808700550199,-0.727291553503988,-0.678664799241963,-0.676086604778511,
-0.671634634653937,-0.669805992682046,-0.668448562896624,-0.666967512786282,
-0.664932672995948,-0.66016444508058,-0.639798857059222,-0.583519883951563,
-0.571864926345619,-0.569877615655351,-0.568856753530014,-0.568047175675012,
-0.567108451917473,-0.565444111897216,-0.557874383597566,-0.509016016821418,
-0.475301642092305,-0.471410891307572,-0.46953725809826,-0.468081403714759,
-0.466478192390659,-0.463864299432147,-0.454688686861974,-0.439338771628266,
-0.409086590448366,-0.372533950981189,-0.370253955200523,-0.369199870324798,
-0.368384832564936,-0.368383319540139,-0.368382272221675,-0.368381225017134,
-0.368380177959486,-0.368379131076913,-0.368378084328339,-0.368377037698587,
-0.368375991213697,-0.368374944861903,-0.368373898606277,-0.368372852471212,
-0.368371806486869,-0.36837076064387,-0.368369714916329,-0.368368669289933,
-0.36836762382266,-0.368366578487437,-0.368365533305993,-0.368364488214365,
-0.368363443206881,-0.368362398312207,-0.368361353537718,-0.368360308853475,
-0.368359264386209,-0.368358220053414,-0.368357175811266,-0.368356131622976,
-0.36745770110628,-0.365984347803652,-0.364179848601488,-0.360563941382592,
-0.313953809935299,-0.275587280122757,-0.271674393658817,-0.269796473049413,
-0.268340110753364,-0.266739186170573,-0.264135421636745,-0.255059780812809,
-0.239939208821071,-0.192696679347792,-0.187694572590075,-0.172574189801506,
-0.170421422503793,-0.169380625704051,-0.168569275656492,-0.167807751793634,
-0.166413642124588,-0.161945734624372,-0.154620083623877,-0.131233799457145,
-0.079072857372386,-0.0729821580967447,-0.0706658261729997,-0.069281865159288,
-0.06781792596521,-0.065885919103819,-0.061689948373313,-0.0208029638340278,
-0.00059283742129488),.UNSPECIFIED.);
#800=B_SPLINE_CURVE_WITH_KNOTS('',3,(#18304,#18305,#18306,#18307,#18308,
#18309,#18310,#18311,#18312,#18313,#18314,#18315,#18316,#18317,#18318,#18319,
#18320,#18321,#18322,#18323,#18324,#18325,#18326,#18327,#18328,#18329,#18330,
#18331,#18332,#18333,#18334,#18335,#18336,#18337,#18338,#18339,#18340,#18341,
#18342,#18343,#18344,#18345,#18346,#18347,#18348,#18349,#18350,#18351,#18352,
#18353,#18354,#18355,#18356,#18357,#18358,#18359,#18360,#18361,#18362,#18363,
#18364,#18365,#18366,#18367,#18368,#18369,#18370,#18371,#18372,#18373,#18374,
#18375,#18376,#18377,#18378,#18379,#18380,#18381,#18382,#18383,#18384,#18385,
#18386,#18387,#18388,#18389,#18390,#18391,#18392,#18393,#18394,#18395,#18396,
#18397,#18398,#18399,#18400,#18401,#18402,#18403,#18404,#18405,#18406,#18407,
#18408,#18409,#18410,#18411,#18412,#18413,#18414,#18415,#18416,#18417,#18418,
#18419,#18420,#18421,#18422,#18423,#18424,#18425,#18426,#18427,#18428,#18429,
#18430,#18431,#18432,#18433,#18434,#18435,#18436,#18437,#18438,#18439,#18440,
#18441,#18442,#18443,#18444,#18445,#18446,#18447,#18448,#18449,#18450,#18451,
#18452,#18453,#18454,#18455,#18456,#18457,#18458,#18459,#18460,#18461,#18462,
#18463,#18464,#18465,#18466,#18467,#18468,#18469,#18470,#18471,#18472,#18473,
#18474,#18475,#18476,#18477,#18478,#18479,#18480,#18481,#18482,#18483,#18484,
#18485,#18486,#18487,#18488,#18489,#18490),.UNSPECIFIED.,.F.,.F.,(4,3,3,
3,3,3,3,3,3,3,3,3,3,3,3,3,3,3,3,3,3,3,3,3,3,3,3,3,3,3,3,3,3,3,3,3,3,3,3,
3,3,3,3,3,3,3,3,3,3,3,3,3,3,3,3,3,3,3,3,3,3,3,4),(204.203522483337,204.361800790967,
204.466746605831,204.57153467083,204.676199201471,204.780797709263,204.885365778675,
204.989938950007,205.094622905074,205.199367968475,205.304295814935,205.360481659328,
205.465427474192,205.570215539191,205.674880069832,205.779478577624,205.884046647036,
205.988619818368,206.093303773436,206.198048836836,206.302976683297,206.359162527688,
206.464108342552,206.568896407551,206.673560938192,206.778159445984,206.882727515396,
206.987300686728,207.091984641796,207.196729705196,207.301657551657,207.357843396049,
207.462789210913,207.567577275912,207.672241806554,207.776840314345,207.881408383758,
207.98598155509,208.090665510158,208.195410573558,208.300338420019,208.35652426441,
208.461470079274,208.566258144273,208.670922674914,208.775521182706,208.880089252118,
208.984662423451,209.089346378518,209.194091441919,209.299019288379,209.355205132771,
209.460150947635,209.564939012634,209.669603543275,209.774202051067,209.878770120479,
209.983343291811,210.088027246879,210.192772310279,210.297700156739,210.353886001131,
210.486707790516),.UNSPECIFIED.);
#801=B_SPLINE_CURVE_WITH_KNOTS('',3,(#18492,#18493,#18494,#18495,#18496,
#18497,#18498,#18499,#18500,#18501,#18502,#18503,#18504,#18505,#18506,#18507,
#18508,#18509,#18510,#18511,#18512,#18513,#18514,#18515,#18516,#18517,#18518,
#18519,#18520,#18521,#18522,#18523,#18524,#18525,#18526,#18527,#18528,#18529,
#18530,#18531,#18532,#18533,#18534,#18535,#18536,#18537,#18538,#18539,#18540,
#18541,#18542,#18543,#18544,#18545,#18546,#18547,#18548,#18549,#18550,#18551,
#18552,#18553,#18554,#18555,#18556,#18557,#18558,#18559,#18560,#18561,#18562,
#18563,#18564,#18565,#18566,#18567,#18568,#18569,#18570,#18571,#18572,#18573,
#18574,#18575,#18576,#18577,#18578,#18579,#18580,#18581,#18582,#18583,#18584,
#18585,#18586,#18587,#18588,#18589,#18590,#18591,#18592,#18593,#18594,#18595,
#18596,#18597,#18598,#18599,#18600,#18601,#18602,#18603,#18604,#18605,#18606,
#18607,#18608,#18609,#18610,#18611,#18612,#18613,#18614,#18615,#18616,#18617,
#18618,#18619,#18620,#18621,#18622,#18623,#18624,#18625,#18626,#18627,#18628,
#18629,#18630,#18631,#18632,#18633,#18634,#18635,#18636,#18637,#18638,#18639,
#18640,#18641,#18642,#18643,#18644,#18645,#18646,#18647,#18648,#18649,#18650,
#18651,#18652,#18653,#18654,#18655,#18656,#18657,#18658,#18659,#18660,#18661,
#18662,#18663,#18664,#18665,#18666,#18667,#18668,#18669,#18670,#18671,#18672,
#18673,#18674,#18675,#18676,#18677,#18678,#18679,#18680,#18681,#18682,#18683,
#18684,#18685,#18686,#18687,#18688,#18689,#18690,#18691,#18692,#18693,#18694,
#18695,#18696,#18697,#18698,#18699,#18700,#18701,#18702,#18703,#18704,#18705,
#18706,#18707,#18708,#18709,#18710,#18711,#18712,#18713,#18714,#18715,#18716,
#18717,#18718,#18719,#18720,#18721,#18722,#18723,#18724,#18725,#18726,#18727,
#18728,#18729,#18730,#18731,#18732,#18733,#18734,#18735,#18736,#18737,#18738,
#18739,#18740,#18741,#18742,#18743,#18744,#18745,#18746,#18747,#18748,#18749,
#18750,#18751,#18752,#18753,#18754,#18755,#18756,#18757,#18758,#18759,#18760,
#18761,#18762,#18763,#18764,#18765,#18766,#18767,#18768,#18769,#18770,#18771,
#18772,#18773,#18774,#18775,#18776,#18777,#18778,#18779,#18780,#18781,#18782,
#18783,#18784,#18785,#18786,#18787,#18788,#18789,#18790,#18791,#18792,#18793,
#18794,#18795,#18796,#18797,#18798,#18799,#18800,#18801,#18802,#18803,#18804,
#18805,#18806,#18807,#18808,#18809,#18810,#18811,#18812,#18813,#18814,#18815,
#18816,#18817,#18818,#18819,#18820,#18821,#18822,#18823,#18824,#18825,#18826,
#18827,#18828,#18829,#18830,#18831,#18832,#18833,#18834,#18835,#18836,#18837,
#18838,#18839,#18840,#18841,#18842,#18843,#18844,#18845,#18846,#18847,#18848,
#18849,#18850,#18851,#18852,#18853,#18854,#18855,#18856,#18857,#18858,#18859,
#18860,#18861,#18862,#18863,#18864,#18865,#18866,#18867,#18868,#18869,#18870,
#18871,#18872,#18873,#18874,#18875,#18876,#18877,#18878,#18879,#18880,#18881,
#18882,#18883,#18884,#18885,#18886,#18887,#18888,#18889,#18890,#18891,#18892,
#18893,#18894,#18895,#18896,#18897,#18898,#18899,#18900,#18901,#18902,#18903,
#18904,#18905,#18906,#18907,#18908,#18909,#18910,#18911,#18912,#18913,#18914,
#18915,#18916,#18917,#18918,#18919,#18920,#18921,#18922,#18923,#18924,#18925,
#18926,#18927,#18928,#18929,#18930,#18931,#18932,#18933,#18934,#18935,#18936,
#18937,#18938,#18939,#18940,#18941,#18942,#18943,#18944,#18945,#18946,#18947,
#18948,#18949,#18950,#18951,#18952,#18953,#18954,#18955,#18956,#18957,#18958,
#18959,#18960,#18961),.UNSPECIFIED.,.F.,.F.,(4,2,2,2,2,2,2,2,2,2,2,2,2,
2,2,2,2,2,2,2,2,2,2,2,2,2,2,2,2,2,2,2,2,2,2,2,2,2,2,2,2,2,2,2,2,2,2,2,2,
2,2,2,2,2,2,2,2,2,2,2,2,2,2,2,2,2,2,2,2,2,2,2,2,2,2,2,2,2,2,2,2,2,2,2,2,
2,2,2,2,2,2,2,2,2,2,2,2,2,2,2,2,2,2,2,2,2,2,2,2,2,2,2,2,2,2,2,2,2,2,2,2,
2,2,2,2,2,2,2,2,2,2,2,2,2,2,2,2,2,2,2,2,2,2,2,2,2,2,2,2,2,2,2,2,2,2,2,2,
2,2,2,2,2,2,2,2,2,2,2,2,2,2,2,2,2,2,2,2,2,2,2,2,2,2,2,2,2,2,2,2,2,2,2,2,
2,2,2,2,2,2,2,2,2,2,2,2,2,2,2,2,2,2,2,2,2,2,2,2,2,2,2,2,2,2,2,2,2,2,2,2,
2,2,2,2,2,4),(-2.51398629788239,-2.46795087027503,-2.45375792511426,-2.44802915902984,
-2.44372066163785,-2.44176833910706,-2.4403018443564,-2.4389248649769,-2.43664237175022,
-2.43076455586678,-2.37620732677608,-2.35512773261379,-2.34767501984731,
-2.34314505555221,-2.34174758160813,-2.34098617084092,-2.34017543526592,
-2.33913733429327,-2.33747475214223,-2.32867022671071,-2.29639307256834,
-2.27006620876583,-2.25472359085531,-2.24555126402546,-2.24293845690623,
-2.24133593971715,-2.23988073387095,-2.23800796090869,-2.2341190923721,
-2.20044650173763,-2.14899255054784,-2.14543282438832,-2.14364879179028,
-2.14221717507587,-2.14131504662893,-2.14050325883575,-2.13945604594684,
-2.13726952002486,-2.12112379858218,-2.11383712146277,-2.07301062995499,
-2.04741343427391,-2.04392878158255,-2.04213721919746,-2.04070351937282,
-2.03905594847783,-2.03624103787606,-2.02622526019384,-2.02422571609486,
-1.96229465709312,-1.95042955722146,-1.94621591151312,-1.94326177926346,
-1.94207804158348,-1.94124441069749,-1.94048395585791,-1.93944539085576,
-1.93738890901078,-1.90102604353356,-1.8707498351434,-1.85533307661067,
-1.84612785235754,-1.84351125960014,-1.84190760244773,-1.84045213619855,
-1.83858011333105,-1.83469673224155,-1.8015428631071,-1.74982927243646,
-1.74421850177414,-1.74270998574529,-1.74180588608246,-1.74099011554124,
-1.73993057960137,-1.73815926555082,-1.72735498866087,-1.70439004597293,
-1.67305654960071,-1.65629095477371,-1.64651143199589,-1.64383890037829,
-1.64222263885693,-1.64076968816644,-1.63892014226971,-1.63515145912288,
-1.58790912082465,-1.56059992226594,-1.55029203425454,-1.54452954770775,
-1.5430070281963,-1.54209976539471,-1.54128475449979,-1.54023095940987,
-1.53795254811452,-1.50134976579041,-1.47114503159617,-1.45582242719179,
-1.44665756377709,-1.44404467412986,-1.44244163736467,-1.4409856518575,
-1.43911144379228,-1.43521802906191,-1.40130362551224,-1.35256430487385,
-1.34502941999764,-1.34336733830977,-1.34242905943818,-1.34161934954842,
-1.34059766170652,-1.33860677522959,-1.32688557014606,-1.2754546390385,
-1.25738389272865,-1.24726459093063,-1.24447149821661,-1.24281226010264,
-1.24136531117254,-1.239581695986,-1.2361375512184,-1.21201628512939,-1.18120307382977,
-1.14632193050641,-1.14401154815011,-1.14295170194368,-1.14213579848125,
-1.14123165945308,-1.13972332033393,-1.13411584544945,-1.08241697174498,
-1.04926714359544,-1.04538330725497,-1.04351098147952,-1.04205524187987,
-1.04045124517652,-1.03783401235416,-1.02862572017281,-1.01320069702563,
-0.982887796839183,-0.957295450767591,-0.946065469682763,-0.94427328013483,
-0.943207602619392,-0.942390908167608,-0.941489893791444,-0.93999533270989,
-0.934533003263245,-0.887610383266269,-0.849571398535599,-0.845659993460124,
-0.843782354890947,-0.842326021382814,-0.840724937130614,-0.838120483254904,
-0.829038137833757,-0.813902253134339,-0.783822569963408,-0.746760700981982,
-0.744489072019817,-0.74343658076552,-0.742621776878917,-0.741713858657482,
-0.740188306727009,-0.734391777268359,-0.723999242427689,-0.696448676037504,
-0.649637519628826,-0.645857546669602,-0.644005798882366,-0.642552643705676,
-0.640937727852791,-0.638271064914987,-0.628553074240353,-0.611931652762077,
-0.580682067616873,-0.559228155728193,-0.556701905803012,-0.546514272292528,
-0.544774254392505,-0.543723952193214,-0.542909480711512,-0.542000435784042,
-0.540469695156486,-0.534614694140527,-0.524073647573948,-0.495787577525803,
-0.449980564436194,-0.446172688183363,-0.444315464396133,-0.442861733823497,
-0.441250000783348,-0.438662442267103,-0.435576713547999,-0.429546323112597,
-0.414289137702652,-0.369351229931412,-0.347390861158746,-0.345105559693886,
-0.344034282753848,-0.34321680111517,-0.342318685981859,-0.340836900981359,
-0.335617083853237,-0.326596388419606,-0.304521875158874,-0.265846398271644,
-0.264246566349837,-0.249331186080131,-0.246425209104387,-0.244583521476723,
-0.243131510861447,-0.24151085964431,-0.238959994599779,-0.229897518825946,
-0.214743514231785,-0.187954762381855,-0.150423878930759,-0.146171892594143,
-0.144755803688894,-0.143960391515718,-0.143227884822282,-0.142207334824263,
-0.14015576801684,-0.126838923942786,-0.105241763439404,-0.0849281950929156,
-0.0507288998778756,-0.0468327651080157,-0.044958088681128,-0.0435021124828918,
-0.0418994628204193,-0.0402501591703931,-0.0378240400501954,-0.028648503744147,
-0.000592063665398865),.UNSPECIFIED.);
#802=B_SPLINE_CURVE_WITH_KNOTS('',3,(#18963,#18964,#18965,#18966,#18967,
#18968,#18969,#18970,#18971,#18972,#18973,#18974,#18975,#18976,#18977,#18978,
#18979,#18980,#18981,#18982,#18983,#18984,#18985,#18986,#18987,#18988,#18989,
#18990,#18991,#18992,#18993,#18994,#18995,#18996,#18997,#18998,#18999,#19000,
#19001,#19002,#19003,#19004,#19005,#19006,#19007,#19008,#19009,#19010,#19011,
#19012,#19013,#19014,#19015,#19016,#19017,#19018,#19019,#19020,#19021,#19022,
#19023,#19024,#19025,#19026,#19027,#19028,#19029,#19030,#19031,#19032,#19033,
#19034,#19035,#19036,#19037,#19038,#19039,#19040,#19041,#19042,#19043,#19044,
#19045,#19046,#19047,#19048,#19049,#19050,#19051,#19052,#19053,#19054,#19055,
#19056,#19057,#19058,#19059,#19060,#19061,#19062,#19063,#19064,#19065,#19066,
#19067,#19068,#19069,#19070,#19071,#19072,#19073,#19074,#19075,#19076,#19077,
#19078,#19079,#19080,#19081,#19082,#19083,#19084,#19085,#19086,#19087,#19088,
#19089,#19090,#19091,#19092,#19093,#19094,#19095,#19096,#19097,#19098,#19099,
#19100,#19101,#19102,#19103,#19104,#19105,#19106,#19107,#19108,#19109,#19110,
#19111,#19112,#19113,#19114,#19115,#19116,#19117,#19118,#19119,#19120,#19121,
#19122,#19123,#19124,#19125,#19126,#19127,#19128,#19129,#19130,#19131,#19132,
#19133,#19134,#19135,#19136,#19137,#19138,#19139,#19140,#19141,#19142,#19143,
#19144,#19145,#19146,#19147,#19148,#19149,#19150,#19151,#19152,#19153,#19154,
#19155,#19156,#19157,#19158,#19159,#19160,#19161,#19162,#19163,#19164,#19165,
#19166,#19167,#19168,#19169,#19170,#19171,#19172,#19173,#19174,#19175,#19176,
#19177,#19178,#19179,#19180,#19181,#19182,#19183,#19184,#19185,#19186,#19187,
#19188,#19189,#19190,#19191,#19192,#19193,#19194,#19195,#19196,#19197,#19198,
#19199,#19200,#19201,#19202,#19203,#19204,#19205,#19206,#19207,#19208,#19209,
#19210,#19211,#19212,#19213,#19214,#19215,#19216,#19217,#19218,#19219,#19220,
#19221,#19222,#19223,#19224,#19225,#19226,#19227,#19228,#19229,#19230,#19231,
#19232,#19233,#19234,#19235,#19236,#19237,#19238,#19239,#19240,#19241,#19242,
#19243,#19244,#19245,#19246,#19247,#19248,#19249,#19250,#19251,#19252,#19253,
#19254,#19255,#19256,#19257,#19258,#19259,#19260,#19261,#19262,#19263,#19264,
#19265,#19266,#19267,#19268,#19269,#19270,#19271,#19272,#19273,#19274,#19275,
#19276,#19277,#19278,#19279,#19280,#19281,#19282,#19283,#19284,#19285,#19286,
#19287,#19288,#19289,#19290,#19291,#19292,#19293,#19294,#19295,#19296,#19297,
#19298,#19299,#19300,#19301,#19302,#19303,#19304,#19305,#19306,#19307,#19308,
#19309,#19310,#19311,#19312,#19313,#19314,#19315,#19316,#19317,#19318,#19319,
#19320,#19321,#19322,#19323,#19324,#19325,#19326,#19327,#19328,#19329,#19330,
#19331,#19332,#19333,#19334,#19335,#19336,#19337,#19338,#19339,#19340,#19341,
#19342,#19343,#19344,#19345,#19346,#19347,#19348,#19349,#19350,#19351,#19352,
#19353,#19354,#19355,#19356,#19357,#19358,#19359,#19360,#19361,#19362,#19363,
#19364,#19365,#19366,#19367,#19368,#19369,#19370,#19371,#19372,#19373,#19374,
#19375,#19376,#19377,#19378,#19379,#19380,#19381,#19382,#19383,#19384,#19385,
#19386,#19387,#19388,#19389,#19390,#19391,#19392,#19393,#19394,#19395,#19396,
#19397,#19398,#19399,#19400,#19401,#19402,#19403,#19404,#19405,#19406,#19407,
#19408,#19409,#19410,#19411,#19412,#19413,#19414,#19415,#19416,#19417,#19418,
#19419,#19420,#19421,#19422,#19423,#19424,#19425,#19426,#19427,#19428,#19429,
#19430,#19431,#19432,#19433,#19434,#19435,#19436,#19437,#19438,#19439,#19440,
#19441,#19442,#19443,#19444),.UNSPECIFIED.,.F.,.F.,(4,2,2,2,2,2,2,2,2,2,
2,2,2,2,2,2,2,2,2,2,2,2,2,2,2,2,2,2,2,2,2,2,2,2,2,2,2,2,2,2,2,2,2,2,2,2,
2,2,2,2,2,2,2,2,2,2,2,2,2,2,2,2,2,2,2,2,2,2,2,2,2,2,2,2,2,2,2,2,2,2,2,2,
2,2,2,2,2,2,2,2,2,2,2,2,2,2,2,2,2,2,2,2,2,2,2,2,2,2,2,2,2,2,2,2,2,2,2,2,
2,2,2,2,2,2,2,2,2,2,2,2,2,2,2,2,2,2,2,2,2,2,2,2,2,2,2,2,2,2,2,2,2,2,2,2,
2,2,2,2,2,2,2,2,2,2,2,2,2,2,2,2,2,2,2,2,2,2,2,2,2,2,2,2,2,2,2,2,2,2,2,2,
2,2,2,2,2,2,2,2,2,2,2,2,2,2,2,2,2,2,2,2,2,2,2,2,2,2,2,2,2,2,2,2,2,2,2,2,
2,2,2,2,2,2,2,2,2,2,2,2,2,2,4),(-2.51309486647585,-2.46452588930045,-2.46094116663356,
-2.45914826323717,-2.4576494174572,-2.4567478098884,-2.45593197253983,-2.45486927608813,
-2.453086102597,-2.4420255352352,-2.43843277892963,-2.43111971628948,-2.405392421698,
-2.38767560925038,-2.36508982731207,-2.36024618075138,-2.35864528251184,
-2.35728744241274,-2.35583828260136,-2.35401780075283,-2.35117926008268,
-2.33730556066251,-2.334453758959,-2.32625480943977,-2.29801301078951,-2.2744626637411,
-2.26500393823296,-2.25960626366736,-2.25810574279304,-2.25720374812444,
-2.25638799578237,-2.25532598790854,-2.25354520754058,-2.24253428624706,
-2.22097714946139,-2.18292362379156,-2.16980775565783,-2.16439254806274,
-2.16031387905904,-2.15840633487012,-2.15694081271484,-2.1555622038298,
-2.15327103465229,-2.1473369659475,-2.14591981266485,-2.14438456107695,
-2.08057895573882,-2.06709187948396,-2.06016038206725,-2.05853246833197,
-2.05760202894418,-2.05679186086151,-2.05576019222634,-2.054118872483,-2.04566050926726,
-1.98635478540625,-1.97116324576591,-1.96205681197062,-1.95945073368042,
-1.95784977531602,-1.95639429613266,-1.95451879930779,-1.95061564964523,
-1.9122884712373,-1.86562962491964,-1.86018177766145,-1.85868902080573,
-1.85778865759155,-1.85697224120178,-1.85590651960106,-1.85411338303643,
-1.84285209157823,-1.81731873832905,-1.78704944468702,-1.77163613179805,
-1.76243298576702,-1.75981699392366,-1.75821370721278,-1.75675857858477,
-1.7548869919427,-1.75100452292647,-1.71785927177196,-1.66615802778751,
-1.66054743981812,-1.65903916937886,-1.65813525603069,-1.65731968091199,
-1.65626043488747,-1.6539520179117,-1.61902442816531,-1.5882746936776,-1.57225488523342,
-1.56279070335583,-1.56014875015394,-1.55853954252568,-1.55708553295307,
-1.5552244118891,-1.55139597138592,-1.54758985539059,-1.50318070305179,
-1.476648339805,-1.46656096278245,-1.46088681024162,-1.45937260904248,-1.45846734449927,
-1.45765207990477,-1.45659525603037,-1.45429992149832,-1.41862252411368,
-1.38812023390852,-1.37241671979743,-1.36308782632622,-1.36045903942732,
-1.35885271605285,-1.35739796783441,-1.35553124698121,-1.35167462769991,
-1.3204085977723,-1.27007144186592,-1.26156056395693,-1.25983660101191,
-1.25888492787562,-1.25807657615387,-1.25707290305206,-1.25510375362371,
-1.24079202067717,-1.21609063419052,-1.16915613609416,-1.16279362666882,
-1.16043543835808,-1.15904342312763,-1.15758332852073,-1.15567692560501,
-1.1516158636112,-1.11588193122916,-1.07805959045072,-1.0625660108618,-1.06040029108135,
-1.05935701981257,-1.05854550079585,-1.05762210306724,-1.05602676657596,
-1.04939948221175,-1.03681228632728,-0.99747920820392,-0.965762754836832,
-0.96189920898257,-0.960031037518745,-0.958576010118798,-0.956970243233074,
-0.9543443313374,-0.945046024365567,-0.929411703607346,-0.898935442968246,
-0.863069605757695,-0.861003928934717,-0.859963008211846,-0.859201916306653,
-0.858368770369099,-0.857187762410253,-0.854250818055072,-0.815658168617676,
-0.769761600799003,-0.763559876006967,-0.761108077076767,-0.75969763367226,
-0.758389399258267,-0.756605539491975,-0.753159061395943,-0.72893837933841,
-0.6980750608891,-0.663372750675305,-0.661060458493613,-0.66000039729537,
-0.65918461428771,-0.658280921010864,-0.656773995080385,-0.651179249914653,
-0.599488007319517,-0.593077098673279,-0.566173045694003,-0.562399896453556,
-0.560549652098457,-0.559096835471611,-0.557481427861126,-0.554811942654126,
-0.545061626370288,-0.528362147765403,-0.468629265392385,-0.464876122725742,
-0.461714294190704,-0.460460154051417,-0.459696633159729,-0.458865475647186,
-0.457695213919508,-0.454824521605239,-0.450763715170569,-0.439517832063242,
-0.387719494778871,-0.385273888980008,-0.378997049002927,-0.365329186619738,
-0.362503240472882,-0.360686132528895,-0.359236618089068,-0.357633641330818,
-0.35499843718957,-0.351827658283479,-0.345566581213642,-0.329474825495522,
-0.294574901946369,-0.263910933857402,-0.261556569363376,-0.260488630919481,
-0.25967163669215,-0.258771830705841,-0.257282562398658,-0.251874872386638,
-0.24244542573165,-0.217008085240243,-0.18719000997461,-0.184706759178928,
-0.180765860424814,-0.165809038263223,-0.162900401956594,-0.161057853269173,
-0.159605686019269,-0.158248603253918,-0.156659059434375,-0.151938552659457,
-0.130901286092268,-0.11320563896908,-0.066909887167199,-0.0626285276468794,
-0.0612084644784653,-0.0604122096964392,-0.0596798623458036,-0.0586609273637555,
-0.0566175285972577,-0.0539782932526428,-0.000592842301724799),
 .UNSPECIFIED.);
#803=B_SPLINE_CURVE_WITH_KNOTS('',3,(#19446,#19447,#19448,#19449,#19450,
#19451,#19452,#19453,#19454,#19455,#19456,#19457,#19458,#19459,#19460,#19461,
#19462,#19463,#19464,#19465,#19466,#19467,#19468,#19469,#19470,#19471,#19472,
#19473,#19474,#19475,#19476,#19477,#19478,#19479,#19480,#19481,#19482,#19483,
#19484,#19485,#19486,#19487,#19488,#19489,#19490,#19491,#19492,#19493,#19494,
#19495,#19496,#19497,#19498,#19499,#19500,#19501,#19502,#19503,#19504,#19505,
#19506,#19507,#19508,#19509,#19510,#19511,#19512,#19513,#19514,#19515,#19516,
#19517,#19518,#19519,#19520,#19521,#19522,#19523,#19524,#19525,#19526,#19527,
#19528,#19529,#19530,#19531,#19532,#19533,#19534,#19535,#19536,#19537,#19538,
#19539,#19540,#19541,#19542,#19543,#19544,#19545,#19546,#19547,#19548,#19549,
#19550,#19551,#19552,#19553,#19554,#19555,#19556,#19557,#19558,#19559,#19560,
#19561,#19562,#19563,#19564,#19565,#19566,#19567,#19568,#19569,#19570,#19571,
#19572,#19573,#19574,#19575,#19576,#19577,#19578,#19579,#19580,#19581,#19582,
#19583,#19584,#19585,#19586,#19587,#19588,#19589,#19590,#19591,#19592,#19593,
#19594,#19595,#19596,#19597,#19598,#19599,#19600,#19601,#19602,#19603,#19604,
#19605,#19606,#19607,#19608,#19609,#19610,#19611,#19612,#19613,#19614,#19615,
#19616,#19617,#19618,#19619,#19620,#19621,#19622,#19623,#19624,#19625,#19626,
#19627,#19628,#19629,#19630,#19631,#19632,#19633,#19634,#19635),
 .UNSPECIFIED.,.F.,.F.,(4,3,3,3,3,3,3,3,3,3,3,3,3,3,3,3,3,3,3,3,3,3,3,3,
3,3,3,3,3,3,3,3,3,3,3,3,3,3,3,3,3,3,3,3,3,3,3,3,3,3,3,3,3,3,3,3,3,3,3,3,
3,3,3,4),(235.619449019234,235.723424947678,235.82736120438,235.93129418189,
236.035333686848,236.139428244564,236.243714282079,236.319588578511,236.42453468062,
236.529323029562,236.63398783797,236.738586619568,236.843154958456,236.947728394564,
237.052412605536,237.157157920198,237.262086008044,237.318269446872,237.423216296437,
237.528005403782,237.632670982987,237.737270542601,237.841839665513,237.946413890446,
238.051098892008,238.155844999439,238.26077387488,238.316950315232,238.421892950261,
238.52667783165,238.631339188293,238.735934529757,238.840499445106,238.945069479249,
239.049750344019,239.154492339076,239.259417184133,239.315631183593,239.420579802777,
239.525370652109,239.630037924636,239.734639146622,239.839209898787,239.943785717648,
240.048472249213,240.153219852705,240.258150155706,240.314312051954,240.419263637437,
240.524057528087,240.628727937091,240.733332352526,240.837906349875,240.942485460475,
241.047175330889,241.151926304909,241.256859991014,241.312992920315,241.419748621657,
241.526327456451,241.63273345532,241.739038016702,241.845270670712,241.902634326414),
 .UNSPECIFIED.);
#804=B_SPLINE_CURVE_WITH_KNOTS('',3,(#19637,#19638,#19639,#19640,#19641,
#19642,#19643,#19644,#19645,#19646,#19647,#19648,#19649,#19650,#19651,#19652,
#19653,#19654,#19655,#19656,#19657,#19658,#19659,#19660,#19661,#19662,#19663,
#19664,#19665,#19666,#19667,#19668,#19669,#19670,#19671,#19672,#19673,#19674,
#19675,#19676,#19677,#19678,#19679,#19680,#19681,#19682,#19683,#19684,#19685,
#19686,#19687,#19688,#19689,#19690,#19691,#19692,#19693,#19694,#19695,#19696,
#19697,#19698,#19699,#19700,#19701,#19702,#19703,#19704,#19705,#19706,#19707,
#19708,#19709,#19710,#19711,#19712,#19713,#19714,#19715,#19716,#19717,#19718,
#19719,#19720,#19721,#19722,#19723,#19724,#19725,#19726,#19727,#19728,#19729,
#19730,#19731,#19732,#19733,#19734,#19735,#19736,#19737,#19738,#19739,#19740,
#19741,#19742,#19743,#19744,#19745,#19746,#19747,#19748,#19749,#19750,#19751,
#19752,#19753,#19754,#19755,#19756,#19757,#19758,#19759,#19760,#19761,#19762,
#19763,#19764,#19765,#19766,#19767,#19768,#19769,#19770,#19771,#19772,#19773,
#19774,#19775,#19776,#19777,#19778,#19779,#19780,#19781,#19782,#19783,#19784,
#19785,#19786,#19787,#19788,#19789,#19790,#19791,#19792,#19793,#19794,#19795,
#19796),.UNSPECIFIED.,.F.,.F.,(4,3,3,3,3,3,3,3,3,3,3,3,3,3,3,3,3,3,3,3,
3,3,3,3,3,3,3,3,3,3,3,3,3,3,3,3,3,3,3,3,3,3,3,3,3,3,3,3,3,3,3,3,3,4),(241.902634326753,
242.017552757131,242.132857082377,242.248701473426,242.311673788675,242.416644276006,
242.521456897853,242.626145699382,242.730768288196,242.83536021486,242.939956985551,
243.044663990786,243.149431827377,243.254381774431,243.310354657036,243.415329956237,
243.520147893875,243.624842722105,243.729471772774,243.834070582838,243.938674645314,
244.043389504012,244.148165524066,244.253124075436,244.309035525397,244.413831203907,
244.518468768063,244.622982970788,244.727431334325,244.831849657905,244.93627369689,
245.040810459789,245.14540920448,245.250193661039,245.307716393758,245.41286648623,
245.517858182872,245.622724415093,245.727523312383,245.832290166372,245.937060222967,
246.041936850911,246.146872475353,246.251985582833,246.306397262118,246.410386347413,
246.514201221025,246.617918810421,246.721576030725,246.825209715847,246.928926859748,
247.032682017607,247.136621574968,247.235465738518),.UNSPECIFIED.);
#805=B_SPLINE_CURVE_WITH_KNOTS('',3,(#19800,#19801,#19802,#19803,#19804,
#19805,#19806,#19807,#19808,#19809,#19810,#19811,#19812,#19813,#19814,#19815,
#19816,#19817,#19818,#19819,#19820,#19821,#19822,#19823,#19824,#19825,#19826,
#19827,#19828,#19829,#19830,#19831,#19832,#19833,#19834,#19835,#19836,#19837,
#19838,#19839,#19840,#19841,#19842,#19843,#19844,#19845,#19846,#19847,#19848,
#19849,#19850,#19851,#19852,#19853,#19854,#19855,#19856,#19857,#19858,#19859,
#19860,#19861,#19862,#19863,#19864,#19865,#19866,#19867,#19868,#19869,#19870,
#19871,#19872,#19873,#19874,#19875,#19876,#19877,#19878,#19879,#19880,#19881,
#19882,#19883,#19884,#19885,#19886,#19887,#19888,#19889,#19890,#19891,#19892,
#19893,#19894,#19895,#19896,#19897,#19898,#19899,#19900,#19901,#19902,#19903,
#19904,#19905,#19906,#19907,#19908,#19909,#19910,#19911,#19912,#19913,#19914,
#19915,#19916,#19917,#19918,#19919,#19920,#19921,#19922,#19923),
 .UNSPECIFIED.,.F.,.F.,(4,3,3,3,3,3,3,3,3,3,3,3,3,3,3,3,3,3,3,3,3,3,3,3,
3,3,3,3,3,3,3,3,3,3,3,3,3,3,3,3,3,4),(241.902634326414,241.999480923579,
242.104630987599,242.20962265607,242.314488860666,242.419287730683,242.524054557789,
242.628824587929,242.733701190235,242.838636789468,242.943749872662,242.99816179194,
243.103254328513,243.208191752163,243.313008759831,243.417761577378,243.522485535044,
243.627215920643,243.7320579726,243.836961863511,243.942047941096,243.9968426603,
244.100644682838,244.204288219948,244.307812192971,244.411272931668,244.514707444671,
244.618152699577,244.721724761877,244.825365012194,244.929211277103,244.995523528661,
245.103416970472,245.214765398791,245.322299074973,245.429730709313,245.537089219953,
245.644403430638,245.751731684544,245.859066936612,245.966474699844,245.994204397022),
 .UNSPECIFIED.);
#806=B_SPLINE_CURVE_WITH_KNOTS('',3,(#19925,#19926,#19927,#19928,#19929,
#19930,#19931,#19932,#19933,#19934,#19935,#19936,#19937,#19938,#19939,#19940,
#19941,#19942,#19943,#19944,#19945,#19946,#19947,#19948,#19949,#19950,#19951,
#19952,#19953,#19954,#19955,#19956,#19957,#19958,#19959,#19960,#19961,#19962,
#19963,#19964,#19965,#19966,#19967,#19968,#19969,#19970,#19971,#19972,#19973,
#19974,#19975,#19976,#19977,#19978,#19979,#19980,#19981,#19982,#19983,#19984,
#19985,#19986,#19987,#19988,#19989,#19990,#19991,#19992,#19993,#19994,#19995,
#19996,#19997,#19998,#19999,#20000,#20001,#20002,#20003,#20004,#20005,#20006,
#20007,#20008,#20009,#20010,#20011,#20012,#20013,#20014,#20015,#20016,#20017,
#20018,#20019,#20020,#20021,#20022,#20023,#20024,#20025,#20026,#20027,#20028,
#20029,#20030,#20031,#20032,#20033,#20034,#20035,#20036,#20037,#20038,#20039,
#20040,#20041,#20042,#20043,#20044,#20045,#20046,#20047,#20048,#20049,#20050,
#20051,#20052,#20053,#20054,#20055,#20056,#20057,#20058,#20059,#20060,#20061,
#20062,#20063,#20064,#20065,#20066,#20067,#20068,#20069,#20070,#20071,#20072,
#20073,#20074,#20075,#20076,#20077,#20078,#20079,#20080,#20081,#20082,#20083,
#20084,#20085,#20086,#20087,#20088,#20089,#20090,#20091,#20092,#20093,#20094,
#20095,#20096,#20097,#20098,#20099,#20100,#20101,#20102,#20103,#20104,#20105,
#20106,#20107,#20108,#20109,#20110,#20111,#20112,#20113,#20114),
 .UNSPECIFIED.,.F.,.F.,(4,3,3,3,3,3,3,3,3,3,3,3,3,3,3,3,3,3,3,3,3,3,3,3,
3,3,3,3,3,3,3,3,3,3,3,3,3,3,3,3,3,3,3,3,3,3,3,3,3,3,3,3,3,3,3,3,3,3,3,3,
3,3,3,4),(235.619449019605,235.736021958153,235.853076834015,235.970735614475,
236.007395713414,236.112344331345,236.217135179442,236.321802450764,236.426403671564,
236.530974422564,236.635550240284,236.740236770748,236.844984373159,236.949914675127,
237.006076581775,237.111028161415,237.21582204618,237.320492449269,237.425096858772,
237.529670850182,237.634249954846,237.738939819366,237.843690787507,237.948624467821,
238.004757450136,238.109681185845,238.214447131041,238.319089587424,238.423666061042,
238.528212168383,238.632763481826,238.737425885531,238.842149538951,238.947056424382,
239.003438318497,239.108408798266,239.213221412623,239.317910206801,239.422532788354,
239.527124707856,239.631721471494,239.736428469887,239.841196299746,239.946146240309,
240.002119186857,240.107094458936,240.211912369256,240.316607170012,240.421236193124,
240.525834975592,240.630439010474,240.735153841768,240.839929834487,240.944888358919,
241.000800055218,241.104319830401,241.207661617074,241.310904203503,241.414085012755,
241.517241378582,241.620474637911,241.723746229367,241.827185633363,241.902634326145),
 .UNSPECIFIED.);
#807=B_SPLINE_CURVE_WITH_KNOTS('',3,(#20116,#20117,#20118,#20119,#20120,
#20121,#20122,#20123,#20124,#20125,#20126,#20127,#20128,#20129,#20130,#20131,
#20132,#20133,#20134,#20135,#20136,#20137,#20138,#20139,#20140,#20141,#20142,
#20143,#20144,#20145,#20146,#20147,#20148,#20149,#20150,#20151,#20152,#20153,
#20154,#20155,#20156,#20157,#20158,#20159,#20160,#20161,#20162,#20163,#20164,
#20165,#20166,#20167,#20168,#20169,#20170,#20171,#20172,#20173,#20174,#20175,
#20176,#20177,#20178,#20179,#20180,#20181,#20182,#20183,#20184,#20185,#20186,
#20187,#20188,#20189,#20190,#20191,#20192,#20193,#20194,#20195,#20196,#20197,
#20198,#20199,#20200,#20201,#20202,#20203,#20204,#20205,#20206,#20207,#20208,
#20209,#20210,#20211,#20212,#20213,#20214,#20215,#20216,#20217,#20218,#20219,
#20220,#20221,#20222,#20223,#20224,#20225,#20226,#20227,#20228,#20229,#20230,
#20231,#20232,#20233,#20234,#20235,#20236,#20237,#20238,#20239,#20240,#20241,
#20242,#20243,#20244,#20245,#20246,#20247,#20248,#20249,#20250,#20251,#20252,
#20253,#20254,#20255,#20256,#20257,#20258,#20259,#20260,#20261,#20262,#20263,
#20264,#20265,#20266,#20267,#20268,#20269,#20270,#20271,#20272,#20273,#20274,
#20275,#20276,#20277,#20278,#20279,#20280,#20281,#20282,#20283,#20284,#20285,
#20286,#20287,#20288,#20289,#20290,#20291,#20292,#20293,#20294,#20295,#20296,
#20297,#20298,#20299,#20300,#20301,#20302,#20303,#20304,#20305,#20306,#20307,
#20308,#20309,#20310,#20311,#20312,#20313,#20314,#20315,#20316,#20317,#20318,
#20319,#20320,#20321,#20322,#20323,#20324,#20325,#20326,#20327,#20328,#20329,
#20330,#20331,#20332,#20333,#20334,#20335,#20336,#20337,#20338,#20339,#20340,
#20341,#20342,#20343,#20344,#20345,#20346,#20347,#20348,#20349,#20350,#20351,
#20352,#20353,#20354,#20355,#20356,#20357,#20358,#20359,#20360,#20361,#20362,
#20363,#20364,#20365,#20366,#20367,#20368,#20369,#20370,#20371,#20372,#20373,
#20374,#20375,#20376,#20377,#20378,#20379,#20380,#20381,#20382,#20383,#20384,
#20385,#20386,#20387,#20388,#20389,#20390,#20391,#20392,#20393,#20394,#20395,
#20396,#20397,#20398,#20399,#20400,#20401,#20402,#20403,#20404,#20405,#20406,
#20407,#20408,#20409,#20410,#20411,#20412,#20413,#20414,#20415,#20416,#20417,
#20418,#20419,#20420,#20421,#20422,#20423,#20424,#20425,#20426,#20427,#20428,
#20429,#20430,#20431,#20432,#20433,#20434,#20435,#20436,#20437,#20438,#20439,
#20440,#20441,#20442,#20443,#20444,#20445,#20446,#20447,#20448,#20449,#20450,
#20451,#20452,#20453,#20454,#20455,#20456,#20457,#20458,#20459,#20460,#20461,
#20462,#20463,#20464,#20465,#20466,#20467,#20468,#20469,#20470,#20471,#20472,
#20473,#20474,#20475,#20476,#20477,#20478,#20479,#20480,#20481,#20482,#20483,
#20484,#20485,#20486,#20487,#20488,#20489,#20490,#20491,#20492,#20493,#20494,
#20495,#20496,#20497,#20498,#20499,#20500,#20501,#20502,#20503,#20504,#20505,
#20506,#20507,#20508,#20509,#20510,#20511,#20512,#20513,#20514,#20515,#20516,
#20517,#20518,#20519,#20520,#20521,#20522,#20523,#20524,#20525,#20526,#20527,
#20528,#20529,#20530,#20531,#20532,#20533,#20534,#20535,#20536,#20537,#20538,
#20539,#20540,#20541,#20542,#20543,#20544,#20545,#20546,#20547,#20548,#20549,
#20550,#20551,#20552,#20553,#20554,#20555,#20556,#20557,#20558,#20559,#20560,
#20561,#20562,#20563,#20564,#20565,#20566,#20567,#20568,#20569,#20570,#20571,
#20572,#20573,#20574,#20575,#20576,#20577,#20578,#20579,#20580,#20581,#20582,
#20583,#20584,#20585,#20586,#20587,#20588,#20589,#20590,#20591,#20592,#20593,
#20594,#20595,#20596,#20597,#20598,#20599,#20600,#20601,#20602,#20603,#20604,
#20605,#20606,#20607,#20608,#20609,#20610,#20611,#20612,#20613,#20614,#20615,
#20616,#20617,#20618,#20619,#20620,#20621,#20622,#20623,#20624,#20625,#20626,
#20627,#20628,#20629,#20630,#20631,#20632,#20633,#20634,#20635,#20636,#20637,
#20638,#20639,#20640,#20641,#20642,#20643,#20644,#20645,#20646,#20647,#20648,
#20649,#20650,#20651,#20652,#20653,#20654,#20655,#20656,#20657,#20658,#20659,
#20660,#20661,#20662,#20663,#20664,#20665,#20666,#20667,#20668,#20669,#20670,
#20671,#20672,#20673,#20674,#20675,#20676,#20677,#20678,#20679,#20680,#20681,
#20682,#20683,#20684,#20685,#20686,#20687,#20688,#20689,#20690,#20691,#20692,
#20693,#20694,#20695,#20696,#20697,#20698,#20699,#20700,#20701,#20702,#20703,
#20704,#20705,#20706,#20707),.UNSPECIFIED.,.F.,.F.,(4,2,2,2,2,2,2,2,2,2,
2,2,2,2,2,2,2,2,2,2,2,2,2,2,2,2,2,2,2,2,2,2,2,2,2,2,2,2,2,2,2,2,2,2,2,2,
2,2,2,2,2,2,2,2,2,2,2,2,2,2,2,2,2,2,2,2,2,2,2,2,2,2,2,2,2,2,2,2,2,2,2,2,
2,2,2,2,2,2,2,2,2,2,2,2,2,2,2,2,2,2,2,2,2,2,2,2,2,2,2,2,2,2,2,2,2,2,2,2,
2,2,2,2,2,2,2,2,2,2,2,2,2,2,2,2,2,2,2,2,2,2,2,2,2,2,2,2,2,2,2,2,2,2,2,2,
2,2,2,2,2,2,2,2,2,2,2,2,2,2,2,2,2,2,2,2,2,2,2,2,2,2,2,2,2,2,2,2,2,2,2,2,
2,2,2,2,2,2,2,2,2,2,2,2,2,2,2,2,2,2,2,2,2,2,2,2,2,2,2,2,2,2,2,2,2,2,2,2,
2,2,2,2,2,2,2,2,2,2,2,2,2,2,2,2,2,2,2,2,2,2,2,2,2,2,2,2,2,2,2,2,2,2,2,2,
2,2,2,2,2,2,2,2,2,2,2,2,2,2,2,2,2,2,2,2,2,2,2,2,2,2,2,2,2,2,2,2,2,4),(-2.50844686278328,
-2.49269359710946,-2.49008558575366,-2.4883622708675,-2.48698020238702,
-2.48554093339258,-2.48387676855305,-2.48104923796445,-2.47052748535395,
-2.46169824884854,-2.40927370879475,-2.39011232208988,-2.3880333482175,
-2.38700899492203,-2.38627765490984,-2.38548735144296,-2.38408995207614,
-2.37997857323955,-2.37897365427641,-2.32263193855691,-2.30281138695002,
-2.29558160206105,-2.29206441235338,-2.28996182551875,-2.28806477277046,
-2.28662885521865,-2.28525843155444,-2.28299955405137,-2.27725042745633,
-2.22172230361342,-2.19202878921717,-2.18914609840988,-2.18797568070041,
-2.18714608395993,-2.18638531331559,-2.18534072643063,-2.18325517163135,
-2.14909405293217,-2.11819372661656,-2.10192373615194,-2.09561856306411,
-2.09243384275858,-2.08977484950361,-2.088176364545,-2.08817427098319,-2.08817217107111,
-2.08817006480479,-2.08816795214411,-2.08816583306421,-2.08816370755129,
-2.08816157559251,-2.08815943717582,-2.08815729225299,-2.08815514079884,
-2.08815298280516,-2.08815081825945,-2.08814864714711,-2.0881464694097,
-2.08814428503242,-2.08814209399277,-2.08813989626466,-2.08813769183457,
-2.08813548069715,-2.08813326282433,-2.08813103816966,-2.08812880668532,
-2.08812656837791,-2.08812432322499,-2.0881220711897,-2.08811981229296,
-2.08811754646833,-2.08811527370018,-2.08811299399686,-2.08666373707491,
-2.08481666097653,-2.08104518969416,-2.03433451508834,-2.00684839706169,
-1.9964792606921,-1.99069713800261,-1.98917561554482,-1.98827014606644,
-1.98745757131758,-1.9864080104069,-1.98414288410256,-1.94725244983937,
-1.91726077027866,-1.90214232785487,-1.89307326998441,-1.89047470587722,
-1.88887768387116,-1.88742533595696,-1.88555324500763,-1.88165489192682,
-1.84324567770113,-1.79685196372753,-1.79142418549507,-1.78993550419921,
-1.7890373084161,-1.78822263806428,-1.78715891620403,-1.78536855488355,
-1.77410780094252,-1.74865370783611,-1.71845208817896,-1.70307401279213,
-1.6938916628575,-1.6912814623574,-1.68968169940482,-1.68822975202871,-1.68636223337577,
-1.68248811662138,-1.64940378717861,-1.59780878021409,-1.59222814442454,
-1.59072481862256,-1.58982324821766,-1.5890093617776,-1.58795173884615,
-1.58564462829548,-1.55106779783426,-1.52029431890468,-1.49841117253796,
-1.49345329273414,-1.49138908764739,-1.48990525784851,-1.48855795832365,
-1.48676178085577,-1.48238408982283,-1.45014957706135,-1.39855283743501,
-1.39296169726821,-1.39145727788409,-1.39055539804282,-1.38974146572909,
-1.38868410010867,-1.38637879858871,-1.35165356876045,-1.32092379656759,
-1.30488127634249,-1.29541287945244,-1.29277407933726,-1.29116768456516,
-1.28971679482699,-1.28786046831306,-1.28404473999148,-1.254718216548,-1.19693448664752,
-1.19329172453027,-1.19196328705032,-1.19118643839055,-1.19036713646807,
-1.18925662110608,-1.18672562130276,-1.15734303138751,-1.13407748154567,
-1.0982284729303,-1.09432909402739,-1.09245613562873,-1.09100294778709,
-1.0894048337026,-1.08680411426573,-1.07772378660507,-1.06258064529406,
-1.03253252345372,-0.995639022139298,-0.993372450542699,-0.992322219882699,
-0.99150913023227,-0.990603083563992,-0.989080588794925,-0.983294653148478,
-0.972919967976401,-0.945402347789396,-0.898720070387428,-0.89494797745694,
-0.893100102700481,-0.891649992693026,-0.890038466985203,-0.88737741597309,
-0.877680028515178,-0.861094004779503,-0.82991036920981,-0.808512175631676,
-0.805846629480951,-0.795801296732919,-0.794071266208014,-0.793025039191454,
-0.792212524494808,-0.791304338142976,-0.789772113086288,-0.783876550087764,
-0.773222830194575,-0.744543315535899,-0.739068822164123,-0.723124995494738,
-0.71540510415052,-0.698774944894874,-0.695771989103465,-0.693902755948108,
-0.692450050601219,-0.690850034129862,-0.688240734129375,-0.679074988119818,
-0.663735488894132,-0.633529878655933,-0.597108125846816,-0.59483199244795,
-0.593779963638399,-0.592966633888785,-0.592061580143386,-0.590543515768746,
-0.584806458302125,-0.574555012695112,-0.547417638352997,-0.50014862611173,
-0.496392404918132,-0.494547696410197,-0.493097959067071,-0.491484665484791,
-0.488815633917845,-0.479033445576717,-0.462244550613607,-0.43090363297541,
-0.397885518314212,-0.395787033605954,-0.394738922216473,-0.393976970327035,
-0.393165350691325,-0.392033481749677,-0.390752245266113,-0.388514951048301,
-0.371187040586769,-0.339478903250186,-0.301097868591413,-0.297192630978884,
-0.295318546281585,-0.293865231833646,-0.292267731171303,-0.28966970043705,
-0.280615696875707,-0.265532762976925,-0.233216036697687,-0.198564908727071,
-0.196256549317674,-0.195198479051473,-0.194406587686545,-0.194403937985589,
-0.194401311447691,-0.194398703853166,-0.19439611503573,-0.194393544745997,
-0.194390992798672,-0.194388458983883,-0.194385943142771,-0.194383445079622,
-0.194380964588035,-0.194378501484192,-0.194376055600439,-0.194373626762146,
-0.194371214753002,-0.194368819396897,-0.194366440572387,-0.194364078053524,
-0.194361731694794,-0.194359401371431,-0.194357086893942,-0.19435478807974,
-0.194352504782314,-0.194350236864088,-0.194347984188797,-0.194345746569172,
-0.194343523870016,-0.194341315909406,-0.194339122571006,-0.194336943742128,
-0.194334779261849,-0.194332622756615,-0.19433046769248,-0.194328326223556,
-0.193423887794132,-0.192463386738545,-0.191009349453049,-0.188334345306307,
-0.163726432554852,-0.130494358594067,-0.101480257205338,-0.0976618852201546,
-0.095802557755683,-0.094348545910109,-0.0927378994912179,-0.0900902939150393,
-0.0805710127471456,-0.0644203342906257,-0.0357172148943006,-0.000592664738489131),
 .UNSPECIFIED.);
#808=B_SPLINE_CURVE_WITH_KNOTS('',3,(#20709,#20710,#20711,#20712,#20713,
#20714,#20715,#20716,#20717,#20718,#20719,#20720,#20721,#20722,#20723,#20724,
#20725,#20726,#20727,#20728,#20729,#20730,#20731,#20732,#20733,#20734,#20735,
#20736,#20737,#20738,#20739,#20740,#20741,#20742,#20743,#20744,#20745,#20746,
#20747,#20748,#20749,#20750,#20751,#20752,#20753,#20754,#20755,#20756,#20757,
#20758,#20759,#20760,#20761,#20762,#20763,#20764,#20765,#20766,#20767,#20768,
#20769,#20770,#20771,#20772,#20773,#20774,#20775,#20776,#20777,#20778,#20779,
#20780,#20781,#20782,#20783,#20784,#20785,#20786,#20787,#20788,#20789,#20790,
#20791,#20792,#20793,#20794,#20795,#20796,#20797,#20798,#20799,#20800,#20801,
#20802,#20803,#20804,#20805,#20806,#20807,#20808,#20809,#20810,#20811,#20812,
#20813,#20814,#20815,#20816,#20817,#20818,#20819,#20820,#20821,#20822,#20823,
#20824,#20825,#20826,#20827,#20828,#20829,#20830,#20831,#20832,#20833,#20834,
#20835,#20836,#20837,#20838,#20839,#20840,#20841,#20842,#20843,#20844,#20845,
#20846,#20847,#20848,#20849,#20850,#20851,#20852,#20853,#20854,#20855,#20856,
#20857,#20858,#20859,#20860,#20861,#20862,#20863,#20864,#20865,#20866,#20867,
#20868,#20869,#20870,#20871,#20872,#20873,#20874,#20875,#20876,#20877,#20878,
#20879,#20880,#20881,#20882,#20883,#20884,#20885,#20886,#20887,#20888,#20889,
#20890,#20891,#20892,#20893,#20894,#20895,#20896,#20897,#20898,#20899,#20900,
#20901,#20902,#20903,#20904,#20905,#20906,#20907,#20908,#20909,#20910,#20911,
#20912,#20913,#20914,#20915,#20916,#20917,#20918,#20919,#20920,#20921,#20922,
#20923,#20924,#20925,#20926,#20927,#20928,#20929,#20930,#20931,#20932,#20933,
#20934,#20935,#20936,#20937,#20938,#20939,#20940,#20941,#20942,#20943,#20944,
#20945,#20946,#20947,#20948,#20949,#20950,#20951,#20952,#20953,#20954,#20955,
#20956,#20957,#20958,#20959,#20960,#20961,#20962,#20963,#20964,#20965,#20966,
#20967,#20968,#20969,#20970,#20971,#20972,#20973,#20974,#20975,#20976,#20977,
#20978,#20979,#20980,#20981,#20982,#20983,#20984,#20985,#20986,#20987,#20988,
#20989,#20990,#20991,#20992,#20993,#20994,#20995,#20996,#20997,#20998,#20999,
#21000,#21001,#21002,#21003,#21004,#21005,#21006,#21007,#21008,#21009,#21010,
#21011,#21012,#21013,#21014,#21015,#21016,#21017,#21018,#21019,#21020,#21021,
#21022,#21023,#21024,#21025,#21026,#21027,#21028,#21029,#21030,#21031,#21032,
#21033,#21034,#21035,#21036,#21037,#21038,#21039,#21040,#21041,#21042,#21043,
#21044,#21045,#21046,#21047,#21048,#21049,#21050,#21051,#21052,#21053,#21054,
#21055,#21056,#21057,#21058,#21059,#21060,#21061,#21062,#21063,#21064,#21065,
#21066,#21067,#21068,#21069,#21070,#21071,#21072,#21073,#21074,#21075,#21076,
#21077,#21078,#21079,#21080,#21081,#21082,#21083,#21084,#21085,#21086,#21087,
#21088,#21089,#21090,#21091,#21092,#21093,#21094,#21095,#21096,#21097,#21098,
#21099,#21100,#21101,#21102,#21103,#21104,#21105,#21106,#21107,#21108,#21109,
#21110,#21111,#21112,#21113,#21114,#21115,#21116,#21117,#21118,#21119,#21120,
#21121,#21122,#21123,#21124,#21125,#21126,#21127,#21128,#21129,#21130,#21131,
#21132,#21133,#21134,#21135,#21136,#21137,#21138,#21139,#21140,#21141,#21142,
#21143,#21144,#21145,#21146,#21147,#21148,#21149,#21150,#21151,#21152,#21153,
#21154,#21155,#21156,#21157,#21158,#21159,#21160,#21161,#21162,#21163,#21164,
#21165,#21166,#21167,#21168,#21169,#21170,#21171,#21172,#21173,#21174,#21175,
#21176,#21177,#21178,#21179,#21180,#21181,#21182,#21183,#21184,#21185,#21186,
#21187,#21188,#21189,#21190,#21191,#21192),.UNSPECIFIED.,.F.,.F.,(4,2,2,
2,2,2,2,2,2,2,2,2,2,2,2,2,2,2,2,2,2,2,2,2,2,2,2,2,2,2,2,2,2,2,2,2,2,2,2,
2,2,2,2,2,2,2,2,2,2,2,2,2,2,2,2,2,2,2,2,2,2,2,2,2,2,2,2,2,2,2,2,2,2,2,2,
2,2,2,2,2,2,2,2,2,2,2,2,2,2,2,2,2,2,2,2,2,2,2,2,2,2,2,2,2,2,2,2,2,2,2,2,
2,2,2,2,2,2,2,2,2,2,2,2,2,2,2,2,2,2,2,2,2,2,2,2,2,2,2,2,2,2,2,2,2,2,2,2,
2,2,2,2,2,2,2,2,2,2,2,2,2,2,2,2,2,2,2,2,2,2,2,2,2,2,2,2,2,2,2,2,2,2,2,2,
2,2,2,2,2,2,2,2,2,2,2,2,2,2,2,2,2,2,2,2,2,2,2,2,2,2,2,2,2,2,2,2,2,2,2,2,
2,2,2,2,2,2,2,2,2,2,2,2,2,2,2,2,2,2,2,2,2,2,4),(-2.51451748014498,-2.51281605016616,
-2.51112153504224,-2.51011910525733,-2.50933438295832,-2.50853123892221,
-2.50759577763298,-2.50598921910066,-2.50071265804853,-2.43820386699382,
-2.42275426919092,-2.41353438027086,-2.41091602920107,-2.40931180366378,
-2.40785615515298,-2.40598436480432,-2.4021031548632,-2.36042595208092,
-2.32978339185942,-2.31806381459503,-2.31388564373787,-2.31188277546981,
-2.31069533939669,-2.30963013725907,-2.30882797316081,-2.30793356974985,
-2.30646860546513,-2.30257562753262,-2.24873238746428,-2.24061865229924,
-2.22371821589601,-2.21388251872479,-2.21120474638526,-2.20958733574491,
-2.2081346443482,-2.20628719739557,-2.20336246847933,-2.18814361314187,
-2.18424700857255,-2.13467158779746,-2.11493228061176,-2.11253938706279,
-2.11119548225122,-2.11028051572967,-2.10940858707538,-2.10861505222497,
-2.10754363488924,-2.10525796284905,-2.07068628877292,-2.03980463626495,
-2.02362316378698,-2.01408937389062,-2.01144012611985,-2.00982896796326,
-2.0083748090838,-2.00651572927726,-2.00269941385288,-1.95705037396175,
-1.92861687067096,-1.91803713685547,-1.91216723084284,-1.91063498547112,
-1.90972550995586,-1.90891096551386,-1.90786098681056,-1.9061223815688,
-1.89596544710767,-1.87582394808309,-1.86972866210272,-1.83926647145265,
-1.82362157076758,-1.8143170350921,-1.81169007767494,-1.81008381726709,
-1.80862843759378,-1.8067599463239,-1.80289621854521,-1.77123819256394,
-1.73176453243519,-1.71918649634105,-1.71256266027901,-1.71096729541546,
-1.7100437379389,-1.70923198229582,-1.70818828567957,-1.70602125087846,
-1.69050152996651,-1.66958925878186,-1.63926702826325,-1.62380030092132,
-1.61457254875713,-1.61195311354543,-1.61034846637739,-1.60889259416414,
-1.60702073847571,-1.60314019665794,-1.56069632060757,-1.53108510546635,
-1.51359606203268,-1.51154530321925,-1.51052476780479,-1.50979211744674,
-1.50899638908513,-1.50757934882004,-1.50332178714741,-1.46623727881674,
-1.44183979188548,-1.42482121508968,-1.41493572369333,-1.41225286546038,
-1.41063406822525,-1.40918120752971,-1.40733501564324,-1.4044151714081,
-1.38928404185894,-1.38795139028439,-1.33062660049781,-1.31376553139023,
-1.31172858472524,-1.31071075924285,-1.30997835801467,-1.30918118672126,
-1.30775733932055,-1.30344932228793,-1.25785940126824,-1.2171369548455,
-1.21323988210491,-1.21136466546735,-1.20990823020054,-1.20830503531544,
-1.20569264837331,-1.19653730570096,-1.18123584184052,-1.15101685903073,
-1.11432623181867,-1.11204740576523,-1.11099334633399,-1.11017810255916,
-1.10927054220857,-1.10774744890466,-1.10198184587937,-1.09166878447475,
-1.0643494981221,-1.0171422841484,-1.01337199237491,-1.01152180083855,-1.01006840821142,
-1.00845172243285,-1.00577864625508,-0.995998936109896,-0.979232241683642,
-0.947863762797864,-0.924854021013472,-0.914056234885205,-0.912284849432861,
-0.91122513042845,-0.910409132582326,-0.909504679679514,-0.907995364834063,
-0.902379201757033,-0.850674081855965,-0.817525186560206,-0.813640778523217,
-0.811768152790026,-0.810312169114916,-0.808707892487975,-0.806090178075104,
-0.796879938141076,-0.781451404656237,-0.751132663914669,-0.725548825271818,
-0.714307085208493,-0.712514118145953,-0.71144812175965,-0.710631268781825,
-0.709730172278738,-0.708235672675589,-0.702775705085686,-0.655911952764586,
-0.617793122243397,-0.613882863709909,-0.612005260178234,-0.610548725540387,
-0.60894719013894,-0.606341485594939,-0.597249598935944,-0.582092821239112,
-0.551993247914644,-0.514967319096778,-0.512695704590364,-0.51164311067651,
-0.510828179271047,-0.509920066255509,-0.508394071355859,-0.502594508459982,
-0.492195024529594,-0.464607160059865,-0.417833124275506,-0.414049560375358,
-0.412196913027027,-0.410781802732475,-0.409212482696472,-0.407573839880407,
-0.405173646659386,-0.400927396223008,-0.366828311922889,-0.325473031412894,
-0.314706415372037,-0.312936709286618,-0.311877541517773,-0.311061693701066,
-0.310157108311761,-0.308646926398554,-0.30302028997174,-0.251324038314476,
-0.218195101883811,-0.214306882080081,-0.212433630198597,-0.211016651966711,
-0.209458889563924,-0.20783588102246,-0.205473467782535,-0.201321584235745,
-0.192246664524157,-0.164335347075445,-0.118213306621763,-0.113931713909945,
-0.11251151817116,-0.111715175874615,-0.110982727684619,-0.109963631395247,
-0.107919860740196,-0.0907425573702373,-0.0254247460849162,-0.0166005098880669,
-0.0137791124022887,-0.012113383123493,-0.0106716896885479,-0.00928464804163324,
-0.00755312043015414,-0.00448544266794431,-0.000592058400578167),
 .UNSPECIFIED.);
#809=B_SPLINE_CURVE_WITH_KNOTS('',3,(#21194,#21195,#21196,#21197,#21198,
#21199,#21200,#21201,#21202,#21203,#21204,#21205,#21206,#21207,#21208,#21209,
#21210,#21211,#21212,#21213,#21214,#21215,#21216,#21217,#21218,#21219,#21220,
#21221,#21222,#21223,#21224,#21225,#21226,#21227,#21228,#21229,#21230,#21231,
#21232,#21233,#21234,#21235,#21236,#21237,#21238,#21239,#21240,#21241,#21242,
#21243,#21244,#21245,#21246,#21247,#21248,#21249,#21250,#21251,#21252,#21253,
#21254,#21255,#21256,#21257,#21258,#21259,#21260,#21261,#21262,#21263,#21264,
#21265,#21266,#21267,#21268,#21269,#21270,#21271,#21272,#21273,#21274,#21275,
#21276,#21277,#21278,#21279,#21280,#21281,#21282,#21283,#21284,#21285,#21286,
#21287,#21288,#21289,#21290,#21291,#21292,#21293,#21294,#21295,#21296,#21297,
#21298,#21299,#21300,#21301,#21302,#21303,#21304,#21305,#21306,#21307,#21308,
#21309,#21310,#21311,#21312,#21313,#21314,#21315,#21316,#21317,#21318,#21319,
#21320,#21321,#21322,#21323,#21324,#21325,#21326,#21327,#21328,#21329,#21330,
#21331,#21332,#21333,#21334,#21335,#21336,#21337,#21338,#21339,#21340,#21341,
#21342,#21343,#21344,#21345,#21346,#21347,#21348,#21349,#21350,#21351,#21352,
#21353,#21354,#21355,#21356,#21357,#21358,#21359,#21360,#21361,#21362,#21363,
#21364,#21365,#21366,#21367,#21368,#21369,#21370,#21371,#21372,#21373,#21374,
#21375,#21376,#21377,#21378,#21379,#21380,#21381,#21382,#21383,#21384,#21385,
#21386,#21387,#21388,#21389,#21390,#21391,#21392,#21393,#21394,#21395,#21396,
#21397,#21398,#21399,#21400,#21401,#21402,#21403,#21404,#21405,#21406,#21407,
#21408,#21409,#21410,#21411,#21412,#21413,#21414,#21415,#21416,#21417,#21418,
#21419,#21420,#21421,#21422,#21423,#21424,#21425,#21426,#21427,#21428,#21429,
#21430,#21431,#21432,#21433,#21434,#21435,#21436,#21437,#21438,#21439,#21440,
#21441,#21442,#21443,#21444,#21445,#21446,#21447,#21448,#21449,#21450,#21451,
#21452,#21453,#21454,#21455,#21456,#21457,#21458,#21459,#21460,#21461,#21462,
#21463,#21464,#21465,#21466,#21467,#21468,#21469,#21470,#21471,#21472,#21473,
#21474,#21475,#21476,#21477,#21478,#21479,#21480,#21481,#21482,#21483,#21484,
#21485,#21486,#21487,#21488,#21489,#21490,#21491,#21492,#21493,#21494,#21495,
#21496,#21497,#21498,#21499,#21500,#21501,#21502,#21503,#21504,#21505,#21506,
#21507,#21508,#21509,#21510,#21511,#21512,#21513,#21514,#21515,#21516,#21517,
#21518,#21519,#21520,#21521,#21522,#21523,#21524,#21525,#21526,#21527,#21528,
#21529,#21530,#21531,#21532,#21533,#21534,#21535,#21536,#21537,#21538,#21539,
#21540,#21541,#21542,#21543,#21544,#21545,#21546,#21547,#21548,#21549,#21550,
#21551,#21552,#21553,#21554,#21555,#21556,#21557,#21558,#21559,#21560,#21561,
#21562,#21563,#21564,#21565,#21566,#21567,#21568,#21569,#21570,#21571,#21572,
#21573,#21574,#21575,#21576,#21577,#21578,#21579,#21580,#21581,#21582,#21583,
#21584,#21585,#21586,#21587,#21588,#21589,#21590,#21591,#21592,#21593,#21594,
#21595,#21596,#21597,#21598,#21599,#21600,#21601,#21602,#21603,#21604,#21605,
#21606,#21607,#21608,#21609,#21610,#21611,#21612,#21613,#21614,#21615,#21616,
#21617,#21618,#21619,#21620,#21621,#21622,#21623,#21624,#21625,#21626,#21627,
#21628,#21629,#21630,#21631,#21632,#21633,#21634,#21635,#21636,#21637,#21638,
#21639,#21640,#21641,#21642,#21643,#21644,#21645,#21646,#21647,#21648,#21649,
#21650,#21651,#21652,#21653,#21654,#21655,#21656,#21657,#21658,#21659,#21660,
#21661,#21662,#21663,#21664,#21665,#21666,#21667,#21668,#21669,#21670,#21671,
#21672,#21673,#21674,#21675,#21676,#21677,#21678,#21679,#21680,#21681,#21682,
#21683,#21684,#21685,#21686,#21687,#21688,#21689,#21690,#21691,#21692,#21693,
#21694,#21695,#21696,#21697,#21698,#21699,#21700,#21701,#21702,#21703,#21704,
#21705,#21706,#21707,#21708,#21709,#21710,#21711,#21712,#21713,#21714,#21715,
#21716,#21717,#21718,#21719,#21720,#21721,#21722,#21723,#21724,#21725,#21726,
#21727,#21728,#21729,#21730,#21731),.UNSPECIFIED.,.F.,.F.,(4,2,2,2,2,2,
2,2,2,2,2,2,2,2,2,2,2,2,2,2,2,2,2,2,2,2,2,2,2,2,2,2,2,2,2,2,2,2,2,2,2,2,
2,2,2,2,2,2,2,2,2,2,2,2,2,2,2,2,2,2,2,2,2,2,2,2,2,2,2,2,2,2,2,2,2,2,2,2,
2,2,2,2,2,2,2,2,2,2,2,2,2,2,2,2,2,2,2,2,2,2,2,2,2,2,2,2,2,2,2,2,2,2,2,2,
2,2,2,2,2,2,2,2,2,2,2,2,2,2,2,2,2,2,2,2,2,2,2,2,2,2,2,2,2,2,2,2,2,2,2,2,
2,2,2,2,2,2,2,2,2,2,2,2,2,2,2,2,2,2,2,2,2,2,2,2,2,2,2,2,2,2,2,2,2,2,2,2,
2,2,2,2,2,2,2,2,2,2,2,2,2,2,2,2,2,2,2,2,2,2,2,2,2,2,2,2,2,2,2,2,2,2,2,2,
2,2,2,2,2,2,2,2,2,2,2,2,2,2,2,2,2,2,2,2,2,2,2,2,2,2,2,2,2,2,2,2,2,2,2,2,
2,2,2,2,2,2,2,2,2,2,4),(-2.51337701081457,-2.44175496188814,-2.43232013167534,
-2.42691106705794,-2.42542187443154,-2.4245222114906,-2.42370540418666,
-2.422637803107,-2.42083854640493,-2.40945366880344,-2.38403577169911,-2.33627303079072,
-2.33126759941285,-2.3285694654559,-2.32680669341505,-2.32514847326009,
-2.32513968378661,-2.32513062619519,-2.32512128988085,-2.32511166368,-2.32510173584106,
-2.32509149399477,-2.32508092509959,-2.32507001540138,-2.32505875038494,
-2.3250471147153,-2.32503509218982,-2.32502266565727,-2.32500981697094,
-2.32499652691343,-2.3249827750869,-2.32496853985471,-2.32495379823724,
-2.32493852580531,-2.32492269656457,-2.32490628282391,-2.32488925506893,
-2.32487158181167,-2.32485460570236,-2.32343193866557,-2.32155744886606,
-2.31765931856103,-2.28301565004191,-2.23486676217071,-2.22751227007412,
-2.22586333200029,-2.22492827553432,-2.2241187287339,-2.22309386349109,
-2.22108661600093,-2.20897206153336,-2.19667625325695,-2.18340034720444,
-2.1705284005456,-2.13525484307865,-2.1309361846584,-2.12850745587442,-2.12685732122389,
-2.12527894809992,-2.12527638253071,-2.12527381140904,-2.12527123473,-2.12526865245837,
-2.12526606455742,-2.12526347100091,-2.12526087176631,-2.12525826683488,
-2.12383743314929,-2.12198603083567,-2.11820571215948,-2.07138824939126,
-2.04383786312378,-2.03344494286484,-2.02764946809671,-2.02612438352324,
-2.02521678446522,-2.02440229137655,-2.02335024192047,-2.02107970375484,
-1.98409026661811,-1.95403300340289,-1.9388849465808,-1.92979715559465,
-1.92719273570985,-1.9255920100286,-1.92413622479654,-1.92225960568385,
-1.91835146735431,-1.88025662741589,-1.83337358987405,-1.82791425729708,
-1.82642027044494,-1.8255195560909,-1.82470309695526,-1.82363768674076,
-1.82184586508555,-1.81061543093734,-1.78504896347642,-1.75477371264236,
-1.73935595049575,-1.73015053686047,-1.72753409021477,-1.7259305648945,
-1.7244752460035,-1.72260345146334,-1.71872068439475,-1.68558826879106,
-1.63388601061939,-1.62825470498433,-1.62674437656348,-1.62583992724974,
-1.6250243539895,-1.62396575204902,-1.62219744047129,-1.6114512541093,-1.6074487561025,
-1.60023750005035,-1.56836135826275,-1.53287156310491,-1.52881747805682,
-1.52691240211694,-1.52545248796916,-1.52406001135835,-1.52169949866923,
-1.51538385695729,-1.46749362985565,-1.44476620087261,-1.43437243572969,
-1.4285761170391,-1.42705065311463,-1.42614279782867,-1.42532805385597,
-1.42427565286181,-1.42200425147217,-1.38507969267971,-1.35498717312345,
-1.33980202010157,-1.33069728992017,-1.32809064791164,-1.3264891187462,
-1.32503297288439,-1.32315640929157,-1.31925028299771,-1.28373035405147,
-1.2568487800976,-1.23026014804358,-1.22790305777441,-1.22683463808489,
-1.22601759816784,-1.22511809574486,-1.22363006178803,-1.21823465894979,
-1.20883484843506,-1.18516764214781,-1.13675914105684,-1.13318962580626,
-1.12929649643632,-1.12742252236514,-1.12596676095213,-1.12436401360257,
-1.12175169260301,-1.11258986543445,-1.09727104272567,-1.06704575803358,
-1.03042666948668,-1.02814843632754,-1.02709475331427,-1.02627984542228,
-1.0253727079959,-1.02385043168163,-1.01808916334942,-1.00778523665731,
-0.980492200535458,-0.933282303576771,-0.929514228888169,-0.927664944807788,
-0.926212182325873,-0.924596112064336,-0.921923855420353,-0.912144958699017,
-0.895377393069233,-0.864016021147467,-0.840970858773963,-0.830235678913826,
-0.828467925237498,-0.827409501255432,-0.826593969118352,-0.825689453552467,
-0.824178781859182,-0.818543501620052,-0.80855460774344,-0.78241196238822,
-0.737497024983468,-0.733079692343254,-0.729979966827759,-0.728100113551347,
-0.726639294218764,-0.72505503853134,-0.722525611942107,-0.714153855801022,
-0.700607919723632,-0.644693830842097,-0.642315277417697,-0.630576911641671,
-0.628585388550131,-0.627563678257295,-0.626754108467323,-0.625816167135859,
-0.624155122414832,-0.6166320182895,-0.567958280853421,-0.53402057135248,
-0.530127586891729,-0.528253629259245,-0.526797856906971,-0.525195073556982,
-0.522582639860281,-0.513419870160197,-0.498098939934887,-0.467871775514895,
-0.43126357593716,-0.429207007670072,-0.428168379694435,-0.427407867547,
-0.426591323531362,-0.425449245758386,-0.424149242383244,-0.421866934738057,
-0.403882436285767,-0.362607584903254,-0.334182778948562,-0.330378163671569,
-0.328521578285634,-0.32706791515303,-0.325455813320718,-0.32280158310927,
-0.313213181689532,-0.296899260920132,-0.243764744231135,-0.240237139387362,
-0.230882634924572,-0.22918786178731,-0.22813976010179,-0.227327639154328,
-0.226566885683579,-0.225185861025886,-0.220767167053036,-0.213575914891285,
-0.187113952443034,-0.138082375652246,-0.131803064687726,-0.129456507495738,
-0.128066671179677,-0.126605443410526,-0.124691895206008,-0.120593875903446,
-0.0835466320727342,-0.0586127139958924,-0.0515117633699154,-0.046961085874668,
-0.0316015195739975,-0.0294403800752858,-0.0283979762831173,-0.0275865095537347,
-0.0268252214746157,-0.0259135823220781,-0.0245776849928189,-0.0192352210050872,
-0.000591821998673919),.UNSPECIFIED.);
#810=B_SPLINE_CURVE_WITH_KNOTS('',3,(#21733,#21734,#21735,#21736,#21737,
#21738,#21739,#21740,#21741,#21742,#21743,#21744,#21745,#21746,#21747,#21748,
#21749,#21750,#21751,#21752,#21753,#21754,#21755,#21756,#21757,#21758,#21759,
#21760,#21761,#21762,#21763,#21764,#21765,#21766,#21767,#21768,#21769,#21770,
#21771,#21772,#21773,#21774,#21775,#21776,#21777,#21778,#21779,#21780,#21781,
#21782,#21783,#21784,#21785,#21786,#21787,#21788,#21789,#21790,#21791,#21792,
#21793,#21794,#21795,#21796,#21797,#21798,#21799,#21800,#21801,#21802,#21803,
#21804,#21805,#21806,#21807,#21808,#21809,#21810,#21811,#21812,#21813,#21814,
#21815,#21816,#21817,#21818,#21819,#21820,#21821,#21822,#21823,#21824,#21825,
#21826,#21827,#21828,#21829,#21830,#21831,#21832,#21833,#21834,#21835,#21836,
#21837,#21838,#21839,#21840,#21841,#21842,#21843,#21844,#21845,#21846,#21847,
#21848,#21849,#21850,#21851,#21852,#21853,#21854,#21855,#21856,#21857,#21858,
#21859,#21860,#21861,#21862,#21863,#21864,#21865,#21866,#21867,#21868,#21869,
#21870,#21871,#21872,#21873,#21874,#21875,#21876,#21877,#21878,#21879,#21880,
#21881,#21882,#21883,#21884,#21885,#21886,#21887,#21888,#21889,#21890,#21891,
#21892,#21893,#21894,#21895,#21896,#21897,#21898,#21899,#21900,#21901,#21902,
#21903,#21904,#21905,#21906,#21907,#21908,#21909,#21910,#21911,#21912,#21913,
#21914,#21915,#21916,#21917,#21918,#21919,#21920,#21921,#21922),
 .UNSPECIFIED.,.F.,.F.,(4,3,3,3,3,3,3,3,3,3,3,3,3,3,3,3,3,3,3,3,3,3,3,3,
3,3,3,3,3,3,3,3,3,3,3,3,3,3,3,3,3,3,3,3,3,3,3,3,3,3,3,3,3,3,3,3,3,3,3,3,
3,3,3,4),(191.637151868978,191.750774088638,191.864712447052,191.979141592408,
192.065437505541,192.170383320405,192.275171385404,192.379835916045,192.484434423837,
192.589002493249,192.693575664582,192.798259619649,192.90300468305,193.00793252951,
193.064118373902,193.169064188766,193.273852253765,193.378516784406,193.483115292198,
193.58768336161,193.692256532943,193.79694048801,193.901685551411,194.006613397871,
194.062799242263,194.167745057127,194.272533122126,194.377197652767,194.481796160559,
194.586364229971,194.690937401303,194.79562135637,194.900366419771,195.005294266231,
195.061480110623,195.166425925487,195.271213990486,195.375878521127,195.480477028919,
195.585045098331,195.689618269664,195.794302224731,195.899047288131,196.003975134592,
196.060160978984,196.165106793848,196.269894858847,196.374559389488,196.47915789728,
196.583725966692,196.688299138025,196.792983093092,196.897728156493,197.002656002953,
197.058841847345,197.166528763385,197.269778351084,197.372930295233,197.476022111771,
197.579091227138,197.682228012493,197.785405386153,197.888722207365,197.920337175666),
 .UNSPECIFIED.);
#811=B_SPLINE_CURVE_WITH_KNOTS('',3,(#21924,#21925,#21926,#21927,#21928,
#21929,#21930,#21931,#21932,#21933),.UNSPECIFIED.,.F.,.F.,(4,1,1,1,1,1,
1,4),(185.353966561798,186.073352295377,187.072033163737,188.070714032098,
189.069394900459,190.06807576882,191.06675663718,191.637151868978),
 .UNSPECIFIED.);
#812=B_SPLINE_CURVE_WITH_KNOTS('',3,(#21935,#21936,#21937,#21938,#21939,
#21940,#21941,#21942,#21943,#21944,#21945,#21946,#21947,#21948,#21949,#21950,
#21951,#21952,#21953,#21954,#21955,#21956,#21957,#21958,#21959,#21960,#21961,
#21962,#21963,#21964,#21965,#21966,#21967,#21968,#21969,#21970,#21971,#21972,
#21973,#21974,#21975,#21976,#21977,#21978,#21979,#21980,#21981,#21982,#21983,
#21984,#21985,#21986,#21987,#21988,#21989,#21990,#21991,#21992,#21993,#21994,
#21995,#21996,#21997,#21998,#21999,#22000,#22001,#22002,#22003,#22004,#22005,
#22006,#22007,#22008,#22009,#22010,#22011,#22012,#22013,#22014,#22015,#22016,
#22017,#22018,#22019,#22020,#22021,#22022,#22023,#22024,#22025,#22026,#22027,
#22028,#22029,#22030,#22031,#22032,#22033,#22034,#22035,#22036,#22037,#22038,
#22039,#22040,#22041,#22042,#22043,#22044,#22045,#22046,#22047,#22048,#22049,
#22050,#22051,#22052,#22053,#22054,#22055,#22056,#22057,#22058,#22059,#22060,
#22061,#22062,#22063,#22064,#22065,#22066,#22067,#22068,#22069,#22070,#22071,
#22072,#22073,#22074,#22075,#22076,#22077,#22078,#22079,#22080,#22081,#22082,
#22083,#22084,#22085,#22086,#22087,#22088,#22089,#22090,#22091,#22092,#22093,
#22094,#22095,#22096,#22097,#22098,#22099,#22100,#22101,#22102,#22103,#22104,
#22105,#22106,#22107,#22108,#22109,#22110,#22111,#22112,#22113,#22114,#22115,
#22116,#22117,#22118,#22119,#22120,#22121,#22122,#22123,#22124,#22125,#22126,
#22127,#22128,#22129,#22130,#22131,#22132,#22133,#22134,#22135,#22136,#22137,
#22138,#22139,#22140,#22141,#22142,#22143,#22144,#22145,#22146,#22147,#22148,
#22149,#22150,#22151,#22152,#22153,#22154,#22155,#22156,#22157,#22158,#22159,
#22160,#22161,#22162,#22163,#22164,#22165,#22166,#22167,#22168,#22169,#22170,
#22171,#22172,#22173,#22174,#22175,#22176,#22177,#22178,#22179,#22180,#22181,
#22182,#22183,#22184,#22185,#22186,#22187,#22188,#22189,#22190,#22191,#22192,
#22193,#22194,#22195,#22196,#22197,#22198,#22199,#22200,#22201,#22202,#22203,
#22204,#22205,#22206,#22207,#22208,#22209,#22210,#22211,#22212,#22213,#22214,
#22215,#22216,#22217,#22218,#22219,#22220,#22221,#22222,#22223,#22224,#22225,
#22226,#22227,#22228,#22229,#22230,#22231,#22232,#22233,#22234,#22235,#22236,
#22237,#22238,#22239,#22240,#22241,#22242,#22243,#22244,#22245,#22246,#22247,
#22248,#22249,#22250,#22251,#22252,#22253,#22254,#22255,#22256,#22257,#22258,
#22259,#22260,#22261,#22262,#22263,#22264,#22265,#22266,#22267,#22268,#22269,
#22270,#22271,#22272,#22273,#22274,#22275,#22276,#22277,#22278,#22279,#22280,
#22281,#22282,#22283,#22284,#22285,#22286,#22287,#22288,#22289,#22290,#22291,
#22292,#22293,#22294,#22295,#22296,#22297,#22298,#22299,#22300,#22301,#22302,
#22303,#22304,#22305,#22306,#22307,#22308,#22309,#22310,#22311,#22312,#22313,
#22314,#22315,#22316,#22317,#22318,#22319,#22320,#22321,#22322,#22323,#22324,
#22325,#22326,#22327,#22328,#22329,#22330,#22331,#22332,#22333,#22334,#22335,
#22336,#22337,#22338,#22339,#22340,#22341,#22342,#22343,#22344,#22345,#22346,
#22347,#22348,#22349,#22350,#22351,#22352,#22353,#22354,#22355,#22356,#22357,
#22358,#22359,#22360,#22361,#22362,#22363,#22364,#22365,#22366,#22367,#22368,
#22369,#22370,#22371,#22372,#22373,#22374,#22375,#22376,#22377,#22378,#22379,
#22380,#22381,#22382,#22383,#22384,#22385,#22386,#22387,#22388,#22389,#22390,
#22391,#22392,#22393,#22394,#22395,#22396,#22397,#22398,#22399,#22400,#22401,
#22402,#22403,#22404,#22405,#22406,#22407,#22408),.UNSPECIFIED.,.F.,.F.,
(4,2,2,2,2,2,2,2,2,2,2,2,2,2,2,2,2,2,2,2,2,2,2,2,2,2,2,2,2,2,2,2,2,2,2,
2,2,2,2,2,2,2,2,2,2,2,2,2,2,2,2,2,2,2,2,2,2,2,2,2,2,2,2,2,2,2,2,2,2,2,2,
2,2,2,2,2,2,2,2,2,2,2,2,2,2,2,2,2,2,2,2,2,2,2,2,2,2,2,2,2,2,2,2,2,2,2,2,
2,2,2,2,2,2,2,2,2,2,2,2,2,2,2,2,2,2,2,2,2,2,2,2,2,2,2,2,2,2,2,2,2,2,2,2,
2,2,2,2,2,2,2,2,2,2,2,2,2,2,2,2,2,2,2,2,2,2,2,2,2,2,2,2,2,2,2,2,2,2,2,2,
2,2,2,2,2,2,2,2,2,2,2,2,2,2,2,2,2,2,2,2,2,2,2,2,2,2,2,2,2,2,2,2,2,2,2,2,
2,2,2,2,2,2,2,2,2,2,2,2,2,2,2,2,2,2,2,2,2,4),(-2.51299292533393,-2.46610032634122,
-2.46206378997104,-2.46011041784798,-2.45850469333273,-2.45757913799288,
-2.4567682118256,-2.45572898942691,-2.45358302022776,-2.43863427872868,
-2.43316037388253,-2.40673806167597,-2.38893652783773,-2.36566745758289,
-2.36093429796256,-2.35934391675669,-2.35798712656598,-2.35653568341548,
-2.35469615275721,-2.35179637727749,-2.33697269141598,-2.32547217752391,
-2.29699651997549,-2.27462371193185,-2.2655322000705,-2.26028687978431,
-2.25880080711061,-2.25790189603071,-2.25708496729721,-2.2560161327386,
-2.25365587296462,-2.22451387920756,-2.16999360416562,-2.16480385946966,
-2.16086376694101,-2.15898225384938,-2.15752056097361,-2.15613353016986,
-2.15379957661019,-2.14760046125139,-2.09710347535054,-2.07485550658659,
-2.06142571189698,-2.05944847028688,-2.05844328900751,-2.0577128102949,
-2.05679240390574,-2.05520987130727,-2.04955943588014,-2.04653170144409,
-1.98701560576162,-1.97182627808625,-1.96272074299377,-1.96011471053441,
-1.95851373520106,-1.95705821089759,-1.95518261419357,-1.95127910466021,
-1.91303016559547,-1.86629553548218,-1.8608438570258,-1.85935070707653,
-1.85845024074039,-1.85763382537925,-1.85656823109102,-1.85477558022048,
-1.84352510351551,-1.81798063684283,-1.78770996798438,-1.77229553056732,
-1.76309182924484,-1.76047573615312,-1.758872399353,-1.75741723310318,-1.75554560904556,
-1.75166310211164,-1.71852209800046,-1.66682131944643,-1.66120458745397,
-1.65969571875036,-1.6587916564594,-1.6579760929404,-1.65691705506076,-1.6546098411465,
-1.61957674401776,-1.5888612071534,-1.57288577854611,-1.56344045462846,
-1.56080029019318,-1.55919145338704,-1.55773731249577,-1.55587537643359,
-1.55204295474933,-1.52218890243156,-1.48035045393073,-1.46247803346655,
-1.46041977583916,-1.45939796528743,-1.45866539178634,-1.45787074520855,
-1.45645808246911,-1.45263812095128,-1.44841242693519,-1.38677694363034,
-1.37232739742528,-1.36354746496801,-1.36097460841757,-1.35938084450656,
-1.35792311275027,-1.35606353015883,-1.35213968277445,-1.34847991301223,
-1.30448661852658,-1.26659330698944,-1.26329337279937,-1.2608540115656,
-1.2597588675079,-1.25894074574546,-1.25815682943634,-1.25679763219949,
-1.25258907853114,-1.22532319393729,-1.20364082273283,-1.16616660489521,
-1.16225731661163,-1.16038034418743,-1.1589243723157,-1.15732352944667,
-1.15471911733276,-1.14563340123966,-1.13048851089312,-1.10040561445415,
-1.06338078137792,-1.06110997146444,-1.06005777661735,-1.05924316570366,
-1.05833542247115,-1.05681007670588,-1.05101330486018,-1.04061918806097,
-1.01305002369911,-0.966280312953325,-0.962501154673286,-0.960649818816324,
-0.959196992760356,-0.957582448703555,-0.954916413668964,-0.945200863852007,
-0.928583773945686,-0.897341724027673,-0.875902743865246,-0.873242016439939,
-0.863169666209752,-0.861435962530015,-0.860387647753016,-0.859573594058342,
-0.858663778337828,-0.857129004969654,-0.851226035918646,-0.840561660960375,
-0.811855754216749,-0.808721060416394,-0.766794006787699,-0.762913985947473,
-0.761042791253477,-0.759587615216392,-0.757983919675891,-0.755366455331668,
-0.74614997146241,-0.730704019666438,-0.7003806679752,-0.676933827109281,
-0.66377556885267,-0.661698076332219,-0.660672476293721,-0.659862788128503,
-0.658928060004274,-0.657280907945926,-0.649953497122562,-0.635361763496325,
-0.627958062434114,-0.591352052038193,-0.58191173820703,-0.566209770861689,
-0.563255205789475,-0.561398929389737,-0.559945579242589,-0.55833389742747,
-0.555680526470597,-0.546097031080555,-0.529793288114636,-0.470390524506826,
-0.463447520394626,-0.461763543492189,-0.460810381162685,-0.46000988678922,
-0.459011838063871,-0.457069756412612,-0.443622053739423,-0.421490555613157,
-0.370842893860754,-0.364652952795936,-0.362320399412465,-0.360933427717102,
-0.359471225114624,-0.357588124787432,-0.353632377656631,-0.348422104912957,
-0.293861808142017,-0.26473991407143,-0.262378762688631,-0.261309605297285,
-0.260492467645774,-0.259593359841965,-0.258107041695583,-0.252729151400296,
-0.243371670503992,-0.217523700028426,-0.18705412150265,-0.167107334113529,
-0.163940212793613,-0.16204038194702,-0.16057638547168,-0.159222387948782,
-0.157677014250814,-0.153394738580995,-0.132342780601224,-0.114548811848656,
-0.0676986060079104,-0.0634446307204431,-0.0620282532650802,-0.0612327688530294,
-0.0605002554972148,-0.059479786098308,-0.0574287014922809,-0.0399052997808067,
-0.000592787106899905),.UNSPECIFIED.);
#813=B_SPLINE_CURVE_WITH_KNOTS('',3,(#22410,#22411,#22412,#22413,#22414,
#22415,#22416,#22417,#22418,#22419,#22420,#22421,#22422,#22423,#22424,#22425,
#22426,#22427,#22428,#22429,#22430,#22431,#22432,#22433,#22434,#22435,#22436,
#22437,#22438,#22439,#22440,#22441,#22442,#22443,#22444,#22445,#22446,#22447,
#22448,#22449,#22450,#22451,#22452,#22453,#22454,#22455,#22456,#22457,#22458,
#22459,#22460,#22461,#22462,#22463,#22464,#22465,#22466,#22467,#22468,#22469,
#22470,#22471,#22472,#22473,#22474,#22475,#22476,#22477,#22478,#22479,#22480,
#22481,#22482,#22483,#22484,#22485,#22486,#22487,#22488,#22489,#22490,#22491,
#22492,#22493,#22494,#22495,#22496,#22497,#22498,#22499,#22500,#22501,#22502,
#22503,#22504,#22505,#22506,#22507,#22508,#22509,#22510,#22511,#22512,#22513,
#22514,#22515,#22516,#22517,#22518,#22519,#22520,#22521,#22522,#22523,#22524,
#22525,#22526,#22527,#22528,#22529,#22530,#22531,#22532,#22533,#22534,#22535,
#22536,#22537,#22538,#22539,#22540,#22541,#22542,#22543,#22544,#22545,#22546,
#22547,#22548,#22549,#22550,#22551,#22552,#22553,#22554,#22555,#22556,#22557,
#22558,#22559,#22560,#22561,#22562,#22563,#22564,#22565,#22566,#22567,#22568,
#22569,#22570,#22571,#22572,#22573,#22574,#22575,#22576,#22577,#22578,#22579,
#22580,#22581,#22582,#22583,#22584,#22585,#22586,#22587,#22588,#22589,#22590,
#22591,#22592,#22593,#22594,#22595,#22596,#22597,#22598,#22599),
 .UNSPECIFIED.,.F.,.F.,(4,3,3,3,3,3,3,3,3,3,3,3,3,3,3,3,3,3,3,3,3,3,3,3,
3,3,3,3,3,3,3,3,3,3,3,3,3,3,3,3,3,3,3,3,3,3,3,3,3,3,3,3,3,3,3,3,3,3,3,3,
3,3,3,4),(166.504410640259,166.610530706907,166.716694140663,166.823018116949,
166.929429397535,167.036059350254,167.098415796522,167.203361611386,167.308149676385,
167.412814207026,167.517412714818,167.62198078423,167.726553955562,167.831237910629,
167.93598297403,168.04091082049,168.097096664883,168.202042479747,168.306830544746,
168.411495075388,168.516093583179,168.620661652592,168.725234823924,168.829918778992,
168.934663842393,169.039591688853,169.095777533244,169.200723348108,169.305511413107,
169.410175943748,169.51477445154,169.619342520952,169.723915692285,169.828599647352,
169.933344710753,170.038272557213,170.094458401605,170.199404216469,170.304192281468,
170.408856812109,170.513455319901,170.618023389313,170.722596560645,170.827280515712,
170.932025579113,171.036953425573,171.093139269965,171.198085084829,171.302873149828,
171.407537680469,171.512136188261,171.616704257673,171.721277429005,171.825961384073,
171.930706447474,172.035634293934,172.091820138326,172.196174855182,172.300380791839,
172.404474543733,172.508507006465,172.61250123859,172.716536906099,172.787595947439),
 .UNSPECIFIED.);
#814=B_SPLINE_CURVE_WITH_KNOTS('',3,(#22601,#22602,#22603,#22604,#22605,
#22606,#22607,#22608,#22609,#22610),.UNSPECIFIED.,.F.,.F.,(4,1,1,1,1,1,
1,4),(160.221234148943,161.106330586358,162.105011454719,163.103692323079,
164.10237319144,165.101054059801,166.099734928162,166.504404121023),
 .UNSPECIFIED.);
#815=B_SPLINE_CURVE_WITH_KNOTS('',3,(#22612,#22613,#22614,#22615,#22616,
#22617,#22618,#22619,#22620,#22621,#22622,#22623,#22624,#22625,#22626,#22627,
#22628,#22629,#22630,#22631,#22632,#22633,#22634,#22635,#22636,#22637,#22638,
#22639,#22640,#22641,#22642,#22643,#22644,#22645,#22646,#22647,#22648,#22649,
#22650,#22651,#22652,#22653,#22654,#22655,#22656,#22657,#22658,#22659,#22660,
#22661,#22662,#22663,#22664,#22665,#22666,#22667,#22668,#22669,#22670,#22671,
#22672,#22673,#22674,#22675,#22676,#22677,#22678,#22679,#22680,#22681,#22682,
#22683,#22684,#22685,#22686,#22687,#22688,#22689,#22690,#22691,#22692,#22693,
#22694,#22695,#22696,#22697,#22698,#22699,#22700,#22701,#22702,#22703,#22704,
#22705,#22706,#22707,#22708,#22709,#22710,#22711,#22712,#22713,#22714,#22715,
#22716,#22717,#22718,#22719,#22720,#22721,#22722,#22723,#22724,#22725,#22726,
#22727,#22728,#22729,#22730,#22731,#22732,#22733,#22734,#22735,#22736,#22737,
#22738,#22739,#22740,#22741,#22742,#22743,#22744,#22745,#22746,#22747,#22748,
#22749,#22750,#22751,#22752,#22753,#22754,#22755,#22756,#22757,#22758,#22759,
#22760,#22761,#22762,#22763,#22764,#22765,#22766,#22767,#22768,#22769,#22770,
#22771,#22772,#22773,#22774,#22775,#22776,#22777,#22778,#22779,#22780,#22781,
#22782,#22783,#22784,#22785,#22786,#22787,#22788,#22789,#22790,#22791,#22792,
#22793,#22794,#22795,#22796,#22797,#22798,#22799,#22800,#22801),
 .UNSPECIFIED.,.F.,.F.,(4,3,3,3,3,3,3,3,3,3,3,3,3,3,3,3,3,3,3,3,3,3,3,3,
3,3,3,3,3,3,3,3,3,3,3,3,3,3,3,3,3,3,3,3,3,3,3,3,3,3,3,3,3,3,3,3,3,3,3,3,
3,3,3,4),(153.9380400259,154.098367385836,154.115564507833,154.220510322697,
154.325298387696,154.429962918337,154.534561426129,154.639129495541,154.743702666873,
154.84838662194,154.953131685341,155.058059531801,155.114245376193,155.219191191057,
155.323979256056,155.428643786697,155.533242294489,155.637810363901,155.742383535233,
155.847067490301,155.951812553701,156.056740400161,156.112926244554,156.217872059418,
156.322660124417,156.427324655059,156.53192316285,156.636491232262,156.741064403595,
156.845748358663,156.950493422063,157.055421268524,157.111607112915,157.216552927779,
157.321340992778,157.426005523419,157.530604031211,157.635172100623,157.739745271955,
157.844429227023,157.949174290423,158.054102136884,158.110287981276,158.21523379614,
158.320021861139,158.42468639178,158.529284899572,158.633852968984,158.738426140316,
158.843110095383,158.947855158784,159.052783005244,159.108968849636,159.2139146645,
159.318702729499,159.42336726014,159.527965767932,159.632533837343,159.737107008676,
159.841790963743,159.946536027144,160.051463873604,160.107649717997,160.22122533308),
 .UNSPECIFIED.);
#816=B_SPLINE_CURVE_WITH_KNOTS('',3,(#22803,#22804,#22805,#22806,#22807,
#22808,#22809,#22810,#22811,#22812,#22813,#22814,#22815,#22816,#22817,#22818,
#22819,#22820,#22821,#22822,#22823,#22824,#22825,#22826,#22827,#22828,#22829,
#22830,#22831,#22832,#22833,#22834,#22835,#22836,#22837,#22838,#22839,#22840,
#22841,#22842,#22843,#22844,#22845,#22846,#22847,#22848,#22849,#22850,#22851,
#22852,#22853,#22854,#22855,#22856,#22857,#22858,#22859,#22860,#22861,#22862,
#22863,#22864,#22865,#22866,#22867,#22868,#22869,#22870,#22871,#22872,#22873,
#22874,#22875,#22876,#22877,#22878,#22879,#22880,#22881,#22882,#22883,#22884,
#22885,#22886,#22887,#22888,#22889,#22890,#22891,#22892,#22893,#22894,#22895,
#22896,#22897,#22898,#22899,#22900,#22901,#22902,#22903,#22904,#22905,#22906,
#22907,#22908,#22909,#22910,#22911,#22912,#22913,#22914,#22915,#22916,#22917,
#22918,#22919,#22920,#22921,#22922,#22923,#22924,#22925,#22926,#22927,#22928,
#22929,#22930,#22931,#22932,#22933,#22934,#22935,#22936,#22937,#22938,#22939,
#22940,#22941,#22942,#22943,#22944,#22945,#22946,#22947,#22948,#22949,#22950,
#22951,#22952,#22953,#22954,#22955,#22956,#22957,#22958,#22959,#22960,#22961,
#22962,#22963,#22964,#22965,#22966,#22967,#22968,#22969,#22970,#22971,#22972,
#22973,#22974,#22975,#22976,#22977,#22978,#22979,#22980,#22981,#22982,#22983,
#22984,#22985,#22986,#22987,#22988,#22989,#22990,#22991,#22992,#22993,#22994,
#22995,#22996,#22997,#22998,#22999,#23000,#23001,#23002,#23003,#23004,#23005,
#23006,#23007,#23008,#23009,#23010,#23011,#23012,#23013,#23014,#23015,#23016,
#23017,#23018,#23019,#23020,#23021,#23022,#23023,#23024,#23025,#23026,#23027,
#23028,#23029,#23030,#23031,#23032,#23033,#23034,#23035,#23036,#23037,#23038,
#23039,#23040,#23041,#23042,#23043,#23044,#23045,#23046,#23047,#23048,#23049,
#23050,#23051,#23052,#23053,#23054,#23055,#23056,#23057,#23058,#23059,#23060,
#23061,#23062,#23063,#23064,#23065,#23066,#23067,#23068,#23069,#23070,#23071,
#23072,#23073,#23074,#23075,#23076,#23077,#23078,#23079,#23080,#23081,#23082,
#23083,#23084,#23085,#23086,#23087,#23088,#23089,#23090,#23091,#23092,#23093,
#23094,#23095,#23096,#23097,#23098,#23099,#23100,#23101,#23102,#23103,#23104,
#23105,#23106,#23107,#23108,#23109,#23110,#23111,#23112,#23113,#23114,#23115,
#23116,#23117,#23118,#23119,#23120,#23121,#23122,#23123,#23124,#23125,#23126,
#23127,#23128,#23129,#23130,#23131,#23132,#23133,#23134,#23135,#23136,#23137,
#23138,#23139,#23140,#23141,#23142,#23143,#23144,#23145,#23146,#23147,#23148,
#23149,#23150,#23151,#23152,#23153,#23154,#23155,#23156,#23157,#23158,#23159,
#23160,#23161,#23162,#23163,#23164,#23165,#23166,#23167,#23168,#23169,#23170,
#23171,#23172,#23173,#23174,#23175,#23176,#23177,#23178,#23179,#23180,#23181,
#23182,#23183,#23184,#23185,#23186,#23187,#23188,#23189,#23190,#23191,#23192,
#23193,#23194,#23195,#23196,#23197,#23198,#23199,#23200,#23201,#23202,#23203,
#23204,#23205,#23206,#23207,#23208,#23209,#23210,#23211,#23212,#23213,#23214,
#23215,#23216,#23217,#23218,#23219,#23220,#23221,#23222,#23223,#23224,#23225,
#23226,#23227,#23228,#23229,#23230,#23231,#23232,#23233,#23234,#23235,#23236,
#23237,#23238,#23239,#23240,#23241,#23242,#23243,#23244,#23245,#23246,#23247,
#23248,#23249,#23250,#23251,#23252,#23253,#23254,#23255,#23256,#23257,#23258,
#23259,#23260,#23261,#23262,#23263,#23264,#23265,#23266,#23267,#23268,#23269,
#23270,#23271,#23272,#23273,#23274),.UNSPECIFIED.,.F.,.F.,(4,2,2,2,2,2,
2,2,2,2,2,2,2,2,2,2,2,2,2,2,2,2,2,2,2,2,2,2,2,2,2,2,2,2,2,2,2,2,2,2,2,2,
2,2,2,2,2,2,2,2,2,2,2,2,2,2,2,2,2,2,2,2,2,2,2,2,2,2,2,2,2,2,2,2,2,2,2,2,
2,2,2,2,2,2,2,2,2,2,2,2,2,2,2,2,2,2,2,2,2,2,2,2,2,2,2,2,2,2,2,2,2,2,2,2,
2,2,2,2,2,2,2,2,2,2,2,2,2,2,2,2,2,2,2,2,2,2,2,2,2,2,2,2,2,2,2,2,2,2,2,2,
2,2,2,2,2,2,2,2,2,2,2,2,2,2,2,2,2,2,2,2,2,2,2,2,2,2,2,2,2,2,2,2,2,2,2,2,
2,2,2,2,2,2,2,2,2,2,2,2,2,2,2,2,2,2,2,2,2,2,2,2,2,2,2,2,2,2,2,2,2,2,2,2,
2,2,2,2,2,2,2,2,2,2,2,2,2,4),(-2.51391341080619,-2.46179105637164,-2.45646047624814,
-2.45239245541763,-2.45048498056078,-2.44902500250497,-2.44763380211385,
-2.44527872354363,-2.43893617240994,-2.39141999370173,-2.37440683007866,
-2.35421939631866,-2.35143874649784,-2.35053108790662,-2.34977064764138,
-2.34895871525468,-2.34791023253071,-2.34621361432944,-2.33681950298222,
-2.33334898385338,-2.32150584311304,-2.27609323468591,-2.26253190319611,
-2.25698556062711,-2.25278659141177,-2.25085436174359,-2.24939073407475,
-2.24800742062708,-2.24569302364923,-2.23961207572437,-2.18732651562046,
-2.15666978477067,-2.15222637690514,-2.15083815367759,-2.15007715390696,
-2.14926570876715,-2.14822215420747,-2.14605451854881,-2.13049721943133,
-2.0759995059429,-2.06266279375167,-2.05718217169216,-2.0530229400672,-2.05109815612437,
-2.04963563271675,-2.0482499910716,-2.04592361493768,-2.03976769426212,
-1.98854620835413,-1.95419984125791,-1.95177623722019,-1.95068398276447,
-1.94986628644607,-1.94896953730749,-1.94749336834567,-1.9437121983998,
-1.8891145568725,-1.85787475887526,-1.85341249799428,-1.85143189730792,
-1.84996054334067,-1.84859078761762,-1.84671278233194,-1.84197255977692,
-1.83982448374706,-1.79110790555178,-1.76763721775764,-1.7582844284931,
-1.75290927375168,-1.75142339841012,-1.75052449763613,-1.74970750080907,
-1.74863847358257,-1.74627737467739,-1.71795847904892,-1.66650674285726,
-1.65542918680646,-1.65264275372697,-1.6510015031532,-1.64955323703508,
-1.64774577847719,-1.6449501826694,-1.64007628583328,-1.59189649948304,
-1.56805296809368,-1.55861239011388,-1.55320103597566,-1.55171167186411,
-1.55081199953163,-1.5499952504192,-1.54892781446164,-1.54657527710547,
-1.52075940821706,-1.49122308519841,-1.4605940037698,-1.45461941460919,
-1.45239318426608,-1.45087478567476,-1.44939701878785,-1.44762559290574,
-1.44323236780215,-1.44043069598607,-1.39183491897399,-1.36827757995644,
-1.358904164305,-1.35352041311632,-1.35203365696884,-1.35113453176544,-1.35031754991976,
-1.34924883499607,-1.3468895942435,-1.31959018242947,-1.28267587884756,
-1.25727988501442,-1.25414780973755,-1.25225844314356,-1.25079624427474,
-1.24921648202506,-1.24670710396124,-1.23851607656586,-1.22536318988242,
-1.17234525530424,-1.15505807771875,-1.15305816416419,-1.15203397286243,
-1.15127713800862,-1.15043982362538,-1.14923746533013,-1.14616637531344,
-1.13105285439884,-1.10103987751716,-1.05816979468867,-1.05430245608908,
-1.052433558414,-1.05097846103737,-1.04937312003295,-1.04674904577157,-1.03746901211778,
-1.02187699205744,-0.991434534160672,-0.972458603521345,-0.955369730963324,
-0.953155366604645,-0.952113862259828,-0.951300595898236,-0.950386668261615,
-0.948833788722708,-0.942724154853327,-0.931526244234803,-0.901683171377436,
-0.858486132769825,-0.854624265048591,-0.85275649199072,-0.851301589884239,
-0.849695773340386,-0.847069353598386,-0.837764840218069,-0.822115738278513,
-0.791628926051631,-0.755804523715857,-0.753510010816469,-0.752453308612617,
-0.75163802963243,-0.750732623601054,-0.749217922912605,-0.743538833003712,
-0.733440720432717,-0.706869236547874,-0.662549343293129,-0.658379109069224,
-0.655141656053671,-0.653221349920203,-0.651754195660049,-0.650187604366442,
-0.647737995076812,-0.640067070216302,-0.585133087501146,-0.556159397042375,
-0.55379800434309,-0.552728805350092,-0.551911664501675,-0.551012583969879,
-0.549526376038066,-0.544149575082301,-0.53479471213359,-0.511317746976424,
-0.462636720749346,-0.460430115401939,-0.455729234910676,-0.453857713395475,
-0.452489465921522,-0.451016678662117,-0.449028796616842,-0.444629193742244,
-0.438693255864835,-0.423772615512908,-0.373589266652928,-0.356206879713412,
-0.354204538545188,-0.35317969231942,-0.352422660527237,-0.351585447213904,
-0.350383794618626,-0.347467516921108,-0.312517156781276,-0.277940832295828,
-0.272439533961448,-0.258198572823757,-0.255335144968495,-0.253506498620078,
-0.25205585472538,-0.250427366546338,-0.247871253947722,-0.238625569207456,
-0.223047109894977,-0.190779511911257,-0.185486372018215,-0.156726573020153,
-0.154364801535007,-0.153295506971903,-0.15247832517276,-0.151579234129652,
-0.150645996444047,-0.147597909679877,-0.11342651764459,-0.100055177249121,
-0.0874958998967663,-0.0595261843350611,-0.0557308786672539,-0.0538760753636376,
-0.0524225515501624,-0.0508093135378623,-0.0491448044903754,-0.0466820551587498,
-0.037302115107823,-0.000592337695832264),.UNSPECIFIED.);
#817=B_SPLINE_CURVE_WITH_KNOTS('',3,(#23276,#23277,#23278,#23279,#23280,
#23281,#23282,#23283,#23284,#23285,#23286,#23287,#23288,#23289,#23290,#23291,
#23292,#23293,#23294,#23295,#23296,#23297,#23298,#23299,#23300,#23301,#23302,
#23303,#23304,#23305,#23306,#23307,#23308,#23309,#23310,#23311,#23312,#23313,
#23314,#23315,#23316,#23317,#23318,#23319,#23320,#23321,#23322,#23323,#23324,
#23325,#23326,#23327,#23328,#23329,#23330,#23331,#23332,#23333,#23334,#23335,
#23336,#23337,#23338,#23339,#23340,#23341,#23342,#23343,#23344,#23345,#23346,
#23347,#23348,#23349,#23350,#23351,#23352,#23353,#23354,#23355,#23356,#23357,
#23358,#23359,#23360,#23361,#23362,#23363,#23364,#23365,#23366,#23367,#23368,
#23369,#23370,#23371,#23372,#23373,#23374,#23375,#23376,#23377,#23378,#23379,
#23380,#23381,#23382,#23383,#23384,#23385,#23386,#23387,#23388,#23389,#23390,
#23391,#23392,#23393,#23394,#23395,#23396,#23397,#23398,#23399,#23400,#23401,
#23402,#23403,#23404,#23405,#23406,#23407,#23408,#23409,#23410,#23411,#23412,
#23413,#23414,#23415,#23416,#23417,#23418,#23419,#23420,#23421,#23422,#23423,
#23424,#23425,#23426,#23427,#23428,#23429,#23430,#23431,#23432,#23433,#23434,
#23435,#23436,#23437,#23438,#23439,#23440,#23441,#23442,#23443,#23444,#23445,
#23446,#23447,#23448,#23449,#23450,#23451,#23452,#23453,#23454,#23455,#23456,
#23457,#23458,#23459,#23460,#23461,#23462,#23463,#23464,#23465,#23466,#23467,
#23468,#23469,#23470,#23471,#23472,#23473,#23474,#23475,#23476,#23477,#23478,
#23479,#23480,#23481,#23482,#23483,#23484,#23485,#23486,#23487,#23488,#23489,
#23490,#23491,#23492,#23493,#23494,#23495,#23496,#23497,#23498,#23499,#23500,
#23501,#23502,#23503,#23504,#23505,#23506,#23507,#23508,#23509,#23510,#23511,
#23512,#23513,#23514,#23515,#23516,#23517,#23518,#23519,#23520,#23521,#23522,
#23523,#23524,#23525,#23526,#23527,#23528,#23529,#23530,#23531,#23532,#23533,
#23534,#23535,#23536,#23537,#23538,#23539,#23540,#23541,#23542,#23543,#23544,
#23545,#23546,#23547,#23548,#23549,#23550,#23551,#23552,#23553,#23554,#23555,
#23556,#23557,#23558,#23559,#23560,#23561,#23562,#23563,#23564,#23565,#23566,
#23567,#23568,#23569,#23570,#23571,#23572,#23573,#23574,#23575,#23576,#23577,
#23578,#23579,#23580,#23581,#23582,#23583,#23584,#23585,#23586,#23587,#23588,
#23589,#23590,#23591,#23592,#23593,#23594,#23595,#23596,#23597,#23598,#23599,
#23600,#23601,#23602,#23603,#23604,#23605,#23606,#23607,#23608,#23609,#23610,
#23611,#23612,#23613,#23614,#23615,#23616,#23617,#23618,#23619,#23620,#23621,
#23622,#23623,#23624,#23625,#23626,#23627,#23628,#23629,#23630,#23631,#23632,
#23633,#23634,#23635,#23636,#23637,#23638,#23639,#23640,#23641,#23642,#23643,
#23644,#23645,#23646,#23647,#23648,#23649,#23650,#23651,#23652,#23653,#23654,
#23655,#23656,#23657,#23658,#23659,#23660,#23661,#23662,#23663,#23664,#23665,
#23666,#23667,#23668,#23669,#23670,#23671,#23672,#23673,#23674,#23675,#23676,
#23677,#23678,#23679,#23680,#23681,#23682,#23683,#23684,#23685,#23686,#23687,
#23688,#23689,#23690,#23691,#23692,#23693,#23694,#23695,#23696,#23697,#23698,
#23699,#23700,#23701,#23702,#23703,#23704,#23705,#23706,#23707,#23708,#23709,
#23710,#23711,#23712,#23713,#23714,#23715,#23716,#23717,#23718,#23719,#23720,
#23721,#23722,#23723,#23724,#23725,#23726,#23727,#23728,#23729,#23730,#23731,
#23732,#23733,#23734,#23735,#23736,#23737,#23738,#23739,#23740,#23741,#23742,
#23743,#23744,#23745,#23746,#23747,#23748,#23749),.UNSPECIFIED.,.F.,.F.,
(4,2,2,2,2,2,2,2,2,2,2,2,2,2,2,2,2,2,2,2,2,2,2,2,2,2,2,2,2,2,2,2,2,2,2,
2,2,2,2,2,2,2,2,2,2,2,2,2,2,2,2,2,2,2,2,2,2,2,2,2,2,2,2,2,2,2,2,2,2,2,2,
2,2,2,2,2,2,2,2,2,2,2,2,2,2,2,2,2,2,2,2,2,2,2,2,2,2,2,2,2,2,2,2,2,2,2,2,
2,2,2,2,2,2,2,2,2,2,2,2,2,2,2,2,2,2,2,2,2,2,2,2,2,2,2,2,2,2,2,2,2,2,2,2,
2,2,2,2,2,2,2,2,2,2,2,2,2,2,2,2,2,2,2,2,2,2,2,2,2,2,2,2,2,2,2,2,2,2,2,2,
2,2,2,2,2,2,2,2,2,2,2,2,2,2,2,2,2,2,2,2,2,2,2,2,2,2,2,2,2,2,2,2,2,2,2,2,
2,2,2,2,2,2,2,2,2,2,2,2,2,2,2,2,2,2,2,2,2,4),(-2.51356825422661,-2.47394218197505,
-2.47035764364301,-2.46856460930196,-2.46746334599422,-2.46644534921851,
-2.46571328584953,-2.46491694785596,-2.46349574152554,-2.45920389941625,
-2.42128676523049,-2.40237491188082,-2.37511750803352,-2.36979029470891,
-2.36814327223351,-2.36654227980619,-2.36508628863625,-2.36320945561377,
-2.35930105980408,-2.32289862526151,-2.28907209137147,-2.27592950555056,
-2.27140987911008,-2.26831759641163,-2.26738442327779,-2.26648543088389,
-2.26566838390759,-2.26459933535138,-2.26223836622955,-2.23422475439631,
-2.19372428850427,-2.17337512531339,-2.16947772407708,-2.16757294700741,
-2.16611318093781,-2.16472078445636,-2.16236025783666,-2.1559841076186,
-2.1097009288288,-2.07387810337846,-2.07066336847685,-2.06829608724467,
-2.06720164898327,-2.06638356620263,-2.06548769629021,-2.06401569760017,
-2.05932580979843,-1.99590980774065,-1.98049688165391,-1.97129367007065,
-1.96867751474784,-1.96707409719654,-1.96561882973147,-1.96374703638707,
-1.95986403677172,-1.92670244367806,-1.87499047400447,-1.86939589912413,
-1.86788903030803,-1.86698537756707,-1.86616963333975,-1.86510963264811,
-1.86279749107987,-1.82812447199477,-1.79728582954517,-1.78115424267524,
-1.77164224225226,-1.76899549189785,-1.76738512136143,-1.76593120010981,
-1.76407176928262,-1.76025240985229,-1.75656512302494,-1.70816707242092,
-1.68446523734727,-1.67505730941136,-1.66965913119662,-1.66817086172729,
-1.66727132983777,-1.66645433909318,-1.66538609431153,-1.6630298117515,
-1.63680898624427,-1.58401010853708,-1.57225570299218,-1.56941475437926,
-1.56776125692786,-1.56631416819616,-1.56452374344591,-1.56178359544932,
-1.55679881985351,-1.5086302796843,-1.4847696108149,-1.47532438259311,-1.46991086762184,
-1.46842113896675,-1.46752129367456,-1.46670442100115,-1.46563686821688,
-1.46328425094685,-1.43193736664937,-1.42669060984774,-1.39869983371182,
-1.38199428027506,-1.37224012200973,-1.36957014727232,-1.36795455237303,
-1.36650163688166,-1.36465136212075,-1.36087848773287,-1.31380889220081,
-1.27512274021726,-1.2717908044124,-1.26933268834605,-1.26823396891744,
-1.26741516102899,-1.26652106997336,-1.26505733380767,-1.26043511541086,
-1.25725185627739,-1.242305402245,-1.19354591972506,-1.17394496003048,-1.17079245707546,
-1.16889693523588,-1.16743362307259,-1.16585627364041,-1.16335844265841,
-1.1552722249205,-1.14234597843094,-1.09189387336379,-1.08656929456985,
-1.07157226112248,-1.0694239703701,-1.06838407636168,-1.06757284006429,
-1.06664716301918,-1.06504178248724,-1.05828655798903,-1.0453447488131,
-1.02040556202218,-0.974696250056967,-0.970884046106176,-0.969025901865425,
-0.967571990442836,-0.965960610073872,-0.963309858028534,-0.953758560199666,
-0.937532620694539,-0.906590565463561,-0.872113286393838,-0.869825951878624,
-0.868754255298571,-0.867936692823698,-0.867038745940872,-0.86555777966523,
-0.860235373081425,-0.851011934353765,-0.828091080754851,-0.778598776251994,
-0.772342415381426,-0.769999493465719,-0.768610404681683,-0.767148934905921,
-0.765233361386714,-0.761124413032057,-0.723669009395699,-0.683510118705204,
-0.671886725918484,-0.669901835467375,-0.668881545756867,-0.668072073851384,
-0.667133077089268,-0.665467273505235,-0.657874530018301,-0.608920538508744,
-0.605638840734015,-0.575273825582681,-0.571426086081437,-0.569560977684702,
-0.568106278805076,-0.566498780814453,-0.563865274570097,-0.554490583410462,
-0.538678736710341,-0.478971156066348,-0.477469801850242,-0.47142031050116,
-0.469818005080321,-0.468883558823451,-0.468081159595123,-0.467058149499422,
-0.464994804736573,-0.44689685800373,-0.40601053555134,-0.37547381796058,
-0.371628188459321,-0.369763309381278,-0.368308432541423,-0.368305850660745,
-0.36830327472084,-0.368300704708948,-0.368298140574993,-0.366719169944355,
-0.364178851443436,-0.361154211920972,-0.355288743722237,-0.340618973668368,
-0.304955982196178,-0.283209580502759,-0.272292806438492,-0.270515768706503,
-0.269454487671194,-0.268638384959143,-0.267735008714936,-0.266230061381181,
-0.260658779533736,-0.208943657690746,-0.175765854248469,-0.171883522994864,
-0.170011501897731,-0.168555811528997,-0.167200257655818,-0.16497475149422,
-0.158580379106579,-0.14903515131864,-0.127500661488512,-0.0983596945928476,
-0.0731308756767082,-0.0707796542191637,-0.0697122651376716,-0.0688953219904742,
-0.0679951803681352,-0.066504506316771,-0.0610826183693228,-0.014973403458735,
-0.00059288335019173),.UNSPECIFIED.);
#818=B_SPLINE_CURVE_WITH_KNOTS('',3,(#23751,#23752,#23753,#23754,#23755,
#23756,#23757,#23758,#23759,#23760,#23761,#23762,#23763,#23764,#23765,#23766,
#23767,#23768,#23769,#23770,#23771,#23772,#23773,#23774,#23775,#23776,#23777,
#23778,#23779,#23780,#23781,#23782,#23783,#23784,#23785,#23786,#23787,#23788,
#23789,#23790,#23791,#23792,#23793,#23794,#23795,#23796,#23797,#23798,#23799,
#23800,#23801,#23802,#23803,#23804,#23805,#23806,#23807,#23808,#23809,#23810,
#23811,#23812,#23813,#23814,#23815,#23816,#23817,#23818,#23819,#23820,#23821,
#23822,#23823,#23824,#23825,#23826,#23827,#23828,#23829,#23830,#23831,#23832,
#23833,#23834,#23835,#23836,#23837,#23838,#23839,#23840,#23841,#23842,#23843,
#23844,#23845,#23846,#23847,#23848,#23849,#23850,#23851,#23852,#23853,#23854,
#23855,#23856,#23857,#23858,#23859,#23860,#23861,#23862,#23863,#23864,#23865,
#23866,#23867,#23868,#23869,#23870,#23871,#23872,#23873,#23874,#23875,#23876,
#23877,#23878,#23879,#23880,#23881,#23882,#23883,#23884,#23885,#23886,#23887,
#23888,#23889,#23890,#23891,#23892,#23893,#23894,#23895,#23896,#23897,#23898,
#23899,#23900,#23901,#23902,#23903,#23904,#23905,#23906,#23907,#23908,#23909,
#23910,#23911,#23912,#23913,#23914,#23915,#23916,#23917,#23918,#23919,#23920,
#23921,#23922,#23923,#23924,#23925,#23926,#23927,#23928,#23929,#23930,#23931,
#23932,#23933,#23934,#23935,#23936,#23937,#23938,#23939,#23940,#23941,#23942,
#23943,#23944,#23945,#23946,#23947,#23948,#23949,#23950,#23951,#23952,#23953,
#23954,#23955,#23956,#23957,#23958,#23959,#23960,#23961,#23962,#23963,#23964,
#23965,#23966,#23967,#23968,#23969,#23970,#23971,#23972,#23973,#23974,#23975,
#23976,#23977,#23978,#23979,#23980,#23981,#23982,#23983,#23984,#23985,#23986,
#23987,#23988,#23989,#23990,#23991,#23992,#23993,#23994,#23995,#23996,#23997,
#23998,#23999,#24000,#24001,#24002,#24003,#24004,#24005,#24006,#24007,#24008,
#24009,#24010,#24011,#24012,#24013,#24014,#24015,#24016,#24017,#24018,#24019,
#24020,#24021,#24022,#24023,#24024,#24025,#24026,#24027,#24028,#24029,#24030,
#24031,#24032,#24033,#24034,#24035,#24036,#24037,#24038,#24039,#24040,#24041,
#24042,#24043,#24044,#24045,#24046,#24047,#24048,#24049,#24050,#24051,#24052,
#24053,#24054,#24055,#24056,#24057,#24058,#24059,#24060,#24061,#24062,#24063,
#24064,#24065,#24066,#24067,#24068,#24069,#24070,#24071,#24072,#24073,#24074,
#24075,#24076,#24077,#24078,#24079,#24080,#24081,#24082,#24083,#24084,#24085,
#24086,#24087,#24088,#24089,#24090,#24091,#24092,#24093,#24094,#24095,#24096,
#24097,#24098,#24099,#24100,#24101,#24102,#24103,#24104,#24105,#24106,#24107,
#24108,#24109,#24110,#24111,#24112,#24113,#24114,#24115,#24116,#24117,#24118,
#24119,#24120,#24121,#24122,#24123,#24124,#24125,#24126,#24127,#24128,#24129,
#24130,#24131,#24132,#24133,#24134,#24135,#24136,#24137,#24138,#24139,#24140,
#24141,#24142,#24143,#24144,#24145,#24146,#24147,#24148,#24149,#24150,#24151,
#24152,#24153,#24154,#24155,#24156,#24157,#24158,#24159,#24160,#24161,#24162,
#24163,#24164,#24165,#24166,#24167,#24168,#24169,#24170,#24171,#24172,#24173,
#24174,#24175,#24176,#24177,#24178,#24179,#24180,#24181,#24182,#24183,#24184,
#24185,#24186,#24187,#24188,#24189,#24190,#24191,#24192,#24193,#24194,#24195,
#24196,#24197,#24198,#24199,#24200,#24201,#24202,#24203,#24204,#24205,#24206,
#24207,#24208,#24209,#24210,#24211,#24212,#24213,#24214,#24215,#24216,#24217,
#24218,#24219,#24220,#24221,#24222,#24223,#24224,#24225,#24226,#24227,#24228,
#24229,#24230,#24231,#24232,#24233,#24234,#24235,#24236,#24237,#24238,#24239,
#24240,#24241,#24242,#24243,#24244,#24245,#24246,#24247,#24248,#24249,#24250,
#24251,#24252,#24253,#24254,#24255,#24256,#24257,#24258,#24259,#24260,#24261,
#24262,#24263,#24264,#24265,#24266,#24267,#24268,#24269,#24270,#24271,#24272,
#24273,#24274,#24275,#24276,#24277,#24278,#24279,#24280,#24281,#24282,#24283,
#24284,#24285,#24286,#24287,#24288,#24289,#24290,#24291,#24292),
 .UNSPECIFIED.,.F.,.F.,(4,2,2,2,2,2,2,2,2,2,2,2,2,2,2,2,2,2,2,2,2,2,2,2,
2,2,2,2,2,2,2,2,2,2,2,2,2,2,2,2,2,2,2,2,2,2,2,2,2,2,2,2,2,2,2,2,2,2,2,2,
2,2,2,2,2,2,2,2,2,2,2,2,2,2,2,2,2,2,2,2,2,2,2,2,2,2,2,2,2,2,2,2,2,2,2,2,
2,2,2,2,2,2,2,2,2,2,2,2,2,2,2,2,2,2,2,2,2,2,2,2,2,2,2,2,2,2,2,2,2,2,2,2,
2,2,2,2,2,2,2,2,2,2,2,2,2,2,2,2,2,2,2,2,2,2,2,2,2,2,2,2,2,2,2,2,2,2,2,2,
2,2,2,2,2,2,2,2,2,2,2,2,2,2,2,2,2,2,2,2,2,2,2,2,2,2,2,2,2,2,2,2,2,2,2,2,
2,2,2,2,2,2,2,2,2,2,2,2,2,2,2,2,2,2,2,2,2,2,2,2,2,2,2,2,2,2,2,2,2,2,2,2,
2,2,2,2,2,2,2,2,2,2,2,2,2,2,2,2,2,2,2,2,2,2,2,2,2,2,2,2,2,2,4),(-2.51318058552356,
-2.49534092889612,-2.48754131701959,-2.48526379985214,-2.48367623155305,
-2.48232029791119,-2.480869105159,-2.47902670392536,-2.47611614204028,-2.46110366271849,
-2.45719216229731,-2.4482463481611,-2.41465704566012,-2.38634278217323,
-2.38383158492869,-2.38272372698508,-2.3819039748108,-2.38112477548954,
-2.37978800445029,-2.37609803990247,-2.37524392204819,-2.33016470889085,
-2.30324810779577,-2.29308957097751,-2.28637664838568,-2.28405597765139,
-2.28270176040486,-2.28124666331771,-2.27937141888137,-2.27546792034526,
-2.23801034675361,-2.19055472552387,-2.18506878635465,-2.18357266925265,
-2.18267171609894,-2.18185577671024,-2.18079202416924,-2.17900509632798,
-2.16786519214015,-2.16437661174598,-2.15434279719327,-2.1132390026198,
-2.09696724467837,-2.09065782633207,-2.08746979911785,-2.08480910481439,
-2.08320752016455,-2.0832054331407,-2.08320333982577,-2.08320124020769,
-2.08319913426817,-2.08319702195549,-2.08319490324864,-2.08319277812535,
-2.08319064655953,-2.08318850854315,-2.08318636404106,-2.0831842130326,
-2.0831820555194,-2.08317989145589,-2.08317772080522,-2.08317554354486,
-2.08317335968841,-2.08317116920818,-2.08316897204192,-2.08316676816492,
-2.08316455755618,-2.0831623402143,-2.08316011610567,-2.08315788522021,
-2.08315564752342,-2.08315340300327,-2.08315115160638,-2.08314889327832,
-2.08314662805286,-2.08314435592246,-2.08169224444141,-2.07984155320643,
-2.07606278056042,-2.0292704157726,-2.00172461431719,-1.99133372423346,
-1.98553967116006,-1.98401508285565,-1.98310780279515,-1.98229361223924,
-1.9812419748891,-1.97897240728259,-1.94202195080193,-1.91196687912686,
-1.89681340039215,-1.88772415087907,-1.88512020222295,-1.88351995625251,
-1.88206473245219,-1.88018901309947,-1.87628339030214,-1.83776640312309,
-1.79131134701107,-1.78587434794294,-1.78438285874438,-1.78348291167112,
-1.78266662643691,-1.78160074787566,-1.77980663951805,-1.76851896269361,
-1.74301947834166,-1.71275854981441,-1.69735044221196,-1.68815014341382,
-1.68553483348406,-1.6839319377448,-1.68247714628894,-1.68060596857258,
-1.67672425828234,-1.64354873583983,-1.59182459669076,-1.58627733888035,
-1.58477522626193,-1.58387282123464,-1.58305708060438,-1.58199559583834,
-1.58021677907269,-1.56924845026757,-1.56766416131119,-1.56144581662258,
-1.55533910553312,-1.5154984543267,-1.49850617663551,-1.48863362841935,
-1.48595324239052,-1.4843357298402,-1.48288388999399,-1.48103881481722,
-1.47812038107284,-1.46298891176632,-1.45911271195835,-1.40502627474109,
-1.3931350771096,-1.38676476843716,-1.38519031651931,-1.38427171525415,
-1.3834596094917,-1.38240918883224,-1.38020604855366,-1.3634991266006,-1.3161611418744,
-1.29893642924169,-1.28896746900223,-1.28627799879721,-1.28465837988368,
-1.28320679838385,-1.28136498019625,-1.2784574540511,-1.26350586866066,
-1.2595644555537,-1.25707920268081,-1.19818496567701,-1.18769553955751,
-1.1859402499901,-1.18488554711709,-1.18407060456433,-1.18316425345828,
-1.18164509823361,-1.17591641972404,-1.16569378427659,-1.13866659953425,
-1.09500224789981,-1.09139448151434,-1.08743691617553,-1.0855708355205,
-1.08411214328927,-1.0825215256938,-1.07996298772627,-1.07131957188705,
-1.05717343852155,-0.997553406806989,-0.987875418513911,-0.986162710283493,
-0.985120517427023,-0.984307130637433,-0.983393530613857,-0.981842248098768,
-0.975751869820542,-0.96460444933425,-0.934845820278877,-0.89147750456786,
-0.88762127482329,-0.885754554977527,-0.884299722786788,-0.88269322044028,
-0.880063945258876,-0.870731355925798,-0.855017281231994,-0.824478255646457,
-0.788802633804009,-0.786506373492071,-0.785449312819604,-0.784633951202238,
-0.783728664988438,-0.782214624289928,-0.776543228298057,-0.766464519659003,
-0.739968165316298,-0.695543863200072,-0.691719000764627,-0.687902830832579,
-0.686044019862492,-0.684590160279556,-0.682979424836922,-0.680331081846468,
-0.670802852433895,-0.65463063542025,-0.623732438967976,-0.589139203738715,
-0.586852593937324,-0.585781106660395,-0.584963645398563,-0.584065746903173,
-0.582584728297276,-0.577260750486654,-0.568033153939062,-0.545093120873518,
-0.495637588274032,-0.489380288351041,-0.487037363823574,-0.485648373281111,
-0.484187079863851,-0.482271858869356,-0.478164135434446,-0.440742043267341,
-0.401882958403301,-0.38902711823129,-0.386987443148679,-0.385955469221269,
-0.385167502629641,-0.384263583410721,-0.383303794109438,-0.381851407165306,
-0.379180597538454,-0.354647661989461,-0.322872841020084,-0.292366122780154,
-0.288521935163989,-0.286657595045587,-0.2852030665876,-0.283595320016953,
-0.280960410859299,-0.271570321804609,-0.255722155692761,-0.225827442850909,
-0.213778914816316,-0.189793851315745,-0.187453506656475,-0.186388247083305,
-0.185588426080104,-0.184710696221019,-0.183309708626243,-0.181624394564604,
-0.178335755906451,-0.170007143365875,-0.13587047045507,-0.0927143190723946,
-0.0888514489127676,-0.0869834940039257,-0.0855285859264952,-0.083922900606705,
-0.0812970083287391,-0.0719975956823138,-0.0563602581642413,-0.000592940430143267),
 .UNSPECIFIED.);
#819=B_SPLINE_CURVE_WITH_KNOTS('',3,(#24294,#24295,#24296,#24297,#24298,
#24299,#24300,#24301,#24302,#24303,#24304,#24305,#24306,#24307,#24308,#24309,
#24310,#24311,#24312,#24313,#24314,#24315,#24316,#24317,#24318,#24319,#24320,
#24321,#24322,#24323,#24324,#24325,#24326,#24327,#24328,#24329,#24330,#24331,
#24332,#24333,#24334,#24335,#24336,#24337,#24338,#24339,#24340,#24341,#24342,
#24343,#24344,#24345,#24346,#24347,#24348,#24349,#24350,#24351,#24352,#24353,
#24354,#24355,#24356,#24357,#24358,#24359,#24360,#24361,#24362,#24363,#24364,
#24365,#24366,#24367,#24368,#24369,#24370,#24371,#24372,#24373,#24374,#24375,
#24376,#24377,#24378,#24379,#24380,#24381,#24382,#24383,#24384,#24385,#24386,
#24387,#24388,#24389,#24390,#24391,#24392,#24393,#24394,#24395,#24396,#24397,
#24398,#24399,#24400,#24401,#24402,#24403,#24404,#24405,#24406,#24407,#24408,
#24409,#24410,#24411,#24412,#24413,#24414,#24415,#24416,#24417,#24418,#24419,
#24420,#24421,#24422,#24423,#24424,#24425,#24426,#24427,#24428,#24429,#24430,
#24431,#24432,#24433,#24434,#24435,#24436,#24437,#24438,#24439,#24440,#24441,
#24442,#24443,#24444,#24445,#24446,#24447,#24448,#24449,#24450,#24451,#24452,
#24453,#24454,#24455,#24456,#24457,#24458,#24459,#24460,#24461,#24462,#24463,
#24464,#24465,#24466,#24467,#24468,#24469,#24470,#24471,#24472,#24473,#24474,
#24475,#24476,#24477,#24478,#24479,#24480,#24481,#24482,#24483),
 .UNSPECIFIED.,.F.,.F.,(4,3,3,3,3,3,3,3,3,3,3,3,3,3,3,3,3,3,3,3,3,3,3,3,
3,3,3,3,3,3,3,3,3,3,3,3,3,3,3,3,3,3,3,3,3,3,3,3,3,3,3,3,3,3,3,3,3,3,3,3,
3,3,3,4),(109.955742875643,110.100021482593,110.17360629996,110.278552114824,
110.383340179823,110.488004710464,110.592603218256,110.697171287668,110.801744459001,
110.906428414068,111.011173477469,111.116101323929,111.17228716832,111.277232983184,
111.382021048183,111.486685578824,111.591284086616,111.695852156028,111.80042532736,
111.905109282428,112.009854345828,112.114782192288,112.170968036681,112.275913851545,
112.380701916544,112.485366447186,112.589964954977,112.694533024389,112.799106195722,
112.90379015079,113.00853521419,113.113463060651,113.169648905042,113.274594719906,
113.379382784905,113.484047315546,113.588645823338,113.69321389275,113.797787064082,
113.90247101915,114.00721608255,114.112143929011,114.168329773403,114.273275588267,
114.378063653266,114.482728183907,114.587326691699,114.691894761111,114.796467932443,
114.90115188751,115.005896950911,115.110824797371,115.167010641763,115.271956456627,
115.376744521626,115.481409052267,115.586007560059,115.69057562947,115.795148800803,
115.89983275587,116.004577819271,116.109505665731,116.165691510124,116.238928182823),
 .UNSPECIFIED.);
#820=B_SPLINE_CURVE_WITH_KNOTS('',3,(#24485,#24486,#24487,#24488,#24489,
#24490,#24491,#24492,#24493,#24494,#24495,#24496,#24497,#24498,#24499,#24500,
#24501,#24502,#24503,#24504,#24505,#24506,#24507,#24508,#24509,#24510,#24511,
#24512,#24513,#24514,#24515,#24516,#24517,#24518,#24519,#24520,#24521,#24522,
#24523,#24524,#24525,#24526,#24527,#24528,#24529,#24530,#24531,#24532,#24533,
#24534,#24535,#24536,#24537,#24538,#24539,#24540,#24541,#24542,#24543,#24544,
#24545,#24546,#24547,#24548,#24549,#24550,#24551,#24552,#24553,#24554,#24555,
#24556,#24557,#24558,#24559,#24560,#24561,#24562,#24563,#24564,#24565,#24566,
#24567,#24568,#24569,#24570,#24571,#24572,#24573,#24574,#24575,#24576,#24577,
#24578,#24579,#24580,#24581,#24582,#24583,#24584,#24585,#24586,#24587,#24588,
#24589,#24590,#24591,#24592,#24593,#24594,#24595,#24596,#24597,#24598,#24599,
#24600,#24601,#24602,#24603,#24604,#24605,#24606,#24607,#24608,#24609,#24610,
#24611,#24612,#24613,#24614,#24615,#24616,#24617,#24618,#24619,#24620,#24621,
#24622,#24623,#24624,#24625,#24626,#24627,#24628,#24629,#24630,#24631,#24632,
#24633,#24634,#24635,#24636,#24637,#24638,#24639,#24640,#24641,#24642,#24643,
#24644,#24645,#24646,#24647,#24648,#24649,#24650,#24651,#24652,#24653,#24654,
#24655,#24656,#24657,#24658,#24659,#24660,#24661,#24662,#24663,#24664,#24665,
#24666,#24667,#24668,#24669,#24670,#24671,#24672,#24673,#24674,#24675,#24676,
#24677,#24678,#24679,#24680,#24681,#24682,#24683,#24684,#24685,#24686,#24687,
#24688,#24689,#24690,#24691,#24692,#24693,#24694,#24695,#24696,#24697,#24698,
#24699,#24700,#24701,#24702,#24703,#24704,#24705,#24706,#24707,#24708,#24709,
#24710,#24711,#24712,#24713,#24714,#24715,#24716,#24717,#24718,#24719,#24720,
#24721,#24722,#24723,#24724,#24725,#24726,#24727,#24728,#24729,#24730,#24731,
#24732,#24733,#24734,#24735,#24736,#24737,#24738,#24739,#24740,#24741,#24742,
#24743,#24744,#24745,#24746,#24747,#24748,#24749,#24750,#24751,#24752,#24753,
#24754,#24755,#24756,#24757,#24758,#24759,#24760,#24761,#24762,#24763,#24764,
#24765,#24766,#24767,#24768,#24769,#24770,#24771,#24772,#24773,#24774,#24775,
#24776,#24777,#24778,#24779,#24780,#24781,#24782,#24783,#24784,#24785,#24786,
#24787,#24788,#24789,#24790,#24791,#24792,#24793,#24794,#24795,#24796,#24797,
#24798,#24799,#24800,#24801,#24802,#24803,#24804,#24805,#24806,#24807,#24808,
#24809,#24810,#24811,#24812,#24813,#24814,#24815,#24816,#24817,#24818,#24819,
#24820,#24821,#24822,#24823,#24824,#24825,#24826,#24827,#24828,#24829,#24830,
#24831,#24832,#24833,#24834,#24835,#24836,#24837,#24838,#24839,#24840,#24841,
#24842,#24843,#24844,#24845,#24846,#24847,#24848,#24849,#24850,#24851,#24852,
#24853,#24854,#24855,#24856,#24857,#24858,#24859,#24860,#24861,#24862,#24863,
#24864,#24865,#24866,#24867,#24868,#24869,#24870,#24871,#24872,#24873,#24874,
#24875,#24876,#24877,#24878,#24879,#24880,#24881,#24882,#24883,#24884,#24885,
#24886,#24887,#24888,#24889,#24890,#24891,#24892,#24893,#24894,#24895,#24896,
#24897,#24898,#24899,#24900,#24901,#24902,#24903,#24904,#24905,#24906,#24907,
#24908,#24909,#24910,#24911,#24912,#24913,#24914,#24915,#24916,#24917,#24918,
#24919,#24920,#24921,#24922,#24923,#24924,#24925,#24926,#24927,#24928,#24929,
#24930,#24931,#24932,#24933,#24934,#24935,#24936,#24937,#24938,#24939,#24940,
#24941,#24942,#24943,#24944),.UNSPECIFIED.,.F.,.F.,(4,2,2,2,2,2,2,2,2,2,
2,2,2,2,2,2,2,2,2,2,2,2,2,2,2,2,2,2,2,2,2,2,2,2,2,2,2,2,2,2,2,2,2,2,2,2,
2,2,2,2,2,2,2,2,2,2,2,2,2,2,2,2,2,2,2,2,2,2,2,2,2,2,2,2,2,2,2,2,2,2,2,2,
2,2,2,2,2,2,2,2,2,2,2,2,2,2,2,2,2,2,2,2,2,2,2,2,2,2,2,2,2,2,2,2,2,2,2,2,
2,2,2,2,2,2,2,2,2,2,2,2,2,2,2,2,2,2,2,2,2,2,2,2,2,2,2,2,2,2,2,2,2,2,2,2,
2,2,2,2,2,2,2,2,2,2,2,2,2,2,2,2,2,2,2,2,2,2,2,2,2,2,2,2,2,2,2,2,2,2,2,2,
2,2,2,2,2,2,2,2,2,2,2,2,2,2,2,2,2,2,2,2,2,2,2,2,2,2,2,2,2,2,2,2,2,2,2,2,
2,2,2,4),(-2.51385589383474,-2.4728953440402,-2.46356778281143,-2.46111336745769,
-2.45945262149794,-2.45784219742815,-2.45638892076038,-2.45453127252685,
-2.45071897222209,-2.40504719134649,-2.38668747924314,-2.36264631260151,
-2.35959871399723,-2.35866578942519,-2.3577670380385,-2.3569502149354,-2.3558814657657,
-2.35352118364814,-2.32459373769145,-2.29654575680122,-2.27463584481604,
-2.26689192179572,-2.26146401312443,-2.25981092590806,-2.25820581745774,
-2.25675124292062,-2.25488345237392,-2.25101997570405,-2.21924373342984,
-2.17928482583811,-2.1671699136665,-2.16073726948799,-2.15915968220089,
-2.15823322510564,-2.15742249621327,-2.15638482491187,-2.1542465136086,
-2.1395065492948,-2.08577624589031,-2.07140004749863,-2.06268103618726,
-2.06019187668445,-2.05857393964201,-2.05712216952763,-2.0552777984127,
-2.05236169027266,-2.04772232155495,-1.99953853325816,-1.97570526743478,
-1.96626767744714,-1.96085778159424,-1.95936870277049,-1.95846917893778,
-1.95765254775973,-1.95658524340341,-1.95478663059995,-1.9434099790743,
-1.91799120439229,-1.88772694968919,-1.87231927551921,-1.86311865031507,
-1.86050296187752,-1.85889977370593,-1.85744467721869,-1.8555730516855,
-1.85169021162132,-1.81850809897601,-1.76677185779097,-1.76122507661614,
-1.75972280899328,-1.75882025373135,-1.75800433728985,-1.75694257068182,
-1.75516316811648,-1.74418804933658,-1.72136985290494,-1.6900611230536,
-1.67332130951317,-1.66355328482702,-1.66088229386068,-1.65926664241411,
-1.65781403399879,-1.65596464115179,-1.65219528178667,-1.60502639272108,
-1.57768490415826,-1.5673668522046,-1.56160077034645,-1.56007818673895,
-1.55917105812497,-1.55835628651143,-1.55730295681437,-1.55502614719526,
-1.51836052359748,-1.48818810323082,-1.47290003241031,-1.46375083867949,
-1.46113996585804,-1.45953764543231,-1.45808196835307,-1.45620767716562,
-1.45231234645534,-1.41813850482374,-1.36961995146683,-1.36214511310618,
-1.360487451742,-1.35955029536359,-1.35874070175038,-1.35771806198026,-1.35572203363081,
-1.34386172073376,-1.32341833564824,-1.30132878670211,-1.26646888227994,
-1.26243306022236,-1.26053145396173,-1.2590719992533,-1.2574828237227,-1.25493158618636,
-1.24635937654294,-1.2323723237916,-1.17374781362434,-1.16292588504123,
-1.16115357533532,-1.16009370333893,-1.15927782947073,-1.1583737770197,
-1.15686569843996,-1.15126049009605,-1.09956352502326,-1.06641374910587,
-1.06253008648706,-1.06065785035423,-1.05920218307705,-1.05759826871704,
-1.05498117624992,-1.04577343891089,-1.0303494043819,-1.00003819826751,
-0.974444529098934,-0.963217064323069,-0.961425058549284,-0.960359461856212,
-0.959542812311369,-0.958641829059151,-0.957147280329022,-0.951684571195959,
-0.904750996535913,-0.866727930669484,-0.862816770061061,-0.860939234965246,
-0.859482975563456,-0.857881966587124,-0.855277621240369,-0.846195514747425,
-0.83105989349639,-0.800981321099322,-0.763922464213916,-0.761650962621176,
-0.760598526628658,-0.759783763875141,-0.758875889670408,-0.757350407703591,
-0.751554097394565,-0.74116190298647,-0.713611560223404,-0.666802986407777,
-0.663023968231003,-0.661172465233725,-0.65971940029886,-0.658104479717108,
-0.655437565964306,-0.645716002822019,-0.629085730864907,-0.59783019688253,
-0.576207046348278,-0.575397576877177,-0.563810623372752,-0.56182706548919,
-0.560807109344381,-0.559997719658555,-0.559058610687896,-0.557392093929252,
-0.54978748685632,-0.500782696499861,-0.467264820523939,-0.463377021456817,
-0.461504146732965,-0.460048586572978,-0.458445400808202,-0.455830875924833,
-0.446813068080903,-0.431760931719797,-0.374633846899037,-0.363951823021318,
-0.36218656076733,-0.361128799619181,-0.360313275574986,-0.359408221056493,
-0.357925848431869,-0.352588311743646,-0.301104387464563,-0.267469121873336,
-0.263579616080021,-0.26170632064315,-0.260250612210734,-0.258647443819501,
-0.25603335505551,-0.247877716442591,-0.23441891968878,-0.192651306027249,
-0.164825144212551,-0.162463942226863,-0.161394754082083,-0.160577589612655,
-0.159678448732992,-0.158745138479979,-0.155696271316655,-0.13363858630103,
-0.116108180047193,-0.0714612329704776,-0.0674035483814212,-0.0637812269603037,
-0.061936393232011,-0.0604840607567945,-0.0588652913045161,-0.0561811721654837,
-0.0530004676672074,-0.0467122517117062,-0.000592615563380933),
 .UNSPECIFIED.);
#821=B_SPLINE_CURVE_WITH_KNOTS('',3,(#24946,#24947,#24948,#24949,#24950,
#24951,#24952,#24953,#24954,#24955,#24956,#24957,#24958,#24959,#24960,#24961,
#24962,#24963,#24964,#24965,#24966,#24967,#24968,#24969,#24970,#24971,#24972,
#24973,#24974,#24975,#24976,#24977,#24978,#24979,#24980,#24981,#24982,#24983,
#24984,#24985,#24986,#24987,#24988,#24989,#24990,#24991,#24992,#24993,#24994,
#24995,#24996,#24997,#24998,#24999,#25000,#25001,#25002,#25003,#25004,#25005,
#25006,#25007,#25008,#25009,#25010,#25011,#25012,#25013,#25014,#25015,#25016,
#25017,#25018,#25019,#25020,#25021,#25022,#25023,#25024,#25025,#25026,#25027,
#25028,#25029,#25030,#25031,#25032,#25033,#25034,#25035,#25036,#25037,#25038,
#25039,#25040,#25041,#25042,#25043,#25044,#25045,#25046,#25047,#25048,#25049,
#25050,#25051,#25052,#25053,#25054,#25055,#25056,#25057,#25058,#25059,#25060,
#25061,#25062,#25063,#25064,#25065,#25066,#25067,#25068,#25069,#25070,#25071,
#25072,#25073,#25074,#25075,#25076,#25077,#25078,#25079,#25080,#25081,#25082,
#25083,#25084,#25085,#25086,#25087,#25088,#25089,#25090,#25091,#25092,#25093,
#25094,#25095,#25096,#25097,#25098,#25099,#25100,#25101,#25102,#25103,#25104,
#25105,#25106,#25107,#25108,#25109,#25110,#25111,#25112,#25113,#25114,#25115,
#25116,#25117,#25118,#25119,#25120,#25121,#25122,#25123,#25124,#25125,#25126,
#25127,#25128,#25129,#25130,#25131,#25132,#25133,#25134,#25135,#25136,#25137,
#25138,#25139,#25140,#25141,#25142,#25143,#25144,#25145,#25146,#25147,#25148,
#25149,#25150,#25151,#25152,#25153,#25154,#25155,#25156,#25157,#25158,#25159,
#25160,#25161,#25162,#25163,#25164,#25165,#25166,#25167,#25168,#25169,#25170,
#25171,#25172,#25173,#25174,#25175,#25176,#25177,#25178,#25179,#25180,#25181,
#25182,#25183,#25184,#25185,#25186,#25187,#25188,#25189,#25190,#25191,#25192,
#25193,#25194,#25195,#25196,#25197,#25198,#25199,#25200,#25201,#25202,#25203,
#25204,#25205,#25206,#25207,#25208,#25209,#25210,#25211,#25212,#25213,#25214,
#25215,#25216,#25217,#25218,#25219,#25220,#25221,#25222,#25223,#25224,#25225,
#25226,#25227,#25228,#25229,#25230,#25231,#25232,#25233,#25234,#25235,#25236,
#25237,#25238,#25239,#25240,#25241,#25242,#25243,#25244,#25245,#25246,#25247,
#25248,#25249,#25250,#25251,#25252,#25253,#25254,#25255,#25256,#25257,#25258,
#25259,#25260,#25261,#25262,#25263,#25264,#25265,#25266,#25267,#25268,#25269,
#25270,#25271,#25272,#25273,#25274,#25275,#25276,#25277,#25278,#25279,#25280,
#25281,#25282,#25283,#25284,#25285,#25286,#25287,#25288,#25289,#25290,#25291,
#25292,#25293,#25294,#25295,#25296,#25297,#25298,#25299,#25300,#25301,#25302,
#25303,#25304,#25305,#25306,#25307,#25308,#25309,#25310,#25311,#25312,#25313,
#25314,#25315,#25316,#25317,#25318,#25319,#25320,#25321,#25322,#25323,#25324,
#25325,#25326,#25327,#25328,#25329,#25330,#25331,#25332,#25333,#25334,#25335,
#25336,#25337,#25338,#25339,#25340,#25341,#25342,#25343,#25344,#25345,#25346,
#25347,#25348,#25349,#25350,#25351,#25352,#25353,#25354,#25355,#25356,#25357,
#25358,#25359,#25360,#25361,#25362,#25363,#25364,#25365,#25366,#25367,#25368,
#25369,#25370,#25371,#25372,#25373,#25374,#25375,#25376,#25377,#25378,#25379,
#25380,#25381,#25382,#25383,#25384,#25385,#25386,#25387,#25388,#25389,#25390,
#25391,#25392,#25393,#25394,#25395,#25396,#25397,#25398,#25399,#25400,#25401,
#25402,#25403,#25404,#25405,#25406,#25407,#25408,#25409,#25410,#25411,#25412,
#25413,#25414,#25415,#25416,#25417,#25418,#25419,#25420,#25421,#25422,#25423,
#25424,#25425,#25426,#25427,#25428,#25429,#25430,#25431,#25432,#25433,#25434,
#25435,#25436,#25437,#25438,#25439,#25440,#25441,#25442,#25443,#25444,#25445,
#25446,#25447,#25448,#25449),.UNSPECIFIED.,.F.,.F.,(4,2,2,2,2,2,2,2,2,2,
2,2,2,2,2,2,2,2,2,2,2,2,2,2,2,2,2,2,2,2,2,2,2,2,2,2,2,2,2,2,2,2,2,2,2,2,
2,2,2,2,2,2,2,2,2,2,2,2,2,2,2,2,2,2,2,2,2,2,2,2,2,2,2,2,2,2,2,2,2,2,2,2,
2,2,2,2,2,2,2,2,2,2,2,2,2,2,2,2,2,2,2,2,2,2,2,2,2,2,2,2,2,2,2,2,2,2,2,2,
2,2,2,2,2,2,2,2,2,2,2,2,2,2,2,2,2,2,2,2,2,2,2,2,2,2,2,2,2,2,2,2,2,2,2,2,
2,2,2,2,2,2,2,2,2,2,2,2,2,2,2,2,2,2,2,2,2,2,2,2,2,2,2,2,2,2,2,2,2,2,2,2,
2,2,2,2,2,2,2,2,2,2,2,2,2,2,2,2,2,2,2,2,2,2,2,2,2,2,2,2,2,2,2,2,2,2,2,2,
2,2,2,2,2,2,2,2,2,2,2,2,2,2,2,2,2,2,2,2,2,2,2,2,2,4),(-2.51289715151977,
-2.47972640089436,-2.4768752173438,-2.47545123771563,-2.47450337870612,
-2.47359423931493,-2.4727802537463,-2.47173133266218,-2.46999518265789,
-2.45987087398384,-2.43689502740499,-2.42524062078833,-2.41514200848716,
-2.38743176820728,-2.37826035077444,-2.37562763474891,-2.37402071742516,
-2.37256660773301,-2.370702343459,-2.36685666586062,-2.32290528012821,-2.29115758319708,
-2.2817425175326,-2.27636157504926,-2.27487764146156,-2.27397247433261,
-2.27315741957376,-2.27210102859931,-2.27033967033494,-2.259725047596,-2.24629664299976,
-2.2005665046346,-2.18686447011953,-2.17857500778693,-2.17596069937408,
-2.17435786716931,-2.17290277256296,-2.17103069948715,-2.16714530157488,
-2.13374945859055,-2.08201329160179,-2.07667048902124,-2.07519211461073,
-2.07428815772761,-2.07347267626837,-2.07241372771533,-2.07010664154477,
-2.0350864889324,-2.00549111007562,-1.98876800224782,-1.97900711171298,
-1.97633688797576,-1.97472146276348,-1.97326890526985,-1.97141936813974,
-1.96764898339249,-1.92052813144785,-1.89315895174763,-1.88283174289908,
-1.87706212037299,-1.87553927054924,-1.87463211338769,-1.87381740569389,
-1.87276427629076,-1.87048834849328,-1.83356479458625,-1.803483209101,-1.78063170329132,
-1.77722809410557,-1.77545331755989,-1.77414629985647,-1.7727319081527,
-1.77025958348092,-1.76411053959124,-1.71785832347955,-1.67958101061963,
-1.67664572735292,-1.67546506617423,-1.67463205509275,-1.67387100196087,
-1.6728300235922,-1.6707639031627,-1.63497248436216,-1.60450792182737,-1.58885237755332,
-1.57954411197088,-1.57691735353388,-1.57531147709936,-1.57385661652084,
-1.57198903045255,-1.56812803289837,-1.52486435117493,-1.49502140709829,
-1.4838389281787,-1.477735840258,-1.47618352669626,-1.47526973319552,-1.47445644884759,
-1.47341475113685,-1.47170360939251,-1.46205251553749,-1.45888924903372,
-1.40401450461822,-1.38885922138649,-1.37976796394562,-1.37716298134187,
-1.3755620018936,-1.37410604651243,-1.37222929335983,-1.3683211868747,-1.33201926574934,
-1.29816507435623,-1.28497179813062,-1.27812818553261,-1.27651628052509,
-1.2755892835107,-1.2747784578422,-1.27374115624603,-1.27160529590393,-1.25694088016128,
-1.23050686048361,-1.18600387191342,-1.18209736062994,-1.17833424367952,
-1.17648607169198,-1.17503357716437,-1.17341717887167,-1.17074292618847,
-1.16094066541488,-1.14411634756192,-1.11271303806091,-1.08943276810935,
-1.07903834866974,-1.07728790477791,-1.07623463406456,-1.07541989458437,
-1.07451277982174,-1.07299018083451,-1.06722351048025,-1.05690526936063,
-1.02956790520883,-0.982441725275819,-0.978672216904429,-0.976822830780169,
-0.975370263585332,-0.973754695043602,-0.971083927791218,-0.961317750343273,
-0.944579525204524,-0.913243976293078,-0.890366723660837,-0.879427532941609,
-0.877649906380281,-0.876588675830873,-0.875772854335678,-0.874870052571093,
-0.873366628446128,-0.867807256263376,-0.816106831082813,-0.782940911764785,
-0.779058324616186,-0.777186712484757,-0.775731577407039,-0.774128297051813,
-0.771512346654275,-0.762309723954097,-0.746895326883556,-0.716598503404048,
-0.690990207577226,-0.679780807210232,-0.677990136832804,-0.676925131933392,
-0.676108814817793,-0.67520806739347,-0.673713630647349,-0.668248308879818,
-0.621237503132578,-0.583327360996343,-0.579418492049704,-0.577541818563347,
-0.576086121810634,-0.574485624990618,-0.571881873711318,-0.562799443690345,
-0.54766097574086,-0.517586744244526,-0.480561134962328,-0.478290693298444,
-0.477238689433416,-0.476424235318645,-0.47551667661698,-0.473991662449225,
-0.468196401982876,-0.457805276146846,-0.430247531516478,-0.383481798468726,
-0.379701893144844,-0.377850623335885,-0.376398046389941,-0.37492107837684,
-0.372466840650849,-0.369569347572885,-0.364041484016353,-0.350541511930078,
-0.294915708414671,-0.292086570921313,-0.280457542112901,-0.278472121437683,
-0.277451899961462,-0.276642658933393,-0.275704131002375,-0.274039656527685,
-0.266461282860458,-0.217573750587891,-0.183930882811766,-0.180043669558134,
-0.17817116608226,-0.176715934090724,-0.176698684454885,-0.176682067532365,
-0.1766660547917,-0.176650619204641,-0.176635735227564,-0.176621378708022,
-0.176607526789569,-0.176594157831531,-0.176581251341022,-0.176568787887566,
-0.176556749046612,-0.176545117334244,-0.176533876138712,-0.176523009688158,
-0.176512502997364,-0.176502341813206,-0.176492512568804,-0.176483002346398,
-0.176473798843879,-0.176464890344472,-0.174808911736105,-0.171925382564298,
-0.168396814929211,-0.161141469404808,-0.141239909810671,-0.0830116117044468,
-0.0794416450292309,-0.0781226243214013,-0.0773465217319725,-0.0765241265629663,
-0.075403103231885,-0.072821025816527,-0.0410478306117794,-0.000592895662585235),
 .UNSPECIFIED.);
#822=B_SPLINE_CURVE_WITH_KNOTS('',3,(#25451,#25452,#25453,#25454,#25455,
#25456,#25457,#25458,#25459,#25460,#25461,#25462,#25463,#25464,#25465,#25466,
#25467,#25468,#25469,#25470,#25471,#25472,#25473,#25474,#25475,#25476,#25477,
#25478,#25479,#25480,#25481,#25482,#25483,#25484,#25485,#25486,#25487,#25488,
#25489,#25490,#25491,#25492,#25493,#25494,#25495,#25496,#25497,#25498,#25499,
#25500,#25501,#25502,#25503,#25504,#25505,#25506,#25507,#25508,#25509,#25510,
#25511,#25512,#25513,#25514,#25515,#25516,#25517,#25518,#25519,#25520,#25521,
#25522,#25523,#25524,#25525,#25526,#25527,#25528,#25529,#25530,#25531,#25532,
#25533,#25534,#25535,#25536,#25537,#25538,#25539,#25540,#25541,#25542,#25543,
#25544,#25545,#25546,#25547,#25548,#25549,#25550,#25551,#25552,#25553,#25554,
#25555,#25556,#25557,#25558,#25559,#25560,#25561,#25562,#25563,#25564,#25565,
#25566,#25567,#25568,#25569,#25570,#25571,#25572,#25573,#25574,#25575,#25576,
#25577,#25578,#25579,#25580,#25581,#25582,#25583,#25584,#25585,#25586,#25587,
#25588,#25589,#25590,#25591,#25592,#25593,#25594,#25595,#25596,#25597,#25598,
#25599,#25600,#25601,#25602,#25603,#25604,#25605,#25606,#25607,#25608,#25609,
#25610,#25611,#25612,#25613,#25614,#25615,#25616,#25617,#25618,#25619,#25620,
#25621,#25622,#25623,#25624,#25625,#25626,#25627,#25628,#25629,#25630,#25631,
#25632,#25633,#25634,#25635,#25636,#25637,#25638,#25639,#25640),
 .UNSPECIFIED.,.F.,.F.,(4,3,3,3,3,3,3,3,3,3,3,3,3,3,3,3,3,3,3,3,3,3,3,3,
3,3,3,3,3,3,3,3,3,3,3,3,3,3,3,3,3,3,3,3,3,3,3,3,3,3,3,3,3,3,3,3,3,3,3,3,
3,3,3,4),(78.5398163397452,78.6441703164354,78.7485007550361,78.852843436871,
78.9573058341078,79.0618360039011,79.1665532872366,79.2144993807763,79.3194451956405,
79.4242332606396,79.5288977912809,79.6334962990726,79.7380643684846,79.8426375398172,
79.9473214948844,80.0520665582851,80.1569944047453,80.213180249137,80.3181260640012,
80.422914129,80.5275786596412,80.6321771674329,80.7367452368449,80.8413184081774,
80.9460023632446,81.0507474266453,81.1556752731056,81.2118611174978,81.3168069323619,
81.4215949973606,81.5262595280019,81.6308580357935,81.7354261052054,81.8399992765384,
81.9446832316056,82.0494282950062,82.1543561414665,82.2105419858585,82.3154878007227,
82.4202758657216,82.5249403963629,82.6295389041546,82.7341069735665,82.8386801448994,
82.9433640999666,83.0481091633673,83.1530370098276,83.2092228542193,83.3141686690836,
83.4189567340828,83.5236212647241,83.6282197725159,83.7327878419278,83.8373610132607,
83.9420449683279,84.0467900317286,84.1517178781889,84.20790372258,84.3139463242525,
84.4198215071954,84.5255441086588,84.6311761129126,84.736764788714,84.8230016469248),
 .UNSPECIFIED.);
#823=B_SPLINE_CURVE_WITH_KNOTS('',3,(#25642,#25643,#25644,#25645,#25646,
#25647,#25648,#25649,#25650,#25651,#25652,#25653,#25654,#25655,#25656,#25657,
#25658,#25659,#25660,#25661,#25662,#25663,#25664,#25665,#25666,#25667,#25668,
#25669,#25670,#25671,#25672,#25673,#25674,#25675,#25676,#25677,#25678,#25679,
#25680,#25681,#25682,#25683,#25684,#25685,#25686,#25687,#25688,#25689,#25690,
#25691,#25692,#25693,#25694,#25695,#25696,#25697,#25698,#25699,#25700,#25701,
#25702,#25703,#25704,#25705,#25706,#25707,#25708,#25709,#25710,#25711,#25712,
#25713,#25714,#25715,#25716,#25717,#25718,#25719,#25720,#25721,#25722,#25723,
#25724,#25725,#25726,#25727,#25728,#25729,#25730,#25731,#25732,#25733,#25734,
#25735,#25736,#25737,#25738,#25739,#25740,#25741,#25742,#25743,#25744,#25745,
#25746,#25747,#25748,#25749,#25750,#25751,#25752,#25753,#25754,#25755,#25756,
#25757,#25758,#25759,#25760,#25761,#25762,#25763,#25764,#25765,#25766,#25767,
#25768,#25769,#25770,#25771,#25772,#25773,#25774,#25775,#25776,#25777,#25778,
#25779,#25780,#25781,#25782,#25783,#25784,#25785,#25786,#25787,#25788,#25789,
#25790,#25791,#25792,#25793,#25794,#25795,#25796,#25797,#25798,#25799,#25800,
#25801,#25802,#25803,#25804,#25805,#25806,#25807,#25808,#25809,#25810,#25811,
#25812,#25813,#25814,#25815,#25816,#25817,#25818,#25819,#25820,#25821,#25822,
#25823,#25824,#25825,#25826,#25827,#25828,#25829,#25830,#25831),
 .UNSPECIFIED.,.F.,.F.,(4,3,3,3,3,3,3,3,3,3,3,3,3,3,3,3,3,3,3,3,3,3,3,3,
3,3,3,3,3,3,3,3,3,3,3,3,3,3,3,3,3,3,3,3,3,3,3,3,3,3,3,3,3,3,3,3,3,3,3,3,
3,3,3,4),(72.2566313277358,72.361007636202,72.4686834530033,72.5727829330681,
72.6768214388177,72.7808353386096,72.8848609619492,72.9890000281572,73.0932076440146,
73.1975874607193,73.2224141706118,73.3273599854761,73.4321480504749,73.5368125811162,
73.6414110889079,73.74597915832,73.8505523296524,73.9552362847196,74.0599813481202,
74.1649091945805,74.2210950389725,74.3260408538366,74.4308289188352,74.5354934494765,
74.6400919572682,74.7446600266802,74.8492331980132,74.9539171530804,75.058662216481,
75.1635900629414,75.2197759073333,75.3247217221975,75.4295097871962,75.5341743178374,
75.6387728256293,75.7433408950412,75.8479140663737,75.9525980214409,76.0573430848416,
76.1622709313019,76.218456775694,76.3234025905581,76.4281906555569,76.5328551861981,
76.6374536939898,76.7420217634016,76.8465949347344,76.9512788898016,77.0560239532023,
77.1609517996625,77.2171376440548,77.322083458919,77.4268715239178,77.5315360545591,
77.6361345623507,77.7407026317626,77.8452758030951,77.9499597581623,78.0547048215629,
78.1596326680231,78.2158185124155,78.3402426631434,78.4633027052255,78.5398163393914),
 .UNSPECIFIED.);
#824=B_SPLINE_CURVE_WITH_KNOTS('',3,(#25833,#25834,#25835,#25836,#25837,
#25838,#25839,#25840,#25841,#25842,#25843),.UNSPECIFIED.,.F.,.F.,(4,1,1,
1,1,1,1,1,4),(65.9734480974445,66.2316480920865,67.2303289604472,68.229009828808,
69.2276906971688,70.2263715655295,71.2250524338903,72.223733302251,72.2566310325656),
 .UNSPECIFIED.);
#825=B_SPLINE_CURVE_WITH_KNOTS('',3,(#25845,#25846,#25847,#25848,#25849,
#25850,#25851,#25852,#25853,#25854,#25855,#25856,#25857,#25858,#25859,#25860,
#25861,#25862,#25863,#25864,#25865,#25866,#25867,#25868,#25869,#25870,#25871,
#25872,#25873,#25874,#25875,#25876,#25877,#25878,#25879,#25880,#25881,#25882,
#25883,#25884,#25885,#25886,#25887,#25888,#25889,#25890,#25891,#25892,#25893,
#25894,#25895,#25896,#25897,#25898,#25899,#25900,#25901,#25902,#25903,#25904,
#25905,#25906,#25907,#25908,#25909,#25910,#25911,#25912,#25913,#25914,#25915,
#25916,#25917,#25918,#25919,#25920,#25921,#25922,#25923,#25924,#25925,#25926,
#25927,#25928,#25929,#25930,#25931,#25932,#25933,#25934,#25935,#25936,#25937,
#25938,#25939,#25940,#25941,#25942,#25943,#25944,#25945,#25946,#25947,#25948,
#25949,#25950,#25951,#25952,#25953,#25954,#25955,#25956,#25957,#25958,#25959,
#25960,#25961,#25962,#25963,#25964,#25965,#25966,#25967,#25968,#25969,#25970,
#25971,#25972,#25973,#25974,#25975,#25976,#25977,#25978,#25979,#25980,#25981,
#25982,#25983,#25984,#25985,#25986,#25987,#25988,#25989,#25990,#25991,#25992,
#25993,#25994,#25995,#25996,#25997,#25998,#25999,#26000,#26001,#26002,#26003,
#26004,#26005,#26006,#26007,#26008,#26009,#26010,#26011,#26012,#26013,#26014,
#26015,#26016,#26017,#26018,#26019,#26020,#26021,#26022,#26023,#26024,#26025,
#26026,#26027,#26028,#26029,#26030,#26031,#26032,#26033,#26034,#26035,#26036,
#26037,#26038,#26039,#26040,#26041,#26042,#26043,#26044,#26045,#26046,#26047,
#26048,#26049,#26050,#26051,#26052,#26053,#26054,#26055,#26056,#26057,#26058,
#26059,#26060,#26061,#26062,#26063,#26064,#26065,#26066,#26067,#26068,#26069,
#26070,#26071,#26072,#26073,#26074,#26075,#26076,#26077,#26078,#26079,#26080,
#26081,#26082,#26083,#26084,#26085,#26086,#26087,#26088,#26089,#26090,#26091,
#26092,#26093,#26094,#26095,#26096,#26097,#26098,#26099,#26100,#26101,#26102,
#26103,#26104,#26105,#26106,#26107,#26108,#26109,#26110,#26111,#26112,#26113,
#26114,#26115,#26116,#26117,#26118,#26119,#26120,#26121,#26122,#26123,#26124,
#26125,#26126,#26127,#26128,#26129,#26130,#26131,#26132,#26133,#26134,#26135,
#26136,#26137,#26138,#26139,#26140,#26141,#26142,#26143,#26144,#26145,#26146,
#26147,#26148,#26149,#26150,#26151,#26152,#26153,#26154,#26155,#26156,#26157,
#26158,#26159,#26160,#26161,#26162,#26163,#26164,#26165,#26166,#26167,#26168,
#26169,#26170,#26171,#26172,#26173,#26174,#26175,#26176,#26177,#26178,#26179,
#26180,#26181,#26182,#26183,#26184,#26185,#26186,#26187,#26188,#26189,#26190,
#26191,#26192,#26193,#26194,#26195,#26196,#26197,#26198,#26199,#26200,#26201,
#26202,#26203,#26204,#26205,#26206,#26207,#26208,#26209,#26210,#26211,#26212,
#26213,#26214,#26215,#26216,#26217,#26218,#26219,#26220,#26221,#26222,#26223,
#26224,#26225,#26226,#26227,#26228,#26229,#26230,#26231,#26232,#26233,#26234,
#26235,#26236,#26237,#26238,#26239,#26240,#26241,#26242,#26243,#26244,#26245,
#26246,#26247,#26248,#26249,#26250,#26251,#26252,#26253,#26254,#26255,#26256,
#26257,#26258,#26259,#26260,#26261,#26262,#26263,#26264,#26265,#26266,#26267,
#26268,#26269,#26270,#26271,#26272,#26273,#26274,#26275,#26276,#26277,#26278,
#26279,#26280,#26281,#26282,#26283,#26284,#26285,#26286,#26287,#26288,#26289,
#26290,#26291,#26292,#26293,#26294,#26295,#26296,#26297,#26298,#26299,#26300,
#26301,#26302,#26303,#26304,#26305,#26306,#26307,#26308,#26309,#26310,#26311,
#26312,#26313,#26314),.UNSPECIFIED.,.F.,.F.,(4,2,2,2,2,2,2,2,2,2,2,2,2,
2,2,2,2,2,2,2,2,2,2,2,2,2,2,2,2,2,2,2,2,2,2,2,2,2,2,2,2,2,2,2,2,2,2,2,2,
2,2,2,2,2,2,2,2,2,2,2,2,2,2,2,2,2,2,2,2,2,2,2,2,2,2,2,2,2,2,2,2,2,2,2,2,
2,2,2,2,2,2,2,2,2,2,2,2,2,2,2,2,2,2,2,2,2,2,2,2,2,2,2,2,2,2,2,2,2,2,2,2,
2,2,2,2,2,2,2,2,2,2,2,2,2,2,2,2,2,2,2,2,2,2,2,2,2,2,2,2,2,2,2,2,2,2,2,2,
2,2,2,2,2,2,2,2,2,2,2,2,2,2,2,2,2,2,2,2,2,2,2,2,2,2,2,2,2,2,2,2,2,2,2,2,
2,2,2,2,2,2,2,2,2,2,2,2,2,2,2,2,2,2,2,2,2,2,2,2,2,2,2,2,2,2,2,2,2,2,2,2,
2,2,2,2,2,4),(-2.51416891162704,-2.48112270253285,-2.47186008798328,-2.46943928752675,
-2.46779239009978,-2.46619153174604,-2.46473569892957,-2.46285912126152,
-2.45895144398875,-2.4200747924581,-2.3996149906461,-2.37391068630378,-2.36858079106766,
-2.36706981317024,-2.36616532792609,-2.36534996776999,-2.36429196677082,
-2.36207219254794,-2.32414945231398,-2.29061359006509,-2.27200515469304,
-2.26877725039748,-2.26733773690969,-2.26586997598837,-2.26449431452899,
-2.26221985462322,-2.256394743407,-2.21543503076707,-2.17397878663389,-2.16903892556346,
-2.1674653268296,-2.16653967575371,-2.16572866133809,-2.16468932009309,
-2.16254308567906,-2.14759180221069,-2.14209604215475,-2.09393030920172,
-2.07965863482546,-2.07098620890914,-2.06849689389138,-2.06688088309571,
-2.06542837744966,-2.06357969908709,-2.05981383516076,-2.01251557648366,
-1.98525906830234,-1.97496842007012,-1.96921324341968,-1.96769166551787,
-1.96678477093518,-1.96596995787136,-1.96491624380949,-1.96263734014924,
-1.92603178272515,-1.8958405270843,-1.88052852510911,-1.87136896766193,
-1.86875708210059,-1.86715455330332,-1.86569895822228,-1.8638251532161,
-1.85993221462304,-1.82597341276369,-1.77728992516677,-1.76976838612602,
-1.76810753649167,-1.7671696881328,-1.76636018550611,-1.76533854769543,
-1.76334712711815,-1.75160843290355,-1.74898896811829,-1.74125508505489,
-1.72642761673244,-1.6962056936859,-1.68085816534065,-1.67168285245546,
-1.66906916991145,-1.66746611052446,-1.66601040886064,-1.66413699295306,
-1.66024677170934,-1.62633665827277,-1.57760219289598,-1.5700677892355,
-1.56840591323352,-1.56746776586281,-1.5666581789851,-1.56563665861495,
-1.56364613505438,-1.55192789941672,-1.54934855957861,-1.52697197490935,
-1.49665820613985,-1.48119809749935,-1.47197366045526,-1.46935485770892,
-1.46775053282128,-1.46629491033399,-1.46442331601354,-1.46054310021216,
-1.41879944532561,-1.38989265679177,-1.3710613131453,-1.368983545232,-1.3679576737996,
-1.36722444284156,-1.36643134282357,-1.36502693662354,-1.36086526791762,
-1.31984189903675,-1.27488666430804,-1.27067183813501,-1.26873627636904,
-1.26727176775314,-1.26588883628996,-1.26357797155384,-1.25752231947305,
-1.22495740135979,-1.19145095654736,-1.18666365140535,-1.17143598408825,
-1.16927945211793,-1.16823793600518,-1.16742653848506,-1.16650190127689,
-1.16490119778426,-1.15820638732285,-1.14543283256662,-1.13269258449123,
-1.07755754527285,-1.07173958921664,-1.06946598452273,-1.06809028017392,
-1.06662204527329,-1.06466208733977,-1.06031489260978,-1.05452168404084,
-1.04010480592576,-0.978680353774963,-0.975736221608437,-0.973868883035947,
-0.970164949376239,-0.968825262300434,-0.968045034186847,-0.967224737471353,
-0.96611700916113,-0.963609719510077,-0.935553159304165,-0.898137150389062,
-0.890914222607529,-0.873991319715326,-0.870967677952838,-0.869090028091327,
-0.86763352473352,-0.866032091453499,-0.863426705226515,-0.854337454798115,
-0.839186541994366,-0.809092250677893,-0.772054981788037,-0.769783350459396,
-0.768730772434134,-0.767915863734272,-0.767007787432175,-0.765481879268838,
-0.759682938413996,-0.749284896909411,-0.721704884042302,-0.674919046907078,
-0.671138479929674,-0.669286461572267,-0.66783310339603,-0.666217971562694,
-0.663550974227376,-0.653832008059458,-0.637209168153602,-0.605955943969575,
-0.572391827746307,-0.570293766106476,-0.569244586849225,-0.568481256768335,
-0.567649779227091,-0.566478168594516,-0.56359972742884,-0.542478475642401,
-0.477843504409794,-0.472271215811136,-0.47003870833555,-0.468670737969772,
-0.467197544666218,-0.465207876070659,-0.460696951540999,-0.454628024984922,
-0.439232901114029,-0.408972928124254,-0.372503523125898,-0.370448004676696,
-0.369409613902607,-0.368649135420992,-0.367815310540694,-0.36665477269793,
-0.363863429954477,-0.359892400164121,-0.349002675361108,-0.312057429386215,
-0.275580973259992,-0.271672066872095,-0.269794921876307,-0.268338658432807,
-0.266737336061764,-0.26413178674946,-0.255038522276201,-0.239877597092108,
-0.192686910300566,-0.187704220519794,-0.17257470970358,-0.17042161555553,
-0.169380754104277,-0.168569397249749,-0.167807880252338,-0.166413887879585,
-0.161947025489448,-0.154623662908096,-0.131234738674594,-0.0790727568882605,
-0.0729821347089623,-0.0706658145245276,-0.0692818555094672,-0.0678179147098098,
-0.0658858994621991,-0.0616898857032018,-0.0208011237217479,-0.000592836805715096),
 .UNSPECIFIED.);
#826=B_SPLINE_CURVE_WITH_KNOTS('',3,(#26316,#26317,#26318,#26319,#26320,
#26321,#26322,#26323,#26324,#26325,#26326,#26327,#26328,#26329,#26330,#26331,
#26332,#26333,#26334,#26335,#26336,#26337,#26338,#26339,#26340,#26341,#26342,
#26343,#26344,#26345,#26346,#26347,#26348,#26349,#26350,#26351,#26352,#26353,
#26354,#26355,#26356,#26357,#26358,#26359,#26360,#26361,#26362,#26363,#26364,
#26365,#26366,#26367,#26368,#26369,#26370,#26371,#26372,#26373,#26374,#26375,
#26376,#26377,#26378,#26379,#26380,#26381,#26382,#26383,#26384,#26385,#26386,
#26387,#26388,#26389,#26390,#26391,#26392,#26393,#26394,#26395,#26396,#26397,
#26398,#26399,#26400,#26401,#26402,#26403,#26404,#26405,#26406,#26407,#26408,
#26409,#26410,#26411,#26412,#26413,#26414,#26415,#26416,#26417,#26418,#26419,
#26420,#26421,#26422,#26423,#26424,#26425,#26426,#26427,#26428,#26429,#26430,
#26431,#26432,#26433,#26434,#26435,#26436,#26437,#26438,#26439,#26440,#26441,
#26442,#26443,#26444,#26445,#26446,#26447,#26448,#26449,#26450,#26451,#26452,
#26453,#26454,#26455,#26456,#26457,#26458,#26459,#26460,#26461,#26462,#26463,
#26464,#26465,#26466,#26467,#26468,#26469,#26470,#26471,#26472,#26473,#26474,
#26475,#26476,#26477,#26478,#26479,#26480,#26481,#26482,#26483,#26484,#26485,
#26486,#26487,#26488,#26489,#26490,#26491,#26492,#26493,#26494,#26495,#26496,
#26497,#26498,#26499,#26500,#26501,#26502),.UNSPECIFIED.,.F.,.F.,(4,3,3,
3,3,3,3,3,3,3,3,3,3,3,3,3,3,3,3,3,3,3,3,3,3,3,3,3,3,3,3,3,3,3,3,3,3,3,3,
3,3,3,3,3,3,3,3,3,3,3,3,3,3,3,3,3,3,3,3,3,3,3,4),(47.1238898038472,47.2567115932322,
47.3616574080963,47.4664454730952,47.5711100037364,47.6757085115281,47.7802765809401,
47.8848497522726,47.9895337073398,48.0942787707405,48.1992066172007,48.255392461593,
48.3603382764572,48.465126341456,48.5697908720972,48.6743893798889,48.7789574493009,
48.8835306206336,48.9882145757009,49.0929596391015,49.1978874855618,49.2540733299537,
49.3590191448179,49.4638072098166,49.5684717404579,49.6730702482496,49.7776383176615,
49.8822114889942,49.9868954440615,50.0916405074622,50.1965683539224,50.2527541983145,
50.3577000131787,50.4624880781775,50.5671526088188,50.6717511166105,50.7763191860225,
50.8808923573552,50.9855763124224,51.0903213758231,51.1952492222833,51.2514350666752,
51.3563808815394,51.4611689465382,51.5658334771794,51.6704319849711,51.7750000543831,
51.8795732257158,51.984257180783,52.0890022441837,52.193930090644,52.250115935036,
52.3550617499002,52.459849814899,52.5645143455403,52.6691128533319,52.7736809227439,
52.8782540940765,52.9829380491437,53.0876831125444,53.1926109590046,53.2487968033967,
53.4070751110268),.UNSPECIFIED.);
#827=B_SPLINE_CURVE_WITH_KNOTS('',3,(#26504,#26505,#26506,#26507,#26508,
#26509,#26510,#26511,#26512,#26513,#26514,#26515,#26516,#26517,#26518,#26519,
#26520,#26521,#26522,#26523,#26524,#26525,#26526,#26527,#26528,#26529,#26530,
#26531,#26532,#26533,#26534,#26535,#26536,#26537,#26538,#26539,#26540,#26541,
#26542,#26543,#26544,#26545,#26546,#26547,#26548,#26549,#26550,#26551,#26552,
#26553,#26554,#26555,#26556,#26557,#26558,#26559,#26560,#26561,#26562,#26563,
#26564,#26565,#26566,#26567,#26568,#26569,#26570,#26571,#26572,#26573,#26574,
#26575,#26576,#26577,#26578,#26579,#26580,#26581,#26582,#26583,#26584,#26585,
#26586,#26587,#26588,#26589,#26590,#26591,#26592,#26593,#26594,#26595,#26596,
#26597,#26598,#26599,#26600,#26601,#26602,#26603,#26604,#26605,#26606,#26607,
#26608,#26609,#26610,#26611,#26612,#26613,#26614,#26615,#26616,#26617,#26618,
#26619,#26620,#26621,#26622,#26623,#26624,#26625,#26626,#26627,#26628,#26629,
#26630,#26631,#26632,#26633,#26634,#26635,#26636,#26637,#26638,#26639,#26640,
#26641,#26642,#26643,#26644,#26645,#26646,#26647,#26648,#26649,#26650,#26651,
#26652,#26653,#26654,#26655,#26656,#26657,#26658,#26659,#26660,#26661,#26662,
#26663,#26664,#26665,#26666,#26667,#26668,#26669,#26670,#26671,#26672,#26673,
#26674,#26675,#26676,#26677,#26678,#26679,#26680,#26681,#26682,#26683,#26684,
#26685,#26686,#26687,#26688,#26689,#26690,#26691,#26692,#26693,#26694,#26695,
#26696,#26697,#26698,#26699,#26700,#26701,#26702,#26703,#26704,#26705,#26706,
#26707,#26708,#26709,#26710,#26711,#26712,#26713,#26714,#26715,#26716,#26717,
#26718,#26719,#26720,#26721,#26722,#26723,#26724,#26725,#26726,#26727,#26728,
#26729,#26730,#26731,#26732,#26733,#26734,#26735,#26736,#26737,#26738,#26739,
#26740,#26741,#26742,#26743,#26744,#26745,#26746,#26747,#26748,#26749,#26750,
#26751,#26752,#26753,#26754,#26755,#26756,#26757,#26758,#26759,#26760,#26761,
#26762,#26763,#26764,#26765,#26766,#26767,#26768,#26769,#26770,#26771,#26772,
#26773,#26774,#26775,#26776,#26777,#26778,#26779,#26780,#26781,#26782,#26783,
#26784,#26785,#26786,#26787,#26788,#26789,#26790,#26791,#26792,#26793,#26794,
#26795,#26796,#26797,#26798,#26799,#26800,#26801,#26802,#26803,#26804,#26805,
#26806,#26807,#26808,#26809,#26810,#26811,#26812,#26813,#26814,#26815,#26816,
#26817,#26818,#26819,#26820,#26821,#26822,#26823,#26824,#26825,#26826,#26827,
#26828,#26829,#26830,#26831,#26832,#26833,#26834,#26835,#26836,#26837,#26838,
#26839,#26840,#26841,#26842,#26843,#26844,#26845,#26846,#26847,#26848,#26849,
#26850,#26851,#26852,#26853,#26854,#26855,#26856,#26857,#26858,#26859,#26860,
#26861,#26862,#26863,#26864,#26865,#26866,#26867,#26868,#26869,#26870,#26871,
#26872,#26873,#26874,#26875,#26876,#26877,#26878,#26879,#26880,#26881,#26882,
#26883,#26884,#26885,#26886,#26887,#26888,#26889,#26890,#26891,#26892,#26893,
#26894,#26895,#26896,#26897,#26898,#26899,#26900,#26901,#26902,#26903,#26904,
#26905,#26906,#26907,#26908,#26909,#26910,#26911,#26912,#26913,#26914,#26915,
#26916,#26917,#26918,#26919,#26920,#26921,#26922,#26923,#26924,#26925,#26926,
#26927,#26928,#26929,#26930,#26931,#26932,#26933,#26934,#26935,#26936,#26937,
#26938,#26939,#26940,#26941,#26942,#26943,#26944,#26945,#26946,#26947,#26948,
#26949,#26950,#26951,#26952,#26953,#26954,#26955,#26956,#26957,#26958,#26959,
#26960,#26961,#26962,#26963,#26964,#26965,#26966,#26967,#26968,#26969,#26970,
#26971,#26972,#26973),.UNSPECIFIED.,.F.,.F.,(4,2,2,2,2,2,2,2,2,2,2,2,2,
2,2,2,2,2,2,2,2,2,2,2,2,2,2,2,2,2,2,2,2,2,2,2,2,2,2,2,2,2,2,2,2,2,2,2,2,
2,2,2,2,2,2,2,2,2,2,2,2,2,2,2,2,2,2,2,2,2,2,2,2,2,2,2,2,2,2,2,2,2,2,2,2,
2,2,2,2,2,2,2,2,2,2,2,2,2,2,2,2,2,2,2,2,2,2,2,2,2,2,2,2,2,2,2,2,2,2,2,2,
2,2,2,2,2,2,2,2,2,2,2,2,2,2,2,2,2,2,2,2,2,2,2,2,2,2,2,2,2,2,2,2,2,2,2,2,
2,2,2,2,2,2,2,2,2,2,2,2,2,2,2,2,2,2,2,2,2,2,2,2,2,2,2,2,2,2,2,2,2,2,2,2,
2,2,2,2,2,2,2,2,2,2,2,2,2,2,2,2,2,2,2,2,2,2,2,2,2,2,2,2,2,2,2,2,2,2,2,2,
2,2,2,2,2,4),(-2.5139883673475,-2.46796189057673,-2.45376184525105,-2.44803099167605,
-2.44372121743481,-2.44176862456714,-2.44030205188033,-2.43892509066694,
-2.43664284139591,-2.4307668503137,-2.37618862860514,-2.35506701823993,
-2.34765131853795,-2.34313811010895,-2.34174248311774,-2.34098116445121,
-2.34017030178535,-2.33913114717567,-2.33746514750599,-2.32860442250549,
-2.29627776636585,-2.26977167225771,-2.25461853545282,-2.24552863384444,
-2.24292407356314,-2.24132336089935,-2.23986765289813,-2.2379912253208,
-2.23408382122551,-2.19522871381193,-2.14906705702404,-2.14546636955356,
-2.1436675682756,-2.14223632790328,-2.14132913532577,-2.14051821451748,
-2.13947927204239,-2.13733481994395,-2.12242954689244,-2.11385539126091,
-2.07301147089012,-2.04741353437713,-2.04392886096236,-2.04213729394979,
-2.04070359332995,-2.03905602474411,-2.03624112604167,-2.02622546872829,
-2.02422581088746,-1.9622947201022,-1.95042962099684,-1.94621597514117,
-1.94326184262198,-1.9420781046726,-1.94124447354048,-1.9404840184286,-1.93944545298245,
-1.93738897003632,-1.90102614388073,-1.87074992148099,-1.85533314684365,
-1.84612791497397,-1.84351132092197,-1.84190766315403,-1.84045219646113,
-1.83858017318179,-1.83469679180234,-1.80154296690654,-1.74982937259077,
-1.74421856611467,-1.74271004643852,-1.74180594577909,-1.74099017516398,
-1.73993064020917,-1.73815933010255,-1.72735514048054,-1.70439012884219,
-1.67305662256649,-1.65629101659279,-1.64651148847798,-1.64383895580823,
-1.64222269372535,-1.64076974257636,-1.63892019615758,-1.63515151215182,
-1.58790917442322,-1.56059997381375,-1.55029208664757,-1.54452960001577,
-1.54300708017979,-1.54209981712395,-1.54128480595519,-1.54023101044057,
-1.5379525979515,-1.50134984868042,-1.47114510260012,-1.45582248480633,
-1.44665761493957,-1.44404472411244,-1.44244168675724,-1.44098570080046,
-1.43911149227542,-1.43521807701067,-1.40130370261824,-1.3525643572676,
-1.34502946737985,-1.34336738498775,-1.34242910577765,-1.34161939562965,
-1.34059770749452,-1.33860682053732,-1.32688561431306,-1.27545468040192,
-1.25738393664283,-1.24726463514544,-1.24447154191107,-1.24281230335258,
-1.24136535394898,-1.23958173806679,-1.23613759159561,-1.21201629567094,
-1.18120306699415,-1.14632197293124,-1.14401158940787,-1.14295174278235,
-1.14213583904628,-1.14123169975911,-1.13972336029486,-1.13411588506325,
-1.08241699620839,-1.04926718253818,-1.0453833455229,-1.04351101926021,
-1.04205527920723,-1.04045128192738,-1.03783404798626,-1.02862574995025,
-1.01320071476077,-0.982887803774222,-0.957295620588936,-0.946065516060176,
-0.944273320188244,-0.943207640651296,-0.942390945689695,-0.941489931865512,
-0.939995374066424,-0.934533082180191,-0.887611238046503,-0.849571437427456,
-0.845660028620719,-0.843782388966488,-0.842326054927193,-0.840724970402151,
-0.838120516777198,-0.829038179088114,-0.813902313534164,-0.783822644632941,
-0.746760732518862,-0.74448910253652,-0.743436610889292,-0.74262180673222,
-0.741713888237294,-0.740188335900028,-0.73439180546879,-0.723999269245736,
-0.696448691938276,-0.649637548726214,-0.645857574530095,-0.644005826143996,
-0.642552670498336,-0.640937754123617,-0.638271090318463,-0.62855309630134,
-0.611931668473617,-0.580682077105611,-0.559228038624472,-0.556703510775538,
-0.54651443390152,-0.544774340432485,-0.54372401574617,-0.542909541035049,
-0.542000508113727,-0.540469822111087,-0.53461543681671,-0.524075957486153,
-0.49579602973353,-0.44998021110871,-0.446172559634251,-0.444315380009893,
-0.442861654297179,-0.441249896171482,-0.438662228264077,-0.435576340281137,
-0.429545520260564,-0.414286797838816,-0.369349975765009,-0.347390837687695,
-0.345105554082086,-0.344034280513075,-0.343216799199853,-0.342318682001304,
-0.340836888481372,-0.335616987926469,-0.326596094793215,-0.304520764377662,
-0.265845573130727,-0.264252023667119,-0.249331763160838,-0.246425483574686,
-0.244583703065853,-0.243131681925652,-0.241511084198875,-0.238960219779077,
-0.229898875729598,-0.214747461188375,-0.187955806428541,-0.150423863246312,
-0.146171888935498,-0.144755801385972,-0.143960389335609,-0.143227882326773,
-0.142207331236432,-0.140155759901981,-0.126838913437522,-0.105241758511448,
-0.084928191612275,-0.0507289004174123,-0.0468327649219579,-0.0449580880292513,
-0.0435021114150737,-0.0418994612384761,-0.0402501570404879,-0.0378240370510129,
-0.028648498628005,-0.000592063050680485),.UNSPECIFIED.);
#828=B_SPLINE_CURVE_WITH_KNOTS('',3,(#26974,#26975,#26976,#26977,#26978,
#26979,#26980,#26981,#26982,#26983,#26984,#26985,#26986,#26987,#26988,#26989,
#26990,#26991,#26992,#26993,#26994,#26995,#26996,#26997,#26998,#26999,#27000,
#27001,#27002,#27003,#27004,#27005,#27006,#27007,#27008,#27009,#27010,#27011,
#27012,#27013,#27014,#27015,#27016,#27017,#27018,#27019,#27020,#27021,#27022,
#27023,#27024,#27025,#27026,#27027,#27028,#27029,#27030,#27031,#27032,#27033,
#27034,#27035,#27036,#27037,#27038,#27039,#27040,#27041,#27042,#27043,#27044,
#27045,#27046,#27047,#27048,#27049,#27050,#27051,#27052,#27053,#27054,#27055,
#27056,#27057,#27058,#27059,#27060,#27061,#27062,#27063,#27064,#27065,#27066,
#27067,#27068,#27069,#27070,#27071,#27072,#27073,#27074,#27075,#27076,#27077,
#27078,#27079,#27080,#27081,#27082,#27083,#27084,#27085,#27086,#27087,#27088,
#27089,#27090,#27091,#27092,#27093,#27094,#27095,#27096,#27097,#27098,#27099,
#27100,#27101,#27102,#27103,#27104,#27105,#27106,#27107,#27108,#27109,#27110,
#27111,#27112,#27113,#27114,#27115,#27116,#27117,#27118,#27119,#27120,#27121,
#27122,#27123,#27124,#27125,#27126,#27127,#27128,#27129,#27130,#27131,#27132,
#27133,#27134,#27135,#27136,#27137,#27138,#27139,#27140,#27141,#27142,#27143,
#27144,#27145,#27146,#27147,#27148,#27149,#27150,#27151,#27152,#27153,#27154,
#27155,#27156,#27157,#27158,#27159,#27160,#27161,#27162,#27163,#27164,#27165,
#27166,#27167,#27168,#27169,#27170,#27171,#27172,#27173,#27174,#27175,#27176,
#27177,#27178,#27179,#27180,#27181,#27182,#27183,#27184,#27185,#27186,#27187,
#27188,#27189,#27190,#27191,#27192,#27193,#27194,#27195,#27196,#27197,#27198,
#27199,#27200,#27201,#27202,#27203,#27204,#27205,#27206,#27207,#27208,#27209,
#27210,#27211,#27212,#27213,#27214,#27215,#27216,#27217,#27218,#27219,#27220,
#27221,#27222,#27223,#27224,#27225,#27226,#27227,#27228,#27229,#27230,#27231,
#27232,#27233,#27234,#27235,#27236,#27237,#27238,#27239,#27240,#27241,#27242,
#27243,#27244,#27245,#27246,#27247,#27248,#27249,#27250,#27251,#27252,#27253,
#27254,#27255,#27256,#27257,#27258,#27259,#27260,#27261,#27262,#27263,#27264,
#27265,#27266,#27267,#27268,#27269,#27270,#27271,#27272,#27273,#27274,#27275,
#27276,#27277,#27278,#27279,#27280,#27281,#27282,#27283,#27284,#27285,#27286,
#27287,#27288,#27289,#27290,#27291,#27292,#27293,#27294,#27295,#27296,#27297,
#27298,#27299,#27300,#27301,#27302,#27303,#27304,#27305,#27306,#27307,#27308,
#27309,#27310,#27311,#27312,#27313,#27314,#27315,#27316,#27317,#27318,#27319,
#27320,#27321,#27322,#27323,#27324,#27325,#27326,#27327,#27328,#27329,#27330,
#27331,#27332,#27333,#27334,#27335,#27336,#27337,#27338,#27339,#27340,#27341,
#27342,#27343,#27344,#27345,#27346,#27347,#27348,#27349,#27350,#27351,#27352,
#27353,#27354,#27355,#27356,#27357,#27358,#27359,#27360,#27361,#27362,#27363,
#27364,#27365,#27366,#27367,#27368,#27369,#27370,#27371,#27372,#27373,#27374,
#27375,#27376,#27377,#27378,#27379,#27380,#27381,#27382,#27383,#27384,#27385,
#27386,#27387,#27388,#27389,#27390,#27391,#27392,#27393,#27394,#27395,#27396,
#27397,#27398,#27399,#27400,#27401,#27402,#27403,#27404,#27405,#27406,#27407,
#27408,#27409,#27410,#27411,#27412,#27413,#27414,#27415,#27416,#27417,#27418,
#27419,#27420,#27421,#27422,#27423,#27424,#27425,#27426,#27427,#27428,#27429,
#27430,#27431,#27432,#27433,#27434,#27435,#27436,#27437,#27438,#27439,#27440,
#27441,#27442,#27443,#27444,#27445,#27446,#27447,#27448,#27449,#27450,#27451,
#27452,#27453),.UNSPECIFIED.,.F.,.F.,(4,2,2,2,2,2,2,2,2,2,2,2,2,2,2,2,2,
2,2,2,2,2,2,2,2,2,2,2,2,2,2,2,2,2,2,2,2,2,2,2,2,2,2,2,2,2,2,2,2,2,2,2,2,
2,2,2,2,2,2,2,2,2,2,2,2,2,2,2,2,2,2,2,2,2,2,2,2,2,2,2,2,2,2,2,2,2,2,2,2,
2,2,2,2,2,2,2,2,2,2,2,2,2,2,2,2,2,2,2,2,2,2,2,2,2,2,2,2,2,2,2,2,2,2,2,2,
2,2,2,2,2,2,2,2,2,2,2,2,2,2,2,2,2,2,2,2,2,2,2,2,2,2,2,2,2,2,2,2,2,2,2,2,
2,2,2,2,2,2,2,2,2,2,2,2,2,2,2,2,2,2,2,2,2,2,2,2,2,2,2,2,2,2,2,2,2,2,2,2,
2,2,2,2,2,2,2,2,2,2,2,2,2,2,2,2,2,2,2,2,2,2,2,2,2,2,2,2,2,2,2,2,2,2,2,2,
2,2,2,2,2,2,4),(-2.51332395769527,-2.46474828361658,-2.46116306924221,-2.4593699194601,
-2.45787086751029,-2.45696913561548,-2.45615318554831,-2.45509034196855,
-2.45330692094798,-2.44224479945897,-2.43865158241955,-2.4313375094352,
-2.40560667303955,-2.38788740616807,-2.36529844435069,-2.36045418606504,
-2.35885307230337,-2.35749504545638,-2.35604568463502,-2.3542249422401,
-2.35138597987877,-2.33750991168437,-2.33465826145439,-2.32645813380707,
-2.2982124093394,-2.27465882310025,-2.26519882645719,-2.25980042106438,
-2.25829969436402,-2.25739757544443,-2.2565817103599,-2.25551955520539,
-2.25373852679323,-2.24272604101519,-2.22116599881277,-2.18310722642188,
-2.16998954510344,-2.1645735891904,-2.16049435664933,-2.15858654898353,
-2.1571208244371,-2.15574202518615,-2.15345053968071,-2.14751565193713,
-2.14609830693586,-2.14456286037487,-2.08074844137598,-2.06725950949993,
-2.06032705747805,-2.05869891913456,-2.05776835130141,-2.0569580713294,
-2.05592626014152,-2.05428471346218,-2.0458251775807,-1.98651126146365,
-1.97131764782859,-1.96220996706017,-1.95960352996115,-1.95800235075195,
-1.95654667051234,-1.95467091421605,-1.95076722311105,-1.91243527507579,
-1.86576952138576,-1.86032089928283,-1.85882793412789,-1.85792744609472,
-1.85711091709718,-1.85604504925556,-1.85425166825216,-1.84298888763837,
-1.81745195756351,-1.78717848952787,-1.77176304952694,-1.76255863335647,
-1.75994228034119,-1.75833877224081,-1.75688344265723,-1.75501159750981,
-1.75112859210124,-1.71797872664734,-1.66627032069229,-1.66065903308598,
-1.65915056135955,-1.65824652474706,-1.65743083657232,-1.65637144127167,
-1.65406268949003,-1.61913161913508,-1.58837720144721,-1.57235461573101,
-1.56288888624091,-1.56024654480853,-1.55863710974485,-1.55718290052906,
-1.55532153204203,-1.55149261146515,-1.54768589551934,-1.50327062482036,
-1.47673460526656,-1.46664583848783,-1.46097090378476,-1.45945649361129,
-1.45855110408222,-1.45773572688925,-1.45667875699208,-1.45438310506596,
-1.4187008248078,-1.38819432029752,-1.37248862920222,-1.36315844401215,
-1.3605292937554,-1.3589227484772,-1.35746779937504,-1.3556008208601,-1.35174366963999,
-1.32047334928139,-1.27012925756055,-1.26161719079115,-1.25989298897333,
-1.25894118423916,-1.25813272089357,-1.25712890938093,-1.2551594889612,
-1.24084581064947,-1.21614110238151,-1.1692000228423,-1.16283663969254,
-1.16047812651329,-1.1590859192022,-1.15762562289127,-1.15571895623606,
-1.15165733095664,-1.11591837415816,-1.07808917102712,-1.06259512034142,
-1.06042915914553,-1.05938575513482,-1.05857412522969,-1.05765059287603,
-1.05605500406282,-1.04942639686582,-1.03683633828169,-0.997506801881617,
-0.965778788437095,-0.961914603358767,-0.960046153125368,-0.958590922179214,
-0.956984944443865,-0.95435871902511,-0.945059624745885,-0.929424297942888,
-0.898944744922087,-0.863071237870986,-0.861005321815355,-0.859964268948691,
-0.859203074905411,-0.858369811136605,-0.857188625769793,-0.854251187562669,
-0.81563597083389,-0.769750962378527,-0.763583330847972,-0.76111395999698,
-0.759699901105109,-0.758392347772969,-0.756615561898078,-0.753203749833357,
-0.730122509032019,-0.699881529130821,-0.689482833722177,-0.663424074653541,
-0.66106941433786,-0.660001407686329,-0.659184392516423,-0.658284604894092,
-0.656795432413241,-0.651388791851969,-0.641961932862458,-0.618180764598795,
-0.569929693877353,-0.565703153692123,-0.562564867068603,-0.560673507729573,
-0.559210807901309,-0.557631538481867,-0.555125156250188,-0.546963296060805,
-0.533874216787375,-0.481472992293541,-0.46348392730341,-0.461467305363734,
-0.460438762915992,-0.459680755320231,-0.458844406858479,-0.457647398334057,
-0.454611028127832,-0.437439505877787,-0.391869766866492,-0.380384043658242,
-0.365509490772975,-0.362605889808877,-0.360764855569276,-0.359312819313376,
-0.357724058518867,-0.355151434155842,-0.352071998322744,-0.346058870197086,
-0.33086419188426,-0.295248831152963,-0.279751570060649,-0.263686141486495,
-0.261501451205079,-0.26045438554456,-0.259642374119812,-0.258721119785569,
-0.257135779989148,-0.250636286419062,-0.238399815691751,-0.192238898274493,
-0.180764963804175,-0.1658089436138,-0.162900356336665,-0.161057822386082,
-0.15960565640638,-0.158248572266005,-0.156659019389015,-0.151938423830255,
-0.130901259995497,-0.113205627287674,-0.0669098856791247,-0.062628526562833,
-0.0612084632076815,-0.0604122082424815,-0.0596798606573647,-0.0586609252498538,
-0.0566175252987397,-0.0539782882255648,-0.000592841608242558),
 .UNSPECIFIED.);
#829=B_SPLINE_CURVE_WITH_KNOTS('',3,(#28433,#28434,#28435,#28436,#28437,
#28438,#28439,#28440,#28441,#28442,#28443,#28444,#28445,#28446,#28447,#28448,
#28449,#28450,#28451,#28452,#28453,#28454,#28455,#28456,#28457,#28458,#28459,
#28460,#28461,#28462,#28463,#28464,#28465,#28466,#28467,#28468,#28469,#28470,
#28471,#28472,#28473,#28474,#28475,#28476,#28477,#28478,#28479,#28480,#28481,
#28482,#28483,#28484,#28485,#28486,#28487,#28488,#28489,#28490,#28491,#28492,
#28493,#28494,#28495,#28496,#28497,#28498,#28499,#28500,#28501,#28502,#28503,
#28504,#28505,#28506,#28507,#28508,#28509,#28510,#28511,#28512,#28513,#28514,
#28515,#28516,#28517),.UNSPECIFIED.,.F.,.F.,(4,3,3,3,3,3,3,3,3,3,3,3,3,
3,3,3,3,3,3,3,3,3,3,3,3,3,3,3,4),(0.,0.0170098241792627,0.0424826395433647,
0.0682962769238695,0.0913512330686695,0.0964562008288006,0.121594894041372,
0.146637962453068,0.171052849770118,0.182468804955695,0.186977115896109,
0.211109611306723,0.234543633473231,0.251322674972674,0.264602698464612,
0.269910529014969,0.273918093975593,0.297399013310025,0.321140231227419,
0.342399840472737,0.351520822404548,0.355793196577609,0.378788067002577,
0.400130399022457,0.407097962113538,0.413428647993403,0.435399867888606,
0.457192780488514,0.463803050843695),.UNSPECIFIED.);
#830=B_SPLINE_CURVE_WITH_KNOTS('',3,(#28519,#28520,#28521,#28522,#28523,
#28524,#28525,#28526,#28527,#28528,#28529,#28530,#28531,#28532,#28533,#28534,
#28535,#28536,#28537,#28538,#28539,#28540,#28541,#28542,#28543,#28544,#28545,
#28546,#28547,#28548,#28549,#28550,#28551,#28552,#28553,#28554,#28555,#28556,
#28557,#28558,#28559,#28560,#28561,#28562,#28563,#28564,#28565,#28566,#28567,
#28568,#28569,#28570,#28571,#28572,#28573,#28574,#28575,#28576,#28577,#28578,
#28579,#28580,#28581,#28582,#28583,#28584,#28585,#28586,#28587,#28588,#28589,
#28590,#28591,#28592,#28593,#28594,#28595,#28596,#28597,#28598,#28599,#28600,
#28601,#28602,#28603,#28604,#28605,#28606),.UNSPECIFIED.,.F.,.F.,(4,3,3,
3,3,3,3,3,3,3,3,3,3,3,3,3,3,3,3,3,3,3,3,3,3,3,3,3,3,4),(-0.463803050843694,
-0.449790106353243,-0.427990665865324,-0.416071534428731,-0.41053262250662,
-0.406065555453362,-0.383649085978725,-0.360658636559499,-0.357654820809351,
-0.351701489295335,-0.328241177350174,-0.304498488949914,-0.280901268184384,
-0.274909285295064,-0.270960497067351,-0.246531766448708,-0.235762608198985,
-0.211934962645635,-0.188107317092285,-0.183891756486896,-0.180496953448606,
-0.156079531689618,-0.131226048105235,-0.106117747812671,-0.0959943972028356,
-0.0910045065255718,-0.0652633795699505,-0.0394823888695457,-0.0142475767317681,
0.),.UNSPECIFIED.);
#831=B_SPLINE_CURVE_WITH_KNOTS('',3,(#28607,#28608,#28609,#28610),
 .UNSPECIFIED.,.F.,.F.,(4,4),(-0.0140491024708372,0.),.UNSPECIFIED.);
#832=B_SPLINE_CURVE_WITH_KNOTS('',3,(#29575,#29576,#29577,#29578,#29579,
#29580,#29581,#29582,#29583,#29584,#29585,#29586,#29587,#29588,#29589,#29590,
#29591,#29592,#29593,#29594,#29595,#29596,#29597,#29598,#29599,#29600,#29601,
#29602,#29603,#29604,#29605,#29606,#29607,#29608,#29609,#29610,#29611,#29612,
#29613,#29614,#29615,#29616,#29617,#29618,#29619,#29620,#29621,#29622,#29623,
#29624,#29625,#29626,#29627,#29628,#29629,#29630,#29631,#29632,#29633,#29634,
#29635,#29636,#29637,#29638,#29639,#29640,#29641,#29642,#29643,#29644,#29645,
#29646,#29647,#29648,#29649,#29650,#29651,#29652,#29653,#29654,#29655,#29656,
#29657,#29658,#29659,#29660,#29661,#29662,#29663,#29664,#29665,#29666,#29667,
#29668),.UNSPECIFIED.,.F.,.F.,(4,3,3,3,3,3,3,3,3,3,3,3,3,3,3,3,3,3,3,3,
3,3,3,3,3,3,3,3,3,3,3,4),(0.,0.0139666598681629,0.0354492048263863,0.0576250686896674,
0.0685265859231677,0.0770896876198345,0.0816411102851959,0.104504088810244,
0.127761520890668,0.145893898052724,0.154960086633753,0.160934662671419,
0.164026275214781,0.18805909179815,0.211994708341173,0.227291834558635,
0.241947905204957,0.246523482387956,0.250638107839803,0.274355640976877,
0.298561537524763,0.323231579885226,0.329929774781174,0.335709929194683,
0.339916350947803,0.365091941017713,0.390436885206924,0.397901145376386,
0.402692087010053,0.428435843892961,0.45394520469992,0.461788964899784),
 .UNSPECIFIED.);
#833=B_SPLINE_CURVE_WITH_KNOTS('',3,(#29669,#29670,#29671,#29672,#29673,
#29674,#29675,#29676,#29677,#29678,#29679,#29680,#29681,#29682,#29683,#29684,
#29685,#29686,#29687,#29688,#29689,#29690,#29691,#29692,#29693,#29694,#29695,
#29696,#29697,#29698,#29699,#29700,#29701,#29702,#29703,#29704,#29705,#29706,
#29707,#29708,#29709,#29710,#29711,#29712,#29713,#29714,#29715,#29716,#29717,
#29718,#29719,#29720,#29721,#29722,#29723,#29724,#29725,#29726,#29727,#29728,
#29729,#29730,#29731,#29732,#29733,#29734,#29735,#29736,#29737,#29738,#29739,
#29740,#29741,#29742,#29743,#29744,#29745,#29746,#29747,#29748,#29749,#29750,
#29751,#29752,#29753,#29754,#29755,#29756),.UNSPECIFIED.,.F.,.F.,(4,3,3,
3,3,3,3,3,3,3,3,3,3,3,3,3,3,3,3,3,3,3,3,3,3,3,3,3,3,4),(-0.461788964899782,
-0.444855550134428,-0.419152893345616,-0.406271531682089,-0.400199974555711,
-0.395168529208714,-0.369855739683799,-0.344556768713737,-0.341034351191149,
-0.33606198793914,-0.331746083665484,-0.307015393549491,-0.282570742889413,
-0.258867857593402,-0.248690711882788,-0.244217611698179,-0.220731256812843,
-0.211799399012893,-0.187739266633416,-0.164360764291082,-0.158727229016938,
-0.135371887906763,-0.112003733335168,-0.0891062190630772,-0.0803325096073959,
-0.0766178882203682,-0.0541551504458856,-0.0320568974934828,-0.0106664530521837,
-1.30075470011633E-14),.UNSPECIFIED.);
#834=B_SPLINE_CURVE_WITH_KNOTS('',3,(#29760,#29761,#29762,#29763,#29764,
#29765,#29766,#29767,#29768,#29769,#29770,#29771,#29772,#29773,#29774,#29775,
#29776,#29777,#29778,#29779,#29780,#29781,#29782,#29783,#29784,#29785,#29786,
#29787,#29788,#29789,#29790,#29791,#29792,#29793),.UNSPECIFIED.,.F.,.F.,
(4,2,2,2,2,2,2,2,2,2,2,2,2,2,2,2,4),(-0.22533843255893,-0.216182593404494,
-0.18091865643817,-0.156950339943155,-0.140921103226519,-0.129823782034954,
-0.118153571207391,-0.114481377626862,-0.112295015626103,-0.110369884265133,
-0.107992250297265,-0.103463255811762,-0.0921160616035588,-0.0805188447194219,
-0.0652099958826858,-0.043221973238958,0.),.UNSPECIFIED.);
#835=B_SPLINE_CURVE_WITH_KNOTS('',3,(#29802,#29803,#29804,#29805,#29806,
#29807,#29808,#29809,#29810,#29811,#29812,#29813,#29814,#29815,#29816,#29817,
#29818,#29819,#29820,#29821,#29822,#29823,#29824,#29825,#29826,#29827,#29828,
#29829,#29830,#29831,#29832,#29833,#29834,#29835),.UNSPECIFIED.,.F.,.F.,
(4,2,2,2,2,2,2,2,2,2,2,2,2,2,2,2,4),(-0.225338432559487,-0.216182593405045,
-0.180918656438646,-0.156950339943541,-0.140921103226827,-0.129823782035196,
-0.118153571207555,-0.114481377627008,-0.112295015626236,-0.110369884265256,
-0.107992250297385,-0.103463255811877,-0.0921160616036507,-0.0805188447194852,
-0.0652099958827053,-0.0432219732389482,0.),.UNSPECIFIED.);
#836=B_SPLINE_CURVE_WITH_KNOTS('',3,(#29844,#29845,#29846,#29847,#29848,
#29849,#29850,#29851,#29852,#29853,#29854,#29855,#29856,#29857,#29858,#29859,
#29860,#29861,#29862,#29863,#29864,#29865,#29866,#29867,#29868,#29869,#29870,
#29871,#29872,#29873,#29874,#29875,#29876,#29877),.UNSPECIFIED.,.F.,.F.,
(4,2,2,2,2,2,2,2,2,2,2,2,2,2,2,2,4),(-0.225338432559843,-0.216182593405344,
-0.180918656438743,-0.156950339943502,-0.140921103226703,-0.129823782035015,
-0.118153571207324,-0.114481377626746,-0.112295015625973,-0.110369884265002,
-0.107992250297144,-0.103463255811654,-0.0921160616034753,-0.0805188447193631,
-0.0652099958826622,-0.0432219732389638,0.),.UNSPECIFIED.);
#837=B_SPLINE_CURVE_WITH_KNOTS('',3,(#29886,#29887,#29888,#29889,#29890,
#29891,#29892,#29893,#29894,#29895,#29896,#29897,#29898,#29899,#29900,#29901,
#29902,#29903,#29904,#29905,#29906,#29907,#29908,#29909,#29910,#29911,#29912,
#29913,#29914,#29915,#29916,#29917,#29918,#29919),.UNSPECIFIED.,.F.,.F.,
(4,2,2,2,2,2,2,2,2,2,2,2,2,2,2,2,4),(-0.225338432559394,-0.216182593404911,
-0.180918656438384,-0.15695033994328,-0.140921103226616,-0.12982378203502,
-0.118153571207424,-0.114481377626883,-0.112295015626127,-0.110369884265165,
-0.107992250297307,-0.103463255811807,-0.0921160616035986,-0.0805188447194506,
-0.0652099958826983,-0.0432219732389566,0.),.UNSPECIFIED.);
#838=B_SPLINE_CURVE_WITH_KNOTS('',3,(#29928,#29929,#29930,#29931,#29932,
#29933,#29934,#29935,#29936,#29937,#29938,#29939,#29940,#29941,#29942,#29943,
#29944,#29945,#29946,#29947,#29948,#29949,#29950,#29951,#29952,#29953,#29954,
#29955,#29956,#29957,#29958,#29959,#29960,#29961),.UNSPECIFIED.,.F.,.F.,
(4,2,2,2,2,2,2,2,2,2,2,2,2,2,2,2,4),(-0.225338432559585,-0.216182593405109,
-0.180918656438604,-0.156950339943452,-0.140921103226724,-0.129823782035084,
-0.118153571207435,-0.114481377626872,-0.112295015626095,-0.110369884265119,
-0.107992250297262,-0.103463255811765,-0.0921160616035663,-0.0805188447194236,
-0.065209995882676,-0.0432219732389438,0.),.UNSPECIFIED.);
#839=B_SPLINE_CURVE_WITH_KNOTS('',3,(#29970,#29971,#29972,#29973,#29974,
#29975,#29976,#29977,#29978,#29979,#29980,#29981,#29982,#29983,#29984,#29985,
#29986,#29987,#29988,#29989,#29990,#29991,#29992,#29993,#29994,#29995,#29996,
#29997,#29998,#29999,#30000,#30001,#30002,#30003),.UNSPECIFIED.,.F.,.F.,
(4,2,2,2,2,2,2,2,2,2,2,2,2,2,2,2,4),(-0.225338432560591,-0.216182593406049,
-0.180918656439286,-0.156950339943944,-0.140921103227085,-0.129823782035365,
-0.118153571207645,-0.11448137762707,-0.112295015626274,-0.110369884265278,
-0.107992250297404,-0.103463255811892,-0.0921160616036589,-0.0805188447194971,
-0.0652099958827318,-0.043221973238974,0.),.UNSPECIFIED.);
#840=B_SPLINE_CURVE_WITH_KNOTS('',3,(#30012,#30013,#30014,#30015,#30016,
#30017,#30018,#30019,#30020,#30021,#30022,#30023,#30024,#30025,#30026,#30027,
#30028,#30029,#30030,#30031,#30032,#30033,#30034,#30035,#30036,#30037,#30038,
#30039,#30040,#30041,#30042,#30043,#30044,#30045),.UNSPECIFIED.,.F.,.F.,
(4,2,2,2,2,2,2,2,2,2,2,2,2,2,2,2,4),(-0.225338432560395,-0.21618259340586,
-0.180918656439119,-0.156950339943809,-0.140921103226983,-0.129823782035285,
-0.118153571207591,-0.114481377627025,-0.112295015626251,-0.110369884265274,
-0.107992250297403,-0.103463255811889,-0.0921160616036515,-0.0805188447194844,
-0.0652099958827251,-0.0432219732389749,0.),.UNSPECIFIED.);
#841=B_SPLINE_CURVE_WITH_KNOTS('',3,(#30054,#30055,#30056,#30057,#30058,
#30059,#30060,#30061,#30062,#30063,#30064,#30065,#30066,#30067,#30068,#30069,
#30070,#30071,#30072,#30073,#30074,#30075,#30076,#30077,#30078,#30079,#30080,
#30081,#30082,#30083,#30084,#30085,#30086,#30087),.UNSPECIFIED.,.F.,.F.,
(4,2,2,2,2,2,2,2,2,2,2,2,2,2,2,2,4),(-0.225338432558288,-0.216182593403889,
-0.180918656437663,-0.156950339942723,-0.140921103226146,-0.129823782034617,
-0.118153571207095,-0.114481377626574,-0.112295015625834,-0.110369884264885,
-0.107992250297034,-0.103463255811553,-0.0921160616033991,-0.0805188447193084,
-0.0652099958826347,-0.0432219732389551,0.),.UNSPECIFIED.);
#842=B_SPLINE_CURVE_WITH_KNOTS('',3,(#30096,#30097,#30098,#30099,#30100,
#30101,#30102,#30103,#30104,#30105,#30106,#30107,#30108,#30109,#30110,#30111,
#30112,#30113,#30114,#30115,#30116,#30117,#30118,#30119,#30120,#30121,#30122,
#30123,#30124,#30125,#30126,#30127,#30128,#30129),.UNSPECIFIED.,.F.,.F.,
(4,2,2,2,2,2,2,2,2,2,2,2,2,2,2,2,4),(-0.225338432559953,-0.216182593405462,
-0.180918656438873,-0.156950339943631,-0.14092110322683,-0.129823782035144,
-0.118153571207449,-0.114481377626881,-0.112295015626082,-0.110369884265086,
-0.107992250297227,-0.103463255811732,-0.0921160616035443,-0.0805188447194133,
-0.0652099958826861,-0.043221973238957,0.),.UNSPECIFIED.);
#843=B_SPLINE_CURVE_WITH_KNOTS('',3,(#30138,#30139,#30140,#30141,#30142,
#30143,#30144,#30145,#30146,#30147,#30148,#30149,#30150,#30151,#30152,#30153,
#30154,#30155,#30156,#30157),.UNSPECIFIED.,.F.,.F.,(4,2,2,2,2,2,2,2,2,4),
(-0.475220070020625,-0.441790011987763,-0.414059721280184,-0.394580184974582,
-0.380386463975323,-0.36989470508298,-0.361499869486035,-0.358160690967077,
-0.355853630537146,-0.355774891916115),.UNSPECIFIED.);
#844=B_SPLINE_CURVE_WITH_KNOTS('',3,(#30164,#30165,#30166,#30167,#30168,
#30169,#30170,#30171,#30172,#30173,#30174,#30175,#30176,#30177,#30178,#30179,
#30180,#30181),.UNSPECIFIED.,.F.,.F.,(4,2,2,2,2,2,2,2,4),(-0.355774891916115,
-0.353603695467602,-0.350430609151558,-0.343375404346486,-0.330600159177977,
-0.316000108246756,-0.296556237452606,-0.264901408087306,-0.225338432559845),
 .UNSPECIFIED.);
#845=B_SPLINE_CURVE_WITH_KNOTS('',3,(#30185,#30186,#30187,#30188,#30189,
#30190,#30191,#30192,#30193,#30194,#30195,#30196,#30197,#30198,#30199,#30200,
#30201,#30202,#30203,#30204,#30205,#30206,#30207,#30208,#30209,#30210,#30211,
#30212,#30213,#30214,#30215,#30216,#30217,#30218),.UNSPECIFIED.,.F.,.F.,
(4,2,2,2,2,2,2,2,2,2,2,2,2,2,2,2,4),(-0.225338432559478,-0.216182593404956,
-0.180918656438277,-0.156950339943081,-0.140921103226373,-0.129823782034755,
-0.118153571207149,-0.114481377626612,-0.112295015625852,-0.110369884264885,
-0.107992250297023,-0.103463255811539,-0.0921160616033758,-0.0805188447192899,
-0.0652099958826333,-0.0432219732389767,0.),.UNSPECIFIED.);
#846=B_SPLINE_CURVE_WITH_KNOTS('',3,(#30227,#30228,#30229,#30230,#30231,
#30232,#30233,#30234,#30235,#30236,#30237,#30238,#30239,#30240,#30241,#30242,
#30243,#30244,#30245,#30246,#30247,#30248,#30249,#30250,#30251,#30252,#30253,
#30254,#30255,#30256,#30257,#30258,#30259,#30260),.UNSPECIFIED.,.F.,.F.,
(4,2,2,2,2,2,2,2,2,2,2,2,2,2,2,2,4),(-0.225338432560806,-0.216182593406188,
-0.180918656439175,-0.156950339943746,-0.140921103226884,-0.12982378203515,
-0.118153571207415,-0.114481377626832,-0.11229501562605,-0.110369884265066,
-0.107992250297192,-0.103463255811689,-0.0921160616035007,-0.0805188447193768,
-0.0652099958826869,-0.0432219732389717,0.),.UNSPECIFIED.);
#847=B_SPLINE_CURVE_WITH_KNOTS('',3,(#30269,#30270,#30271,#30272,#30273,
#30274,#30275,#30276,#30277,#30278,#30279,#30280,#30281,#30282,#30283,#30284,
#30285,#30286,#30287,#30288,#30289,#30290,#30291,#30292,#30293,#30294,#30295,
#30296,#30297,#30298,#30299,#30300,#30301,#30302),.UNSPECIFIED.,.F.,.F.,
(4,2,2,2,2,2,2,2,2,2,2,2,2,2,2,2,4),(-0.225338432559276,-0.21618259340483,
-0.180918656438373,-0.156950339943235,-0.140921103226506,-0.129823782034874,
-0.118153571207256,-0.114481377626715,-0.112295015625943,-0.11036988426497,
-0.107992250297116,-0.103463255811614,-0.0921160616034403,-0.0805188447193372,
-0.065209995882666,-0.0432219732389822,0.),.UNSPECIFIED.);
#848=B_SPLINE_CURVE_WITH_KNOTS('',3,(#30311,#30312,#30313,#30314,#30315,
#30316,#30317,#30318,#30319,#30320,#30321,#30322,#30323,#30324,#30325,#30326,
#30327,#30328,#30329,#30330,#30331,#30332,#30333,#30334,#30335,#30336,#30337,
#30338,#30339,#30340,#30341,#30342,#30343,#30344),.UNSPECIFIED.,.F.,.F.,
(4,2,2,2,2,2,2,2,2,2,2,2,2,2,2,2,4),(-0.225338432560726,-0.21618259340622,
-0.180918656439635,-0.156950339944368,-0.140921103227535,-0.129823782035824,
-0.118153571208108,-0.114481377627516,-0.112295015626722,-0.110369884265733,
-0.107992250297856,-0.103463255812308,-0.092116061603986,-0.0805188447197293,
-0.0652099958828215,-0.0432219732389566,0.),.UNSPECIFIED.);
#849=B_SPLINE_CURVE_WITH_KNOTS('',3,(#30353,#30354,#30355,#30356,#30357,
#30358,#30359,#30360,#30361,#30362,#30363,#30364,#30365,#30366,#30367,#30368,
#30369,#30370,#30371,#30372,#30373,#30374,#30375,#30376,#30377,#30378,#30379,
#30380,#30381,#30382,#30383,#30384,#30385,#30386),.UNSPECIFIED.,.F.,.F.,
(4,2,2,2,2,2,2,2,2,2,2,2,2,2,2,2,4),(-0.225338432561249,-0.216182593406692,
-0.180918656439827,-0.156950339944366,-0.140921103227389,-0.129823782035595,
-0.1181535712078,-0.114481377627208,-0.112295015626422,-0.110369884265441,
-0.107992250297571,-0.103463255812037,-0.0921160616037674,-0.0805188447195652,
-0.0652099958827499,-0.0432219732389706,0.),.UNSPECIFIED.);
#850=B_SPLINE_CURVE_WITH_KNOTS('',3,(#30395,#30396,#30397,#30398,#30399,
#30400,#30401,#30402,#30403,#30404,#30405,#30406,#30407,#30408,#30409,#30410,
#30411,#30412,#30413,#30414,#30415,#30416,#30417,#30418,#30419,#30420,#30421,
#30422,#30423,#30424,#30425,#30426,#30427,#30428),.UNSPECIFIED.,.F.,.F.,
(4,2,2,2,2,2,2,2,2,2,2,2,2,2,2,2,4),(-0.225338432560144,-0.216182593405564,
-0.180918656438685,-0.156950339943354,-0.140921103226555,-0.129823782034876,
-0.118153571207208,-0.114481377626656,-0.112295015625892,-0.110369884264924,
-0.107992250297063,-0.103463255811581,-0.0921160616034071,-0.0805188447193141,
-0.0652099958826549,-0.0432219732389826,0.),.UNSPECIFIED.);
#851=B_SPLINE_CURVE_WITH_KNOTS('',3,(#30437,#30438,#30439,#30440,#30441,
#30442,#30443,#30444,#30445,#30446,#30447,#30448,#30449,#30450,#30451,#30452,
#30453,#30454,#30455,#30456,#30457,#30458,#30459,#30460,#30461,#30462,#30463,
#30464,#30465,#30466,#30467,#30468,#30469,#30470),.UNSPECIFIED.,.F.,.F.,
(4,2,2,2,2,2,2,2,2,2,2,2,2,2,2,2,4),(-0.225338432560541,-0.216182593406004,
-0.180918656439237,-0.156950339943896,-0.140921103227052,-0.129823782035331,
-0.118153571207599,-0.114481377627011,-0.112295015626233,-0.11036988426526,
-0.107992250297404,-0.1034632558119,-0.092116061603665,-0.0805188447195002,
-0.0652099958827254,-0.0432219732389589,0.),.UNSPECIFIED.);
#852=B_SPLINE_CURVE_WITH_KNOTS('',3,(#30479,#30480,#30481,#30482,#30483,
#30484,#30485,#30486,#30487,#30488,#30489,#30490,#30491,#30492,#30493,#30494,
#30495,#30496,#30497,#30498,#30499,#30500,#30501,#30502,#30503,#30504,#30505,
#30506,#30507,#30508,#30509,#30510,#30511,#30512),.UNSPECIFIED.,.F.,.F.,
(4,2,2,2,2,2,2,2,2,2,2,2,2,2,2,2,4),(-0.225338432560968,-0.216182593406323,
-0.180918656439217,-0.15695033994371,-0.140921103226774,-0.129823782034991,
-0.118153571207195,-0.114481377626593,-0.112295015625806,-0.11036988426482,
-0.107992250296948,-0.103463255811474,-0.0921160616033362,-0.0805188447192614,
-0.0652099958826226,-0.0432219732389696,0.),.UNSPECIFIED.);
#853=B_SPLINE_CURVE_WITH_KNOTS('',3,(#30521,#30522,#30523,#30524,#30525,
#30526,#30527,#30528,#30529,#30530,#30531,#30532,#30533,#30534,#30535,#30536,
#30537,#30538,#30539,#30540,#30541,#30542,#30543,#30544,#30545,#30546,#30547,
#30548,#30549,#30550,#30551,#30552,#30553,#30554),.UNSPECIFIED.,.F.,.F.,
(4,2,2,2,2,2,2,2,2,2,2,2,2,2,2,2,4),(-0.225338432559187,-0.216182593404789,
-0.180918656438548,-0.156950339943463,-0.140921103226717,-0.129823782035056,
-0.118153571207385,-0.114481377626823,-0.112295015626038,-0.110369884265052,
-0.107992250297197,-0.103463255811722,-0.0921160616035283,-0.0805188447194076,
-0.0652099958826757,-0.0432219732389471,0.),.UNSPECIFIED.);
#854=B_SPLINE_CURVE_WITH_KNOTS('',3,(#30563,#30564,#30565,#30566,#30567,
#30568,#30569,#30570,#30571,#30572,#30573,#30574,#30575,#30576,#30577,#30578,
#30579,#30580,#30581,#30582,#30583,#30584,#30585,#30586,#30587,#30588,#30589,
#30590,#30591,#30592,#30593,#30594,#30595,#30596),.UNSPECIFIED.,.F.,.F.,
(4,2,2,2,2,2,2,2,2,2,2,2,2,2,2,2,4),(-0.225338432560443,-0.216182593405909,
-0.180918656439139,-0.156950339943792,-0.140921103226935,-0.1298237820352,
-0.118153571207452,-0.114481377626862,-0.112295015626078,-0.110369884265102,
-0.10799225029725,-0.103463255811758,-0.092116061603562,-0.0805188447194234,
-0.0652099958826702,-0.0432219732389456,0.),.UNSPECIFIED.);
#855=B_SPLINE_CURVE_WITH_KNOTS('',3,(#30605,#30606,#30607,#30608,#30609,
#30610,#30611,#30612,#30613,#30614,#30615,#30616,#30617,#30618,#30619,#30620,
#30621,#30622,#30623,#30624,#30625,#30626,#30627,#30628,#30629,#30630,#30631,
#30632,#30633,#30634,#30635,#30636,#30637,#30638),.UNSPECIFIED.,.F.,.F.,
(4,2,2,2,2,2,2,2,2,2,2,2,2,2,2,2,4),(-0.225338432559121,-0.216182593404619,
-0.18091865643809,-0.156950339942956,-0.14092110322627,-0.129823782034653,
-0.118153571207027,-0.114481377626479,-0.112295015625724,-0.110369884264759,
-0.107992250296894,-0.103463255811428,-0.0921160616033008,-0.0805188447192374,
-0.0652099958825975,-0.0432219732389517,0.),.UNSPECIFIED.);
#856=B_SPLINE_CURVE_WITH_KNOTS('',3,(#30647,#30648,#30649,#30650,#30651,
#30652,#30653,#30654,#30655,#30656,#30657,#30658,#30659,#30660,#30661,#30662,
#30663,#30664,#30665,#30666,#30667,#30668,#30669,#30670,#30671,#30672,#30673,
#30674,#30675,#30676,#30677,#30678,#30679,#30680),.UNSPECIFIED.,.F.,.F.,
(4,2,2,2,2,2,2,2,2,2,2,2,2,2,2,2,4),(-0.225338432559561,-0.216182593405078,
-0.180918656438519,-0.156950339943348,-0.140921103226635,-0.12982378203501,
-0.118153571207387,-0.114481377626829,-0.112295015626078,-0.110369884265122,
-0.10799225029726,-0.103463255811752,-0.0921160616035431,-0.0805188447194093,
-0.0652099958827019,-0.0432219732389723,0.),.UNSPECIFIED.);
#857=B_SPLINE_CURVE_WITH_KNOTS('',3,(#30689,#30690,#30691,#30692,#30693,
#30694,#30695,#30696,#30697,#30698,#30699,#30700,#30701,#30702,#30703,#30704,
#30705,#30706,#30707,#30708,#30709,#30710,#30711,#30712,#30713,#30714,#30715,
#30716,#30717,#30718,#30719,#30720,#30721,#30722),.UNSPECIFIED.,.F.,.F.,
(4,2,2,2,2,2,2,2,2,2,2,2,2,2,2,2,4),(-0.225338432559738,-0.216182593405211,
-0.180918656438537,-0.156950339943277,-0.140921103226497,-0.129823782034835,
-0.11815357120718,-0.114481377626615,-0.112295015625857,-0.110369884264898,
-0.107992250297039,-0.103463255811543,-0.0921160616033831,-0.0805188447192948,
-0.0652099958826484,-0.0432219732389855,0.),.UNSPECIFIED.);
#858=B_SPLINE_CURVE_WITH_KNOTS('',3,(#30731,#30732,#30733,#30734,#30735,
#30736,#30737,#30738,#30739,#30740,#30741,#30742,#30743,#30744,#30745,#30746,
#30747,#30748,#30749,#30750,#30751,#30752,#30753,#30754,#30755,#30756,#30757,
#30758,#30759,#30760,#30761,#30762,#30763,#30764),.UNSPECIFIED.,.F.,.F.,
(4,2,2,2,2,2,2,2,2,2,2,2,2,2,2,2,4),(-0.225338432559396,-0.216182593405001,
-0.180918656438744,-0.15695033994371,-0.140921103227021,-0.129823782035391,
-0.118153571207753,-0.114481377627195,-0.112295015626432,-0.110369884265467,
-0.107992250297605,-0.103463255812088,-0.0921160616038249,-0.080518844719617,
-0.0652099958827568,-0.0432219732389323,0.),.UNSPECIFIED.);
#859=B_SPLINE_CURVE_WITH_KNOTS('',3,(#30773,#30774,#30775,#30776,#30777,
#30778,#30779,#30780,#30781,#30782,#30783,#30784,#30785,#30786,#30787,#30788,
#30789,#30790,#30791,#30792,#30793,#30794,#30795,#30796,#30797,#30798,#30799,
#30800,#30801,#30802,#30803,#30804,#30805,#30806),.UNSPECIFIED.,.F.,.F.,
(4,2,2,2,2,2,2,2,2,2,2,2,2,2,2,2,4),(-0.225338432560286,-0.216182593405743,
-0.180918656439008,-0.156950339943687,-0.140921103226838,-0.129823782035135,
-0.11815357120744,-0.114481377626867,-0.112295015626096,-0.110369884265129,
-0.107992250297272,-0.103463255811758,-0.0921160616035475,-0.0805188447194081,
-0.0652099958826912,-0.0432219732389774,0.),.UNSPECIFIED.);
#860=B_SPLINE_CURVE_WITH_KNOTS('',3,(#30815,#30816,#30817,#30818,#30819,
#30820,#30821,#30822,#30823,#30824,#30825,#30826,#30827,#30828,#30829,#30830,
#30831,#30832,#30833,#30834,#30835,#30836,#30837,#30838,#30839,#30840,#30841,
#30842,#30843,#30844,#30845,#30846,#30847,#30848),.UNSPECIFIED.,.F.,.F.,
(4,2,2,2,2,2,2,2,2,2,2,2,2,2,2,2,4),(-0.225338432557624,-0.216182593403256,
-0.180918656437128,-0.156950339942263,-0.14092110322575,-0.129823782034263,
-0.118153571206773,-0.114481377626263,-0.112295015625533,-0.110369884264596,
-0.107992250296765,-0.103463255811312,-0.0921160616032174,-0.0805188447191867,
-0.0652099958825827,-0.0432219732389505,0.),.UNSPECIFIED.);
#861=B_SPLINE_CURVE_WITH_KNOTS('',3,(#30857,#30858,#30859,#30860,#30861,
#30862,#30863,#30864,#30865,#30866,#30867,#30868,#30869,#30870,#30871,#30872,
#30873,#30874,#30875,#30876,#30877,#30878,#30879,#30880,#30881,#30882,#30883,
#30884,#30885,#30886,#30887,#30888,#30889,#30890),.UNSPECIFIED.,.F.,.F.,
(4,2,2,2,2,2,2,2,2,2,2,2,2,2,2,2,4),(-0.225338432559972,-0.216182593405463,
-0.180918656438837,-0.156950339943573,-0.140921103226747,-0.129823782035054,
-0.118153571207361,-0.114481377626792,-0.112295015626031,-0.110369884265071,
-0.107992250297217,-0.103463255811723,-0.0921160616035288,-0.0805188447194011,
-0.0652099958826789,-0.0432219732389621,0.),.UNSPECIFIED.);
#862=B_SPLINE_CURVE_WITH_KNOTS('',3,(#30899,#30900,#30901,#30902,#30903,
#30904,#30905,#30906,#30907,#30908,#30909,#30910,#30911,#30912,#30913,#30914,
#30915,#30916,#30917,#30918,#30919,#30920,#30921,#30922,#30923,#30924,#30925,
#30926,#30927,#30928,#30929,#30930,#30931,#30932),.UNSPECIFIED.,.F.,.F.,
(4,2,2,2,2,2,2,2,2,2,2,2,2,2,2,2,4),(-0.225338432559886,-0.216182593405346,
-0.180918656438623,-0.156950339943384,-0.140921103226634,-0.129823782034983,
-0.118153571207324,-0.11448137762676,-0.112295015626009,-0.110369884265057,
-0.1079922502972,-0.103463255811702,-0.0921160616035172,-0.080518844719388,
-0.0652099958826653,-0.0432219732389498,0.),.UNSPECIFIED.);
#863=B_SPLINE_CURVE_WITH_KNOTS('',3,(#30941,#30942,#30943,#30944,#30945,
#30946,#30947,#30948,#30949,#30950,#30951,#30952,#30953,#30954,#30955,#30956,
#30957,#30958,#30959,#30960,#30961,#30962,#30963,#30964,#30965,#30966,#30967,
#30968,#30969,#30970,#30971,#30972,#30973,#30974),.UNSPECIFIED.,.F.,.F.,
(4,2,2,2,2,2,2,2,2,2,2,2,2,2,2,2,4),(-0.225338432560165,-0.216182593405626,
-0.180918656438868,-0.156950339943628,-0.140921103226887,-0.12982378203525,
-0.118153571207617,-0.114481377627066,-0.112295015626281,-0.110369884265287,
-0.107992250297409,-0.103463255811908,-0.0921160616036701,-0.0805188447195032,
-0.0652099958827271,-0.0432219732389648,0.),.UNSPECIFIED.);
#864=B_SPLINE_CURVE_WITH_KNOTS('',3,(#30983,#30984,#30985,#30986,#30987,
#30988,#30989,#30990,#30991,#30992,#30993,#30994,#30995,#30996,#30997,#30998,
#30999,#31000,#31001,#31002,#31003,#31004,#31005,#31006,#31007,#31008,#31009,
#31010,#31011,#31012,#31013,#31014,#31015,#31016),.UNSPECIFIED.,.F.,.F.,
(4,2,2,2,2,2,2,2,2,2,2,2,2,2,2,2,4),(-0.225338432558513,-0.216182593404118,
-0.180918656437953,-0.156950339943,-0.14092110322638,-0.129823782034829,
-0.118153571207289,-0.114481377626764,-0.112295015626003,-0.110369884265039,
-0.10799225029719,-0.103463255811691,-0.0921160616035001,-0.0805188447193769,
-0.0652099958826662,-0.0432219732389656,0.),.UNSPECIFIED.);
#865=B_SPLINE_CURVE_WITH_KNOTS('',3,(#31025,#31026,#31027,#31028,#31029,
#31030,#31031,#31032,#31033,#31034,#31035,#31036,#31037,#31038,#31039,#31040,
#31041,#31042,#31043,#31044,#31045,#31046,#31047,#31048,#31049,#31050,#31051,
#31052,#31053,#31054,#31055,#31056,#31057,#31058),.UNSPECIFIED.,.F.,.F.,
(4,2,2,2,2,2,2,2,2,2,2,2,2,2,2,2,4),(-0.225338432558754,-0.21618259340434,
-0.18091865643812,-0.156950339943179,-0.140921103226598,-0.129823782035052,
-0.118153571207509,-0.114481377626976,-0.112295015626201,-0.110369884265216,
-0.107992250297339,-0.103463255811827,-0.0921160616036153,-0.0805188447194577,
-0.065209995882691,-0.0432219732389451,0.),.UNSPECIFIED.);
#866=B_SPLINE_CURVE_WITH_KNOTS('',3,(#31067,#31068,#31069,#31070,#31071,
#31072,#31073,#31074,#31075,#31076,#31077,#31078,#31079,#31080,#31081,#31082,
#31083,#31084,#31085,#31086,#31087,#31088,#31089,#31090,#31091,#31092,#31093,
#31094,#31095,#31096,#31097,#31098,#31099,#31100),.UNSPECIFIED.,.F.,.F.,
(4,2,2,2,2,2,2,2,2,2,2,2,2,2,2,2,4),(-0.225338432559566,-0.216182593405091,
-0.18091865643861,-0.156950339943494,-0.140921103226803,-0.129823782035189,
-0.118153571207577,-0.114481377627025,-0.11229501562625,-0.11036988426527,
-0.1079922502974,-0.103463255811888,-0.0921160616036564,-0.0805188447194867,
-0.0652099958827102,-0.0432219732389514,0.),.UNSPECIFIED.);
#867=B_SPLINE_CURVE_WITH_KNOTS('',3,(#31109,#31110,#31111,#31112,#31113,
#31114,#31115,#31116,#31117,#31118,#31119,#31120,#31121,#31122,#31123,#31124,
#31125,#31126,#31127,#31128,#31129,#31130,#31131,#31132,#31133,#31134,#31135,
#31136,#31137,#31138,#31139,#31140,#31141,#31142),.UNSPECIFIED.,.F.,.F.,
(4,2,2,2,2,2,2,2,2,2,2,2,2,2,2,2,4),(-0.225338432560737,-0.216182593406169,
-0.180918656439285,-0.156950339943892,-0.140921103227009,-0.129823782035269,
-0.118153571207521,-0.114481377626936,-0.112295015626147,-0.11036988426516,
-0.107992250297296,-0.103463255811794,-0.0921160616035909,-0.0805188447194464,
-0.0652099958826976,-0.0432219732389541,0.),.UNSPECIFIED.);
#868=B_SPLINE_CURVE_WITH_KNOTS('',3,(#31151,#31152,#31153,#31154,#31155,
#31156,#31157,#31158,#31159,#31160,#31161,#31162,#31163,#31164,#31165,#31166,
#31167,#31168,#31169,#31170,#31171,#31172,#31173,#31174,#31175,#31176,#31177,
#31178,#31179,#31180,#31181,#31182,#31183,#31184),.UNSPECIFIED.,.F.,.F.,
(4,2,2,2,2,2,2,2,2,2,2,2,2,2,2,2,4),(-0.225338432559896,-0.216182593405404,
-0.180918656438774,-0.156950339943504,-0.140921103226688,-0.129823782034989,
-0.118153571207288,-0.114481377626717,-0.112295015625947,-0.110369884264978,
-0.107992250297119,-0.103463255811626,-0.0921160616034505,-0.0805188447193407,
-0.0652099958826552,-0.0432219732389624,0.),.UNSPECIFIED.);
#869=B_SPLINE_CURVE_WITH_KNOTS('',3,(#31193,#31194,#31195,#31196,#31197,
#31198,#31199,#31200,#31201,#31202,#31203,#31204,#31205,#31206,#31207,#31208,
#31209,#31210,#31211,#31212,#31213,#31214,#31215,#31216,#31217,#31218,#31219,
#31220,#31221,#31222,#31223,#31224,#31225,#31226),.UNSPECIFIED.,.F.,.F.,
(4,2,2,2,2,2,2,2,2,2,2,2,2,2,2,2,4),(-0.225338432559856,-0.216182593405332,
-0.180918656438658,-0.156950339943401,-0.140921103226618,-0.129823782034946,
-0.118153571207272,-0.114481377626712,-0.11229501562595,-0.110369884264986,
-0.107992250297126,-0.103463255811634,-0.0921160616034556,-0.0805188447193506,
-0.0652099958826651,-0.0432219732389713,0.),.UNSPECIFIED.);
#870=B_SPLINE_CURVE_WITH_KNOTS('',3,(#31235,#31236,#31237,#31238,#31239,
#31240,#31241,#31242,#31243,#31244,#31245,#31246,#31247,#31248,#31249,#31250,
#31251,#31252,#31253,#31254,#31255,#31256,#31257,#31258,#31259,#31260,#31261,
#31262,#31263,#31264,#31265,#31266,#31267,#31268),.UNSPECIFIED.,.F.,.F.,
(4,2,2,2,2,2,2,2,2,2,2,2,2,2,2,2,4),(-0.225338432559793,-0.216182593405304,
-0.180918656438779,-0.156950339943631,-0.140921103226917,-0.129823782035281,
-0.118153571207644,-0.114481377627095,-0.112295015626322,-0.110369884265348,
-0.107992250297489,-0.10346325581197,-0.0921160616037223,-0.0805188447195313,
-0.0652099958827248,-0.0432219732389509,0.),.UNSPECIFIED.);
#871=B_SPLINE_CURVE_WITH_KNOTS('',3,(#31277,#31278,#31279,#31280,#31281,
#31282,#31283,#31284,#31285,#31286,#31287,#31288,#31289,#31290,#31291,#31292,
#31293,#31294,#31295,#31296,#31297,#31298,#31299,#31300,#31301,#31302,#31303,
#31304,#31305,#31306,#31307,#31308,#31309,#31310),.UNSPECIFIED.,.F.,.F.,
(4,2,2,2,2,2,2,2,2,2,2,2,2,2,2,2,4),(-0.225338432558185,-0.216182593403776,
-0.180918656437544,-0.156950339942601,-0.140921103226024,-0.129823782034494,
-0.118153571206967,-0.114481377626462,-0.112295015625713,-0.110369884264754,
-0.107992250296906,-0.103463255811428,-0.0921160616033045,-0.0805188447192422,
-0.0652099958826089,-0.0432219732389611,0.),.UNSPECIFIED.);
#872=B_SPLINE_CURVE_WITH_KNOTS('',3,(#31319,#31320,#31321,#31322,#31323,
#31324,#31325,#31326,#31327,#31328,#31329,#31330,#31331,#31332,#31333,#31334,
#31335,#31336,#31337,#31338,#31339,#31340,#31341,#31342,#31343,#31344,#31345,
#31346,#31347,#31348,#31349,#31350,#31351,#31352),.UNSPECIFIED.,.F.,.F.,
(4,2,2,2,2,2,2,2,2,2,2,2,2,2,2,2,4),(-0.22533843255964,-0.216182593405169,
-0.180918656438643,-0.156950339943465,-0.14092110322672,-0.12982378203507,
-0.118153571207417,-0.114481377626855,-0.112295015626077,-0.110369884265096,
-0.107992250297229,-0.10346325581173,-0.0921160616035346,-0.0805188447194051,
-0.0652099958826819,-0.0432219732389622,0.),.UNSPECIFIED.);
#873=B_SPLINE_CURVE_WITH_KNOTS('',3,(#31361,#31362,#31363,#31364,#31365,
#31366,#31367,#31368,#31369,#31370,#31371,#31372,#31373,#31374,#31375,#31376,
#31377,#31378,#31379,#31380,#31381,#31382,#31383,#31384,#31385,#31386,#31387,
#31388,#31389,#31390,#31391,#31392,#31393,#31394),.UNSPECIFIED.,.F.,.F.,
(4,2,2,2,2,2,2,2,2,2,2,2,2,2,2,2,4),(-0.225338432560957,-0.216182593406373,
-0.180918656439496,-0.156950339944078,-0.140921103227165,-0.129823782035403,
-0.118153571207639,-0.114481377627053,-0.11229501562626,-0.110369884265268,
-0.107992250297394,-0.103463255811882,-0.0921160616036502,-0.0805188447194852,
-0.0652099958827201,-0.0432219732389695,0.),.UNSPECIFIED.);
#874=B_SPLINE_CURVE_WITH_KNOTS('',3,(#31528,#31529,#31530,#31531,#31532,
#31533,#31534,#31535,#31536,#31537,#31538,#31539,#31540,#31541,#31542,#31543,
#31544,#31545,#31546,#31547,#31548,#31549,#31550,#31551,#31552,#31553,#31554,
#31555,#31556,#31557,#31558,#31559,#31560,#31561),.UNSPECIFIED.,.F.,.F.,
(4,2,2,2,2,2,2,2,2,2,2,2,2,2,2,2,4),(-0.225338432560343,-0.216182593405787,
-0.180918656438999,-0.156950339943695,-0.140921103226895,-0.129823782035217,
-0.118153571207545,-0.114481377627,-0.112295015626234,-0.110369884265269,
-0.10799225029742,-0.10346325581189,-0.0921160616036499,-0.0805188447194839,
-0.0652099958827262,-0.04322197323898,0.),.UNSPECIFIED.);
#888=VERTEX_POINT('',#3811);
#889=VERTEX_POINT('',#3812);
#890=VERTEX_POINT('',#3819);
#891=VERTEX_POINT('',#3821);
#892=VERTEX_POINT('',#3856);
#893=VERTEX_POINT('',#4047);
#894=VERTEX_POINT('',#4058);
#895=VERTEX_POINT('',#4249);
#896=VERTEX_POINT('',#4262);
#897=VERTEX_POINT('',#4456);
#898=VERTEX_POINT('',#4467);
#899=VERTEX_POINT('',#4479);
#900=VERTEX_POINT('',#4490);
#901=VERTEX_POINT('',#4501);
#902=VERTEX_POINT('',#4692);
#903=VERTEX_POINT('',#4703);
#904=VERTEX_POINT('',#4894);
#905=VERTEX_POINT('',#4905);
#906=VERTEX_POINT('',#5096);
#907=VERTEX_POINT('',#5290);
#908=VERTEX_POINT('',#5481);
#909=VERTEX_POINT('',#5493);
#910=VERTEX_POINT('',#5687);
#911=VERTEX_POINT('',#5881);
#912=VERTEX_POINT('',#6072);
#913=VERTEX_POINT('',#6085);
#914=VERTEX_POINT('',#6096);
#915=VERTEX_POINT('',#6290);
#916=VERTEX_POINT('',#6302);
#917=VERTEX_POINT('',#6493);
#918=VERTEX_POINT('',#6504);
#919=VERTEX_POINT('',#6695);
#920=VERTEX_POINT('',#6708);
#921=VERTEX_POINT('',#6902);
#922=VERTEX_POINT('',#6913);
#923=VERTEX_POINT('',#6925);
#924=VERTEX_POINT('',#6936);
#925=VERTEX_POINT('',#6947);
#926=VERTEX_POINT('',#7138);
#927=VERTEX_POINT('',#7329);
#928=VERTEX_POINT('',#7340);
#929=VERTEX_POINT('',#7351);
#930=VERTEX_POINT('',#7358);
#931=VERTEX_POINT('',#7360);
#932=VERTEX_POINT('',#7395);
#933=VERTEX_POINT('',#7586);
#934=VERTEX_POINT('',#7597);
#935=VERTEX_POINT('',#7788);
#936=VERTEX_POINT('',#7801);
#937=VERTEX_POINT('',#7995);
#938=VERTEX_POINT('',#8006);
#939=VERTEX_POINT('',#8018);
#940=VERTEX_POINT('',#8029);
#941=VERTEX_POINT('',#8040);
#942=VERTEX_POINT('',#8231);
#943=VERTEX_POINT('',#8242);
#944=VERTEX_POINT('',#8433);
#945=VERTEX_POINT('',#8444);
#946=VERTEX_POINT('',#8635);
#947=VERTEX_POINT('',#8829);
#948=VERTEX_POINT('',#9020);
#949=VERTEX_POINT('',#9032);
#950=VERTEX_POINT('',#9226);
#951=VERTEX_POINT('',#9420);
#952=VERTEX_POINT('',#9611);
#953=VERTEX_POINT('',#9624);
#954=VERTEX_POINT('',#9635);
#955=VERTEX_POINT('',#9829);
#956=VERTEX_POINT('',#9841);
#957=VERTEX_POINT('',#10032);
#958=VERTEX_POINT('',#10043);
#959=VERTEX_POINT('',#10234);
#960=VERTEX_POINT('',#10247);
#961=VERTEX_POINT('',#10441);
#962=VERTEX_POINT('',#10452);
#963=VERTEX_POINT('',#10464);
#964=VERTEX_POINT('',#10475);
#965=VERTEX_POINT('',#10486);
#966=VERTEX_POINT('',#10677);
#967=VERTEX_POINT('',#10868);
#968=VERTEX_POINT('',#10890);
#969=VERTEX_POINT('',#10891);
#970=VERTEX_POINT('',#11490);
#971=VERTEX_POINT('',#11492);
#972=VERTEX_POINT('',#11617);
#973=VERTEX_POINT('',#11808);
#974=VERTEX_POINT('',#12417);
#975=VERTEX_POINT('',#12910);
#976=VERTEX_POINT('',#13471);
#977=VERTEX_POINT('',#13662);
#978=VERTEX_POINT('',#13673);
#979=VERTEX_POINT('',#14174);
#980=VERTEX_POINT('',#14365);
#981=VERTEX_POINT('',#14376);
#982=VERTEX_POINT('',#14567);
#983=VERTEX_POINT('',#15040);
#984=VERTEX_POINT('',#15525);
#985=VERTEX_POINT('',#16018);
#986=VERTEX_POINT('',#16209);
#987=VERTEX_POINT('',#16670);
#988=VERTEX_POINT('',#17181);
#989=VERTEX_POINT('',#17772);
#990=VERTEX_POINT('',#17784);
#991=VERTEX_POINT('',#18303);
#992=VERTEX_POINT('',#18491);
#993=VERTEX_POINT('',#18962);
#994=VERTEX_POINT('',#19445);
#995=VERTEX_POINT('',#19636);
#996=VERTEX_POINT('',#19797);
#997=VERTEX_POINT('',#19799);
#998=VERTEX_POINT('',#19924);
#999=VERTEX_POINT('',#20115);
#1000=VERTEX_POINT('',#20708);
#1001=VERTEX_POINT('',#21193);
#1002=VERTEX_POINT('',#21732);
#1003=VERTEX_POINT('',#21923);
#1004=VERTEX_POINT('',#21934);
#1005=VERTEX_POINT('',#22409);
#1006=VERTEX_POINT('',#22600);
#1007=VERTEX_POINT('',#22611);
#1008=VERTEX_POINT('',#22802);
#1009=VERTEX_POINT('',#23275);
#1010=VERTEX_POINT('',#23750);
#1011=VERTEX_POINT('',#24293);
#1012=VERTEX_POINT('',#24484);
#1013=VERTEX_POINT('',#24945);
#1014=VERTEX_POINT('',#25450);
#1015=VERTEX_POINT('',#25641);
#1016=VERTEX_POINT('',#25832);
#1017=VERTEX_POINT('',#25844);
#1018=VERTEX_POINT('',#26315);
#1019=VERTEX_POINT('',#26503);
#1020=VERTEX_POINT('',#27455);
#1021=VERTEX_POINT('',#27457);
#1022=VERTEX_POINT('',#27461);
#1023=VERTEX_POINT('',#27463);
#1024=VERTEX_POINT('',#27465);
#1025=VERTEX_POINT('',#28518);
#1026=VERTEX_POINT('',#29758);
#1027=VERTEX_POINT('',#29759);
#1028=VERTEX_POINT('',#29794);
#1029=VERTEX_POINT('',#29796);
#1030=VERTEX_POINT('',#29800);
#1031=VERTEX_POINT('',#29801);
#1032=VERTEX_POINT('',#29836);
#1033=VERTEX_POINT('',#29838);
#1034=VERTEX_POINT('',#29842);
#1035=VERTEX_POINT('',#29843);
#1036=VERTEX_POINT('',#29878);
#1037=VERTEX_POINT('',#29880);
#1038=VERTEX_POINT('',#29884);
#1039=VERTEX_POINT('',#29885);
#1040=VERTEX_POINT('',#29920);
#1041=VERTEX_POINT('',#29922);
#1042=VERTEX_POINT('',#29926);
#1043=VERTEX_POINT('',#29927);
#1044=VERTEX_POINT('',#29962);
#1045=VERTEX_POINT('',#29964);
#1046=VERTEX_POINT('',#29968);
#1047=VERTEX_POINT('',#29969);
#1048=VERTEX_POINT('',#30004);
#1049=VERTEX_POINT('',#30006);
#1050=VERTEX_POINT('',#30010);
#1051=VERTEX_POINT('',#30011);
#1052=VERTEX_POINT('',#30046);
#1053=VERTEX_POINT('',#30048);
#1054=VERTEX_POINT('',#30052);
#1055=VERTEX_POINT('',#30053);
#1056=VERTEX_POINT('',#30088);
#1057=VERTEX_POINT('',#30090);
#1058=VERTEX_POINT('',#30094);
#1059=VERTEX_POINT('',#30095);
#1060=VERTEX_POINT('',#30130);
#1061=VERTEX_POINT('',#30132);
#1062=VERTEX_POINT('',#30136);
#1063=VERTEX_POINT('',#30137);
#1064=VERTEX_POINT('',#30158);
#1065=VERTEX_POINT('',#30160);
#1066=VERTEX_POINT('',#30162);
#1067=VERTEX_POINT('',#30183);
#1068=VERTEX_POINT('',#30184);
#1069=VERTEX_POINT('',#30219);
#1070=VERTEX_POINT('',#30221);
#1071=VERTEX_POINT('',#30225);
#1072=VERTEX_POINT('',#30226);
#1073=VERTEX_POINT('',#30261);
#1074=VERTEX_POINT('',#30263);
#1075=VERTEX_POINT('',#30267);
#1076=VERTEX_POINT('',#30268);
#1077=VERTEX_POINT('',#30303);
#1078=VERTEX_POINT('',#30305);
#1079=VERTEX_POINT('',#30309);
#1080=VERTEX_POINT('',#30310);
#1081=VERTEX_POINT('',#30345);
#1082=VERTEX_POINT('',#30347);
#1083=VERTEX_POINT('',#30351);
#1084=VERTEX_POINT('',#30352);
#1085=VERTEX_POINT('',#30387);
#1086=VERTEX_POINT('',#30389);
#1087=VERTEX_POINT('',#30393);
#1088=VERTEX_POINT('',#30394);
#1089=VERTEX_POINT('',#30429);
#1090=VERTEX_POINT('',#30431);
#1091=VERTEX_POINT('',#30435);
#1092=VERTEX_POINT('',#30436);
#1093=VERTEX_POINT('',#30471);
#1094=VERTEX_POINT('',#30473);
#1095=VERTEX_POINT('',#30477);
#1096=VERTEX_POINT('',#30478);
#1097=VERTEX_POINT('',#30513);
#1098=VERTEX_POINT('',#30515);
#1099=VERTEX_POINT('',#30519);
#1100=VERTEX_POINT('',#30520);
#1101=VERTEX_POINT('',#30555);
#1102=VERTEX_POINT('',#30557);
#1103=VERTEX_POINT('',#30561);
#1104=VERTEX_POINT('',#30562);
#1105=VERTEX_POINT('',#30597);
#1106=VERTEX_POINT('',#30599);
#1107=VERTEX_POINT('',#30603);
#1108=VERTEX_POINT('',#30604);
#1109=VERTEX_POINT('',#30639);
#1110=VERTEX_POINT('',#30641);
#1111=VERTEX_POINT('',#30645);
#1112=VERTEX_POINT('',#30646);
#1113=VERTEX_POINT('',#30681);
#1114=VERTEX_POINT('',#30683);
#1115=VERTEX_POINT('',#30687);
#1116=VERTEX_POINT('',#30688);
#1117=VERTEX_POINT('',#30723);
#1118=VERTEX_POINT('',#30725);
#1119=VERTEX_POINT('',#30729);
#1120=VERTEX_POINT('',#30730);
#1121=VERTEX_POINT('',#30765);
#1122=VERTEX_POINT('',#30767);
#1123=VERTEX_POINT('',#30771);
#1124=VERTEX_POINT('',#30772);
#1125=VERTEX_POINT('',#30807);
#1126=VERTEX_POINT('',#30809);
#1127=VERTEX_POINT('',#30813);
#1128=VERTEX_POINT('',#30814);
#1129=VERTEX_POINT('',#30849);
#1130=VERTEX_POINT('',#30851);
#1131=VERTEX_POINT('',#30855);
#1132=VERTEX_POINT('',#30856);
#1133=VERTEX_POINT('',#30891);
#1134=VERTEX_POINT('',#30893);
#1135=VERTEX_POINT('',#30897);
#1136=VERTEX_POINT('',#30898);
#1137=VERTEX_POINT('',#30933);
#1138=VERTEX_POINT('',#30935);
#1139=VERTEX_POINT('',#30939);
#1140=VERTEX_POINT('',#30940);
#1141=VERTEX_POINT('',#30975);
#1142=VERTEX_POINT('',#30977);
#1143=VERTEX_POINT('',#30981);
#1144=VERTEX_POINT('',#30982);
#1145=VERTEX_POINT('',#31017);
#1146=VERTEX_POINT('',#31019);
#1147=VERTEX_POINT('',#31023);
#1148=VERTEX_POINT('',#31024);
#1149=VERTEX_POINT('',#31059);
#1150=VERTEX_POINT('',#31061);
#1151=VERTEX_POINT('',#31065);
#1152=VERTEX_POINT('',#31066);
#1153=VERTEX_POINT('',#31101);
#1154=VERTEX_POINT('',#31103);
#1155=VERTEX_POINT('',#31107);
#1156=VERTEX_POINT('',#31108);
#1157=VERTEX_POINT('',#31143);
#1158=VERTEX_POINT('',#31145);
#1159=VERTEX_POINT('',#31149);
#1160=VERTEX_POINT('',#31150);
#1161=VERTEX_POINT('',#31185);
#1162=VERTEX_POINT('',#31187);
#1163=VERTEX_POINT('',#31191);
#1164=VERTEX_POINT('',#31192);
#1165=VERTEX_POINT('',#31227);
#1166=VERTEX_POINT('',#31229);
#1167=VERTEX_POINT('',#31233);
#1168=VERTEX_POINT('',#31234);
#1169=VERTEX_POINT('',#31269);
#1170=VERTEX_POINT('',#31271);
#1171=VERTEX_POINT('',#31275);
#1172=VERTEX_POINT('',#31276);
#1173=VERTEX_POINT('',#31311);
#1174=VERTEX_POINT('',#31313);
#1175=VERTEX_POINT('',#31317);
#1176=VERTEX_POINT('',#31318);
#1177=VERTEX_POINT('',#31353);
#1178=VERTEX_POINT('',#31355);
#1179=VERTEX_POINT('',#31359);
#1180=VERTEX_POINT('',#31360);
#1181=VERTEX_POINT('',#31395);
#1182=VERTEX_POINT('',#31397);
#1183=VERTEX_POINT('',#31439);
#1184=VERTEX_POINT('',#31441);
#1185=VERTEX_POINT('',#31445);
#1186=VERTEX_POINT('',#31526);
#1231=EDGE_CURVE('',#888,#889,#701,.T.);
#1232=EDGE_CURVE('',#889,#890,#545,.F.);
#1233=EDGE_CURVE('',#890,#891,#702,.T.);
#1234=EDGE_CURVE('',#891,#892,#703,.T.);
#1235=EDGE_CURVE('',#892,#893,#704,.T.);
#1236=EDGE_CURVE('',#893,#894,#705,.T.);
#1237=EDGE_CURVE('',#894,#895,#706,.T.);
#1238=EDGE_CURVE('',#895,#896,#707,.T.);
#1239=EDGE_CURVE('',#896,#897,#708,.T.);
#1240=EDGE_CURVE('',#897,#898,#709,.T.);
#1241=EDGE_CURVE('',#898,#899,#710,.T.);
#1242=EDGE_CURVE('',#899,#900,#711,.T.);
#1243=EDGE_CURVE('',#900,#901,#712,.T.);
#1244=EDGE_CURVE('',#901,#902,#713,.T.);
#1245=EDGE_CURVE('',#902,#903,#714,.T.);
#1246=EDGE_CURVE('',#903,#904,#715,.T.);
#1247=EDGE_CURVE('',#904,#905,#716,.T.);
#1248=EDGE_CURVE('',#905,#906,#717,.T.);
#1249=EDGE_CURVE('',#906,#907,#718,.T.);
#1250=EDGE_CURVE('',#907,#908,#719,.T.);
#1251=EDGE_CURVE('',#908,#909,#720,.T.);
#1252=EDGE_CURVE('',#909,#910,#721,.T.);
#1253=EDGE_CURVE('',#910,#911,#722,.T.);
#1254=EDGE_CURVE('',#911,#912,#723,.T.);
#1255=EDGE_CURVE('',#912,#913,#724,.T.);
#1256=EDGE_CURVE('',#913,#914,#725,.T.);
#1257=EDGE_CURVE('',#914,#915,#726,.T.);
#1258=EDGE_CURVE('',#915,#916,#727,.T.);
#1259=EDGE_CURVE('',#916,#917,#728,.T.);
#1260=EDGE_CURVE('',#917,#918,#729,.T.);
#1261=EDGE_CURVE('',#918,#919,#730,.T.);
#1262=EDGE_CURVE('',#919,#920,#731,.T.);
#1263=EDGE_CURVE('',#920,#921,#732,.T.);
#1264=EDGE_CURVE('',#921,#922,#733,.T.);
#1265=EDGE_CURVE('',#922,#923,#734,.T.);
#1266=EDGE_CURVE('',#923,#924,#735,.T.);
#1267=EDGE_CURVE('',#924,#925,#736,.T.);
#1268=EDGE_CURVE('',#925,#926,#737,.T.);
#1269=EDGE_CURVE('',#926,#927,#738,.T.);
#1270=EDGE_CURVE('',#927,#928,#739,.T.);
#1271=EDGE_CURVE('',#928,#929,#740,.T.);
#1272=EDGE_CURVE('',#930,#929,#546,.F.);
#1273=EDGE_CURVE('',#930,#931,#741,.T.);
#1274=EDGE_CURVE('',#931,#932,#742,.T.);
#1275=EDGE_CURVE('',#932,#933,#743,.T.);
#1276=EDGE_CURVE('',#933,#934,#744,.T.);
#1277=EDGE_CURVE('',#934,#935,#745,.T.);
#1278=EDGE_CURVE('',#935,#936,#746,.T.);
#1279=EDGE_CURVE('',#936,#937,#747,.T.);
#1280=EDGE_CURVE('',#937,#938,#748,.T.);
#1281=EDGE_CURVE('',#938,#939,#749,.T.);
#1282=EDGE_CURVE('',#939,#940,#750,.T.);
#1283=EDGE_CURVE('',#940,#941,#751,.T.);
#1284=EDGE_CURVE('',#941,#942,#752,.T.);
#1285=EDGE_CURVE('',#942,#943,#753,.T.);
#1286=EDGE_CURVE('',#943,#944,#754,.T.);
#1287=EDGE_CURVE('',#944,#945,#755,.T.);
#1288=EDGE_CURVE('',#945,#946,#756,.T.);
#1289=EDGE_CURVE('',#946,#947,#757,.T.);
#1290=EDGE_CURVE('',#947,#948,#758,.T.);
#1291=EDGE_CURVE('',#948,#949,#759,.T.);
#1292=EDGE_CURVE('',#949,#950,#760,.T.);
#1293=EDGE_CURVE('',#950,#951,#761,.T.);
#1294=EDGE_CURVE('',#951,#952,#762,.T.);
#1295=EDGE_CURVE('',#952,#953,#763,.T.);
#1296=EDGE_CURVE('',#953,#954,#764,.T.);
#1297=EDGE_CURVE('',#954,#955,#765,.T.);
#1298=EDGE_CURVE('',#955,#956,#766,.T.);
#1299=EDGE_CURVE('',#956,#957,#767,.T.);
#1300=EDGE_CURVE('',#957,#958,#768,.T.);
#1301=EDGE_CURVE('',#958,#959,#769,.T.);
#1302=EDGE_CURVE('',#959,#960,#770,.T.);
#1303=EDGE_CURVE('',#960,#961,#771,.T.);
#1304=EDGE_CURVE('',#961,#962,#772,.T.);
#1305=EDGE_CURVE('',#962,#963,#773,.T.);
#1306=EDGE_CURVE('',#963,#964,#774,.T.);
#1307=EDGE_CURVE('',#964,#965,#775,.T.);
#1308=EDGE_CURVE('',#965,#966,#776,.T.);
#1309=EDGE_CURVE('',#966,#967,#777,.T.);
#1310=EDGE_CURVE('',#967,#888,#778,.T.);
#1311=EDGE_CURVE('',#968,#969,#779,.F.);
#1312=EDGE_CURVE('',#970,#968,#547,.T.);
#1313=EDGE_CURVE('',#970,#971,#780,.T.);
#1314=EDGE_CURVE('',#971,#972,#781,.T.);
#1315=EDGE_CURVE('',#972,#973,#782,.T.);
#1316=EDGE_CURVE('',#973,#974,#783,.T.);
#1317=EDGE_CURVE('',#974,#975,#784,.T.);
#1318=EDGE_CURVE('',#975,#976,#785,.T.);
#1319=EDGE_CURVE('',#976,#977,#786,.T.);
#1320=EDGE_CURVE('',#977,#978,#787,.T.);
#1321=EDGE_CURVE('',#978,#979,#788,.T.);
#1322=EDGE_CURVE('',#979,#980,#789,.T.);
#1323=EDGE_CURVE('',#980,#981,#790,.T.);
#1324=EDGE_CURVE('',#981,#982,#791,.T.);
#1325=EDGE_CURVE('',#982,#983,#792,.T.);
#1326=EDGE_CURVE('',#983,#984,#793,.T.);
#1327=EDGE_CURVE('',#984,#985,#794,.T.);
#1328=EDGE_CURVE('',#985,#986,#795,.T.);
#1329=EDGE_CURVE('',#986,#987,#796,.T.);
#1330=EDGE_CURVE('',#987,#988,#797,.T.);
#1331=EDGE_CURVE('',#988,#989,#798,.T.);
#1332=EDGE_CURVE('',#989,#990,#799,.T.);
#1333=EDGE_CURVE('',#990,#991,#800,.T.);
#1334=EDGE_CURVE('',#991,#992,#801,.T.);
#1335=EDGE_CURVE('',#992,#993,#802,.T.);
#1336=EDGE_CURVE('',#993,#994,#803,.T.);
#1337=EDGE_CURVE('',#994,#995,#804,.T.);
#1338=EDGE_CURVE('',#996,#995,#548,.T.);
#1339=EDGE_CURVE('',#997,#996,#805,.T.);
#1340=EDGE_CURVE('',#998,#997,#806,.T.);
#1341=EDGE_CURVE('',#999,#998,#807,.F.);
#1342=EDGE_CURVE('',#1000,#999,#808,.F.);
#1343=EDGE_CURVE('',#1001,#1000,#809,.F.);
#1344=EDGE_CURVE('',#1002,#1001,#810,.T.);
#1345=EDGE_CURVE('',#1003,#1002,#811,.T.);
#1346=EDGE_CURVE('',#1004,#1003,#812,.F.);
#1347=EDGE_CURVE('',#1005,#1004,#813,.T.);
#1348=EDGE_CURVE('',#1006,#1005,#814,.T.);
#1349=EDGE_CURVE('',#1007,#1006,#815,.T.);
#1350=EDGE_CURVE('',#1008,#1007,#816,.F.);
#1351=EDGE_CURVE('',#1009,#1008,#817,.F.);
#1352=EDGE_CURVE('',#1010,#1009,#818,.F.);
#1353=EDGE_CURVE('',#1011,#1010,#819,.T.);
#1354=EDGE_CURVE('',#1012,#1011,#820,.F.);
#1355=EDGE_CURVE('',#1013,#1012,#821,.F.);
#1356=EDGE_CURVE('',#1014,#1013,#822,.T.);
#1357=EDGE_CURVE('',#1015,#1014,#823,.T.);
#1358=EDGE_CURVE('',#1016,#1015,#824,.T.);
#1359=EDGE_CURVE('',#1017,#1016,#825,.F.);
#1360=EDGE_CURVE('',#1018,#1017,#826,.T.);
#1361=EDGE_CURVE('',#1019,#1018,#827,.F.);
#1362=EDGE_CURVE('',#969,#1019,#828,.F.);
#1363=EDGE_CURVE('',#1020,#1020,#549,.T.);
#1364=EDGE_CURVE('',#1020,#1021,#105,.T.);
#1365=EDGE_CURVE('',#1021,#1021,#550,.T.);
#1366=EDGE_CURVE('',#1022,#1022,#551,.T.);
#1367=EDGE_CURVE('',#1022,#1023,#106,.T.);
#1368=EDGE_CURVE('',#1024,#1023,#552,.T.);
#1369=EDGE_CURVE('',#1023,#1024,#553,.T.);
#1370=EDGE_CURVE('',#929,#996,#829,.T.);
#1371=EDGE_CURVE('',#1025,#890,#830,.T.);
#1372=EDGE_CURVE('',#1025,#968,#831,.T.);
#1373=EDGE_CURVE('',#995,#930,#832,.T.);
#1374=EDGE_CURVE('',#889,#970,#833,.T.);
#1375=EDGE_CURVE('',#1026,#1027,#834,.T.);
#1376=EDGE_CURVE('',#1028,#1026,#107,.T.);
#1377=EDGE_CURVE('',#1029,#1028,#554,.T.);
#1378=EDGE_CURVE('',#1027,#1029,#108,.T.);
#1379=EDGE_CURVE('',#1030,#1031,#835,.T.);
#1380=EDGE_CURVE('',#1032,#1030,#109,.T.);
#1381=EDGE_CURVE('',#1033,#1032,#555,.T.);
#1382=EDGE_CURVE('',#1031,#1033,#110,.T.);
#1383=EDGE_CURVE('',#1034,#1035,#836,.T.);
#1384=EDGE_CURVE('',#1036,#1034,#111,.T.);
#1385=EDGE_CURVE('',#1037,#1036,#556,.T.);
#1386=EDGE_CURVE('',#1035,#1037,#112,.T.);
#1387=EDGE_CURVE('',#1038,#1039,#837,.T.);
#1388=EDGE_CURVE('',#1040,#1038,#113,.T.);
#1389=EDGE_CURVE('',#1041,#1040,#557,.T.);
#1390=EDGE_CURVE('',#1039,#1041,#114,.T.);
#1391=EDGE_CURVE('',#1042,#1043,#838,.T.);
#1392=EDGE_CURVE('',#1044,#1042,#115,.T.);
#1393=EDGE_CURVE('',#1045,#1044,#558,.T.);
#1394=EDGE_CURVE('',#1043,#1045,#116,.T.);
#1395=EDGE_CURVE('',#1046,#1047,#839,.T.);
#1396=EDGE_CURVE('',#1048,#1046,#117,.T.);
#1397=EDGE_CURVE('',#1049,#1048,#559,.T.);
#1398=EDGE_CURVE('',#1047,#1049,#118,.T.);
#1399=EDGE_CURVE('',#1050,#1051,#840,.T.);
#1400=EDGE_CURVE('',#1052,#1050,#119,.T.);
#1401=EDGE_CURVE('',#1053,#1052,#560,.T.);
#1402=EDGE_CURVE('',#1051,#1053,#120,.T.);
#1403=EDGE_CURVE('',#1054,#1055,#841,.T.);
#1404=EDGE_CURVE('',#1056,#1054,#121,.T.);
#1405=EDGE_CURVE('',#1057,#1056,#561,.T.);
#1406=EDGE_CURVE('',#1055,#1057,#122,.T.);
#1407=EDGE_CURVE('',#1058,#1059,#842,.T.);
#1408=EDGE_CURVE('',#1060,#1058,#123,.T.);
#1409=EDGE_CURVE('',#1061,#1060,#562,.T.);
#1410=EDGE_CURVE('',#1059,#1061,#124,.T.);
#1411=EDGE_CURVE('',#1062,#1063,#843,.T.);
#1412=EDGE_CURVE('',#1064,#1062,#125,.T.);
#1413=EDGE_CURVE('',#1065,#1064,#563,.T.);
#1414=EDGE_CURVE('',#1066,#1065,#126,.T.);
#1415=EDGE_CURVE('',#1063,#1066,#844,.T.);
#1416=EDGE_CURVE('',#1067,#1068,#845,.T.);
#1417=EDGE_CURVE('',#1069,#1067,#127,.T.);
#1418=EDGE_CURVE('',#1070,#1069,#564,.T.);
#1419=EDGE_CURVE('',#1068,#1070,#128,.T.);
#1420=EDGE_CURVE('',#1071,#1072,#846,.T.);
#1421=EDGE_CURVE('',#1073,#1071,#129,.T.);
#1422=EDGE_CURVE('',#1074,#1073,#565,.T.);
#1423=EDGE_CURVE('',#1072,#1074,#130,.T.);
#1424=EDGE_CURVE('',#1075,#1076,#847,.T.);
#1425=EDGE_CURVE('',#1077,#1075,#131,.T.);
#1426=EDGE_CURVE('',#1078,#1077,#566,.T.);
#1427=EDGE_CURVE('',#1076,#1078,#132,.T.);
#1428=EDGE_CURVE('',#1079,#1080,#848,.T.);
#1429=EDGE_CURVE('',#1081,#1079,#133,.T.);
#1430=EDGE_CURVE('',#1082,#1081,#567,.T.);
#1431=EDGE_CURVE('',#1080,#1082,#134,.T.);
#1432=EDGE_CURVE('',#1083,#1084,#849,.T.);
#1433=EDGE_CURVE('',#1085,#1083,#135,.T.);
#1434=EDGE_CURVE('',#1086,#1085,#568,.T.);
#1435=EDGE_CURVE('',#1084,#1086,#136,.T.);
#1436=EDGE_CURVE('',#1087,#1088,#850,.T.);
#1437=EDGE_CURVE('',#1089,#1087,#137,.T.);
#1438=EDGE_CURVE('',#1090,#1089,#569,.T.);
#1439=EDGE_CURVE('',#1088,#1090,#138,.T.);
#1440=EDGE_CURVE('',#1091,#1092,#851,.T.);
#1441=EDGE_CURVE('',#1093,#1091,#139,.T.);
#1442=EDGE_CURVE('',#1094,#1093,#570,.T.);
#1443=EDGE_CURVE('',#1092,#1094,#140,.T.);
#1444=EDGE_CURVE('',#1095,#1096,#852,.T.);
#1445=EDGE_CURVE('',#1097,#1095,#141,.T.);
#1446=EDGE_CURVE('',#1098,#1097,#571,.T.);
#1447=EDGE_CURVE('',#1096,#1098,#142,.T.);
#1448=EDGE_CURVE('',#1099,#1100,#853,.T.);
#1449=EDGE_CURVE('',#1101,#1099,#143,.T.);
#1450=EDGE_CURVE('',#1102,#1101,#572,.T.);
#1451=EDGE_CURVE('',#1100,#1102,#144,.T.);
#1452=EDGE_CURVE('',#1103,#1104,#854,.T.);
#1453=EDGE_CURVE('',#1105,#1103,#145,.T.);
#1454=EDGE_CURVE('',#1106,#1105,#573,.T.);
#1455=EDGE_CURVE('',#1104,#1106,#146,.T.);
#1456=EDGE_CURVE('',#1107,#1108,#855,.T.);
#1457=EDGE_CURVE('',#1109,#1107,#147,.T.);
#1458=EDGE_CURVE('',#1110,#1109,#574,.T.);
#1459=EDGE_CURVE('',#1108,#1110,#148,.T.);
#1460=EDGE_CURVE('',#1111,#1112,#856,.T.);
#1461=EDGE_CURVE('',#1113,#1111,#149,.T.);
#1462=EDGE_CURVE('',#1114,#1113,#575,.T.);
#1463=EDGE_CURVE('',#1112,#1114,#150,.T.);
#1464=EDGE_CURVE('',#1115,#1116,#857,.T.);
#1465=EDGE_CURVE('',#1117,#1115,#151,.T.);
#1466=EDGE_CURVE('',#1118,#1117,#576,.T.);
#1467=EDGE_CURVE('',#1116,#1118,#152,.T.);
#1468=EDGE_CURVE('',#1119,#1120,#858,.T.);
#1469=EDGE_CURVE('',#1121,#1119,#153,.T.);
#1470=EDGE_CURVE('',#1122,#1121,#577,.T.);
#1471=EDGE_CURVE('',#1120,#1122,#154,.T.);
#1472=EDGE_CURVE('',#1123,#1124,#859,.T.);
#1473=EDGE_CURVE('',#1125,#1123,#155,.T.);
#1474=EDGE_CURVE('',#1126,#1125,#578,.T.);
#1475=EDGE_CURVE('',#1124,#1126,#156,.T.);
#1476=EDGE_CURVE('',#1127,#1128,#860,.T.);
#1477=EDGE_CURVE('',#1129,#1127,#157,.T.);
#1478=EDGE_CURVE('',#1130,#1129,#579,.T.);
#1479=EDGE_CURVE('',#1128,#1130,#158,.T.);
#1480=EDGE_CURVE('',#1131,#1132,#861,.T.);
#1481=EDGE_CURVE('',#1133,#1131,#159,.T.);
#1482=EDGE_CURVE('',#1134,#1133,#580,.T.);
#1483=EDGE_CURVE('',#1132,#1134,#160,.T.);
#1484=EDGE_CURVE('',#1135,#1136,#862,.T.);
#1485=EDGE_CURVE('',#1137,#1135,#161,.T.);
#1486=EDGE_CURVE('',#1138,#1137,#581,.T.);
#1487=EDGE_CURVE('',#1136,#1138,#162,.T.);
#1488=EDGE_CURVE('',#1139,#1140,#863,.T.);
#1489=EDGE_CURVE('',#1141,#1139,#163,.T.);
#1490=EDGE_CURVE('',#1142,#1141,#582,.T.);
#1491=EDGE_CURVE('',#1140,#1142,#164,.T.);
#1492=EDGE_CURVE('',#1143,#1144,#864,.T.);
#1493=EDGE_CURVE('',#1145,#1143,#165,.T.);
#1494=EDGE_CURVE('',#1146,#1145,#583,.T.);
#1495=EDGE_CURVE('',#1144,#1146,#166,.T.);
#1496=EDGE_CURVE('',#1147,#1148,#865,.T.);
#1497=EDGE_CURVE('',#1149,#1147,#167,.T.);
#1498=EDGE_CURVE('',#1150,#1149,#584,.T.);
#1499=EDGE_CURVE('',#1148,#1150,#168,.T.);
#1500=EDGE_CURVE('',#1151,#1152,#866,.T.);
#1501=EDGE_CURVE('',#1153,#1151,#169,.T.);
#1502=EDGE_CURVE('',#1154,#1153,#585,.T.);
#1503=EDGE_CURVE('',#1152,#1154,#170,.T.);
#1504=EDGE_CURVE('',#1155,#1156,#867,.T.);
#1505=EDGE_CURVE('',#1157,#1155,#171,.T.);
#1506=EDGE_CURVE('',#1158,#1157,#586,.T.);
#1507=EDGE_CURVE('',#1156,#1158,#172,.T.);
#1508=EDGE_CURVE('',#1159,#1160,#868,.T.);
#1509=EDGE_CURVE('',#1161,#1159,#173,.T.);
#1510=EDGE_CURVE('',#1162,#1161,#587,.T.);
#1511=EDGE_CURVE('',#1160,#1162,#174,.T.);
#1512=EDGE_CURVE('',#1163,#1164,#869,.T.);
#1513=EDGE_CURVE('',#1165,#1163,#175,.T.);
#1514=EDGE_CURVE('',#1166,#1165,#588,.T.);
#1515=EDGE_CURVE('',#1164,#1166,#176,.T.);
#1516=EDGE_CURVE('',#1167,#1168,#870,.T.);
#1517=EDGE_CURVE('',#1169,#1167,#177,.T.);
#1518=EDGE_CURVE('',#1170,#1169,#589,.T.);
#1519=EDGE_CURVE('',#1168,#1170,#178,.T.);
#1520=EDGE_CURVE('',#1171,#1172,#871,.T.);
#1521=EDGE_CURVE('',#1173,#1171,#179,.T.);
#1522=EDGE_CURVE('',#1174,#1173,#590,.T.);
#1523=EDGE_CURVE('',#1172,#1174,#180,.T.);
#1524=EDGE_CURVE('',#1175,#1176,#872,.T.);
#1525=EDGE_CURVE('',#1177,#1175,#181,.T.);
#1526=EDGE_CURVE('',#1178,#1177,#591,.T.);
#1527=EDGE_CURVE('',#1176,#1178,#182,.T.);
#1528=EDGE_CURVE('',#1179,#1180,#873,.T.);
#1529=EDGE_CURVE('',#1181,#1179,#183,.T.);
#1530=EDGE_CURVE('',#1182,#1181,#592,.T.);
#1531=EDGE_CURVE('',#1180,#1182,#184,.T.);
#1532=EDGE_CURVE('',#1033,#1028,#593,.T.);
#1533=EDGE_CURVE('',#1037,#1032,#594,.T.);
#1534=EDGE_CURVE('',#1041,#1036,#595,.T.);
#1535=EDGE_CURVE('',#1045,#1040,#596,.T.);
#1536=EDGE_CURVE('',#1049,#1044,#597,.T.);
#1537=EDGE_CURVE('',#1053,#1048,#598,.T.);
#1538=EDGE_CURVE('',#1057,#1052,#599,.T.);
#1539=EDGE_CURVE('',#1061,#1056,#600,.T.);
#1540=EDGE_CURVE('',#1065,#1060,#601,.T.);
#1541=EDGE_CURVE('',#1070,#1064,#602,.T.);
#1542=EDGE_CURVE('',#1074,#1069,#603,.T.);
#1543=EDGE_CURVE('',#1078,#1073,#604,.T.);
#1544=EDGE_CURVE('',#1082,#1077,#605,.T.);
#1545=EDGE_CURVE('',#1086,#1081,#606,.T.);
#1546=EDGE_CURVE('',#1090,#1085,#607,.T.);
#1547=EDGE_CURVE('',#1094,#1089,#608,.T.);
#1548=EDGE_CURVE('',#1098,#1093,#609,.T.);
#1549=EDGE_CURVE('',#1102,#1097,#610,.T.);
#1550=EDGE_CURVE('',#1106,#1101,#611,.T.);
#1551=EDGE_CURVE('',#1110,#1105,#612,.T.);
#1552=EDGE_CURVE('',#1114,#1109,#613,.T.);
#1553=EDGE_CURVE('',#1118,#1113,#614,.T.);
#1554=EDGE_CURVE('',#1122,#1117,#615,.T.);
#1555=EDGE_CURVE('',#1126,#1121,#616,.T.);
#1556=EDGE_CURVE('',#1130,#1125,#617,.T.);
#1557=EDGE_CURVE('',#1134,#1129,#618,.T.);
#1558=EDGE_CURVE('',#1138,#1133,#619,.T.);
#1559=EDGE_CURVE('',#1142,#1137,#620,.T.);
#1560=EDGE_CURVE('',#1146,#1141,#621,.T.);
#1561=EDGE_CURVE('',#1150,#1145,#622,.T.);
#1562=EDGE_CURVE('',#1154,#1149,#623,.T.);
#1563=EDGE_CURVE('',#1158,#1153,#624,.T.);
#1564=EDGE_CURVE('',#1162,#1157,#625,.T.);
#1565=EDGE_CURVE('',#1166,#1161,#626,.T.);
#1566=EDGE_CURVE('',#1170,#1165,#627,.T.);
#1567=EDGE_CURVE('',#1174,#1169,#628,.T.);
#1568=EDGE_CURVE('',#1178,#1173,#629,.T.);
#1569=EDGE_CURVE('',#1182,#1177,#630,.T.);
#1570=EDGE_CURVE('',#1183,#1181,#631,.T.);
#1571=EDGE_CURVE('',#1183,#1184,#632,.T.);
#1572=EDGE_CURVE('',#1029,#1184,#633,.T.);
#1573=EDGE_CURVE('',#1185,#1179,#634,.T.);
#1574=EDGE_CURVE('',#1185,#1183,#185,.T.);
#1575=EDGE_CURVE('',#1180,#1175,#635,.T.);
#1576=EDGE_CURVE('',#1176,#1171,#636,.T.);
#1577=EDGE_CURVE('',#1172,#1167,#637,.T.);
#1578=EDGE_CURVE('',#1168,#1163,#638,.T.);
#1579=EDGE_CURVE('',#1164,#1159,#639,.T.);
#1580=EDGE_CURVE('',#1160,#1155,#640,.T.);
#1581=EDGE_CURVE('',#1156,#1151,#641,.T.);
#1582=EDGE_CURVE('',#1152,#1147,#642,.T.);
#1583=EDGE_CURVE('',#1148,#1143,#643,.T.);
#1584=EDGE_CURVE('',#1144,#1139,#644,.T.);
#1585=EDGE_CURVE('',#1140,#1135,#645,.T.);
#1586=EDGE_CURVE('',#1136,#1131,#646,.T.);
#1587=EDGE_CURVE('',#1132,#1127,#647,.T.);
#1588=EDGE_CURVE('',#1128,#1123,#648,.T.);
#1589=EDGE_CURVE('',#1124,#1119,#649,.T.);
#1590=EDGE_CURVE('',#1120,#1115,#650,.T.);
#1591=EDGE_CURVE('',#1116,#1111,#651,.T.);
#1592=EDGE_CURVE('',#1112,#1107,#652,.T.);
#1593=EDGE_CURVE('',#1108,#1103,#653,.T.);
#1594=EDGE_CURVE('',#1104,#1099,#654,.T.);
#1595=EDGE_CURVE('',#1100,#1095,#655,.T.);
#1596=EDGE_CURVE('',#1096,#1091,#656,.T.);
#1597=EDGE_CURVE('',#1092,#1087,#657,.T.);
#1598=EDGE_CURVE('',#1088,#1083,#658,.T.);
#1599=EDGE_CURVE('',#1084,#1079,#659,.T.);
#1600=EDGE_CURVE('',#1080,#1075,#660,.T.);
#1601=EDGE_CURVE('',#1076,#1071,#661,.T.);
#1602=EDGE_CURVE('',#1072,#1067,#662,.T.);
#1603=EDGE_CURVE('',#1068,#1062,#663,.T.);
#1604=EDGE_CURVE('',#1066,#1058,#664,.T.);
#1605=EDGE_CURVE('',#1059,#1054,#665,.T.);
#1606=EDGE_CURVE('',#1055,#1050,#666,.T.);
#1607=EDGE_CURVE('',#1051,#1046,#667,.T.);
#1608=EDGE_CURVE('',#1047,#1042,#668,.T.);
#1609=EDGE_CURVE('',#1043,#1038,#669,.T.);
#1610=EDGE_CURVE('',#1039,#1034,#670,.T.);
#1611=EDGE_CURVE('',#1035,#1030,#671,.T.);
#1612=EDGE_CURVE('',#1031,#1026,#672,.T.);
#1613=EDGE_CURVE('',#1024,#1063,#673,.T.);
#1614=EDGE_CURVE('',#1027,#1186,#674,.T.);
#1615=EDGE_CURVE('',#1186,#1185,#874,.T.);
#1616=EDGE_CURVE('',#1184,#1186,#186,.T.);
#1687=ORIENTED_EDGE('',*,*,#1231,.T.);
#1688=ORIENTED_EDGE('',*,*,#1232,.T.);
#1689=ORIENTED_EDGE('',*,*,#1233,.T.);
#1690=ORIENTED_EDGE('',*,*,#1234,.T.);
#1691=ORIENTED_EDGE('',*,*,#1235,.T.);
#1692=ORIENTED_EDGE('',*,*,#1236,.T.);
#1693=ORIENTED_EDGE('',*,*,#1237,.T.);
#1694=ORIENTED_EDGE('',*,*,#1238,.T.);
#1695=ORIENTED_EDGE('',*,*,#1239,.T.);
#1696=ORIENTED_EDGE('',*,*,#1240,.T.);
#1697=ORIENTED_EDGE('',*,*,#1241,.T.);
#1698=ORIENTED_EDGE('',*,*,#1242,.T.);
#1699=ORIENTED_EDGE('',*,*,#1243,.T.);
#1700=ORIENTED_EDGE('',*,*,#1244,.T.);
#1701=ORIENTED_EDGE('',*,*,#1245,.T.);
#1702=ORIENTED_EDGE('',*,*,#1246,.T.);
#1703=ORIENTED_EDGE('',*,*,#1247,.T.);
#1704=ORIENTED_EDGE('',*,*,#1248,.T.);
#1705=ORIENTED_EDGE('',*,*,#1249,.T.);
#1706=ORIENTED_EDGE('',*,*,#1250,.T.);
#1707=ORIENTED_EDGE('',*,*,#1251,.T.);
#1708=ORIENTED_EDGE('',*,*,#1252,.T.);
#1709=ORIENTED_EDGE('',*,*,#1253,.T.);
#1710=ORIENTED_EDGE('',*,*,#1254,.T.);
#1711=ORIENTED_EDGE('',*,*,#1255,.T.);
#1712=ORIENTED_EDGE('',*,*,#1256,.T.);
#1713=ORIENTED_EDGE('',*,*,#1257,.T.);
#1714=ORIENTED_EDGE('',*,*,#1258,.T.);
#1715=ORIENTED_EDGE('',*,*,#1259,.T.);
#1716=ORIENTED_EDGE('',*,*,#1260,.T.);
#1717=ORIENTED_EDGE('',*,*,#1261,.T.);
#1718=ORIENTED_EDGE('',*,*,#1262,.T.);
#1719=ORIENTED_EDGE('',*,*,#1263,.T.);
#1720=ORIENTED_EDGE('',*,*,#1264,.T.);
#1721=ORIENTED_EDGE('',*,*,#1265,.T.);
#1722=ORIENTED_EDGE('',*,*,#1266,.T.);
#1723=ORIENTED_EDGE('',*,*,#1267,.T.);
#1724=ORIENTED_EDGE('',*,*,#1268,.T.);
#1725=ORIENTED_EDGE('',*,*,#1269,.T.);
#1726=ORIENTED_EDGE('',*,*,#1270,.T.);
#1727=ORIENTED_EDGE('',*,*,#1271,.T.);
#1728=ORIENTED_EDGE('',*,*,#1272,.F.);
#1729=ORIENTED_EDGE('',*,*,#1273,.T.);
#1730=ORIENTED_EDGE('',*,*,#1274,.T.);
#1731=ORIENTED_EDGE('',*,*,#1275,.T.);
#1732=ORIENTED_EDGE('',*,*,#1276,.T.);
#1733=ORIENTED_EDGE('',*,*,#1277,.T.);
#1734=ORIENTED_EDGE('',*,*,#1278,.T.);
#1735=ORIENTED_EDGE('',*,*,#1279,.T.);
#1736=ORIENTED_EDGE('',*,*,#1280,.T.);
#1737=ORIENTED_EDGE('',*,*,#1281,.T.);
#1738=ORIENTED_EDGE('',*,*,#1282,.T.);
#1739=ORIENTED_EDGE('',*,*,#1283,.T.);
#1740=ORIENTED_EDGE('',*,*,#1284,.T.);
#1741=ORIENTED_EDGE('',*,*,#1285,.T.);
#1742=ORIENTED_EDGE('',*,*,#1286,.T.);
#1743=ORIENTED_EDGE('',*,*,#1287,.T.);
#1744=ORIENTED_EDGE('',*,*,#1288,.T.);
#1745=ORIENTED_EDGE('',*,*,#1289,.T.);
#1746=ORIENTED_EDGE('',*,*,#1290,.T.);
#1747=ORIENTED_EDGE('',*,*,#1291,.T.);
#1748=ORIENTED_EDGE('',*,*,#1292,.T.);
#1749=ORIENTED_EDGE('',*,*,#1293,.T.);
#1750=ORIENTED_EDGE('',*,*,#1294,.T.);
#1751=ORIENTED_EDGE('',*,*,#1295,.T.);
#1752=ORIENTED_EDGE('',*,*,#1296,.T.);
#1753=ORIENTED_EDGE('',*,*,#1297,.T.);
#1754=ORIENTED_EDGE('',*,*,#1298,.T.);
#1755=ORIENTED_EDGE('',*,*,#1299,.T.);
#1756=ORIENTED_EDGE('',*,*,#1300,.T.);
#1757=ORIENTED_EDGE('',*,*,#1301,.T.);
#1758=ORIENTED_EDGE('',*,*,#1302,.T.);
#1759=ORIENTED_EDGE('',*,*,#1303,.T.);
#1760=ORIENTED_EDGE('',*,*,#1304,.T.);
#1761=ORIENTED_EDGE('',*,*,#1305,.T.);
#1762=ORIENTED_EDGE('',*,*,#1306,.T.);
#1763=ORIENTED_EDGE('',*,*,#1307,.T.);
#1764=ORIENTED_EDGE('',*,*,#1308,.T.);
#1765=ORIENTED_EDGE('',*,*,#1309,.T.);
#1766=ORIENTED_EDGE('',*,*,#1310,.T.);
#1767=ORIENTED_EDGE('',*,*,#1311,.F.);
#1768=ORIENTED_EDGE('',*,*,#1312,.F.);
#1769=ORIENTED_EDGE('',*,*,#1313,.T.);
#1770=ORIENTED_EDGE('',*,*,#1314,.T.);
#1771=ORIENTED_EDGE('',*,*,#1315,.T.);
#1772=ORIENTED_EDGE('',*,*,#1316,.T.);
#1773=ORIENTED_EDGE('',*,*,#1317,.T.);
#1774=ORIENTED_EDGE('',*,*,#1318,.T.);
#1775=ORIENTED_EDGE('',*,*,#1319,.T.);
#1776=ORIENTED_EDGE('',*,*,#1320,.T.);
#1777=ORIENTED_EDGE('',*,*,#1321,.T.);
#1778=ORIENTED_EDGE('',*,*,#1322,.T.);
#1779=ORIENTED_EDGE('',*,*,#1323,.T.);
#1780=ORIENTED_EDGE('',*,*,#1324,.T.);
#1781=ORIENTED_EDGE('',*,*,#1325,.T.);
#1782=ORIENTED_EDGE('',*,*,#1326,.T.);
#1783=ORIENTED_EDGE('',*,*,#1327,.T.);
#1784=ORIENTED_EDGE('',*,*,#1328,.T.);
#1785=ORIENTED_EDGE('',*,*,#1329,.T.);
#1786=ORIENTED_EDGE('',*,*,#1330,.T.);
#1787=ORIENTED_EDGE('',*,*,#1331,.T.);
#1788=ORIENTED_EDGE('',*,*,#1332,.T.);
#1789=ORIENTED_EDGE('',*,*,#1333,.T.);
#1790=ORIENTED_EDGE('',*,*,#1334,.T.);
#1791=ORIENTED_EDGE('',*,*,#1335,.T.);
#1792=ORIENTED_EDGE('',*,*,#1336,.T.);
#1793=ORIENTED_EDGE('',*,*,#1337,.T.);
#1794=ORIENTED_EDGE('',*,*,#1338,.F.);
#1795=ORIENTED_EDGE('',*,*,#1339,.F.);
#1796=ORIENTED_EDGE('',*,*,#1340,.F.);
#1797=ORIENTED_EDGE('',*,*,#1341,.F.);
#1798=ORIENTED_EDGE('',*,*,#1342,.F.);
#1799=ORIENTED_EDGE('',*,*,#1343,.F.);
#1800=ORIENTED_EDGE('',*,*,#1344,.F.);
#1801=ORIENTED_EDGE('',*,*,#1345,.F.);
#1802=ORIENTED_EDGE('',*,*,#1346,.F.);
#1803=ORIENTED_EDGE('',*,*,#1347,.F.);
#1804=ORIENTED_EDGE('',*,*,#1348,.F.);
#1805=ORIENTED_EDGE('',*,*,#1349,.F.);
#1806=ORIENTED_EDGE('',*,*,#1350,.F.);
#1807=ORIENTED_EDGE('',*,*,#1351,.F.);
#1808=ORIENTED_EDGE('',*,*,#1352,.F.);
#1809=ORIENTED_EDGE('',*,*,#1353,.F.);
#1810=ORIENTED_EDGE('',*,*,#1354,.F.);
#1811=ORIENTED_EDGE('',*,*,#1355,.F.);
#1812=ORIENTED_EDGE('',*,*,#1356,.F.);
#1813=ORIENTED_EDGE('',*,*,#1357,.F.);
#1814=ORIENTED_EDGE('',*,*,#1358,.F.);
#1815=ORIENTED_EDGE('',*,*,#1359,.F.);
#1816=ORIENTED_EDGE('',*,*,#1360,.F.);
#1817=ORIENTED_EDGE('',*,*,#1361,.F.);
#1818=ORIENTED_EDGE('',*,*,#1362,.F.);
#1819=ORIENTED_EDGE('',*,*,#1363,.F.);
#1820=ORIENTED_EDGE('',*,*,#1364,.T.);
#1821=ORIENTED_EDGE('',*,*,#1365,.F.);
#1822=ORIENTED_EDGE('',*,*,#1364,.F.);
#1823=ORIENTED_EDGE('',*,*,#1366,.F.);
#1824=ORIENTED_EDGE('',*,*,#1367,.T.);
#1825=ORIENTED_EDGE('',*,*,#1368,.F.);
#1826=ORIENTED_EDGE('',*,*,#1369,.F.);
#1827=ORIENTED_EDGE('',*,*,#1367,.F.);
#1828=ORIENTED_EDGE('',*,*,#1366,.T.);
#1829=ORIENTED_EDGE('',*,*,#1365,.T.);
#1830=ORIENTED_EDGE('',*,*,#1370,.F.);
#1831=ORIENTED_EDGE('',*,*,#1271,.F.);
#1832=ORIENTED_EDGE('',*,*,#1270,.F.);
#1833=ORIENTED_EDGE('',*,*,#1269,.F.);
#1834=ORIENTED_EDGE('',*,*,#1268,.F.);
#1835=ORIENTED_EDGE('',*,*,#1267,.F.);
#1836=ORIENTED_EDGE('',*,*,#1266,.F.);
#1837=ORIENTED_EDGE('',*,*,#1265,.F.);
#1838=ORIENTED_EDGE('',*,*,#1264,.F.);
#1839=ORIENTED_EDGE('',*,*,#1263,.F.);
#1840=ORIENTED_EDGE('',*,*,#1262,.F.);
#1841=ORIENTED_EDGE('',*,*,#1261,.F.);
#1842=ORIENTED_EDGE('',*,*,#1260,.F.);
#1843=ORIENTED_EDGE('',*,*,#1259,.F.);
#1844=ORIENTED_EDGE('',*,*,#1258,.F.);
#1845=ORIENTED_EDGE('',*,*,#1257,.F.);
#1846=ORIENTED_EDGE('',*,*,#1256,.F.);
#1847=ORIENTED_EDGE('',*,*,#1255,.F.);
#1848=ORIENTED_EDGE('',*,*,#1254,.F.);
#1849=ORIENTED_EDGE('',*,*,#1253,.F.);
#1850=ORIENTED_EDGE('',*,*,#1252,.F.);
#1851=ORIENTED_EDGE('',*,*,#1251,.F.);
#1852=ORIENTED_EDGE('',*,*,#1250,.F.);
#1853=ORIENTED_EDGE('',*,*,#1249,.F.);
#1854=ORIENTED_EDGE('',*,*,#1248,.F.);
#1855=ORIENTED_EDGE('',*,*,#1247,.F.);
#1856=ORIENTED_EDGE('',*,*,#1246,.F.);
#1857=ORIENTED_EDGE('',*,*,#1245,.F.);
#1858=ORIENTED_EDGE('',*,*,#1244,.F.);
#1859=ORIENTED_EDGE('',*,*,#1243,.F.);
#1860=ORIENTED_EDGE('',*,*,#1242,.F.);
#1861=ORIENTED_EDGE('',*,*,#1241,.F.);
#1862=ORIENTED_EDGE('',*,*,#1240,.F.);
#1863=ORIENTED_EDGE('',*,*,#1239,.F.);
#1864=ORIENTED_EDGE('',*,*,#1238,.F.);
#1865=ORIENTED_EDGE('',*,*,#1237,.F.);
#1866=ORIENTED_EDGE('',*,*,#1236,.F.);
#1867=ORIENTED_EDGE('',*,*,#1235,.F.);
#1868=ORIENTED_EDGE('',*,*,#1234,.F.);
#1869=ORIENTED_EDGE('',*,*,#1233,.F.);
#1870=ORIENTED_EDGE('',*,*,#1371,.F.);
#1871=ORIENTED_EDGE('',*,*,#1372,.T.);
#1872=ORIENTED_EDGE('',*,*,#1311,.T.);
#1873=ORIENTED_EDGE('',*,*,#1362,.T.);
#1874=ORIENTED_EDGE('',*,*,#1361,.T.);
#1875=ORIENTED_EDGE('',*,*,#1360,.T.);
#1876=ORIENTED_EDGE('',*,*,#1359,.T.);
#1877=ORIENTED_EDGE('',*,*,#1358,.T.);
#1878=ORIENTED_EDGE('',*,*,#1357,.T.);
#1879=ORIENTED_EDGE('',*,*,#1356,.T.);
#1880=ORIENTED_EDGE('',*,*,#1355,.T.);
#1881=ORIENTED_EDGE('',*,*,#1354,.T.);
#1882=ORIENTED_EDGE('',*,*,#1353,.T.);
#1883=ORIENTED_EDGE('',*,*,#1352,.T.);
#1884=ORIENTED_EDGE('',*,*,#1351,.T.);
#1885=ORIENTED_EDGE('',*,*,#1350,.T.);
#1886=ORIENTED_EDGE('',*,*,#1349,.T.);
#1887=ORIENTED_EDGE('',*,*,#1348,.T.);
#1888=ORIENTED_EDGE('',*,*,#1347,.T.);
#1889=ORIENTED_EDGE('',*,*,#1346,.T.);
#1890=ORIENTED_EDGE('',*,*,#1345,.T.);
#1891=ORIENTED_EDGE('',*,*,#1344,.T.);
#1892=ORIENTED_EDGE('',*,*,#1343,.T.);
#1893=ORIENTED_EDGE('',*,*,#1342,.T.);
#1894=ORIENTED_EDGE('',*,*,#1341,.T.);
#1895=ORIENTED_EDGE('',*,*,#1340,.T.);
#1896=ORIENTED_EDGE('',*,*,#1339,.T.);
#1897=ORIENTED_EDGE('',*,*,#1373,.F.);
#1898=ORIENTED_EDGE('',*,*,#1337,.F.);
#1899=ORIENTED_EDGE('',*,*,#1336,.F.);
#1900=ORIENTED_EDGE('',*,*,#1335,.F.);
#1901=ORIENTED_EDGE('',*,*,#1334,.F.);
#1902=ORIENTED_EDGE('',*,*,#1333,.F.);
#1903=ORIENTED_EDGE('',*,*,#1332,.F.);
#1904=ORIENTED_EDGE('',*,*,#1331,.F.);
#1905=ORIENTED_EDGE('',*,*,#1330,.F.);
#1906=ORIENTED_EDGE('',*,*,#1329,.F.);
#1907=ORIENTED_EDGE('',*,*,#1328,.F.);
#1908=ORIENTED_EDGE('',*,*,#1327,.F.);
#1909=ORIENTED_EDGE('',*,*,#1326,.F.);
#1910=ORIENTED_EDGE('',*,*,#1325,.F.);
#1911=ORIENTED_EDGE('',*,*,#1324,.F.);
#1912=ORIENTED_EDGE('',*,*,#1323,.F.);
#1913=ORIENTED_EDGE('',*,*,#1322,.F.);
#1914=ORIENTED_EDGE('',*,*,#1321,.F.);
#1915=ORIENTED_EDGE('',*,*,#1320,.F.);
#1916=ORIENTED_EDGE('',*,*,#1319,.F.);
#1917=ORIENTED_EDGE('',*,*,#1318,.F.);
#1918=ORIENTED_EDGE('',*,*,#1317,.F.);
#1919=ORIENTED_EDGE('',*,*,#1316,.F.);
#1920=ORIENTED_EDGE('',*,*,#1315,.F.);
#1921=ORIENTED_EDGE('',*,*,#1314,.F.);
#1922=ORIENTED_EDGE('',*,*,#1313,.F.);
#1923=ORIENTED_EDGE('',*,*,#1374,.F.);
#1924=ORIENTED_EDGE('',*,*,#1231,.F.);
#1925=ORIENTED_EDGE('',*,*,#1310,.F.);
#1926=ORIENTED_EDGE('',*,*,#1309,.F.);
#1927=ORIENTED_EDGE('',*,*,#1308,.F.);
#1928=ORIENTED_EDGE('',*,*,#1307,.F.);
#1929=ORIENTED_EDGE('',*,*,#1306,.F.);
#1930=ORIENTED_EDGE('',*,*,#1305,.F.);
#1931=ORIENTED_EDGE('',*,*,#1304,.F.);
#1932=ORIENTED_EDGE('',*,*,#1303,.F.);
#1933=ORIENTED_EDGE('',*,*,#1302,.F.);
#1934=ORIENTED_EDGE('',*,*,#1301,.F.);
#1935=ORIENTED_EDGE('',*,*,#1300,.F.);
#1936=ORIENTED_EDGE('',*,*,#1299,.F.);
#1937=ORIENTED_EDGE('',*,*,#1298,.F.);
#1938=ORIENTED_EDGE('',*,*,#1297,.F.);
#1939=ORIENTED_EDGE('',*,*,#1296,.F.);
#1940=ORIENTED_EDGE('',*,*,#1295,.F.);
#1941=ORIENTED_EDGE('',*,*,#1294,.F.);
#1942=ORIENTED_EDGE('',*,*,#1293,.F.);
#1943=ORIENTED_EDGE('',*,*,#1292,.F.);
#1944=ORIENTED_EDGE('',*,*,#1291,.F.);
#1945=ORIENTED_EDGE('',*,*,#1290,.F.);
#1946=ORIENTED_EDGE('',*,*,#1289,.F.);
#1947=ORIENTED_EDGE('',*,*,#1288,.F.);
#1948=ORIENTED_EDGE('',*,*,#1287,.F.);
#1949=ORIENTED_EDGE('',*,*,#1286,.F.);
#1950=ORIENTED_EDGE('',*,*,#1285,.F.);
#1951=ORIENTED_EDGE('',*,*,#1284,.F.);
#1952=ORIENTED_EDGE('',*,*,#1283,.F.);
#1953=ORIENTED_EDGE('',*,*,#1282,.F.);
#1954=ORIENTED_EDGE('',*,*,#1281,.F.);
#1955=ORIENTED_EDGE('',*,*,#1280,.F.);
#1956=ORIENTED_EDGE('',*,*,#1279,.F.);
#1957=ORIENTED_EDGE('',*,*,#1278,.F.);
#1958=ORIENTED_EDGE('',*,*,#1277,.F.);
#1959=ORIENTED_EDGE('',*,*,#1276,.F.);
#1960=ORIENTED_EDGE('',*,*,#1275,.F.);
#1961=ORIENTED_EDGE('',*,*,#1274,.F.);
#1962=ORIENTED_EDGE('',*,*,#1273,.F.);
#1963=ORIENTED_EDGE('',*,*,#1375,.F.);
#1964=ORIENTED_EDGE('',*,*,#1376,.F.);
#1965=ORIENTED_EDGE('',*,*,#1377,.F.);
#1966=ORIENTED_EDGE('',*,*,#1378,.F.);
#1967=ORIENTED_EDGE('',*,*,#1379,.F.);
#1968=ORIENTED_EDGE('',*,*,#1380,.F.);
#1969=ORIENTED_EDGE('',*,*,#1381,.F.);
#1970=ORIENTED_EDGE('',*,*,#1382,.F.);
#1971=ORIENTED_EDGE('',*,*,#1383,.F.);
#1972=ORIENTED_EDGE('',*,*,#1384,.F.);
#1973=ORIENTED_EDGE('',*,*,#1385,.F.);
#1974=ORIENTED_EDGE('',*,*,#1386,.F.);
#1975=ORIENTED_EDGE('',*,*,#1387,.F.);
#1976=ORIENTED_EDGE('',*,*,#1388,.F.);
#1977=ORIENTED_EDGE('',*,*,#1389,.F.);
#1978=ORIENTED_EDGE('',*,*,#1390,.F.);
#1979=ORIENTED_EDGE('',*,*,#1391,.F.);
#1980=ORIENTED_EDGE('',*,*,#1392,.F.);
#1981=ORIENTED_EDGE('',*,*,#1393,.F.);
#1982=ORIENTED_EDGE('',*,*,#1394,.F.);
#1983=ORIENTED_EDGE('',*,*,#1395,.F.);
#1984=ORIENTED_EDGE('',*,*,#1396,.F.);
#1985=ORIENTED_EDGE('',*,*,#1397,.F.);
#1986=ORIENTED_EDGE('',*,*,#1398,.F.);
#1987=ORIENTED_EDGE('',*,*,#1399,.F.);
#1988=ORIENTED_EDGE('',*,*,#1400,.F.);
#1989=ORIENTED_EDGE('',*,*,#1401,.F.);
#1990=ORIENTED_EDGE('',*,*,#1402,.F.);
#1991=ORIENTED_EDGE('',*,*,#1403,.F.);
#1992=ORIENTED_EDGE('',*,*,#1404,.F.);
#1993=ORIENTED_EDGE('',*,*,#1405,.F.);
#1994=ORIENTED_EDGE('',*,*,#1406,.F.);
#1995=ORIENTED_EDGE('',*,*,#1407,.F.);
#1996=ORIENTED_EDGE('',*,*,#1408,.F.);
#1997=ORIENTED_EDGE('',*,*,#1409,.F.);
#1998=ORIENTED_EDGE('',*,*,#1410,.F.);
#1999=ORIENTED_EDGE('',*,*,#1411,.F.);
#2000=ORIENTED_EDGE('',*,*,#1412,.F.);
#2001=ORIENTED_EDGE('',*,*,#1413,.F.);
#2002=ORIENTED_EDGE('',*,*,#1414,.F.);
#2003=ORIENTED_EDGE('',*,*,#1415,.F.);
#2004=ORIENTED_EDGE('',*,*,#1416,.F.);
#2005=ORIENTED_EDGE('',*,*,#1417,.F.);
#2006=ORIENTED_EDGE('',*,*,#1418,.F.);
#2007=ORIENTED_EDGE('',*,*,#1419,.F.);
#2008=ORIENTED_EDGE('',*,*,#1420,.F.);
#2009=ORIENTED_EDGE('',*,*,#1421,.F.);
#2010=ORIENTED_EDGE('',*,*,#1422,.F.);
#2011=ORIENTED_EDGE('',*,*,#1423,.F.);
#2012=ORIENTED_EDGE('',*,*,#1424,.F.);
#2013=ORIENTED_EDGE('',*,*,#1425,.F.);
#2014=ORIENTED_EDGE('',*,*,#1426,.F.);
#2015=ORIENTED_EDGE('',*,*,#1427,.F.);
#2016=ORIENTED_EDGE('',*,*,#1428,.F.);
#2017=ORIENTED_EDGE('',*,*,#1429,.F.);
#2018=ORIENTED_EDGE('',*,*,#1430,.F.);
#2019=ORIENTED_EDGE('',*,*,#1431,.F.);
#2020=ORIENTED_EDGE('',*,*,#1432,.F.);
#2021=ORIENTED_EDGE('',*,*,#1433,.F.);
#2022=ORIENTED_EDGE('',*,*,#1434,.F.);
#2023=ORIENTED_EDGE('',*,*,#1435,.F.);
#2024=ORIENTED_EDGE('',*,*,#1436,.F.);
#2025=ORIENTED_EDGE('',*,*,#1437,.F.);
#2026=ORIENTED_EDGE('',*,*,#1438,.F.);
#2027=ORIENTED_EDGE('',*,*,#1439,.F.);
#2028=ORIENTED_EDGE('',*,*,#1440,.F.);
#2029=ORIENTED_EDGE('',*,*,#1441,.F.);
#2030=ORIENTED_EDGE('',*,*,#1442,.F.);
#2031=ORIENTED_EDGE('',*,*,#1443,.F.);
#2032=ORIENTED_EDGE('',*,*,#1444,.F.);
#2033=ORIENTED_EDGE('',*,*,#1445,.F.);
#2034=ORIENTED_EDGE('',*,*,#1446,.F.);
#2035=ORIENTED_EDGE('',*,*,#1447,.F.);
#2036=ORIENTED_EDGE('',*,*,#1448,.F.);
#2037=ORIENTED_EDGE('',*,*,#1449,.F.);
#2038=ORIENTED_EDGE('',*,*,#1450,.F.);
#2039=ORIENTED_EDGE('',*,*,#1451,.F.);
#2040=ORIENTED_EDGE('',*,*,#1452,.F.);
#2041=ORIENTED_EDGE('',*,*,#1453,.F.);
#2042=ORIENTED_EDGE('',*,*,#1454,.F.);
#2043=ORIENTED_EDGE('',*,*,#1455,.F.);
#2044=ORIENTED_EDGE('',*,*,#1456,.F.);
#2045=ORIENTED_EDGE('',*,*,#1457,.F.);
#2046=ORIENTED_EDGE('',*,*,#1458,.F.);
#2047=ORIENTED_EDGE('',*,*,#1459,.F.);
#2048=ORIENTED_EDGE('',*,*,#1460,.F.);
#2049=ORIENTED_EDGE('',*,*,#1461,.F.);
#2050=ORIENTED_EDGE('',*,*,#1462,.F.);
#2051=ORIENTED_EDGE('',*,*,#1463,.F.);
#2052=ORIENTED_EDGE('',*,*,#1464,.F.);
#2053=ORIENTED_EDGE('',*,*,#1465,.F.);
#2054=ORIENTED_EDGE('',*,*,#1466,.F.);
#2055=ORIENTED_EDGE('',*,*,#1467,.F.);
#2056=ORIENTED_EDGE('',*,*,#1468,.F.);
#2057=ORIENTED_EDGE('',*,*,#1469,.F.);
#2058=ORIENTED_EDGE('',*,*,#1470,.F.);
#2059=ORIENTED_EDGE('',*,*,#1471,.F.);
#2060=ORIENTED_EDGE('',*,*,#1472,.F.);
#2061=ORIENTED_EDGE('',*,*,#1473,.F.);
#2062=ORIENTED_EDGE('',*,*,#1474,.F.);
#2063=ORIENTED_EDGE('',*,*,#1475,.F.);
#2064=ORIENTED_EDGE('',*,*,#1476,.F.);
#2065=ORIENTED_EDGE('',*,*,#1477,.F.);
#2066=ORIENTED_EDGE('',*,*,#1478,.F.);
#2067=ORIENTED_EDGE('',*,*,#1479,.F.);
#2068=ORIENTED_EDGE('',*,*,#1480,.F.);
#2069=ORIENTED_EDGE('',*,*,#1481,.F.);
#2070=ORIENTED_EDGE('',*,*,#1482,.F.);
#2071=ORIENTED_EDGE('',*,*,#1483,.F.);
#2072=ORIENTED_EDGE('',*,*,#1484,.F.);
#2073=ORIENTED_EDGE('',*,*,#1485,.F.);
#2074=ORIENTED_EDGE('',*,*,#1486,.F.);
#2075=ORIENTED_EDGE('',*,*,#1487,.F.);
#2076=ORIENTED_EDGE('',*,*,#1488,.F.);
#2077=ORIENTED_EDGE('',*,*,#1489,.F.);
#2078=ORIENTED_EDGE('',*,*,#1490,.F.);
#2079=ORIENTED_EDGE('',*,*,#1491,.F.);
#2080=ORIENTED_EDGE('',*,*,#1492,.F.);
#2081=ORIENTED_EDGE('',*,*,#1493,.F.);
#2082=ORIENTED_EDGE('',*,*,#1494,.F.);
#2083=ORIENTED_EDGE('',*,*,#1495,.F.);
#2084=ORIENTED_EDGE('',*,*,#1496,.F.);
#2085=ORIENTED_EDGE('',*,*,#1497,.F.);
#2086=ORIENTED_EDGE('',*,*,#1498,.F.);
#2087=ORIENTED_EDGE('',*,*,#1499,.F.);
#2088=ORIENTED_EDGE('',*,*,#1500,.F.);
#2089=ORIENTED_EDGE('',*,*,#1501,.F.);
#2090=ORIENTED_EDGE('',*,*,#1502,.F.);
#2091=ORIENTED_EDGE('',*,*,#1503,.F.);
#2092=ORIENTED_EDGE('',*,*,#1504,.F.);
#2093=ORIENTED_EDGE('',*,*,#1505,.F.);
#2094=ORIENTED_EDGE('',*,*,#1506,.F.);
#2095=ORIENTED_EDGE('',*,*,#1507,.F.);
#2096=ORIENTED_EDGE('',*,*,#1508,.F.);
#2097=ORIENTED_EDGE('',*,*,#1509,.F.);
#2098=ORIENTED_EDGE('',*,*,#1510,.F.);
#2099=ORIENTED_EDGE('',*,*,#1511,.F.);
#2100=ORIENTED_EDGE('',*,*,#1512,.F.);
#2101=ORIENTED_EDGE('',*,*,#1513,.F.);
#2102=ORIENTED_EDGE('',*,*,#1514,.F.);
#2103=ORIENTED_EDGE('',*,*,#1515,.F.);
#2104=ORIENTED_EDGE('',*,*,#1516,.F.);
#2105=ORIENTED_EDGE('',*,*,#1517,.F.);
#2106=ORIENTED_EDGE('',*,*,#1518,.F.);
#2107=ORIENTED_EDGE('',*,*,#1519,.F.);
#2108=ORIENTED_EDGE('',*,*,#1520,.F.);
#2109=ORIENTED_EDGE('',*,*,#1521,.F.);
#2110=ORIENTED_EDGE('',*,*,#1522,.F.);
#2111=ORIENTED_EDGE('',*,*,#1523,.F.);
#2112=ORIENTED_EDGE('',*,*,#1524,.F.);
#2113=ORIENTED_EDGE('',*,*,#1525,.F.);
#2114=ORIENTED_EDGE('',*,*,#1526,.F.);
#2115=ORIENTED_EDGE('',*,*,#1527,.F.);
#2116=ORIENTED_EDGE('',*,*,#1528,.F.);
#2117=ORIENTED_EDGE('',*,*,#1529,.F.);
#2118=ORIENTED_EDGE('',*,*,#1530,.F.);
#2119=ORIENTED_EDGE('',*,*,#1531,.F.);
#2120=ORIENTED_EDGE('',*,*,#1377,.T.);
#2121=ORIENTED_EDGE('',*,*,#1532,.F.);
#2122=ORIENTED_EDGE('',*,*,#1381,.T.);
#2123=ORIENTED_EDGE('',*,*,#1533,.F.);
#2124=ORIENTED_EDGE('',*,*,#1385,.T.);
#2125=ORIENTED_EDGE('',*,*,#1534,.F.);
#2126=ORIENTED_EDGE('',*,*,#1389,.T.);
#2127=ORIENTED_EDGE('',*,*,#1535,.F.);
#2128=ORIENTED_EDGE('',*,*,#1393,.T.);
#2129=ORIENTED_EDGE('',*,*,#1536,.F.);
#2130=ORIENTED_EDGE('',*,*,#1397,.T.);
#2131=ORIENTED_EDGE('',*,*,#1537,.F.);
#2132=ORIENTED_EDGE('',*,*,#1401,.T.);
#2133=ORIENTED_EDGE('',*,*,#1538,.F.);
#2134=ORIENTED_EDGE('',*,*,#1405,.T.);
#2135=ORIENTED_EDGE('',*,*,#1539,.F.);
#2136=ORIENTED_EDGE('',*,*,#1409,.T.);
#2137=ORIENTED_EDGE('',*,*,#1540,.F.);
#2138=ORIENTED_EDGE('',*,*,#1413,.T.);
#2139=ORIENTED_EDGE('',*,*,#1541,.F.);
#2140=ORIENTED_EDGE('',*,*,#1418,.T.);
#2141=ORIENTED_EDGE('',*,*,#1542,.F.);
#2142=ORIENTED_EDGE('',*,*,#1422,.T.);
#2143=ORIENTED_EDGE('',*,*,#1543,.F.);
#2144=ORIENTED_EDGE('',*,*,#1426,.T.);
#2145=ORIENTED_EDGE('',*,*,#1544,.F.);
#2146=ORIENTED_EDGE('',*,*,#1430,.T.);
#2147=ORIENTED_EDGE('',*,*,#1545,.F.);
#2148=ORIENTED_EDGE('',*,*,#1434,.T.);
#2149=ORIENTED_EDGE('',*,*,#1546,.F.);
#2150=ORIENTED_EDGE('',*,*,#1438,.T.);
#2151=ORIENTED_EDGE('',*,*,#1547,.F.);
#2152=ORIENTED_EDGE('',*,*,#1442,.T.);
#2153=ORIENTED_EDGE('',*,*,#1548,.F.);
#2154=ORIENTED_EDGE('',*,*,#1446,.T.);
#2155=ORIENTED_EDGE('',*,*,#1549,.F.);
#2156=ORIENTED_EDGE('',*,*,#1450,.T.);
#2157=ORIENTED_EDGE('',*,*,#1550,.F.);
#2158=ORIENTED_EDGE('',*,*,#1454,.T.);
#2159=ORIENTED_EDGE('',*,*,#1551,.F.);
#2160=ORIENTED_EDGE('',*,*,#1458,.T.);
#2161=ORIENTED_EDGE('',*,*,#1552,.F.);
#2162=ORIENTED_EDGE('',*,*,#1462,.T.);
#2163=ORIENTED_EDGE('',*,*,#1553,.F.);
#2164=ORIENTED_EDGE('',*,*,#1466,.T.);
#2165=ORIENTED_EDGE('',*,*,#1554,.F.);
#2166=ORIENTED_EDGE('',*,*,#1470,.T.);
#2167=ORIENTED_EDGE('',*,*,#1555,.F.);
#2168=ORIENTED_EDGE('',*,*,#1474,.T.);
#2169=ORIENTED_EDGE('',*,*,#1556,.F.);
#2170=ORIENTED_EDGE('',*,*,#1478,.T.);
#2171=ORIENTED_EDGE('',*,*,#1557,.F.);
#2172=ORIENTED_EDGE('',*,*,#1482,.T.);
#2173=ORIENTED_EDGE('',*,*,#1558,.F.);
#2174=ORIENTED_EDGE('',*,*,#1486,.T.);
#2175=ORIENTED_EDGE('',*,*,#1559,.F.);
#2176=ORIENTED_EDGE('',*,*,#1490,.T.);
#2177=ORIENTED_EDGE('',*,*,#1560,.F.);
#2178=ORIENTED_EDGE('',*,*,#1494,.T.);
#2179=ORIENTED_EDGE('',*,*,#1561,.F.);
#2180=ORIENTED_EDGE('',*,*,#1498,.T.);
#2181=ORIENTED_EDGE('',*,*,#1562,.F.);
#2182=ORIENTED_EDGE('',*,*,#1502,.T.);
#2183=ORIENTED_EDGE('',*,*,#1563,.F.);
#2184=ORIENTED_EDGE('',*,*,#1506,.T.);
#2185=ORIENTED_EDGE('',*,*,#1564,.F.);
#2186=ORIENTED_EDGE('',*,*,#1510,.T.);
#2187=ORIENTED_EDGE('',*,*,#1565,.F.);
#2188=ORIENTED_EDGE('',*,*,#1514,.T.);
#2189=ORIENTED_EDGE('',*,*,#1566,.F.);
#2190=ORIENTED_EDGE('',*,*,#1518,.T.);
#2191=ORIENTED_EDGE('',*,*,#1567,.F.);
#2192=ORIENTED_EDGE('',*,*,#1522,.T.);
#2193=ORIENTED_EDGE('',*,*,#1568,.F.);
#2194=ORIENTED_EDGE('',*,*,#1526,.T.);
#2195=ORIENTED_EDGE('',*,*,#1569,.F.);
#2196=ORIENTED_EDGE('',*,*,#1530,.T.);
#2197=ORIENTED_EDGE('',*,*,#1570,.F.);
#2198=ORIENTED_EDGE('',*,*,#1571,.T.);
#2199=ORIENTED_EDGE('',*,*,#1572,.F.);
#2200=ORIENTED_EDGE('',*,*,#1529,.T.);
#2201=ORIENTED_EDGE('',*,*,#1573,.F.);
#2202=ORIENTED_EDGE('',*,*,#1574,.T.);
#2203=ORIENTED_EDGE('',*,*,#1570,.T.);
#2204=ORIENTED_EDGE('',*,*,#1525,.T.);
#2205=ORIENTED_EDGE('',*,*,#1575,.F.);
#2206=ORIENTED_EDGE('',*,*,#1531,.T.);
#2207=ORIENTED_EDGE('',*,*,#1569,.T.);
#2208=ORIENTED_EDGE('',*,*,#1521,.T.);
#2209=ORIENTED_EDGE('',*,*,#1576,.F.);
#2210=ORIENTED_EDGE('',*,*,#1527,.T.);
#2211=ORIENTED_EDGE('',*,*,#1568,.T.);
#2212=ORIENTED_EDGE('',*,*,#1517,.T.);
#2213=ORIENTED_EDGE('',*,*,#1577,.F.);
#2214=ORIENTED_EDGE('',*,*,#1523,.T.);
#2215=ORIENTED_EDGE('',*,*,#1567,.T.);
#2216=ORIENTED_EDGE('',*,*,#1513,.T.);
#2217=ORIENTED_EDGE('',*,*,#1578,.F.);
#2218=ORIENTED_EDGE('',*,*,#1519,.T.);
#2219=ORIENTED_EDGE('',*,*,#1566,.T.);
#2220=ORIENTED_EDGE('',*,*,#1509,.T.);
#2221=ORIENTED_EDGE('',*,*,#1579,.F.);
#2222=ORIENTED_EDGE('',*,*,#1515,.T.);
#2223=ORIENTED_EDGE('',*,*,#1565,.T.);
#2224=ORIENTED_EDGE('',*,*,#1505,.T.);
#2225=ORIENTED_EDGE('',*,*,#1580,.F.);
#2226=ORIENTED_EDGE('',*,*,#1511,.T.);
#2227=ORIENTED_EDGE('',*,*,#1564,.T.);
#2228=ORIENTED_EDGE('',*,*,#1501,.T.);
#2229=ORIENTED_EDGE('',*,*,#1581,.F.);
#2230=ORIENTED_EDGE('',*,*,#1507,.T.);
#2231=ORIENTED_EDGE('',*,*,#1563,.T.);
#2232=ORIENTED_EDGE('',*,*,#1497,.T.);
#2233=ORIENTED_EDGE('',*,*,#1582,.F.);
#2234=ORIENTED_EDGE('',*,*,#1503,.T.);
#2235=ORIENTED_EDGE('',*,*,#1562,.T.);
#2236=ORIENTED_EDGE('',*,*,#1493,.T.);
#2237=ORIENTED_EDGE('',*,*,#1583,.F.);
#2238=ORIENTED_EDGE('',*,*,#1499,.T.);
#2239=ORIENTED_EDGE('',*,*,#1561,.T.);
#2240=ORIENTED_EDGE('',*,*,#1489,.T.);
#2241=ORIENTED_EDGE('',*,*,#1584,.F.);
#2242=ORIENTED_EDGE('',*,*,#1495,.T.);
#2243=ORIENTED_EDGE('',*,*,#1560,.T.);
#2244=ORIENTED_EDGE('',*,*,#1485,.T.);
#2245=ORIENTED_EDGE('',*,*,#1585,.F.);
#2246=ORIENTED_EDGE('',*,*,#1491,.T.);
#2247=ORIENTED_EDGE('',*,*,#1559,.T.);
#2248=ORIENTED_EDGE('',*,*,#1481,.T.);
#2249=ORIENTED_EDGE('',*,*,#1586,.F.);
#2250=ORIENTED_EDGE('',*,*,#1487,.T.);
#2251=ORIENTED_EDGE('',*,*,#1558,.T.);
#2252=ORIENTED_EDGE('',*,*,#1477,.T.);
#2253=ORIENTED_EDGE('',*,*,#1587,.F.);
#2254=ORIENTED_EDGE('',*,*,#1483,.T.);
#2255=ORIENTED_EDGE('',*,*,#1557,.T.);
#2256=ORIENTED_EDGE('',*,*,#1473,.T.);
#2257=ORIENTED_EDGE('',*,*,#1588,.F.);
#2258=ORIENTED_EDGE('',*,*,#1479,.T.);
#2259=ORIENTED_EDGE('',*,*,#1556,.T.);
#2260=ORIENTED_EDGE('',*,*,#1469,.T.);
#2261=ORIENTED_EDGE('',*,*,#1589,.F.);
#2262=ORIENTED_EDGE('',*,*,#1475,.T.);
#2263=ORIENTED_EDGE('',*,*,#1555,.T.);
#2264=ORIENTED_EDGE('',*,*,#1465,.T.);
#2265=ORIENTED_EDGE('',*,*,#1590,.F.);
#2266=ORIENTED_EDGE('',*,*,#1471,.T.);
#2267=ORIENTED_EDGE('',*,*,#1554,.T.);
#2268=ORIENTED_EDGE('',*,*,#1461,.T.);
#2269=ORIENTED_EDGE('',*,*,#1591,.F.);
#2270=ORIENTED_EDGE('',*,*,#1467,.T.);
#2271=ORIENTED_EDGE('',*,*,#1553,.T.);
#2272=ORIENTED_EDGE('',*,*,#1457,.T.);
#2273=ORIENTED_EDGE('',*,*,#1592,.F.);
#2274=ORIENTED_EDGE('',*,*,#1463,.T.);
#2275=ORIENTED_EDGE('',*,*,#1552,.T.);
#2276=ORIENTED_EDGE('',*,*,#1453,.T.);
#2277=ORIENTED_EDGE('',*,*,#1593,.F.);
#2278=ORIENTED_EDGE('',*,*,#1459,.T.);
#2279=ORIENTED_EDGE('',*,*,#1551,.T.);
#2280=ORIENTED_EDGE('',*,*,#1449,.T.);
#2281=ORIENTED_EDGE('',*,*,#1594,.F.);
#2282=ORIENTED_EDGE('',*,*,#1455,.T.);
#2283=ORIENTED_EDGE('',*,*,#1550,.T.);
#2284=ORIENTED_EDGE('',*,*,#1445,.T.);
#2285=ORIENTED_EDGE('',*,*,#1595,.F.);
#2286=ORIENTED_EDGE('',*,*,#1451,.T.);
#2287=ORIENTED_EDGE('',*,*,#1549,.T.);
#2288=ORIENTED_EDGE('',*,*,#1441,.T.);
#2289=ORIENTED_EDGE('',*,*,#1596,.F.);
#2290=ORIENTED_EDGE('',*,*,#1447,.T.);
#2291=ORIENTED_EDGE('',*,*,#1548,.T.);
#2292=ORIENTED_EDGE('',*,*,#1437,.T.);
#2293=ORIENTED_EDGE('',*,*,#1597,.F.);
#2294=ORIENTED_EDGE('',*,*,#1443,.T.);
#2295=ORIENTED_EDGE('',*,*,#1547,.T.);
#2296=ORIENTED_EDGE('',*,*,#1433,.T.);
#2297=ORIENTED_EDGE('',*,*,#1598,.F.);
#2298=ORIENTED_EDGE('',*,*,#1439,.T.);
#2299=ORIENTED_EDGE('',*,*,#1546,.T.);
#2300=ORIENTED_EDGE('',*,*,#1429,.T.);
#2301=ORIENTED_EDGE('',*,*,#1599,.F.);
#2302=ORIENTED_EDGE('',*,*,#1435,.T.);
#2303=ORIENTED_EDGE('',*,*,#1545,.T.);
#2304=ORIENTED_EDGE('',*,*,#1425,.T.);
#2305=ORIENTED_EDGE('',*,*,#1600,.F.);
#2306=ORIENTED_EDGE('',*,*,#1431,.T.);
#2307=ORIENTED_EDGE('',*,*,#1544,.T.);
#2308=ORIENTED_EDGE('',*,*,#1421,.T.);
#2309=ORIENTED_EDGE('',*,*,#1601,.F.);
#2310=ORIENTED_EDGE('',*,*,#1427,.T.);
#2311=ORIENTED_EDGE('',*,*,#1543,.T.);
#2312=ORIENTED_EDGE('',*,*,#1417,.T.);
#2313=ORIENTED_EDGE('',*,*,#1602,.F.);
#2314=ORIENTED_EDGE('',*,*,#1423,.T.);
#2315=ORIENTED_EDGE('',*,*,#1542,.T.);
#2316=ORIENTED_EDGE('',*,*,#1412,.T.);
#2317=ORIENTED_EDGE('',*,*,#1603,.F.);
#2318=ORIENTED_EDGE('',*,*,#1419,.T.);
#2319=ORIENTED_EDGE('',*,*,#1541,.T.);
#2320=ORIENTED_EDGE('',*,*,#1408,.T.);
#2321=ORIENTED_EDGE('',*,*,#1604,.F.);
#2322=ORIENTED_EDGE('',*,*,#1414,.T.);
#2323=ORIENTED_EDGE('',*,*,#1540,.T.);
#2324=ORIENTED_EDGE('',*,*,#1404,.T.);
#2325=ORIENTED_EDGE('',*,*,#1605,.F.);
#2326=ORIENTED_EDGE('',*,*,#1410,.T.);
#2327=ORIENTED_EDGE('',*,*,#1539,.T.);
#2328=ORIENTED_EDGE('',*,*,#1400,.T.);
#2329=ORIENTED_EDGE('',*,*,#1606,.F.);
#2330=ORIENTED_EDGE('',*,*,#1406,.T.);
#2331=ORIENTED_EDGE('',*,*,#1538,.T.);
#2332=ORIENTED_EDGE('',*,*,#1396,.T.);
#2333=ORIENTED_EDGE('',*,*,#1607,.F.);
#2334=ORIENTED_EDGE('',*,*,#1402,.T.);
#2335=ORIENTED_EDGE('',*,*,#1537,.T.);
#2336=ORIENTED_EDGE('',*,*,#1392,.T.);
#2337=ORIENTED_EDGE('',*,*,#1608,.F.);
#2338=ORIENTED_EDGE('',*,*,#1398,.T.);
#2339=ORIENTED_EDGE('',*,*,#1536,.T.);
#2340=ORIENTED_EDGE('',*,*,#1388,.T.);
#2341=ORIENTED_EDGE('',*,*,#1609,.F.);
#2342=ORIENTED_EDGE('',*,*,#1394,.T.);
#2343=ORIENTED_EDGE('',*,*,#1535,.T.);
#2344=ORIENTED_EDGE('',*,*,#1384,.T.);
#2345=ORIENTED_EDGE('',*,*,#1610,.F.);
#2346=ORIENTED_EDGE('',*,*,#1390,.T.);
#2347=ORIENTED_EDGE('',*,*,#1534,.T.);
#2348=ORIENTED_EDGE('',*,*,#1380,.T.);
#2349=ORIENTED_EDGE('',*,*,#1611,.F.);
#2350=ORIENTED_EDGE('',*,*,#1386,.T.);
#2351=ORIENTED_EDGE('',*,*,#1533,.T.);
#2352=ORIENTED_EDGE('',*,*,#1376,.T.);
#2353=ORIENTED_EDGE('',*,*,#1612,.F.);
#2354=ORIENTED_EDGE('',*,*,#1382,.T.);
#2355=ORIENTED_EDGE('',*,*,#1532,.T.);
#2356=ORIENTED_EDGE('',*,*,#1368,.T.);
#2357=ORIENTED_EDGE('',*,*,#1369,.T.);
#2358=ORIENTED_EDGE('',*,*,#1613,.T.);
#2359=ORIENTED_EDGE('',*,*,#1415,.T.);
#2360=ORIENTED_EDGE('',*,*,#1604,.T.);
#2361=ORIENTED_EDGE('',*,*,#1407,.T.);
#2362=ORIENTED_EDGE('',*,*,#1605,.T.);
#2363=ORIENTED_EDGE('',*,*,#1403,.T.);
#2364=ORIENTED_EDGE('',*,*,#1606,.T.);
#2365=ORIENTED_EDGE('',*,*,#1399,.T.);
#2366=ORIENTED_EDGE('',*,*,#1607,.T.);
#2367=ORIENTED_EDGE('',*,*,#1395,.T.);
#2368=ORIENTED_EDGE('',*,*,#1608,.T.);
#2369=ORIENTED_EDGE('',*,*,#1391,.T.);
#2370=ORIENTED_EDGE('',*,*,#1609,.T.);
#2371=ORIENTED_EDGE('',*,*,#1387,.T.);
#2372=ORIENTED_EDGE('',*,*,#1610,.T.);
#2373=ORIENTED_EDGE('',*,*,#1383,.T.);
#2374=ORIENTED_EDGE('',*,*,#1611,.T.);
#2375=ORIENTED_EDGE('',*,*,#1379,.T.);
#2376=ORIENTED_EDGE('',*,*,#1612,.T.);
#2377=ORIENTED_EDGE('',*,*,#1375,.T.);
#2378=ORIENTED_EDGE('',*,*,#1614,.T.);
#2379=ORIENTED_EDGE('',*,*,#1615,.T.);
#2380=ORIENTED_EDGE('',*,*,#1573,.T.);
#2381=ORIENTED_EDGE('',*,*,#1528,.T.);
#2382=ORIENTED_EDGE('',*,*,#1575,.T.);
#2383=ORIENTED_EDGE('',*,*,#1524,.T.);
#2384=ORIENTED_EDGE('',*,*,#1576,.T.);
#2385=ORIENTED_EDGE('',*,*,#1520,.T.);
#2386=ORIENTED_EDGE('',*,*,#1577,.T.);
#2387=ORIENTED_EDGE('',*,*,#1516,.T.);
#2388=ORIENTED_EDGE('',*,*,#1578,.T.);
#2389=ORIENTED_EDGE('',*,*,#1512,.T.);
#2390=ORIENTED_EDGE('',*,*,#1579,.T.);
#2391=ORIENTED_EDGE('',*,*,#1508,.T.);
#2392=ORIENTED_EDGE('',*,*,#1580,.T.);
#2393=ORIENTED_EDGE('',*,*,#1504,.T.);
#2394=ORIENTED_EDGE('',*,*,#1581,.T.);
#2395=ORIENTED_EDGE('',*,*,#1500,.T.);
#2396=ORIENTED_EDGE('',*,*,#1582,.T.);
#2397=ORIENTED_EDGE('',*,*,#1496,.T.);
#2398=ORIENTED_EDGE('',*,*,#1583,.T.);
#2399=ORIENTED_EDGE('',*,*,#1492,.T.);
#2400=ORIENTED_EDGE('',*,*,#1584,.T.);
#2401=ORIENTED_EDGE('',*,*,#1488,.T.);
#2402=ORIENTED_EDGE('',*,*,#1585,.T.);
#2403=ORIENTED_EDGE('',*,*,#1484,.T.);
#2404=ORIENTED_EDGE('',*,*,#1586,.T.);
#2405=ORIENTED_EDGE('',*,*,#1480,.T.);
#2406=ORIENTED_EDGE('',*,*,#1587,.T.);
#2407=ORIENTED_EDGE('',*,*,#1476,.T.);
#2408=ORIENTED_EDGE('',*,*,#1588,.T.);
#2409=ORIENTED_EDGE('',*,*,#1472,.T.);
#2410=ORIENTED_EDGE('',*,*,#1589,.T.);
#2411=ORIENTED_EDGE('',*,*,#1468,.T.);
#2412=ORIENTED_EDGE('',*,*,#1590,.T.);
#2413=ORIENTED_EDGE('',*,*,#1464,.T.);
#2414=ORIENTED_EDGE('',*,*,#1591,.T.);
#2415=ORIENTED_EDGE('',*,*,#1460,.T.);
#2416=ORIENTED_EDGE('',*,*,#1592,.T.);
#2417=ORIENTED_EDGE('',*,*,#1456,.T.);
#2418=ORIENTED_EDGE('',*,*,#1593,.T.);
#2419=ORIENTED_EDGE('',*,*,#1452,.T.);
#2420=ORIENTED_EDGE('',*,*,#1594,.T.);
#2421=ORIENTED_EDGE('',*,*,#1448,.T.);
#2422=ORIENTED_EDGE('',*,*,#1595,.T.);
#2423=ORIENTED_EDGE('',*,*,#1444,.T.);
#2424=ORIENTED_EDGE('',*,*,#1596,.T.);
#2425=ORIENTED_EDGE('',*,*,#1440,.T.);
#2426=ORIENTED_EDGE('',*,*,#1597,.T.);
#2427=ORIENTED_EDGE('',*,*,#1436,.T.);
#2428=ORIENTED_EDGE('',*,*,#1598,.T.);
#2429=ORIENTED_EDGE('',*,*,#1432,.T.);
#2430=ORIENTED_EDGE('',*,*,#1599,.T.);
#2431=ORIENTED_EDGE('',*,*,#1428,.T.);
#2432=ORIENTED_EDGE('',*,*,#1600,.T.);
#2433=ORIENTED_EDGE('',*,*,#1424,.T.);
#2434=ORIENTED_EDGE('',*,*,#1601,.T.);
#2435=ORIENTED_EDGE('',*,*,#1420,.T.);
#2436=ORIENTED_EDGE('',*,*,#1602,.T.);
#2437=ORIENTED_EDGE('',*,*,#1416,.T.);
#2438=ORIENTED_EDGE('',*,*,#1603,.T.);
#2439=ORIENTED_EDGE('',*,*,#1411,.T.);
#2440=ORIENTED_EDGE('',*,*,#1613,.F.);
#2441=ORIENTED_EDGE('',*,*,#1615,.F.);
#2442=ORIENTED_EDGE('',*,*,#1616,.F.);
#2443=ORIENTED_EDGE('',*,*,#1571,.F.);
#2444=ORIENTED_EDGE('',*,*,#1574,.F.);
#2445=ORIENTED_EDGE('',*,*,#1378,.T.);
#2446=ORIENTED_EDGE('',*,*,#1572,.T.);
#2447=ORIENTED_EDGE('',*,*,#1616,.T.);
#2448=ORIENTED_EDGE('',*,*,#1614,.F.);
#2449=ORIENTED_EDGE('',*,*,#1363,.T.);
#2450=ORIENTED_EDGE('',*,*,#1374,.T.);
#2451=ORIENTED_EDGE('',*,*,#1312,.T.);
#2452=ORIENTED_EDGE('',*,*,#1372,.F.);
#2453=ORIENTED_EDGE('',*,*,#1371,.T.);
#2454=ORIENTED_EDGE('',*,*,#1232,.F.);
#2455=ORIENTED_EDGE('',*,*,#1373,.T.);
#2456=ORIENTED_EDGE('',*,*,#1272,.T.);
#2457=ORIENTED_EDGE('',*,*,#1370,.T.);
#2458=ORIENTED_EDGE('',*,*,#1338,.T.);
#2599=CYLINDRICAL_SURFACE('',#2870,2.4505);
#2600=CYLINDRICAL_SURFACE('',#2873,1.99475);
#2601=CYLINDRICAL_SURFACE('',#2876,4.);
#2602=CYLINDRICAL_SURFACE('',#2879,4.5);
#2603=CYLINDRICAL_SURFACE('',#2884,0.25);
#2604=CYLINDRICAL_SURFACE('',#2886,0.25);
#2605=CYLINDRICAL_SURFACE('',#2888,0.25);
#2606=CYLINDRICAL_SURFACE('',#2890,0.25);
#2607=CYLINDRICAL_SURFACE('',#2892,0.25);
#2608=CYLINDRICAL_SURFACE('',#2894,0.25);
#2609=CYLINDRICAL_SURFACE('',#2896,0.25);
#2610=CYLINDRICAL_SURFACE('',#2898,0.25);
#2611=CYLINDRICAL_SURFACE('',#2900,0.25);
#2612=CYLINDRICAL_SURFACE('',#2902,0.25);
#2613=CYLINDRICAL_SURFACE('',#2904,0.25);
#2614=CYLINDRICAL_SURFACE('',#2906,0.25);
#2615=CYLINDRICAL_SURFACE('',#2908,0.25);
#2616=CYLINDRICAL_SURFACE('',#2910,0.25);
#2617=CYLINDRICAL_SURFACE('',#2912,0.25);
#2618=CYLINDRICAL_SURFACE('',#2914,0.25);
#2619=CYLINDRICAL_SURFACE('',#2916,0.25);
#2620=CYLINDRICAL_SURFACE('',#2918,0.25);
#2621=CYLINDRICAL_SURFACE('',#2920,0.25);
#2622=CYLINDRICAL_SURFACE('',#2922,0.25);
#2623=CYLINDRICAL_SURFACE('',#2924,0.25);
#2624=CYLINDRICAL_SURFACE('',#2926,0.25);
#2625=CYLINDRICAL_SURFACE('',#2928,0.25);
#2626=CYLINDRICAL_SURFACE('',#2930,0.25);
#2627=CYLINDRICAL_SURFACE('',#2932,0.25);
#2628=CYLINDRICAL_SURFACE('',#2934,0.25);
#2629=CYLINDRICAL_SURFACE('',#2936,0.25);
#2630=CYLINDRICAL_SURFACE('',#2938,0.25);
#2631=CYLINDRICAL_SURFACE('',#2940,0.25);
#2632=CYLINDRICAL_SURFACE('',#2942,0.25);
#2633=CYLINDRICAL_SURFACE('',#2944,0.25);
#2634=CYLINDRICAL_SURFACE('',#2946,0.25);
#2635=CYLINDRICAL_SURFACE('',#2948,0.25);
#2636=CYLINDRICAL_SURFACE('',#2950,0.25);
#2637=CYLINDRICAL_SURFACE('',#2952,0.25);
#2638=CYLINDRICAL_SURFACE('',#2954,0.25);
#2639=CYLINDRICAL_SURFACE('',#2956,0.25);
#2640=CYLINDRICAL_SURFACE('',#2958,0.25);
#2641=CYLINDRICAL_SURFACE('',#2960,0.25);
#2642=CYLINDRICAL_SURFACE('',#3004,5.5);
#2643=CYLINDRICAL_SURFACE('',#3006,5.5);
#2644=CYLINDRICAL_SURFACE('',#3008,5.5);
#2645=CYLINDRICAL_SURFACE('',#3010,5.5);
#2646=CYLINDRICAL_SURFACE('',#3012,5.5);
#2647=CYLINDRICAL_SURFACE('',#3014,5.5);
#2648=CYLINDRICAL_SURFACE('',#3016,5.5);
#2649=CYLINDRICAL_SURFACE('',#3018,5.5);
#2650=CYLINDRICAL_SURFACE('',#3020,5.5);
#2651=CYLINDRICAL_SURFACE('',#3022,5.5);
#2652=CYLINDRICAL_SURFACE('',#3024,5.5);
#2653=CYLINDRICAL_SURFACE('',#3026,5.5);
#2654=CYLINDRICAL_SURFACE('',#3028,5.5);
#2655=CYLINDRICAL_SURFACE('',#3030,5.5);
#2656=CYLINDRICAL_SURFACE('',#3032,5.5);
#2657=CYLINDRICAL_SURFACE('',#3034,5.5);
#2658=CYLINDRICAL_SURFACE('',#3036,5.5);
#2659=CYLINDRICAL_SURFACE('',#3038,5.5);
#2660=CYLINDRICAL_SURFACE('',#3040,5.5);
#2661=CYLINDRICAL_SURFACE('',#3042,5.5);
#2662=CYLINDRICAL_SURFACE('',#3044,5.5);
#2663=CYLINDRICAL_SURFACE('',#3046,5.5);
#2664=CYLINDRICAL_SURFACE('',#3048,5.5);
#2665=CYLINDRICAL_SURFACE('',#3050,5.5);
#2666=CYLINDRICAL_SURFACE('',#3052,5.5);
#2667=CYLINDRICAL_SURFACE('',#3054,5.5);
#2668=CYLINDRICAL_SURFACE('',#3056,5.5);
#2669=CYLINDRICAL_SURFACE('',#3058,5.5);
#2670=CYLINDRICAL_SURFACE('',#3060,5.5);
#2671=CYLINDRICAL_SURFACE('',#3062,5.5);
#2672=CYLINDRICAL_SURFACE('',#3064,5.5);
#2673=CYLINDRICAL_SURFACE('',#3066,5.5);
#2674=CYLINDRICAL_SURFACE('',#3068,5.5);
#2675=CYLINDRICAL_SURFACE('',#3070,5.5);
#2676=CYLINDRICAL_SURFACE('',#3072,5.5);
#2677=CYLINDRICAL_SURFACE('',#3074,5.5);
#2678=CYLINDRICAL_SURFACE('',#3076,5.5);
#2679=CYLINDRICAL_SURFACE('',#3078,5.5);
#2680=CYLINDRICAL_SURFACE('',#3080,5.5);
#2681=CYLINDRICAL_SURFACE('',#3085,0.25);
#2682=CYLINDRICAL_SURFACE('',#3086,5.5);
#2686=ADVANCED_FACE('',(#299),#2599,.T.);
#2687=ADVANCED_FACE('',(#300),#2600,.T.);
#2688=ADVANCED_FACE('',(#301),#2601,.F.);
#2689=ADVANCED_FACE('',(#302),#2602,.T.);
#2690=ADVANCED_FACE('',(#303,#87),#91,.T.);
#2691=ADVANCED_FACE('',(#304),#84,.F.);
#2692=ADVANCED_FACE('',(#305),#85,.F.);
#2693=ADVANCED_FACE('',(#306),#2603,.F.);
#2694=ADVANCED_FACE('',(#307),#2604,.F.);
#2695=ADVANCED_FACE('',(#308),#2605,.F.);
#2696=ADVANCED_FACE('',(#309),#2606,.F.);
#2697=ADVANCED_FACE('',(#310),#2607,.F.);
#2698=ADVANCED_FACE('',(#311),#2608,.F.);
#2699=ADVANCED_FACE('',(#312),#2609,.F.);
#2700=ADVANCED_FACE('',(#313),#2610,.F.);
#2701=ADVANCED_FACE('',(#314),#2611,.F.);
#2702=ADVANCED_FACE('',(#315),#2612,.F.);
#2703=ADVANCED_FACE('',(#316),#2613,.F.);
#2704=ADVANCED_FACE('',(#317),#2614,.F.);
#2705=ADVANCED_FACE('',(#318),#2615,.F.);
#2706=ADVANCED_FACE('',(#319),#2616,.F.);
#2707=ADVANCED_FACE('',(#320),#2617,.F.);
#2708=ADVANCED_FACE('',(#321),#2618,.F.);
#2709=ADVANCED_FACE('',(#322),#2619,.F.);
#2710=ADVANCED_FACE('',(#323),#2620,.F.);
#2711=ADVANCED_FACE('',(#324),#2621,.F.);
#2712=ADVANCED_FACE('',(#325),#2622,.F.);
#2713=ADVANCED_FACE('',(#326),#2623,.F.);
#2714=ADVANCED_FACE('',(#327),#2624,.F.);
#2715=ADVANCED_FACE('',(#328),#2625,.F.);
#2716=ADVANCED_FACE('',(#329),#2626,.F.);
#2717=ADVANCED_FACE('',(#330),#2627,.F.);
#2718=ADVANCED_FACE('',(#331),#2628,.F.);
#2719=ADVANCED_FACE('',(#332),#2629,.F.);
#2720=ADVANCED_FACE('',(#333),#2630,.F.);
#2721=ADVANCED_FACE('',(#334),#2631,.F.);
#2722=ADVANCED_FACE('',(#335),#2632,.F.);
#2723=ADVANCED_FACE('',(#336),#2633,.F.);
#2724=ADVANCED_FACE('',(#337),#2634,.F.);
#2725=ADVANCED_FACE('',(#338),#2635,.F.);
#2726=ADVANCED_FACE('',(#339),#2636,.F.);
#2727=ADVANCED_FACE('',(#340),#2637,.F.);
#2728=ADVANCED_FACE('',(#341),#2638,.F.);
#2729=ADVANCED_FACE('',(#342),#2639,.F.);
#2730=ADVANCED_FACE('',(#343),#2640,.F.);
#2731=ADVANCED_FACE('',(#344),#2641,.F.);
#2732=ADVANCED_FACE('',(#345),#92,.F.);
#2733=ADVANCED_FACE('',(#346),#2642,.T.);
#2734=ADVANCED_FACE('',(#347),#2643,.T.);
#2735=ADVANCED_FACE('',(#348),#2644,.T.);
#2736=ADVANCED_FACE('',(#349),#2645,.T.);
#2737=ADVANCED_FACE('',(#350),#2646,.T.);
#2738=ADVANCED_FACE('',(#351),#2647,.T.);
#2739=ADVANCED_FACE('',(#352),#2648,.T.);
#2740=ADVANCED_FACE('',(#353),#2649,.T.);
#2741=ADVANCED_FACE('',(#354),#2650,.T.);
#2742=ADVANCED_FACE('',(#355),#2651,.T.);
#2743=ADVANCED_FACE('',(#356),#2652,.T.);
#2744=ADVANCED_FACE('',(#357),#2653,.T.);
#2745=ADVANCED_FACE('',(#358),#2654,.T.);
#2746=ADVANCED_FACE('',(#359),#2655,.T.);
#2747=ADVANCED_FACE('',(#360),#2656,.T.);
#2748=ADVANCED_FACE('',(#361),#2657,.T.);
#2749=ADVANCED_FACE('',(#362),#2658,.T.);
#2750=ADVANCED_FACE('',(#363),#2659,.T.);
#2751=ADVANCED_FACE('',(#364),#2660,.T.);
#2752=ADVANCED_FACE('',(#365),#2661,.T.);
#2753=ADVANCED_FACE('',(#366),#2662,.T.);
#2754=ADVANCED_FACE('',(#367),#2663,.T.);
#2755=ADVANCED_FACE('',(#368),#2664,.T.);
#2756=ADVANCED_FACE('',(#369),#2665,.T.);
#2757=ADVANCED_FACE('',(#370),#2666,.T.);
#2758=ADVANCED_FACE('',(#371),#2667,.T.);
#2759=ADVANCED_FACE('',(#372),#2668,.T.);
#2760=ADVANCED_FACE('',(#373),#2669,.T.);
#2761=ADVANCED_FACE('',(#374),#2670,.T.);
#2762=ADVANCED_FACE('',(#375),#2671,.T.);
#2763=ADVANCED_FACE('',(#376),#2672,.T.);
#2764=ADVANCED_FACE('',(#377),#2673,.T.);
#2765=ADVANCED_FACE('',(#378),#2674,.T.);
#2766=ADVANCED_FACE('',(#379),#2675,.T.);
#2767=ADVANCED_FACE('',(#380),#2676,.T.);
#2768=ADVANCED_FACE('',(#381),#2677,.T.);
#2769=ADVANCED_FACE('',(#382),#2678,.T.);
#2770=ADVANCED_FACE('',(#383),#2679,.T.);
#2771=ADVANCED_FACE('',(#384),#2680,.T.);
#2772=ADVANCED_FACE('',(#385),#77,.T.);
#2773=ADVANCED_FACE('',(#386),#2681,.F.);
#2774=ADVANCED_FACE('',(#387),#2682,.T.);
#2775=ADVANCED_FACE('',(#388,#88),#93,.T.);
#2776=ADVANCED_FACE('',(#389),#94,.T.);
#2807=CLOSED_SHELL('',(#2686,#2687,#2688,#2689,#2690,#2691,#2692,#2693,
#2694,#2695,#2696,#2697,#2698,#2699,#2700,#2701,#2702,#2703,#2704,#2705,
#2706,#2707,#2708,#2709,#2710,#2711,#2712,#2713,#2714,#2715,#2716,#2717,
#2718,#2719,#2720,#2721,#2722,#2723,#2724,#2725,#2726,#2727,#2728,#2729,
#2730,#2731,#2732,#2733,#2734,#2735,#2736,#2737,#2738,#2739,#2740,#2741,
#2742,#2743,#2744,#2745,#2746,#2747,#2748,#2749,#2750,#2751,#2752,#2753,
#2754,#2755,#2756,#2757,#2758,#2759,#2760,#2761,#2762,#2763,#2764,#2765,
#2766,#2767,#2768,#2769,#2770,#2771,#2772,#2773,#2774,#2775,#2776));
#2869=AXIS2_PLACEMENT_3D('',#3809,#3151,#3152);
#2870=AXIS2_PLACEMENT_3D('',#3810,#3153,#3154);
#2871=AXIS2_PLACEMENT_3D('',#3820,#3155,#3156);
#2872=AXIS2_PLACEMENT_3D('',#7359,#3157,#3158);
#2873=AXIS2_PLACEMENT_3D('',#10889,#3159,#3160);
#2874=AXIS2_PLACEMENT_3D('',#11491,#3161,#3162);
#2875=AXIS2_PLACEMENT_3D('',#19798,#3163,#3164);
#2876=AXIS2_PLACEMENT_3D('',#27454,#3165,#3166);
#2877=AXIS2_PLACEMENT_3D('',#27456,#3167,#3168);
#2878=AXIS2_PLACEMENT_3D('',#27459,#3170,#3171);
#2879=AXIS2_PLACEMENT_3D('',#27460,#3172,#3173);
#2880=AXIS2_PLACEMENT_3D('',#27462,#3174,#3175);
#2881=AXIS2_PLACEMENT_3D('',#27466,#3177,#3178);
#2882=AXIS2_PLACEMENT_3D('',#27467,#3179,#3180);
#2883=AXIS2_PLACEMENT_3D('',#27468,#3181,#3182);
#2884=AXIS2_PLACEMENT_3D('',#29757,#3183,#3184);
#2885=AXIS2_PLACEMENT_3D('',#29797,#3186,#3187);
#2886=AXIS2_PLACEMENT_3D('',#29799,#3189,#3190);
#2887=AXIS2_PLACEMENT_3D('',#29839,#3192,#3193);
#2888=AXIS2_PLACEMENT_3D('',#29841,#3195,#3196);
#2889=AXIS2_PLACEMENT_3D('',#29881,#3198,#3199);
#2890=AXIS2_PLACEMENT_3D('',#29883,#3201,#3202);
#2891=AXIS2_PLACEMENT_3D('',#29923,#3204,#3205);
#2892=AXIS2_PLACEMENT_3D('',#29925,#3207,#3208);
#2893=AXIS2_PLACEMENT_3D('',#29965,#3210,#3211);
#2894=AXIS2_PLACEMENT_3D('',#29967,#3213,#3214);
#2895=AXIS2_PLACEMENT_3D('',#30007,#3216,#3217);
#2896=AXIS2_PLACEMENT_3D('',#30009,#3219,#3220);
#2897=AXIS2_PLACEMENT_3D('',#30049,#3222,#3223);
#2898=AXIS2_PLACEMENT_3D('',#30051,#3225,#3226);
#2899=AXIS2_PLACEMENT_3D('',#30091,#3228,#3229);
#2900=AXIS2_PLACEMENT_3D('',#30093,#3231,#3232);
#2901=AXIS2_PLACEMENT_3D('',#30133,#3234,#3235);
#2902=AXIS2_PLACEMENT_3D('',#30135,#3237,#3238);
#2903=AXIS2_PLACEMENT_3D('',#30161,#3240,#3241);
#2904=AXIS2_PLACEMENT_3D('',#30182,#3243,#3244);
#2905=AXIS2_PLACEMENT_3D('',#30222,#3246,#3247);
#2906=AXIS2_PLACEMENT_3D('',#30224,#3249,#3250);
#2907=AXIS2_PLACEMENT_3D('',#30264,#3252,#3253);
#2908=AXIS2_PLACEMENT_3D('',#30266,#3255,#3256);
#2909=AXIS2_PLACEMENT_3D('',#30306,#3258,#3259);
#2910=AXIS2_PLACEMENT_3D('',#30308,#3261,#3262);
#2911=AXIS2_PLACEMENT_3D('',#30348,#3264,#3265);
#2912=AXIS2_PLACEMENT_3D('',#30350,#3267,#3268);
#2913=AXIS2_PLACEMENT_3D('',#30390,#3270,#3271);
#2914=AXIS2_PLACEMENT_3D('',#30392,#3273,#3274);
#2915=AXIS2_PLACEMENT_3D('',#30432,#3276,#3277);
#2916=AXIS2_PLACEMENT_3D('',#30434,#3279,#3280);
#2917=AXIS2_PLACEMENT_3D('',#30474,#3282,#3283);
#2918=AXIS2_PLACEMENT_3D('',#30476,#3285,#3286);
#2919=AXIS2_PLACEMENT_3D('',#30516,#3288,#3289);
#2920=AXIS2_PLACEMENT_3D('',#30518,#3291,#3292);
#2921=AXIS2_PLACEMENT_3D('',#30558,#3294,#3295);
#2922=AXIS2_PLACEMENT_3D('',#30560,#3297,#3298);
#2923=AXIS2_PLACEMENT_3D('',#30600,#3300,#3301);
#2924=AXIS2_PLACEMENT_3D('',#30602,#3303,#3304);
#2925=AXIS2_PLACEMENT_3D('',#30642,#3306,#3307);
#2926=AXIS2_PLACEMENT_3D('',#30644,#3309,#3310);
#2927=AXIS2_PLACEMENT_3D('',#30684,#3312,#3313);
#2928=AXIS2_PLACEMENT_3D('',#30686,#3315,#3316);
#2929=AXIS2_PLACEMENT_3D('',#30726,#3318,#3319);
#2930=AXIS2_PLACEMENT_3D('',#30728,#3321,#3322);
#2931=AXIS2_PLACEMENT_3D('',#30768,#3324,#3325);
#2932=AXIS2_PLACEMENT_3D('',#30770,#3327,#3328);
#2933=AXIS2_PLACEMENT_3D('',#30810,#3330,#3331);
#2934=AXIS2_PLACEMENT_3D('',#30812,#3333,#3334);
#2935=AXIS2_PLACEMENT_3D('',#30852,#3336,#3337);
#2936=AXIS2_PLACEMENT_3D('',#30854,#3339,#3340);
#2937=AXIS2_PLACEMENT_3D('',#30894,#3342,#3343);
#2938=AXIS2_PLACEMENT_3D('',#30896,#3345,#3346);
#2939=AXIS2_PLACEMENT_3D('',#30936,#3348,#3349);
#2940=AXIS2_PLACEMENT_3D('',#30938,#3351,#3352);
#2941=AXIS2_PLACEMENT_3D('',#30978,#3354,#3355);
#2942=AXIS2_PLACEMENT_3D('',#30980,#3357,#3358);
#2943=AXIS2_PLACEMENT_3D('',#31020,#3360,#3361);
#2944=AXIS2_PLACEMENT_3D('',#31022,#3363,#3364);
#2945=AXIS2_PLACEMENT_3D('',#31062,#3366,#3367);
#2946=AXIS2_PLACEMENT_3D('',#31064,#3369,#3370);
#2947=AXIS2_PLACEMENT_3D('',#31104,#3372,#3373);
#2948=AXIS2_PLACEMENT_3D('',#31106,#3375,#3376);
#2949=AXIS2_PLACEMENT_3D('',#31146,#3378,#3379);
#2950=AXIS2_PLACEMENT_3D('',#31148,#3381,#3382);
#2951=AXIS2_PLACEMENT_3D('',#31188,#3384,#3385);
#2952=AXIS2_PLACEMENT_3D('',#31190,#3387,#3388);
#2953=AXIS2_PLACEMENT_3D('',#31230,#3390,#3391);
#2954=AXIS2_PLACEMENT_3D('',#31232,#3393,#3394);
#2955=AXIS2_PLACEMENT_3D('',#31272,#3396,#3397);
#2956=AXIS2_PLACEMENT_3D('',#31274,#3399,#3400);
#2957=AXIS2_PLACEMENT_3D('',#31314,#3402,#3403);
#2958=AXIS2_PLACEMENT_3D('',#31316,#3405,#3406);
#2959=AXIS2_PLACEMENT_3D('',#31356,#3408,#3409);
#2960=AXIS2_PLACEMENT_3D('',#31358,#3411,#3412);
#2961=AXIS2_PLACEMENT_3D('',#31398,#3414,#3415);
#2962=AXIS2_PLACEMENT_3D('',#31400,#3417,#3418);
#2963=AXIS2_PLACEMENT_3D('',#31401,#3419,#3420);
#2964=AXIS2_PLACEMENT_3D('',#31402,#3421,#3422);
#2965=AXIS2_PLACEMENT_3D('',#31403,#3423,#3424);
#2966=AXIS2_PLACEMENT_3D('',#31404,#3425,#3426);
#2967=AXIS2_PLACEMENT_3D('',#31405,#3427,#3428);
#2968=AXIS2_PLACEMENT_3D('',#31406,#3429,#3430);
#2969=AXIS2_PLACEMENT_3D('',#31407,#3431,#3432);
#2970=AXIS2_PLACEMENT_3D('',#31408,#3433,#3434);
#2971=AXIS2_PLACEMENT_3D('',#31409,#3435,#3436);
#2972=AXIS2_PLACEMENT_3D('',#31410,#3437,#3438);
#2973=AXIS2_PLACEMENT_3D('',#31411,#3439,#3440);
#2974=AXIS2_PLACEMENT_3D('',#31412,#3441,#3442);
#2975=AXIS2_PLACEMENT_3D('',#31413,#3443,#3444);
#2976=AXIS2_PLACEMENT_3D('',#31414,#3445,#3446);
#2977=AXIS2_PLACEMENT_3D('',#31415,#3447,#3448);
#2978=AXIS2_PLACEMENT_3D('',#31416,#3449,#3450);
#2979=AXIS2_PLACEMENT_3D('',#31417,#3451,#3452);
#2980=AXIS2_PLACEMENT_3D('',#31418,#3453,#3454);
#2981=AXIS2_PLACEMENT_3D('',#31419,#3455,#3456);
#2982=AXIS2_PLACEMENT_3D('',#31420,#3457,#3458);
#2983=AXIS2_PLACEMENT_3D('',#31421,#3459,#3460);
#2984=AXIS2_PLACEMENT_3D('',#31422,#3461,#3462);
#2985=AXIS2_PLACEMENT_3D('',#31423,#3463,#3464);
#2986=AXIS2_PLACEMENT_3D('',#31424,#3465,#3466);
#2987=AXIS2_PLACEMENT_3D('',#31425,#3467,#3468);
#2988=AXIS2_PLACEMENT_3D('',#31426,#3469,#3470);
#2989=AXIS2_PLACEMENT_3D('',#31427,#3471,#3472);
#2990=AXIS2_PLACEMENT_3D('',#31428,#3473,#3474);
#2991=AXIS2_PLACEMENT_3D('',#31429,#3475,#3476);
#2992=AXIS2_PLACEMENT_3D('',#31430,#3477,#3478);
#2993=AXIS2_PLACEMENT_3D('',#31431,#3479,#3480);
#2994=AXIS2_PLACEMENT_3D('',#31432,#3481,#3482);
#2995=AXIS2_PLACEMENT_3D('',#31433,#3483,#3484);
#2996=AXIS2_PLACEMENT_3D('',#31434,#3485,#3486);
#2997=AXIS2_PLACEMENT_3D('',#31435,#3487,#3488);
#2998=AXIS2_PLACEMENT_3D('',#31436,#3489,#3490);
#2999=AXIS2_PLACEMENT_3D('',#31437,#3491,#3492);
#3000=AXIS2_PLACEMENT_3D('',#31438,#3493,#3494);
#3001=AXIS2_PLACEMENT_3D('',#31440,#3495,#3496);
#3002=AXIS2_PLACEMENT_3D('',#31442,#3497,#3498);
#3003=AXIS2_PLACEMENT_3D('',#31443,#3499,#3500);
#3004=AXIS2_PLACEMENT_3D('',#31444,#3501,#3502);
#3005=AXIS2_PLACEMENT_3D('',#31446,#3503,#3504);
#3006=AXIS2_PLACEMENT_3D('',#31448,#3506,#3507);
#3007=AXIS2_PLACEMENT_3D('',#31449,#3508,#3509);
#3008=AXIS2_PLACEMENT_3D('',#31450,#3510,#3511);
#3009=AXIS2_PLACEMENT_3D('',#31451,#3512,#3513);
#3010=AXIS2_PLACEMENT_3D('',#31452,#3514,#3515);
#3011=AXIS2_PLACEMENT_3D('',#31453,#3516,#3517);
#3012=AXIS2_PLACEMENT_3D('',#31454,#3518,#3519);
#3013=AXIS2_PLACEMENT_3D('',#31455,#3520,#3521);
#3014=AXIS2_PLACEMENT_3D('',#31456,#3522,#3523);
#3015=AXIS2_PLACEMENT_3D('',#31457,#3524,#3525);
#3016=AXIS2_PLACEMENT_3D('',#31458,#3526,#3527);
#3017=AXIS2_PLACEMENT_3D('',#31459,#3528,#3529);
#3018=AXIS2_PLACEMENT_3D('',#31460,#3530,#3531);
#3019=AXIS2_PLACEMENT_3D('',#31461,#3532,#3533);
#3020=AXIS2_PLACEMENT_3D('',#31462,#3534,#3535);
#3021=AXIS2_PLACEMENT_3D('',#31463,#3536,#3537);
#3022=AXIS2_PLACEMENT_3D('',#31464,#3538,#3539);
#3023=AXIS2_PLACEMENT_3D('',#31465,#3540,#3541);
#3024=AXIS2_PLACEMENT_3D('',#31466,#3542,#3543);
#3025=AXIS2_PLACEMENT_3D('',#31467,#3544,#3545);
#3026=AXIS2_PLACEMENT_3D('',#31468,#3546,#3547);
#3027=AXIS2_PLACEMENT_3D('',#31469,#3548,#3549);
#3028=AXIS2_PLACEMENT_3D('',#31470,#3550,#3551);
#3029=AXIS2_PLACEMENT_3D('',#31471,#3552,#3553);
#3030=AXIS2_PLACEMENT_3D('',#31472,#3554,#3555);
#3031=AXIS2_PLACEMENT_3D('',#31473,#3556,#3557);
#3032=AXIS2_PLACEMENT_3D('',#31474,#3558,#3559);
#3033=AXIS2_PLACEMENT_3D('',#31475,#3560,#3561);
#3034=AXIS2_PLACEMENT_3D('',#31476,#3562,#3563);
#3035=AXIS2_PLACEMENT_3D('',#31477,#3564,#3565);
#3036=AXIS2_PLACEMENT_3D('',#31478,#3566,#3567);
#3037=AXIS2_PLACEMENT_3D('',#31479,#3568,#3569);
#3038=AXIS2_PLACEMENT_3D('',#31480,#3570,#3571);
#3039=AXIS2_PLACEMENT_3D('',#31481,#3572,#3573);
#3040=AXIS2_PLACEMENT_3D('',#31482,#3574,#3575);
#3041=AXIS2_PLACEMENT_3D('',#31483,#3576,#3577);
#3042=AXIS2_PLACEMENT_3D('',#31484,#3578,#3579);
#3043=AXIS2_PLACEMENT_3D('',#31485,#3580,#3581);
#3044=AXIS2_PLACEMENT_3D('',#31486,#3582,#3583);
#3045=AXIS2_PLACEMENT_3D('',#31487,#3584,#3585);
#3046=AXIS2_PLACEMENT_3D('',#31488,#3586,#3587);
#3047=AXIS2_PLACEMENT_3D('',#31489,#3588,#3589);
#3048=AXIS2_PLACEMENT_3D('',#31490,#3590,#3591);
#3049=AXIS2_PLACEMENT_3D('',#31491,#3592,#3593);
#3050=AXIS2_PLACEMENT_3D('',#31492,#3594,#3595);
#3051=AXIS2_PLACEMENT_3D('',#31493,#3596,#3597);
#3052=AXIS2_PLACEMENT_3D('',#31494,#3598,#3599);
#3053=AXIS2_PLACEMENT_3D('',#31495,#3600,#3601);
#3054=AXIS2_PLACEMENT_3D('',#31496,#3602,#3603);
#3055=AXIS2_PLACEMENT_3D('',#31497,#3604,#3605);
#3056=AXIS2_PLACEMENT_3D('',#31498,#3606,#3607);
#3057=AXIS2_PLACEMENT_3D('',#31499,#3608,#3609);
#3058=AXIS2_PLACEMENT_3D('',#31500,#3610,#3611);
#3059=AXIS2_PLACEMENT_3D('',#31501,#3612,#3613);
#3060=AXIS2_PLACEMENT_3D('',#31502,#3614,#3615);
#3061=AXIS2_PLACEMENT_3D('',#31503,#3616,#3617);
#3062=AXIS2_PLACEMENT_3D('',#31504,#3618,#3619);
#3063=AXIS2_PLACEMENT_3D('',#31505,#3620,#3621);
#3064=AXIS2_PLACEMENT_3D('',#31506,#3622,#3623);
#3065=AXIS2_PLACEMENT_3D('',#31507,#3624,#3625);
#3066=AXIS2_PLACEMENT_3D('',#31508,#3626,#3627);
#3067=AXIS2_PLACEMENT_3D('',#31509,#3628,#3629);
#3068=AXIS2_PLACEMENT_3D('',#31510,#3630,#3631);
#3069=AXIS2_PLACEMENT_3D('',#31511,#3632,#3633);
#3070=AXIS2_PLACEMENT_3D('',#31512,#3634,#3635);
#3071=AXIS2_PLACEMENT_3D('',#31513,#3636,#3637);
#3072=AXIS2_PLACEMENT_3D('',#31514,#3638,#3639);
#3073=AXIS2_PLACEMENT_3D('',#31515,#3640,#3641);
#3074=AXIS2_PLACEMENT_3D('',#31516,#3642,#3643);
#3075=AXIS2_PLACEMENT_3D('',#31517,#3644,#3645);
#3076=AXIS2_PLACEMENT_3D('',#31518,#3646,#3647);
#3077=AXIS2_PLACEMENT_3D('',#31519,#3648,#3649);
#3078=AXIS2_PLACEMENT_3D('',#31520,#3650,#3651);
#3079=AXIS2_PLACEMENT_3D('',#31521,#3652,#3653);
#3080=AXIS2_PLACEMENT_3D('',#31522,#3654,#3655);
#3081=AXIS2_PLACEMENT_3D('',#31523,#3656,#3657);
#3082=AXIS2_PLACEMENT_3D('',#31524,#3658,#3659);
#3083=AXIS2_PLACEMENT_3D('',#31525,#3660,#3661);
#3084=AXIS2_PLACEMENT_3D('',#31527,#3662,#3663);
#3085=AXIS2_PLACEMENT_3D('',#31562,#3664,#3665);
#3086=AXIS2_PLACEMENT_3D('',#31564,#3667,#3668);
#3087=AXIS2_PLACEMENT_3D('',#31565,#3669,#3670);
#3088=AXIS2_PLACEMENT_3D('',#31566,#3671,#3672);
#3151=DIRECTION('axis',(0.,0.,1.));
#3152=DIRECTION('refdir',(1.,0.,0.));
#3153=DIRECTION('center_axis',(0.,0.,1.));
#3154=DIRECTION('ref_axis',(1.,0.,0.));
#3155=DIRECTION('center_axis',(0.,0.,-1.));
#3156=DIRECTION('ref_axis',(1.,0.,0.));
#3157=DIRECTION('center_axis',(0.,0.,-1.));
#3158=DIRECTION('ref_axis',(1.,0.,0.));
#3159=DIRECTION('center_axis',(0.,0.,1.));
#3160=DIRECTION('ref_axis',(1.,-3.42306004707827E-13,0.));
#3161=DIRECTION('center_axis',(0.,0.,-1.));
#3162=DIRECTION('ref_axis',(1.,-3.42306004707827E-13,0.));
#3163=DIRECTION('center_axis',(0.,0.,1.));
#3164=DIRECTION('ref_axis',(1.,-3.42306004707827E-13,0.));
#3165=DIRECTION('center_axis',(0.,0.,1.));
#3166=DIRECTION('ref_axis',(-1.,0.,0.));
#3167=DIRECTION('center_axis',(0.,0.,1.));
#3168=DIRECTION('ref_axis',(-1.,0.,0.));
#3169=DIRECTION('',(0.,0.,1.));
#3170=DIRECTION('center_axis',(0.,0.,-1.));
#3171=DIRECTION('ref_axis',(-1.,0.,0.));
#3172=DIRECTION('center_axis',(0.,0.,1.));
#3173=DIRECTION('ref_axis',(-1.,0.,0.));
#3174=DIRECTION('center_axis',(0.,0.,1.));
#3175=DIRECTION('ref_axis',(-1.,0.,0.));
#3176=DIRECTION('',(0.,0.,-1.));
#3177=DIRECTION('center_axis',(0.,0.,-1.));
#3178=DIRECTION('ref_axis',(1.,0.,0.));
#3179=DIRECTION('center_axis',(0.,0.,-1.));
#3180=DIRECTION('ref_axis',(1.,0.,0.));
#3181=DIRECTION('center_axis',(0.,0.,1.));
#3182=DIRECTION('ref_axis',(-1.,0.,0.));
#3183=DIRECTION('center_axis',(0.,0.,1.));
#3184=DIRECTION('ref_axis',(0.987688340595138,-0.156434465040231,0.));
#3185=DIRECTION('',(0.,0.,1.));
#3186=DIRECTION('center_axis',(0.,0.,1.));
#3187=DIRECTION('ref_axis',(0.987688340595138,-0.156434465040231,0.));
#3188=DIRECTION('',(0.,0.,-1.));
#3189=DIRECTION('center_axis',(0.,0.,1.));
#3190=DIRECTION('ref_axis',(0.951056516295154,-0.309016994374948,0.));
#3191=DIRECTION('',(0.,0.,1.));
#3192=DIRECTION('center_axis',(0.,0.,1.));
#3193=DIRECTION('ref_axis',(0.951056516295154,-0.309016994374948,0.));
#3194=DIRECTION('',(0.,0.,-1.));
#3195=DIRECTION('center_axis',(0.,0.,1.));
#3196=DIRECTION('ref_axis',(0.891006524188368,-0.453990499739547,0.));
#3197=DIRECTION('',(0.,0.,1.));
#3198=DIRECTION('center_axis',(0.,0.,1.));
#3199=DIRECTION('ref_axis',(0.891006524188368,-0.453990499739547,0.));
#3200=DIRECTION('',(0.,0.,-1.));
#3201=DIRECTION('center_axis',(0.,0.,1.));
#3202=DIRECTION('ref_axis',(0.809016994374947,-0.587785252292473,0.));
#3203=DIRECTION('',(0.,0.,1.));
#3204=DIRECTION('center_axis',(0.,0.,1.));
#3205=DIRECTION('ref_axis',(0.809016994374947,-0.587785252292473,0.));
#3206=DIRECTION('',(0.,0.,-1.));
#3207=DIRECTION('center_axis',(0.,0.,1.));
#3208=DIRECTION('ref_axis',(0.707106781186547,-0.707106781186548,0.));
#3209=DIRECTION('',(0.,0.,1.));
#3210=DIRECTION('center_axis',(0.,0.,1.));
#3211=DIRECTION('ref_axis',(0.707106781186547,-0.707106781186548,0.));
#3212=DIRECTION('',(0.,0.,-1.));
#3213=DIRECTION('center_axis',(0.,0.,1.));
#3214=DIRECTION('ref_axis',(0.587785252292473,-0.809016994374948,0.));
#3215=DIRECTION('',(0.,0.,1.));
#3216=DIRECTION('center_axis',(0.,0.,1.));
#3217=DIRECTION('ref_axis',(0.587785252292473,-0.809016994374948,0.));
#3218=DIRECTION('',(0.,0.,-1.));
#3219=DIRECTION('center_axis',(0.,0.,1.));
#3220=DIRECTION('ref_axis',(0.453990499739547,-0.891006524188368,0.));
#3221=DIRECTION('',(0.,0.,1.));
#3222=DIRECTION('center_axis',(0.,0.,1.));
#3223=DIRECTION('ref_axis',(0.453990499739547,-0.891006524188368,0.));
#3224=DIRECTION('',(0.,0.,-1.));
#3225=DIRECTION('center_axis',(0.,0.,1.));
#3226=DIRECTION('ref_axis',(0.309016994374947,-0.951056516295154,0.));
#3227=DIRECTION('',(0.,0.,1.));
#3228=DIRECTION('center_axis',(0.,0.,1.));
#3229=DIRECTION('ref_axis',(0.309016994374947,-0.951056516295154,0.));
#3230=DIRECTION('',(0.,0.,-1.));
#3231=DIRECTION('center_axis',(0.,0.,1.));
#3232=DIRECTION('ref_axis',(0.156434465040231,-0.987688340595138,0.));
#3233=DIRECTION('',(0.,0.,1.));
#3234=DIRECTION('center_axis',(0.,0.,1.));
#3235=DIRECTION('ref_axis',(0.156434465040231,-0.987688340595138,0.));
#3236=DIRECTION('',(0.,0.,-1.));
#3237=DIRECTION('center_axis',(0.,0.,1.));
#3238=DIRECTION('ref_axis',(-1.73472347597681E-16,-1.,0.));
#3239=DIRECTION('',(0.,0.,1.));
#3240=DIRECTION('center_axis',(0.,0.,1.));
#3241=DIRECTION('ref_axis',(-1.73472347597681E-16,-1.,0.));
#3242=DIRECTION('',(0.,0.,-1.));
#3243=DIRECTION('center_axis',(0.,0.,1.));
#3244=DIRECTION('ref_axis',(-0.156434465040231,-0.987688340595138,0.));
#3245=DIRECTION('',(0.,0.,1.));
#3246=DIRECTION('center_axis',(0.,0.,1.));
#3247=DIRECTION('ref_axis',(-0.156434465040231,-0.987688340595138,0.));
#3248=DIRECTION('',(0.,0.,-1.));
#3249=DIRECTION('center_axis',(0.,0.,1.));
#3250=DIRECTION('ref_axis',(-0.309016994374948,-0.951056516295154,0.));
#3251=DIRECTION('',(0.,0.,1.));
#3252=DIRECTION('center_axis',(0.,0.,1.));
#3253=DIRECTION('ref_axis',(-0.309016994374948,-0.951056516295154,0.));
#3254=DIRECTION('',(0.,0.,-1.));
#3255=DIRECTION('center_axis',(0.,0.,1.));
#3256=DIRECTION('ref_axis',(-0.453990499739547,-0.891006524188368,0.));
#3257=DIRECTION('',(0.,0.,1.));
#3258=DIRECTION('center_axis',(0.,0.,1.));
#3259=DIRECTION('ref_axis',(-0.453990499739547,-0.891006524188368,0.));
#3260=DIRECTION('',(0.,0.,-1.));
#3261=DIRECTION('center_axis',(0.,0.,1.));
#3262=DIRECTION('ref_axis',(-0.587785252292473,-0.809016994374947,0.));
#3263=DIRECTION('',(0.,0.,1.));
#3264=DIRECTION('center_axis',(0.,0.,1.));
#3265=DIRECTION('ref_axis',(-0.587785252292473,-0.809016994374947,0.));
#3266=DIRECTION('',(0.,0.,-1.));
#3267=DIRECTION('center_axis',(0.,0.,1.));
#3268=DIRECTION('ref_axis',(-0.707106781186548,-0.707106781186548,0.));
#3269=DIRECTION('',(0.,0.,1.));
#3270=DIRECTION('center_axis',(0.,0.,1.));
#3271=DIRECTION('ref_axis',(-0.707106781186548,-0.707106781186548,0.));
#3272=DIRECTION('',(0.,0.,-1.));
#3273=DIRECTION('center_axis',(0.,0.,1.));
#3274=DIRECTION('ref_axis',(-0.809016994374947,-0.587785252292473,0.));
#3275=DIRECTION('',(0.,0.,1.));
#3276=DIRECTION('center_axis',(0.,0.,1.));
#3277=DIRECTION('ref_axis',(-0.809016994374947,-0.587785252292473,0.));
#3278=DIRECTION('',(0.,0.,-1.));
#3279=DIRECTION('center_axis',(0.,0.,1.));
#3280=DIRECTION('ref_axis',(-0.891006524188368,-0.453990499739547,0.));
#3281=DIRECTION('',(0.,0.,1.));
#3282=DIRECTION('center_axis',(0.,0.,1.));
#3283=DIRECTION('ref_axis',(-0.891006524188368,-0.453990499739547,0.));
#3284=DIRECTION('',(0.,0.,-1.));
#3285=DIRECTION('center_axis',(0.,0.,1.));
#3286=DIRECTION('ref_axis',(-0.951056516295154,-0.309016994374947,0.));
#3287=DIRECTION('',(0.,0.,1.));
#3288=DIRECTION('center_axis',(0.,0.,1.));
#3289=DIRECTION('ref_axis',(-0.951056516295154,-0.309016994374947,0.));
#3290=DIRECTION('',(0.,0.,-1.));
#3291=DIRECTION('center_axis',(0.,0.,1.));
#3292=DIRECTION('ref_axis',(-0.987688340595138,-0.156434465040231,0.));
#3293=DIRECTION('',(0.,0.,1.));
#3294=DIRECTION('center_axis',(0.,0.,1.));
#3295=DIRECTION('ref_axis',(-0.987688340595138,-0.156434465040231,0.));
#3296=DIRECTION('',(0.,0.,-1.));
#3297=DIRECTION('center_axis',(0.,0.,1.));
#3298=DIRECTION('ref_axis',(-1.,1.04083408558608E-16,0.));
#3299=DIRECTION('',(0.,0.,1.));
#3300=DIRECTION('center_axis',(0.,0.,1.));
#3301=DIRECTION('ref_axis',(-1.,1.04083408558608E-16,0.));
#3302=DIRECTION('',(0.,0.,-1.));
#3303=DIRECTION('center_axis',(0.,0.,1.));
#3304=DIRECTION('ref_axis',(-0.987688340595138,0.156434465040231,0.));
#3305=DIRECTION('',(0.,0.,1.));
#3306=DIRECTION('center_axis',(0.,0.,1.));
#3307=DIRECTION('ref_axis',(-0.987688340595138,0.156434465040231,0.));
#3308=DIRECTION('',(0.,0.,-1.));
#3309=DIRECTION('center_axis',(0.,0.,1.));
#3310=DIRECTION('ref_axis',(-0.951056516295154,0.309016994374948,0.));
#3311=DIRECTION('',(0.,0.,1.));
#3312=DIRECTION('center_axis',(0.,0.,1.));
#3313=DIRECTION('ref_axis',(-0.951056516295154,0.309016994374948,0.));
#3314=DIRECTION('',(0.,0.,-1.));
#3315=DIRECTION('center_axis',(0.,0.,1.));
#3316=DIRECTION('ref_axis',(-0.891006524188368,0.453990499739547,0.));
#3317=DIRECTION('',(0.,0.,1.));
#3318=DIRECTION('center_axis',(0.,0.,1.));
#3319=DIRECTION('ref_axis',(-0.891006524188368,0.453990499739547,0.));
#3320=DIRECTION('',(0.,0.,-1.));
#3321=DIRECTION('center_axis',(0.,0.,1.));
#3322=DIRECTION('ref_axis',(-0.809016994374947,0.587785252292473,0.));
#3323=DIRECTION('',(0.,0.,1.));
#3324=DIRECTION('center_axis',(0.,0.,1.));
#3325=DIRECTION('ref_axis',(-0.809016994374947,0.587785252292473,0.));
#3326=DIRECTION('',(0.,0.,-1.));
#3327=DIRECTION('center_axis',(0.,0.,1.));
#3328=DIRECTION('ref_axis',(-0.707106781186548,0.707106781186548,0.));
#3329=DIRECTION('',(0.,0.,1.));
#3330=DIRECTION('center_axis',(0.,0.,1.));
#3331=DIRECTION('ref_axis',(-0.707106781186548,0.707106781186548,0.));
#3332=DIRECTION('',(0.,0.,-1.));
#3333=DIRECTION('center_axis',(0.,0.,1.));
#3334=DIRECTION('ref_axis',(-0.587785252292473,0.809016994374947,0.));
#3335=DIRECTION('',(0.,0.,1.));
#3336=DIRECTION('center_axis',(0.,0.,1.));
#3337=DIRECTION('ref_axis',(-0.587785252292473,0.809016994374947,0.));
#3338=DIRECTION('',(0.,0.,-1.));
#3339=DIRECTION('center_axis',(0.,0.,1.));
#3340=DIRECTION('ref_axis',(-0.453990499739547,0.891006524188368,0.));
#3341=DIRECTION('',(0.,0.,1.));
#3342=DIRECTION('center_axis',(0.,0.,1.));
#3343=DIRECTION('ref_axis',(-0.453990499739547,0.891006524188368,0.));
#3344=DIRECTION('',(0.,0.,-1.));
#3345=DIRECTION('center_axis',(0.,0.,1.));
#3346=DIRECTION('ref_axis',(-0.309016994374947,0.951056516295154,0.));
#3347=DIRECTION('',(0.,0.,1.));
#3348=DIRECTION('center_axis',(0.,0.,1.));
#3349=DIRECTION('ref_axis',(-0.309016994374947,0.951056516295154,0.));
#3350=DIRECTION('',(0.,0.,-1.));
#3351=DIRECTION('center_axis',(0.,0.,1.));
#3352=DIRECTION('ref_axis',(-0.156434465040231,0.987688340595138,0.));
#3353=DIRECTION('',(0.,0.,1.));
#3354=DIRECTION('center_axis',(0.,0.,1.));
#3355=DIRECTION('ref_axis',(-0.156434465040231,0.987688340595138,0.));
#3356=DIRECTION('',(0.,0.,-1.));
#3357=DIRECTION('center_axis',(0.,0.,1.));
#3358=DIRECTION('ref_axis',(3.46944695195361E-17,1.,0.));
#3359=DIRECTION('',(0.,0.,1.));
#3360=DIRECTION('center_axis',(0.,0.,1.));
#3361=DIRECTION('ref_axis',(3.46944695195361E-17,1.,0.));
#3362=DIRECTION('',(0.,0.,-1.));
#3363=DIRECTION('center_axis',(0.,0.,1.));
#3364=DIRECTION('ref_axis',(0.156434465040231,0.987688340595138,0.));
#3365=DIRECTION('',(0.,0.,1.));
#3366=DIRECTION('center_axis',(0.,0.,1.));
#3367=DIRECTION('ref_axis',(0.156434465040231,0.987688340595138,0.));
#3368=DIRECTION('',(0.,0.,-1.));
#3369=DIRECTION('center_axis',(0.,0.,1.));
#3370=DIRECTION('ref_axis',(0.309016994374948,0.951056516295154,0.));
#3371=DIRECTION('',(0.,0.,1.));
#3372=DIRECTION('center_axis',(0.,0.,1.));
#3373=DIRECTION('ref_axis',(0.309016994374948,0.951056516295154,0.));
#3374=DIRECTION('',(0.,0.,-1.));
#3375=DIRECTION('center_axis',(0.,0.,1.));
#3376=DIRECTION('ref_axis',(0.453990499739547,0.891006524188368,0.));
#3377=DIRECTION('',(0.,0.,1.));
#3378=DIRECTION('center_axis',(0.,0.,1.));
#3379=DIRECTION('ref_axis',(0.453990499739547,0.891006524188368,0.));
#3380=DIRECTION('',(0.,0.,-1.));
#3381=DIRECTION('center_axis',(0.,0.,1.));
#3382=DIRECTION('ref_axis',(0.587785252292473,0.809016994374947,0.));
#3383=DIRECTION('',(0.,0.,1.));
#3384=DIRECTION('center_axis',(0.,0.,1.));
#3385=DIRECTION('ref_axis',(0.587785252292473,0.809016994374947,0.));
#3386=DIRECTION('',(0.,0.,-1.));
#3387=DIRECTION('center_axis',(0.,0.,1.));
#3388=DIRECTION('ref_axis',(0.707106781186548,0.707106781186548,0.));
#3389=DIRECTION('',(0.,0.,1.));
#3390=DIRECTION('center_axis',(0.,0.,1.));
#3391=DIRECTION('ref_axis',(0.707106781186548,0.707106781186548,0.));
#3392=DIRECTION('',(0.,0.,-1.));
#3393=DIRECTION('center_axis',(0.,0.,1.));
#3394=DIRECTION('ref_axis',(0.809016994374947,0.587785252292473,0.));
#3395=DIRECTION('',(0.,0.,1.));
#3396=DIRECTION('center_axis',(0.,0.,1.));
#3397=DIRECTION('ref_axis',(0.809016994374947,0.587785252292473,0.));
#3398=DIRECTION('',(0.,0.,-1.));
#3399=DIRECTION('center_axis',(0.,0.,1.));
#3400=DIRECTION('ref_axis',(0.891006524188368,0.453990499739547,0.));
#3401=DIRECTION('',(0.,0.,1.));
#3402=DIRECTION('center_axis',(0.,0.,1.));
#3403=DIRECTION('ref_axis',(0.891006524188368,0.453990499739547,0.));
#3404=DIRECTION('',(0.,0.,-1.));
#3405=DIRECTION('center_axis',(0.,0.,1.));
#3406=DIRECTION('ref_axis',(0.951056516295154,0.309016994374947,0.));
#3407=DIRECTION('',(0.,0.,1.));
#3408=DIRECTION('center_axis',(0.,0.,1.));
#3409=DIRECTION('ref_axis',(0.951056516295154,0.309016994374947,0.));
#3410=DIRECTION('',(0.,0.,-1.));
#3411=DIRECTION('center_axis',(0.,0.,1.));
#3412=DIRECTION('ref_axis',(0.987688340595138,0.156434465040231,0.));
#3413=DIRECTION('',(0.,0.,1.));
#3414=DIRECTION('center_axis',(0.,0.,1.));
#3415=DIRECTION('ref_axis',(0.987688340595138,0.156434465040231,0.));
#3416=DIRECTION('',(0.,0.,-1.));
#3417=DIRECTION('center_axis',(0.,0.,1.));
#3418=DIRECTION('ref_axis',(1.,0.,0.));
#3419=DIRECTION('center_axis',(0.,0.,1.));
#3420=DIRECTION('ref_axis',(1.,0.,0.));
#3421=DIRECTION('center_axis',(0.,0.,1.));
#3422=DIRECTION('ref_axis',(1.,0.,0.));
#3423=DIRECTION('center_axis',(0.,0.,1.));
#3424=DIRECTION('ref_axis',(1.,0.,0.));
#3425=DIRECTION('center_axis',(0.,0.,1.));
#3426=DIRECTION('ref_axis',(1.,0.,0.));
#3427=DIRECTION('center_axis',(0.,0.,1.));
#3428=DIRECTION('ref_axis',(1.,0.,0.));
#3429=DIRECTION('center_axis',(0.,0.,1.));
#3430=DIRECTION('ref_axis',(1.,0.,0.));
#3431=DIRECTION('center_axis',(0.,0.,1.));
#3432=DIRECTION('ref_axis',(1.,0.,0.));
#3433=DIRECTION('center_axis',(0.,0.,1.));
#3434=DIRECTION('ref_axis',(1.,0.,0.));
#3435=DIRECTION('center_axis',(0.,0.,1.));
#3436=DIRECTION('ref_axis',(1.,0.,0.));
#3437=DIRECTION('center_axis',(0.,0.,1.));
#3438=DIRECTION('ref_axis',(1.,0.,0.));
#3439=DIRECTION('center_axis',(0.,0.,1.));
#3440=DIRECTION('ref_axis',(1.,0.,0.));
#3441=DIRECTION('center_axis',(0.,0.,1.));
#3442=DIRECTION('ref_axis',(1.,0.,0.));
#3443=DIRECTION('center_axis',(0.,0.,1.));
#3444=DIRECTION('ref_axis',(1.,0.,0.));
#3445=DIRECTION('center_axis',(0.,0.,1.));
#3446=DIRECTION('ref_axis',(1.,0.,0.));
#3447=DIRECTION('center_axis',(0.,0.,1.));
#3448=DIRECTION('ref_axis',(1.,0.,0.));
#3449=DIRECTION('center_axis',(0.,0.,1.));
#3450=DIRECTION('ref_axis',(1.,0.,0.));
#3451=DIRECTION('center_axis',(0.,0.,1.));
#3452=DIRECTION('ref_axis',(1.,0.,0.));
#3453=DIRECTION('center_axis',(0.,0.,1.));
#3454=DIRECTION('ref_axis',(1.,0.,0.));
#3455=DIRECTION('center_axis',(0.,0.,1.));
#3456=DIRECTION('ref_axis',(1.,0.,0.));
#3457=DIRECTION('center_axis',(0.,0.,1.));
#3458=DIRECTION('ref_axis',(1.,0.,0.));
#3459=DIRECTION('center_axis',(0.,0.,1.));
#3460=DIRECTION('ref_axis',(1.,0.,0.));
#3461=DIRECTION('center_axis',(0.,0.,1.));
#3462=DIRECTION('ref_axis',(1.,0.,0.));
#3463=DIRECTION('center_axis',(0.,0.,1.));
#3464=DIRECTION('ref_axis',(1.,0.,0.));
#3465=DIRECTION('center_axis',(0.,0.,1.));
#3466=DIRECTION('ref_axis',(1.,0.,0.));
#3467=DIRECTION('center_axis',(0.,0.,1.));
#3468=DIRECTION('ref_axis',(1.,0.,0.));
#3469=DIRECTION('center_axis',(0.,0.,1.));
#3470=DIRECTION('ref_axis',(1.,0.,0.));
#3471=DIRECTION('center_axis',(0.,0.,1.));
#3472=DIRECTION('ref_axis',(1.,0.,0.));
#3473=DIRECTION('center_axis',(0.,0.,1.));
#3474=DIRECTION('ref_axis',(1.,0.,0.));
#3475=DIRECTION('center_axis',(0.,0.,1.));
#3476=DIRECTION('ref_axis',(1.,0.,0.));
#3477=DIRECTION('center_axis',(0.,0.,1.));
#3478=DIRECTION('ref_axis',(1.,0.,0.));
#3479=DIRECTION('center_axis',(0.,0.,1.));
#3480=DIRECTION('ref_axis',(1.,0.,0.));
#3481=DIRECTION('center_axis',(0.,0.,1.));
#3482=DIRECTION('ref_axis',(1.,0.,0.));
#3483=DIRECTION('center_axis',(0.,0.,1.));
#3484=DIRECTION('ref_axis',(1.,0.,0.));
#3485=DIRECTION('center_axis',(0.,0.,1.));
#3486=DIRECTION('ref_axis',(1.,0.,0.));
#3487=DIRECTION('center_axis',(0.,0.,1.));
#3488=DIRECTION('ref_axis',(1.,0.,0.));
#3489=DIRECTION('center_axis',(0.,0.,1.));
#3490=DIRECTION('ref_axis',(1.,0.,0.));
#3491=DIRECTION('center_axis',(0.,0.,1.));
#3492=DIRECTION('ref_axis',(1.,0.,0.));
#3493=DIRECTION('center_axis',(0.,0.,1.));
#3494=DIRECTION('ref_axis',(1.,0.,0.));
#3495=DIRECTION('center_axis',(0.,0.,1.));
#3496=DIRECTION('ref_axis',(1.,0.,0.));
#3497=DIRECTION('center_axis',(0.,0.,1.));
#3498=DIRECTION('ref_axis',(1.,0.,0.));
#3499=DIRECTION('center_axis',(0.,0.,1.));
#3500=DIRECTION('ref_axis',(1.,0.,0.));
#3501=DIRECTION('center_axis',(0.,0.,1.));
#3502=DIRECTION('ref_axis',(1.,0.,0.));
#3503=DIRECTION('center_axis',(0.,0.,1.));
#3504=DIRECTION('ref_axis',(1.,0.,0.));
#3505=DIRECTION('',(0.,0.,-1.));
#3506=DIRECTION('center_axis',(0.,0.,1.));
#3507=DIRECTION('ref_axis',(1.,0.,0.));
#3508=DIRECTION('center_axis',(0.,0.,1.));
#3509=DIRECTION('ref_axis',(1.,0.,0.));
#3510=DIRECTION('center_axis',(0.,0.,1.));
#3511=DIRECTION('ref_axis',(1.,0.,0.));
#3512=DIRECTION('center_axis',(0.,0.,1.));
#3513=DIRECTION('ref_axis',(1.,0.,0.));
#3514=DIRECTION('center_axis',(0.,0.,1.));
#3515=DIRECTION('ref_axis',(1.,0.,0.));
#3516=DIRECTION('center_axis',(0.,0.,1.));
#3517=DIRECTION('ref_axis',(1.,0.,0.));
#3518=DIRECTION('center_axis',(0.,0.,1.));
#3519=DIRECTION('ref_axis',(1.,0.,0.));
#3520=DIRECTION('center_axis',(0.,0.,1.));
#3521=DIRECTION('ref_axis',(1.,0.,0.));
#3522=DIRECTION('center_axis',(0.,0.,1.));
#3523=DIRECTION('ref_axis',(1.,0.,0.));
#3524=DIRECTION('center_axis',(0.,0.,1.));
#3525=DIRECTION('ref_axis',(1.,0.,0.));
#3526=DIRECTION('center_axis',(0.,0.,1.));
#3527=DIRECTION('ref_axis',(1.,0.,0.));
#3528=DIRECTION('center_axis',(0.,0.,1.));
#3529=DIRECTION('ref_axis',(1.,0.,0.));
#3530=DIRECTION('center_axis',(0.,0.,1.));
#3531=DIRECTION('ref_axis',(1.,0.,0.));
#3532=DIRECTION('center_axis',(0.,0.,1.));
#3533=DIRECTION('ref_axis',(1.,0.,0.));
#3534=DIRECTION('center_axis',(0.,0.,1.));
#3535=DIRECTION('ref_axis',(1.,0.,0.));
#3536=DIRECTION('center_axis',(0.,0.,1.));
#3537=DIRECTION('ref_axis',(1.,0.,0.));
#3538=DIRECTION('center_axis',(0.,0.,1.));
#3539=DIRECTION('ref_axis',(1.,0.,0.));
#3540=DIRECTION('center_axis',(0.,0.,1.));
#3541=DIRECTION('ref_axis',(1.,0.,0.));
#3542=DIRECTION('center_axis',(0.,0.,1.));
#3543=DIRECTION('ref_axis',(1.,0.,0.));
#3544=DIRECTION('center_axis',(0.,0.,1.));
#3545=DIRECTION('ref_axis',(1.,0.,0.));
#3546=DIRECTION('center_axis',(0.,0.,1.));
#3547=DIRECTION('ref_axis',(1.,0.,0.));
#3548=DIRECTION('center_axis',(0.,0.,1.));
#3549=DIRECTION('ref_axis',(1.,0.,0.));
#3550=DIRECTION('center_axis',(0.,0.,1.));
#3551=DIRECTION('ref_axis',(1.,0.,0.));
#3552=DIRECTION('center_axis',(0.,0.,1.));
#3553=DIRECTION('ref_axis',(1.,0.,0.));
#3554=DIRECTION('center_axis',(0.,0.,1.));
#3555=DIRECTION('ref_axis',(1.,0.,0.));
#3556=DIRECTION('center_axis',(0.,0.,1.));
#3557=DIRECTION('ref_axis',(1.,0.,0.));
#3558=DIRECTION('center_axis',(0.,0.,1.));
#3559=DIRECTION('ref_axis',(1.,0.,0.));
#3560=DIRECTION('center_axis',(0.,0.,1.));
#3561=DIRECTION('ref_axis',(1.,0.,0.));
#3562=DIRECTION('center_axis',(0.,0.,1.));
#3563=DIRECTION('ref_axis',(1.,0.,0.));
#3564=DIRECTION('center_axis',(0.,0.,1.));
#3565=DIRECTION('ref_axis',(1.,0.,0.));
#3566=DIRECTION('center_axis',(0.,0.,1.));
#3567=DIRECTION('ref_axis',(1.,0.,0.));
#3568=DIRECTION('center_axis',(0.,0.,1.));
#3569=DIRECTION('ref_axis',(1.,0.,0.));
#3570=DIRECTION('center_axis',(0.,0.,1.));
#3571=DIRECTION('ref_axis',(1.,0.,0.));
#3572=DIRECTION('center_axis',(0.,0.,1.));
#3573=DIRECTION('ref_axis',(1.,0.,0.));
#3574=DIRECTION('center_axis',(0.,0.,1.));
#3575=DIRECTION('ref_axis',(1.,0.,0.));
#3576=DIRECTION('center_axis',(0.,0.,1.));
#3577=DIRECTION('ref_axis',(1.,0.,0.));
#3578=DIRECTION('center_axis',(0.,0.,1.));
#3579=DIRECTION('ref_axis',(1.,0.,0.));
#3580=DIRECTION('center_axis',(0.,0.,1.));
#3581=DIRECTION('ref_axis',(1.,0.,0.));
#3582=DIRECTION('center_axis',(0.,0.,1.));
#3583=DIRECTION('ref_axis',(1.,0.,0.));
#3584=DIRECTION('center_axis',(0.,0.,1.));
#3585=DIRECTION('ref_axis',(1.,0.,0.));
#3586=DIRECTION('center_axis',(0.,0.,1.));
#3587=DIRECTION('ref_axis',(1.,0.,0.));
#3588=DIRECTION('center_axis',(0.,0.,1.));
#3589=DIRECTION('ref_axis',(1.,0.,0.));
#3590=DIRECTION('center_axis',(0.,0.,1.));
#3591=DIRECTION('ref_axis',(1.,0.,0.));
#3592=DIRECTION('center_axis',(0.,0.,1.));
#3593=DIRECTION('ref_axis',(1.,0.,0.));
#3594=DIRECTION('center_axis',(0.,0.,1.));
#3595=DIRECTION('ref_axis',(1.,0.,0.));
#3596=DIRECTION('center_axis',(0.,0.,1.));
#3597=DIRECTION('ref_axis',(1.,0.,0.));
#3598=DIRECTION('center_axis',(0.,0.,1.));
#3599=DIRECTION('ref_axis',(1.,0.,0.));
#3600=DIRECTION('center_axis',(0.,0.,1.));
#3601=DIRECTION('ref_axis',(1.,0.,0.));
#3602=DIRECTION('center_axis',(0.,0.,1.));
#3603=DIRECTION('ref_axis',(1.,0.,0.));
#3604=DIRECTION('center_axis',(0.,0.,1.));
#3605=DIRECTION('ref_axis',(1.,0.,0.));
#3606=DIRECTION('center_axis',(0.,0.,1.));
#3607=DIRECTION('ref_axis',(1.,0.,0.));
#3608=DIRECTION('center_axis',(0.,0.,1.));
#3609=DIRECTION('ref_axis',(1.,0.,0.));
#3610=DIRECTION('center_axis',(0.,0.,1.));
#3611=DIRECTION('ref_axis',(1.,0.,0.));
#3612=DIRECTION('center_axis',(0.,0.,1.));
#3613=DIRECTION('ref_axis',(1.,0.,0.));
#3614=DIRECTION('center_axis',(0.,0.,1.));
#3615=DIRECTION('ref_axis',(1.,0.,0.));
#3616=DIRECTION('center_axis',(0.,0.,1.));
#3617=DIRECTION('ref_axis',(1.,0.,0.));
#3618=DIRECTION('center_axis',(0.,0.,1.));
#3619=DIRECTION('ref_axis',(1.,0.,0.));
#3620=DIRECTION('center_axis',(0.,0.,1.));
#3621=DIRECTION('ref_axis',(1.,0.,0.));
#3622=DIRECTION('center_axis',(0.,0.,1.));
#3623=DIRECTION('ref_axis',(1.,0.,0.));
#3624=DIRECTION('center_axis',(0.,0.,1.));
#3625=DIRECTION('ref_axis',(1.,0.,0.));
#3626=DIRECTION('center_axis',(0.,0.,1.));
#3627=DIRECTION('ref_axis',(1.,0.,0.));
#3628=DIRECTION('center_axis',(0.,0.,1.));
#3629=DIRECTION('ref_axis',(1.,0.,0.));
#3630=DIRECTION('center_axis',(0.,0.,1.));
#3631=DIRECTION('ref_axis',(1.,0.,0.));
#3632=DIRECTION('center_axis',(0.,0.,1.));
#3633=DIRECTION('ref_axis',(1.,0.,0.));
#3634=DIRECTION('center_axis',(0.,0.,1.));
#3635=DIRECTION('ref_axis',(1.,0.,0.));
#3636=DIRECTION('center_axis',(0.,0.,1.));
#3637=DIRECTION('ref_axis',(1.,0.,0.));
#3638=DIRECTION('center_axis',(0.,0.,1.));
#3639=DIRECTION('ref_axis',(1.,0.,0.));
#3640=DIRECTION('center_axis',(0.,0.,1.));
#3641=DIRECTION('ref_axis',(1.,0.,0.));
#3642=DIRECTION('center_axis',(0.,0.,1.));
#3643=DIRECTION('ref_axis',(1.,0.,0.));
#3644=DIRECTION('center_axis',(0.,0.,1.));
#3645=DIRECTION('ref_axis',(1.,0.,0.));
#3646=DIRECTION('center_axis',(0.,0.,1.));
#3647=DIRECTION('ref_axis',(1.,0.,0.));
#3648=DIRECTION('center_axis',(0.,0.,1.));
#3649=DIRECTION('ref_axis',(1.,0.,0.));
#3650=DIRECTION('center_axis',(0.,0.,1.));
#3651=DIRECTION('ref_axis',(1.,0.,0.));
#3652=DIRECTION('center_axis',(0.,0.,1.));
#3653=DIRECTION('ref_axis',(1.,0.,0.));
#3654=DIRECTION('center_axis',(0.,0.,1.));
#3655=DIRECTION('ref_axis',(1.,0.,0.));
#3656=DIRECTION('center_axis',(0.,0.,1.));
#3657=DIRECTION('ref_axis',(1.,0.,0.));
#3658=DIRECTION('center_axis',(0.,0.,1.));
#3659=DIRECTION('ref_axis',(1.,0.,0.));
#3660=DIRECTION('center_axis',(1.22464679914735E-16,-1.,0.));
#3661=DIRECTION('ref_axis',(-1.,-1.22464679914735E-16,0.));
#3662=DIRECTION('center_axis',(0.,0.,1.));
#3663=DIRECTION('ref_axis',(1.,0.,0.));
#3664=DIRECTION('center_axis',(0.,0.,1.));
#3665=DIRECTION('ref_axis',(1.,0.,0.));
#3666=DIRECTION('',(0.,0.,1.));
#3667=DIRECTION('center_axis',(0.,0.,1.));
#3668=DIRECTION('ref_axis',(1.,0.,0.));
#3669=DIRECTION('center_axis',(0.,0.,1.));
#3670=DIRECTION('ref_axis',(1.,0.,0.));
#3671=DIRECTION('center_axis',(0.,0.,1.));
#3672=DIRECTION('ref_axis',(1.,0.,0.));
#3809=CARTESIAN_POINT('',(0.,0.,0.));
#3810=CARTESIAN_POINT('Origin',(0.,0.,0.));
#3811=CARTESIAN_POINT('',(-2.45356474526275,0.00152995343032009,5.25782749621206));
#3812=CARTESIAN_POINT('',(1.07686357729864,2.20575430139124,5.00004572388937));
#3813=CARTESIAN_POINT('Ctrl Pts',(-2.45356474526275,0.00152995343032009,
5.25782749621206));
#3814=CARTESIAN_POINT('Ctrl Pts',(-2.45409117603731,0.080350384053512,5.25371719896929));
#3815=CARTESIAN_POINT('Ctrl Pts',(-2.41487113252746,0.971399642855625,5.2072215692543));
#3816=CARTESIAN_POINT('Ctrl Pts',(-1.36218010227536,2.52198105473234,5.12129431181338));
#3817=CARTESIAN_POINT('Ctrl Pts',(0.395824647622223,2.53385365630773,5.03947735161525));
#3818=CARTESIAN_POINT('Ctrl Pts',(1.07686357729864,2.20575430139124,5.00004572388937));
#3819=CARTESIAN_POINT('',(-1.07508846035114,2.20207516956615,5.));
#3820=CARTESIAN_POINT('Origin',(0.,0.,5.));
#3821=CARTESIAN_POINT('',(-2.45049860469171,0.00261503422208265,5.14217250381425));
#3822=CARTESIAN_POINT('Ctrl Pts',(-1.07508846035114,2.20207516956616,4.99999999999999));
#3823=CARTESIAN_POINT('Ctrl Pts',(-1.14997601337418,2.16551386358001,5.00432999723329));
#3824=CARTESIAN_POINT('Ctrl Pts',(-1.22304980119226,2.12510255608252,5.00865999446659));
#3825=CARTESIAN_POINT('Ctrl Pts',(-1.29390582758922,2.08104732270332,5.01298999169989));
#3826=CARTESIAN_POINT('Ctrl Pts',(-1.36471897746647,2.03701874810219,5.01731736875787));
#3827=CARTESIAN_POINT('Ctrl Pts',(-1.43331666889977,1.98935086391144,5.02164474581584));
#3828=CARTESIAN_POINT('Ctrl Pts',(-1.49932095835489,1.9382948469822,5.02597212287382));
#3829=CARTESIAN_POINT('Ctrl Pts',(-1.56531867275687,1.88724391602582,5.03029906885778));
#3830=CARTESIAN_POINT('Ctrl Pts',(-1.62872314993186,1.83280578064197,5.03462601484175));
#3831=CARTESIAN_POINT('Ctrl Pts',(-1.68918738086506,1.77527356830609,5.03895296082571));
#3832=CARTESIAN_POINT('Ctrl Pts',(-1.7496502279544,1.717742672709,5.04327980777893));
#3833=CARTESIAN_POINT('Ctrl Pts',(-1.80717264793702,1.65711813963895,5.04760665473215));
#3834=CARTESIAN_POINT('Ctrl Pts',(-1.86144348904875,1.59373096445982,5.05193350168537));
#3835=CARTESIAN_POINT('Ctrl Pts',(-1.91572620376788,1.53032992116261,5.05626129528472));
#3836=CARTESIAN_POINT('Ctrl Pts',(-1.96675564225295,1.46416536295762,5.06058908888408));
#3837=CARTESIAN_POINT('Ctrl Pts',(-2.01426073044554,1.39560164795869,5.06491688248343));
#3838=CARTESIAN_POINT('Ctrl Pts',(-2.06178769630728,1.32700635709431,5.06924666917532));
#3839=CARTESIAN_POINT('Ctrl Pts',(-2.1057868362227,1.25601006801191,5.07357645586721));
#3840=CARTESIAN_POINT('Ctrl Pts',(-2.14603079884992,1.18300552001569,5.0779062425591));
#3841=CARTESIAN_POINT('Ctrl Pts',(-2.18633477118484,1.10989211142771,5.08224248560412));
#3842=CARTESIAN_POINT('Ctrl Pts',(-2.22287217294086,1.03476484378008,5.08657872864913));
#3843=CARTESIAN_POINT('Ctrl Pts',(-2.25546198297408,0.958040444531769,5.09091497169414));
#3844=CARTESIAN_POINT('Ctrl Pts',(-2.28807677467307,0.881257232320273,5.09525453867919));
#3845=CARTESIAN_POINT('Ctrl Pts',(-2.3167377947772,0.802874856085788,5.09959410566424));
#3846=CARTESIAN_POINT('Ctrl Pts',(-2.3413133247558,0.723327149580979,5.10393367264929));
#3847=CARTESIAN_POINT('Ctrl Pts',(-2.36593742471167,0.643622228550178,5.10828181616026));
#3848=CARTESIAN_POINT('Ctrl Pts',(-2.38645979089026,0.562747795751204,5.11262995967123));
#3849=CARTESIAN_POINT('Ctrl Pts',(-2.40279937300748,0.481150104515044,5.1169781031822));
#3850=CARTESIAN_POINT('Ctrl Pts',(-2.41554830353427,0.417483647854612,5.12037073459371));
#3851=CARTESIAN_POINT('Ctrl Pts',(-2.4257518367838,0.353377142239134,5.12376336600522));
#3852=CARTESIAN_POINT('Ctrl Pts',(-2.4333934596506,0.289044149793245,5.12715599741673));
#3853=CARTESIAN_POINT('Ctrl Pts',(-2.44466794097471,0.194126992207884,5.13216149954048));
#3854=CARTESIAN_POINT('Ctrl Pts',(-2.45039629736826,0.0984852538315921,
5.13716700166423));
#3855=CARTESIAN_POINT('Ctrl Pts',(-2.45049860469117,0.00261503472503235,
5.14217250378799));
#3856=CARTESIAN_POINT('',(-2.45037982140539,0.00118543379578927,5.94217245212152));
#3857=CARTESIAN_POINT('Ctrl Pts',(-2.45049860469171,0.00261503422208265,
5.14217250381425));
#3858=CARTESIAN_POINT('Ctrl Pts',(-2.45058302321086,-0.0764919471070318,
5.14630277666366));
#3859=CARTESIAN_POINT('Ctrl Pts',(-2.44683272820233,-0.155776824651178,
5.15043304951307));
#3860=CARTESIAN_POINT('Ctrl Pts',(-2.43922269256381,-0.234825267128065,
5.15456332236248));
#3861=CARTESIAN_POINT('Ctrl Pts',(-2.43156489589117,-0.314369822308958,
5.15871951704877));
#3862=CARTESIAN_POINT('Ctrl Pts',(-2.41999865856044,-0.393674469734343,
5.16287571173506));
#3863=CARTESIAN_POINT('Ctrl Pts',(-2.40455179794988,-0.472314409028569,
5.16703190642135));
#3864=CARTESIAN_POINT('Ctrl Pts',(-2.38923709986016,-0.550281509169413,
5.17115254092615));
#3865=CARTESIAN_POINT('Ctrl Pts',(-2.37010800517999,-0.627594741949263,
5.17527317543095));
#3866=CARTESIAN_POINT('Ctrl Pts',(-2.34724361971563,-0.703844897476893,
5.17939380993574));
#3867=CARTESIAN_POINT('Ctrl Pts',(-2.32439056232828,-0.780057275140982,
5.18351240288709));
#3868=CARTESIAN_POINT('Ctrl Pts',(-2.29780602312865,-0.855207153541872,
5.18763099583844));
#3869=CARTESIAN_POINT('Ctrl Pts',(-2.26761965700325,-0.928897917519714,
5.19174958878978));
#3870=CARTESIAN_POINT('Ctrl Pts',(-2.23743809527637,-1.00257695303062,5.19586752623454));
#3871=CARTESIAN_POINT('Ctrl Pts',(-2.20365602983411,-1.0747968840735,5.1999854636793));
#3872=CARTESIAN_POINT('Ctrl Pts',(-2.16645157775396,-1.14518025273202,5.20410340112406));
#3873=CARTESIAN_POINT('Ctrl Pts',(-2.12864982133805,-1.21669360151161,5.20828745059984));
#3874=CARTESIAN_POINT('Ctrl Pts',(-2.08731503604085,-1.28631042558811,5.21247150007563));
#3875=CARTESIAN_POINT('Ctrl Pts',(-2.04268202130169,-1.3536618521074,5.21665554955141));
#3876=CARTESIAN_POINT('Ctrl Pts',(-1.99869777550263,-1.42003428328317,5.22077878123661));
#3877=CARTESIAN_POINT('Ctrl Pts',(-1.9515109020942,-1.48420638414124,5.2249020129218));
#3878=CARTESIAN_POINT('Ctrl Pts',(-1.90138785861859,-1.54585719298317,5.229025244607));
#3879=CARTESIAN_POINT('Ctrl Pts',(-1.85015584055906,-1.60887202873456,5.23323970297808));
#3880=CARTESIAN_POINT('Ctrl Pts',(-1.79585653538997,-1.66925227002323,5.23745416134915));
#3881=CARTESIAN_POINT('Ctrl Pts',(-1.73881377385387,-1.72669537262832,5.24166861972023));
#3882=CARTESIAN_POINT('Ctrl Pts',(-1.68177101231777,-1.78413847523342,5.24588307809131));
#3883=CARTESIAN_POINT('Ctrl Pts',(-1.62198524404679,-1.83864413938822,5.25009753646239));
#3884=CARTESIAN_POINT('Ctrl Pts',(-1.55981367463781,-1.88995543609178,5.25431199483346));
#3885=CARTESIAN_POINT('Ctrl Pts',(-1.49730868428688,-1.94154191100047,5.25854905499332));
#3886=CARTESIAN_POINT('Ctrl Pts',(-1.43212632800358,-1.99011962445967,5.26278611515318));
#3887=CARTESIAN_POINT('Ctrl Pts',(-1.36458787377452,-2.03539926912327,5.26702317531304));
#3888=CARTESIAN_POINT('Ctrl Pts',(-1.29714621498398,-2.08061401945206,5.27125416296056));
#3889=CARTESIAN_POINT('Ctrl Pts',(-1.22735554698235,-2.12253983351051,5.27548515060809));
#3890=CARTESIAN_POINT('Ctrl Pts',(-1.15557029346231,-2.16092747376385,5.27971613825561));
#3891=CARTESIAN_POINT('Ctrl Pts',(-1.08363789016749,-2.19939380333486,5.28395579883872));
#3892=CARTESIAN_POINT('Ctrl Pts',(-1.00970308479543,-2.23430714871968,5.28819545942183));
#3893=CARTESIAN_POINT('Ctrl Pts',(-0.934151886214295,-2.26546032926694,
5.29243512000494));
#3894=CARTESIAN_POINT('Ctrl Pts',(-0.858891746631583,-2.29649349300841,
5.29665844740755));
#3895=CARTESIAN_POINT('Ctrl Pts',(-0.782028071175863,-2.32379522194956,
5.30088177481017));
#3896=CARTESIAN_POINT('Ctrl Pts',(-0.703965558134562,-2.34720743500874,
5.30510510221278));
#3897=CARTESIAN_POINT('Ctrl Pts',(-0.625929411642454,-2.37061174031241,
5.30932700313595));
#3898=CARTESIAN_POINT('Ctrl Pts',(-0.54669567529644,-2.39012900583903,5.31354890405913));
#3899=CARTESIAN_POINT('Ctrl Pts',(-0.46668533523853,-2.40565064959011,5.31777080498231));
#3900=CARTESIAN_POINT('Ctrl Pts',(-0.386677700793962,-2.42117176846444,
5.32199256313854));
#3901=CARTESIAN_POINT('Ctrl Pts',(-0.305893969996252,-2.43269744697983,
5.32621432129477));
#3902=CARTESIAN_POINT('Ctrl Pts',(-0.224765082065273,-2.44017026206865,
5.33043607945101));
#3903=CARTESIAN_POINT('Ctrl Pts',(-0.143042369608102,-2.44769777457774,
5.33468873885094));
#3904=CARTESIAN_POINT('Ctrl Pts',(-0.0609698994006798,-2.45111278889587,
5.33894139825088));
#3905=CARTESIAN_POINT('Ctrl Pts',(0.0210086863910375,-2.45040994225377,
5.34319405765081));
#3906=CARTESIAN_POINT('Ctrl Pts',(0.102506869309902,-2.44971121436467,5.34742179603297));
#3907=CARTESIAN_POINT('Ctrl Pts',(0.183911801552402,-2.44494284287907,5.35164953441514));
#3908=CARTESIAN_POINT('Ctrl Pts',(0.264791488201769,-2.43615182568244,5.3558772727973));
#3909=CARTESIAN_POINT('Ctrl Pts',(0.346386310436315,-2.42728307859481,5.36014239270612));
#3910=CARTESIAN_POINT('Ctrl Pts',(0.427446077354026,-2.41432027290381,5.36440751261494));
#3911=CARTESIAN_POINT('Ctrl Pts',(0.507538340512369,-2.39736419488361,5.36867263252375));
#3912=CARTESIAN_POINT('Ctrl Pts',(0.587630603670713,-2.38040811686342,5.37293775243257));
#3913=CARTESIAN_POINT('Ctrl Pts',(0.666754917165274,-2.35945894848903,5.37720287234138));
#3914=CARTESIAN_POINT('Ctrl Pts',(0.744496850786636,-2.33466800405728,5.3814679922502));
#3915=CARTESIAN_POINT('Ctrl Pts',(0.821746571718491,-2.31003402018549,5.38570610812086));
#3916=CARTESIAN_POINT('Ctrl Pts',(0.897911818200014,-2.28151738336742,5.38994422399153));
#3917=CARTESIAN_POINT('Ctrl Pts',(0.972575382730247,-2.2492326191186,5.39418233986219));
#3918=CARTESIAN_POINT('Ctrl Pts',(1.04713454354207,-2.21699299937175,5.39841452948143));
#3919=CARTESIAN_POINT('Ctrl Pts',(1.12019577159397,-2.18099590050983,5.40264671910067));
#3920=CARTESIAN_POINT('Ctrl Pts',(1.19135773665969,-2.14140537808727,5.4068789087199));
#3921=CARTESIAN_POINT('Ctrl Pts',(1.26264057670397,-2.10174760761241,5.41111828709269));
#3922=CARTESIAN_POINT('Ctrl Pts',(1.33201725536202,-2.05848435350727,5.41535766546549));
#3923=CARTESIAN_POINT('Ctrl Pts',(1.39910526965682,-2.01182869410358,5.41959704383828));
#3924=CARTESIAN_POINT('Ctrl Pts',(1.46596383919209,-1.9653325996634,5.42382192330003));
#3925=CARTESIAN_POINT('Ctrl Pts',(1.53054898433385,-1.91546752127288,5.42804680276178));
#3926=CARTESIAN_POINT('Ctrl Pts',(1.59250901370515,-1.86248900433475,5.43227168222353));
#3927=CARTESIAN_POINT('Ctrl Pts',(1.65445001563708,-1.80952675668392,5.43649526425791));
#3928=CARTESIAN_POINT('Ctrl Pts',(1.71376715112393,-1.75345327018786,5.44071884629229));
#3929=CARTESIAN_POINT('Ctrl Pts',(1.77014163171871,-1.69456450265437,5.44494242832668));
#3930=CARTESIAN_POINT('Ctrl Pts',(1.82651590672143,-1.63567594988227,5.44916599495808));
#3931=CARTESIAN_POINT('Ctrl Pts',(1.87994722879997,-1.5739724719131,5.45338956158949));
#3932=CARTESIAN_POINT('Ctrl Pts',(1.93015452266398,-1.50978600094179,5.45761312822089));
#3933=CARTESIAN_POINT('Ctrl Pts',(1.98068680052275,-1.44518406093918,5.46186403334139));
#3934=CARTESIAN_POINT('Ctrl Pts',(2.02795285798575,-1.37806723247651,5.4661149384619));
#3935=CARTESIAN_POINT('Ctrl Pts',(2.07170921576142,-1.30880524728823,5.4703658435824));
#3936=CARTESIAN_POINT('Ctrl Pts',(2.11524878101552,-1.23988642321256,5.47459568743348));
#3937=CARTESIAN_POINT('Ctrl Pts',(2.15531316372334,-1.16884408430403,5.47882553128456));
#3938=CARTESIAN_POINT('Ctrl Pts',(2.19170859473218,-1.09606737282755,5.48305537513565));
#3939=CARTESIAN_POINT('Ctrl Pts',(2.2283758563352,-1.02274710585042,5.48731681089086));
#3940=CARTESIAN_POINT('Ctrl Pts',(2.26131894199366,-0.947666889131624,5.49157824664608));
#3941=CARTESIAN_POINT('Ctrl Pts',(2.29038969987444,-0.871243520899339,5.49583968240129));
#3942=CARTESIAN_POINT('Ctrl Pts',(2.31946045775522,-0.794820152667054,5.50010111815651));
#3943=CARTESIAN_POINT('Ctrl Pts',(2.34465880176593,-0.717054103088672,5.50436255391172));
#3944=CARTESIAN_POINT('Ctrl Pts',(2.36588855649591,-0.638374175732132,5.50862398966694));
#3945=CARTESIAN_POINT('Ctrl Pts',(2.38693658795721,-0.560367735835114,5.51284894822095));
#3946=CARTESIAN_POINT('Ctrl Pts',(2.40416312148486,-0.481168656178992,5.51707390677496));
#3947=CARTESIAN_POINT('Ctrl Pts',(2.41743659529903,-0.401186437593617,5.52129886532898));
#3948=CARTESIAN_POINT('Ctrl Pts',(2.43069072165616,-0.321320801340671,5.52551766557016));
#3949=CARTESIAN_POINT('Ctrl Pts',(2.4400031551689,-0.240674749196244,5.52973646581135));
#3950=CARTESIAN_POINT('Ctrl Pts',(2.4452924611764,-0.159671629646227,5.53395526605254));
#3951=CARTESIAN_POINT('Ctrl Pts',(2.4506117272974,-0.0782096856960176,5.53819796276217));
#3952=CARTESIAN_POINT('Ctrl Pts',(2.45186201374226,0.00361292325704207,
5.54244065947179));
#3953=CARTESIAN_POINT('Ctrl Pts',(2.4490129663411,0.0853565503823599,5.54668335618143));
#3954=CARTESIAN_POINT('Ctrl Pts',(2.44618518850525,0.166489920403897,5.55089437903589));
#3955=CARTESIAN_POINT('Ctrl Pts',(2.4393190927792,0.247545010874237,5.55510540189036));
#3956=CARTESIAN_POINT('Ctrl Pts',(2.42843718689821,0.328090047532528,5.55931642474482));
#3957=CARTESIAN_POINT('Ctrl Pts',(2.41755900899864,0.408607490642109,5.56352600496459));
#3958=CARTESIAN_POINT('Ctrl Pts',(2.4026678150993,0.488614764977163,5.56773558518437));
#3959=CARTESIAN_POINT('Ctrl Pts',(2.38383792694924,0.567685641916697,5.57194516540414));
#3960=CARTESIAN_POINT('Ctrl Pts',(2.36500867370359,0.646753852751756,5.57615460368568));
#3961=CARTESIAN_POINT('Ctrl Pts',(2.34224109929169,0.724885275372057,5.58036404196721));
#3962=CARTESIAN_POINT('Ctrl Pts',(2.3156602336019,0.801665723674642,5.58457348024875));
#3963=CARTESIAN_POINT('Ctrl Pts',(2.28871457027766,0.879499912146572,5.58884068915166));
#3964=CARTESIAN_POINT('Ctrl Pts',(2.25785029518011,0.955945291480569,5.59310789805457));
#3965=CARTESIAN_POINT('Ctrl Pts',(2.22324864085516,1.03058999167257,5.59737510695748));
#3966=CARTESIAN_POINT('Ctrl Pts',(2.18906589337937,1.10433100165746,5.60159065465889));
#3967=CARTESIAN_POINT('Ctrl Pts',(2.15123604551934,1.17631430736382,5.60580620236031));
#3968=CARTESIAN_POINT('Ctrl Pts',(2.10997992000107,1.24616812155996,5.61002175006172));
#3969=CARTESIAN_POINT('Ctrl Pts',(2.06796540868183,1.31730601515435,5.61431478956538));
#3970=CARTESIAN_POINT('Ctrl Pts',(2.02239767096814,1.38623491878807,5.61860782906904));
#3971=CARTESIAN_POINT('Ctrl Pts',(1.97355452117658,1.4525951954841,5.6229008685727));
#3972=CARTESIAN_POINT('Ctrl Pts',(1.92471137138501,1.51895547218013,5.62719390807635));
#3973=CARTESIAN_POINT('Ctrl Pts',(1.87259318065766,1.5827467750005,5.63148694758001));
#3974=CARTESIAN_POINT('Ctrl Pts',(1.81751760834157,1.64364837887194,5.63577998708367));
#3975=CARTESIAN_POINT('Ctrl Pts',(1.7632259634663,1.7036831295005,5.64001192088601));
#3976=CARTESIAN_POINT('Ctrl Pts',(1.70585489581572,1.7611374720248,5.64424385468836));
#3977=CARTESIAN_POINT('Ctrl Pts',(1.64567929753346,1.8156789087473,5.64847578849071));
#3978=CARTESIAN_POINT('Ctrl Pts',(1.58559005334727,1.87014207659335,5.65270164931948));
#3979=CARTESIAN_POINT('Ctrl Pts',(1.52270461319807,1.92170033126185,5.65692751014826));
#3980=CARTESIAN_POINT('Ctrl Pts',(1.45733653481368,1.97005595714875,5.66115337097703));
#3981=CARTESIAN_POINT('Ctrl Pts',(1.39173516852258,2.01858415630105,5.66539431320717));
#3982=CARTESIAN_POINT('Ctrl Pts',(1.32363372862786,2.06388647329623,5.66963525543731));
#3983=CARTESIAN_POINT('Ctrl Pts',(1.25338478014428,2.10570103359966,5.67387619766745));
#3984=CARTESIAN_POINT('Ctrl Pts',(1.1835118772948,2.14729175876843,5.67809443795195));
#3985=CARTESIAN_POINT('Ctrl Pts',(1.11151480069387,2.18543173083046,5.68231267823645));
#3986=CARTESIAN_POINT('Ctrl Pts',(1.03777019224463,2.21990614172954,5.68653091852094));
#3987=CARTESIAN_POINT('Ctrl Pts',(0.964050048999357,2.25436911554173,5.69074775937962));
#3988=CARTESIAN_POINT('Ctrl Pts',(0.888583945905484,2.28516874649065,5.6949646002383));
#3989=CARTESIAN_POINT('Ctrl Pts',(0.811771830668873,2.31213683525273,5.69918144109697));
#3990=CARTESIAN_POINT('Ctrl Pts',(0.734961688191492,2.33910423139561,5.70339817365488));
#3991=CARTESIAN_POINT('Ctrl Pts',(0.656806041170815,2.36224012807259,5.70761490621278));
#3992=CARTESIAN_POINT('Ctrl Pts',(0.577722099748643,2.38142550281591,5.71183163877068));
#3993=CARTESIAN_POINT('Ctrl Pts',(0.497851152504282,2.40080180129611,5.71609033424816));
#3994=CARTESIAN_POINT('Ctrl Pts',(0.417033796931697,2.41614838032182,5.72034902972563));
#3995=CARTESIAN_POINT('Ctrl Pts',(0.335710752587426,2.42739542320512,5.72460772520311));
#3996=CARTESIAN_POINT('Ctrl Pts',(0.255072182046584,2.43854780280716,5.7288305764065));
#3997=CARTESIAN_POINT('Ctrl Pts',(0.173936876646031,2.44566941692095,5.7330534276099));
#3998=CARTESIAN_POINT('Ctrl Pts',(0.0927381853600384,2.44874455159703,5.73727627881329));
#3999=CARTESIAN_POINT('Ctrl Pts',(0.010505651769704,2.4518588396667,5.74155289642781));
#4000=CARTESIAN_POINT('Ctrl Pts',(-0.0717914012442349,2.45082288489509,
5.74582951404233));
#4001=CARTESIAN_POINT('Ctrl Pts',(-0.153706383479221,2.44567467126716,5.75010613165685));
#4002=CARTESIAN_POINT('Ctrl Pts',(-0.235621365714208,2.44052645763923,5.75438274927137));
#4003=CARTESIAN_POINT('Ctrl Pts',(-0.317153799599896,2.43126610463908,5.75865936688589));
#4004=CARTESIAN_POINT('Ctrl Pts',(-0.397867900035402,2.41798498426302,5.76293598450042));
#4005=CARTESIAN_POINT('Ctrl Pts',(-0.477732100735661,2.404843710836,5.7671675703775));
#4006=CARTESIAN_POINT('Ctrl Pts',(-0.557093977187023,2.38771681514626,5.77139915625458));
#4007=CARTESIAN_POINT('Ctrl Pts',(-0.635525202983672,2.36665543887837,5.77563074213167));
#4008=CARTESIAN_POINT('Ctrl Pts',(-0.713844126625363,2.34562421945065,5.7798562689907));
#4009=CARTESIAN_POINT('Ctrl Pts',(-0.791234601033947,2.32066982780576,5.78408179584973));
#4010=CARTESIAN_POINT('Ctrl Pts',(-0.867276616693171,2.29189474455902,5.78830732270876));
#4011=CARTESIAN_POINT('Ctrl Pts',(-0.943597579218515,2.26301410494025,5.79254835017578));
#4012=CARTESIAN_POINT('Ctrl Pts',(-1.01855970287114,2.23028476543546,5.7967893776428));
#4013=CARTESIAN_POINT('Ctrl Pts',(-1.09175188487455,2.19386145229658,5.80103040510981));
#4014=CARTESIAN_POINT('Ctrl Pts',(-1.16454567512727,2.15763639458732,5.80524834827587));
#4015=CARTESIAN_POINT('Ctrl Pts',(-1.23558832118943,2.11775768035901,5.80946629144192));
#4016=CARTESIAN_POINT('Ctrl Pts',(-1.30449538176471,2.07442571545827,5.81368423460798));
#4017=CARTESIAN_POINT('Ctrl Pts',(-1.37337981915064,2.0311079770713,5.817900792962));
#4018=CARTESIAN_POINT('Ctrl Pts',(-1.44012967023436,1.98433948674289,5.82211735131602));
#4019=CARTESIAN_POINT('Ctrl Pts',(-1.50438707258409,1.9343654736998,5.82633390967004));
#4020=CARTESIAN_POINT('Ctrl Pts',(-1.5686430541751,1.88439256560357,5.83055037479415));
#4021=CARTESIAN_POINT('Ctrl Pts',(-1.63040633035506,1.83121456195291,5.83476683991825));
#4022=CARTESIAN_POINT('Ctrl Pts',(-1.68935104864667,1.77511782269132,5.83898330504236));
#4023=CARTESIAN_POINT('Ctrl Pts',(-1.74889117827283,1.71845444005005,5.84324236144859));
#4024=CARTESIAN_POINT('Ctrl Pts',(-1.80555512371633,1.65881334288088,5.84750141785482));
#4025=CARTESIAN_POINT('Ctrl Pts',(-1.85904556160285,1.59652743474227,5.85176047426105));
#4026=CARTESIAN_POINT('Ctrl Pts',(-1.91207843569271,1.53477432793661,5.855983098174));
#4027=CARTESIAN_POINT('Ctrl Pts',(-1.96199164935102,1.47042189497707,5.86020572208694));
#4028=CARTESIAN_POINT('Ctrl Pts',(-2.00853749382785,1.40382598134089,5.86442834599988));
#4029=CARTESIAN_POINT('Ctrl Pts',(-2.05568572956717,1.33636819062541,5.86870561865276));
#4030=CARTESIAN_POINT('Ctrl Pts',(-2.09937854910837,1.26660885034991,5.87298289130563));
#4031=CARTESIAN_POINT('Ctrl Pts',(-2.13940611243684,1.19494423973166,5.87726016395851));
#4032=CARTESIAN_POINT('Ctrl Pts',(-2.17943367576532,1.12327962911341,5.88153743661139));
#4033=CARTESIAN_POINT('Ctrl Pts',(-2.21579582487487,1.04971021501664,5.88581470926427));
#4034=CARTESIAN_POINT('Ctrl Pts',(-2.24833350639357,0.974652088710637,5.89009198191714));
#4035=CARTESIAN_POINT('Ctrl Pts',(-2.28384508024982,0.892733769044993,5.89476019048722));
#4036=CARTESIAN_POINT('Ctrl Pts',(-2.31491649951914,0.808778738740961,5.8994283990573));
#4037=CARTESIAN_POINT('Ctrl Pts',(-2.3413338304259,0.72326077213077,5.90409660762737));
#4038=CARTESIAN_POINT('Ctrl Pts',(-2.36767363498142,0.637993773187956,5.90875111650998));
#4039=CARTESIAN_POINT('Ctrl Pts',(-2.38938646907818,0.551173257307184,5.91340562539258));
#4040=CARTESIAN_POINT('Ctrl Pts',(-2.40630646574033,0.463291962952379,5.91806013427519));
#4041=CARTESIAN_POINT('Ctrl Pts',(-2.42314171533485,0.37585083901515,5.92269133015207));
#4042=CARTESIAN_POINT('Ctrl Pts',(-2.43523189434834,0.287359813896116,5.92732252602895));
#4043=CARTESIAN_POINT('Ctrl Pts',(-2.44246149855737,0.198323165729345,5.93195372190583));
#4044=CARTESIAN_POINT('Ctrl Pts',(-2.44777886968742,0.132836745063649,5.93535996470161));
#4045=CARTESIAN_POINT('Ctrl Pts',(-2.45046784596014,0.0670555759183701,
5.93876620749739));
#4046=CARTESIAN_POINT('Ctrl Pts',(-2.45049971322697,0.00118552710434612,
5.94217245029317));
#4047=CARTESIAN_POINT('',(-2.45049908813342,-0.00211401449528276,6.74217252662557));
#4048=CARTESIAN_POINT('Ctrl Pts',(-2.44699185673277,0.00118279703466509,
5.94217250378798));
#4049=CARTESIAN_POINT('Ctrl Pts',(-2.44492517590112,-0.482063010132467,
5.96719766230328));
#4050=CARTESIAN_POINT('Ctrl Pts',(-2.07248530679735,-1.7867484728855,6.03460815329083));
#4051=CARTESIAN_POINT('Ctrl Pts',(0.0507853919948306,-2.89698604679681,
6.14440397675062));
#4052=CARTESIAN_POINT('Ctrl Pts',(2.46316813457006,-1.52579265015265,6.27155997416736));
#4053=CARTESIAN_POINT('Ctrl Pts',(2.61640506990387,1.24485975887081,6.39871597158408));
#4054=CARTESIAN_POINT('Ctrl Pts',(0.369930108240046,2.87373628563431,6.52587196900083));
#4055=CARTESIAN_POINT('Ctrl Pts',(-1.95817338645522,1.967226842049,6.64035747973544));
#4056=CARTESIAN_POINT('Ctrl Pts',(-2.44423549538377,0.570546928646848,6.71245765799784));
#4057=CARTESIAN_POINT('Ctrl Pts',(-2.44892931063419,-0.00211222014950052,
6.74217250378799));
#4058=CARTESIAN_POINT('',(-2.45089802721206,-0.000113383326009888,7.54217250378798));
#4059=CARTESIAN_POINT('Ctrl Pts',(-2.45049908813342,-0.00211401449528276,
6.74217252662557));
#4060=CARTESIAN_POINT('Ctrl Pts',(-2.45041450413157,-0.100161128108063,
6.74725689713589));
#4061=CARTESIAN_POINT('Ctrl Pts',(-2.44444165686557,-0.197950871715524,
6.7523412676462));
#4062=CARTESIAN_POINT('Ctrl Pts',(-2.43269561264666,-0.294859807721695,
6.75742563815651));
#4063=CARTESIAN_POINT('Ctrl Pts',(-2.42078374824785,-0.393136817685654,
6.76258178527664));
#4064=CARTESIAN_POINT('Ctrl Pts',(-2.402934606887,-0.490507979483392,6.76773793239676));
#4065=CARTESIAN_POINT('Ctrl Pts',(-2.37931704734039,-0.586345152819918,
6.77289407951689));
#4066=CARTESIAN_POINT('Ctrl Pts',(-2.36818669018654,-0.631510783322305,
6.77532404095602));
#4067=CARTESIAN_POINT('Ctrl Pts',(-2.35577585904011,-0.67633603002058,6.77775400239516));
#4068=CARTESIAN_POINT('Ctrl Pts',(-2.34210586547315,-0.720756800117959,
6.78018396383429));
#4069=CARTESIAN_POINT('Ctrl Pts',(-2.31830558549057,-0.798096029297579,
6.78441467267223));
#4070=CARTESIAN_POINT('Ctrl Pts',(-2.29062567513868,-0.87440055912202,6.78864538151017));
#4071=CARTESIAN_POINT('Ctrl Pts',(-2.25917440233834,-0.949253006220778,
6.7928760903481));
#4072=CARTESIAN_POINT('Ctrl Pts',(-2.22776831573623,-1.02399791244086,6.79710072090586));
#4073=CARTESIAN_POINT('Ctrl Pts',(-2.19260180642005,-1.09729445416125,6.80132535146361));
#4074=CARTESIAN_POINT('Ctrl Pts',(-2.15383289580862,-1.16874039330069,6.80554998202137));
#4075=CARTESIAN_POINT('Ctrl Pts',(-2.11491147857911,-1.24046738182692,6.80979123115594));
#4076=CARTESIAN_POINT('Ctrl Pts',(-2.07235939710418,-1.31032872344714,6.81403248029051));
#4077=CARTESIAN_POINT('Ctrl Pts',(-2.02638541890485,-1.37793772865461,6.81827372942508));
#4078=CARTESIAN_POINT('Ctrl Pts',(-1.98067422542635,-1.44516028452148,6.82249073581378));
#4079=CARTESIAN_POINT('Ctrl Pts',(-1.93158041197976,-1.51015579415148,6.82670774220249));
#4080=CARTESIAN_POINT('Ctrl Pts',(-1.87935425791776,-1.5725704509644,6.83092474859119));
#4081=CARTESIAN_POINT('Ctrl Pts',(-1.82714541753076,-1.63496441647614,6.83514035698536));
#4082=CARTESIAN_POINT('Ctrl Pts',(-1.77180659684868,-1.69477887183925,6.83935596537953));
#4083=CARTESIAN_POINT('Ctrl Pts',(-1.71362891028703,-1.75169238390435,6.8435715737737));
#4084=CARTESIAN_POINT('Ctrl Pts',(-1.65545267508404,-1.80860447614814,6.84778707700109));
#4085=CARTESIAN_POINT('Ctrl Pts',(-1.59443804800848,-1.86261544454416,6.85200258022848));
#4086=CARTESIAN_POINT('Ctrl Pts',(-1.53091258600426,-1.91344111589924,6.85621808345588));
#4087=CARTESIAN_POINT('Ctrl Pts',(-1.46671422244237,-1.96480516465994,6.86047823993881));
#4088=CARTESIAN_POINT('Ctrl Pts',(-1.39995188287686,-2.01291571814626,6.86473839642174));
#4089=CARTESIAN_POINT('Ctrl Pts',(-1.33099594387263,-2.0575227938943,6.86899855290467));
#4090=CARTESIAN_POINT('Ctrl Pts',(-1.26266340470618,-2.10172659699916,6.8732201952161));
#4091=CARTESIAN_POINT('Ctrl Pts',(-1.19217720728943,-2.14248983244165,6.87744183752754));
#4092=CARTESIAN_POINT('Ctrl Pts',(-1.11992323469428,-2.17961514914718,6.88166347983897));
#4093=CARTESIAN_POINT('Ctrl Pts',(-1.04668049930741,-2.21724850894669,6.88594289340765));
#4094=CARTESIAN_POINT('Ctrl Pts',(-0.971621690954015,-2.25114342631593,
6.89022230697633));
#4095=CARTESIAN_POINT('Ctrl Pts',(-0.895168574025098,-2.28114521108979,
6.89450172054501));
#4096=CARTESIAN_POINT('Ctrl Pts',(-0.818715457096181,-2.31114699586365,
6.89878113411369));
#4097=CARTESIAN_POINT('Ctrl Pts',(-0.740868517526701,-2.33725555414097,
6.90306054768236));
#4098=CARTESIAN_POINT('Ctrl Pts',(-0.66206232679372,-2.3593693490932,6.90733996125104));
#4099=CARTESIAN_POINT('Ctrl Pts',(-0.584153156659504,-2.38123143121165,
6.91157066389883));
#4100=CARTESIAN_POINT('Ctrl Pts',(-0.505013440057136,-2.39927149929305,
6.91580136654663));
#4101=CARTESIAN_POINT('Ctrl Pts',(-0.425052711369318,-2.41335460356691,
6.92003206919443));
#4102=CARTESIAN_POINT('Ctrl Pts',(-0.345206863613683,-2.42741747440651,
6.92425669352013));
#4103=CARTESIAN_POINT('Ctrl Pts',(-0.264542800572244,-2.43753459225192,
6.92848131784583));
#4104=CARTESIAN_POINT('Ctrl Pts',(-0.183484260366025,-2.443621037763,6.93270594217153));
#4105=CARTESIAN_POINT('Ctrl Pts',(-0.102106707509254,-2.4497314369884,6.93694719285887));
#4106=CARTESIAN_POINT('Ctrl Pts',(-0.02033202273886,-2.45177924153041,6.94118844354621));
#4107=CARTESIAN_POINT('Ctrl Pts',(0.0614016513397831,-2.44973061523359,
6.94542969423356));
#4108=CARTESIAN_POINT('Ctrl Pts',(0.142667989329953,-2.44769370255433,6.94964669433473));
#4109=CARTESIAN_POINT('Ctrl Pts',(0.223893314749414,-2.44160708876568,6.9538636944359));
#4110=CARTESIAN_POINT('Ctrl Pts',(0.304644658900765,-2.43148964254492,6.95808069453707));
#4111=CARTESIAN_POINT('Ctrl Pts',(0.385369232722055,-2.42137555041539,6.96229629663693));
#4112=CARTESIAN_POINT('Ctrl Pts',(0.46561967622631,-2.40723333725683,6.9665118987368));
#4113=CARTESIAN_POINT('Ctrl Pts',(0.544968130282486,-2.38913373149692,6.97072750083666));
#4114=CARTESIAN_POINT('Ctrl Pts',(0.624314604864237,-2.3710345772607,6.97494299777157));
#4115=CARTESIAN_POINT('Ctrl Pts',(0.702758681563797,-2.34897833119276,6.97915849470648));
#4116=CARTESIAN_POINT('Ctrl Pts',(0.779884097391443,-2.32308653403956,6.98337399164139));
#4117=CARTESIAN_POINT('Ctrl Pts',(0.857826726412317,-2.29692038999302,6.98763415556025));
#4118=CARTESIAN_POINT('Ctrl Pts',(0.934422118975503,-2.26683706758557,6.99189431947912));
#4119=CARTESIAN_POINT('Ctrl Pts',(1.00925957122563,-2.23301262152489,6.99615448339798));
#4120=CARTESIAN_POINT('Ctrl Pts',(1.08342021273652,-2.19949407508605,7.00037611948614));
#4121=CARTESIAN_POINT('Ctrl Pts',(1.1558541926515,-2.16230207004578,7.00459775557429));
#4122=CARTESIAN_POINT('Ctrl Pts',(1.22618666595462,-2.12165419195379,7.00881939166244));
#4123=CARTESIAN_POINT('Ctrl Pts',(1.29748194996728,-2.08044986801952,7.01309881949666));
#4124=CARTESIAN_POINT('Ctrl Pts',(1.3666173396932,-2.03569460567398,7.01737824733088));
#4125=CARTESIAN_POINT('Ctrl Pts',(1.43323442603924,-1.98765925903208,7.0216576751651));
#4126=CARTESIAN_POINT('Ctrl Pts',(1.49985151238528,-1.93962391239019,7.02593710299932));
#4127=CARTESIAN_POINT('Ctrl Pts',(1.56394995330399,-1.88830883917688,7.03021653083354));
#4128=CARTESIAN_POINT('Ctrl Pts',(1.62520909567545,-1.83402443967734,7.03449595866776));
#4129=CARTESIAN_POINT('Ctrl Pts',(1.68577070383461,-1.78035815568479,7.0387266583088));
#4130=CARTESIAN_POINT('Ctrl Pts',(1.74378516384833,-1.72358800008596,7.04295735794985));
#4131=CARTESIAN_POINT('Ctrl Pts',(1.79891728889183,-1.66398522761654,7.04718805759089));
#4132=CARTESIAN_POINT('Ctrl Pts',(1.85397020369154,-1.60446808852574,7.05141267883844));
#4133=CARTESIAN_POINT('Ctrl Pts',(1.90614869495937,-1.54212675375599,7.05563730008599));
#4134=CARTESIAN_POINT('Ctrl Pts',(1.95515194917686,-1.47727150707984,7.05986192133354));
#4135=CARTESIAN_POINT('Ctrl Pts',(2.0043481044594,-1.41216095804961,7.0641031727815));
#4136=CARTESIAN_POINT('Ctrl Pts',(2.05034361527978,-1.34451697738083,7.06834442422946));
#4137=CARTESIAN_POINT('Ctrl Pts',(2.0928728171472,-1.27468961761142,7.07258567567741));
#4138=CARTESIAN_POINT('Ctrl Pts',(2.13515880594148,-1.20526158174212,7.07680267254844));
#4139=CARTESIAN_POINT('Ctrl Pts',(2.17401777962351,-1.1336754725011,7.08101966941946));
#4140=CARTESIAN_POINT('Ctrl Pts',(2.20923118761774,-1.06030552656162,7.08523666629049));
#4141=CARTESIAN_POINT('Ctrl Pts',(2.2444329213901,-0.986959904795115,7.08945226511003));
#4142=CARTESIAN_POINT('Ctrl Pts',(2.27599128849376,-0.911832039673232,7.09366786392958));
#4143=CARTESIAN_POINT('Ctrl Pts',(2.30373410617456,-0.835319949509226,7.09788346274913));
#4144=CARTESIAN_POINT('Ctrl Pts',(2.33147623146361,-0.758809768896756,7.10209895635781));
#4145=CARTESIAN_POINT('Ctrl Pts',(2.35540283915505,-0.680915869507141,7.10631444996649));
#4146=CARTESIAN_POINT('Ctrl Pts',(2.37539074560114,-0.60205403055912,7.11052994357517));
#4147=CARTESIAN_POINT('Ctrl Pts',(2.39559047581516,-0.522356445660494,7.11479011128428));
#4148=CARTESIAN_POINT('Ctrl Pts',(2.41176739147823,-0.441670749031801,7.1190502789934));
#4149=CARTESIAN_POINT('Ctrl Pts',(2.42384715139712,-0.360437562781768,7.12331044670251));
#4150=CARTESIAN_POINT('Ctrl Pts',(2.43581764475536,-0.279939165213943,7.12753207938472));
#4151=CARTESIAN_POINT('Ctrl Pts',(2.44376482075147,-0.198903616741039,7.13175371206694));
#4152=CARTESIAN_POINT('Ctrl Pts',(2.44766867038456,-0.117763873993241,7.13597534474915));
#4153=CARTESIAN_POINT('Ctrl Pts',(2.45162597147657,-0.0355131669321832,
7.14025477997171));
#4154=CARTESIAN_POINT('Ctrl Pts',(2.45142838658748,0.0468441146066864,7.14453421519427));
#4155=CARTESIAN_POINT('Ctrl Pts',(2.44710959158739,0.128859988984182,7.14881365041683));
#4156=CARTESIAN_POINT('Ctrl Pts',(2.4427907965873,0.21087586336168,7.15309308563939));
#4157=CARTESIAN_POINT('Ctrl Pts',(2.43435090704917,0.292549849315418,7.15737252086195));
#4158=CARTESIAN_POINT('Ctrl Pts',(2.42187728965929,0.373444298165804,7.16165195608451));
#4159=CARTESIAN_POINT('Ctrl Pts',(2.40954571588641,0.453417559541066,7.1658826591359));
#4160=CARTESIAN_POINT('Ctrl Pts',(2.39322547574155,0.532929756284854,7.1701133621873));
#4161=CARTESIAN_POINT('Ctrl Pts',(2.37296315532827,0.611552216457846,7.17434406523869));
#4162=CARTESIAN_POINT('Ctrl Pts',(2.35272994622341,0.69006171806341,7.17856868994867));
#4163=CARTESIAN_POINT('Ctrl Pts',(2.32856602028905,0.767683575355329,7.18279331465865));
#4164=CARTESIAN_POINT('Ctrl Pts',(2.30056938768783,0.84399688532224,7.18701793936863));
#4165=CARTESIAN_POINT('Ctrl Pts',(2.27246257521156,0.920610523942117,7.19125918995749));
#4166=CARTESIAN_POINT('Ctrl Pts',(2.24049289669693,0.995904824643573,7.19550044054635));
#4167=CARTESIAN_POINT('Ctrl Pts',(2.20481082779162,1.06946690629155,7.19974169113521));
#4168=CARTESIAN_POINT('Ctrl Pts',(2.1693327778759,1.14260838280003,7.20395869157024));
#4169=CARTESIAN_POINT('Ctrl Pts',(2.13018487997237,1.2140369724477,7.20817569200528));
#4170=CARTESIAN_POINT('Ctrl Pts',(2.08756345116152,1.28336631067462,7.21239269244031));
#4171=CARTESIAN_POINT('Ctrl Pts',(2.04495615221826,1.35267266482063,7.21660829485422));
#4172=CARTESIAN_POINT('Ctrl Pts',(1.99887785250892,1.41988075370587,7.22082389726814));
#4173=CARTESIAN_POINT('Ctrl Pts',(1.94956996776746,1.48463032125145,7.22503949968205));
#4174=CARTESIAN_POINT('Ctrl Pts',(1.90026331332807,1.54937827320294,7.22925499691067));
#4175=CARTESIAN_POINT('Ctrl Pts',(1.84772751669397,1.61166745644557,7.23347049413928));
#4176=CARTESIAN_POINT('Ctrl Pts',(1.79224545488461,1.67116919533764,7.2376859913679));
#4177=CARTESIAN_POINT('Ctrl Pts',(1.73617551996997,1.73130139875953,7.24194615487901));
#4178=CARTESIAN_POINT('Ctrl Pts',(1.67709683107441,1.78858637078493,7.24620631839012));
#4179=CARTESIAN_POINT('Ctrl Pts',(1.61533959407928,1.84272305184469,7.25046648190124));
#4180=CARTESIAN_POINT('Ctrl Pts',(1.55414086436869,1.89637014282231,7.25468811822962));
#4181=CARTESIAN_POINT('Ctrl Pts',(1.49031224602932,1.94692541394981,7.25890975455801));
#4182=CARTESIAN_POINT('Ctrl Pts',(1.42420691800064,1.99413763434702,7.2631313908864));
#4183=CARTESIAN_POINT('Ctrl Pts',(1.35719666169748,2.0419961517132,7.26741081798887));
#4184=CARTESIAN_POINT('Ctrl Pts',(1.28784730768326,2.08641913126966,7.27169024509135));
#4185=CARTESIAN_POINT('Ctrl Pts',(1.2165537296308,2.12719234506929,7.27596967219382));
#4186=CARTESIAN_POINT('Ctrl Pts',(1.14526015157833,2.16796555886892,7.28024909929629));
#4187=CARTESIAN_POINT('Ctrl Pts',(1.07202281667777,2.20508884352166,7.28452852639877));
#4188=CARTESIAN_POINT('Ctrl Pts',(0.997256979740272,2.23839870585187,7.28880795350124));
#4189=CARTESIAN_POINT('Ctrl Pts',(0.92334241970013,2.2713293051735,7.29303865544293));
#4190=CARTESIAN_POINT('Ctrl Pts',(0.847655992314498,2.30065677971353,7.29726935738461));
#4191=CARTESIAN_POINT('Ctrl Pts',(0.770583328745483,2.32618820895033,7.3015000593263));
#4192=CARTESIAN_POINT('Ctrl Pts',(0.693621397328081,2.35168295656796,7.30572468291663));
#4193=CARTESIAN_POINT('Ctrl Pts',(0.615277622954306,2.37339234556574,7.30994930650696));
#4194=CARTESIAN_POINT('Ctrl Pts',(0.535958946618911,2.39117089676567,7.3141739300973));
#4195=CARTESIAN_POINT('Ctrl Pts',(0.456328087768331,2.40901942080285,7.31841518096483));
#4196=CARTESIAN_POINT('Ctrl Pts',(0.375715069936116,2.42290590556192,7.32265643183236));
#4197=CARTESIAN_POINT('Ctrl Pts',(0.294548495546354,2.43273332565889,7.32689768269988));
#4198=CARTESIAN_POINT('Ctrl Pts',(0.213846033457668,2.44250455234634,7.33111468199939));
#4199=CARTESIAN_POINT('Ctrl Pts',(0.132596794460656,2.44826295159285,7.33533168129891));
#4200=CARTESIAN_POINT('Ctrl Pts',(0.0512319056561366,2.44996439603575,7.33954868059842));
#4201=CARTESIAN_POINT('Ctrl Pts',(-0.0301060089648669,2.4516652764138,7.34376428187336));
#4202=CARTESIAN_POINT('Ctrl Pts',(-0.111559032665591,2.44931186314808,7.34797988314831));
#4203=CARTESIAN_POINT('Ctrl Pts',(-0.192693572290218,2.44291208134841,7.35219548442326));
#4204=CARTESIAN_POINT('Ctrl Pts',(-0.273826087455323,2.43651245923535,7.35641098051102));
#4205=CARTESIAN_POINT('Ctrl Pts',(-0.354639670809366,2.42606670698216,7.36062647659878));
#4206=CARTESIAN_POINT('Ctrl Pts',(-0.434704833047805,2.41163470660979,7.36484197268654));
#4207=CARTESIAN_POINT('Ctrl Pts',(-0.515618391733778,2.39704978007697,7.36910213753916));
#4208=CARTESIAN_POINT('Ctrl Pts',(-0.595767094195178,2.37839369334412,7.37336230239178));
#4209=CARTESIAN_POINT('Ctrl Pts',(-0.674719044389303,2.3557810724128,7.3776224672444));
#4210=CARTESIAN_POINT('Ctrl Pts',(-0.752956939670165,2.33337296388475,7.38184410243896));
#4211=CARTESIAN_POINT('Ctrl Pts',(-0.830019217768804,2.30707981069314,7.38606573763352));
#4212=CARTESIAN_POINT('Ctrl Pts',(-0.905503439360926,2.2770625312682,7.39028737282807));
#4213=CARTESIAN_POINT('Ctrl Pts',(-0.982021045333626,2.24663431314572,7.39456680250973));
#4214=CARTESIAN_POINT('Ctrl Pts',(-1.05691661040126,2.21237943536682,7.39884623219138));
#4215=CARTESIAN_POINT('Ctrl Pts',(-1.12979623071021,2.17451390592771,7.40312566187303));
#4216=CARTESIAN_POINT('Ctrl Pts',(-1.20267585101917,2.13664837648861,7.40740509155468));
#4217=CARTESIAN_POINT('Ctrl Pts',(-1.27353913625396,2.09517249972326,7.41168452123633));
#4218=CARTESIAN_POINT('Ctrl Pts',(-1.34202380373791,2.0503468877731,7.41596395091798));
#4219=CARTESIAN_POINT('Ctrl Pts',(-1.40963924107054,2.00609021738154,7.42018906465642));
#4220=CARTESIAN_POINT('Ctrl Pts',(-1.47519193951934,1.95840092729194,7.42441417839486));
#4221=CARTESIAN_POINT('Ctrl Pts',(-1.53831148277856,1.90749784585766,7.4286392921333));
#4222=CARTESIAN_POINT('Ctrl Pts',(-1.60134028251237,1.85666794500781,7.43285833165612));
#4223=CARTESIAN_POINT('Ctrl Pts',(-1.66194251383471,1.80263371861981,7.43707737117893));
#4224=CARTESIAN_POINT('Ctrl Pts',(-1.71977605476889,1.74565763294054,7.44129641070175));
#4225=CARTESIAN_POINT('Ctrl Pts',(-1.77754248223635,1.68874766568611,7.44551055420118));
#4226=CARTESIAN_POINT('Ctrl Pts',(-1.83254627380443,1.62890294915343,7.44972469770062));
#4227=CARTESIAN_POINT('Ctrl Pts',(-1.88447894381472,1.56642566383437,7.45393884120005));
#4228=CARTESIAN_POINT('Ctrl Pts',(-1.93637859007007,1.50398810754445,7.45815030494429));
#4229=CARTESIAN_POINT('Ctrl Pts',(-1.98521069369888,1.43892166294857,7.46236176868853));
#4230=CARTESIAN_POINT('Ctrl Pts',(-2.03070498785838,1.37156388924727,7.46657323243277));
#4231=CARTESIAN_POINT('Ctrl Pts',(-2.0761844000306,1.30422814946363,7.47078331853283));
#4232=CARTESIAN_POINT('Ctrl Pts',(-2.1183279099878,1.23460295519288,7.47499340463288));
#4233=CARTESIAN_POINT('Ctrl Pts',(-2.15690765425705,1.16305615556917,7.47920349073293));
#4234=CARTESIAN_POINT('Ctrl Pts',(-2.19548669081132,1.09151066841509,7.48341349960228));
#4235=CARTESIAN_POINT('Ctrl Pts',(-2.23050187135428,1.01804405714918,7.48762350847162));
#4236=CARTESIAN_POINT('Ctrl Pts',(-2.26177122547569,0.943048871273492,7.49183351734097));
#4237=CARTESIAN_POINT('Ctrl Pts',(-2.29307152277315,0.867979472504542,7.49604769230358));
#4238=CARTESIAN_POINT('Ctrl Pts',(-2.32061840874255,0.791378908907118,7.50026186726618));
#4239=CARTESIAN_POINT('Ctrl Pts',(-2.34427827871066,0.713659303845589,7.50447604222879));
#4240=CARTESIAN_POINT('Ctrl Pts',(-2.36794930503256,0.635903051608447,7.50869220430405));
#4241=CARTESIAN_POINT('Ctrl Pts',(-2.38772955056502,0.557027159822053,7.5129083663793));
#4242=CARTESIAN_POINT('Ctrl Pts',(-2.40353614316832,0.477456027801041,7.51712452845455));
#4243=CARTESIAN_POINT('Ctrl Pts',(-2.41937149876783,0.397740101501748,7.52134836261049));
#4244=CARTESIAN_POINT('Ctrl Pts',(-2.43121868418161,0.317326869613289,7.52557219676642));
#4245=CARTESIAN_POINT('Ctrl Pts',(-2.43904654598825,0.236647832237695,7.52979603092236));
#4246=CARTESIAN_POINT('Ctrl Pts',(-2.44669215229988,0.157847238587433,7.53392152187756));
#4247=CARTESIAN_POINT('Ctrl Pts',(-2.45050364776306,0.0787934941983163,
7.53804701283277));
#4248=CARTESIAN_POINT('Ctrl Pts',(-2.45049999737776,-0.000113364912372915,
7.54217250378798));
#4249=CARTESIAN_POINT('',(-2.45049903342988,0.00217650160213615,8.34217250378799));
#4250=CARTESIAN_POINT('Ctrl Pts',(-2.45453280350633,-0.000113551477855291,
7.54217250378798));
#4251=CARTESIAN_POINT('Ctrl Pts',(-2.45453687676125,-0.00616397550014873,
7.54248831863689));
#4252=CARTESIAN_POINT('Ctrl Pts',(-2.45451644395713,-0.0122143712099649,
7.5428041334858));
#4253=CARTESIAN_POINT('Ctrl Pts',(-2.44842908042641,-0.830260217324654,
7.58550528080696));
#4254=CARTESIAN_POINT('Ctrl Pts',(-1.55054422260318,-2.44765991029051,7.67027594575146));
#4255=CARTESIAN_POINT('Ctrl Pts',(1.21840547693069,-2.62882380370893,7.79743194316818));
#4256=CARTESIAN_POINT('Ctrl Pts',(2.86986254650355,-0.398892772318102,7.92458794058493));
#4257=CARTESIAN_POINT('Ctrl Pts',(1.8891496807097,2.19689325024607,8.05174393800165));
#4258=CARTESIAN_POINT('Ctrl Pts',(-0.824246511156764,2.77774083901823,8.1788999354184));
#4259=CARTESIAN_POINT('Ctrl Pts',(-2.31451209905297,1.28030821412869,8.2757092634905));
#4260=CARTESIAN_POINT('Ctrl Pts',(-2.45124442572433,0.23411249554893,8.33013325909037));
#4261=CARTESIAN_POINT('Ctrl Pts',(-2.44926690043473,0.00218661114913343,
8.342171922218));
#4262=CARTESIAN_POINT('',(-2.45028722013793,-0.000988674397566302,9.14217254507401));
#4263=CARTESIAN_POINT('Ctrl Pts',(-2.45049903342988,0.00217650160213615,
8.34217250378799));
#4264=CARTESIAN_POINT('Ctrl Pts',(-2.45057066460465,-0.0784722442460898,
8.34635669788586));
#4265=CARTESIAN_POINT('Ctrl Pts',(-2.44665665890771,-0.159202294317952,
8.35054089198374));
#4266=CARTESIAN_POINT('Ctrl Pts',(-2.43875966949261,-0.239586152471894,
8.35472508608161));
#4267=CARTESIAN_POINT('Ctrl Pts',(-2.43086623907028,-0.319933783456873,
8.35890739445876));
#4268=CARTESIAN_POINT('Ctrl Pts',(-2.41899343344881,-0.399935061913083,
8.36308970283592));
#4269=CARTESIAN_POINT('Ctrl Pts',(-2.40319591535469,-0.479165568903431,
8.36727201121308));
#4270=CARTESIAN_POINT('Ctrl Pts',(-2.38740048245362,-0.558385617864723,
8.37145376754653));
#4271=CARTESIAN_POINT('Ctrl Pts',(-2.36768145903396,-0.636834633535446,
8.37563552387998));
#4272=CARTESIAN_POINT('Ctrl Pts',(-2.3441447116268,-0.714097907119257,8.37981728021343));
#4273=CARTESIAN_POINT('Ctrl Pts',(-2.32060357007519,-0.791375605210379,
8.38399981725125));
#4274=CARTESIAN_POINT('Ctrl Pts',(-2.29324342983371,-0.867466669906543,
8.38818235428906));
#4275=CARTESIAN_POINT('Ctrl Pts',(-2.26221968959487,-0.941972571792464,
8.39236489132688));
#4276=CARTESIAN_POINT('Ctrl Pts',(-2.23116118125722,-1.01656197194577,8.39655211570606));
#4277=CARTESIAN_POINT('Ctrl Pts',(-2.19643106527865,-1.08956222842722,8.40073934008525));
#4278=CARTESIAN_POINT('Ctrl Pts',(-2.15823215230383,-1.16059649610102,8.40492656446443));
#4279=CARTESIAN_POINT('Ctrl Pts',(-2.1200075469554,-1.23167854102297,8.40911660514713));
#4280=CARTESIAN_POINT('Ctrl Pts',(-2.07830974907275,-1.30079156321441,8.41330664582984));
#4281=CARTESIAN_POINT('Ctrl Pts',(-2.03338528483849,-1.36758712095511,8.41749668651254));
#4282=CARTESIAN_POINT('Ctrl Pts',(-1.98838819436034,-1.43449066240915,8.4216935009414));
#4283=CARTESIAN_POINT('Ctrl Pts',(-1.94015431715338,-1.49906889049394,8.42589031537025));
#4284=CARTESIAN_POINT('Ctrl Pts',(-1.88897035835948,-1.56100648148535,8.4300871297991));
#4285=CARTESIAN_POINT('Ctrl Pts',(-1.87626709970743,-1.57637866560688,8.43112872995002));
#4286=CARTESIAN_POINT('Ctrl Pts',(-1.86338229759534,-1.59158837468582,8.43217033010094));
#4287=CARTESIAN_POINT('Ctrl Pts',(-1.85032066881286,-1.60663115635293,8.43321193025186));
#4288=CARTESIAN_POINT('Ctrl Pts',(-1.79726781722413,-1.66773092243547,8.43744263219124));
#4289=CARTESIAN_POINT('Ctrl Pts',(-1.74108556238777,-1.72631496655,8.44167333413062));
#4290=CARTESIAN_POINT('Ctrl Pts',(-1.68204176569164,-1.78204538339205,8.44590403607));
#4291=CARTESIAN_POINT('Ctrl Pts',(-1.62308279868508,-1.83769573095969,8.45012865965479));
#4292=CARTESIAN_POINT('Ctrl Pts',(-1.56127079031436,-1.89050027732404,8.45435328323959));
#4293=CARTESIAN_POINT('Ctrl Pts',(-1.49691297561597,-1.94015509520052,8.45857790682439));
#4294=CARTESIAN_POINT('Ctrl Pts',(-1.43230186127501,-1.99000534462916,8.4628191576929));
#4295=CARTESIAN_POINT('Ctrl Pts',(-1.36512516917711,-2.03668066064801,8.46706040856141));
#4296=CARTESIAN_POINT('Ctrl Pts',(-1.29573025478907,-2.07991186275387,8.47130165942991));
#4297=CARTESIAN_POINT('Ctrl Pts',(-1.22673214232091,-2.1228958677251,8.47551865871598));
#4298=CARTESIAN_POINT('Ctrl Pts',(-1.15554150512803,-2.16247479059064,8.47973565800205));
#4299=CARTESIAN_POINT('Ctrl Pts',(-1.08253035737817,-2.19842631792714,8.48395265728812));
#4300=CARTESIAN_POINT('Ctrl Pts',(-1.00954341442105,-2.23436592654582,8.48816825854667));
#4301=CARTESIAN_POINT('Ctrl Pts',(-0.93473757632392,-2.26668032243561,8.49238385980521));
#4302=CARTESIAN_POINT('Ctrl Pts',(-0.858509105248819,-2.29519331782856,
8.49659946106376));
#4303=CARTESIAN_POINT('Ctrl Pts',(-0.782282536270929,-2.32370560174864,
8.50081495713217));
#4304=CARTESIAN_POINT('Ctrl Pts',(-0.704633840860815,-2.34841651185334,
8.50503045320058));
#4305=CARTESIAN_POINT('Ctrl Pts',(-0.62597753528704,-2.36919867789005,8.509245949269));
#4306=CARTESIAN_POINT('Ctrl Pts',(-0.546487761341905,-2.39020105866928,
8.51350611413563));
#4307=CARTESIAN_POINT('Ctrl Pts',(-0.465969360420922,-2.40719079973591,
8.51776627900226));
#4308=CARTESIAN_POINT('Ctrl Pts',(-0.384862181302826,-2.42008912054966,
8.5220264438689));
#4309=CARTESIAN_POINT('Ctrl Pts',(-0.304488550124497,-2.43287078662628,
8.52624807903699));
#4310=CARTESIAN_POINT('Ctrl Pts',(-0.223537222083469,-2.44163475260477,
8.53046971420508));
#4311=CARTESIAN_POINT('Ctrl Pts',(-0.142440930413969,-2.44635664434743,
8.53469134937317));
#4312=CARTESIAN_POINT('Ctrl Pts',(-0.0602344235506632,-2.45114317919334,
8.53897077908907));
#4313=CARTESIAN_POINT('Ctrl Pts',(0.0221205514842775,-2.45177612534295,
8.54325020880498));
#4314=CARTESIAN_POINT('Ctrl Pts',(0.104175698326146,-2.44828463906431,8.54752963852088));
#4315=CARTESIAN_POINT('Ctrl Pts',(0.186230845168012,-2.44479315278567,8.55180906823679));
#4316=CARTESIAN_POINT('Ctrl Pts',(0.267985681418476,-2.4371773447912,8.55608849795269));
#4317=CARTESIAN_POINT('Ctrl Pts',(0.349001701606052,-2.42552016323841,8.5603679276686));
#4318=CARTESIAN_POINT('Ctrl Pts',(0.429095231937527,-2.41399571631895,8.56459862960827));
#4319=CARTESIAN_POINT('Ctrl Pts',(0.508767946089158,-2.39847815840017,8.56882933154794));
#4320=CARTESIAN_POINT('Ctrl Pts',(0.587590724305493,-2.37900975002419,8.57306003348762));
#4321=CARTESIAN_POINT('Ctrl Pts',(0.666300255877846,-2.35956931239426,8.57728465707269));
#4322=CARTESIAN_POINT('Ctrl Pts',(0.744161829072428,-2.33618940828937,8.58150928065777));
#4323=CARTESIAN_POINT('Ctrl Pts',(0.820753574049848,-2.30896379804544,8.58573390424285));
#4324=CARTESIAN_POINT('Ctrl Pts',(0.897646768995828,-2.28163103318119,8.58997515511128));
#4325=CARTESIAN_POINT('Ctrl Pts',(0.973259648983159,-2.25042229295733,8.59421640597972));
#4326=CARTESIAN_POINT('Ctrl Pts',(1.04717783611411,-2.21548388158239,8.59845765684816));
#4327=CARTESIAN_POINT('Ctrl Pts',(1.12067335714017,-2.1807452489469,8.60267465613449));
#4328=CARTESIAN_POINT('Ctrl Pts',(1.19249308862886,-2.14231968286406,8.60689165542082));
#4329=CARTESIAN_POINT('Ctrl Pts',(1.26224870601951,-2.10039959392304,8.61110865470715));
#4330=CARTESIAN_POINT('Ctrl Pts',(1.33198119789681,-2.05849340240867,8.61532425596595));
#4331=CARTESIAN_POINT('Ctrl Pts',(1.39965053627586,-2.01309522800395,8.61953985722476));
#4332=CARTESIAN_POINT('Ctrl Pts',(1.46489404893636,-1.96444284095792,8.62375545848356));
#4333=CARTESIAN_POINT('Ctrl Pts',(1.53013593360273,-1.9157916679146,8.62797095455223));
#4334=CARTESIAN_POINT('Ctrl Pts',(1.59295174073334,-1.86388672255779,8.63218645062089));
#4335=CARTESIAN_POINT('Ctrl Pts',(1.65300995881168,-1.80900755279502,8.63640194668956));
#4336=CARTESIAN_POINT('Ctrl Pts',(1.7137045737332,-1.75354686510662,8.64066211155587));
#4337=CARTESIAN_POINT('Ctrl Pts',(1.77158244245994,-1.69504886087427,8.64492227642219));
#4338=CARTESIAN_POINT('Ctrl Pts',(1.82633919032058,-1.63384069354977,8.64918244128851));
#4339=CARTESIAN_POINT('Ctrl Pts',(1.88060070829574,-1.5731861039098,8.65340407645682));
#4340=CARTESIAN_POINT('Ctrl Pts',(1.931797086613,-1.5098705808574,8.65762571162513));
#4341=CARTESIAN_POINT('Ctrl Pts',(1.97967354563323,-1.44424475166778,8.66184734679344));
#4342=CARTESIAN_POINT('Ctrl Pts',(2.02820543747774,-1.37772049925617,8.66612677650875));
#4343=CARTESIAN_POINT('Ctrl Pts',(2.07332555080613,-1.30882261898726,8.67040620622407));
#4344=CARTESIAN_POINT('Ctrl Pts',(2.11481568600756,-1.23794380495092,8.67468563593939));
#4345=CARTESIAN_POINT('Ctrl Pts',(2.15630582120899,-1.16706499091459,8.67896506565471));
#4346=CARTESIAN_POINT('Ctrl Pts',(2.19416581018959,-1.09420570863186,8.68324449537002));
#4347=CARTESIAN_POINT('Ctrl Pts',(2.22822798017978,-1.01977954399171,8.68752392508534));
#4348=CARTESIAN_POINT('Ctrl Pts',(2.26190230088903,-0.946200833710673,8.69175462702617));
#4349=CARTESIAN_POINT('Ctrl Pts',(2.29199154861773,-0.870814010199191,8.695985328967));
#4350=CARTESIAN_POINT('Ctrl Pts',(2.31829892371557,-0.794002739478404,8.70021603090783));
#4351=CARTESIAN_POINT('Ctrl Pts',(2.34456850235416,-0.717301825418201,8.70444065449409));
#4352=CARTESIAN_POINT('Ctrl Pts',(2.36706685020363,-0.639180964925148,8.70866527808035));
#4353=CARTESIAN_POINT('Ctrl Pts',(2.38564439164319,-0.560045611197326,8.71288990166661));
#4354=CARTESIAN_POINT('Ctrl Pts',(2.40429505060717,-0.480598796387484,8.71713115253475));
#4355=CARTESIAN_POINT('Ctrl Pts',(2.418993776443,-0.400129917035782,8.7213724034029));
#4356=CARTESIAN_POINT('Ctrl Pts',(2.42963922641219,-0.319066575308621,8.72561365427104));
#4357=CARTESIAN_POINT('Ctrl Pts',(2.44022380542706,-0.238466755836126,8.72983065355859));
#4358=CARTESIAN_POINT('Ctrl Pts',(2.44680127509918,-0.157279719579152,8.73404765284614));
#4359=CARTESIAN_POINT('Ctrl Pts',(2.44932316256163,-0.0759361267060359,
8.7382646521337));
#4360=CARTESIAN_POINT('Ctrl Pts',(2.45184421396321,0.00538049898668423,
8.74248025339374));
#4361=CARTESIAN_POINT('Ctrl Pts',(2.45031233873225,0.0868531137583524,8.74669585465378));
#4362=CARTESIAN_POINT('Ctrl Pts',(2.44473108895808,0.168048066581625,8.75091145591382));
#4363=CARTESIAN_POINT('Ctrl Pts',(2.43914997845053,0.249240993380991,8.75512695198372));
#4364=CARTESIAN_POINT('Ctrl Pts',(2.42951972727187,0.330155808116043,8.75934244805361));
#4365=CARTESIAN_POINT('Ctrl Pts',(2.4158958831663,0.410362439436317,8.76355794412351));
#4366=CARTESIAN_POINT('Ctrl Pts',(2.40212767628843,0.491418966833192,8.76781810898839));
#4367=CARTESIAN_POINT('Ctrl Pts',(2.38428080292132,0.571751732834513,8.77207827385327));
#4368=CARTESIAN_POINT('Ctrl Pts',(2.36246552773785,0.650927707391768,8.77633843871815));
#4369=CARTESIAN_POINT('Ctrl Pts',(2.34084755381676,0.729387600231115,8.78056007388773));
#4370=CARTESIAN_POINT('Ctrl Pts',(2.31533287718715,0.806711114715091,8.7847817090573));
#4371=CARTESIAN_POINT('Ctrl Pts',(2.28607834965371,0.882494209184735,8.78900334422688));
#4372=CARTESIAN_POINT('Ctrl Pts',(2.25642332516109,0.959314780634891,8.79328277393941));
#4373=CARTESIAN_POINT('Ctrl Pts',(2.22292547788995,1.03455198387359,8.79756220365194));
#4374=CARTESIAN_POINT('Ctrl Pts',(2.18579683249587,1.10780975670511,8.80184163336447));
#4375=CARTESIAN_POINT('Ctrl Pts',(2.14866818710179,1.18106752953663,8.806121063077));
#4376=CARTESIAN_POINT('Ctrl Pts',(2.10790904396707,1.25234547859619,8.81040049278953));
#4377=CARTESIAN_POINT('Ctrl Pts',(2.06377634851482,1.32127871144238,8.81467992250206));
#4378=CARTESIAN_POINT('Ctrl Pts',(2.02014617047389,1.38942703529153,8.81891062444216));
#4379=CARTESIAN_POINT('Ctrl Pts',(1.97305480665095,1.45554011598564,8.82314132638225));
#4380=CARTESIAN_POINT('Ctrl Pts',(1.92271827747735,1.51924477140931,8.82737202832234));
#4381=CARTESIAN_POINT('Ctrl Pts',(1.87245406804581,1.58285790077181,8.83159665190785));
#4382=CARTESIAN_POINT('Ctrl Pts',(1.8189542389445,1.6440691152987,8.83582127549335));
#4383=CARTESIAN_POINT('Ctrl Pts',(1.76247869598671,1.70253314099696,8.84004589907886));
#4384=CARTESIAN_POINT('Ctrl Pts',(1.70578087646237,1.76122726953653,8.84428714994719));
#4385=CARTESIAN_POINT('Ctrl Pts',(1.64608412507283,1.81715213841906,8.84852840081552));
#4386=CARTESIAN_POINT('Ctrl Pts',(1.5836930833972,1.86999103409611,8.85276965168385));
#4387=CARTESIAN_POINT('Ctrl Pts',(1.52165879530245,1.92252779560878,8.85698665097064));
#4388=CARTESIAN_POINT('Ctrl Pts',(1.4569613038109,1.97201347592082,8.86120365025743));
#4389=CARTESIAN_POINT('Ctrl Pts',(1.3899364459144,2.01817415658779,8.86542064954422));
#4390=CARTESIAN_POINT('Ctrl Pts',(1.32293380822476,2.06431953397915,8.86963625080348));
#4391=CARTESIAN_POINT('Ctrl Pts',(1.25360571905227,2.10714183715056,8.87385185206275));
#4392=CARTESIAN_POINT('Ctrl Pts',(1.18231869690365,2.14640926874444,8.87806745332201));
#4393=CARTESIAN_POINT('Ctrl Pts',(1.11103345355034,2.18567572051449,8.88228294939113));
#4394=CARTESIAN_POINT('Ctrl Pts',(1.03778978228036,2.22138725363865,8.88649844546026));
#4395=CARTESIAN_POINT('Ctrl Pts',(0.962979343023657,2.25335772457675,8.89071394152938));
#4396=CARTESIAN_POINT('Ctrl Pts',(0.887376187501839,2.28566696524496,8.89497410639517));
#4397=CARTESIAN_POINT('Ctrl Pts',(0.810173301462104,2.31415518338324,8.89923427126095));
#4398=CARTESIAN_POINT('Ctrl Pts',(0.731794456775938,2.33868063724657,8.90349443612674));
#4399=CARTESIAN_POINT('Ctrl Pts',(0.654124484452999,2.36298427849567,8.90771607129554));
#4400=CARTESIAN_POINT('Ctrl Pts',(0.575300209773041,2.3833964889253,8.91193770646433));
#4401=CARTESIAN_POINT('Ctrl Pts',(0.495746255225524,2.39983038992964,8.91615934163313));
#4402=CARTESIAN_POINT('Ctrl Pts',(0.415103200255845,2.41648927244023,8.92043877134741));
#4403=CARTESIAN_POINT('Ctrl Pts',(0.333710824244754,2.42906001847969,8.92471820106169));
#4404=CARTESIAN_POINT('Ctrl Pts',(0.252016912123801,2.43750645660757,8.92899763077597));
#4405=CARTESIAN_POINT('Ctrl Pts',(0.17032300000285,2.44595289473544,8.93327706049026));
#4406=CARTESIAN_POINT('Ctrl Pts',(0.0883280451269847,2.45027506452807,8.93755649020454));
#4407=CARTESIAN_POINT('Ctrl Pts',(0.00647794685802633,2.45049143769255,
8.94183591991882));
#4408=CARTESIAN_POINT('Ctrl Pts',(-0.0744401643555323,2.45070534712159,
8.94606662185901));
#4409=CARTESIAN_POINT('Ctrl Pts',(-0.155521056560432,2.44690733381109,8.95029732379919));
#4410=CARTESIAN_POINT('Ctrl Pts',(-0.236334018065072,2.4390769733457,8.95452802573937));
#4411=CARTESIAN_POINT('Ctrl Pts',(-0.317030873580234,2.43125786295372,8.95875264932497));
#4412=CARTESIAN_POINT('Ctrl Pts',(-0.397460103947487,2.4194179558364,8.96297727291058));
#4413=CARTESIAN_POINT('Ctrl Pts',(-0.477190701373381,2.40358883433144,8.96720189649618));
#4414=CARTESIAN_POINT('Ctrl Pts',(-0.557235102658202,2.38769741253561,8.97144314736449));
#4415=CARTESIAN_POINT('Ctrl Pts',(-0.636574885291669,2.36778530622891,8.9756843982328));
#4416=CARTESIAN_POINT('Ctrl Pts',(-0.714778833415444,2.34393717264377,8.9799256491011));
#4417=CARTESIAN_POINT('Ctrl Pts',(-0.792535609354803,2.32022540329912,8.98414264838799));
#4418=CARTESIAN_POINT('Ctrl Pts',(-0.869169055689855,2.2926226341566,8.98835964767487));
#4419=CARTESIAN_POINT('Ctrl Pts',(-0.944267047301864,2.26126292000285,8.99257664696175));
#4420=CARTESIAN_POINT('Ctrl Pts',(-1.01934014228681,2.22991360228036,8.99679224822112));
#4421=CARTESIAN_POINT('Ctrl Pts',(-1.09287836460284,2.19480999197975,9.0010078494805));
#4422=CARTESIAN_POINT('Ctrl Pts',(-1.16448839141626,2.15613474445749,9.00522345073987));
#4423=CARTESIAN_POINT('Ctrl Pts',(-1.23609663137471,2.11746046198247,9.00943894680911));
#4424=CARTESIAN_POINT('Ctrl Pts',(-1.30577636281228,2.07521494143496,9.01365444287835));
#4425=CARTESIAN_POINT('Ctrl Pts',(-1.37315903482134,2.02962669352975,9.01786993894759));
#4426=CARTESIAN_POINT('Ctrl Pts',(-1.44125571600252,1.98355537740873,9.02213010381325));
#4427=CARTESIAN_POINT('Ctrl Pts',(-1.50700595679968,1.9340703289569,9.02639026867891));
#4428=CARTESIAN_POINT('Ctrl Pts',(-1.57006115166297,1.88145109690333,9.03065043354457));
#4429=CARTESIAN_POINT('Ctrl Pts',(-1.6325460640103,1.8293077626423,9.03487206871347));
#4430=CARTESIAN_POINT('Ctrl Pts',(-1.69238417959119,1.77408707324531,9.03909370388235));
#4431=CARTESIAN_POINT('Ctrl Pts',(-1.74927255891815,1.71609899615843,9.04331533905125));
#4432=CARTESIAN_POINT('Ctrl Pts',(-1.80693974500516,1.65731705735545,9.0475947687653));
#4433=CARTESIAN_POINT('Ctrl Pts',(-1.86157549088788,1.59569175573465,9.05187419847934));
#4434=CARTESIAN_POINT('Ctrl Pts',(-1.91290694908905,1.53157998619949,9.05615362819339));
#4435=CARTESIAN_POINT('Ctrl Pts',(-1.96423840729021,1.46746821666433,9.06043305790744));
#4436=CARTESIAN_POINT('Ctrl Pts',(-2.01226534397572,1.40087041543378,9.06471248762149));
#4437=CARTESIAN_POINT('Ctrl Pts',(-2.05676187417548,1.33217147655179,9.06899191733554));
#4438=CARTESIAN_POINT('Ctrl Pts',(-2.10171929270989,1.26276096444394,9.07331567273578));
#4439=CARTESIAN_POINT('Ctrl Pts',(-2.14323638783505,1.19095353206654,9.07763942813602));
#4440=CARTESIAN_POINT('Ctrl Pts',(-2.18105535464625,1.11711583551973,9.08196318353626));
#4441=CARTESIAN_POINT('Ctrl Pts',(-2.21881263121907,1.04339858290581,9.08627988603359));
#4442=CARTESIAN_POINT('Ctrl Pts',(-2.25288357200913,0.967658035312121,9.09059658853091));
#4443=CARTESIAN_POINT('Ctrl Pts',(-2.28305401222146,0.890289069504666,9.09491329102823));
#4444=CARTESIAN_POINT('Ctrl Pts',(-2.31317310560235,0.813051777322742,9.09922264696402));
#4445=CARTESIAN_POINT('Ctrl Pts',(-2.33940475210908,0.734191988265807,9.10353200289981));
#4446=CARTESIAN_POINT('Ctrl Pts',(-2.3615816991856,0.654126996898643,9.1078413588356));
#4447=CARTESIAN_POINT('Ctrl Pts',(-2.38373640869621,0.574142289373843,9.11214639363619));
#4448=CARTESIAN_POINT('Ctrl Pts',(-2.40184438315027,0.492955201522529,9.11645142843678));
#4449=CARTESIAN_POINT('Ctrl Pts',(-2.41578745660378,0.411000260968077,9.12075646323736));
#4450=CARTESIAN_POINT('Ctrl Pts',(-2.42971883039754,0.329114088961891,9.12505788567497));
#4451=CARTESIAN_POINT('Ctrl Pts',(-2.43949218192697,0.246461776577874,9.12935930811257));
#4452=CARTESIAN_POINT('Ctrl Pts',(-2.44504020385111,0.163488995200726,9.13366073055018));
#4453=CARTESIAN_POINT('Ctrl Pts',(-2.44869973006766,0.108759386547032,9.13649798829612));
#4454=CARTESIAN_POINT('Ctrl Pts',(-2.45052192610961,0.0538905871464149,
9.13933524604205));
#4455=CARTESIAN_POINT('Ctrl Pts',(-2.4504998008426,-0.000987962737744003,
9.14217250378799));
#4456=CARTESIAN_POINT('',(-2.45288802918575,-0.00174278630456637,9.94217250378798));
#4457=CARTESIAN_POINT('Ctrl Pts',(-2.44683804691476,-0.0010002212498868,
9.14217321494963));
#4458=CARTESIAN_POINT('Ctrl Pts',(-2.44809247353642,-0.348475610399284,
9.16016478155052));
#4459=CARTESIAN_POINT('Ctrl Pts',(-2.2164011699741,-1.51294856493534,9.22054168062364));
#4460=CARTESIAN_POINT('Ctrl Pts',(-0.427813805281666,-2.86569395165591,
9.32330391216903));
#4461=CARTESIAN_POINT('Ctrl Pts',(2.17773028627945,-1.91120832897776,9.45045990958575));
#4462=CARTESIAN_POINT('Ctrl Pts',(2.78591175602507,0.796192290953494,9.57761590700248));
#4463=CARTESIAN_POINT('Ctrl Pts',(0.838920969493999,2.77334420573432,9.70477190441923));
#4464=CARTESIAN_POINT('Ctrl Pts',(-1.757082399502,2.23196455382522,9.82629077001439));
#4465=CARTESIAN_POINT('Ctrl Pts',(-2.44721011341078,0.703532295850273,9.90542430313731));
#4466=CARTESIAN_POINT('Ctrl Pts',(-2.45288802918575,-0.00174278630456637,
9.94217250378798));
#4467=CARTESIAN_POINT('',(-2.45231825334198,0.00195314577384671,10.742172503788));
#4468=CARTESIAN_POINT('Ctrl Pts',(-2.45288802918575,-0.00174278630456637,
9.94217250378798));
#4469=CARTESIAN_POINT('Ctrl Pts',(-2.45375901495182,-0.109931174801997,
9.94780963560955));
#4470=CARTESIAN_POINT('Ctrl Pts',(-2.39807267662402,-1.03068064077238,9.99583209990337));
#4471=CARTESIAN_POINT('Ctrl Pts',(-1.23228710005795,-2.62234532042679,10.0862398966695));
#4472=CARTESIAN_POINT('Ctrl Pts',(1.53758172190995,-2.4558234718693,10.2133958940861));
#4473=CARTESIAN_POINT('Ctrl Pts',(2.89721701832281,-0.0368785205104102,
10.340551891503));
#4474=CARTESIAN_POINT('Ctrl Pts',(1.5995935090241,2.4158905361011,10.4677078889196));
#4475=CARTESIAN_POINT('Ctrl Pts',(-1.16513926773105,2.65286203247095,10.5948638863363));
#4476=CARTESIAN_POINT('Ctrl Pts',(-2.38547222680609,1.0727264530832,10.6863520912925));
#4477=CARTESIAN_POINT('Ctrl Pts',(-2.45344104862174,0.130954817715624,10.7354549637764));
#4478=CARTESIAN_POINT('Ctrl Pts',(-2.45231825334198,0.00195314577384671,
10.742172503788));
#4479=CARTESIAN_POINT('',(-2.44662748352118,0.00066590285712469,11.542172503788));
#4480=CARTESIAN_POINT('Ctrl Pts',(-2.45231825334198,0.00195314577384671,
10.742172503788));
#4481=CARTESIAN_POINT('Ctrl Pts',(-2.44635660235887,-0.683000699522043,
10.7778402962486));
#4482=CARTESIAN_POINT('Ctrl Pts',(-1.79037428776405,-2.19191629563671,10.8558934211814));
#4483=CARTESIAN_POINT('Ctrl Pts',(0.768057096932581,-2.79379934361555,10.9763318785866));
#4484=CARTESIAN_POINT('Ctrl Pts',(2.76474302699328,-0.866846278890543,11.1034878760034));
#4485=CARTESIAN_POINT('Ctrl Pts',(2.22567215749589,1.85515765472443,11.23064387342));
#4486=CARTESIAN_POINT('Ctrl Pts',(-0.354732482212946,2.8756549415042,11.3577998708367));
#4487=CARTESIAN_POINT('Ctrl Pts',(-2.19633755390064,1.55513205657248,11.4616427476261));
#4488=CARTESIAN_POINT('Ctrl Pts',(-2.44752205661339,0.369091202994485,11.5231002919432));
#4489=CARTESIAN_POINT('Ctrl Pts',(-2.44662748352118,0.00066590285712469,
11.542172503788));
#4490=CARTESIAN_POINT('',(-2.45049897433078,-0.00224205347296723,12.3421725236924));
#4491=CARTESIAN_POINT('Ctrl Pts',(-2.44662748352118,0.00066590285712469,
11.542172503788));
#4492=CARTESIAN_POINT('Ctrl Pts',(-2.44553399260474,-0.449682674129272,
11.5654856244154));
#4493=CARTESIAN_POINT('Ctrl Pts',(-2.11046030797052,-1.72031872164123,11.631184077515));
#4494=CARTESIAN_POINT('Ctrl Pts',(-0.066093817566476,-2.89669778952078,
11.7392678630871));
#4495=CARTESIAN_POINT('Ctrl Pts',(2.39963648265557,-1.62387537318686,11.8664238605037));
#4496=CARTESIAN_POINT('Ctrl Pts',(2.66447705535063,1.13832706110551,11.9935798579205));
#4497=CARTESIAN_POINT('Ctrl Pts',(0.485522402085563,2.85648288522925,12.1207358553373));
#4498=CARTESIAN_POINT('Ctrl Pts',(-1.91257980658966,2.03245349049535,12.2369334039597));
#4499=CARTESIAN_POINT('Ctrl Pts',(-2.44444428856106,0.602821897078908,12.31074562011));
#4500=CARTESIAN_POINT('Ctrl Pts',(-2.44987021777706,-0.00224109498362596,
12.342172503788));
#4501=CARTESIAN_POINT('',(-2.45083983812899,0.00049556074693392,13.1421725532727));
#4502=CARTESIAN_POINT('Ctrl Pts',(-2.45049897433078,-0.00224205347296723,
12.3421725236924));
#4503=CARTESIAN_POINT('Ctrl Pts',(-2.45040243216092,-0.107759825940935,
12.3476517447721));
#4504=CARTESIAN_POINT('Ctrl Pts',(-2.44348655931372,-0.212972878406652,
12.3531309658518));
#4505=CARTESIAN_POINT('Ctrl Pts',(-2.42989259424978,-0.317131251077622,
12.3586101869315));
#4506=CARTESIAN_POINT('Ctrl Pts',(-2.41629862918585,-0.421289623748593,
12.3640894080113));
#4507=CARTESIAN_POINT('Ctrl Pts',(-2.39602674807031,-0.524393675044689,
12.369568629091));
#4508=CARTESIAN_POINT('Ctrl Pts',(-2.36926728014896,-0.625717831946268,
12.3750478501708));
#4509=CARTESIAN_POINT('Ctrl Pts',(-2.34860534094121,-0.70395382588797,12.379278552111));
#4510=CARTESIAN_POINT('Ctrl Pts',(-2.32402521275318,-0.781312427764938,
12.3835092540513));
#4511=CARTESIAN_POINT('Ctrl Pts',(-2.29561824173242,-0.857372228513002,
12.3877399559916));
#4512=CARTESIAN_POINT('Ctrl Pts',(-2.26725208371266,-0.933322752255728,
12.3919645795773));
#4513=CARTESIAN_POINT('Ctrl Pts',(-2.23507016376243,-1.00797774891747,12.3961892031629));
#4514=CARTESIAN_POINT('Ctrl Pts',(-2.19921415187082,-1.08092893578214,12.4004138267486));
#4515=CARTESIAN_POINT('Ctrl Pts',(-2.1632170178103,-1.15416724408536,12.4046550776169));
#4516=CARTESIAN_POINT('Ctrl Pts',(-2.12351692995344,-1.22568784328583,12.4088963284852));
#4517=CARTESIAN_POINT('Ctrl Pts',(-2.08030689143503,-1.2950959375459,12.4131375793535));
#4518=CARTESIAN_POINT('Ctrl Pts',(-2.03734392902606,-1.36410715454132,12.4173545786404));
#4519=CARTESIAN_POINT('Ctrl Pts',(-1.99091129526494,-1.4310295609814,12.4215715779274));
#4520=CARTESIAN_POINT('Ctrl Pts',(-1.94124479636664,-1.49549954549624,12.4257885772143));
#4521=CARTESIAN_POINT('Ctrl Pts',(-1.89159476299925,-1.55994815680082,12.4300041784738));
#4522=CARTESIAN_POINT('Ctrl Pts',(-1.83871327709118,-1.62194559260165,12.4342197797332));
#4523=CARTESIAN_POINT('Ctrl Pts',(-1.78287825230524,-1.68115894175923,12.4384353809926));
#4524=CARTESIAN_POINT('Ctrl Pts',(-1.7270446207474,-1.74037081339079,12.4426508770619));
#4525=CARTESIAN_POINT('Ctrl Pts',(-1.66825791668527,-1.79679839888931,12.4468663731312));
#4526=CARTESIAN_POINT('Ctrl Pts',(-1.60683396932452,-1.85014454706242,12.4510818692005));
#4527=CARTESIAN_POINT('Ctrl Pts',(-1.54475915341902,-1.9040559687375,12.4553420340661));
#4528=CARTESIAN_POINT('Ctrl Pts',(-1.47999122643177,-1.95481993054753,12.4596021989316));
#4529=CARTESIAN_POINT('Ctrl Pts',(-1.41289018521115,-2.00217171454748,12.4638623637972));
#4530=CARTESIAN_POINT('Ctrl Pts',(-1.34639601786583,-2.04909524050351,12.4680839989661));
#4531=CARTESIAN_POINT('Ctrl Pts',(-1.27761119900921,-2.09266786159513,12.4723056341351));
#4532=CARTESIAN_POINT('Ctrl Pts',(-1.20691333802504,-2.13267682607967,12.476527269304));
#4533=CARTESIAN_POINT('Ctrl Pts',(-1.13524761730405,-2.17323351669478,12.4808066990179));
#4534=CARTESIAN_POINT('Ctrl Pts',(-1.06161652068031,-2.21012801679272,12.4850861287318));
#4535=CARTESIAN_POINT('Ctrl Pts',(-0.986435236874027,-2.24318875118731,
12.4893655584457));
#4536=CARTESIAN_POINT('Ctrl Pts',(-0.911253953067751,-2.2762494855819,12.4936449881596));
#4537=CARTESIAN_POINT('Ctrl Pts',(-0.834522963846906,-2.30547634084911,
12.4979244178735));
#4538=CARTESIAN_POINT('Ctrl Pts',(-0.756672398389139,-2.33075033659035,
12.5022038475874));
#4539=CARTESIAN_POINT('Ctrl Pts',(-0.679708279253695,-2.35573654970029,
12.5064345495276));
#4540=CARTESIAN_POINT('Ctrl Pts',(-0.601360480166753,-2.37695348549062,
12.5106652514679));
#4541=CARTESIAN_POINT('Ctrl Pts',(-0.52203275985569,-2.39424978806253,12.5148959534081));
#4542=CARTESIAN_POINT('Ctrl Pts',(-0.442819011651081,-2.41152124060684,
12.5191205769938));
#4543=CARTESIAN_POINT('Ctrl Pts',(-0.362628588873684,-2.424883148893,12.5233452005795));
#4544=CARTESIAN_POINT('Ctrl Pts',(-0.281881460098961,-2.43423357393092,
12.5275698241652));
#4545=CARTESIAN_POINT('Ctrl Pts',(-0.200816526600817,-2.44362080039184,
12.5318110750334));
#4546=CARTESIAN_POINT('Ctrl Pts',(-0.119190946900967,-2.4489647525341,12.5360523259017));
#4547=CARTESIAN_POINT('Ctrl Pts',(-0.0374411427535529,-2.4502139520518,
12.54029357677));
#4548=CARTESIAN_POINT('Ctrl Pts',(0.0438412139152897,-2.45145600861459,
12.544510576057));
#4549=CARTESIAN_POINT('Ctrl Pts',(0.125245908568908,-2.448650006106,12.5487275753439));
#4550=CARTESIAN_POINT('Ctrl Pts',(0.20633956393436,-2.44179733687204,12.5529445746309));
#4551=CARTESIAN_POINT('Ctrl Pts',(0.287406334978989,-2.43494693944784,12.5571601758903));
#4552=CARTESIAN_POINT('Ctrl Pts',(0.368161808465367,-2.42405257853431,12.5613757771498));
#4553=CARTESIAN_POINT('Ctrl Pts',(0.448175621099132,-2.40916767009945,12.5655913784092));
#4554=CARTESIAN_POINT('Ctrl Pts',(0.528187437181607,-2.3942831330815,12.5698068744785));
#4555=CARTESIAN_POINT('Ctrl Pts',(0.607457172188748,-2.3754083326432,12.5740223705478));
#4556=CARTESIAN_POINT('Ctrl Pts',(0.685564000346674,-2.35264792338944,12.5782378666171));
#4557=CARTESIAN_POINT('Ctrl Pts',(0.764498474394502,-2.32964633728066,12.5824980314827));
#4558=CARTESIAN_POINT('Ctrl Pts',(0.842244780125857,-2.3026764257124,12.5867581963483));
#4559=CARTESIAN_POINT('Ctrl Pts',(0.918385447378562,-2.27189753731177,12.5910183612139));
#4560=CARTESIAN_POINT('Ctrl Pts',(0.993837484753712,-2.24139701870898,12.5952399963829));
#4561=CARTESIAN_POINT('Ctrl Pts',(1.0677124095195,-2.20715639802551,12.5994616315518));
#4562=CARTESIAN_POINT('Ctrl Pts',(1.13962690685403,-2.16937796687768,12.6036832667208));
#4563=CARTESIAN_POINT('Ctrl Pts',(1.21252591978051,-2.13108234579064,12.6079626964347));
#4564=CARTESIAN_POINT('Ctrl Pts',(1.28340999627542,-2.08915156679782,12.6122421261486));
#4565=CARTESIAN_POINT('Ctrl Pts',(1.35191009511859,-2.04384181010088,12.6165215558625));
#4566=CARTESIAN_POINT('Ctrl Pts',(1.42041019396175,-1.99853205340395,12.6208009855764));
#4567=CARTESIAN_POINT('Ctrl Pts',(1.48652595895617,-1.94984366264381,12.6250804152903));
#4568=CARTESIAN_POINT('Ctrl Pts',(1.54992447940436,-1.89807385476517,12.6293598450042));
#4569=CARTESIAN_POINT('Ctrl Pts',(1.61260111190023,-1.84689352437492,12.6335905469444));
#4570=CARTESIAN_POINT('Ctrl Pts',(1.6728578368507,-1.79250912326258,12.6378212488847));
#4571=CARTESIAN_POINT('Ctrl Pts',(1.7303488008871,-1.73517816873904,12.642051950825));
#4572=CARTESIAN_POINT('Ctrl Pts',(1.78775716622726,-1.67792958302209,12.6462765744106));
#4573=CARTESIAN_POINT('Ctrl Pts',(1.84240733600462,-1.61774317723492,12.6505011979963));
#4574=CARTESIAN_POINT('Ctrl Pts',(1.89398622828447,-1.55491685213994,12.654725821582));
#4575=CARTESIAN_POINT('Ctrl Pts',(1.94576812487967,-1.49184325505931,12.6589670724503));
#4576=CARTESIAN_POINT('Ctrl Pts',(1.99445414866907,-1.42610921385226,12.6632083233186));
#4577=CARTESIAN_POINT('Ctrl Pts',(2.03976473497199,-1.35805378242714,12.6674495741869));
#4578=CARTESIAN_POINT('Ctrl Pts',(2.08481623417936,-1.29038749370581,12.6716665734738));
#4579=CARTESIAN_POINT('Ctrl Pts',(2.12653053250305,-1.22042668126703,12.6758835727608));
#4580=CARTESIAN_POINT('Ctrl Pts',(2.16467416497889,-1.14853646414597,12.6801005720478));
#4581=CARTESIAN_POINT('Ctrl Pts',(2.20280515200609,-1.07667008020465,12.6843161733072));
#4582=CARTESIAN_POINT('Ctrl Pts',(2.23736760612099,-1.00287597228756,12.6885317745666));
#4583=CARTESIAN_POINT('Ctrl Pts',(2.26817343341471,-0.927544891609961,12.6927473758261));
#4584=CARTESIAN_POINT('Ctrl Pts',(2.29897849202349,-0.852215690637342,12.6969628718954));
#4585=CARTESIAN_POINT('Ctrl Pts',(2.32602693515753,-0.775350024025249,12.7011783679647));
#4586=CARTESIAN_POINT('Ctrl Pts',(2.34917891190397,-0.697358365451837,12.705393864034));
#4587=CARTESIAN_POINT('Ctrl Pts',(2.37257621468461,-0.618540281363785,12.7096540288995));
#4588=CARTESIAN_POINT('Ctrl Pts',(2.39199382957925,-0.538572660312077,12.7139141937651));
#4589=CARTESIAN_POINT('Ctrl Pts',(2.40733970685362,-0.457892766710644,12.7181743586307));
#4590=CARTESIAN_POINT('Ctrl Pts',(2.42254679325618,-0.377942556565532,12.7223959937997));
#4591=CARTESIAN_POINT('Ctrl Pts',(2.43375549324763,-0.297293380137965,12.7266176289686));
#4592=CARTESIAN_POINT('Ctrl Pts',(2.44092835384074,-0.216377035325659,12.7308392641376));
#4593=CARTESIAN_POINT('Ctrl Pts',(2.44819941150613,-0.134352938863017,12.7351186938515));
#4594=CARTESIAN_POINT('Ctrl Pts',(2.45132327236096,-0.0520547978097172,
12.7393981235654));
#4595=CARTESIAN_POINT('Ctrl Pts',(2.45031551854859,0.030068414656077,12.7436775532793));
#4596=CARTESIAN_POINT('Ctrl Pts',(2.44930776473623,0.112191627121871,12.7479569829932));
#4597=CARTESIAN_POINT('Ctrl Pts',(2.44416849232609,0.194139425473585,12.752236412707));
#4598=CARTESIAN_POINT('Ctrl Pts',(2.43496734690495,0.275470995762991,12.7565158424209));
#4599=CARTESIAN_POINT('Ctrl Pts',(2.42587097042763,0.355876483230287,12.7607465443612));
#4600=CARTESIAN_POINT('Ctrl Pts',(2.41277058077403,0.435982137069594,12.7649772463014));
#4601=CARTESIAN_POINT('Ctrl Pts',(2.39569543844962,0.515357755536542,12.7692079482417));
#4602=CARTESIAN_POINT('Ctrl Pts',(2.37864482840639,0.594619333080539,12.7734325718274));
#4603=CARTESIAN_POINT('Ctrl Pts',(2.35763090428529,0.673152507543908,12.777657195413));
#4604=CARTESIAN_POINT('Ctrl Pts',(2.3327346221251,0.750532765932898,12.7818818189987));
#4605=CARTESIAN_POINT('Ctrl Pts',(2.30774035312392,0.828217577709613,12.786123069867));
#4606=CARTESIAN_POINT('Ctrl Pts',(2.2788331534967,0.904739907101411,12.7903643207353));
#4607=CARTESIAN_POINT('Ctrl Pts',(2.24614672573761,0.979681140197254,12.7946055716036));
#4608=CARTESIAN_POINT('Ctrl Pts',(2.2136471998115,1.05419385739856,12.7988225708905));
#4609=CARTESIAN_POINT('Ctrl Pts',(2.17741173571577,1.12714308017367,12.8030395701775));
#4610=CARTESIAN_POINT('Ctrl Pts',(2.13762090932871,1.19813484132659,12.8072565694644));
#4611=CARTESIAN_POINT('Ctrl Pts',(2.0978432744711,1.2691030671576,12.8114721707239));
#4612=CARTESIAN_POINT('Ctrl Pts',(2.05451284518539,1.3381147146936,12.8156877719833));
#4613=CARTESIAN_POINT('Ctrl Pts',(2.0078563122249,1.40480008522873,12.8199033732427));
#4614=CARTESIAN_POINT('Ctrl Pts',(1.96120094346539,1.47148379179165,12.824118869312));
#4615=CARTESIAN_POINT('Ctrl Pts',(1.91121990354004,1.53584095633197,12.8283343653813));
#4616=CARTESIAN_POINT('Ctrl Pts',(1.85818258434079,1.59753176283058,12.8325498614506));
#4617=CARTESIAN_POINT('Ctrl Pts',(1.80458326409398,1.65987626560194,12.8368100263162));
#4618=CARTESIAN_POINT('Ctrl Pts',(1.74786281183033,1.71949718877392,12.8410701911818));
#4619=CARTESIAN_POINT('Ctrl Pts',(1.68833902407878,1.7760804007062,12.8453303560474));
#4620=CARTESIAN_POINT('Ctrl Pts',(1.62935358016044,1.83215186390142,12.8495519912163));
#4621=CARTESIAN_POINT('Ctrl Pts',(1.56761570131212,1.88524008226713,12.8537736263853));
#4622=CARTESIAN_POINT('Ctrl Pts',(1.50346814737377,1.93507978642548,12.8579952615543));
#4623=CARTESIAN_POINT('Ctrl Pts',(1.43844240795988,1.98560180037758,12.8622746912682));
#4624=CARTESIAN_POINT('Ctrl Pts',(1.37094092201193,2.03278539839958,12.8665541209821));
#4625=CARTESIAN_POINT('Ctrl Pts',(1.30134960346411,2.07640060189834,12.870833550696));
#4626=CARTESIAN_POINT('Ctrl Pts',(1.2317582849163,2.1200158053971,12.8751129804098));
#4627=CARTESIAN_POINT('Ctrl Pts',(1.16007759399185,2.16006243227386,12.8793924101237));
#4628=CARTESIAN_POINT('Ctrl Pts',(1.08671585527975,2.19636037568601,12.8836718398376));
#4629=CARTESIAN_POINT('Ctrl Pts',(1.01418945081465,2.23224501216514,12.8879025417779));
#4630=CARTESIAN_POINT('Ctrl Pts',(0.939747313560946,2.26460091096586,12.8921332437181));
#4631=CARTESIAN_POINT('Ctrl Pts',(0.863766980855926,2.29321975675752,12.8963639456584));
#4632=CARTESIAN_POINT('Ctrl Pts',(0.787895810982456,2.32179748514247,12.9005885692441));
#4633=CARTESIAN_POINT('Ctrl Pts',(0.710491266285847,2.34664866134351,12.9048131928298));
#4634=CARTESIAN_POINT('Ctrl Pts',(0.63195408981764,2.36761151339546,12.9090378164154));
#4635=CARTESIAN_POINT('Ctrl Pts',(0.553107806561057,2.3886568710857,12.9132790672837));
#4636=CARTESIAN_POINT('Ctrl Pts',(0.473120382119683,2.40578302118053,12.917520318152));
#4637=CARTESIAN_POINT('Ctrl Pts',(0.392416157402715,2.41887573252726,12.9217615690203));
#4638=CARTESIAN_POINT('Ctrl Pts',(0.312173401514297,2.43189357941443,12.9259785683072));
#4639=CARTESIAN_POINT('Ctrl Pts',(0.231222484144265,2.44092391377575,12.9301955675942));
#4640=CARTESIAN_POINT('Ctrl Pts',(0.149992402096151,2.44590525763232,12.9344125668812));
#4641=CARTESIAN_POINT('Ctrl Pts',(0.0687892495973066,2.45088495006443,12.9386281681406));
#4642=CARTESIAN_POINT('Ctrl Pts',(-0.0126924199720212,2.45181828918592,
12.9428437694));
#4643=CARTESIAN_POINT('Ctrl Pts',(-0.0940190465842783,2.44869570769407,
12.9470593706595));
#4644=CARTESIAN_POINT('Ctrl Pts',(-0.175343643887187,2.4455732041187,12.9512748667288));
#4645=CARTESIAN_POINT('Ctrl Pts',(-0.256512741248561,2.43839500007924,12.9554903627981));
#4646=CARTESIAN_POINT('Ctrl Pts',(-0.337094783832249,2.42720360841712,12.9597058588674));
#4647=CARTESIAN_POINT('Ctrl Pts',(-0.418530700499861,2.41589362905237,12.9639660237329));
#4648=CARTESIAN_POINT('Ctrl Pts',(-0.499366564978021,2.40048495620425,12.9682261885985));
#4649=CARTESIAN_POINT('Ctrl Pts',(-0.579166209921358,2.38107470510384,12.9724863534641));
#4650=CARTESIAN_POINT('Ctrl Pts',(-0.658244132535397,2.36184000380251,12.9767079886331));
#4651=CARTESIAN_POINT('Ctrl Pts',(-0.736304070493699,2.33867600803559,12.980929623802));
#4652=CARTESIAN_POINT('Ctrl Pts',(-0.812937422333354,2.31172727573345,12.985151258971));
#4653=CARTESIAN_POINT('Ctrl Pts',(-0.890619891284911,2.28440961299145,12.9894306886849));
#4654=CARTESIAN_POINT('Ctrl Pts',(-0.966835960430611,2.2532029897929,12.9937101183988));
#4655=CARTESIAN_POINT('Ctrl Pts',(-1.04118333516246,2.21830735304646,12.9979895481127));
#4656=CARTESIAN_POINT('Ctrl Pts',(-1.1155307098943,2.18341171630001,13.0022689778266));
#4657=CARTESIAN_POINT('Ctrl Pts',(-1.18800898794108,2.1448273543514,13.0065484075405));
#4658=CARTESIAN_POINT('Ctrl Pts',(-1.25824567135025,2.1028000571924,13.0108278372544));
#4659=CARTESIAN_POINT('Ctrl Pts',(-1.32768260398911,2.06125130431604,13.0150585391946));
#4660=CARTESIAN_POINT('Ctrl Pts',(-1.39518992430448,2.01618138430343,13.0192892411349));
#4661=CARTESIAN_POINT('Ctrl Pts',(-1.46038808642804,1.96779493012332,13.0235199430751));
#4662=CARTESIAN_POINT('Ctrl Pts',(-1.52549257673233,1.91947799396403,13.0277445666608));
#4663=CARTESIAN_POINT('Ctrl Pts',(-1.58829412754736,1.86785426188777,13.0319691902465));
#4664=CARTESIAN_POINT('Ctrl Pts',(-1.64843976084091,1.81317307637158,13.0361938138322));
#4665=CARTESIAN_POINT('Ctrl Pts',(-1.70882211544763,1.75827667652755,13.0404350647005));
#4666=CARTESIAN_POINT('Ctrl Pts',(-1.76652719414015,1.70029894822673,13.0446763155687));
#4667=CARTESIAN_POINT('Ctrl Pts',(-1.8212292130223,1.63953481318152,13.048917566437));
#4668=CARTESIAN_POINT('Ctrl Pts',(-1.87561844435633,1.57911812902027,13.053134565724));
#4669=CARTESIAN_POINT('Ctrl Pts',(-1.92703855155145,1.51594716624645,13.0573515650109));
#4670=CARTESIAN_POINT('Ctrl Pts',(-1.97520558258288,1.45034932224393,13.0615685642979));
#4671=CARTESIAN_POINT('Ctrl Pts',(-2.02335664518979,1.38477322536175,13.0657841655573));
#4672=CARTESIAN_POINT('Ctrl Pts',(-2.06825649825139,1.31677221953997,13.0699997668168));
#4673=CARTESIAN_POINT('Ctrl Pts',(-2.10966236345087,1.2467056437824,13.0742153680762));
#4674=CARTESIAN_POINT('Ctrl Pts',(-2.15106719546708,1.17664081636685,13.0784308641455));
#4675=CARTESIAN_POINT('Ctrl Pts',(-2.1889779772965,1.10451092242006,13.0826463602148));
#4676=CARTESIAN_POINT('Ctrl Pts',(-2.22319680302972,1.03070181187308,13.0868618562841));
#4677=CARTESIAN_POINT('Ctrl Pts',(-2.25777822280421,0.956110595479309,13.0911220211497));
#4678=CARTESIAN_POINT('Ctrl Pts',(-2.28858875983413,0.87980479627115,13.0953821860153));
#4679=CARTESIAN_POINT('Ctrl Pts',(-2.3154739183128,0.802203704562095,13.0996423508809));
#4680=CARTESIAN_POINT('Ctrl Pts',(-2.34211592258677,0.725304451071835,13.1038639860498));
#4681=CARTESIAN_POINT('Ctrl Pts',(-2.3649031940265,0.647133709267337,13.1080856212188));
#4682=CARTESIAN_POINT('Ctrl Pts',(-2.38373604912697,0.568113279278458,13.1123072563877));
#4683=CARTESIAN_POINT('Ctrl Pts',(-2.40282672761737,0.488011052874501,13.1165866861016));
#4684=CARTESIAN_POINT('Ctrl Pts',(-2.41785380712066,0.407036183877513,13.1208661158155));
#4685=CARTESIAN_POINT('Ctrl Pts',(-2.42876758743796,0.325635158130646,13.1251455455294));
#4686=CARTESIAN_POINT('Ctrl Pts',(-2.43968136775527,0.244234132383773,13.1294249752433));
#4687=CARTESIAN_POINT('Ctrl Pts',(-2.44648187352101,0.162407444213362,13.1337044049572));
#4688=CARTESIAN_POINT('Ctrl Pts',(-2.4491740797156,0.0806013476886166,13.1379838346711));
#4689=CARTESIAN_POINT('Ctrl Pts',(-2.45005244916337,0.0539109790339228,
13.13938005771));
#4690=CARTESIAN_POINT('Ctrl Pts',(-2.4504945386623,0.0272061736954524,13.140776280749));
#4691=CARTESIAN_POINT('Ctrl Pts',(-2.45049994971379,0.00049644004570383,
13.142172503788));
#4692=CARTESIAN_POINT('',(-2.45049921122159,0.00196616437485418,13.942172503788));
#4693=CARTESIAN_POINT('Ctrl Pts',(-2.45441644957311,0.000486307974839832,
13.1421730739958));
#4694=CARTESIAN_POINT('Ctrl Pts',(-2.4522381490858,-0.784885048141428,13.1831619933598));
#4695=CARTESIAN_POINT('Ctrl Pts',(-1.61768875870369,-2.38635259292605,13.2665362451961));
#4696=CARTESIAN_POINT('Ctrl Pts',(1.11139908544534,-2.67582109816901,13.3922958295045));
#4697=CARTESIAN_POINT('Ctrl Pts',(2.8514413495468,-0.514304099370272,13.5194518269214));
#4698=CARTESIAN_POINT('Ctrl Pts',(1.97620916677945,2.11892043401155,13.646607824338));
#4699=CARTESIAN_POINT('Ctrl Pts',(-0.711555241617889,2.80872134870322,13.7737638217548));
#4700=CARTESIAN_POINT('Ctrl Pts',(-2.2883966915673,1.34721062141272,13.8722850888502));
#4701=CARTESIAN_POINT('Ctrl Pts',(-2.45037336834511,0.267128840959013,13.9284210234732));
#4702=CARTESIAN_POINT('Ctrl Pts',(-2.44838630074066,0.00198140226147181,
13.9421716256242));
#4703=CARTESIAN_POINT('',(-2.45049957242558,-0.00144759872526646,14.742172503788));
#4704=CARTESIAN_POINT('Ctrl Pts',(-2.45049921122159,0.00196616437485418,
13.942172503788));
#4705=CARTESIAN_POINT('Ctrl Pts',(-2.45056435292043,-0.079222206062589,
13.9463793468358));
#4706=CARTESIAN_POINT('Ctrl Pts',(-2.44659036857388,-0.160464817053646,
13.9505861898836));
#4707=CARTESIAN_POINT('Ctrl Pts',(-2.43858777176843,-0.241329503752571,
13.9547930329314));
#4708=CARTESIAN_POINT('Ctrl Pts',(-2.43058695487124,-0.322176204824231,
13.9589989403086));
#4709=CARTESIAN_POINT('Ctrl Pts',(-2.41855935099307,-0.402644684116547,
13.9632048476858));
#4710=CARTESIAN_POINT('Ctrl Pts',(-2.40256742063332,-0.482306996954589,
13.9674107550629));
#4711=CARTESIAN_POINT('Ctrl Pts',(-2.38657409952595,-0.561976237672478,
13.9716170282093));
#4712=CARTESIAN_POINT('Ctrl Pts',(-2.36661586067399,-0.640838715262248,
13.9758233013557));
#4713=CARTESIAN_POINT('Ctrl Pts',(-2.34280616296429,-0.718477231912426,
13.9800295745021));
#4714=CARTESIAN_POINT('Ctrl Pts',(-2.3189701885327,-0.796201431536588,13.9842404897515));
#4715=CARTESIAN_POINT('Ctrl Pts',(-2.2912744051616,-0.872698525713307,13.9884514050009));
#4716=CARTESIAN_POINT('Ctrl Pts',(-2.25988184464756,-0.947567569217272,
13.9926623202503));
#4717=CARTESIAN_POINT('Ctrl Pts',(-2.2284715477322,-1.02247891278789,13.9968756146138));
#4718=CARTESIAN_POINT('Ctrl Pts',(-2.19336051763534,-1.09575995335298,14.0010889089773));
#4719=CARTESIAN_POINT('Ctrl Pts',(-2.15475843919274,-1.16703312666252,14.0053022033408));
#4720=CARTESIAN_POINT('Ctrl Pts',(-2.11608554479169,-1.2384370514311,14.0095232270414));
#4721=CARTESIAN_POINT('Ctrl Pts',(-2.07390905318627,-1.30782535253099,14.0137442507421));
#4722=CARTESIAN_POINT('Ctrl Pts',(-2.02848263731509,-1.37484851533222,14.0179652744427));
#4723=CARTESIAN_POINT('Ctrl Pts',(-1.99221294503478,-1.42836164076451,14.0213354551579));
#4724=CARTESIAN_POINT('Ctrl Pts',(-1.95387236655151,-1.4803675466113,14.0247056358731));
#4725=CARTESIAN_POINT('Ctrl Pts',(-1.91360765035879,-1.53070441643327,14.0280758165883));
#4726=CARTESIAN_POINT('Ctrl Pts',(-1.8630619890676,-1.59389399314112,14.0323065185285));
#4727=CARTESIAN_POINT('Ctrl Pts',(-1.80928801626886,-1.6546960970155,14.0365372204688));
#4728=CARTESIAN_POINT('Ctrl Pts',(-1.75253974839791,-1.71276229532454,14.040767922409));
#4729=CARTESIAN_POINT('Ctrl Pts',(-1.69587301217313,-1.77074506848401,14.0449925459947));
#4730=CARTESIAN_POINT('Ctrl Pts',(-1.6362407900663,-1.82599941297279,14.0492171695804));
#4731=CARTESIAN_POINT('Ctrl Pts',(-1.57393781039641,-1.87820925857705,14.0534417931661));
#4732=CARTESIAN_POINT('Ctrl Pts',(-1.51138961852498,-1.93062459180406,14.0576830440344));
#4733=CARTESIAN_POINT('Ctrl Pts',(-1.44614989728259,-1.97997103907282,14.0619242949027));
#4734=CARTESIAN_POINT('Ctrl Pts',(-1.37855486404845,-2.02596563070758,14.0661655457709));
#4735=CARTESIAN_POINT('Ctrl Pts',(-1.31134634094944,-2.07169722408673,14.0703825450579));
#4736=CARTESIAN_POINT('Ctrl Pts',(-1.24180975659261,-2.11411492555338,14.0745995443449));
#4737=CARTESIAN_POINT('Ctrl Pts',(-1.17030785705411,-2.15298159994864,14.0788165436318));
#4738=CARTESIAN_POINT('Ctrl Pts',(-1.09882966195957,-2.19183538919105,14.0830321448912));
#4739=CARTESIAN_POINT('Ctrl Pts',(-1.02538785381415,-2.22714026723997,14.0872477461507));
#4740=CARTESIAN_POINT('Ctrl Pts',(-0.950371267117993,-2.25870420919529,
14.0914633474101));
#4741=CARTESIAN_POINT('Ctrl Pts',(-0.875356552279458,-2.29026736354873,
14.0956788434794));
#4742=CARTESIAN_POINT('Ctrl Pts',(-0.798767566099872,-2.31808958804037,
14.0998943395487));
#4743=CARTESIAN_POINT('Ctrl Pts',(-0.721013351049024,-2.34202689942047,
14.104109835618));
#4744=CARTESIAN_POINT('Ctrl Pts',(-0.642435226513823,-2.36621785850138,
14.1083700004835));
#4745=CARTESIAN_POINT('Ctrl Pts',(-0.562667490049711,-2.38644092464532,
14.1126301653491));
#4746=CARTESIAN_POINT('Ctrl Pts',(-0.482146455553999,-2.40259964317751,
14.1168903302147));
#4747=CARTESIAN_POINT('Ctrl Pts',(-0.402353667764279,-2.4186122193555,14.1211119653837));
#4748=CARTESIAN_POINT('Ctrl Pts',(-0.321821627248609,-2.43063366121305,
14.1253336005526));
#4749=CARTESIAN_POINT('Ctrl Pts',(-0.240981732250492,-2.43862216317361,
14.1295552357216));
#4750=CARTESIAN_POINT('Ctrl Pts',(-0.159035132206545,-2.44672002840622,
14.1338346654355));
#4751=CARTESIAN_POINT('Ctrl Pts',(-0.0767726788328666,-2.45067367133576,
14.1381140951494));
#4752=CARTESIAN_POINT('Ctrl Pts',(0.00535652038376576,-2.45049414561418,
14.1423935248633));
#4753=CARTESIAN_POINT('Ctrl Pts',(0.0874857196003865,-2.45031461989261,
14.1466729545772));
#4754=CARTESIAN_POINT('Ctrl Pts',(0.169481178189257,-2.44600201668813,14.1509523842911));
#4755=CARTESIAN_POINT('Ctrl Pts',(0.250901402272344,-2.43762153262925,14.1552318140049));
#4756=CARTESIAN_POINT('Ctrl Pts',(0.331394534075985,-2.42933647304453,14.1594625159452));
#4757=CARTESIAN_POINT('Ctrl Pts',(0.411628226228095,-2.41704458019804,14.1636932178855));
#4758=CARTESIAN_POINT('Ctrl Pts',(0.491172003780826,-2.40077077471006,14.1679239198257));
#4759=CARTESIAN_POINT('Ctrl Pts',(0.570601498812235,-2.38452035020271,14.1721485434114));
#4760=CARTESIAN_POINT('Ctrl Pts',(0.649342596099766,-2.36429946752609,14.1763731669971));
#4761=CARTESIAN_POINT('Ctrl Pts',(0.726969987829958,-2.34018479757358,14.1805977905828));
#4762=CARTESIAN_POINT('Ctrl Pts',(0.804902905615784,-2.31597521705111,14.1848390414511));
#4763=CARTESIAN_POINT('Ctrl Pts',(0.881712860331415,-2.28784118174837,14.1890802923193));
#4764=CARTESIAN_POINT('Ctrl Pts',(0.956979911021107,-2.25591216582163,14.1933215431876));
#4765=CARTESIAN_POINT('Ctrl Pts',(1.03181658278293,-2.22416572082754,14.1975385424746));
#4766=CARTESIAN_POINT('Ctrl Pts',(1.10512751493307,-2.1886677604776,14.2017555417616));
#4767=CARTESIAN_POINT('Ctrl Pts',(1.17651693927987,-2.14959487848002,14.2059725410485));
#4768=CARTESIAN_POINT('Ctrl Pts',(1.24788269647073,-2.11053494999761,14.210188142308));
#4769=CARTESIAN_POINT('Ctrl Pts',(1.31732780324473,-2.06790267650819,14.2144037435674));
#4770=CARTESIAN_POINT('Ctrl Pts',(1.38448029361778,-2.02192100898725,14.2186193448268));
#4771=CARTESIAN_POINT('Ctrl Pts',(1.45163110836261,-1.97594048882778,14.2228348408961));
#4772=CARTESIAN_POINT('Ctrl Pts',(1.5164890373366,-1.92661100445113,14.2270503369654));
#4773=CARTESIAN_POINT('Ctrl Pts',(1.57871156510052,-1.87419850715389,14.2312658330347));
#4774=CARTESIAN_POINT('Ctrl Pts',(1.64159342343243,-1.82123062962935,14.2355259979003));
#4775=CARTESIAN_POINT('Ctrl Pts',(1.70178331591802,-1.76511431268457,14.2397861627659));
#4776=CARTESIAN_POINT('Ctrl Pts',(1.75896392205107,-1.70616416880753,14.2440463276315));
#4777=CARTESIAN_POINT('Ctrl Pts',(1.81562737650659,-1.64774718062538,14.2482679628004));
#4778=CARTESIAN_POINT('Ctrl Pts',(1.86933549494015,-1.58654781275061,14.2524895979694));
#4779=CARTESIAN_POINT('Ctrl Pts',(1.91981956487922,-1.52290613246745,14.2567112331384));
#4780=CARTESIAN_POINT('Ctrl Pts',(1.97099476603439,-1.45839319216223,14.2609906628523));
#4781=CARTESIAN_POINT('Ctrl Pts',(2.01885668784563,-1.39137096474464,14.2652700925662));
#4782=CARTESIAN_POINT('Ctrl Pts',(2.06317147164031,-1.32222302529095,14.2695495222801));
#4783=CARTESIAN_POINT('Ctrl Pts',(2.10748625543499,-1.25307508583727,14.273828951994));
#4784=CARTESIAN_POINT('Ctrl Pts',(2.14825371448245,-1.18180189271094,14.2781083817079));
#4785=CARTESIAN_POINT('Ctrl Pts',(2.1852896333229,-1.10880993343831,14.2823878114218));
#4786=CARTESIAN_POINT('Ctrl Pts',(2.22190384226498,-1.03664909791501,14.286618513362));
#4787=CARTESIAN_POINT('Ctrl Pts',(2.25500881229795,-0.962537041235813,14.2908492153023));
#4788=CARTESIAN_POINT('Ctrl Pts',(2.28439243138442,-0.886849180770644,14.2950799172425));
#4789=CARTESIAN_POINT('Ctrl Pts',(2.31373383429534,-0.811270062934999,14.2993045408282));
#4790=CARTESIAN_POINT('Ctrl Pts',(2.33936433793701,-0.734120067592675,14.3035291644139));
#4791=CARTESIAN_POINT('Ctrl Pts',(2.36111813725122,-0.65579828601737,14.3077537879995));
#4792=CARTESIAN_POINT('Ctrl Pts',(2.38295755521568,-0.57716824540526,14.3119950388678));
#4793=CARTESIAN_POINT('Ctrl Pts',(2.40088947279053,-0.497357598133571,14.3162362897361));
#4794=CARTESIAN_POINT('Ctrl Pts',(2.41479538533844,-0.416789511562107,14.3204775406044));
#4795=CARTESIAN_POINT('Ctrl Pts',(2.42862178352145,-0.336682115377783,14.3246945398914));
#4796=CARTESIAN_POINT('Ctrl Pts',(2.43846801344591,-0.255826381394331,14.3289115391783));
#4797=CARTESIAN_POINT('Ctrl Pts',(2.44426827401313,-0.174650664621922,14.3331285384653));
#4798=CARTESIAN_POINT('Ctrl Pts',(2.45006661166708,-0.0935018593754865,
14.3373441397247));
#4799=CARTESIAN_POINT('Ctrl Pts',(2.45182161049296,-0.0120337455097168,
14.3415597409841));
#4800=CARTESIAN_POINT('Ctrl Pts',(2.44951933141044,0.0693202354766672,14.3457753422436));
#4801=CARTESIAN_POINT('Ctrl Pts',(2.44721710977573,0.150672186471123,14.3499908383129));
#4802=CARTESIAN_POINT('Ctrl Pts',(2.44085782576217,0.231909545404855,14.3542063343822));
#4803=CARTESIAN_POINT('Ctrl Pts',(2.43047963800674,0.312600350663004,14.3584218304514));
#4804=CARTESIAN_POINT('Ctrl Pts',(2.41999147952733,0.394146182490494,14.362681995317));
#4805=CARTESIAN_POINT('Ctrl Pts',(2.40539878472013,0.475133326180942,14.3669421601826));
#4806=CARTESIAN_POINT('Ctrl Pts',(2.38679426532006,0.555124657203479,14.3712023250482));
#4807=CARTESIAN_POINT('Ctrl Pts',(2.36835800853678,0.634392532253334,14.3754239602172));
#4808=CARTESIAN_POINT('Ctrl Pts',(2.34598239116248,0.712682099636594,14.3796455953861));
#4809=CARTESIAN_POINT('Ctrl Pts',(2.31980784320882,0.789583320864148,14.3838672305551));
#4810=CARTESIAN_POINT('Ctrl Pts',(2.29327496346493,0.867537326358365,14.388146660269));
#4811=CARTESIAN_POINT('Ctrl Pts',(2.26283853301648,0.944064225087086,14.3924260899829));
#4812=CARTESIAN_POINT('Ctrl Pts',(2.22869443163873,1.01875972652167,14.3967055196968));
#4813=CARTESIAN_POINT('Ctrl Pts',(2.19455033026098,1.09345522795625,14.4009849494106));
#4814=CARTESIAN_POINT('Ctrl Pts',(2.15669884222827,1.1663189269381,14.4052643791245));
#4815=CARTESIAN_POINT('Ctrl Pts',(2.11538198855414,1.23697586577132,14.4095438088384));
#4816=CARTESIAN_POINT('Ctrl Pts',(2.07453558969008,1.30682826859122,14.4137745107787));
#4817=CARTESIAN_POINT('Ctrl Pts',(2.03014874344269,1.37478666664704,14.4180052127189));
#4818=CARTESIAN_POINT('Ctrl Pts',(1.98242224482019,1.4404694697362,14.4222359146592));
#4819=CARTESIAN_POINT('Ctrl Pts',(1.93476431604388,1.50605790471047,14.4264605382449));
#4820=CARTESIAN_POINT('Ctrl Pts',(1.88377653536069,1.56937686489836,14.4306851618305));
#4821=CARTESIAN_POINT('Ctrl Pts',(1.82970467293867,1.63007087570645,14.4349097854162));
#4822=CARTESIAN_POINT('Ctrl Pts',(1.77541999436405,1.69100376613302,14.4391510362845));
#4823=CARTESIAN_POINT('Ctrl Pts',(1.7180271448577,1.7492905906423,14.4433922871528));
#4824=CARTESIAN_POINT('Ctrl Pts',(1.65781774574636,1.80460260774732,14.4476335380211));
#4825=CARTESIAN_POINT('Ctrl Pts',(1.59795262552468,1.85959834931873,14.451850537308));
#4826=CARTESIAN_POINT('Ctrl Pts',(1.53530342442256,1.91165289343346,14.456067536595));
#4827=CARTESIAN_POINT('Ctrl Pts',(1.47019465964299,1.96047900084577,14.460284535882));
#4828=CARTESIAN_POINT('Ctrl Pts',(1.40510747984326,2.00928892133536,14.4645001371414));
#4829=CARTESIAN_POINT('Ctrl Pts',(1.33756272737892,2.05487225175629,14.4687157384008));
#4830=CARTESIAN_POINT('Ctrl Pts',(1.26791727466758,2.09698260235977,14.4729313396603));
#4831=CARTESIAN_POINT('Ctrl Pts',(1.19827355979026,2.13909190220117,14.4771468357296));
#4832=CARTESIAN_POINT('Ctrl Pts',(1.12652964741637,2.177728154827,14.4813623317989));
#4833=CARTESIAN_POINT('Ctrl Pts',(1.05306937206137,2.21268957326288,14.4855778278682));
#4834=CARTESIAN_POINT('Ctrl Pts',(0.978830687233028,2.24802145449896,14.4898379927337));
#4835=CARTESIAN_POINT('Ctrl Pts',(0.902839479066865,2.27959993556306,14.4940981575993));
#4836=CARTESIAN_POINT('Ctrl Pts',(0.825513458532294,2.3072663001444,14.4983583224649));
#4837=CARTESIAN_POINT('Ctrl Pts',(0.748886788423378,2.33468244515266,14.5025799576339));
#4838=CARTESIAN_POINT('Ctrl Pts',(0.670949821353555,2.35825687574795,14.5068015928028));
#4839=CARTESIAN_POINT('Ctrl Pts',(0.592123330739176,2.37788565982352,14.5110232279718));
#4840=CARTESIAN_POINT('Ctrl Pts',(0.512217698756271,2.39778316362446,14.5153026576857));
#4841=CARTESIAN_POINT('Ctrl Pts',(0.431398488927928,2.41362607529504,14.5195820873996));
#4842=CARTESIAN_POINT('Ctrl Pts',(0.350111663188402,2.42536019454832,14.5238615171135));
#4843=CARTESIAN_POINT('Ctrl Pts',(0.268824837448876,2.43709431380159,14.5281409468274));
#4844=CARTESIAN_POINT('Ctrl Pts',(0.187070890347798,2.44471966028567,14.5324203765413));
#4845=CARTESIAN_POINT('Ctrl Pts',(0.105296103432629,2.44823670844996,14.5366998062552));
#4846=CARTESIAN_POINT('Ctrl Pts',(0.0244524460306887,2.45171370970653,14.5409305081954));
#4847=CARTESIAN_POINT('Ctrl Pts',(-0.0567156527722998,2.45118861657421,
14.5451612101357));
#4848=CARTESIAN_POINT('Ctrl Pts',(-0.137778655346634,2.44662365151056,14.5493919120759));
#4849=CARTESIAN_POINT('Ctrl Pts',(-0.21872519269157,2.44206524504561,14.5536165356616));
#4850=CARTESIAN_POINT('Ctrl Pts',(-0.299566473305872,2.43347852000482,14.5578411592473));
#4851=CARTESIAN_POINT('Ctrl Pts',(-0.379870566370386,2.42087765134991,14.562065782833));
#4852=CARTESIAN_POINT('Ctrl Pts',(-0.460490720457274,2.40822718816901,14.5663070337013));
#4853=CARTESIAN_POINT('Ctrl Pts',(-0.540568975281024,2.39153089546031,14.5705482845696));
#4854=CARTESIAN_POINT('Ctrl Pts',(-0.61967105172237,2.37085597151267,14.5747895354379));
#4855=CARTESIAN_POINT('Ctrl Pts',(-0.698320820460222,2.35029926731085,14.5790065347248));
#4856=CARTESIAN_POINT('Ctrl Pts',(-0.776005089679829,2.3258094270183,14.5832235340118));
#4857=CARTESIAN_POINT('Ctrl Pts',(-0.85230666336635,2.29750377618434,14.5874405332987));
#4858=CARTESIAN_POINT('Ctrl Pts',(-0.928582941411809,2.26920750929294,14.5916561345582));
#4859=CARTESIAN_POINT('Ctrl Pts',(-1.00347699853749,2.23709810560857,14.5958717358176));
#4860=CARTESIAN_POINT('Ctrl Pts',(-1.07658846575391,2.20134220997228,14.600087337077));
#4861=CARTESIAN_POINT('Ctrl Pts',(-1.14969810865047,2.16558720653789,14.6043028331463));
#4862=CARTESIAN_POINT('Ctrl Pts',(-1.22102483277727,2.12618609735261,14.6085183292156));
#4863=CARTESIAN_POINT('Ctrl Pts',(-1.29019117166378,2.08335234431453,14.6127338252849));
#4864=CARTESIAN_POINT('Ctrl Pts',(-1.36009042004676,2.04006471060448,14.6169939901505));
#4865=CARTESIAN_POINT('Ctrl Pts',(-1.42778280589453,1.99327149439629,14.6212541550161));
#4866=CARTESIAN_POINT('Ctrl Pts',(-1.49290873360751,1.94323795843906,14.6255143198817));
#4867=CARTESIAN_POINT('Ctrl Pts',(-1.55744565072687,1.89365693477226,14.6297359550507));
#4868=CARTESIAN_POINT('Ctrl Pts',(-1.61946202784922,1.8408943193843,14.6339575902196));
#4869=CARTESIAN_POINT('Ctrl Pts',(-1.67864267156163,1.78524761061664,14.6381792253886));
#4870=CARTESIAN_POINT('Ctrl Pts',(-1.73863350332548,1.72883909366784,14.6424586551025));
#4871=CARTESIAN_POINT('Ctrl Pts',(-1.79571002812112,1.66946727506073,14.6467380848164));
#4872=CARTESIAN_POINT('Ctrl Pts',(-1.84958522757528,1.60747775596906,14.6510175145303));
#4873=CARTESIAN_POINT('Ctrl Pts',(-1.90346042702943,1.54548823687739,14.6552969442442));
#4874=CARTESIAN_POINT('Ctrl Pts',(-1.95413404990639,1.4808814437352,14.659576373958));
#4875=CARTESIAN_POINT('Ctrl Pts',(-2.00136487298638,1.41403284798345,14.6638558036719));
#4876=CARTESIAN_POINT('Ctrl Pts',(-2.04854588977583,1.34725474603989,14.6681307206015));
#4877=CARTESIAN_POINT('Ctrl Pts',(-2.09246741364618,1.27799073561833,14.672405637531));
#4878=CARTESIAN_POINT('Ctrl Pts',(-2.13286079451428,1.20658819869245,14.6766805544605));
#4879=CARTESIAN_POINT('Ctrl Pts',(-2.17319329701726,1.13529327518295,14.6809490285039));
#4880=CARTESIAN_POINT('Ctrl Pts',(-2.21000799855832,1.06186661759444,14.6852175025473));
#4881=CARTESIAN_POINT('Ctrl Pts',(-2.24307855145289,0.986685797005316,14.6894859765907));
#4882=CARTESIAN_POINT('Ctrl Pts',(-2.27709485655393,0.909354954093206,14.6938765205238));
#4883=CARTESIAN_POINT('Ctrl Pts',(-2.30714929978574,0.830168471242125,14.6982670644569));
#4884=CARTESIAN_POINT('Ctrl Pts',(-2.33304538151732,0.749566206402557,14.70265760839));
#4885=CARTESIAN_POINT('Ctrl Pts',(-2.35816409428244,0.671383523797928,14.7069163535191));
#4886=CARTESIAN_POINT('Ctrl Pts',(-2.37937041262091,0.591869318872894,14.7111750986483));
#4887=CARTESIAN_POINT('Ctrl Pts',(-2.39653373568161,0.511445308649865,14.7154338437774));
#4888=CARTESIAN_POINT('Ctrl Pts',(-2.41449380944567,0.427287878827075,14.7198902871125));
#4889=CARTESIAN_POINT('Ctrl Pts',(-2.4280262260801,0.342134607466912,14.7243467304476));
#4890=CARTESIAN_POINT('Ctrl Pts',(-2.4370404068577,0.256484512871338,14.7288031737827));
#4891=CARTESIAN_POINT('Ctrl Pts',(-2.4460545876353,0.170834418275776,14.7332596171178));
#4892=CARTESIAN_POINT('Ctrl Pts',(-2.45055045587725,0.0846880646948334,
14.7377160604529));
#4893=CARTESIAN_POINT('Ctrl Pts',(-2.45049957242558,-0.00144759872526646,
14.742172503788));
#4894=CARTESIAN_POINT('',(-2.45049965096235,-0.00130791185444283,15.542172503788));
#4895=CARTESIAN_POINT('Ctrl Pts',(-2.44733426487298,-0.00146391714831885,
14.7421734460211));
#4896=CARTESIAN_POINT('Ctrl Pts',(-2.44901793535173,-0.315713367656626,
14.7584528977103));
#4897=CARTESIAN_POINT('Ctrl Pts',(-2.24674592747447,-1.44605616538801,14.8171176818718));
#4898=CARTESIAN_POINT('Ctrl Pts',(-0.543033491398334,-2.8461098193418,14.9181677985054));
#4899=CARTESIAN_POINT('Ctrl Pts',(2.09888347669716,-1.99747706564621,15.0453237959221));
#4900=CARTESIAN_POINT('Ctrl Pts',(2.81575424861743,0.683194326621678,15.1724797933388));
#4901=CARTESIAN_POINT('Ctrl Pts',(0.950081937109875,2.7372560693716,15.2996357907557));
#4902=CARTESIAN_POINT('Ctrl Pts',(-1.70248634147458,2.29486366106898,15.4228663208472));
#4903=CARTESIAN_POINT('Ctrl Pts',(-2.44889900543195,0.736220053860236,15.5037115184667));
#4904=CARTESIAN_POINT('Ctrl Pts',(-2.45367050467139,-0.00128812380637844,
15.5421713836139));
#4905=CARTESIAN_POINT('',(-2.45049903536358,0.00217432338375172,16.3421725038319));
#4906=CARTESIAN_POINT('Ctrl Pts',(-2.45049965096235,-0.00130791185444283,
15.542172503788));
#4907=CARTESIAN_POINT('Ctrl Pts',(-2.45045953015348,-0.0764781366577363,
15.5460975977217));
#4908=CARTESIAN_POINT('Ctrl Pts',(-2.44696089914346,-0.151553924908697,
15.5500226916554));
#4909=CARTESIAN_POINT('Ctrl Pts',(-2.44002780973267,-0.226306291850654,
15.5539477855891));
#4910=CARTESIAN_POINT('Ctrl Pts',(-2.43255490963965,-0.306878881756149,
15.5581784875294));
#4911=CARTESIAN_POINT('Ctrl Pts',(-2.42107276369846,-0.387232452371849,
15.5624091894696));
#4912=CARTESIAN_POINT('Ctrl Pts',(-2.4056019501097,-0.466936299326177,15.5666398914099));
#4913=CARTESIAN_POINT('Ctrl Pts',(-2.39015336382314,-0.546525633783576,
15.5708645149956));
#4914=CARTESIAN_POINT('Ctrl Pts',(-2.3707275790756,-0.625466645844599,15.5750891385813));
#4915=CARTESIAN_POINT('Ctrl Pts',(-2.34739697381755,-0.703333276130331,
15.5793137621669));
#4916=CARTESIAN_POINT('Ctrl Pts',(-2.32397454391307,-0.781506374067252,
15.5835550130352));
#4917=CARTESIAN_POINT('Ctrl Pts',(-2.29661653419516,-0.858596142455209,
15.5877962639035));
#4918=CARTESIAN_POINT('Ctrl Pts',(-2.26544817731458,-0.934181356002161,
15.5920375147718));
#4919=CARTESIAN_POINT('Ctrl Pts',(-2.23445804189869,-1.00933437135788,15.5962545140588));
#4920=CARTESIAN_POINT('Ctrl Pts',(-2.19970119547367,-1.08299955708573,15.6004715133457));
#4921=CARTESIAN_POINT('Ctrl Pts',(-2.16135023161793,-1.1547793842484,15.6046885126327));
#4922=CARTESIAN_POINT('Ctrl Pts',(-2.12301198194574,-1.226535414828,15.6089041138921));
#4923=CARTESIAN_POINT('Ctrl Pts',(-2.08108219999881,-1.29640691820099,15.6131197151515));
#4924=CARTESIAN_POINT('Ctrl Pts',(-2.03578007430045,-1.36401969893446,15.617335316411));
#4925=CARTESIAN_POINT('Ctrl Pts',(-1.99047907900709,-1.43163079255447,15.6215508124803));
#4926=CARTESIAN_POINT('Ctrl Pts',(-1.94180616703827,-1.49698288984425,15.6257663085496));
#4927=CARTESIAN_POINT('Ctrl Pts',(-1.89002382204775,-1.55973081077858,15.6299818046189));
#4928=CARTESIAN_POINT('Ctrl Pts',(-1.83769277413322,-1.6231436295212,15.6342419694845));
#4929=CARTESIAN_POINT('Ctrl Pts',(-1.78218629959459,-1.68389636994626,15.63850213435));
#4930=CARTESIAN_POINT('Ctrl Pts',(-1.72381579488247,-1.74166855495347,15.6427622992156));
#4931=CARTESIAN_POINT('Ctrl Pts',(-1.66597320350443,-1.79891823793754,15.6469839343846));
#4932=CARTESIAN_POINT('Ctrl Pts',(-1.605318570642,-1.85324079426793,15.6512055695535));
#4933=CARTESIAN_POINT('Ctrl Pts',(-1.54218923643854,-1.90436409570573,15.6554272047225));
#4934=CARTESIAN_POINT('Ctrl Pts',(-1.47819565627453,-1.95618727949325,15.6597066344364));
#4935=CARTESIAN_POINT('Ctrl Pts',(-1.41165950361692,-2.00472265748693,15.6639860641503));
#4936=CARTESIAN_POINT('Ctrl Pts',(-1.34296197567411,-2.04973251471832,15.6682654938642));
#4937=CARTESIAN_POINT('Ctrl Pts',(-1.27426444773129,-2.09474237194971,15.6725449235781));
#4938=CARTESIAN_POINT('Ctrl Pts',(-1.20340600096031,-2.13622651707527,15.6768243532919));
#4939=CARTESIAN_POINT('Ctrl Pts',(-1.13079124448469,-2.17399664475288,15.6811037830058));
#4940=CARTESIAN_POINT('Ctrl Pts',(-1.05900331673451,-2.21133670245514,15.6853344849461));
#4941=CARTESIAN_POINT('Ctrl Pts',(-0.985228877902366,-2.24518737691081,
15.6895651868863));
#4942=CARTESIAN_POINT('Ctrl Pts',(-0.909841187210448,-2.27533278094776,
15.6937958888266));
#4943=CARTESIAN_POINT('Ctrl Pts',(-0.834561807886533,-2.30543487433386,
15.6980205124123));
#4944=CARTESIAN_POINT('Ctrl Pts',(-0.757674208132242,-2.33184209876761,
15.7022451359979));
#4945=CARTESIAN_POINT('Ctrl Pts',(-0.679575786855455,-2.35438463296034,
15.7064697595836));
#4946=CARTESIAN_POINT('Ctrl Pts',(-0.601169985643965,-2.3770158901077,15.7107110104519));
#4947=CARTESIAN_POINT('Ctrl Pts',(-0.521544232367028,-2.39575175146806,
15.7149522613202));
#4948=CARTESIAN_POINT('Ctrl Pts',(-0.441120477798487,-2.4104694509715,15.7191935121885));
#4949=CARTESIAN_POINT('Ctrl Pts',(-0.361156588322953,-2.42510299429139,
15.7234105114754));
#4950=CARTESIAN_POINT('Ctrl Pts',(-0.280404260837503,-2.43576411840727,
15.7276275107624));
#4951=CARTESIAN_POINT('Ctrl Pts',(-0.199291164994801,-2.44238270579265,
15.7318445100494));
#4952=CARTESIAN_POINT('Ctrl Pts',(-0.1182049599179,-2.44899909897151,15.7360601113088));
#4953=CARTESIAN_POINT('Ctrl Pts',(-0.0367586871468292,-2.45157557901659,
15.7402757125682));
#4954=CARTESIAN_POINT('Ctrl Pts',(0.0446143744299721,-2.45009383648754,
15.7444913138277));
#4955=CARTESIAN_POINT('Ctrl Pts',(0.125985405538724,-2.44861213093179,15.748706809897));
#4956=CARTESIAN_POINT('Ctrl Pts',(0.207282764121698,-2.44307241368985,15.7529223059663));
#4957=CARTESIAN_POINT('Ctrl Pts',(0.28807412571626,-2.4335084853135,15.7571378020355));
#4958=CARTESIAN_POINT('Ctrl Pts',(0.36972157940851,-2.42384321437596,15.7613979669011));
#4959=CARTESIAN_POINT('Ctrl Pts',(0.450851765835281,-2.41006798170178,15.7656581317667));
#4960=CARTESIAN_POINT('Ctrl Pts',(0.531026647736233,-2.39227108610082,15.7699182966323));
#4961=CARTESIAN_POINT('Ctrl Pts',(0.610476413597396,-2.37463514882189,15.7741399318013));
#4962=CARTESIAN_POINT('Ctrl Pts',(0.688987648276002,-2.35305018546353,15.7783615669702));
#4963=CARTESIAN_POINT('Ctrl Pts',(0.766148917958076,-2.32765248383681,15.7825832021392));
#4964=CARTESIAN_POINT('Ctrl Pts',(0.844366531992265,-2.30190708551224,15.7868626318531));
#4965=CARTESIAN_POINT('Ctrl Pts',(0.921196477439546,-2.27224394323022,15.791142061567));
#4966=CARTESIAN_POINT('Ctrl Pts',(0.996232508967404,-2.23885484971146,15.7954214912809));
#4967=CARTESIAN_POINT('Ctrl Pts',(1.07126854049527,-2.20546575619269,15.7997009209948));
#4968=CARTESIAN_POINT('Ctrl Pts',(1.14451025009894,-2.1683509916112,15.8039803507086));
#4969=CARTESIAN_POINT('Ctrl Pts',(1.21558025847274,-2.12774878338853,15.8082597804225));
#4970=CARTESIAN_POINT('Ctrl Pts',(1.28584102741231,-2.08760889265761,15.8124904823628));
#4971=CARTESIAN_POINT('Ctrl Pts',(1.35424359176949,-2.04390963436344,15.816721184303));
#4972=CARTESIAN_POINT('Ctrl Pts',(1.42040435581549,-1.99684794513263,15.8209518862433));
#4973=CARTESIAN_POINT('Ctrl Pts',(1.48647006504817,-1.94985387059987,15.825176509829));
#4974=CARTESIAN_POINT('Ctrl Pts',(1.5502999950053,-1.89950722681971,15.8294011334147));
#4975=CARTESIAN_POINT('Ctrl Pts',(1.61153621068436,-1.84605018665612,15.8336257570003));
#4976=CARTESIAN_POINT('Ctrl Pts',(1.67301343999307,-1.79238275015864,15.8378670078686));
#4977=CARTESIAN_POINT('Ctrl Pts',(1.73187608248903,-1.73558061635869,15.8421082587369));
#4978=CARTESIAN_POINT('Ctrl Pts',(1.78779247252783,-1.67593207653915,15.8463495096052));
#4979=CARTESIAN_POINT('Ctrl Pts',(1.84338913121305,-1.61662460860143,15.8505665088921));
#4980=CARTESIAN_POINT('Ctrl Pts',(1.89607281824666,-1.55450354065931,15.8547835081791));
#4981=CARTESIAN_POINT('Ctrl Pts',(1.94555303637445,-1.48989047673115,15.859000507466));
#4982=CARTESIAN_POINT('Ctrl Pts',(1.99501685072745,-1.42529883344721,15.8632161087255));
#4983=CARTESIAN_POINT('Ctrl Pts',(2.04127902263602,-1.35821720371133,15.8674317099849));
#4984=CARTESIAN_POINT('Ctrl Pts',(2.08408957597741,-1.28899995706062,15.8716473112444));
#4985=CARTESIAN_POINT('Ctrl Pts',(2.12689906108494,-1.21978443755897,15.8758628073137));
#4986=CARTESIAN_POINT('Ctrl Pts',(2.16625685516059,-1.14843380318765,15.8800783033829));
#4987=CARTESIAN_POINT('Ctrl Pts',(2.20195731068694,-1.07532983401017,15.8842937994522));
#4988=CARTESIAN_POINT('Ctrl Pts',(2.23803606009593,-1.00145123089796,15.8885539643178));
#4989=CARTESIAN_POINT('Ctrl Pts',(2.27037927363017,-0.925782342157913,15.8928141291834));
#4990=CARTESIAN_POINT('Ctrl Pts',(2.29882403061643,-0.848739256933737,15.897074294049));
#4991=CARTESIAN_POINT('Ctrl Pts',(2.3270115281088,-0.772392963217447,15.901295929218));
#4992=CARTESIAN_POINT('Ctrl Pts',(2.35137072031579,-0.694697697152131,15.9055175643869));
#4993=CARTESIAN_POINT('Ctrl Pts',(2.37179343709891,-0.616073162647547,15.9097391995559));
#4994=CARTESIAN_POINT('Ctrl Pts',(2.39249574261377,-0.536372251570763,15.9140186292698));
#4995=CARTESIAN_POINT('Ctrl Pts',(2.40915287521122,-0.455716920307952,15.9182980589837));
#4996=CARTESIAN_POINT('Ctrl Pts',(2.42170614002846,-0.374552561529669,15.9225774886976));
#4997=CARTESIAN_POINT('Ctrl Pts',(2.43425940484571,-0.293388202751386,15.9268569184115));
#4998=CARTESIAN_POINT('Ctrl Pts',(2.44270881654254,-0.211715311180257,15.9311363481254));
#4999=CARTESIAN_POINT('Ctrl Pts',(2.44705034898912,-0.129980150454718,15.9354157778393));
#5000=CARTESIAN_POINT('Ctrl Pts',(2.45134244652861,-0.0491756680383044,
15.9396464797795));
#5001=CARTESIAN_POINT('Ctrl Pts',(2.45163592503804,0.0319935986607728,15.9438771817198));
#5002=CARTESIAN_POINT('Ctrl Pts',(2.44788867719599,0.113098514825096,15.94810788366));
#5003=CARTESIAN_POINT('Ctrl Pts',(2.44414681311801,0.194086905541516,15.9523325072457));
#5004=CARTESIAN_POINT('Ctrl Pts',(2.43637577383797,0.275010668718802,15.9565571308314));
#5005=CARTESIAN_POINT('Ctrl Pts',(2.42458537776252,0.355437752553385,15.9607817544171));
#5006=CARTESIAN_POINT('Ctrl Pts',(2.41274857702078,0.436181381477818,15.9650230052854));
#5007=CARTESIAN_POINT('Ctrl Pts',(2.39686068766559,0.516423939124441,15.9692642561537));
#5008=CARTESIAN_POINT('Ctrl Pts',(2.3769845250529,0.595730490791806,15.9735055070219));
#5009=CARTESIAN_POINT('Ctrl Pts',(2.35722201484823,0.674583565561007,15.9777225063089));
#5010=CARTESIAN_POINT('Ctrl Pts',(2.33351683191251,0.752510853873331,15.9819395055959));
#5011=CARTESIAN_POINT('Ctrl Pts',(2.30598208858882,0.829093997751474,15.9861565048828));
#5012=CARTESIAN_POINT('Ctrl Pts',(2.27845647363493,0.905651752642007,15.9903721061423));
#5013=CARTESIAN_POINT('Ctrl Pts',(2.24710397669182,0.980865810723941,15.9945877074017));
#5014=CARTESIAN_POINT('Ctrl Pts',(2.21208719657955,1.05433414282609,15.9988033086611));
#5015=CARTESIAN_POINT('Ctrl Pts',(2.17707129022638,1.12780064170363,16.0030188047304));
#5016=CARTESIAN_POINT('Ctrl Pts',(2.13839148356906,1.19952108186293,16.0072343007997));
#5017=CARTESIAN_POINT('Ctrl Pts',(2.096257421066,1.26911586335753,16.011449796869));
#5018=CARTESIAN_POINT('Ctrl Pts',(2.05367689204424,1.33944809426877,16.0157099617346));
#5019=CARTESIAN_POINT('Ctrl Pts',(2.00756870353708,1.40760892713825,16.0199701266002));
#5020=CARTESIAN_POINT('Ctrl Pts',(1.95819447843981,1.4732361095927,16.0242302914658));
#5021=CARTESIAN_POINT('Ctrl Pts',(1.90926680270716,1.53826974801543,16.0284519266347));
#5022=CARTESIAN_POINT('Ctrl Pts',(1.85713227849037,1.60081505957935,16.0326735618037));
#5023=CARTESIAN_POINT('Ctrl Pts',(1.8020852104146,1.66055386675801,16.0368951969727));
#5024=CARTESIAN_POINT('Ctrl Pts',(1.74628454328966,1.72111050329365,16.0411746266866));
#5025=CARTESIAN_POINT('Ctrl Pts',(1.68749133567476,1.77878286466226,16.0454540564005));
#5026=CARTESIAN_POINT('Ctrl Pts',(1.62604827671431,1.83328046184822,16.0497334861144));
#5027=CARTESIAN_POINT('Ctrl Pts',(1.56460521775387,1.88777805903417,16.0540129158283));
#5028=CARTESIAN_POINT('Ctrl Pts',(1.50051273132664,1.93910063651412,16.0582923455422));
#5029=CARTESIAN_POINT('Ctrl Pts',(1.4341438371495,1.98700319686862,16.062571775256));
#5030=CARTESIAN_POINT('Ctrl Pts',(1.36853065311792,2.0343603141913,16.0668024771963));
#5031=CARTESIAN_POINT('Ctrl Pts',(1.30044587424408,2.07855306101479,16.0710331791366));
#5032=CARTESIAN_POINT('Ctrl Pts',(1.23022750145147,2.11931369661796,16.0752638810768));
#5033=CARTESIAN_POINT('Ctrl Pts',(1.16011001313948,2.16001577040334,16.0794885046625));
#5034=CARTESIAN_POINT('Ctrl Pts',(1.08786541773138,2.19729529471072,16.0837131282482));
#5035=CARTESIAN_POINT('Ctrl Pts',(1.01386228183302,2.23092660647462,16.0879377518338));
#5036=CARTESIAN_POINT('Ctrl Pts',(0.939567884232938,2.26469028442781,16.0921790027021));
#5037=CARTESIAN_POINT('Ctrl Pts',(0.863501458712895,2.29477669322709,16.0964202535704));
#5038=CARTESIAN_POINT('Ctrl Pts',(0.786062688873,2.32100316655574,16.1006615044387));
#5039=CARTESIAN_POINT('Ctrl Pts',(0.709066715906823,2.34707967623668,16.1048785037257));
#5040=CARTESIAN_POINT('Ctrl Pts',(0.630714495145698,2.36934012240313,16.1090955030126));
#5041=CARTESIAN_POINT('Ctrl Pts',(0.551419004568888,2.38765310114352,16.1133125022996));
#5042=CARTESIAN_POINT('Ctrl Pts',(0.472149802181945,2.40596000873082,16.117528103559));
#5043=CARTESIAN_POINT('Ctrl Pts',(0.391938403751546,2.42032194312575,16.1217437048184));
#5044=CARTESIAN_POINT('Ctrl Pts',(0.311210851255252,2.43065794715361,16.1259593060779));
#5045=CARTESIAN_POINT('Ctrl Pts',(0.230485313119831,2.44099369327148,16.1301748021472));
#5046=CARTESIAN_POINT('Ctrl Pts',(0.14924410795852,2.44730365077037,16.1343902982165));
#5047=CARTESIAN_POINT('Ctrl Pts',(0.067919891275365,2.44955855989791,16.1386057942858));
#5048=CARTESIAN_POINT('Ctrl Pts',(-0.01426606381486,2.45183736279141,16.1428659591514));
#5049=CARTESIAN_POINT('Ctrl Pts',(-0.0965363163016381,2.44997463881073,
16.1471261240169));
#5050=CARTESIAN_POINT('Ctrl Pts',(-0.178444654042102,2.44399422164697,16.1513862888825));
#5051=CARTESIAN_POINT('Ctrl Pts',(-0.259612198056688,2.43806789245076,16.1556079240515));
#5052=CARTESIAN_POINT('Ctrl Pts',(-0.340423888304079,2.42809817162709,16.1598295592204));
#5053=CARTESIAN_POINT('Ctrl Pts',(-0.420452874624735,2.41416023292154,16.1640511943894));
#5054=CARTESIAN_POINT('Ctrl Pts',(-0.501577464582437,2.40003148264833,16.1683306241033));
#5055=CARTESIAN_POINT('Ctrl Pts',(-0.581897275367252,2.38182515070137,16.1726100538172));
#5056=CARTESIAN_POINT('Ctrl Pts',(-0.660982540191496,2.35967208136258,16.1768894835311));
#5057=CARTESIAN_POINT('Ctrl Pts',(-0.740067805015739,2.33751901202378,16.181168913245));
#5058=CARTESIAN_POINT('Ctrl Pts',(-0.817918079553251,2.31141942332903,16.1854483429589));
#5059=CARTESIAN_POINT('Ctrl Pts',(-0.894125423086832,2.28155428990629,16.1897277726728));
#5060=CARTESIAN_POINT('Ctrl Pts',(-0.969465030862757,2.25202921615465,16.193958474613));
#5061=CARTESIAN_POINT('Ctrl Pts',(-1.04348232106309,2.2187129027707,16.1981891765533));
#5062=CARTESIAN_POINT('Ctrl Pts',(-1.11576919095822,2.18174456857544,16.2024198784935));
#5063=CARTESIAN_POINT('Ctrl Pts',(-1.18795220451158,2.14482934770431,16.2066445020792));
#5064=CARTESIAN_POINT('Ctrl Pts',(-1.2584093248239,2.10427273670739,16.2108691256649));
#5065=CARTESIAN_POINT('Ctrl Pts',(-1.32675127764859,2.06026243407432,16.2150937492506));
#5066=CARTESIAN_POINT('Ctrl Pts',(-1.39536221087849,2.0160789155973,16.2193350001188));
#5067=CARTESIAN_POINT('Ctrl Pts',(-1.46184084931117,1.96841463423303,16.2235762509871));
#5068=CARTESIAN_POINT('Ctrl Pts',(-1.52581722143071,1.91750672926732,16.2278175018554));
#5069=CARTESIAN_POINT('Ctrl Pts',(-1.58942777501225,1.86688991700897,16.2320345011424));
#5070=CARTESIAN_POINT('Ctrl Pts',(-1.65056423310857,1.81306676722036,16.2362515004293));
#5071=CARTESIAN_POINT('Ctrl Pts',(-1.70889252572214,1.75631335061002,16.2404684997163));
#5072=CARTESIAN_POINT('Ctrl Pts',(-1.76720148123065,1.6995787489989,16.2446841009757));
#5073=CARTESIAN_POINT('Ctrl Pts',(-1.82270378694915,1.63991613375578,16.2488997022352));
#5074=CARTESIAN_POINT('Ctrl Pts',(-1.87510071335025,1.577639871705,16.2531153034946));
#5075=CARTESIAN_POINT('Ctrl Pts',(-1.92749633231272,1.51536516360779,16.2573307995639));
#5076=CARTESIAN_POINT('Ctrl Pts',(-1.97678642744433,1.45047729492956,16.2615462956332));
#5077=CARTESIAN_POINT('Ctrl Pts',(-2.02271215357283,1.38332418246366,16.2657617917025));
#5078=CARTESIAN_POINT('Ctrl Pts',(-2.06912452394702,1.31545949331697,16.2700219565681));
#5079=CARTESIAN_POINT('Ctrl Pts',(-2.11210051405406,1.24528165878786,16.2742821214337));
#5080=CARTESIAN_POINT('Ctrl Pts',(-2.15141857770886,1.17317873893502,16.2785422862993));
#5081=CARTESIAN_POINT('Ctrl Pts',(-2.19038104173026,1.1017279308467,16.2827639214682));
#5082=CARTESIAN_POINT('Ctrl Pts',(-2.22575133037719,1.02838716936328,16.2869855566372));
#5083=CARTESIAN_POINT('Ctrl Pts',(-2.25736154480874,0.95355603192402,16.2912071918062));
#5084=CARTESIAN_POINT('Ctrl Pts',(-2.28940450576747,0.877700449841354,16.29548662152));
#5085=CARTESIAN_POINT('Ctrl Pts',(-2.31758349228026,0.800313840879615,16.2997660512339));
#5086=CARTESIAN_POINT('Ctrl Pts',(-2.34177583183142,0.721828375342958,16.3040454809478));
#5087=CARTESIAN_POINT('Ctrl Pts',(-2.36596817138258,0.643342909806301,16.3083249106617));
#5088=CARTESIAN_POINT('Ctrl Pts',(-2.38617380672396,0.563759079312502,16.3126043403756));
#5089=CARTESIAN_POINT('Ctrl Pts',(-2.40232402969856,0.483517844895977,16.3168837700895));
#5090=CARTESIAN_POINT('Ctrl Pts',(-2.42528233781664,0.36945112356297,16.3229671824421));
#5091=CARTESIAN_POINT('Ctrl Pts',(-2.44012249745587,0.253699812650627,16.3290505947948));
#5092=CARTESIAN_POINT('Ctrl Pts',(-2.44665526989177,0.137216035181218,16.3351340071474));
#5093=CARTESIAN_POINT('Ctrl Pts',(-2.44917473836213,0.0922921980931879,
16.3374801726943));
#5094=CARTESIAN_POINT('Ctrl Pts',(-2.45045903119538,0.0472596765101275,
16.3398263382411));
#5095=CARTESIAN_POINT('Ctrl Pts',(-2.45049903536283,0.00217432422689355,
16.342172503788));
#5096=CARTESIAN_POINT('',(-2.45049999653667,0.000130283472662122,17.1421725037616));
#5097=CARTESIAN_POINT('Ctrl Pts',(-2.45049903536358,0.00217432338375008,
16.3421725038319));
#5098=CARTESIAN_POINT('Ctrl Pts',(-2.45057140723682,-0.079389995380578,
16.3464169731516));
#5099=CARTESIAN_POINT('Ctrl Pts',(-2.4465669366815,-0.161087169591855,16.3506614424714));
#5100=CARTESIAN_POINT('Ctrl Pts',(-2.43847466509943,-0.242469704640073,
16.3549059117912));
#5101=CARTESIAN_POINT('Ctrl Pts',(-2.43054759010119,-0.322190887046028,
16.359063734015));
#5102=CARTESIAN_POINT('Ctrl Pts',(-2.41869807736869,-0.40160965200395,16.3632215562389));
#5103=CARTESIAN_POINT('Ctrl Pts',(-2.40296835781613,-0.480305445872146,
16.3673793784627));
#5104=CARTESIAN_POINT('Ctrl Pts',(-2.38724644125933,-0.558962201349099,
16.3715351381279));
#5105=CARTESIAN_POINT('Ctrl Pts',(-2.36764823010998,-0.636896227556718,
16.3756908977931));
#5106=CARTESIAN_POINT('Ctrl Pts',(-2.3442674440548,-0.713694893315605,16.3798466574583));
#5107=CARTESIAN_POINT('Ctrl Pts',(-2.32089060445962,-0.790480596171468,
16.3840017156698));
#5108=CARTESIAN_POINT('Ctrl Pts',(-2.29373259783578,-0.866130860355851,
16.3881567738813));
#5109=CARTESIAN_POINT('Ctrl Pts',(-2.26293718669726,-0.940247594552993,
16.3923118320928));
#5110=CARTESIAN_POINT('Ctrl Pts',(-2.23098851599837,-1.01713993164474,16.3966224933773));
#5111=CARTESIAN_POINT('Ctrl Pts',(-2.19512480414509,-1.09238108773953,16.4009331546617));
#5112=CARTESIAN_POINT('Ctrl Pts',(-2.15556071890026,-1.16555061543211,16.4052438159462));
#5113=CARTESIAN_POINT('Ctrl Pts',(-2.11737709415858,-1.23616712964319,16.4094040706786));
#5114=CARTESIAN_POINT('Ctrl Pts',(-2.07574736520893,-1.3048538028626,16.413564325411));
#5115=CARTESIAN_POINT('Ctrl Pts',(-2.03090962191084,-1.37126086417937,16.4177245801435));
#5116=CARTESIAN_POINT('Ctrl Pts',(-1.98604163029081,-1.4377127248554,16.4218876414561));
#5117=CARTESIAN_POINT('Ctrl Pts',(-1.93796161023166,-1.50188153438697,16.4260507027688));
#5118=CARTESIAN_POINT('Ctrl Pts',(-1.88694812386883,-1.56345035988607,16.4302137640815));
#5119=CARTESIAN_POINT('Ctrl Pts',(-1.83585604644397,-1.6251140379375,16.4343832389807));
#5120=CARTESIAN_POINT('Ctrl Pts',(-1.78182181869666,-1.68416939772259,16.4385527138799));
#5121=CARTESIAN_POINT('Ctrl Pts',(-1.72516030602611,-1.7403367974366,16.4427221887792));
#5122=CARTESIAN_POINT('Ctrl Pts',(-1.71919184832307,-1.7462532076008,16.4431613816882));
#5123=CARTESIAN_POINT('Ctrl Pts',(-1.7131942684475,-1.75213761220032,16.4436005745972));
#5124=CARTESIAN_POINT('Ctrl Pts',(-1.70716795431106,-1.75798971150954,16.4440397675063));
#5125=CARTESIAN_POINT('Ctrl Pts',(-1.64911706508823,-1.8143624064984,16.4482704694465));
#5126=CARTESIAN_POINT('Ctrl Pts',(-1.58816176517468,-1.86796266208124,16.4525011713868));
#5127=CARTESIAN_POINT('Ctrl Pts',(-1.52459764933984,-1.91847654601963,16.456731873327));
#5128=CARTESIAN_POINT('Ctrl Pts',(-1.46112485764922,-1.96891785540615,16.4609564969127));
#5129=CARTESIAN_POINT('Ctrl Pts',(-1.3950510550735,-2.01628131296009,16.4651811204984));
#5130=CARTESIAN_POINT('Ctrl Pts',(-1.32670818167509,-2.06029018603603,16.4694057440841));
#5131=CARTESIAN_POINT('Ctrl Pts',(-1.25809632424838,-2.10447226932939,16.4736469949524));
#5132=CARTESIAN_POINT('Ctrl Pts',(-1.18719783690718,-2.14527297494293,16.4778882458206));
#5133=CARTESIAN_POINT('Ctrl Pts',(-1.11438168379159,-2.18245359923867,16.4821294966889));
#5134=CARTESIAN_POINT('Ctrl Pts',(-1.0419818953087,-2.21942162377026,16.4863464959759));
#5135=CARTESIAN_POINT('Ctrl Pts',(-0.967686730419196,-2.25281064046376,
16.4905634952628));
#5136=CARTESIAN_POINT('Ctrl Pts',(-0.891885742000532,-2.28243073787928,
16.4947804945498));
#5137=CARTESIAN_POINT('Ctrl Pts',(-0.816109883267823,-2.31204101558451,
16.4989960958092));
#5138=CARTESIAN_POINT('Ctrl Pts',(-0.7388296251798,-2.33788468613573,16.5032116970686));
#5139=CARTESIAN_POINT('Ctrl Pts',(-0.660454763104563,-2.3598198566612,16.5074272983281));
#5140=CARTESIAN_POINT('Ctrl Pts',(-0.582081856684622,-2.3817544798475,16.5116427943974));
#5141=CARTESIAN_POINT('Ctrl Pts',(-0.502614848726326,-2.39978067261866,
16.5158582904666));
#5142=CARTESIAN_POINT('Ctrl Pts',(-0.422477576217387,-2.41380673368716,
16.5200737865359));
#5143=CARTESIAN_POINT('Ctrl Pts',(-0.341491142555745,-2.42798141955673,
16.5243339514015));
#5144=CARTESIAN_POINT('Ctrl Pts',(-0.259820629509927,-2.43807059611939,
16.5285941162671));
#5145=CARTESIAN_POINT('Ctrl Pts',(-0.177910987859338,-2.44403312792583,
16.5328542811327));
#5146=CARTESIAN_POINT('Ctrl Pts',(-0.0967421517275273,-2.44994173352311,
16.5370759163016));
#5147=CARTESIAN_POINT('Ctrl Pts',(-0.0153389665501788,-2.45179808934016,
16.5412975514706));
#5148=CARTESIAN_POINT('Ctrl Pts',(0.065865327957158,-2.44961466532455,16.5455191866396));
#5149=CARTESIAN_POINT('Ctrl Pts',(0.148181316170854,-2.44740135004825,16.5497986163535));
#5150=CARTESIAN_POINT('Ctrl Pts',(0.230292433647624,-2.4410368458092,16.5540780460674));
#5151=CARTESIAN_POINT('Ctrl Pts',(0.311754480613395,-2.43058828142848,16.5583574757813));
#5152=CARTESIAN_POINT('Ctrl Pts',(0.393216527579153,-2.42013971704777,16.5626369054952));
#5153=CARTESIAN_POINT('Ctrl Pts',(0.474029032782728,-2.40560724381223,16.5669163352091));
#5154=CARTESIAN_POINT('Ctrl Pts',(0.553762120998581,-2.38711075640557,16.571195764923));
#5155=CARTESIAN_POINT('Ctrl Pts',(0.63258732752593,-2.36882487945679,16.5754264668632));
#5156=CARTESIAN_POINT('Ctrl Pts',(0.710654067120473,-2.34659606583185,16.5796571688035));
#5157=CARTESIAN_POINT('Ctrl Pts',(0.787538360381103,-2.32050287242404,16.5838878707437));
#5158=CARTESIAN_POINT('Ctrl Pts',(0.864312192067739,-2.29444716775538,16.5881124943294));
#5159=CARTESIAN_POINT('Ctrl Pts',(0.939906514777329,-2.26453825817382,16.5923371179151));
#5160=CARTESIAN_POINT('Ctrl Pts',(1.01390894717427,-2.23090539845148,16.5965617415008));
#5161=CARTESIAN_POINT('Ctrl Pts',(1.08820263850401,-2.19714016644742,16.6008029923691));
#5162=CARTESIAN_POINT('Ctrl Pts',(1.16089141963541,-2.15962171520719,16.6050442432373));
#5163=CARTESIAN_POINT('Ctrl Pts',(1.2315748371327,-2.11853101712992,16.6092854941056));
#5164=CARTESIAN_POINT('Ctrl Pts',(1.30185408503437,-2.07767527671902,16.6135024933926));
#5165=CARTESIAN_POINT('Ctrl Pts',(1.37015043441123,-2.0332882670932,16.6177194926796));
#5166=CARTESIAN_POINT('Ctrl Pts',(1.4360933072488,-1.98559468746147,16.6219364919665));
#5167=CARTESIAN_POINT('Ctrl Pts',(1.50201431858144,-1.93791691929474,16.626152093226));
#5168=CARTESIAN_POINT('Ctrl Pts',(1.56558302624584,-1.88693503031828,16.6303676944854));
#5169=CARTESIAN_POINT('Ctrl Pts',(1.62645826467569,-1.83291673658902,16.6345832957448));
#5170=CARTESIAN_POINT('Ctrl Pts',(1.6873319841111,-1.77889979075573,16.6387987918141));
#5171=CARTESIAN_POINT('Ctrl Pts',(1.74551202080585,-1.72184690029531,16.6430142878834));
#5172=CARTESIAN_POINT('Ctrl Pts',(1.80069180584647,-1.66206476118032,16.6472297839527));
#5173=CARTESIAN_POINT('Ctrl Pts',(1.85645629421417,-1.60164915066606,16.6514899488183));
#5174=CARTESIAN_POINT('Ctrl Pts',(1.90915622857922,-1.53844645212566,16.6557501136839));
#5175=CARTESIAN_POINT('Ctrl Pts',(1.95851612238009,-1.47280849005471,16.6600102785495));
#5176=CARTESIAN_POINT('Ctrl Pts',(2.00742959643125,-1.40776416950815,16.6642319137185));
#5177=CARTESIAN_POINT('Ctrl Pts',(2.05306299034396,-1.34032888220273,16.6684535488874));
#5178=CARTESIAN_POINT('Ctrl Pts',(2.0951922272061,-1.2708736290659,16.6726751840564));
#5179=CARTESIAN_POINT('Ctrl Pts',(2.13789821690804,-1.20046752759977,16.6769546137703));
#5180=CARTESIAN_POINT('Ctrl Pts',(2.17700314381611,-1.12798616986567,16.6812340434842));
#5181=CARTESIAN_POINT('Ctrl Pts',(2.21232295197177,-1.05383936450435,16.6855134731981));
#5182=CARTESIAN_POINT('Ctrl Pts',(2.24764276012743,-0.979692559143013,16.689792902912));
#5183=CARTESIAN_POINT('Ctrl Pts',(2.27917732158527,-0.903880784270916,16.6940723326259));
#5184=CARTESIAN_POINT('Ctrl Pts',(2.30679469916295,-0.82683037311997,16.6983517623398));
#5185=CARTESIAN_POINT('Ctrl Pts',(2.33409761116627,-0.750657297325339,16.70258246428));
#5186=CARTESIAN_POINT('Ctrl Pts',(2.35767482651374,-0.672987155684143,16.7068131662203));
#5187=CARTESIAN_POINT('Ctrl Pts',(2.37736284503395,-0.594218943700109,16.7110438681605));
#5188=CARTESIAN_POINT('Ctrl Pts',(2.39702257728888,-0.515563899962941,16.7152684917462));
#5189=CARTESIAN_POINT('Ctrl Pts',(2.41280409839237,-0.435814366485038,16.7194931153319));
#5190=CARTESIAN_POINT('Ctrl Pts',(2.42459281212612,-0.355387036041509,16.7237177389176));
#5191=CARTESIAN_POINT('Ctrl Pts',(2.43642792390476,-0.274643159537652,16.7279589897859));
#5192=CARTESIAN_POINT('Ctrl Pts',(2.44423857098117,-0.193216586000028,16.7322002406541));
#5193=CARTESIAN_POINT('Ctrl Pts',(2.44796009702729,-0.11154198026814,16.7364414915224));
#5194=CARTESIAN_POINT('Ctrl Pts',(2.45166034329195,-0.0303343920283068,
16.7406584908094));
#5195=CARTESIAN_POINT('Ctrl Pts',(2.45131808364671,0.0511179303453776,16.7448754900963));
#5196=CARTESIAN_POINT('Ctrl Pts',(2.44692160031486,0.13238176578573,16.7490924893833));
#5197=CARTESIAN_POINT('Ctrl Pts',(2.44252657451343,0.213618660486784,16.7533080906427));
#5198=CARTESIAN_POINT('Ctrl Pts',(2.4340800192118,0.294666728330832,16.7575236919022));
#5199=CARTESIAN_POINT('Ctrl Pts',(2.42162230761968,0.375094187156699,16.7617392931616));
#5200=CARTESIAN_POINT('Ctrl Pts',(2.40916490687963,0.455519639109805,16.7659547892309));
#5201=CARTESIAN_POINT('Ctrl Pts',(2.39269662110847,0.535324053420373,16.7701702853002));
#5202=CARTESIAN_POINT('Ctrl Pts',(2.37230932721088,0.614083631135268,16.7743857813695));
#5203=CARTESIAN_POINT('Ctrl Pts',(2.35170600277669,0.693677771491064,16.7786459462351));
#5204=CARTESIAN_POINT('Ctrl Pts',(2.32710022727606,0.772204327488877,16.7829061111006));
#5205=CARTESIAN_POINT('Ctrl Pts',(2.29863864811251,0.849241199779836,16.7871662759662));
#5206=CARTESIAN_POINT('Ctrl Pts',(2.27043448058559,0.925581336753914,16.7913879111352));
#5207=CARTESIAN_POINT('Ctrl Pts',(2.23844421552458,1.0004582194032,16.7956095463041));
#5208=CARTESIAN_POINT('Ctrl Pts',(2.20285845685558,1.07348258908092,16.7998311814731));
#5209=CARTESIAN_POINT('Ctrl Pts',(2.16678552612036,1.14750666859735,16.804110611187));
#5210=CARTESIAN_POINT('Ctrl Pts',(2.12701815000923,1.21962669580686,16.8083900409009));
#5211=CARTESIAN_POINT('Ctrl Pts',(2.08380122814352,1.28946604902478,16.8126694706148));
#5212=CARTESIAN_POINT('Ctrl Pts',(2.04058430627781,1.35930540224269,16.8169489003287));
#5213=CARTESIAN_POINT('Ctrl Pts',(1.99391817136637,1.42686371504001,16.8212283300425));
#5214=CARTESIAN_POINT('Ctrl Pts',(1.94408983392776,1.49179923837584,16.8255077597564));
#5215=CARTESIAN_POINT('Ctrl Pts',(1.89482886740289,1.55599537265911,16.8297384616967));
#5216=CARTESIAN_POINT('Ctrl Pts',(1.84229209519928,1.61786962863473,16.8339691636369));
#5217=CARTESIAN_POINT('Ctrl Pts',(1.78672645485866,1.67706852141116,16.8381998655772));
#5218=CARTESIAN_POINT('Ctrl Pts',(1.73124064705382,1.73618236166778,16.8424244891629));
#5219=CARTESIAN_POINT('Ctrl Pts',(1.67273492930515,1.7926281364344,16.8466491127486));
#5220=CARTESIAN_POINT('Ctrl Pts',(1.61149759544796,1.84608389567361,16.8508737363343));
#5221=CARTESIAN_POINT('Ctrl Pts',(1.55001924356036,1.89975004620509,16.8551149872025));
#5222=CARTESIAN_POINT('Ctrl Pts',(1.48578801614026,1.95040221802365,16.8593562380708));
#5223=CARTESIAN_POINT('Ctrl Pts',(1.4191343552195,1.99775071814172,16.8635974889391));
#5224=CARTESIAN_POINT('Ctrl Pts',(1.35286182164279,2.04482847832074,16.8678144882261));
#5225=CARTESIAN_POINT('Ctrl Pts',(1.28419486541293,2.08863997320343,16.872031487513));
#5226=CARTESIAN_POINT('Ctrl Pts',(1.21349137625816,2.128940799963,16.8762484868));
#5227=CARTESIAN_POINT('Ctrl Pts',(1.14281132685682,2.16922826611683,16.8804640880594));
#5228=CARTESIAN_POINT('Ctrl Pts',(1.0700964889884,2.20600714526631,16.8846796893189));
#5229=CARTESIAN_POINT('Ctrl Pts',(0.995731745287223,2.23907760951407,16.8888952905783));
#5230=CARTESIAN_POINT('Ctrl Pts',(0.921368857178305,2.27214724856842,16.8931107866476));
#5231=CARTESIAN_POINT('Ctrl Pts',(0.845356570468824,2.30150846872209,16.8973262827169));
#5232=CARTESIAN_POINT('Ctrl Pts',(0.768100940561478,2.32700906640017,16.9015417787862));
#5233=CARTESIAN_POINT('Ctrl Pts',(0.690026684343838,2.35277987687972,16.9058019436518));
#5234=CARTESIAN_POINT('Ctrl Pts',(0.610683033284415,2.37460759369614,16.9100621085174));
#5235=CARTESIAN_POINT('Ctrl Pts',(0.530504267227748,2.3923869821693,16.9143222733829));
#5236=CARTESIAN_POINT('Ctrl Pts',(0.451050652339837,2.41000557065806,16.9185439085519));
#5237=CARTESIAN_POINT('Ctrl Pts',(0.37077744147681,2.42364874593634,16.9227655437209));
#5238=CARTESIAN_POINT('Ctrl Pts',(0.290115101997907,2.4332660104462,16.9269871788898));
#5239=CARTESIAN_POINT('Ctrl Pts',(0.208348488223305,2.44301493612609,16.9312666086037));
#5240=CARTESIAN_POINT('Ctrl Pts',(0.126182504257374,2.44862685258754,16.9355460383176));
#5241=CARTESIAN_POINT('Ctrl Pts',(0.0440663891710255,2.45010375358788,16.9398254680315));
#5242=CARTESIAN_POINT('Ctrl Pts',(-0.0380497259153342,2.45158065458822,
16.9441048977454));
#5243=CARTESIAN_POINT('Ctrl Pts',(-0.120115483911665,2.44892262146591,16.9483843274593));
#5244=CARTESIAN_POINT('Ctrl Pts',(-0.201688165846049,2.44218593349435,16.9526637571732));
#5245=CARTESIAN_POINT('Ctrl Pts',(-0.2823320195379,2.43552595289467,16.9568944591134));
#5246=CARTESIAN_POINT('Ctrl Pts',(-0.362797296576188,2.42485472160487,16.9611251610537));
#5247=CARTESIAN_POINT('Ctrl Pts',(-0.442653106968677,2.41018847331303,16.9653558629939));
#5248=CARTESIAN_POINT('Ctrl Pts',(-0.522394186534465,2.39554329638447,16.9695804865796));
#5249=CARTESIAN_POINT('Ctrl Pts',(-0.601527084986443,2.37691458518842,16.9738051101653));
#5250=CARTESIAN_POINT('Ctrl Pts',(-0.679625034710922,2.35437041737153,16.9780297337509));
#5251=CARTESIAN_POINT('Ctrl Pts',(-0.758030362514393,2.33173752017031,16.9822709846192));
#5252=CARTESIAN_POINT('Ctrl Pts',(-0.835392104465863,2.30515831837505,16.9865122354875));
#5253=CARTESIAN_POINT('Ctrl Pts',(-0.911287793776045,2.27475379039464,16.9907534863558));
#5254=CARTESIAN_POINT('Ctrl Pts',(-0.98674950958664,2.24452311628566,16.9949704856428));
#5255=CARTESIAN_POINT('Ctrl Pts',(-1.06076145706699,2.21051091859264,16.9991874849297));
#5256=CARTESIAN_POINT('Ctrl Pts',(-1.13292438696323,2.17288577321128,17.0034044842167));
#5257=CARTESIAN_POINT('Ctrl Pts',(-1.20506339326942,2.13527310138878,17.0076200854761));
#5258=CARTESIAN_POINT('Ctrl Pts',(-1.27535418723763,2.09405007528635,17.0118356867356));
#5259=CARTESIAN_POINT('Ctrl Pts',(-1.34342038204212,2.04943209868339,17.016051287995));
#5260=CARTESIAN_POINT('Ctrl Pts',(-1.41148487841935,2.00481523541412,17.0202667840643));
#5261=CARTESIAN_POINT('Ctrl Pts',(-1.4773244976492,1.95680384593853,17.0244822801336));
#5262=CARTESIAN_POINT('Ctrl Pts',(-1.54059143022568,1.90565691957267,17.0286977762029));
#5263=CARTESIAN_POINT('Ctrl Pts',(-1.60452876023013,1.85396802338958,17.0329579410685));
#5264=CARTESIAN_POINT('Ctrl Pts',(-1.66583816997849,1.79907703632268,17.0372181059341));
#5265=CARTESIAN_POINT('Ctrl Pts',(-1.72419605836923,1.74129210711586,17.0414782707997));
#5266=CARTESIAN_POINT('Ctrl Pts',(-1.78202614753013,1.68402979519308,17.0456999059687));
#5267=CARTESIAN_POINT('Ctrl Pts',(-1.8369576170974,1.62392606598167,17.0499215411376));
#5268=CARTESIAN_POINT('Ctrl Pts',(-1.88871495074155,1.56131549817625,17.0541431763066));
#5269=CARTESIAN_POINT('Ctrl Pts',(-1.94118084669036,1.49784778636636,17.0584226060205));
#5270=CARTESIAN_POINT('Ctrl Pts',(-1.99038474476865,1.43180447526388,17.0627020357344));
#5271=CARTESIAN_POINT('Ctrl Pts',(-2.03608509788801,1.36356434544116,17.0669814654483));
#5272=CARTESIAN_POINT('Ctrl Pts',(-2.08178545100736,1.29532421561844,17.0712608951622));
#5273=CARTESIAN_POINT('Ctrl Pts',(-2.12398206323079,1.22488772157969,17.075540324876));
#5274=CARTESIAN_POINT('Ctrl Pts',(-2.16248255848475,1.15265755289646,17.0798197545899));
#5275=CARTESIAN_POINT('Ctrl Pts',(-2.20267916262549,1.07724534122418,17.0842877111973));
#5276=CARTESIAN_POINT('Ctrl Pts',(-2.23898476198777,0.999620428064312,17.0887556678047));
#5277=CARTESIAN_POINT('Ctrl Pts',(-2.27116419083351,0.920197515903829,17.0932236244121));
#5278=CARTESIAN_POINT('Ctrl Pts',(-2.30324859241758,0.841009143078799,17.0976783869481));
#5279=CARTESIAN_POINT('Ctrl Pts',(-2.33123095314881,0.760033706883336,17.1021331494841));
#5280=CARTESIAN_POINT('Ctrl Pts',(-2.35492280758174,0.677708506904951,17.10658791202));
#5281=CARTESIAN_POINT('Ctrl Pts',(-2.37857232061478,0.595530436152888,17.1110347131327));
#5282=CARTESIAN_POINT('Ctrl Pts',(-2.39794647646274,0.5120077714379,17.1154815142454));
#5283=CARTESIAN_POINT('Ctrl Pts',(-2.41290518136713,0.427596580589296,17.1199283153581));
#5284=CARTESIAN_POINT('Ctrl Pts',(-2.42782859230949,0.343384551725846,17.1243646245712));
#5285=CARTESIAN_POINT('Ctrl Pts',(-2.4383572374737,0.258288553179804,17.1288009337843));
#5286=CARTESIAN_POINT('Ctrl Pts',(-2.44440142582966,0.172777080082745,17.1332372429974));
#5287=CARTESIAN_POINT('Ctrl Pts',(-2.44845933346365,0.115366946738365,17.1362156632521));
#5288=CARTESIAN_POINT('Ctrl Pts',(-2.45049693206647,0.0577698600948637,
17.1391940835069));
#5289=CARTESIAN_POINT('Ctrl Pts',(-2.45049999653667,0.000130283472656437,
17.1421725037616));
#5290=CARTESIAN_POINT('',(-2.45049898498602,-0.00223037720147216,17.942172503788));
#5291=CARTESIAN_POINT('Ctrl Pts',(-2.4504999965367,0.000130282960863897,
17.142172503788));
#5292=CARTESIAN_POINT('Ctrl Pts',(-2.45050452194911,-0.0849884696040502,
17.1465708604649));
#5293=CARTESIAN_POINT('Ctrl Pts',(-2.44606980392813,-0.170029198439797,
17.1509692171419));
#5294=CARTESIAN_POINT('Ctrl Pts',(-2.43724598391095,-0.254523601872133,
17.1553675738189));
#5295=CARTESIAN_POINT('Ctrl Pts',(-2.42839970581627,-0.339233057499113,
17.1597771250391));
#5296=CARTESIAN_POINT('Ctrl Pts',(-2.41514204232485,-0.423393005931581,
17.1641866762593));
#5297=CARTESIAN_POINT('Ctrl Pts',(-2.39757477354347,-0.506542649011867,
17.1685962274796));
#5298=CARTESIAN_POINT('Ctrl Pts',(-2.37998497661235,-0.58979892264665,17.1730114334792));
#5299=CARTESIAN_POINT('Ctrl Pts',(-2.35807465958441,-0.672041917858444,
17.1774266394789));
#5300=CARTESIAN_POINT('Ctrl Pts',(-2.33199555060948,-0.752826010401865,
17.1818418454786));
#5301=CARTESIAN_POINT('Ctrl Pts',(-2.305845995393,-0.833828321125292,17.1862689780617));
#5302=CARTESIAN_POINT('Ctrl Pts',(-2.27550527631956,-0.913363471002124,
17.1906961106448));
#5303=CARTESIAN_POINT('Ctrl Pts',(-2.24117371120437,-0.991004866893403,
17.1951232432279));
#5304=CARTESIAN_POINT('Ctrl Pts',(-2.2105357328379,-1.06029315595564,17.1990740794875));
#5305=CARTESIAN_POINT('Ctrl Pts',(-2.17672019184866,-1.12807340583658,17.2030249157471));
#5306=CARTESIAN_POINT('Ctrl Pts',(-2.13989918397987,-1.19406102540963,17.2069757520067));
#5307=CARTESIAN_POINT('Ctrl Pts',(-2.10046988365032,-1.26472301487633,17.2112064539469));
#5308=CARTESIAN_POINT('Ctrl Pts',(-2.05746265756894,-1.33356278892363,17.2154371558872));
#5309=CARTESIAN_POINT('Ctrl Pts',(-2.01107056395207,-1.40019478530863,17.2196678578274));
#5310=CARTESIAN_POINT('Ctrl Pts',(-1.96474512300856,-1.46673104984919,17.2238924814131));
#5311=CARTESIAN_POINT('Ctrl Pts',(-1.91504473643684,-1.53106545800606,17.2281171049988));
#5312=CARTESIAN_POINT('Ctrl Pts',(-1.86220795516761,-1.59283765077,17.2323417285845));
#5313=CARTESIAN_POINT('Ctrl Pts',(-1.80916321878083,-1.65485296666328,17.2365829794528));
#5314=CARTESIAN_POINT('Ctrl Pts',(-1.7529575775228,-1.71428544075453,17.2408242303211));
#5315=CARTESIAN_POINT('Ctrl Pts',(-1.69387596331298,-1.77080051697262,17.2450654811893));
#5316=CARTESIAN_POINT('Ctrl Pts',(-1.63513217928983,-1.82699243853417,17.2492824804763));
#5317=CARTESIAN_POINT('Ctrl Pts',(-1.57354556228432,-1.88029991050138,17.2534994797632));
#5318=CARTESIAN_POINT('Ctrl Pts',(-1.50943477042274,-1.93042920715546,17.2577164790502));
#5319=CARTESIAN_POINT('Ctrl Pts',(-1.44534523269119,-1.98054188485104,17.2619320803096));
#5320=CARTESIAN_POINT('Ctrl Pts',(-1.37873354795455,-2.02747819333673,17.266147681569));
#5321=CARTESIAN_POINT('Ctrl Pts',(-1.30995154682968,-2.07098459553868,17.2703632828285));
#5322=CARTESIAN_POINT('Ctrl Pts',(-1.24117126199333,-2.11448991214358,17.2745787788978));
#5323=CARTESIAN_POINT('Ctrl Pts',(-1.17022116205761,-2.15456524494081,17.2787942749671));
#5324=CARTESIAN_POINT('Ctrl Pts',(-1.09748093380663,-2.19100110678451,17.2830097710364));
#5325=CARTESIAN_POINT('Ctrl Pts',(-1.02396992594062,-2.22782305512038,17.2872699359019));
#5326=CARTESIAN_POINT('Ctrl Pts',(-0.948631052230668,-2.2609277117866,17.2915301007675));
#5327=CARTESIAN_POINT('Ctrl Pts',(-0.871878737678063,-2.29014796831666,
17.2957902656331));
#5328=CARTESIAN_POINT('Ctrl Pts',(-0.795820584851126,-2.3191039515956,17.3000119008021));
#5329=CARTESIAN_POINT('Ctrl Pts',(-0.718374921478922,-2.34424542805932,
17.304233535971));
#5330=CARTESIAN_POINT('Ctrl Pts',(-0.639960339280295,-2.36546000053864,
17.30845517114));
#5331=CARTESIAN_POINT('Ctrl Pts',(-0.560472254774414,-2.38696500232161,
17.3127346008539));
#5332=CARTESIAN_POINT('Ctrl Pts',(-0.479989004807428,-2.40443466179837,
17.3170140305678));
#5333=CARTESIAN_POINT('Ctrl Pts',(-0.398955367489305,-2.4178057954996,17.3212934602817));
#5334=CARTESIAN_POINT('Ctrl Pts',(-0.317921730171183,-2.43117692920084,
17.3255728899955));
#5335=CARTESIAN_POINT('Ctrl Pts',(-0.236338200347234,-2.44044954679654,
17.3298523197094));
#5336=CARTESIAN_POINT('Ctrl Pts',(-0.154650978361386,-2.44561512198708,
17.3341317494233));
#5337=CARTESIAN_POINT('Ctrl Pts',(-0.0738938888296647,-2.45072187929873,
17.3383624513636));
#5338=CARTESIAN_POINT('Ctrl Pts',(0.00726829076739741,-2.45183389960285,
17.3425931533038));
#5339=CARTESIAN_POINT('Ctrl Pts',(0.0884068720681205,-2.44890475008138,
17.3468238552441));
#5340=CARTESIAN_POINT('Ctrl Pts',(0.169428879553403,-2.44597980894179,17.3510484788298));
#5341=CARTESIAN_POINT('Ctrl Pts',(0.250426895263739,-2.43902524574518,17.3552731024155));
#5342=CARTESIAN_POINT('Ctrl Pts',(0.330968790351253,-2.42804652134456,17.3594977260012));
#5343=CARTESIAN_POINT('Ctrl Pts',(0.411827682402982,-2.4170245868568,17.3637389768694));
#5344=CARTESIAN_POINT('Ctrl Pts',(0.492226382121687,-2.40194671666983,17.3679802277377));
#5345=CARTESIAN_POINT('Ctrl Pts',(0.571729343457058,-2.38287133681829,17.372221478606));
#5346=CARTESIAN_POINT('Ctrl Pts',(0.650777704818788,-2.36390503047837,17.376438477893));
#5347=CARTESIAN_POINT('Ctrl Pts',(0.728940086938435,-2.34098691574096,17.3806554771799));
#5348=CARTESIAN_POINT('Ctrl Pts',(0.805797012423679,-2.31422588023924,17.3848724764669));
#5349=CARTESIAN_POINT('Ctrl Pts',(0.882628458156655,-2.28747371660626,17.3890880777263));
#5350=CARTESIAN_POINT('Ctrl Pts',(0.958154867847561,-2.25688131498564,17.3933036789858));
#5351=CARTESIAN_POINT('Ctrl Pts',(1.03197259303029,-2.22260721164004,17.3975192802452));
#5352=CARTESIAN_POINT('Ctrl Pts',(1.10578847627005,-2.18833396352188,17.4017347763145));
#5353=CARTESIAN_POINT('Ctrl Pts',(1.17789533841908,-2.15037939316877,17.4059502723838));
#5354=CARTESIAN_POINT('Ctrl Pts',(1.24791148466067,-2.10894930627837,17.4101657684531));
#5355=CARTESIAN_POINT('Ctrl Pts',(1.31866954523984,-2.06708021242856,17.4144259333187));
#5356=CARTESIAN_POINT('Ctrl Pts',(1.38729189310412,-2.02166174087271,17.4186860981843));
#5357=CARTESIAN_POINT('Ctrl Pts',(1.45341365594795,-1.97295184804495,17.4229462630499));
#5358=CARTESIAN_POINT('Ctrl Pts',(1.51893740168615,-1.9246824962414,17.4271678982188));
#5359=CARTESIAN_POINT('Ctrl Pts',(1.58200528676912,-1.87318136533049,17.4313895333878));
#5360=CARTESIAN_POINT('Ctrl Pts',(1.64229618191589,-1.81873953629003,17.4356111685568));
#5361=CARTESIAN_POINT('Ctrl Pts',(1.70341246455095,-1.76355239397432,17.4398905982707));
#5362=CARTESIAN_POINT('Ctrl Pts',(1.76167479715392,-1.70534377668145,17.4441700279846));
#5363=CARTESIAN_POINT('Ctrl Pts',(1.81678924960985,-1.64445342667467,17.4484494576985));
#5364=CARTESIAN_POINT('Ctrl Pts',(1.87190370206578,-1.5835630766679,17.4527288874124));
#5365=CARTESIAN_POINT('Ctrl Pts',(1.92387001458967,-1.51999141522758,17.4570083171263));
#5366=CARTESIAN_POINT('Ctrl Pts',(1.97243944047889,-1.45410897241002,17.4612877468402));
#5367=CARTESIAN_POINT('Ctrl Pts',(2.02045583006451,-1.38897670075427,17.4655184487804));
#5368=CARTESIAN_POINT('Ctrl Pts',(2.06533293501881,-1.32134104863923,17.4697491507207));
#5369=CARTESIAN_POINT('Ctrl Pts',(2.10679961964322,-1.25153729975226,17.4739798526609));
#5370=CARTESIAN_POINT('Ctrl Pts',(2.14820672805185,-1.18183383964516,17.4782044762466));
#5371=CARTESIAN_POINT('Ctrl Pts',(2.1862129119699,-1.10996886568492,17.4824290998323));
#5372=CARTESIAN_POINT('Ctrl Pts',(2.2205888029732,-1.03630865002182,17.486653723418));
#5373=CARTESIAN_POINT('Ctrl Pts',(2.25509999068222,-0.962358522323541,17.4908949742863));
#5374=CARTESIAN_POINT('Ctrl Pts',(2.28595196635849,-0.886599373155283,17.4951362251546));
#5375=CARTESIAN_POINT('Ctrl Pts',(2.31295804233885,-0.809429023682766,17.4993774760229));
#5376=CARTESIAN_POINT('Ctrl Pts',(2.33980969688355,-0.732699936249384,17.5035944753098));
#5377=CARTESIAN_POINT('Ctrl Pts',(2.36285915913114,-0.654576186647708,17.5078114745968));
#5378=CARTESIAN_POINT('Ctrl Pts',(2.38197086714886,-0.575469406705611,17.5120284738837));
#5379=CARTESIAN_POINT('Ctrl Pts',(2.40107623921725,-0.496388852391768,17.5162440751432));
#5380=CARTESIAN_POINT('Ctrl Pts',(2.4162463403341,-0.416326366608398,17.5204596764026));
#5381=CARTESIAN_POINT('Ctrl Pts',(2.42739592099358,-0.335707153250742,17.524675277662));
#5382=CARTESIAN_POINT('Ctrl Pts',(2.43854522344226,-0.255089951550467,17.5288907737313));
#5383=CARTESIAN_POINT('Ctrl Pts',(2.44567414226284,-0.173916510720612,17.5331062698006));
#5384=CARTESIAN_POINT('Ctrl Pts',(2.44874905604843,-0.0926191691926037,
17.5373217658699));
#5385=CARTESIAN_POINT('Ctrl Pts',(2.45185655264164,-0.0104603740357106,
17.5415819307355));
#5386=CARTESIAN_POINT('Ctrl Pts',(2.45082358306199,0.0718244797267152,17.5458420956011));
#5387=CARTESIAN_POINT('Ctrl Pts',(2.44566947993344,0.153788962289517,17.5501022604666));
#5388=CARTESIAN_POINT('Ctrl Pts',(2.4405619914398,0.235012143342659,17.5543238956356));
#5389=CARTESIAN_POINT('Ctrl Pts',(2.43140772829692,0.31592026456825,17.5585455308046));
#5390=CARTESIAN_POINT('Ctrl Pts',(2.41827755582974,0.39608573941781,17.5627671659735));
#5391=CARTESIAN_POINT('Ctrl Pts',(2.40496763018349,0.477348686443871,17.5670465956874));
#5392=CARTESIAN_POINT('Ctrl Pts',(2.38757221436303,0.557848015856512,17.5713260254013));
#5393=CARTESIAN_POINT('Ctrl Pts',(2.36621781198581,0.6371526632143,17.5756054551152));
#5394=CARTESIAN_POINT('Ctrl Pts',(2.34486340960859,0.716457310572088,17.5798848848291));
#5395=CARTESIAN_POINT('Ctrl Pts',(2.31955023421858,0.794566829372656,17.584164314543));
#5396=CARTESIAN_POINT('Ctrl Pts',(2.29045513733653,0.871071474592463,17.5884437442568));
#5397=CARTESIAN_POINT('Ctrl Pts',(2.26169133209598,0.946704998825821,17.5926744461971));
#5398=CARTESIAN_POINT('Ctrl Pts',(2.2291231450125,1.02105450572532,17.5969051481374));
#5399=CARTESIAN_POINT('Ctrl Pts',(2.1928856722894,1.09371050935239,17.6011358500776));
#5400=CARTESIAN_POINT('Ctrl Pts',(2.1567002628436,1.16626212629407,17.6053604736633));
#5401=CARTESIAN_POINT('Ctrl Pts',(2.11685624355658,1.23712465959145,17.609585097249));
#5402=CARTESIAN_POINT('Ctrl Pts',(2.07353737771213,1.30590696193516,17.6138097208347));
#5403=CARTESIAN_POINT('Ctrl Pts',(2.03004801738214,1.37495997781263,17.6180509717029));
#5404=CARTESIAN_POINT('Ctrl Pts',(1.98305656789875,1.44191590929957,17.6222922225712));
#5405=CARTESIAN_POINT('Ctrl Pts',(1.93279642548741,1.50640241224683,17.6265334734395));
#5406=CARTESIAN_POINT('Ctrl Pts',(1.88282367186057,1.57052017971487,17.6307504727265));
#5407=CARTESIAN_POINT('Ctrl Pts',(1.82961979357151,1.63219631202484,17.6349674720134));
#5408=CARTESIAN_POINT('Ctrl Pts',(1.77345747833991,1.69109397211398,17.6391844713004));
#5409=CARTESIAN_POINT('Ctrl Pts',(1.71731378214439,1.74997210634039,17.6434000725598));
#5410=CARTESIAN_POINT('Ctrl Pts',(1.65821391736659,1.80607326123916,17.6476156738193));
#5411=CARTESIAN_POINT('Ctrl Pts',(1.5964692222879,1.85909555222088,17.6518312750787));
#5412=CARTESIAN_POINT('Ctrl Pts',(1.53472606789875,1.91211652015956,17.656046771148));
#5413=CARTESIAN_POINT('Ctrl Pts',(1.47033856795327,1.9620584747717,17.6602622672173));
#5414=CARTESIAN_POINT('Ctrl Pts',(1.40365201121218,2.00865907545806,17.6644777632866));
#5415=CARTESIAN_POINT('Ctrl Pts',(1.33625882156986,2.05575347158492,17.6687379281522));
#5416=CARTESIAN_POINT('Ctrl Pts',(1.26651794977077,2.09943498925052,17.6729980930178));
#5417=CARTESIAN_POINT('Ctrl Pts',(1.19481520194372,2.13947818011874,17.6772582578834));
#5418=CARTESIAN_POINT('Ctrl Pts',(1.12376094665349,2.17915921317272,17.6814798930524));
#5419=CARTESIAN_POINT('Ctrl Pts',(1.05078060854846,2.21526731287341,17.6857015282213));
#5420=CARTESIAN_POINT('Ctrl Pts',(0.976272051562424,2.24763055935314,17.6899231633903));
#5421=CARTESIAN_POINT('Ctrl Pts',(0.900743466086785,2.28043686143293,17.6942025931042));
#5422=CARTESIAN_POINT('Ctrl Pts',(0.823644965085444,2.30939482529144,17.6984820228181));
#5423=CARTESIAN_POINT('Ctrl Pts',(0.745407459787558,2.33437742640154,17.702761452532));
#5424=CARTESIAN_POINT('Ctrl Pts',(0.667169954489682,2.35936002751163,17.7070408822459));
#5425=CARTESIAN_POINT('Ctrl Pts',(0.587793935910716,2.38036720367035,17.7113203119598));
#5426=CARTESIAN_POINT('Ctrl Pts',(0.507719649770126,2.39732580331446,17.7155997416737));
#5427=CARTESIAN_POINT('Ctrl Pts',(0.428557130371937,2.41409130367665,17.7198304436139));
#5428=CARTESIAN_POINT('Ctrl Pts',(0.348414420808694,2.42696305918836,17.7240611455542));
#5429=CARTESIAN_POINT('Ctrl Pts',(0.267708942148703,2.43583295246074,17.7282918474944));
#5430=CARTESIAN_POINT('Ctrl Pts',(0.187119415054621,2.44469010213713,17.7325164710801));
#5431=CARTESIAN_POINT('Ctrl Pts',(0.105969183031929,2.44955675817102,17.7367410946658));
#5432=CARTESIAN_POINT('Ctrl Pts',(0.0246865977423455,2.4503756491387,17.7409657182515));
#5433=CARTESIAN_POINT('Ctrl Pts',(-0.0569158997213942,2.45119776309921,
17.7452069691197));
#5434=CARTESIAN_POINT('Ctrl Pts',(-0.138651330262372,2.44794008292565,17.749448219988));
#5435=CARTESIAN_POINT('Ctrl Pts',(-0.220080279254648,2.44059724671712,17.7536894708563));
#5436=CARTESIAN_POINT('Ctrl Pts',(-0.301043615426376,2.43329639703452,17.7579064701433));
#5437=CARTESIAN_POINT('Ctrl Pts',(-0.381703497639979,2.42195702478503,17.7621234694302));
#5438=CARTESIAN_POINT('Ctrl Pts',(-0.461629091239075,2.40662602664431,17.7663404687172));
#5439=CARTESIAN_POINT('Ctrl Pts',(-0.541528187755332,2.39130011106488,17.7705560699766));
#5440=CARTESIAN_POINT('Ctrl Pts',(-0.62069302270116,2.37198528500524,17.774771671236));
#5441=CARTESIAN_POINT('Ctrl Pts',(-0.698701222103131,2.34877986457471,17.7789872724955));
#5442=CARTESIAN_POINT('Ctrl Pts',(-0.776707474999244,2.32557502317929,17.7832027685648));
#5443=CARTESIAN_POINT('Ctrl Pts',(-0.853556704287896,2.29847991407354,17.7874182646341));
#5444=CARTESIAN_POINT('Ctrl Pts',(-0.928841401711176,2.26764280707241,17.7916337607034));
#5445=CARTESIAN_POINT('Ctrl Pts',(-1.00492384078969,2.23647893984478,17.795893925569));
#5446=CARTESIAN_POINT('Ctrl Pts',(-1.0794079395581,2.20149346835275,17.8001540904345));
#5447=CARTESIAN_POINT('Ctrl Pts',(-1.15189527062322,2.1628887016016,17.8044142553001));
#5448=CARTESIAN_POINT('Ctrl Pts',(-1.22372701323978,2.12463308329846,17.8086358904691));
#5449=CARTESIAN_POINT('Ctrl Pts',(-1.2935975893135,2.08282366793475,17.812857525638));
#5450=CARTESIAN_POINT('Ctrl Pts',(-1.36114704767522,2.03770188315294,17.817079160807));
#5451=CARTESIAN_POINT('Ctrl Pts',(-1.4296212638737,1.99196237729538,17.8213585905209));
#5452=CARTESIAN_POINT('Ctrl Pts',(-1.49570993162505,1.94281941724692,17.8256380202348));
#5453=CARTESIAN_POINT('Ctrl Pts',(-1.55907295365824,1.89056652228145,17.8299174499487));
#5454=CARTESIAN_POINT('Ctrl Pts',(-1.62243597569142,1.83831362731599,17.8341968796625));
#5455=CARTESIAN_POINT('Ctrl Pts',(-1.68307303386725,1.78295117658104,17.8384763093764));
#5456=CARTESIAN_POINT('Ctrl Pts',(-1.74068427121074,1.72480970485429,17.8427557390903));
#5457=CARTESIAN_POINT('Ctrl Pts',(-1.79684041836039,1.6681367154804,17.8469270830123));
#5458=CARTESIAN_POINT('Ctrl Pts',(-1.85034552545446,1.60859737264218,17.8510984269343));
#5459=CARTESIAN_POINT('Ctrl Pts',(-1.90088679305653,1.54647329430006,17.8552697708562));
#5460=CARTESIAN_POINT('Ctrl Pts',(-1.95136270988477,1.4844295435157,17.859435721155));
#5461=CARTESIAN_POINT('Ctrl Pts',(-1.99888208736877,1.41980805190744,17.8636016714538));
#5462=CARTESIAN_POINT('Ctrl Pts',(-2.04316834329773,1.35292770351782,17.8677676217525));
#5463=CARTESIAN_POINT('Ctrl Pts',(-2.08741180345981,1.28611198456545,17.8719295463094));
#5464=CARTESIAN_POINT('Ctrl Pts',(-2.1284280766816,1.21704213571831,17.8760914708662));
#5465=CARTESIAN_POINT('Ctrl Pts',(-2.16598137453289,1.14606934134747,17.880253395423));
#5466=CARTESIAN_POINT('Ctrl Pts',(-2.20351064302982,1.07514196057606,17.8844126568753));
#5467=CARTESIAN_POINT('Ctrl Pts',(-2.2375811105656,1.00231447313695,17.8885719183275));
#5468=CARTESIAN_POINT('Ctrl Pts',(-2.26800165933593,0.927964828670506,17.8927311797798));
#5469=CARTESIAN_POINT('Ctrl Pts',(-2.29842423865501,0.853610221421215,17.8968907188596));
#5470=CARTESIAN_POINT('Ctrl Pts',(-2.3251962132241,0.777733690129484,17.9010502579394));
#5471=CARTESIAN_POINT('Ctrl Pts',(-2.34817408744007,0.700734404089727,17.9052097970192));
#5472=CARTESIAN_POINT('Ctrl Pts',(-2.37115120639293,0.623737648950773,17.9093691993785));
#5473=CARTESIAN_POINT('Ctrl Pts',(-2.39033434371149,0.545618674236535,17.9135286017379));
#5474=CARTESIAN_POINT('Ctrl Pts',(-2.40563014694911,0.466791009006805,17.9176880040972));
#5475=CARTESIAN_POINT('Ctrl Pts',(-2.42094168019271,0.38788227842697,17.921851683932));
#5476=CARTESIAN_POINT('Ctrl Pts',(-2.43235781014975,0.308263874397381,17.9260153637668));
#5477=CARTESIAN_POINT('Ctrl Pts',(-2.43983664962272,0.228357993417779,17.9301790436017));
#5478=CARTESIAN_POINT('Ctrl Pts',(-2.44701757026798,0.151635155271715,17.9341768636638));
#5479=CARTESIAN_POINT('Ctrl Pts',(-2.45056895731561,0.0746477053583067,
17.9381746837259));
#5480=CARTESIAN_POINT('Ctrl Pts',(-2.45049898498602,-0.00223037720147216,
17.942172503788));
#5481=CARTESIAN_POINT('',(-2.4506184992838,0.00106435978254121,18.742172503788));
#5482=CARTESIAN_POINT('Ctrl Pts',(-2.45086623049305,-0.00223071145829692,
17.942172503788));
#5483=CARTESIAN_POINT('Ctrl Pts',(-2.45251448448338,-0.180067494476928,
17.9514189146944));
#5484=CARTESIAN_POINT('Ctrl Pts',(-2.35363103519027,-1.17128619448211,18.0030506580727));
#5485=CARTESIAN_POINT('Ctrl Pts',(-1.00509395767141,-2.71753796896942,18.0970677339241));
#5486=CARTESIAN_POINT('Ctrl Pts',(1.74062071602852,-2.31634755584424,18.2242237313404));
#5487=CARTESIAN_POINT('Ctrl Pts',(2.8898793093525,0.2093419544921,18.3513797287573));
#5488=CARTESIAN_POINT('Ctrl Pts',(1.38860906978141,2.54302798408779,18.478535726174));
#5489=CARTESIAN_POINT('Ctrl Pts',(-1.38626050840876,2.54430899840504,18.6056917235908));
#5490=CARTESIAN_POINT('Ctrl Pts',(-2.42529377406342,0.93243124355413,18.693570649462));
#5491=CARTESIAN_POINT('Ctrl Pts',(-2.45429862551719,0.0606504956432896,
18.7390642428612));
#5492=CARTESIAN_POINT('Ctrl Pts',(-2.45397396328318,0.00106581713746319,
18.742172503788));
#5493=CARTESIAN_POINT('',(-2.45049945194367,0.00163890932561317,19.5421725037581));
#5494=CARTESIAN_POINT('Ctrl Pts',(-2.45049976887328,0.00106430821520263,
18.742172503788));
#5495=CARTESIAN_POINT('Ctrl Pts',(-2.45053457116055,-0.0790656726323252,
18.7463584563462));
#5496=CARTESIAN_POINT('Ctrl Pts',(-2.44663482555748,-0.159355808443341,
18.7505444089043));
#5497=CARTESIAN_POINT('Ctrl Pts',(-2.43877965671853,-0.239382614188756,
18.7547303614625));
#5498=CARTESIAN_POINT('Ctrl Pts',(-2.43054835629879,-0.323241369261778,
18.7591167513359));
#5499=CARTESIAN_POINT('Ctrl Pts',(-2.41797325303157,-0.406810428678383,
18.7635031412093));
#5500=CARTESIAN_POINT('Ctrl Pts',(-2.40109181530018,-0.489600188417552,
18.7678895310827));
#5501=CARTESIAN_POINT('Ctrl Pts',(-2.38502088583557,-0.568415062501779,
18.7720653224686));
#5502=CARTESIAN_POINT('Ctrl Pts',(-2.36504768720019,-0.646523207224635,
18.7762411138544));
#5503=CARTESIAN_POINT('Ctrl Pts',(-2.34125756179545,-0.72350762216829,18.7804169052403));
#5504=CARTESIAN_POINT('Ctrl Pts',(-2.31747992244937,-0.800451632452265,
18.7845905049952));
#5505=CARTESIAN_POINT('Ctrl Pts',(-2.28988947121388,-0.876272629655242,
18.7887641047501));
#5506=CARTESIAN_POINT('Ctrl Pts',(-2.25862197796099,-0.950566678708845,
18.7929377045049));
#5507=CARTESIAN_POINT('Ctrl Pts',(-2.22736082903732,-1.02484565313201,18.7971104574157));
#5508=CARTESIAN_POINT('Ctrl Pts',(-2.19242430421625,-1.09759785649272,18.8012832103266));
#5509=CARTESIAN_POINT('Ctrl Pts',(-2.15399652099998,-1.16843880349806,18.8054559632374));
#5510=CARTESIAN_POINT('Ctrl Pts',(-2.11556416357172,-1.2392881829833,18.8096292128476));
#5511=CARTESIAN_POINT('Ctrl Pts',(-2.07363995182133,-1.30822543773806,18.8138024624578));
#5512=CARTESIAN_POINT('Ctrl Pts',(-2.02845344465767,-1.37489158585557,18.817975712068));
#5513=CARTESIAN_POINT('Ctrl Pts',(-1.98321910359077,-1.44162830597076,18.822153379431));
#5514=CARTESIAN_POINT('Ctrl Pts',(-1.93471584461297,-1.50608872883522,18.826331046794));
#5515=CARTESIAN_POINT('Ctrl Pts',(-1.88321550237799,-1.56794439365789,18.830508714157));
#5516=CARTESIAN_POINT('Ctrl Pts',(-1.83168330219513,-1.62983832219806,18.8346889658117));
#5517=CARTESIAN_POINT('Ctrl Pts',(-1.7771506534256,-1.68912393887204,18.8388692174664));
#5518=CARTESIAN_POINT('Ctrl Pts',(-1.71992671606776,-1.74550919257286,18.8430494691212));
#5519=CARTESIAN_POINT('Ctrl Pts',(-1.66261026310583,-1.80198560595351,18.8472364791103));
#5520=CARTESIAN_POINT('Ctrl Pts',(-1.60259419652498,-1.85555198760924,18.8514234890995));
#5521=CARTESIAN_POINT('Ctrl Pts',(-1.54022063938599,-1.90595661860637,18.8556104990887));
#5522=CARTESIAN_POINT('Ctrl Pts',(-1.51840549222406,-1.9235856347036,18.8570749055339));
#5523=CARTESIAN_POINT('Ctrl Pts',(-1.49630221864495,-1.94082828205246,18.858539311979));
#5524=CARTESIAN_POINT('Ctrl Pts',(-1.47392622329029,-1.95767508496615,18.8600037184242));
#5525=CARTESIAN_POINT('Ctrl Pts',(-1.40928148802946,-2.00634586349845,18.8642344203645));
#5526=CARTESIAN_POINT('Ctrl Pts',(-1.34210184128869,-2.05190276253577,18.8684651223047));
#5527=CARTESIAN_POINT('Ctrl Pts',(-1.27271981542049,-2.09407127897692,18.872695824245));
#5528=CARTESIAN_POINT('Ctrl Pts',(-1.20343747243254,-2.13617921086289,18.8769204478307));
#5529=CARTESIAN_POINT('Ctrl Pts',(-1.13195942866265,-2.17490818912327,18.8811450714163));
#5530=CARTESIAN_POINT('Ctrl Pts',(-1.05864962455525,-2.21002516330222,18.885369695002));
#5531=CARTESIAN_POINT('Ctrl Pts',(-0.985051287562888,-2.24528035094382,
18.8896109458703));
#5532=CARTESIAN_POINT('Ctrl Pts',(-0.909607119529883,-2.27689475581945,
18.8938521967386));
#5533=CARTESIAN_POINT('Ctrl Pts',(-0.832713038728724,-2.30467768790588,
18.8980934476069));
#5534=CARTESIAN_POINT('Ctrl Pts',(-0.756258640255346,-2.33230175647348,
18.9023104468938));
#5535=CARTESIAN_POINT('Ctrl Pts',(-0.678371307078897,-2.35613789064822,
18.9065274461808));
#5536=CARTESIAN_POINT('Ctrl Pts',(-0.599461283012488,-2.37604638426295,
18.9107444454678));
#5537=CARTESIAN_POINT('Ctrl Pts',(-0.520577419345309,-2.39594827777652,
18.9149600467272));
#5538=CARTESIAN_POINT('Ctrl Pts',(-0.440671988645958,-2.41192500280049,
18.9191756479866));
#5539=CARTESIAN_POINT('Ctrl Pts',(-0.360169313483692,-2.42388702616782,
18.9233912492461));
#5540=CARTESIAN_POINT('Ctrl Pts',(-0.279668647070996,-2.43584875105179,
18.9276067453154));
#5541=CARTESIAN_POINT('Ctrl Pts',(-0.198571225995115,-2.4437959061757,18.9318222413847));
#5542=CARTESIAN_POINT('Ctrl Pts',(-0.117309027645596,-2.44769051189746,
18.936037737454));
#5543=CARTESIAN_POINT('Ctrl Pts',(-0.035185748056052,-2.4516263861548,18.9402979023196));
#5544=CARTESIAN_POINT('Ctrl Pts',(0.0471053385277078,-2.45142327603028,
18.9445580671852));
#5545=CARTESIAN_POINT('Ctrl Pts',(0.129117630040629,-2.44709601111454,18.9488182320507));
#5546=CARTESIAN_POINT('Ctrl Pts',(0.21038818765119,-2.44280788276032,18.9530398672197));
#5547=CARTESIAN_POINT('Ctrl Pts',(0.291384511415768,-2.43447000829624,18.9572615023887));
#5548=CARTESIAN_POINT('Ctrl Pts',(0.371678321882915,-2.42214893741948,18.9614831375577));
#5549=CARTESIAN_POINT('Ctrl Pts',(0.453071361452038,-2.40965919003333,18.9657625672715));
#5550=CARTESIAN_POINT('Ctrl Pts',(0.533742022627916,-2.39307645947105,18.9700419969854));
#5551=CARTESIAN_POINT('Ctrl Pts',(0.613257987155049,-2.37252289582009,18.9743214266993));
#5552=CARTESIAN_POINT('Ctrl Pts',(0.692773951682181,-2.35196933216913,18.9786008564132));
#5553=CARTESIAN_POINT('Ctrl Pts',(0.771134770927409,-2.3274451444598,18.9828802861271));
#5554=CARTESIAN_POINT('Ctrl Pts',(0.847928937232347,-2.29912304311971,18.987159715841));
#5555=CARTESIAN_POINT('Ctrl Pts',(0.923848685915583,-2.27112343169892,18.9913904177812));
#5556=CARTESIAN_POINT('Ctrl Pts',(0.99852284809259,-2.23930668313419,18.9956211197215));
#5557=CARTESIAN_POINT('Ctrl Pts',(1.07154059626096,-2.20380375727166,18.9998518216617));
#5558=CARTESIAN_POINT('Ctrl Pts',(1.14445343801666,-2.16835183934468,19.0040764452474));
#5559=CARTESIAN_POINT('Ctrl Pts',(1.21571417750632,-2.12922446394546,19.008301068833));
#5560=CARTESIAN_POINT('Ctrl Pts',(1.28492983413793,-2.086601440463,19.0125256924187));
#5561=CARTESIAN_POINT('Ctrl Pts',(1.35441790990017,-2.0438106611928,19.016766943287));
#5562=CARTESIAN_POINT('Ctrl Pts',(1.42184432495419,-1.9974968226691,19.0210081941553));
#5563=CARTESIAN_POINT('Ctrl Pts',(1.48683440038543,-1.94788955432039,19.0252494450236));
#5564=CARTESIAN_POINT('Ctrl Pts',(1.55145286089693,-1.89856594160562,19.0294664443105));
#5565=CARTESIAN_POINT('Ctrl Pts',(1.61366239489437,-1.84598674570537,19.0336834435975));
#5566=CARTESIAN_POINT('Ctrl Pts',(1.67312343250635,-1.79042124361787,19.0379004428844));
#5567=CARTESIAN_POINT('Ctrl Pts',(1.73256475748355,-1.73487416270991,19.0421160441438));
#5568=CARTESIAN_POINT('Ctrl Pts',(1.78925905601717,-1.67634305891479,19.0463316454033));
#5569=CARTESIAN_POINT('Ctrl Pts',(1.84290131915776,-1.61513621030754,19.0505472466627));
#5570=CARTESIAN_POINT('Ctrl Pts',(1.8965422437854,-1.55393088896916,19.054762742732));
#5571=CARTESIAN_POINT('Ctrl Pts',(1.94713097872967,-1.49005030603181,19.0589782388013));
#5572=CARTESIAN_POINT('Ctrl Pts',(1.99440171464466,-1.42383708710738,19.0631937348706));
#5573=CARTESIAN_POINT('Ctrl Pts',(2.04217334697579,-1.35692225092613,19.0674538997361));
#5574=CARTESIAN_POINT('Ctrl Pts',(2.08655594974478,-1.28762543457542,19.0717140646017));
#5575=CARTESIAN_POINT('Ctrl Pts',(2.12732019539282,-1.21633015101733,19.0759742294673));
#5576=CARTESIAN_POINT('Ctrl Pts',(2.16771576187756,-1.14567967481608,19.0801958646363));
#5577=CARTESIAN_POINT('Ctrl Pts',(2.20455800040119,-1.07306718226491,19.0844174998052));
#5578=CARTESIAN_POINT('Ctrl Pts',(2.23767098755369,-0.998888783329006,19.0886391349742));
#5579=CARTESIAN_POINT('Ctrl Pts',(2.27123729431996,-0.923694875795193,19.0929185646881));
#5580=CARTESIAN_POINT('Ctrl Pts',(2.30097129046953,-0.846892323751072,19.097197994402));
#5581=CARTESIAN_POINT('Ctrl Pts',(2.32674161238239,-0.768910735526684,19.1014774241159));
#5582=CARTESIAN_POINT('Ctrl Pts',(2.35251193429526,-0.690929147302285,19.1057568538298));
#5583=CARTESIAN_POINT('Ctrl Pts',(2.37431851481993,-0.611769013260816,19.1100362835437));
#5584=CARTESIAN_POINT('Ctrl Pts',(2.39208376642655,-0.531869819033359,19.1143157132576));
#5585=CARTESIAN_POINT('Ctrl Pts',(2.40964673379977,-0.452880397862379,19.1185464151979));
#5586=CARTESIAN_POINT('Ctrl Pts',(2.42332603911252,-0.372871569647813,19.1227771171382));
#5587=CARTESIAN_POINT('Ctrl Pts',(2.43300936096404,-0.292259643915091,19.1270078190784));
#5588=CARTESIAN_POINT('Ctrl Pts',(2.44267877054649,-0.211763535338648,19.1312324426641));
#5589=CARTESIAN_POINT('Ctrl Pts',(2.44836354387022,-0.130666507954575,19.1354570662498));
#5590=CARTESIAN_POINT('Ctrl Pts',(2.45000209268376,-0.0493963140853163,
19.1396816898355));
#5591=CARTESIAN_POINT('Ctrl Pts',(2.45164709050125,0.0321937431880368,19.1439229407038));
#5592=CARTESIAN_POINT('Ctrl Pts',(2.44921384221651,0.113957869726645,19.1481641915721));
#5593=CARTESIAN_POINT('Ctrl Pts',(2.44269255489609,0.195456727321471,19.1524054424403));
#5594=CARTESIAN_POINT('Ctrl Pts',(2.43620855646396,0.276489572356577,19.1566224417273));
#5595=CARTESIAN_POINT('Ctrl Pts',(2.42568318062485,0.357259705606298,19.1608394410143));
#5596=CARTESIAN_POINT('Ctrl Pts',(2.41115897688971,0.437335841389852,19.1650564403012));
#5597=CARTESIAN_POINT('Ctrl Pts',(2.39663958824586,0.517385430182562,19.1692720415607));
#5598=CARTESIAN_POINT('Ctrl Pts',(2.37812408725167,0.59674102116807,19.1734876428201));
#5599=CARTESIAN_POINT('Ctrl Pts',(2.35570652555938,0.674979270375724,19.1777032440795));
#5600=CARTESIAN_POINT('Ctrl Pts',(2.33328952324318,0.753215567336904,19.1819187401488));
#5601=CARTESIAN_POINT('Ctrl Pts',(2.3069707829594,0.830334131182133,19.1861342362181));
#5602=CARTESIAN_POINT('Ctrl Pts',(2.27689445744002,0.905925979138979,19.1903497322874));
#5603=CARTESIAN_POINT('Ctrl Pts',(2.24649943318727,0.982318823420394,19.194609897153));
#5604=CARTESIAN_POINT('Ctrl Pts',(2.21226688043444,1.05715194788344,19.1988700620186));
#5605=CARTESIAN_POINT('Ctrl Pts',(2.17439507993251,1.13002490519691,19.2031302268842));
#5606=CARTESIAN_POINT('Ctrl Pts',(2.13686579880013,1.20223878638869,19.2073518620531));
#5607=CARTESIAN_POINT('Ctrl Pts',(2.09576312380878,1.27252743926019,19.2115734972221));
#5608=CARTESIAN_POINT('Ctrl Pts',(2.05132484037338,1.34052849625329,19.2157951323911));
#5609=CARTESIAN_POINT('Ctrl Pts',(2.00627819305383,1.40946049350692,19.220074562105));
#5610=CARTESIAN_POINT('Ctrl Pts',(1.95780420739321,1.47604138597362,19.2243539918189));
#5611=CARTESIAN_POINT('Ctrl Pts',(1.90619295800689,1.5399281336624,19.2286334215328));
#5612=CARTESIAN_POINT('Ctrl Pts',(1.85458170862056,1.60381488135119,19.2329128512467));
#5613=CARTESIAN_POINT('Ctrl Pts',(1.79983357142846,1.66500716231549,19.2371922809606));
#5614=CARTESIAN_POINT('Ctrl Pts',(1.74227604047339,1.72320180152888,19.2414717106744));
#5615=CARTESIAN_POINT('Ctrl Pts',(1.68537388897927,1.7807338068411,19.2457024126147));
#5616=CARTESIAN_POINT('Ctrl Pts',(1.62551200269707,1.83555251310885,19.249933114555));
#5617=CARTESIAN_POINT('Ctrl Pts',(1.56297958485521,1.88733809036056,19.2541638164952));
#5618=CARTESIAN_POINT('Ctrl Pts',(1.50053700889162,1.93904926598687,19.2583884400809));
#5619=CARTESIAN_POINT('Ctrl Pts',(1.4354318766455,1.98773567326336,19.2626130636666));
#5620=CARTESIAN_POINT('Ctrl Pts',(1.36799047949101,2.03311394122955,19.2668376872523));
#5621=CARTESIAN_POINT('Ctrl Pts',(1.30028364634036,2.07867080908053,19.2710789381206));
#5622=CARTESIAN_POINT('Ctrl Pts',(1.23022245239293,2.12089310400263,19.2753201889889));
#5623=CARTESIAN_POINT('Ctrl Pts',(1.15817097254293,2.15953472960241,19.2795614398571));
#5624=CARTESIAN_POINT('Ctrl Pts',(1.08653148490415,2.19795540139516,19.2837784391441));
#5625=CARTESIAN_POINT('Ctrl Pts',(1.01292482457118,2.23283601945678,19.2879954384311));
#5626=CARTESIAN_POINT('Ctrl Pts',(0.937736635034028,2.26397885443196,19.292212437718));
#5627=CARTESIAN_POINT('Ctrl Pts',(0.862573372026473,2.29511136487609,19.2964280389775));
#5628=CARTESIAN_POINT('Ctrl Pts',(0.785830050330047,2.32250837516458,19.3006436402369));
#5629=CARTESIAN_POINT('Ctrl Pts',(0.707913520251607,2.34601975649076,19.3048592414963));
#5630=CARTESIAN_POINT('Ctrl Pts',(0.62999893439183,2.36953055114726,19.3090747375656));
#5631=CARTESIAN_POINT('Ctrl Pts',(0.550911643900613,2.38915577630448,19.3132902336349));
#5632=CARTESIAN_POINT('Ctrl Pts',(0.47107355011746,2.4047952013383,19.3175057297043));
#5633=CARTESIAN_POINT('Ctrl Pts',(0.390389465379234,2.42060034691347,19.3217658945698));
#5634=CARTESIAN_POINT('Ctrl Pts',(0.308939043421075,2.43233461074559,19.3260260594354));
#5635=CARTESIAN_POINT('Ctrl Pts',(0.227166314896766,2.43994789193872,19.330286224301));
#5636=CARTESIAN_POINT('Ctrl Pts',(0.146133153624064,2.44749231724861,19.3345078594699));
#5637=CARTESIAN_POINT('Ctrl Pts',(0.064783964777887,2.45099004336911,19.3387294946389));
#5638=CARTESIAN_POINT('Ctrl Pts',(-0.0164478485506242,2.45044480008795,
19.3429511298079));
#5639=CARTESIAN_POINT('Ctrl Pts',(-0.0987917323201158,2.44989209237983,
19.3472305595217));
#5640=CARTESIAN_POINT('Ctrl Pts',(-0.181014508632247,2.44518490819366,19.3515099892356));
#5641=CARTESIAN_POINT('Ctrl Pts',(-0.262670714200779,2.4363814040296,19.3557894189495));
#5642=CARTESIAN_POINT('Ctrl Pts',(-0.344326919769299,2.42757789986554,19.3600688486634));
#5643=CARTESIAN_POINT('Ctrl Pts',(-0.425416080387719,2.41467821747543,19.3643482783773));
#5644=CARTESIAN_POINT('Ctrl Pts',(-0.505505990217372,2.39779355738862,19.3686277080912));
#5645=CARTESIAN_POINT('Ctrl Pts',(-0.584683955405516,2.38110115467008,19.3728584100314));
#5646=CARTESIAN_POINT('Ctrl Pts',(-0.663183129486453,2.3604513204167,19.3770891119717));
#5647=CARTESIAN_POINT('Ctrl Pts',(-0.740578034951599,2.33591404468299,19.3813198139119));
#5648=CARTESIAN_POINT('Ctrl Pts',(-0.817861745233491,2.31141202226285,19.3855444374976));
#5649=CARTESIAN_POINT('Ctrl Pts',(-0.89404389828307,2.28303379020035,19.3897690610833));
#5650=CARTESIAN_POINT('Ctrl Pts',(-0.968709589818176,2.25090026002804,19.3939936846689));
#5651=CARTESIAN_POINT('Ctrl Pts',(-1.04366915074293,2.21864025863844,19.3982349355372));
#5652=CARTESIAN_POINT('Ctrl Pts',(-1.11709982321787,2.18259543341046,19.4024761864055));
#5653=CARTESIAN_POINT('Ctrl Pts',(-1.1885975853881,2.14293864354759,19.4067174372738));
#5654=CARTESIAN_POINT('Ctrl Pts',(-1.25968652151896,2.10350861222711,19.4109344365608));
#5655=CARTESIAN_POINT('Ctrl Pts',(-1.32886418144413,2.0605080386378,19.4151514358477));
#5656=CARTESIAN_POINT('Ctrl Pts',(-1.39575553076662,2.0141541024297,19.4193684351347));
#5657=CARTESIAN_POINT('Ctrl Pts',(-1.46262470414334,1.9678155335656,19.4235840363941));
#5658=CARTESIAN_POINT('Ctrl Pts',(-1.52720869015421,1.91812607443534,19.4277996376536));
#5659=CARTESIAN_POINT('Ctrl Pts',(-1.58916099329976,1.86534650598073,19.432015238913));
#5660=CARTESIAN_POINT('Ctrl Pts',(-1.65111175057533,1.81256825451267,19.4362307349823));
#5661=CARTESIAN_POINT('Ctrl Pts',(-1.71043060224302,1.75670034944633,19.4404462310516));
#5662=CARTESIAN_POINT('Ctrl Pts',(-1.76680485626834,1.6980432414596,19.4446617271209));
#5663=CARTESIAN_POINT('Ctrl Pts',(-1.8237764706109,1.63876458327692,19.4489218919865));
#5664=CARTESIAN_POINT('Ctrl Pts',(-1.87774036455189,1.5766375977102,19.4531820568521));
#5665=CARTESIAN_POINT('Ctrl Pts',(-1.92841401193,1.51200848165348,19.4574422217177));
#5666=CARTESIAN_POINT('Ctrl Pts',(-1.97862935773484,1.44796388293663,19.4616638568866));
#5667=CARTESIAN_POINT('Ctrl Pts',(-2.02561351182488,1.38146265077972,19.4658854920556));
#5668=CARTESIAN_POINT('Ctrl Pts',(-2.06913496047938,1.3128711914434,19.4701071272246));
#5669=CARTESIAN_POINT('Ctrl Pts',(-2.1132522214718,1.2433407091882,19.4743865569385));
#5670=CARTESIAN_POINT('Ctrl Pts',(-2.15381100609893,1.17166276615782,19.4786659866523));
#5671=CARTESIAN_POINT('Ctrl Pts',(-2.19061903077547,1.09824337557954,19.4829454163662));
#5672=CARTESIAN_POINT('Ctrl Pts',(-2.22742705545201,1.02482398500127,19.4872248460801));
#5673=CARTESIAN_POINT('Ctrl Pts',(-2.26048418261586,0.949663622313898,19.491504275794));
#5674=CARTESIAN_POINT('Ctrl Pts',(-2.28964990358747,0.873185873111714,19.4957837055079));
#5675=CARTESIAN_POINT('Ctrl Pts',(-2.32256423751001,0.786878588702949,19.5006131619352));
#5676=CARTESIAN_POINT('Ctrl Pts',(-2.35062682282925,0.698624244662392,19.5054426183624));
#5677=CARTESIAN_POINT('Ctrl Pts',(-2.37363404666324,0.608943070016463,19.5102720747896));
#5678=CARTESIAN_POINT('Ctrl Pts',(-2.39654583737175,0.519633889612662,19.5150814988077));
#5679=CARTESIAN_POINT('Ctrl Pts',(-2.41444399167664,0.428909874622092,19.5198909228258));
#5680=CARTESIAN_POINT('Ctrl Pts',(-2.42717418291908,0.337306590168482,19.5247003468439));
#5681=CARTESIAN_POINT('Ctrl Pts',(-2.43981461087022,0.246349219994555,19.5294758585883));
#5682=CARTESIAN_POINT('Ctrl Pts',(-2.44735958946859,0.154525137024291,19.5342513703327));
#5683=CARTESIAN_POINT('Ctrl Pts',(-2.44970596636029,0.0623773066010869,
19.5390268820771));
#5684=CARTESIAN_POINT('Ctrl Pts',(-2.45022115121846,0.0421447654799862,
19.5400754226374));
#5685=CARTESIAN_POINT('Ctrl Pts',(-2.45048590341901,0.0218966818193598,
19.5411239631978));
#5686=CARTESIAN_POINT('Ctrl Pts',(-2.45049945194367,0.00163890932561401,
19.5421725037581));
#5687=CARTESIAN_POINT('',(-2.45049932159731,-0.00182341742444998,20.3421725038169));
#5688=CARTESIAN_POINT('Ctrl Pts',(-2.45049945194406,0.00163890874735187,
19.542172503788));
#5689=CARTESIAN_POINT('Ctrl Pts',(-2.45055421052195,-0.0802362202537292,
19.5464103534165));
#5690=CARTESIAN_POINT('Ctrl Pts',(-2.44650126866438,-0.162135992966076,
19.5506482030451));
#5691=CARTESIAN_POINT('Ctrl Pts',(-2.43835979033724,-0.2436222134095,19.5548860526736));
#5692=CARTESIAN_POINT('Ctrl Pts',(-2.43021791027491,-0.325112454729847,
19.5591241114157));
#5693=CARTESIAN_POINT('Ctrl Pts',(-2.41798713907103,-0.406188647603719,
19.5633621701577));
#5694=CARTESIAN_POINT('Ctrl Pts',(-2.40173848544174,-0.486418027573028,
19.5676002288998));
#5695=CARTESIAN_POINT('Ctrl Pts',(-2.38548424781723,-0.566674979086692,
19.5718397440887));
#5696=CARTESIAN_POINT('Ctrl Pts',(-2.36520947641946,-0.646084091091731,
19.5760792592776));
#5697=CARTESIAN_POINT('Ctrl Pts',(-2.34103593495839,-0.724224413585654,
19.5803187744664));
#5698=CARTESIAN_POINT('Ctrl Pts',(-2.3168305613789,-0.802467632546112,19.5845638723189));
#5699=CARTESIAN_POINT('Ctrl Pts',(-2.28871630843004,-0.879438289975786,
19.5888089701714));
#5700=CARTESIAN_POINT('Ctrl Pts',(-2.25686416502947,-0.954732627810438,
19.5930540680238));
#5701=CARTESIAN_POINT('Ctrl Pts',(-2.22498765303189,-1.03008456984939,19.5973024136037));
#5702=CARTESIAN_POINT('Ctrl Pts',(-2.18936775799712,-1.10375722818418,19.6015507591836));
#5703=CARTESIAN_POINT('Ctrl Pts',(-2.1502216757483,-1.17537100319098,19.6057991047634));
#5704=CARTESIAN_POINT('Ctrl Pts',(-2.11100646740166,-1.2471112373613,19.6100549522831));
#5705=CARTESIAN_POINT('Ctrl Pts',(-2.06825288421315,-1.31678494323608,19.6143107998027));
#5706=CARTESIAN_POINT('Ctrl Pts',(-2.02222143977996,-1.38404143669699,19.6185666473224));
#5707=CARTESIAN_POINT('Ctrl Pts',(-2.00645504894737,-1.40707769321667,19.6200243325231));
#5708=CARTESIAN_POINT('Ctrl Pts',(-1.99030445809036,-1.42983066454289,19.6214820177239));
#5709=CARTESIAN_POINT('Ctrl Pts',(-1.97378117384991,-1.452287205671,19.6229397029246));
#5710=CARTESIAN_POINT('Ctrl Pts',(-1.92582494114591,-1.51746378294187,19.6271704048649));
#5711=CARTESIAN_POINT('Ctrl Pts',(-1.87454674116935,-1.58038502095654,19.6314011068051));
#5712=CARTESIAN_POINT('Ctrl Pts',(-1.82018633211568,-1.64069252645926,19.6356318087454));
#5713=CARTESIAN_POINT('Ctrl Pts',(-1.76590402401204,-1.70091338667074,19.6398564323311));
#5714=CARTESIAN_POINT('Ctrl Pts',(-1.70854861038336,-1.75852762992536,19.6440810559168));
#5715=CARTESIAN_POINT('Ctrl Pts',(-1.64840183330512,-1.81320755732936,19.6483056795025));
#5716=CARTESIAN_POINT('Ctrl Pts',(-1.58801833041233,-1.86810269410921,19.6525469303708));
#5717=CARTESIAN_POINT('Ctrl Pts',(-1.52482172567811,-1.92003998548926,19.6567881812391));
#5718=CARTESIAN_POINT('Ctrl Pts',(-1.45913655136522,-1.96872313301541,19.6610294321073));
#5719=CARTESIAN_POINT('Ctrl Pts',(-1.39382696656495,-2.01712790905449,19.6652464313943));
#5720=CARTESIAN_POINT('Ctrl Pts',(-1.32605757175241,-2.0623153751098,19.6694634306813));
#5721=CARTESIAN_POINT('Ctrl Pts',(-1.25618125472064,-2.10403396010817,19.6736804299682));
#5722=CARTESIAN_POINT('Ctrl Pts',(-1.1863281032167,-2.14573871448291,19.6778960312277));
#5723=CARTESIAN_POINT('Ctrl Pts',(-1.11436981556875,-2.18397663331378,19.6821116324871));
#5724=CARTESIAN_POINT('Ctrl Pts',(-1.04068716597744,-2.21854016699492,19.6863272337466));
#5725=CARTESIAN_POINT('Ctrl Pts',(-0.967006354958359,-2.25310283822671,
19.6905427298159));
#5726=CARTESIAN_POINT('Ctrl Pts',(-0.891601689044287,-2.28399111008071,
19.6947582258852));
#5727=CARTESIAN_POINT('Ctrl Pts',(-0.814876071390042,-2.31104462057225,
19.6989737219545));
#5728=CARTESIAN_POINT('Ctrl Pts',(-0.737337443611625,-2.33838479904505,
19.7032338868201));
#5729=CARTESIAN_POINT('Ctrl Pts',(-0.658450154460479,-2.36180828715453,
19.7074940516857));
#5730=CARTESIAN_POINT('Ctrl Pts',(-0.578646273066033,-2.38120111302401,
19.7117542165512));
#5731=CARTESIAN_POINT('Ctrl Pts',(-0.499564152315685,-2.40041854669144,
19.7159758517202));
#5732=CARTESIAN_POINT('Ctrl Pts',(-0.419582425747597,-2.41567790543166,
19.7201974868892));
#5733=CARTESIAN_POINT('Ctrl Pts',(-0.339130454725297,-2.42692002024744,
19.7244191220581));
#5734=CARTESIAN_POINT('Ctrl Pts',(-0.257577089370006,-2.4383160405722,19.728698551772));
#5735=CARTESIAN_POINT('Ctrl Pts',(-0.175540999423107,-2.44558394767281,
19.7329779814859));
#5736=CARTESIAN_POINT('Ctrl Pts',(-0.0934713727919753,-2.44871667460088,
19.7372574111998));
#5737=CARTESIAN_POINT('Ctrl Pts',(-0.011401746160844,-2.45184940152895,
19.7415368409136));
#5738=CARTESIAN_POINT('Ctrl Pts',(0.0707009274029293,-2.45084701976013,
19.7458162706275));
#5739=CARTESIAN_POINT('Ctrl Pts',(0.152392883928873,-2.44575686831865,19.7500957003414));
#5740=CARTESIAN_POINT('Ctrl Pts',(0.233154654091345,-2.44072467594267,19.7543264022816));
#5741=CARTESIAN_POINT('Ctrl Pts',(0.313818783242086,-2.43167844719997,19.7585571042219));
#5742=CARTESIAN_POINT('Ctrl Pts',(0.393954141627843,-2.41862572224275,19.7627878061621));
#5743=CARTESIAN_POINT('Ctrl Pts',(0.473974367553377,-2.40559175045975,19.7670124297478));
#5744=CARTESIAN_POINT('Ctrl Pts',(0.553466876399462,-2.38856278878793,19.7712370533335));
#5745=CARTESIAN_POINT('Ctrl Pts',(0.632003614358565,-2.36759829393369,19.7754616769192));
#5746=CARTESIAN_POINT('Ctrl Pts',(0.710849457380148,-2.34655128697543,19.7797029277875));
#5747=CARTESIAN_POINT('Ctrl Pts',(0.788731516292138,-2.32153773094152,19.7839441786558));
#5748=CARTESIAN_POINT('Ctrl Pts',(0.865224970328596,-2.2926700592802,19.7881854295241));
#5749=CARTESIAN_POINT('Ctrl Pts',(0.94128103283131,-2.26396745370647,19.792402428811));
#5750=CARTESIAN_POINT('Ctrl Pts',(1.01596388804196,-2.23145485462082,19.796619428098));
#5751=CARTESIAN_POINT('Ctrl Pts',(1.08887096805657,-2.19529275153077,19.8008364273849));
#5752=CARTESIAN_POINT('Ctrl Pts',(1.16175387777927,-2.15914263696897,19.8050520286444));
#5753=CARTESIAN_POINT('Ctrl Pts',(1.23286176508415,-2.11934562752396,19.8092676299038));
#5754=CARTESIAN_POINT('Ctrl Pts',(1.30181397541562,-2.07610949215415,19.8134832311632));
#5755=CARTESIAN_POINT('Ctrl Pts',(1.37076446521134,-2.03287443563761,19.8176987272325));
#5756=CARTESIAN_POINT('Ctrl Pts',(1.43755899154933,-1.98620067179778,19.8219142233018));
#5757=CARTESIAN_POINT('Ctrl Pts',(1.50184459234358,-1.93634012261492,19.8261297193711));
#5758=CARTESIAN_POINT('Ctrl Pts',(1.56681138471259,-1.88595123449461,19.8303898842367));
#5759=CARTESIAN_POINT('Ctrl Pts',(1.62921537143732,-1.83230790661755,19.8346500491023));
#5760=CARTESIAN_POINT('Ctrl Pts',(1.6887268024599,-1.7757116986306,19.8389102139679));
#5761=CARTESIAN_POINT('Ctrl Pts',(1.74770000140581,-1.71962735691929,19.8431318491369));
#5762=CARTESIAN_POINT('Ctrl Pts',(1.80383247632686,-1.66064371619423,19.8473534843058));
#5763=CARTESIAN_POINT('Ctrl Pts',(1.85684201911488,-1.59908973045586,19.8515751194748));
#5764=CARTESIAN_POINT('Ctrl Pts',(1.9105772670573,-1.53669306541155,19.8558545491887));
#5765=CARTESIAN_POINT('Ctrl Pts',(1.96110312556306,-1.47165553663221,19.8601339789026));
#5766=CARTESIAN_POINT('Ctrl Pts',(2.00817045738781,-1.40435097610064,19.8644134086165));
#5767=CARTESIAN_POINT('Ctrl Pts',(2.05523778921256,-1.33704641556908,19.8686928383304));
#5768=CARTESIAN_POINT('Ctrl Pts',(2.09884638929266,-1.2674752737454,19.8729722680443));
#5769=CARTESIAN_POINT('Ctrl Pts',(2.13879579919823,-1.19603627843473,19.8772516977581));
#5770=CARTESIAN_POINT('Ctrl Pts',(2.17829032470731,-1.12541072403208,19.8814823996984));
#5771=CARTESIAN_POINT('Ctrl Pts',(2.21435715494294,-1.05269401520356,19.8857131016387));
#5772=CARTESIAN_POINT('Ctrl Pts',(2.24676921058904,-0.978252709860344,19.8899438035789));
#5773=CARTESIAN_POINT('Ctrl Pts',(2.27913469902963,-0.903918356189735,19.8941684271646));
#5774=CARTESIAN_POINT('Ctrl Pts',(2.3078556573884,-0.827864749771428,19.8983930507503));
#5775=CARTESIAN_POINT('Ctrl Pts',(2.33275032093623,-0.750483970629553,19.9026176743359));
#5776=CARTESIAN_POINT('Ctrl Pts',(2.35774296495447,-0.67279863605048,19.9068589252042));
#5777=CARTESIAN_POINT('Ctrl Pts',(2.37887889886256,-0.593776073553013,19.9111001760725));
#5778=CARTESIAN_POINT('Ctrl Pts',(2.39602264893265,-0.513834327192877,19.9153414269408));
#5779=CARTESIAN_POINT('Ctrl Pts',(2.41306837059979,-0.434349689790429,19.9195584262278));
#5780=CARTESIAN_POINT('Ctrl Pts',(2.42616734086354,-0.353956811127188,19.9237754255147));
#5781=CARTESIAN_POINT('Ctrl Pts',(2.43523653745251,-0.273081044117545,19.9279924248017));
#5782=CARTESIAN_POINT('Ctrl Pts',(2.4443027274044,-0.192232089193979,19.9322080260611));
#5783=CARTESIAN_POINT('Ctrl Pts',(2.44934174488284,-0.110901025629182,19.9364236273205));
#5784=CARTESIAN_POINT('Ctrl Pts',(2.45032218231686,-0.0295203801798546,
19.94063922858));
#5785=CARTESIAN_POINT('Ctrl Pts',(2.45130259528643,0.0518582346122204,19.9448547246493));
#5786=CARTESIAN_POINT('Ctrl Pts',(2.44822462504793,0.133285963789158,19.9490702207186));
#5787=CARTESIAN_POINT('Ctrl Pts',(2.44110897904676,0.21432965827732,19.9532857167879));
#5788=CARTESIAN_POINT('Ctrl Pts',(2.43391793329751,0.296232118666215,19.9575458816535));
#5789=CARTESIAN_POINT('Ctrl Pts',(2.42260315950359,0.377741873167508,19.961806046519));
#5790=CARTESIAN_POINT('Ctrl Pts',(2.407239665619,0.458418413974113,19.9660662113846));
#5791=CARTESIAN_POINT('Ctrl Pts',(2.392015121934,0.538365301647637,19.9702878465536));
#5792=CARTESIAN_POINT('Ctrl Pts',(2.37281496915214,0.617493544058887,19.9745094817226));
#5793=CARTESIAN_POINT('Ctrl Pts',(2.34976298701108,0.695387773025081,19.9787311168915));
#5794=CARTESIAN_POINT('Ctrl Pts',(2.32639542127166,0.774348380618402,19.9830105466054));
#5795=CARTESIAN_POINT('Ctrl Pts',(2.29906992801884,0.852040464809562,19.9872899763193));
#5796=CARTESIAN_POINT('Ctrl Pts',(2.26796592344903,0.928052164522017,19.9915694060332));
#5797=CARTESIAN_POINT('Ctrl Pts',(2.23686191887921,1.00406386423447,19.9958488357471));
#5798=CARTESIAN_POINT('Ctrl Pts',(2.20197967069624,1.07839476317501,20.000128265461));
#5799=CARTESIAN_POINT('Ctrl Pts',(2.16354588173326,1.15066044845343,20.0044076951749));
#5800=CARTESIAN_POINT('Ctrl Pts',(2.12554971953229,1.22210327970922,20.0086383971151));
#5801=CARTESIAN_POINT('Ctrl Pts',(2.08393960868892,1.29179642615617,20.0128690990553));
#5802=CARTESIAN_POINT('Ctrl Pts',(2.03890079209274,1.35935051035544,20.0170998009956));
#5803=CARTESIAN_POINT('Ctrl Pts',(1.9939266838832,1.4268075379238,20.0213244245813));
#5804=CARTESIAN_POINT('Ctrl Pts',(1.94553390923101,1.49213122321264,20.0255490481669));
#5805=CARTESIAN_POINT('Ctrl Pts',(1.89395370278847,1.55495646938873,20.0297736717526));
#5806=CARTESIAN_POINT('Ctrl Pts',(1.84217048685824,1.61802898330412,20.0340149226209));
#5807=CARTESIAN_POINT('Ctrl Pts',(1.78717491795365,1.67858293021672,20.0382561734892));
#5808=CARTESIAN_POINT('Ctrl Pts',(1.72924512267837,1.73627807556655,20.0424974243575));
#5809=CARTESIAN_POINT('Ctrl Pts',(1.67164657145958,1.79364331859418,20.0467144236444));
#5810=CARTESIAN_POINT('Ctrl Pts',(1.61114759160327,1.84818203326596,20.0509314229314));
#5811=CARTESIAN_POINT('Ctrl Pts',(1.54806085253091,1.89959412687586,20.0551484222183));
#5812=CARTESIAN_POINT('Ctrl Pts',(1.48499502809271,1.95098917625198,20.0593640234777));
#5813=CARTESIAN_POINT('Ctrl Pts',(1.41934350830265,1.99925936940418,20.0635796247372));
#5814=CARTESIAN_POINT('Ctrl Pts',(1.35145293885435,2.04414412507091,20.0677952259966));
#5815=CARTESIAN_POINT('Ctrl Pts',(1.28356406345103,2.08902776074712,20.0720107220659));
#5816=CARTESIAN_POINT('Ctrl Pts',(1.21343663801286,2.13052587131964,20.0762262181352));
#5817=CARTESIAN_POINT('Ctrl Pts',(1.14144604713833,2.16842135468923,20.0804417142045));
#5818=CARTESIAN_POINT('Ctrl Pts',(1.06869262005518,2.2067183911855,20.0847018790701));
#5819=CARTESIAN_POINT('Ctrl Pts',(0.994036728186423,2.24133575668558,20.0889620439356));
#5820=CARTESIAN_POINT('Ctrl Pts',(0.917889341979701,2.27209801854587,20.0932222088012));
#5821=CARTESIAN_POINT('Ctrl Pts',(0.842430646418192,2.30258206098165,20.0974438439702));
#5822=CARTESIAN_POINT('Ctrl Pts',(0.765507791157719,2.32928035591761,20.1016654791391));
#5823=CARTESIAN_POINT('Ctrl Pts',(0.68753701593911,2.35207208684461,20.1058871143081));
#5824=CARTESIAN_POINT('Ctrl Pts',(0.608498814168257,2.37517583850879,20.110166544022));
#5825=CARTESIAN_POINT('Ctrl Pts',(0.528384264147741,2.39426513924305,20.1144459737359));
#5826=CARTESIAN_POINT('Ctrl Pts',(0.447636779230287,2.40926784809833,20.1187254034498));
#5827=CARTESIAN_POINT('Ctrl Pts',(0.366889294312832,2.4242705569536,20.1230048331637));
#5828=CARTESIAN_POINT('Ctrl Pts',(0.285509369438124,2.43518667361783,20.1272842628776));
#5829=CARTESIAN_POINT('Ctrl Pts',(0.203942942235041,2.4419986745108,20.1315636925915));
#5830=CARTESIAN_POINT('Ctrl Pts',(0.123305272055105,2.44873311048046,20.1357943945318));
#5831=CARTESIAN_POINT('Ctrl Pts',(0.0421820279336449,2.4514817918581,20.1400250964721));
#5832=CARTESIAN_POINT('Ctrl Pts',(-0.0389991254234243,2.45018964943863,
20.1442557984123));
#5833=CARTESIAN_POINT('Ctrl Pts',(-0.120063643800722,2.44889936347227,20.148480421998));
#5834=CARTESIAN_POINT('Ctrl Pts',(-0.201185445118454,2.44357979119288,20.1527050455837));
#5835=CARTESIAN_POINT('Ctrl Pts',(-0.281932378287374,2.43422767712333,20.1569296691694));
#5836=CARTESIAN_POINT('Ctrl Pts',(-0.362997115409843,2.42483875498307,20.1611709200377));
#5837=CARTESIAN_POINT('Ctrl Pts',(-0.443683554332787,2.4113854409016,20.1654121709059));
#5838=CARTESIAN_POINT('Ctrl Pts',(-0.52355505925226,2.39391736489198,20.1696534217742));
#5839=CARTESIAN_POINT('Ctrl Pts',(-0.60296985685643,2.37654917178936,20.1738704210612));
#5840=CARTESIAN_POINT('Ctrl Pts',(-0.681578555905518,2.35521210555354,20.1780874203482));
#5841=CARTESIAN_POINT('Ctrl Pts',(-0.758959568270523,2.33000657160675,20.1823044196351));
#5842=CARTESIAN_POINT('Ctrl Pts',(-0.836314927137037,2.30480939384589,20.1865200208946));
#5843=CARTESIAN_POINT('Ctrl Pts',(-0.912442965719734,2.2757464390876,20.190735622154));
#5844=CARTESIAN_POINT('Ctrl Pts',(-0.986936920277564,2.24296807052464,20.1949512234135));
#5845=CARTESIAN_POINT('Ctrl Pts',(-1.06142901601894,2.21019051986659,20.1991667194828));
#5846=CARTESIAN_POINT('Ctrl Pts',(-1.13428668356774,2.17369792802846,20.2033822155521));
#5847=CARTESIAN_POINT('Ctrl Pts',(-1.20512415503216,2.13368836078702,20.2075977116214));
#5848=CARTESIAN_POINT('Ctrl Pts',(-1.27671224386866,2.09325483888431,20.211857876487));
#5849=CARTESIAN_POINT('Ctrl Pts',(-1.34623663860525,2.04922958793242,20.2161180413525));
#5850=CARTESIAN_POINT('Ctrl Pts',(-1.41332733865816,2.00186315311548,20.2203782062181));
#5851=CARTESIAN_POINT('Ctrl Pts',(-1.47981125836325,1.954925108847,20.2245998413871));
#5852=CARTESIAN_POINT('Ctrl Pts',(-1.54390499578371,1.90470641275263,20.2288214765561));
#5853=CARTESIAN_POINT('Ctrl Pts',(-1.60528161640392,1.85149161003652,20.233043111725));
#5854=CARTESIAN_POINT('Ctrl Pts',(-1.66749848818651,1.7975482921401,20.2373225414389));
#5855=CARTESIAN_POINT('Ctrl Pts',(-1.72692292784225,1.74052655506493,20.2416019711528));
#5856=CARTESIAN_POINT('Ctrl Pts',(-1.78325421308347,1.68076014395869,20.2458814008667));
#5857=CARTESIAN_POINT('Ctrl Pts',(-1.8395854983247,1.62099373285245,20.2501608305806));
#5858=CARTESIAN_POINT('Ctrl Pts',(-1.89282336092282,1.55848306367045,20.2544402602945));
#5859=CARTESIAN_POINT('Ctrl Pts',(-1.94271163188089,1.49359357435504,20.2587196900084));
#5860=CARTESIAN_POINT('Ctrl Pts',(-1.99209745833045,1.42935761275148,20.262956019893));
#5861=CARTESIAN_POINT('Ctrl Pts',(-2.03838923801818,1.3625456306175,20.2671923497777));
#5862=CARTESIAN_POINT('Ctrl Pts',(-2.08130749356415,1.29348728916589,20.2714286796623));
#5863=CARTESIAN_POINT('Ctrl Pts',(-2.1241647396303,1.22452711604464,20.2756589874876));
#5864=CARTESIAN_POINT('Ctrl Pts',(-2.16365774029402,1.15332731246913,20.2798892953129));
#5865=CARTESIAN_POINT('Ctrl Pts',(-2.19954791923293,1.08024960124876,20.2841196031382));
#5866=CARTESIAN_POINT('Ctrl Pts',(-2.23539796364722,1.007253609855,20.2883451803826));
#5867=CARTESIAN_POINT('Ctrl Pts',(-2.26765298493047,0.932384294424062,20.292570757627));
#5868=CARTESIAN_POINT('Ctrl Pts',(-2.29611906075136,0.856030086418862,20.2967963348715));
#5869=CARTESIAN_POINT('Ctrl Pts',(-2.32456236915141,0.779736947188911,20.3010185324616));
#5870=CARTESIAN_POINT('Ctrl Pts',(-2.34922259155999,0.701961707252038,20.3052407300517));
#5871=CARTESIAN_POINT('Ctrl Pts',(-2.36995348616987,0.623113732308394,20.3094629276419));
#5872=CARTESIAN_POINT('Ctrl Pts',(-2.39067451838823,0.54430326802761,20.313683116589));
#5873=CARTESIAN_POINT('Ctrl Pts',(-2.4074698210759,0.46442153025925,20.3179033055362));
#5874=CARTESIAN_POINT('Ctrl Pts',(-2.42024309441087,0.383892711517824,20.3221234944834));
#5875=CARTESIAN_POINT('Ctrl Pts',(-2.43301721239666,0.303358567693985,20.3263439624965));
#5876=CARTESIAN_POINT('Ctrl Pts',(-2.44176868987456,0.222177713509171,20.3305644305097));
#5877=CARTESIAN_POINT('Ctrl Pts',(-2.44645260879332,0.14078310597631,20.3347848985228));
#5878=CARTESIAN_POINT('Ctrl Pts',(-2.44918555562594,0.0932914352820124,
20.3372474336112));
#5879=CARTESIAN_POINT('Ctrl Pts',(-2.45053470395961,0.0457271215552733,
20.3397099686996));
#5880=CARTESIAN_POINT('Ctrl Pts',(-2.45049932159773,-0.0018234168666027,
20.342172503788));
#5881=CARTESIAN_POINT('',(-2.45075217663585,-0.000775521780153733,21.142172503788));
#5882=CARTESIAN_POINT('Ctrl Pts',(-2.45049932159731,-0.00182341742446744,
20.3421725038169));
#5883=CARTESIAN_POINT('Ctrl Pts',(-2.45042940194528,-0.0957887692889192,
20.3470387573598));
#5884=CARTESIAN_POINT('Ctrl Pts',(-2.44495079787555,-0.189533578807969,
20.3519050109027));
#5885=CARTESIAN_POINT('Ctrl Pts',(-2.43416311526865,-0.282489253363092,
20.3567712644456));
#5886=CARTESIAN_POINT('Ctrl Pts',(-2.4232718287915,-0.376337665311091,20.3616842530213));
#5887=CARTESIAN_POINT('Ctrl Pts',(-2.40696909966942,-0.469381553096781,
20.366597241597));
#5888=CARTESIAN_POINT('Ctrl Pts',(-2.38540708047413,-0.561055532388618,
20.3715102301727));
#5889=CARTESIAN_POINT('Ctrl Pts',(-2.36439147661448,-0.650406349470546,
20.3762987159235));
#5890=CARTESIAN_POINT('Ctrl Pts',(-2.338380089688,-0.7384557897747,20.3810872016743));
#5891=CARTESIAN_POINT('Ctrl Pts',(-2.30755712572132,-0.824700164625149,
20.385875687425));
#5892=CARTESIAN_POINT('Ctrl Pts',(-2.28032455570955,-0.900898416641911,
20.3901063893653));
#5893=CARTESIAN_POINT('Ctrl Pts',(-2.24926248145955,-0.975889639657493,
20.3943370913055));
#5894=CARTESIAN_POINT('Ctrl Pts',(-2.21449771314159,-1.04926170638724,20.3985677932458));
#5895=CARTESIAN_POINT('Ctrl Pts',(-2.17978289222991,-1.12252835764599,20.4027924168314));
#5896=CARTESIAN_POINT('Ctrl Pts',(-2.14137614001279,-1.19418005603748,20.4070170404171));
#5897=CARTESIAN_POINT('Ctrl Pts',(-2.0994532936976,-1.26382202765355,20.4112416640028));
#5898=CARTESIAN_POINT('Ctrl Pts',(-2.05736544735351,-1.33373809629161,20.4154829148711));
#5899=CARTESIAN_POINT('Ctrl Pts',(-2.01173392995459,-1.40162813757682,20.4197241657394));
#5900=CARTESIAN_POINT('Ctrl Pts',(-1.96278458077881,-1.46711517593437,20.4239654166076));
#5901=CARTESIAN_POINT('Ctrl Pts',(-1.91411512523816,-1.53222775772554,20.4281824158946));
#5902=CARTESIAN_POINT('Ctrl Pts',(-1.86216595908491,-1.59496436663692,20.4323994151815));
#5903=CARTESIAN_POINT('Ctrl Pts',(-1.80720292121011,-1.65498273452313,20.4366164144685));
#5904=CARTESIAN_POINT('Ctrl Pts',(-1.75225810478478,-1.71498120500737,20.4408320157279));
#5905=CARTESIAN_POINT('Ctrl Pts',(-1.69430171464561,-1.77226288130747,20.4450476169874));
#5906=CARTESIAN_POINT('Ctrl Pts',(-1.63363893730903,-1.82651966113366,20.4492632182468));
#5907=CARTESIAN_POINT('Ctrl Pts',(-1.57297767366546,-1.88077508711303,20.4534787143161));
#5908=CARTESIAN_POINT('Ctrl Pts',(-1.50961050445715,-1.93200545746302,20.4576942103854));
#5909=CARTESIAN_POINT('Ctrl Pts',(-1.44387735730175,-1.97994152112413,20.4619097064547));
#5910=CARTESIAN_POINT('Ctrl Pts',(-1.3774476798894,-2.02838553123513,20.4661698713203));
#5911=CARTESIAN_POINT('Ctrl Pts',(-1.30860196654479,-2.07346470535092,20.4704300361859));
#5912=CARTESIAN_POINT('Ctrl Pts',(-1.23772139805952,-2.11494586001287,20.4746902010515));
#5913=CARTESIAN_POINT('Ctrl Pts',(-1.16748188617345,-2.15605185165756,20.4789118362204));
#5914=CARTESIAN_POINT('Ctrl Pts',(-1.09524462394142,-2.19362448211044,20.4831334713894));
#5915=CARTESIAN_POINT('Ctrl Pts',(-1.02140392707523,-2.22748384231071,20.4873551065583));
#5916=CARTESIAN_POINT('Ctrl Pts',(-0.946552344781212,-2.26180674003535,
20.4916345362722));
#5917=CARTESIAN_POINT('Ctrl Pts',(-0.870053552593081,-2.29231374449783,
20.4959139659862));
#5918=CARTESIAN_POINT('Ctrl Pts',(-0.792335812250154,-2.31886916634507,
20.5001933957001));
#5919=CARTESIAN_POINT('Ctrl Pts',(-0.714618071907238,-2.34542458819231,
20.504472825414));
#5920=CARTESIAN_POINT('Ctrl Pts',(-0.635681873070596,-2.36802835533114,
20.5087522551279));
#5921=CARTESIAN_POINT('Ctrl Pts',(-0.55596589658677,-2.3865984521558,20.5130316848418));
#5922=CARTESIAN_POINT('Ctrl Pts',(-0.477157606948787,-2.40495710036806,
20.517262386782));
#5923=CARTESIAN_POINT('Ctrl Pts',(-0.397290797063437,-2.41944256428234,
20.5214930887223));
#5924=CARTESIAN_POINT('Ctrl Pts',(-0.316780622574167,-2.42993832990912,
20.5257237906625));
#5925=CARTESIAN_POINT('Ctrl Pts',(-0.236386119052694,-2.44041901600868,
20.5299484142482));
#5926=CARTESIAN_POINT('Ctrl Pts',(-0.155350543958637,-2.44692132847492,
20.5341730378339));
#5927=CARTESIAN_POINT('Ctrl Pts',(-0.0741010067723045,-2.44937936849222,
20.5383976614195));
#5928=CARTESIAN_POINT('Ctrl Pts',(0.00746831251776109,-2.45184708286871,
20.5426389122878));
#5929=CARTESIAN_POINT('Ctrl Pts',(0.0892528195580796,-2.45023851393666,
20.5468801631561));
#5930=CARTESIAN_POINT('Ctrl Pts',(0.170813297237658,-2.44453943872599,20.5511214140244));
#5931=CARTESIAN_POINT('Ctrl Pts',(0.251907410012081,-2.43887295097369,20.5553384133114));
#5932=CARTESIAN_POINT('Ctrl Pts',(0.332779579891918,-2.42916264198655,20.5595554125983));
#5933=CARTESIAN_POINT('Ctrl Pts',(0.412998114034193,-2.41544670978355,20.5637724118853));
#5934=CARTESIAN_POINT('Ctrl Pts',(0.493190053977476,-2.40173532471214,20.5679880131447));
#5935=CARTESIAN_POINT('Ctrl Pts',(0.572728330457082,-2.38402103182902,20.5722036144041));
#5936=CARTESIAN_POINT('Ctrl Pts',(0.651188672559655,-2.36239360876421,20.5764192156636));
#5937=CARTESIAN_POINT('Ctrl Pts',(0.729647056874019,-2.34076672535947,20.5806347117328));
#5938=CARTESIAN_POINT('Ctrl Pts',(0.807027112238553,-2.31522703054067,20.5848502078021));
#5939=CARTESIAN_POINT('Ctrl Pts',(0.882918422960261,-2.28591454529634,20.5890657038714));
#5940=CARTESIAN_POINT('Ctrl Pts',(0.959613903213687,-2.25629145522376,20.593325868737));
#5941=CARTESIAN_POINT('Ctrl Pts',(1.03478844276558,-2.22281530269604,20.5975860336026));
#5942=CARTESIAN_POINT('Ctrl Pts',(1.10803961507263,-2.18568032004447,20.6018461984682));
#5943=CARTESIAN_POINT('Ctrl Pts',(1.1806282906134,-2.14888119284951,20.6060678336371));
#5944=CARTESIAN_POINT('Ctrl Pts',(1.25132787185416,-2.10848943841504,20.6102894688061));
#5945=CARTESIAN_POINT('Ctrl Pts',(1.31977361170098,-2.06473917574539,20.6145111039751));
#5946=CARTESIAN_POINT('Ctrl Pts',(1.38915637955478,-2.02038996825425,20.618790533689));
#5947=CARTESIAN_POINT('Ctrl Pts',(1.45622272539164,-1.9725898868357,20.6230699634029));
#5948=CARTESIAN_POINT('Ctrl Pts',(1.52062670138809,-1.92162553194569,20.6273493931168));
#5949=CARTESIAN_POINT('Ctrl Pts',(1.58503067738455,-1.87066117705569,20.6316288228307));
#5950=CARTESIAN_POINT('Ctrl Pts',(1.64677195781943,-1.81653292134836,20.6359082525446));
#5951=CARTESIAN_POINT('Ctrl Pts',(1.70554408044806,-1.7595651848251,20.6401876822585));
#5952=CARTESIAN_POINT('Ctrl Pts',(1.76364699365394,-1.70324611206228,20.6444183841988));
#5953=CARTESIAN_POINT('Ctrl Pts',(1.81906659342486,-1.64394009257578,20.648649086139));
#5954=CARTESIAN_POINT('Ctrl Pts',(1.87148014956412,-1.58193308954186,20.6528797880793));
#5955=CARTESIAN_POINT('Ctrl Pts',(1.92381840184519,-1.5200151735096,20.657104411665));
#5956=CARTESIAN_POINT('Ctrl Pts',(1.97315889030846,-1.45540433311518,20.6613290352506));
#5957=CARTESIAN_POINT('Ctrl Pts',(2.01921496789655,-1.38842398546789,20.6655536588363));
#5958=CARTESIAN_POINT('Ctrl Pts',(2.06545231309406,-1.32118001642399,20.6697949097046));
#5959=CARTESIAN_POINT('Ctrl Pts',(2.10837899763112,-1.25154817858745,20.6740361605729));
#5960=CARTESIAN_POINT('Ctrl Pts',(2.14774526609161,-1.17989004656411,20.6782774114412));
#5961=CARTESIAN_POINT('Ctrl Pts',(2.18688643721854,-1.1086416575791,20.6824944107281));
#5962=CARTESIAN_POINT('Ctrl Pts',(2.22250757270814,-1.0353904960309,20.6867114100151));
#5963=CARTESIAN_POINT('Ctrl Pts',(2.25440706421301,-0.960520191784876,20.690928409302));
#5964=CARTESIAN_POINT('Ctrl Pts',(2.28629598033859,-0.88567470868263,20.6951440105615));
#5965=CARTESIAN_POINT('Ctrl Pts',(2.31446552046467,-0.80921157634547,20.6993596118209));
#5966=CARTESIAN_POINT('Ctrl Pts',(2.33876146051047,-0.731536110408039,20.7035752130803));
#5967=CARTESIAN_POINT('Ctrl Pts',(2.36305679430983,-0.653862582674075,20.7077907091496));
#5968=CARTESIAN_POINT('Ctrl Pts',(2.38347858240881,-0.574977225664457,20.712006205219));
#5969=CARTESIAN_POINT('Ctrl Pts',(2.39992234458874,-0.495300908482584,20.7162217012882));
#5970=CARTESIAN_POINT('Ctrl Pts',(2.41654035033359,-0.414780314583919,20.7204818661538));
#5971=CARTESIAN_POINT('Ctrl Pts',(2.42909540951905,-0.333452369363806,20.7247420310194));
#5972=CARTESIAN_POINT('Ctrl Pts',(2.437532945941,-0.25176057565112,20.729002195885));
#5973=CARTESIAN_POINT('Ctrl Pts',(2.44589417176728,-0.170807617201268,20.733223831054));
#5974=CARTESIAN_POINT('Ctrl Pts',(2.4502120911814,-0.0894978380484811,20.7374454662229));
#5975=CARTESIAN_POINT('Ctrl Pts',(2.45048606309993,-0.00826465685841186,
20.7416671013919));
#5976=CARTESIAN_POINT('Ctrl Pts',(2.45076378571736,0.0740806134990697,20.7459465311058));
#5977=CARTESIAN_POINT('Ctrl Pts',(2.44688602179799,0.156346678644228,20.7502259608197));
#5978=CARTESIAN_POINT('Ctrl Pts',(2.43890643258138,0.238087511459872,20.7545053905336));
#5979=CARTESIAN_POINT('Ctrl Pts',(2.43092684336478,0.319828344275527,20.7587848202475));
#5980=CARTESIAN_POINT('Ctrl Pts',(2.4188455658134,0.401043469149773,20.7630642499614));
#5981=CARTESIAN_POINT('Ctrl Pts',(2.40276943619427,0.4812995808129,20.7673436796753));
#5982=CARTESIAN_POINT('Ctrl Pts',(2.38687635760234,0.560641855375478,20.7715743816155));
#5983=CARTESIAN_POINT('Ctrl Pts',(2.36701920340017,0.639345282321904,20.7758050835558));
#5984=CARTESIAN_POINT('Ctrl Pts',(2.34326366932778,0.716983699960119,20.780035785496));
#5985=CARTESIAN_POINT('Ctrl Pts',(2.31954226542135,0.794510572554981,20.7842604090817));
#5986=CARTESIAN_POINT('Ctrl Pts',(2.29193374025465,0.870975033819044,20.7884850326674));
#5987=CARTESIAN_POINT('Ctrl Pts',(2.2605548150828,0.945960981228063,20.7927096562531));
#5988=CARTESIAN_POINT('Ctrl Pts',(2.2290523886697,1.02124205849034,20.7969509071214));
#5989=CARTESIAN_POINT('Ctrl Pts',(2.19374991270405,1.09503249334827,20.8011921579897));
#5990=CARTESIAN_POINT('Ctrl Pts',(2.15481616321484,1.16692654128188,20.805433408858));
#5991=CARTESIAN_POINT('Ctrl Pts',(2.11610503790453,1.23840949720407,20.8096504081449));
#5992=CARTESIAN_POINT('Ctrl Pts',(2.07380427750083,1.30801728147431,20.8138674074319));
#5993=CARTESIAN_POINT('Ctrl Pts',(2.02812726855146,1.37537268860408,20.8180844067189));
#5994=CARTESIAN_POINT('Ctrl Pts',(1.98246540252982,1.44270576594285,20.8223000079783));
#5995=CARTESIAN_POINT('Ctrl Pts',(1.93342977151677,1.50778756438828,20.8265156092377));
#5996=CARTESIAN_POINT('Ctrl Pts',(1.88127764893699,1.57026897619806,20.8307312104972));
#5997=CARTESIAN_POINT('Ctrl Pts',(1.82912682768737,1.63274882893525,20.8349467065665));
#5998=CARTESIAN_POINT('Ctrl Pts',(1.77385996832765,1.69262806770978,20.8391622026358));
#5999=CARTESIAN_POINT('Ctrl Pts',(1.71577435289462,1.74959098647343,20.8433776987051));
#6000=CARTESIAN_POINT('Ctrl Pts',(1.65707324299081,1.8071575032411,20.8476378635707));
#6001=CARTESIAN_POINT('Ctrl Pts',(1.59549361899103,1.86174517669302,20.8518980284363));
#6002=CARTESIAN_POINT('Ctrl Pts',(1.53137881103169,1.91306800378951,20.8561581933018));
#6003=CARTESIAN_POINT('Ctrl Pts',(1.46784386891713,1.96392665801488,20.8603798284708));
#6004=CARTESIAN_POINT('Ctrl Pts',(1.40181983312183,2.01157905891197,20.8646014636398));
#6005=CARTESIAN_POINT('Ctrl Pts',(1.33367075655938,2.055790009485,20.8688230988088));
#6006=CARTESIAN_POINT('Ctrl Pts',(1.26458871333628,2.10060621173568,20.8731025285226));
#6007=CARTESIAN_POINT('Ctrl Pts',(1.19332343285252,2.1418857747785,20.8773819582365));
#6008=CARTESIAN_POINT('Ctrl Pts',(1.12027896859314,2.17943233033923,20.8816613879504));
#6009=CARTESIAN_POINT('Ctrl Pts',(1.04723450433375,2.21697888589997,20.8859408176643));
#6010=CARTESIAN_POINT('Ctrl Pts',(0.972411330326129,2.25079229162891,20.8902202473782));
#6011=CARTESIAN_POINT('Ctrl Pts',(0.896231593656129,2.28072777431516,20.894499677092));
#6012=CARTESIAN_POINT('Ctrl Pts',(0.820919278397737,2.31032239629771,20.8987303790323));
#6013=CARTESIAN_POINT('Ctrl Pts',(0.74399788158306,2.33623831222166,20.9029610809726));
#6014=CARTESIAN_POINT('Ctrl Pts',(0.665861270312645,2.3583000272861,20.9071917829128));
#6015=CARTESIAN_POINT('Ctrl Pts',(0.587836919852729,2.38033004573645,20.9114164064985));
#6016=CARTESIAN_POINT('Ctrl Pts',(0.508601266212819,2.39851673566404,20.9156410300842));
#6017=CARTESIAN_POINT('Ctrl Pts',(0.428567344990767,2.41273294850623,20.9198656536698));
#6018=CARTESIAN_POINT('Ctrl Pts',(0.348218426089122,2.42700511354956,20.9241069045381));
#6019=CARTESIAN_POINT('Ctrl Pts',(0.267065384158193,2.43727530688718,20.9283481554064));
#6020=CARTESIAN_POINT('Ctrl Pts',(0.18554072929708,2.44346575334542,20.9325894062747));
#6021=CARTESIAN_POINT('Ctrl Pts',(0.10448223450514,2.44962080267191,20.9368064055617));
#6022=CARTESIAN_POINT('Ctrl Pts',(0.0230568334225161,2.45174259914223,20.9410234048486));
#6023=CARTESIAN_POINT('Ctrl Pts',(-0.0583028055937678,2.44980632558166,
20.9452404041356));
#6024=CARTESIAN_POINT('Ctrl Pts',(-0.139635472109807,2.44787069393813,20.949456005395));
#6025=CARTESIAN_POINT('Ctrl Pts',(-0.220901955293346,2.44187967493463,20.9536716066544));
#6026=CARTESIAN_POINT('Ctrl Pts',(-0.30166944930381,2.43186056207109,20.9578872079139));
#6027=CARTESIAN_POINT('Ctrl Pts',(-0.382434927956733,2.42184169921029,20.9621027039832));
#6028=CARTESIAN_POINT('Ctrl Pts',(-0.462700980802887,2.40779500065897,20.9663182000525));
#6029=CARTESIAN_POINT('Ctrl Pts',(-0.542041223590698,2.38979948153152,20.9705336961218));
#6030=CARTESIAN_POINT('Ctrl Pts',(-0.622222181939403,2.3716132759072,20.9747938609873));
#6031=CARTESIAN_POINT('Ctrl Pts',(-0.701457116992228,2.34939415684168,20.9790540258529));
#6032=CARTESIAN_POINT('Ctrl Pts',(-0.779319686538854,2.3232759362962,20.9833141907185));
#6033=CARTESIAN_POINT('Ctrl Pts',(-0.856478053014138,2.29739393363093,20.9875358258875));
#6034=CARTESIAN_POINT('Ctrl Pts',(-0.932288362688646,2.26768330319341,20.9917574610564));
#6035=CARTESIAN_POINT('Ctrl Pts',(-1.00635576935863,2.23432278676976,20.9959790962254));
#6036=CARTESIAN_POINT('Ctrl Pts',(-1.0814371651327,2.20050556203565,21.0002585259393));
#6037=CARTESIAN_POINT('Ctrl Pts',(-1.15472713540308,2.16293798578629,21.0045379556532));
#6038=CARTESIAN_POINT('Ctrl Pts',(-1.22584182272251,2.12185345291901,21.0088173853671));
#6039=CARTESIAN_POINT('Ctrl Pts',(-1.29695651004194,2.08076892005174,21.013096815081));
#6040=CARTESIAN_POINT('Ctrl Pts',(-1.36589553808481,2.03616775203882,21.0173762447949));
#6041=CARTESIAN_POINT('Ctrl Pts',(-1.43230863225167,1.98832649028709,21.0216556745088));
#6042=CARTESIAN_POINT('Ctrl Pts',(-1.49744651369032,1.94140383934071,21.0258529339321));
#6043=CARTESIAN_POINT('Ctrl Pts',(-1.56040816290392,1.89118166509473,21.0300501933555));
#6044=CARTESIAN_POINT('Ctrl Pts',(-1.62083593804574,1.83789039715087,21.0342474527789));
#6045=CARTESIAN_POINT('Ctrl Pts',(-1.68117667131803,1.78467589145055,21.0384386663516));
#6046=CARTESIAN_POINT('Ctrl Pts',(-1.73899042455939,1.72840137849704,21.0426298799243));
#6047=CARTESIAN_POINT('Ctrl Pts',(-1.79394951889461,1.66933980173534,21.046821093497));
#6048=CARTESIAN_POINT('Ctrl Pts',(-1.84884541217999,1.6103461437358,21.0510074873196));
#6049=CARTESIAN_POINT('Ctrl Pts',(-1.90089284763766,1.54857213380643,21.0551938811423));
#6050=CARTESIAN_POINT('Ctrl Pts',(-1.94979936015366,1.48432904207401,21.0593802749649));
#6051=CARTESIAN_POINT('Ctrl Pts',(-1.9986756118002,1.42012570070844,21.0635640784594));
#6052=CARTESIAN_POINT('Ctrl Pts',(-2.04441451086866,1.35345668447912,21.0677478819538));
#6053=CARTESIAN_POINT('Ctrl Pts',(-2.08676327369869,1.2846669955838,21.0719316854483));
#6054=CARTESIAN_POINT('Ctrl Pts',(-2.12909933263255,1.21589794240503,21.0761142338741));
#6055=CARTESIAN_POINT('Ctrl Pts',(-2.16804702656771,1.145009882353,21.0802967822999));
#6056=CARTESIAN_POINT('Ctrl Pts',(-2.20339726727559,1.07237620850262,21.0844793307257));
#6057=CARTESIAN_POINT('Ctrl Pts',(-2.23874817182219,0.999741170671587,21.0886619576952));
#6058=CARTESIAN_POINT('Ctrl Pts',(-2.27050128388474,0.92536088040813,21.0928445846646));
#6059=CARTESIAN_POINT('Ctrl Pts',(-2.29849448721701,0.849631297818651,21.0970272116341));
#6060=CARTESIAN_POINT('Ctrl Pts',(-2.32651476312671,0.773828476201683,21.1012138836745));
#6061=CARTESIAN_POINT('Ctrl Pts',(-2.35076770707166,0.696674202014863,21.1054005557149));
#6062=CARTESIAN_POINT('Ctrl Pts',(-2.37114045908625,0.618581581753182,21.1095872277552));
#6063=CARTESIAN_POINT('Ctrl Pts',(-2.39152389618704,0.540448003530648,21.1137760956183));
#6064=CARTESIAN_POINT('Ctrl Pts',(-2.40802299471514,0.461375563096551,21.1179649634814));
#6065=CARTESIAN_POINT('Ctrl Pts',(-2.42057614060237,0.38178711024148,21.1221538313445));
#6066=CARTESIAN_POINT('Ctrl Pts',(-2.43314987512159,0.302068122986412,21.1263495694423));
#6067=CARTESIAN_POINT('Ctrl Pts',(-2.4417646874607,0.221831904192904,21.1305453075402));
#6068=CARTESIAN_POINT('Ctrl Pts',(-2.44641093600422,0.141505414026922,21.134741045638));
#6069=CARTESIAN_POINT('Ctrl Pts',(-2.44915406890088,0.0940808659031447,
21.1372181983547));
#6070=CARTESIAN_POINT('Ctrl Pts',(-2.45051487677001,0.0466248548191888,
21.1396953510713));
#6071=CARTESIAN_POINT('Ctrl Pts',(-2.45049987730867,-0.000775441941961462,
21.142172503788));
#6072=CARTESIAN_POINT('',(-2.45034181611172,0.00225396750469473,21.942172503788));
#6073=CARTESIAN_POINT('Ctrl Pts',(-2.45424120969512,-0.000776625857978041,
21.142172503788));
#6074=CARTESIAN_POINT('Ctrl Pts',(-2.4544169492817,-0.0431881484021115,
21.1443855598339));
#6075=CARTESIAN_POINT('Ctrl Pts',(-2.45341298330889,-0.0855911780851724,
21.1465986158797));
#6076=CARTESIAN_POINT('Ctrl Pts',(-2.40888059246768,-0.938845702385758,
21.1911970043977));
#6077=CARTESIAN_POINT('Ctrl Pts',(-1.43961468312248,-2.51450512838468,21.2759676693421));
#6078=CARTESIAN_POINT('Ctrl Pts',(1.33466465959828,-2.57174973956534,21.403123666759));
#6079=CARTESIAN_POINT('Ctrl Pts',(2.8848211986208,-0.270246421845255,21.5302796641756));
#6080=CARTESIAN_POINT('Ctrl Pts',(1.78908808406994,2.27912051106948,21.6574356615925));
#6081=CARTESIAN_POINT('Ctrl Pts',(-0.947554232492991,2.73813211022012,21.7845916590091));
#6082=CARTESIAN_POINT('Ctrl Pts',(-2.3415517179439,1.2062176692426,21.879503939741));
#6083=CARTESIAN_POINT('Ctrl Pts',(-2.45213225552358,0.197415099304688,21.9320308880006));
#6084=CARTESIAN_POINT('Ctrl Pts',(-2.45034181611172,0.00225396750469473,
21.942172503788));
#6085=CARTESIAN_POINT('',(-2.45013029362686,-0.000414097013525958,22.742172523057));
#6086=CARTESIAN_POINT('Ctrl Pts',(-2.45034181611172,0.00225396750469473,
21.942172503788));
#6087=CARTESIAN_POINT('Ctrl Pts',(-2.44464938777012,-0.618231009799729,
21.9744162204729));
#6088=CARTESIAN_POINT('Ctrl Pts',(-1.89007733222012,-2.06341747834654,22.0490452696298));
#6089=CARTESIAN_POINT('Ctrl Pts',(0.540405455967006,-2.84660998728302,22.1660596512595));
#6090=CARTESIAN_POINT('Ctrl Pts',(2.68589067766831,-1.08683841676111,22.293215648676));
#6091=CARTESIAN_POINT('Ctrl Pts',(2.36794060637167,1.66975559925104,22.4203716460929));
#6092=CARTESIAN_POINT('Ctrl Pts',(-0.121828485691317,2.89488934099512,22.5475276435095));
#6093=CARTESIAN_POINT('Ctrl Pts',(-2.12790080642062,1.68857040030348,22.6547945960747));
#6094=CARTESIAN_POINT('Ctrl Pts',(-2.44587090828161,0.434202251858068,22.7196762161674));
#6095=CARTESIAN_POINT('Ctrl Pts',(-2.44652397570074,-0.000413115186416297,
22.742172503788));
#6096=CARTESIAN_POINT('',(-2.45049912112546,-0.00207541883967445,23.542172503788));
#6097=CARTESIAN_POINT('Ctrl Pts',(-2.45049996499496,-0.000414197657279032,
22.7421725250322));
#6098=CARTESIAN_POINT('Ctrl Pts',(-2.45048532431713,-0.0870322165490495,
22.7466487192745));
#6099=CARTESIAN_POINT('Ctrl Pts',(-2.44587388563628,-0.173537469021683,
22.7511249135167));
#6100=CARTESIAN_POINT('Ctrl Pts',(-2.43672683137232,-0.259446717593862,
22.7556011077589));
#6101=CARTESIAN_POINT('Ctrl Pts',(-2.42754837478386,-0.345650897192244,
22.7600926690144));
#6102=CARTESIAN_POINT('Ctrl Pts',(-2.41380320605056,-0.431254610293177,
22.7645842302699));
#6103=CARTESIAN_POINT('Ctrl Pts',(-2.39560398952757,-0.515782682299014,
22.7690757915254));
#6104=CARTESIAN_POINT('Ctrl Pts',(-2.37737168474098,-0.600464436037548,
22.7735755189546));
#6105=CARTESIAN_POINT('Ctrl Pts',(-2.35466927232878,-0.684066288703808,
22.7780752463837));
#6106=CARTESIAN_POINT('Ctrl Pts',(-2.32765907930728,-0.766128879835755,
22.7825749738129));
#6107=CARTESIAN_POINT('Ctrl Pts',(-2.30057021386355,-0.848430494169568,
22.7870878075703));
#6108=CARTESIAN_POINT('Ctrl Pts',(-2.26914861576414,-0.929183536036788,
22.7916006413278));
#6109=CARTESIAN_POINT('Ctrl Pts',(-2.23360485339984,-1.00794821735477,22.7961134750852));
#6110=CARTESIAN_POINT('Ctrl Pts',(-2.21857147695705,-1.04126205432324,22.7980221961712));
#6111=CARTESIAN_POINT('Ctrl Pts',(-2.20280124228042,-1.07422051047084,22.7999309172571));
#6112=CARTESIAN_POINT('Ctrl Pts',(-2.18631246248549,-1.10679178998611,22.8018396383431));
#6113=CARTESIAN_POINT('Ctrl Pts',(-2.14976489501527,-1.1789864005322,22.8060703402833));
#6114=CARTESIAN_POINT('Ctrl Pts',(-2.10956882614387,-1.24950456864088,22.8103010422236));
#6115=CARTESIAN_POINT('Ctrl Pts',(-2.06590160807848,-1.31795326007365,22.8145317441639));
#6116=CARTESIAN_POINT('Ctrl Pts',(-2.0222971277901,-1.38630360957098,22.8187563677495));
#6117=CARTESIAN_POINT('Ctrl Pts',(-1.97523165093686,-1.45258999872332,22.8229809913352));
#6118=CARTESIAN_POINT('Ctrl Pts',(-1.92492900182785,-1.51644274139251,22.8272056149209));
#6119=CARTESIAN_POINT('Ctrl Pts',(-1.87442837144414,-1.58054679582383,22.8314468657892));
#6120=CARTESIAN_POINT('Ctrl Pts',(-1.82066524674817,-1.64219758258895,22.8356881166575));
#6121=CARTESIAN_POINT('Ctrl Pts',(-1.76391083588765,-1.70104932704438,22.8399293675258));
#6122=CARTESIAN_POINT('Ctrl Pts',(-1.70748094820521,-1.7595645557144,22.8441463668127));
#6123=CARTESIAN_POINT('Ctrl Pts',(-1.6480942161064,-1.81531232708116,22.8483633660997));
#6124=CARTESIAN_POINT('Ctrl Pts',(-1.58605719311587,-1.86798630352725,22.8525803653866));
#6125=CARTESIAN_POINT('Ctrl Pts',(-1.52404073675561,-1.92064281739784,22.8567959666461));
#6126=CARTESIAN_POINT('Ctrl Pts',(-1.45937608854149,-1.97022725920252,22.8610115679055));
#6127=CARTESIAN_POINT('Ctrl Pts',(-1.39240456823055,-2.01647210949487,22.8652271691649));
#6128=CARTESIAN_POINT('Ctrl Pts',(-1.32543471903204,-2.06271580585875,22.8694426652342));
#6129=CARTESIAN_POINT('Ctrl Pts',(-1.25615849549141,-2.10561981303346,22.8736581613035));
#6130=CARTESIAN_POINT('Ctrl Pts',(-1.18494682731743,-2.14495950228212,22.8778736573728));
#6131=CARTESIAN_POINT('Ctrl Pts',(-1.11298057665873,-2.18471604794241,22.8821338222384));
#6132=CARTESIAN_POINT('Ctrl Pts',(-1.03903803618359,-2.22083204014725,22.886393987104));
#6133=CARTESIAN_POINT('Ctrl Pts',(-0.963526554605805,-2.25312379344089,
22.8906541519696));
#6134=CARTESIAN_POINT('Ctrl Pts',(-0.888698012437097,-2.2851234943148,22.8948757871385));
#6135=CARTESIAN_POINT('Ctrl Pts',(-0.812329257026773,-2.31336774702277,
22.8990974223075));
#6136=CARTESIAN_POINT('Ctrl Pts',(-0.734834006813902,-2.33772736486311,
22.9033190574765));
#6137=CARTESIAN_POINT('Ctrl Pts',(-0.656277840027232,-2.3624204679458,22.9075984871903));
#6138=CARTESIAN_POINT('Ctrl Pts',(-0.576564580054122,-2.38312164452855,
22.9118779169042));
#6139=CARTESIAN_POINT('Ctrl Pts',(-0.496136095112256,-2.39974982552906,
22.9161573466181));
#6140=CARTESIAN_POINT('Ctrl Pts',(-0.415707610170413,-2.41637800652957,
22.920436776332));
#6141=CARTESIAN_POINT('Ctrl Pts',(-0.334564395092533,-2.42893318165386,
22.9247162060459));
#6142=CARTESIAN_POINT('Ctrl Pts',(-0.253151943387779,-2.4373888371696,22.9289956357597));
#6143=CARTESIAN_POINT('Ctrl Pts',(-0.172666495462007,-2.44574821227058,
22.9332263377));
#6144=CARTESIAN_POINT('Ctrl Pts',(-0.0916151872469884,-2.45013243657524,
22.9374570396403));
#6145=CARTESIAN_POINT('Ctrl Pts',(-0.0104244858215312,-2.45047782689323,
22.9416877415805));
#6146=CARTESIAN_POINT('Ctrl Pts',(0.0706495669062312,-2.45082272098036,
22.9459123651662));
#6147=CARTESIAN_POINT('Ctrl Pts',(0.151862153987473,-2.44714030358704,22.9501369887519));
#6148=CARTESIAN_POINT('Ctrl Pts',(0.232781277887927,-2.43941860423029,22.9543616123376));
#6149=CARTESIAN_POINT('Ctrl Pts',(0.314018883450431,-2.43166651379259,22.9586028632059));
#6150=CARTESIAN_POINT('Ctrl Pts',(0.394960238836241,-2.41984322854105,22.9628441140742));
#6151=CARTESIAN_POINT('Ctrl Pts',(0.475167796108545,-2.40398956227795,22.9670853649425));
#6152=CARTESIAN_POINT('Ctrl Pts',(0.554916724509646,-2.38822654768547,22.9713023642294));
#6153=CARTESIAN_POINT('Ctrl Pts',(0.633939762958542,-2.36847920973697,22.9755193635164));
#6154=CARTESIAN_POINT('Ctrl Pts',(0.711813384088975,-2.34483943079943,22.9797363628034));
#6155=CARTESIAN_POINT('Ctrl Pts',(0.789661188410367,-2.32120748896578,22.9839519640628));
#6156=CARTESIAN_POINT('Ctrl Pts',(0.866359887472451,-2.29368580369894,22.9881675653222));
#6157=CARTESIAN_POINT('Ctrl Pts',(0.941499767728186,-2.26241650395496,22.9923831665817));
#6158=CARTESIAN_POINT('Ctrl Pts',(1.01663777304985,-2.23114798446076,22.996598662651));
#6159=CARTESIAN_POINT('Ctrl Pts',(1.09021660795235,-2.19613221609702,23.0008141587203));
#6160=CARTESIAN_POINT('Ctrl Pts',(1.16184658839672,-2.1575594441477,23.0050296547896));
#6161=CARTESIAN_POINT('Ctrl Pts',(1.23423558390143,-2.11857794229719,23.0092898196552));
#6162=CARTESIAN_POINT('Ctrl Pts',(1.30463374341914,-2.07596382114742,23.0135499845208));
#6163=CARTESIAN_POINT('Ctrl Pts',(1.37266608860179,-2.02996011271223,23.0178101493864));
#6164=CARTESIAN_POINT('Ctrl Pts',(1.44008313702903,-1.98437247008311,23.0220317845553));
#6165=CARTESIAN_POINT('Ctrl Pts',(1.50517665385351,-1.93545663745826,23.0262534197243));
#6166=CARTESIAN_POINT('Ctrl Pts',(1.56761403231989,-1.88349050851704,23.0304750548933));
#6167=CARTESIAN_POINT('Ctrl Pts',(1.63090618381365,-1.830812958846,23.0347544846072));
#6168=CARTESIAN_POINT('Ctrl Pts',(1.69146855702982,-1.77500129807639,23.039033914321));
#6169=CARTESIAN_POINT('Ctrl Pts',(1.74899375983996,-1.71638313847488,23.0433133440349));
#6170=CARTESIAN_POINT('Ctrl Pts',(1.8065189626501,-1.65776497887337,23.0475927737488));
#6171=CARTESIAN_POINT('Ctrl Pts',(1.86100671849117,-1.59634073090099,23.0518722034627));
#6172=CARTESIAN_POINT('Ctrl Pts',(1.91219354027986,-1.53247059172826,23.0561516331766));
#6173=CARTESIAN_POINT('Ctrl Pts',(1.96279752275772,-1.46932771059964,23.0603823351168));
#6174=CARTESIAN_POINT('Ctrl Pts',(2.01036573076248,-1.40355688444331,23.0646130370571));
#6175=CARTESIAN_POINT('Ctrl Pts',(2.05461372784418,-1.33548218983041,23.0688437389973));
#6176=CARTESIAN_POINT('Ctrl Pts',(2.09879815272924,-1.26750529982241,23.073068362583));
#6177=CARTESIAN_POINT('Ctrl Pts',(2.13967158932969,-1.19723150186965,23.0772929861687));
#6178=CARTESIAN_POINT('Ctrl Pts',(2.17699008478924,-1.12501752018773,23.0815176097543));
#6179=CARTESIAN_POINT('Ctrl Pts',(2.21445545846371,-1.05251931856092,23.0857588606226));
#6180=CARTESIAN_POINT('Ctrl Pts',(2.24833755111558,-0.978065998397429,23.0900001114909));
#6181=CARTESIAN_POINT('Ctrl Pts',(2.27843378361977,-0.902047528492861,23.0942413623592));
#6182=CARTESIAN_POINT('Ctrl Pts',(2.30835792509389,-0.82646373415073,23.0984583616461));
#6183=CARTESIAN_POINT('Ctrl Pts',(2.33453921131295,-0.749333077381762,23.1026753609331));
#6184=CARTESIAN_POINT('Ctrl Pts',(2.35682559033486,-0.671061388207306,23.10689236022));
#6185=CARTESIAN_POINT('Ctrl Pts',(2.37910458093457,-0.592815647810155,23.1111079614794));
#6186=CARTESIAN_POINT('Ctrl Pts',(2.39749110128002,-0.513430073130127,23.1153235627389));
#6187=CARTESIAN_POINT('Ctrl Pts',(2.41188282359221,-0.433326084214705,23.1195391639983));
#6188=CARTESIAN_POINT('Ctrl Pts',(2.42627418679377,-0.35322409410068,23.1237546600676));
#6189=CARTESIAN_POINT('Ctrl Pts',(2.43667086898207,-0.27240418331667,23.1279701561368));
#6190=CARTESIAN_POINT('Ctrl Pts',(2.44302184075576,-0.1912969827005,23.1321856522061));
#6191=CARTESIAN_POINT('Ctrl Pts',(2.44944010953551,-0.109330343251132,23.1364458170717));
#6192=CARTESIAN_POINT('Ctrl Pts',(2.45172636412338,-0.0270707710126519,
23.1407059819373));
#6193=CARTESIAN_POINT('Ctrl Pts',(2.44988191779356,0.0550348877364602,23.1449661468029));
#6194=CARTESIAN_POINT('Ctrl Pts',(2.4480541529678,0.136397968152651,23.1491877819719));
#6195=CARTESIAN_POINT('Ctrl Pts',(2.44217019982977,0.217609443384783,23.1534094171408));
#6196=CARTESIAN_POINT('Ctrl Pts',(2.43228362234344,0.298239216871039,23.1576310523097));
#6197=CARTESIAN_POINT('Ctrl Pts',(2.42226169676943,0.379972818822361,23.1619104820237));
#6198=CARTESIAN_POINT('Ctrl Pts',(2.40812680941357,0.461108184027478,23.1661899117376));
#6199=CARTESIAN_POINT('Ctrl Pts',(2.38998797701386,0.541209497079656,23.1704693414515));
#6200=CARTESIAN_POINT('Ctrl Pts',(2.37184914461414,0.621310810131857,23.1747487711654));
#6201=CARTESIAN_POINT('Ctrl Pts',(2.34970656253426,0.700377616280184,23.1790282008793));
#6202=CARTESIAN_POINT('Ctrl Pts',(2.32372041422682,0.777993371761954,23.1833076305932));
#6203=CARTESIAN_POINT('Ctrl Pts',(2.2980301574838,0.854725354587563,23.1875383325335));
#6204=CARTESIAN_POINT('Ctrl Pts',(2.26848683192573,0.930327787756541,23.1917690344737));
#6205=CARTESIAN_POINT('Ctrl Pts',(2.23520891010426,1.00438607028898,23.195999736414));
#6206=CARTESIAN_POINT('Ctrl Pts',(2.20197879949977,1.07833795144711,23.2002243599996));
#6207=CARTESIAN_POINT('Ctrl Pts',(2.16502493798028,1.1507496674678,23.2044489835853));
#6208=CARTESIAN_POINT('Ctrl Pts',(2.12451516514728,1.22122297843564,23.208673607171));
#6209=CARTESIAN_POINT('Ctrl Pts',(2.08384595386308,1.29197365841266,23.2129148580393));
#6210=CARTESIAN_POINT('Ctrl Pts',(2.03959293116593,1.36077019224979,23.2171561089076));
#6211=CARTESIAN_POINT('Ctrl Pts',(1.99197428751635,1.42723112629795,23.2213973597759));
#6212=CARTESIAN_POINT('Ctrl Pts',(1.94462792849352,1.49331203501919,23.2256143590628));
#6213=CARTESIAN_POINT('Ctrl Pts',(1.89395460707359,1.55708359966987,23.2298313583498));
#6214=CARTESIAN_POINT('Ctrl Pts',(1.84021320517734,1.61819826025458,23.2340483576367));
#6215=CARTESIAN_POINT('Ctrl Pts',(1.78648961973151,1.6792926599923,23.2382639588962));
#6216=CARTESIAN_POINT('Ctrl Pts',(1.72970028052972,1.73773155586434,23.2424795601556));
#6217=CARTESIAN_POINT('Ctrl Pts',(1.67014409817548,1.79320075321466,23.246695161415));
#6218=CARTESIAN_POINT('Ctrl Pts',(1.61058940190177,1.84866856646527,23.2509106574843));
#6219=CARTESIAN_POINT('Ctrl Pts',(1.54826834080045,1.90116651235743,23.2551261535536));
#6220=CARTESIAN_POINT('Ctrl Pts',(1.48351534306565,1.95041853890102,23.2593416496229));
#6221=CARTESIAN_POINT('Ctrl Pts',(1.41807620106281,2.00019245627414,23.2636018144885));
#6222=CARTESIAN_POINT('Ctrl Pts',(1.3501536521806,2.04665094891246,23.2678619793541));
#6223=CARTESIAN_POINT('Ctrl Pts',(1.28012409681148,2.08955319309239,23.2721221442197));
#6224=CARTESIAN_POINT('Ctrl Pts',(1.21072790132587,2.13206742166615,23.2763437793886));
#6225=CARTESIAN_POINT('Ctrl Pts',(1.13926310063557,2.17108929855892,23.2805654145576));
#6226=CARTESIAN_POINT('Ctrl Pts',(1.06612030182519,2.20643099870269,23.2847870497266));
#6227=CARTESIAN_POINT('Ctrl Pts',(0.991976171870974,2.24225652973078,23.2890664794405));
#6228=CARTESIAN_POINT('Ctrl Pts',(0.916108207728978,2.27430016473751,23.2933459091544));
#6229=CARTESIAN_POINT('Ctrl Pts',(0.838941847434474,2.30241760474142,23.2976253388683));
#6230=CARTESIAN_POINT('Ctrl Pts',(0.761775487139992,2.33053504474533,23.3019047685822));
#6231=CARTESIAN_POINT('Ctrl Pts',(0.683311218800494,2.35472620779236,23.3061841982961));
#6232=CARTESIAN_POINT('Ctrl Pts',(0.603985979936962,2.37490024759769,23.31046362801));
#6233=CARTESIAN_POINT('Ctrl Pts',(0.525563978780602,2.39484457547629,23.3146943299502));
#6234=CARTESIAN_POINT('Ctrl Pts',(0.446005557894012,2.41093785519662,23.3189250318905));
#6235=CARTESIAN_POINT('Ctrl Pts',(0.365723438613052,2.4230552235657,23.3231557338308));
#6236=CARTESIAN_POINT('Ctrl Pts',(0.285556662647317,2.43515518261062,23.3273803574164));
#6237=CARTESIAN_POINT('Ctrl Pts',(0.204668709248952,2.44329050640896,23.3316049810021));
#6238=CARTESIAN_POINT('Ctrl Pts',(0.123485271971385,2.44738669556042,23.3358296045878));
#6239=CARTESIAN_POINT('Ctrl Pts',(0.0419823127465615,2.45149900650197,23.3400708554561));
#6240=CARTESIAN_POINT('Ctrl Pts',(-0.0398180013644822,2.45154020316717,
23.3443121063244));
#6241=CARTESIAN_POINT('Ctrl Pts',(-0.121476829436484,2.44748720730264,23.3485533571927));
#6242=CARTESIAN_POINT('Ctrl Pts',(-0.202668730233576,2.44345738657249,23.3527703564796));
#6243=CARTESIAN_POINT('Ctrl Pts',(-0.283720289484594,2.43538009094083,23.3569873557666));
#6244=CARTESIAN_POINT('Ctrl Pts',(-0.364199131769934,2.42328480423124,23.3612043550536));
#6245=CARTESIAN_POINT('Ctrl Pts',(-0.444651293558449,2.4111935273738,23.365419956313));
#6246=CARTESIAN_POINT('Ctrl Pts',(-0.524530655896258,2.39508697373109,23.3696355575725));
#6247=CARTESIAN_POINT('Ctrl Pts',(-0.603411223520832,2.37504634593287,23.3738511588319));
#6248=CARTESIAN_POINT('Ctrl Pts',(-0.682289822871506,2.35500621820008,23.3780666549012));
#6249=CARTESIAN_POINT('Ctrl Pts',(-0.760169226587464,2.33103232705677,23.3822821509705));
#6250=CARTESIAN_POINT('Ctrl Pts',(-0.836636278495167,2.30325638770541,23.3864976470398));
#6251=CARTESIAN_POINT('Ctrl Pts',(-0.913913600678824,2.27518612527656,23.3907578119054));
#6252=CARTESIAN_POINT('Ctrl Pts',(-0.989748000478733,2.24323290960372,23.395017976771));
#6253=CARTESIAN_POINT('Ctrl Pts',(-1.0637332159061,2.20758281733168,23.3992781416365));
#6254=CARTESIAN_POINT('Ctrl Pts',(-1.13704929574981,2.17225515090055,23.4034997768055));
#6255=CARTESIAN_POINT('Ctrl Pts',(-1.20854912200814,2.13329748850934,23.4077214119745));
#6256=CARTESIAN_POINT('Ctrl Pts',(-1.27786330003922,2.09093654528608,23.4119430471435));
#6257=CARTESIAN_POINT('Ctrl Pts',(-1.34812639506922,2.04799567714332,23.4162224768573));
#6258=CARTESIAN_POINT('Ctrl Pts',(-1.41614313681858,2.00155791913076,23.4205019065712));
#6259=CARTESIAN_POINT('Ctrl Pts',(-1.48156186764085,1.95190283629912,23.4247813362851));
#6260=CARTESIAN_POINT('Ctrl Pts',(-1.54698059846309,1.90224775346751,23.429060765999));
#6261=CARTESIAN_POINT('Ctrl Pts',(-1.60980098518759,1.84937571182598,23.4333401957129));
#6262=CARTESIAN_POINT('Ctrl Pts',(-1.66971008496689,1.79360488462756,23.4376196254267));
#6263=CARTESIAN_POINT('Ctrl Pts',(-1.73069629536512,1.7368313491524,23.4419759953585));
#6264=CARTESIAN_POINT('Ctrl Pts',(-1.78892059448107,1.67681583651013,23.4463323652902));
#6265=CARTESIAN_POINT('Ctrl Pts',(-1.84401397873797,1.61386576152385,23.4506887352219));
#6266=CARTESIAN_POINT('Ctrl Pts',(-1.89663132731377,1.55374482172135,23.4548493188984));
#6267=CARTESIAN_POINT('Ctrl Pts',(-1.94639272356835,1.49094779758332,23.4590099025749));
#6268=CARTESIAN_POINT('Ctrl Pts',(-1.99301105788344,1.42578300352975,23.4631704862514));
#6269=CARTESIAN_POINT('Ctrl Pts',(-2.03958588784644,1.36067902143325,23.4673271872603));
#6270=CARTESIAN_POINT('Ctrl Pts',(-2.08302319534376,1.29321203995815,23.4714838882691));
#6271=CARTESIAN_POINT('Ctrl Pts',(-2.12307550508346,1.22372409051821,23.475640589278));
#6272=CARTESIAN_POINT('Ctrl Pts',(-2.16310357207426,1.15427820054801,23.4797947743307));
#6273=CARTESIAN_POINT('Ctrl Pts',(-2.19975046767757,1.08281418484751,23.4839489593833));
#6274=CARTESIAN_POINT('Ctrl Pts',(-2.2328124301214,1.00970238283139,23.4881031444359));
#6275=CARTESIAN_POINT('Ctrl Pts',(-2.26586521913785,0.936610866538073,23.4922561768614));
#6276=CARTESIAN_POINT('Ctrl Pts',(-2.2953348535945,0.86187290949826,23.4964092092869));
#6277=CARTESIAN_POINT('Ctrl Pts',(-2.32106460665762,0.785881251666771,23.5005622417124));
#6278=CARTESIAN_POINT('Ctrl Pts',(-2.3468068264979,0.709852773774781,23.504717286397));
#6279=CARTESIAN_POINT('Ctrl Pts',(-2.36880538969028,0.632569836508464,23.5088723310816));
#6280=CARTESIAN_POINT('Ctrl Pts',(-2.38695297832087,0.554441817763704,23.5130273757662));
#6281=CARTESIAN_POINT('Ctrl Pts',(-2.40510579337014,0.476291298523437,23.5171836170838));
#6282=CARTESIAN_POINT('Ctrl Pts',(-2.41940533677258,0.397295685264915,23.5213398584014));
#6283=CARTESIAN_POINT('Ctrl Pts',(-2.42979556890754,0.317873785199872,23.525496099719));
#6284=CARTESIAN_POINT('Ctrl Pts',(-2.44019766461207,0.238361201190058,23.529657086634));
#6285=CARTESIAN_POINT('Ctrl Pts',(-2.44668150234323,0.158421837288855,23.5338180735489));
#6286=CARTESIAN_POINT('Ctrl Pts',(-2.44924304161786,0.0784778509293303,
23.5379790604638));
#6287=CARTESIAN_POINT('Ctrl Pts',(-2.45010354819081,0.0516219965564258,
23.5393768749052));
#6288=CARTESIAN_POINT('Ctrl Pts',(-2.45052185378629,0.0247656044405823,
23.5407746893466));
#6289=CARTESIAN_POINT('Ctrl Pts',(-2.45049912112546,-0.00207541883967445,
23.542172503788));
#6290=CARTESIAN_POINT('',(-2.45049951066269,0.00154862580971605,24.342172503788));
#6291=CARTESIAN_POINT('Ctrl Pts',(-2.45186154582452,-0.00207657272782114,
23.542172503788));
#6292=CARTESIAN_POINT('Ctrl Pts',(-2.45316845875649,-0.146834277057642,
23.5497068768065));
#6293=CARTESIAN_POINT('Ctrl Pts',(-2.37555079931057,-1.10454055339028,23.5996265822973));
#6294=CARTESIAN_POINT('Ctrl Pts',(-1.11386918866955,-2.67479380645871,23.69193162026));
#6295=CARTESIAN_POINT('Ctrl Pts',(1.64579104116926,-2.38465895367458,23.819087617677));
#6296=CARTESIAN_POINT('Ctrl Pts',(2.89597072162243,0.0926285919153641,23.9462436150936));
#6297=CARTESIAN_POINT('Ctrl Pts',(1.49003467016963,2.484959387641,24.0733996125105));
#6298=CARTESIAN_POINT('Ctrl Pts',(-1.28252587751089,2.59814430893544,24.2005556099271));
#6299=CARTESIAN_POINT('Ctrl Pts',(-2.40720983591924,0.998919587715902,24.2901465736863));
#6300=CARTESIAN_POINT('Ctrl Pts',(-2.45396553830505,0.0940230514378206,
24.3373522049733));
#6301=CARTESIAN_POINT('Ctrl Pts',(-2.45328314078313,0.00155038496185235,
24.342172503788));
#6302=CARTESIAN_POINT('',(-2.45039359417306,0.00121703786866738,25.1421724505541));
#6303=CARTESIAN_POINT('Ctrl Pts',(-2.45049951066269,0.00154862580971605,
24.342172503788));
#6304=CARTESIAN_POINT('Ctrl Pts',(-2.45055002102087,-0.0783774655753502,
24.3463435443076));
#6305=CARTESIAN_POINT('Ctrl Pts',(-2.44668598205677,-0.158458895276197,
24.3505145848272));
#6306=CARTESIAN_POINT('Ctrl Pts',(-2.43888821404374,-0.238274063629557,
24.3546856253467));
#6307=CARTESIAN_POINT('Ctrl Pts',(-2.43108444750466,-0.318150630753082,
24.358859874489));
#6308=CARTESIAN_POINT('Ctrl Pts',(-2.41934085684055,-0.397760046305185,
24.3630341236312));
#6309=CARTESIAN_POINT('Ctrl Pts',(-2.40369055215446,-0.476678066920835,
24.3672083727735));
#6310=CARTESIAN_POINT('Ctrl Pts',(-2.38808610712647,-0.555364836227617,
24.3713703902281));
#6311=CARTESIAN_POINT('Ctrl Pts',(-2.36859787333247,-0.633363780969989,
24.3755324076827));
#6312=CARTESIAN_POINT('Ctrl Pts',(-2.34531045813516,-0.710259885508011,
24.3796944251373));
#6313=CARTESIAN_POINT('Ctrl Pts',(-2.32203341019326,-0.787121756896964,
24.3838545897156));
#6314=CARTESIAN_POINT('Ctrl Pts',(-2.29496067507136,-0.862881304691709,
24.388014754294));
#6315=CARTESIAN_POINT('Ctrl Pts',(-2.26422727925646,-0.937136637780686,
24.3921749188724));
#6316=CARTESIAN_POINT('Ctrl Pts',(-2.23349754837497,-1.01138311597927,24.3963345873544));
#6317=CARTESIAN_POINT('Ctrl Pts',(-2.19910820756057,-1.08412529377258,24.4004942558364));
#6318=CARTESIAN_POINT('Ctrl Pts',(-2.16124259240263,-1.15498082528878,24.4046539243184));
#6319=CARTESIAN_POINT('Ctrl Pts',(-2.12315117743541,-1.22625888171145,24.4088383976886));
#6320=CARTESIAN_POINT('Ctrl Pts',(-2.08154210565957,-1.29562727592315,24.4130228710588));
#6321=CARTESIAN_POINT('Ctrl Pts',(-2.0366481729518,-1.36272318157874,24.417207344429));
#6322=CARTESIAN_POINT('Ctrl Pts',(-1.99196174743553,-1.42950895884718,24.4213724764703));
#6323=CARTESIAN_POINT('Ctrl Pts',(-1.94402109266038,-1.49404285456841,24.4255376085116));
#6324=CARTESIAN_POINT('Ctrl Pts',(-1.89309724305004,-1.5559990611682,24.4297027405529));
#6325=CARTESIAN_POINT('Ctrl Pts',(-1.84181868622524,-1.61838682024548,24.4338968845875));
#6326=CARTESIAN_POINT('Ctrl Pts',(-1.78751554941226,-1.67816048007871,24.4380910286221));
#6327=CARTESIAN_POINT('Ctrl Pts',(-1.73050189298297,-1.73502548926013,24.4422851726568));
#6328=CARTESIAN_POINT('Ctrl Pts',(-1.67348823655367,-1.79189049844156,24.4464793166914));
#6329=CARTESIAN_POINT('Ctrl Pts',(-1.61376446905642,-1.84584658183965,24.450673460726));
#6330=CARTESIAN_POINT('Ctrl Pts',(-1.55167630420413,-1.89664200548533,24.4548676047607));
#6331=CARTESIAN_POINT('Ctrl Pts',(-1.48904695305653,-1.94788018319222,24.4590983067009));
#6332=CARTESIAN_POINT('Ctrl Pts',(-1.4237591760496,-1.99610924247822,24.4633290086412));
#6333=CARTESIAN_POINT('Ctrl Pts',(-1.35613416485727,-2.04104149318599,24.4675597105814));
#6334=CARTESIAN_POINT('Ctrl Pts',(-1.28860631219858,-2.08590918861287,24.4717843341671));
#6335=CARTESIAN_POINT('Ctrl Pts',(-1.21874827851865,-2.12748922743726,24.4760089577528));
#6336=CARTESIAN_POINT('Ctrl Pts',(-1.14691430973509,-2.16553407179958,24.4802335813385));
#6337=CARTESIAN_POINT('Ctrl Pts',(-1.07479761666243,-2.20372865314232,24.4844748322068));
#6338=CARTESIAN_POINT('Ctrl Pts',(-1.00068976864271,-2.23835985219343,24.488716083075));
#6339=CARTESIAN_POINT('Ctrl Pts',(-0.924978671719143,-2.26922116746356,
24.4929573339433));
#6340=CARTESIAN_POINT('Ctrl Pts',(-0.849700492791117,-2.29990601694084,
24.4971743332303));
#6341=CARTESIAN_POINT('Ctrl Pts',(-0.772837785029174,-2.32686380092333,
24.5013913325172));
#6342=CARTESIAN_POINT('Ctrl Pts',(-0.694794824440356,-2.34993838258174,
24.5056083318042));
#6343=CARTESIAN_POINT('Ctrl Pts',(-0.616777736800381,-2.37300531451151,
24.5098239330636));
#6344=CARTESIAN_POINT('Ctrl Pts',(-0.537581618970728,-2.39219146885364,
24.5140395343231));
#6345=CARTESIAN_POINT('Ctrl Pts',(-0.457626837638351,-2.40739027319484,
24.5182551355825));
#6346=CARTESIAN_POINT('Ctrl Pts',(-0.37767405138428,-2.42258869828662,24.5224706316518));
#6347=CARTESIAN_POINT('Ctrl Pts',(-0.29696309634789,-2.43379988541412,24.5266861277211));
#6348=CARTESIAN_POINT('Ctrl Pts',(-0.215924066859916,-2.44096846504634,
24.5309016237904));
#6349=CARTESIAN_POINT('Ctrl Pts',(-0.134026320903077,-2.44821300532897,
24.535161788656));
#6350=CARTESIAN_POINT('Ctrl Pts',(-0.0517939874886304,-2.45132869563445,
24.5394219535216));
#6351=CARTESIAN_POINT('Ctrl Pts',(0.0303260965835189,-2.45031234291998,
24.5436821183871));
#6352=CARTESIAN_POINT('Ctrl Pts',(0.111703471857997,-2.44930518228211,24.5479037535561));
#6353=CARTESIAN_POINT('Ctrl Pts',(0.192970154550918,-2.44424051071892,24.5521253887251));
#6354=CARTESIAN_POINT('Ctrl Pts',(0.273695529801835,-2.43516755213404,24.556347023894));
#6355=CARTESIAN_POINT('Ctrl Pts',(0.355526042313421,-2.4259703839736,24.5606264536079));
#6356=CARTESIAN_POINT('Ctrl Pts',(0.436799825928479,-2.41265443022044,24.5649058833218));
#6357=CARTESIAN_POINT('Ctrl Pts',(0.51707998801538,-2.39532430706032,24.5691853130357));
#6358=CARTESIAN_POINT('Ctrl Pts',(0.59736015010228,-2.37799418390021,24.5734647427496));
#6359=CARTESIAN_POINT('Ctrl Pts',(0.676646233963054,-2.35665008210095,24.5777441724635));
#6360=CARTESIAN_POINT('Ctrl Pts',(0.754520101636108,-2.33144797630722,24.5820236021773));
#6361=CARTESIAN_POINT('Ctrl Pts',(0.8315072576559,-2.30653283456911,24.5862543041176));
#6362=CARTESIAN_POINT('Ctrl Pts',(0.907403777978842,-2.27775342892994,24.5904850060578));
#6363=CARTESIAN_POINT('Ctrl Pts',(0.981793887963596,-2.2452240448466,24.5947157079981));
#6364=CARTESIAN_POINT('Ctrl Pts',(1.05607711982936,-2.21274139653745,24.5989403315838));
#6365=CARTESIAN_POINT('Ctrl Pts',(1.12885781728276,-2.17651965477304,24.6031649551694));
#6366=CARTESIAN_POINT('Ctrl Pts',(1.19973606806975,-2.13672263454397,24.6073895787551));
#6367=CARTESIAN_POINT('Ctrl Pts',(1.27089328162899,-2.0967689811169,24.6116308296234));
#6368=CARTESIAN_POINT('Ctrl Pts',(1.34013258959559,-2.05321199180245,24.6158720804917));
#6369=CARTESIAN_POINT('Ctrl Pts',(1.40707035736177,-2.00626599917205,24.62011333136));
#6370=CARTESIAN_POINT('Ctrl Pts',(1.47362537325352,-1.95958844493264,24.6243303306469));
#6371=CARTESIAN_POINT('Ctrl Pts',(1.53790471347347,-1.90956080874431,24.6285473299339));
#6372=CARTESIAN_POINT('Ctrl Pts',(1.59955822498833,-1.85643845437229,24.6327643292208));
#6373=CARTESIAN_POINT('Ctrl Pts',(1.66119129701531,-1.80333371122292,24.6369799304802));
#6374=CARTESIAN_POINT('Ctrl Pts',(1.72019991700233,-1.74713659061232,24.6411955317397));
#6375=CARTESIAN_POINT('Ctrl Pts',(1.77626689188701,-1.68814281942792,24.6454111329991));
#6376=CARTESIAN_POINT('Ctrl Pts',(1.8323324677559,-1.62915052029044,24.6496266290684));
#6377=CARTESIAN_POINT('Ctrl Pts',(1.88545622487061,-1.56736204717701,24.6538421251377));
#6378=CARTESIAN_POINT('Ctrl Pts',(1.93535875271566,-1.50310902741181,24.658057621207));
#6379=CARTESIAN_POINT('Ctrl Pts',(1.98579006431816,-1.43817516131103,24.6623177860726));
#6380=CARTESIAN_POINT('Ctrl Pts',(2.03293116385415,-1.37072457999829,24.6665779509381));
#6381=CARTESIAN_POINT('Ctrl Pts',(2.07653744401198,-1.30113123612347,24.6708381158037));
#6382=CARTESIAN_POINT('Ctrl Pts',(2.11974934113558,-1.23216730695727,24.6750597509727));
#6383=CARTESIAN_POINT('Ctrl Pts',(2.15948992514904,-1.16109965892969,24.6792813861416));
#6384=CARTESIAN_POINT('Ctrl Pts',(2.19556744143292,-1.08831698512873,24.6835030213106));
#6385=CARTESIAN_POINT('Ctrl Pts',(2.23213886198692,-1.01453791032563,24.6877824510245));
#6386=CARTESIAN_POINT('Ctrl Pts',(2.26494596294823,-0.938996950217633,24.6920618807384));
#6387=CARTESIAN_POINT('Ctrl Pts',(2.29384016231569,-0.862118066013883,24.6963413104523));
#6388=CARTESIAN_POINT('Ctrl Pts',(2.32273436168315,-0.785239181810154,24.7006207401662));
#6389=CARTESIAN_POINT('Ctrl Pts',(2.34771557258452,-0.707022860766869,24.7049001698801));
#6390=CARTESIAN_POINT('Ctrl Pts',(2.36868854702988,-0.627905102041274,24.709179599594));
#6391=CARTESIAN_POINT('Ctrl Pts',(2.38942271247033,-0.549688218548305,24.7134103015343));
#6392=CARTESIAN_POINT('Ctrl Pts',(2.40631748587856,-0.47029613696848,24.7176410034746));
#6393=CARTESIAN_POINT('Ctrl Pts',(2.41924384829596,-0.390140298459629,24.7218717054148));
#6394=CARTESIAN_POINT('Ctrl Pts',(2.43215163908734,-0.310099621835258,24.7260963290005));
#6395=CARTESIAN_POINT('Ctrl Pts',(2.44110226899636,-0.229297822830013,24.7303209525862));
#6396=CARTESIAN_POINT('Ctrl Pts',(2.44601694947688,-0.148159822056558,24.7345455761718));
#6397=CARTESIAN_POINT('Ctrl Pts',(2.45095097316743,-0.066702478164706,24.7387868270401));
#6398=CARTESIAN_POINT('Ctrl Pts',(2.45181708829447,0.0150932609078766,24.7430280779084));
#6399=CARTESIAN_POINT('Ctrl Pts',(2.44858779225845,0.0967888092853415,24.7472693287767));
#6400=CARTESIAN_POINT('Ctrl Pts',(2.44537696142007,0.178017220420015,24.7514863280637));
#6401=CARTESIAN_POINT('Ctrl Pts',(2.43811744621298,0.259146114167406,24.7557033273506));
#6402=CARTESIAN_POINT('Ctrl Pts',(2.42683436864361,0.339742839762895,24.7599203266376));
#6403=CARTESIAN_POINT('Ctrl Pts',(2.41555503166129,0.420312845780755,24.764135927897));
#6404=CARTESIAN_POINT('Ctrl Pts',(2.4002548456395,0.500350573793417,24.7683515291565));
#6405=CARTESIAN_POINT('Ctrl Pts',(2.38101071310204,0.579429231307268,24.7725671304159));
#6406=CARTESIAN_POINT('Ctrl Pts',(2.36176706075539,0.658505915604342,24.7767826264852));
#6407=CARTESIAN_POINT('Ctrl Pts',(2.33857976857915,0.736623125367781,24.7809981225545));
#6408=CARTESIAN_POINT('Ctrl Pts',(2.31157637857783,0.813366397142773,24.7852136186238));
#6409=CARTESIAN_POINT('Ctrl Pts',(2.2842868516884,0.890922866111448,24.7894737834894));
#6410=CARTESIAN_POINT('Ctrl Pts',(2.25310001776106,0.967075643962771,24.793733948355));
#6411=CARTESIAN_POINT('Ctrl Pts',(2.21819784700319,1.04141661286461,24.7979941132206));
#6412=CARTESIAN_POINT('Ctrl Pts',(2.18361133774984,1.1150852286841,24.8022157483895));
#6413=CARTESIAN_POINT('Ctrl Pts',(2.14537670099685,1.1869742902046,24.8064373835585));
#6414=CARTESIAN_POINT('Ctrl Pts',(2.10371691515956,1.2567121352448,24.8106590187274));
#6415=CARTESIAN_POINT('Ctrl Pts',(2.06148680330678,1.32740469732185,24.8149384484413));
#6416=CARTESIAN_POINT('Ctrl Pts',(2.01573732590791,1.39588628495846,24.8192178781553));
#6417=CARTESIAN_POINT('Ctrl Pts',(1.96674448748338,1.46180243909829,24.8234973078692));
#6418=CARTESIAN_POINT('Ctrl Pts',(1.91775164905886,1.52771859323813,24.8277767375831));
#6419=CARTESIAN_POINT('Ctrl Pts',(1.86551581223935,1.59106897703644,24.8320561672969));
#6420=CARTESIAN_POINT('Ctrl Pts',(1.81035197820623,1.65153745492035,24.8363355970108));
#6421=CARTESIAN_POINT('Ctrl Pts',(1.75581626777779,1.71131740781386,24.8405662989511));
#6422=CARTESIAN_POINT('Ctrl Pts',(1.69821380838736,1.7685056291386,24.8447970008914));
#6423=CARTESIAN_POINT('Ctrl Pts',(1.63782066989105,1.82277088611752,24.8490277028316));
#6424=CARTESIAN_POINT('Ctrl Pts',(1.57751429971716,1.87695817885362,24.8532523264173));
#6425=CARTESIAN_POINT('Ctrl Pts',(1.51442555639558,1.92823053948165,24.857476950003));
#6426=CARTESIAN_POINT('Ctrl Pts',(1.44886903807584,1.97629166888523,24.8617015735887));
#6427=CARTESIAN_POINT('Ctrl Pts',(1.38305450227006,2.02454195738547,24.8659428244569));
#6428=CARTESIAN_POINT('Ctrl Pts',(1.31475304428376,2.06955533231758,24.8701840753252));
#6429=CARTESIAN_POINT('Ctrl Pts',(1.24431851825835,2.11107121507526,24.8744253261935));
#6430=CARTESIAN_POINT('Ctrl Pts',(1.17428673866064,2.15234970894971,24.8786423254805));
#6431=CARTESIAN_POINT('Ctrl Pts',(1.10214662337518,2.1901703610904,24.8828593247674));
#6432=CARTESIAN_POINT('Ctrl Pts',(1.02827552813907,2.2243200507639,24.8870763240544));
#6433=CARTESIAN_POINT('Ctrl Pts',(0.954428922787074,2.25845841906819,24.8912919253138));
#6434=CARTESIAN_POINT('Ctrl Pts',(0.878852898869528,2.28892804667599,24.8955075265733));
#6435=CARTESIAN_POINT('Ctrl Pts',(0.801947921323598,2.31556251945068,24.8997231278327));
#6436=CARTESIAN_POINT('Ctrl Pts',(0.725044862755625,2.34219632762643,24.903938623902));
#6437=CARTESIAN_POINT('Ctrl Pts',(0.64681335629807,2.36499502006848,24.9081541199713));
#6438=CARTESIAN_POINT('Ctrl Pts',(0.567670917970752,2.38384143325227,24.9123696160406));
#6439=CARTESIAN_POINT('Ctrl Pts',(0.487689860084349,2.4028875492889,24.9166297809062));
#6440=CARTESIAN_POINT('Ctrl Pts',(0.406778917865274,2.41789700011419,24.9208899457718));
#6441=CARTESIAN_POINT('Ctrl Pts',(0.325379740277146,2.42880181871992,24.9251501106373));
#6442=CARTESIAN_POINT('Ctrl Pts',(0.244716751478899,2.43960801218653,24.9293717458063));
#6443=CARTESIAN_POINT('Ctrl Pts',(0.163574796899474,2.44638354323401,24.9335933809753));
#6444=CARTESIAN_POINT('Ctrl Pts',(0.0823870774693992,2.44911466033464,24.9378150161442));
#6445=CARTESIAN_POINT('Ctrl Pts',(8.78912474756577E-5,2.45188316666092,
24.9420944458581));
#6446=CARTESIAN_POINT('Ctrl Pts',(-0.0822578277790784,2.45049569217383,
24.946373875572));
#6447=CARTESIAN_POINT('Ctrl Pts',(-0.164202633375031,2.44499238141813,24.9506533052859));
#6448=CARTESIAN_POINT('Ctrl Pts',(-0.246147438970984,2.43948907066243,24.9549327349998));
#6449=CARTESIAN_POINT('Ctrl Pts',(-0.327690851599038,2.42987004615084,24.9592121647136));
#6450=CARTESIAN_POINT('Ctrl Pts',(-0.40839653252675,2.41622898795212,24.9634915944275));
#6451=CARTESIAN_POINT('Ctrl Pts',(-0.488183257328567,2.40274325381301,24.9677222963678));
#6452=CARTESIAN_POINT('Ctrl Pts',(-0.567451338534409,2.38527593323873,24.971952998308));
#6453=CARTESIAN_POINT('Ctrl Pts',(-0.645772822204555,2.36387980068826,24.9761837002483));
#6454=CARTESIAN_POINT('Ctrl Pts',(-0.723981779453544,2.34251440849292,24.980408323834));
#6455=CARTESIAN_POINT('Ctrl Pts',(-0.801246395387,2.31723153636686,24.9846329474197));
#6456=CARTESIAN_POINT('Ctrl Pts',(-0.877147227128712,2.28813526521935,24.9888575710053));
#6457=CARTESIAN_POINT('Ctrl Pts',(-0.953346789527392,2.25892447690521,24.9930988218736));
#6458=CARTESIAN_POINT('Ctrl Pts',(-1.02817134162205,2.22587028670691,24.9973400727419));
#6459=CARTESIAN_POINT('Ctrl Pts',(-1.101210219165,2.18912911981148,25.0015813236102));
#6460=CARTESIAN_POINT('Ctrl Pts',(-1.17383145853132,2.15259803985147,25.0057983228972));
#6461=CARTESIAN_POINT('Ctrl Pts',(-1.2446869693642,2.11242224432312,25.0100153221841));
#6462=CARTESIAN_POINT('Ctrl Pts',(-1.31339326393733,2.06880361181144,25.0142323214711));
#6463=CARTESIAN_POINT('Ctrl Pts',(-1.38207678087071,2.02519943983068,25.0184479227305));
#6464=CARTESIAN_POINT('Ctrl Pts',(-1.44861210416238,1.97815494650584,25.0226635239899));
#6465=CARTESIAN_POINT('Ctrl Pts',(-1.51264250341395,1.92791672716058,25.0268791252494));
#6466=CARTESIAN_POINT('Ctrl Pts',(-1.57667130494176,1.87767976138859,25.0310946213187));
#6467=CARTESIAN_POINT('Ctrl Pts',(-1.6381949414896,1.82424951596874,25.035310117388));
#6468=CARTESIAN_POINT('Ctrl Pts',(-1.69688885882357,1.7679135869155,25.0395256134573));
#6469=CARTESIAN_POINT('Ctrl Pts',(-1.75620471639741,1.71098070364929,25.0437857783229));
#6470=CARTESIAN_POINT('Ctrl Pts',(-1.81263016772042,1.65108051476925,25.0480459431884));
#6471=CARTESIAN_POINT('Ctrl Pts',(-1.86586895503825,1.58854754182066,25.052306108054));
#6472=CARTESIAN_POINT('Ctrl Pts',(-1.91862624119627,1.52658012831694,25.056527743223));
#6473=CARTESIAN_POINT('Ctrl Pts',(-1.96825403535061,1.46202777234665,25.060749378392));
#6474=CARTESIAN_POINT('Ctrl Pts',(-2.01450623568522,1.3952472456111,25.0649710135609));
#6475=CARTESIAN_POINT('Ctrl Pts',(-2.0613916325807,1.3275524877783,25.0692504432748));
#6476=CARTESIAN_POINT('Ctrl Pts',(-2.10480805075346,1.25756850989394,25.0735298729887));
#6477=CARTESIAN_POINT('Ctrl Pts',(-2.14454698933912,1.18569324047854,25.0778093027026));
#6478=CARTESIAN_POINT('Ctrl Pts',(-2.18428592792479,1.11381797106313,25.0820887324165));
#6479=CARTESIAN_POINT('Ctrl Pts',(-2.22034723029967,1.04005187962111,25.0863681621304));
#6480=CARTESIAN_POINT('Ctrl Pts',(-2.25257341972751,0.964812540723382,25.0906475918443));
#6481=CARTESIAN_POINT('Ctrl Pts',(-2.28784259062639,0.882468672304055,25.0953311098341));
#6482=CARTESIAN_POINT('Ctrl Pts',(-2.3186323432272,0.798096502576319,25.1000146278239));
#6483=CARTESIAN_POINT('Ctrl Pts',(-2.34472986509261,0.712174213056611,25.1046981458138));
#6484=CARTESIAN_POINT('Ctrl Pts',(-2.37074857500766,0.626511400404119,25.1093675200397));
#6485=CARTESIAN_POINT('Ctrl Pts',(-2.39210319657215,0.539308069372609,25.1140368942657));
#6486=CARTESIAN_POINT('Ctrl Pts',(-2.40862911253218,0.451061024987151,25.1187062684916));
#6487=CARTESIAN_POINT('Ctrl Pts',(-2.42506955792525,0.363270386463512,25.1233514931295));
#6488=CARTESIAN_POINT('Ctrl Pts',(-2.43673099334932,0.274447073716838,25.1279967177674));
#6489=CARTESIAN_POINT('Ctrl Pts',(-2.44349925207794,0.185099041311755,25.1326419424054));
#6490=CARTESIAN_POINT('Ctrl Pts',(-2.44812801520265,0.123994569062097,25.1358187778917));
#6491=CARTESIAN_POINT('Ctrl Pts',(-2.45046918747822,0.0626450716972059,
25.1389956133781));
#6492=CARTESIAN_POINT('Ctrl Pts',(-2.45049969773741,0.0012171231945159,
25.1421724488644));
#6493=CARTESIAN_POINT('',(-2.45049910673901,-0.00209233632933992,25.9421725277106));
#6494=CARTESIAN_POINT('Ctrl Pts',(-2.4470507577615,0.00121434964273421,
25.142172503788));
#6495=CARTESIAN_POINT('Ctrl Pts',(-2.4448728557432,-0.48557354190418,25.1673828656123));
#6496=CARTESIAN_POINT('Ctrl Pts',(-2.06824726699471,-1.79388675645704,25.2349785599091));
#6497=CARTESIAN_POINT('Ctrl Pts',(0.0634192777159373,-2.89675757904347,
25.3449595866777));
#6498=CARTESIAN_POINT('Ctrl Pts',(2.46980667520369,-1.51501863475477,25.4721155840945));
#6499=CARTESIAN_POINT('Ctrl Pts',(2.61094590709541,1.25625950613601,25.5992715815113));
#6500=CARTESIAN_POINT('Ctrl Pts',(0.357387413898736,2.8753261924378,25.7264275789279));
#6501=CARTESIAN_POINT('Ctrl Pts',(-1.96297985249653,1.96014493364779,25.8407278863536));
#6502=CARTESIAN_POINT('Ctrl Pts',(-2.44422981805528,0.567055840943636,25.9126428613069));
#6503=CARTESIAN_POINT('Ctrl Pts',(-2.44883297466156,-0.00209045264269275,
25.942172503788));
#6504=CARTESIAN_POINT('',(-2.45089310683891,-0.000179724726367168,26.742172503788));
#6505=CARTESIAN_POINT('Ctrl Pts',(-2.45049910673901,-0.00209233632933992,
25.9421725277106));
#6506=CARTESIAN_POINT('Ctrl Pts',(-2.45041577647178,-0.0996869450663497,
25.9472327318638));
#6507=CARTESIAN_POINT('Ctrl Pts',(-2.4444983547822,-0.197027745374281,25.952292936017));
#6508=CARTESIAN_POINT('Ctrl Pts',(-2.43286032705321,-0.293497664472038,
25.9573531401702));
#6509=CARTESIAN_POINT('Ctrl Pts',(-2.42106460921947,-0.391274708110316,
25.9624819078413));
#6510=CARTESIAN_POINT('Ctrl Pts',(-2.40339228844551,-0.488157094530591,
25.9676106755125));
#6511=CARTESIAN_POINT('Ctrl Pts',(-2.38001045809284,-0.583524180620417,
25.9727394431836));
#6512=CARTESIAN_POINT('Ctrl Pts',(-2.36785304147323,-0.633110435413318,
25.9754061533763));
#6513=CARTESIAN_POINT('Ctrl Pts',(-2.35415285291789,-0.682287388048195,
25.9780728635689));
#6514=CARTESIAN_POINT('Ctrl Pts',(-2.33893842772718,-0.730970096037509,
25.9807395737615));
#6515=CARTESIAN_POINT('Ctrl Pts',(-2.31480093488955,-0.808204595578558,
25.9849702757017));
#6516=CARTESIAN_POINT('Ctrl Pts',(-2.28678837606447,-0.884387484301311,
25.989200977642));
#6517=CARTESIAN_POINT('Ctrl Pts',(-2.25501083799109,-0.959101856187706,
25.9934316795822));
#6518=CARTESIAN_POINT('Ctrl Pts',(-2.22327895549613,-1.03370888407986,25.9976563031679));
#6519=CARTESIAN_POINT('Ctrl Pts',(-2.1877930172753,-1.10685116109401,26.0018809267536));
#6520=CARTESIAN_POINT('Ctrl Pts',(-2.14871279704817,-1.178127143309,26.0061055503393));
#6521=CARTESIAN_POINT('Ctrl Pts',(-2.10947876480593,-1.24968365368861,26.0103468012075));
#6522=CARTESIAN_POINT('Ctrl Pts',(-2.06662223866485,-1.31935869407582,26.0145880520758));
#6523=CARTESIAN_POINT('Ctrl Pts',(-2.0203536715094,-1.38676648792018,26.0188293029441));
#6524=CARTESIAN_POINT('Ctrl Pts',(-1.97434966920874,-1.45378884226887,26.0230463022311));
#6525=CARTESIAN_POINT('Ctrl Pts',(-1.92497280611408,-1.51856942078306,26.027263301518));
#6526=CARTESIAN_POINT('Ctrl Pts',(-1.8724749018644,-1.58075551300253,26.0314803008049));
#6527=CARTESIAN_POINT('Ctrl Pts',(-1.81999440181849,-1.64292098917196,26.0356959020644));
#6528=CARTESIAN_POINT('Ctrl Pts',(-1.76439521510405,-1.70249333203664,26.0399115033238));
#6529=CARTESIAN_POINT('Ctrl Pts',(-1.70596985481669,-1.75915238238668,26.0441271045832));
#6530=CARTESIAN_POINT('Ctrl Pts',(-1.64754595239291,-1.81581001894713,26.0483426006525));
#6531=CARTESIAN_POINT('Ctrl Pts',(-1.58629635121864,-1.86955418454366,26.0525580967218));
#6532=CARTESIAN_POINT('Ctrl Pts',(-1.5225498440212,-1.92010213855175,26.0567735927911));
#6533=CARTESIAN_POINT('Ctrl Pts',(-1.45812785766353,-1.9711857154673,26.0610337576567));
#6534=CARTESIAN_POINT('Ctrl Pts',(-1.39115610371382,-2.01900462760259,26.0652939225222));
#6535=CARTESIAN_POINT('Ctrl Pts',(-1.32200604904805,-2.0633105089347,26.0695540873878));
#6536=CARTESIAN_POINT('Ctrl Pts',(-1.25348139990362,-2.10721567991383,26.0737757225568));
#6537=CARTESIAN_POINT('Ctrl Pts',(-1.1828181321915,-2.14767092938976,26.0779973577257));
#6538=CARTESIAN_POINT('Ctrl Pts',(-1.11040298547257,-2.18448059269329,26.0822189928947));
#6539=CARTESIAN_POINT('Ctrl Pts',(-1.03699646922851,-2.22179418342198,26.0864984226086));
#6540=CARTESIAN_POINT('Ctrl Pts',(-0.961790195748017,-2.25536141382185,
26.0907778523225));
#6541=CARTESIAN_POINT('Ctrl Pts',(-0.885206606296767,-2.28502943398298,
26.0950572820364));
#6542=CARTESIAN_POINT('Ctrl Pts',(-0.808623016845516,-2.3146974541441,26.0993367117503));
#6543=CARTESIAN_POINT('Ctrl Pts',(-0.73066259777886,-2.3404661722849,26.1036161414642));
#6544=CARTESIAN_POINT('Ctrl Pts',(-0.651760365548761,-2.36223594839714,
26.1078955711781));
#6545=CARTESIAN_POINT('Ctrl Pts',(-0.573756554456445,-2.38375784271351,
26.1121262731184));
#6546=CARTESIAN_POINT('Ctrl Pts',(-0.494538886439508,-2.4014523915938,26.1163569750587));
#6547=CARTESIAN_POINT('Ctrl Pts',(-0.414517480633748,-2.41518643343512,
26.1205876769989));
#6548=CARTESIAN_POINT('Ctrl Pts',(-0.334611043569686,-2.42890074323732,
26.1248123005846));
#6549=CARTESIAN_POINT('Ctrl Pts',(-0.253903616583434,-2.43866576896868,
26.1290369241703));
#6550=CARTESIAN_POINT('Ctrl Pts',(-0.172819304132042,-2.44439844095011,
26.133261547756));
#6551=CARTESIAN_POINT('Ctrl Pts',(-0.0914158598690766,-2.45015367559426,
26.1375027986243));
#6552=CARTESIAN_POINT('Ctrl Pts',(-0.00963301454602711,-2.45184462109823,
26.1417440494925));
#6553=CARTESIAN_POINT('Ctrl Pts',(0.0720909456153298,-2.44943935331338,
26.1459853003608));
#6554=CARTESIAN_POINT('Ctrl Pts',(0.153347606074818,-2.44704783891147,26.1502022996478));
#6555=CARTESIAN_POINT('Ctrl Pts',(0.234545583426826,-2.44060684242898,26.1544192989348));
#6556=CARTESIAN_POINT('Ctrl Pts',(0.31525199556275,-2.43013712150029,26.1586362982217));
#6557=CARTESIAN_POINT('Ctrl Pts',(0.395931651757442,-2.41967087151313,26.1628518994812));
#6558=CARTESIAN_POINT('Ctrl Pts',(0.476119605525667,-2.40517860915679,26.1670675007406));
#6559=CARTESIAN_POINT('Ctrl Pts',(0.555388310547945,-2.38673292902803,26.1712831020001));
#6560=CARTESIAN_POINT('Ctrl Pts',(0.634655037611317,-2.36828770916661,26.1754985980694));
#6561=CARTESIAN_POINT('Ctrl Pts',(0.713002108821671,-2.34588937412875,26.1797140941387));
#6562=CARTESIAN_POINT('Ctrl Pts',(0.790013795594285,-2.31966127974985,26.183929590208));
#6563=CARTESIAN_POINT('Ctrl Pts',(0.867841523774748,-2.29315526377283,26.1881897550736));
#6564=CARTESIAN_POINT('Ctrl Pts',(0.944304934861096,-2.26273798332415,26.1924499199392));
#6565=CARTESIAN_POINT('Ctrl Pts',(1.01899409668388,-2.22858728366726,26.1967100848047));
#6566=CARTESIAN_POINT('Ctrl Pts',(1.0930077563053,-2.19474544907504,26.2009317199737));
#6567=CARTESIAN_POINT('Ctrl Pts',(1.16527874189663,-2.15723772646195,26.2051533551427));
#6568=CARTESIAN_POINT('Ctrl Pts',(1.23543316153551,-2.11628333485343,26.2093749903117));
#6569=CARTESIAN_POINT('Ctrl Pts',(1.30654800115254,-2.07476827413675,26.2136544200256));
#6570=CARTESIAN_POINT('Ctrl Pts',(1.37548747002772,-2.02971173012085,26.2179338497394));
#6571=CARTESIAN_POINT('Ctrl Pts',(1.44189434374375,-1.98138611872593,26.2222132794533));
#6572=CARTESIAN_POINT('Ctrl Pts',(1.50830121745975,-1.93306050733102,26.2264927091672));
#6573=CARTESIAN_POINT('Ctrl Pts',(1.572175155532,-1.88146618777238,26.2307721388811));
#6574=CARTESIAN_POINT('Ctrl Pts',(1.63319686181349,-1.82691495712378,26.235051568595));
#6575=CARTESIAN_POINT('Ctrl Pts',(1.69352374376341,-1.77298487466459,26.2392822705352));
#6576=CARTESIAN_POINT('Ctrl Pts',(1.75128995276365,-1.71596206270461,26.2435129724755));
#6577=CARTESIAN_POINT('Ctrl Pts',(1.80616148883622,-1.65611923672329,26.2477436744157));
#6578=CARTESIAN_POINT('Ctrl Pts',(1.86095418960974,-1.59636238841672,26.2519682980014));
#6579=CARTESIAN_POINT('Ctrl Pts',(1.91286016552293,-1.53379391262625,26.2561929215871));
#6580=CARTESIAN_POINT('Ctrl Pts',(1.96157995994097,-1.46872540345634,26.2604175451727));
#6581=CARTESIAN_POINT('Ctrl Pts',(2.01049150583093,-1.40340079750775,26.264658796041));
#6582=CARTESIAN_POINT('Ctrl Pts',(2.05619138227902,-1.33555675297573,26.2689000469093));
#6583=CARTESIAN_POINT('Ctrl Pts',(2.09841545546451,-1.26554447818623,26.2731412977776));
#6584=CARTESIAN_POINT('Ctrl Pts',(2.14039809031562,-1.19593253538123,26.2773582970646));
#6585=CARTESIAN_POINT('Ctrl Pts',(2.17894432091357,-1.12417749326991,26.2815752963515));
#6586=CARTESIAN_POINT('Ctrl Pts',(2.21383723189393,-1.05065453917081,26.2857922956384));
#6587=CARTESIAN_POINT('Ctrl Pts',(2.24871857511094,-0.977155959539449,26.2900078968979));
#6588=CARTESIAN_POINT('Ctrl Pts',(2.27994880462219,-0.901891051631597,26.2942234981573));
#6589=CARTESIAN_POINT('Ctrl Pts',(2.30735747623874,-0.825258581806462,26.2984390994167));
#6590=CARTESIAN_POINT('Ctrl Pts',(2.33476546393814,-0.748628024159358,26.302654595486));
#6591=CARTESIAN_POINT('Ctrl Pts',(2.35835192774011,-0.670630410702349,26.3068700915553));
#6592=CARTESIAN_POINT('Ctrl Pts',(2.37799549961059,-0.591682054681205,26.3110855876246));
#6593=CARTESIAN_POINT('Ctrl Pts',(2.39784722129216,-0.511897135661273,26.3153457524902));
#6594=CARTESIAN_POINT('Ctrl Pts',(2.41367186050755,-0.431141671582436,26.3196059173558));
#6595=CARTESIAN_POINT('Ctrl Pts',(2.42539699986717,-0.349856603532552,26.3238660822214));
#6596=CARTESIAN_POINT('Ctrl Pts',(2.43701609495931,-0.269306692245722,26.3280877173903));
#6597=CARTESIAN_POINT('Ctrl Pts',(2.44460956275498,-0.188237192057598,26.3323093525593));
#6598=CARTESIAN_POINT('Ctrl Pts',(2.44815928378296,-0.107081143192042,26.3365309877282));
#6599=CARTESIAN_POINT('Ctrl Pts',(2.45175760079407,-0.0248140611068261,
26.3408104174421));
#6600=CARTESIAN_POINT('Ctrl Pts',(2.45120061758862,0.0575414626740317,26.345089847156));
#6601=CARTESIAN_POINT('Ctrl Pts',(2.4465239643695,0.139537599827903,26.3493692768699));
#6602=CARTESIAN_POINT('Ctrl Pts',(2.44184731115039,0.221533736981752,26.3536487065838));
#6603=CARTESIAN_POINT('Ctrl Pts',(2.43305110558818,0.303170006760211,26.3579281362977));
#6604=CARTESIAN_POINT('Ctrl Pts',(2.4202246227018,0.384009147896178,26.3622075660116));
#6605=CARTESIAN_POINT('Ctrl Pts',(2.4075441887043,0.463927813259801,26.3664382679519));
#6606=CARTESIAN_POINT('Ctrl Pts',(2.39087714044248,0.543368013966587,26.3706689698921));
#6607=CARTESIAN_POINT('Ctrl Pts',(2.37027193396252,0.621901285631053,26.3748996718324));
#6608=CARTESIAN_POINT('Ctrl Pts',(2.34969633149461,0.700321726593133,26.3791242954181));
#6609=CARTESIAN_POINT('Ctrl Pts',(2.32519392503081,0.777837380339582,26.3833489190038));
#6610=CARTESIAN_POINT('Ctrl Pts',(2.29686456028903,0.85402777571242,26.3875735425894));
#6611=CARTESIAN_POINT('Ctrl Pts',(2.26842369677241,0.930518041407628,26.3918147934577));
#6612=CARTESIAN_POINT('Ctrl Pts',(2.23612576043026,1.0056721257536,26.396056044326));
#6613=CARTESIAN_POINT('Ctrl Pts',(2.20012302712518,1.07907780790523,26.4002972951943));
#6614=CARTESIAN_POINT('Ctrl Pts',(2.16432615837333,1.15206375448197,26.4045142944813));
#6615=CARTESIAN_POINT('Ctrl Pts',(2.12486695278524,1.2233208176833,26.4087312937682));
#6616=CARTESIAN_POINT('Ctrl Pts',(2.08194341137352,1.29246349342579,26.4129482930552));
#6617=CARTESIAN_POINT('Ctrl Pts',(2.03903410005481,1.36158324685864,26.4171638943146));
#6618=CARTESIAN_POINT('Ctrl Pts',(1.99266297873646,1.42858961002957,26.421379495574));
#6619=CARTESIAN_POINT('Ctrl Pts',(1.94307303273185,1.49312338387364,26.4255950968335));
#6620=CARTESIAN_POINT('Ctrl Pts',(1.89348432412446,1.55765554743338,26.4298105929028));
#6621=CARTESIAN_POINT('Ctrl Pts',(1.84067723475091,1.61971487623718,26.4340260889721));
#6622=CARTESIAN_POINT('Ctrl Pts',(1.78493607301311,1.67897393227427,26.4382415850414));
#6623=CARTESIAN_POINT('Ctrl Pts',(1.7286042594142,1.73886091694874,26.442501749907));
#6624=CARTESIAN_POINT('Ctrl Pts',(1.66927614260175,1.79588756633635,26.4467619147726));
#6625=CARTESIAN_POINT('Ctrl Pts',(1.60728323947997,1.84975426424343,26.4510220796382));
#6626=CARTESIAN_POINT('Ctrl Pts',(1.5458510113146,1.90313378205441,26.4552437148071));
#6627=CARTESIAN_POINT('Ctrl Pts',(1.48180241256385,1.95341003501743,26.4594653499761));
#6628=CARTESIAN_POINT('Ctrl Pts',(1.41549171495736,2.00033333594356,26.463686985145));
#6629=CARTESIAN_POINT('Ctrl Pts',(1.3482732182542,2.04789902085493,26.4679664148589));
#6630=CARTESIAN_POINT('Ctrl Pts',(1.27873063476726,2.09201898923055,26.4722458445728));
#6631=CARTESIAN_POINT('Ctrl Pts',(1.20725977014175,2.13248073787251,26.4765252742868));
#6632=CARTESIAN_POINT('Ctrl Pts',(1.13578890551627,2.17294248651446,26.4808047040007));
#6633=CARTESIAN_POINT('Ctrl Pts',(1.06239022765329,2.20974585407228,26.4850841337146));
#6634=CARTESIAN_POINT('Ctrl Pts',(0.987479701805511,2.24272916075974,26.4893635634285));
#6635=CARTESIAN_POINT('Ctrl Pts',(0.91342214548648,2.27533690266184,26.4935942653687));
#6636=CARTESIAN_POINT('Ctrl Pts',(0.837608461737238,2.30433382219647,26.497824967309));
#6637=CARTESIAN_POINT('Ctrl Pts',(0.760425119890666,2.32952868345493,26.5020556692492));
#6638=CARTESIAN_POINT('Ctrl Pts',(0.68335266926873,2.35468734663032,26.5062802928349));
#6639=CARTESIAN_POINT('Ctrl Pts',(0.604914907103,2.37605465728765,26.5105049164206));
#6640=CARTESIAN_POINT('Ctrl Pts',(0.525519405337245,2.39348691339936,26.5147295400063));
#6641=CARTESIAN_POINT('Ctrl Pts',(0.445811418584786,2.41098777942218,26.5189707908746));
#6642=CARTESIAN_POINT('Ctrl Pts',(0.365138571433456,2.42452235803861,26.5232120417429));
#6643=CARTESIAN_POINT('Ctrl Pts',(0.283929885615853,2.4339954950768,26.5274532926112));
#6644=CARTESIAN_POINT('Ctrl Pts',(0.203185553148079,2.44341446447427,26.5316702918981));
#6645=CARTESIAN_POINT('Ctrl Pts',(0.121911959835773,2.44881825868422,26.5358872911851));
#6646=CARTESIAN_POINT('Ctrl Pts',(0.0405404212310668,2.45016463206994,26.5401042904721));
#6647=CARTESIAN_POINT('Ctrl Pts',(-0.0408041409284087,2.45151055910343,
26.5443198917315));
#6648=CARTESIAN_POINT('Ctrl Pts',(-0.122246119270063,2.44880172881243,26.5485354929909));
#6649=CARTESIAN_POINT('Ctrl Pts',(-0.203351959350605,2.44204795829817,26.5527510942504));
#6650=CARTESIAN_POINT('Ctrl Pts',(-0.284455775630999,2.43529435630793,26.5569665903197));
#6651=CARTESIAN_POINT('Ctrl Pts',(-0.365223006960328,2.42449605444537,26.561182086389));
#6652=CARTESIAN_POINT('Ctrl Pts',(-0.445224429430876,2.40971480832026,26.5653975824583));
#6653=CARTESIAN_POINT('Ctrl Pts',(-0.52607357354143,2.39477693520253,26.5696577473239));
#6654=CARTESIAN_POINT('Ctrl Pts',(-0.606140103296564,2.37577127820766,26.5739179121894));
#6655=CARTESIAN_POINT('Ctrl Pts',(-0.684992626948215,2.35281434691022,26.578178077055));
#6656=CARTESIAN_POINT('Ctrl Pts',(-0.763131994206052,2.33006504222483,26.582399712224));
#6657=CARTESIAN_POINT('Ctrl Pts',(-0.840078802226663,2.30343585993539,26.5866213473929));
#6658=CARTESIAN_POINT('Ctrl Pts',(-0.915431317716265,2.27308947306178,26.5908429825619));
#6659=CARTESIAN_POINT('Ctrl Pts',(-0.991815415558578,2.24232764156811,26.5951224122758));
#6660=CARTESIAN_POINT('Ctrl Pts',(-1.0665607894182,2.20774626487489,26.5994018419897));
#6661=CARTESIAN_POINT('Ctrl Pts',(-1.13927448176761,2.16956306780724,26.6036812717035));
#6662=CARTESIAN_POINT('Ctrl Pts',(-1.21198817411702,2.13137987073958,26.6079607014174));
#6663=CARTESIAN_POINT('Ctrl Pts',(-1.28266979597243,2.08959515933178,26.6122401311313));
#6664=CARTESIAN_POINT('Ctrl Pts',(-1.35095820532172,2.04447112414774,26.6165195608451));
#6665=CARTESIAN_POINT('Ctrl Pts',(-1.41832965217767,1.99995300508045,26.6207415272709));
#6666=CARTESIAN_POINT('Ctrl Pts',(-1.48362752635917,1.95201570998207,26.6249634936967));
#6667=CARTESIAN_POINT('Ctrl Pts',(-1.54648268776721,1.90087915092893,26.6291854601224));
#6668=CARTESIAN_POINT('Ctrl Pts',(-1.60924745713461,1.84981613138824,26.6334013549361));
#6669=CARTESIAN_POINT('Ctrl Pts',(-1.66957613039096,1.79556327676192,26.6376172497497));
#6670=CARTESIAN_POINT('Ctrl Pts',(-1.72712802140379,1.73838403342927,26.6418331445633));
#6671=CARTESIAN_POINT('Ctrl Pts',(-1.78461321438355,1.68127105626088,26.6460441534925));
#6672=CARTESIAN_POINT('Ctrl Pts',(-1.83932769036454,1.6212387574482,26.6502551624216));
#6673=CARTESIAN_POINT('Ctrl Pts',(-1.8909645520255,1.55859016838392,26.6544661713508));
#6674=CARTESIAN_POINT('Ctrl Pts',(-1.94256868566679,1.49598128669512,26.6586745112954));
#6675=CARTESIAN_POINT('Ctrl Pts',(-1.99109878021824,1.4307597655692,26.6628828512401));
#6676=CARTESIAN_POINT('Ctrl Pts',(-2.03628630091386,1.36326385953364,26.6670911911847));
#6677=CARTESIAN_POINT('Ctrl Pts',(-2.08145918883104,1.29578981025462,26.6712981683703));
#6678=CARTESIAN_POINT('Ctrl Pts',(-2.1232913924644,1.22604322647842,26.6755051455558));
#6679=CARTESIAN_POINT('Ctrl Pts',(-2.16155690934235,1.15439247124813,26.6797121227413));
#6680=CARTESIAN_POINT('Ctrl Pts',(-2.19982189664528,1.08274270762734,26.6839190417044));
#6681=CARTESIAN_POINT('Ctrl Pts',(-2.23452007640588,1.00918923772036,26.6881259606676));
#6682=CARTESIAN_POINT('Ctrl Pts',(-2.26547144885562,0.934124919065986,26.6923328796307));
#6683=CARTESIAN_POINT('Ctrl Pts',(-2.29645345916513,0.858986296434502,26.6965439629001));
#6684=CARTESIAN_POINT('Ctrl Pts',(-2.32368107498441,0.782334270583932,26.7007550461695));
#6685=CARTESIAN_POINT('Ctrl Pts',(-2.34702275463055,0.704581038097405,26.7049661294388));
#6686=CARTESIAN_POINT('Ctrl Pts',(-2.37037558795416,0.626790651708913,26.7091792249484));
#6687=CARTESIAN_POINT('Ctrl Pts',(-2.38983867445901,0.547898464758642,26.7133923204579));
#6688=CARTESIAN_POINT('Ctrl Pts',(-2.40533126163322,0.46832870060454,26.7176054159674));
#6689=CARTESIAN_POINT('Ctrl Pts',(-2.42085181558977,0.388615299351612,26.7218261168383));
#6690=CARTESIAN_POINT('Ctrl Pts',(-2.43238748256542,0.308222340536783,26.7260468177092));
#6691=CARTESIAN_POINT('Ctrl Pts',(-2.43990926163117,0.227580853778281,26.7302675185802));
#6692=CARTESIAN_POINT('Ctrl Pts',(-2.44698128365247,0.151761241795204,26.7342358469828));
#6693=CARTESIAN_POINT('Ctrl Pts',(-2.45050555932684,0.0757222904315045,
26.7382041753854));
#6694=CARTESIAN_POINT('Ctrl Pts',(-2.45049999341142,-0.000179695899241593,
26.742172503788));
#6695=CARTESIAN_POINT('',(-2.45049902004185,0.00219152320424601,27.542172503788));
#6696=CARTESIAN_POINT('Ctrl Pts',(-2.45452295415184,-0.000179990904159599,
26.742172503788));
#6697=CARTESIAN_POINT('Ctrl Pts',(-2.45453308230378,-0.00977866906062366,
26.742673521946));
#6698=CARTESIAN_POINT('Ctrl Pts',(-2.45448165679552,-0.0193772356258571,
26.7431745401039));
#6699=CARTESIAN_POINT('Ctrl Pts',(-2.44478272895187,-0.840936602767608,
26.7860608907341));
#6700=CARTESIAN_POINT('Ctrl Pts',(-1.53984852038364,-2.45440278088368,26.8708315556785));
#6701=CARTESIAN_POINT('Ctrl Pts',(1.22986537187606,-2.62348196936699,26.9979875530954));
#6702=CARTESIAN_POINT('Ctrl Pts',(2.87157588413716,-0.386365653463097,27.125143550512));
#6703=CARTESIAN_POINT('Ctrl Pts',(1.87954503144942,2.20511608567141,27.2522995479289));
#6704=CARTESIAN_POINT('Ctrl Pts',(-0.836359992199049,2.77411759663995,27.3794555453455));
#6705=CARTESIAN_POINT('Ctrl Pts',(-2.31723874763037,1.2730729954971,27.4760796842579));
#6706=CARTESIAN_POINT('Ctrl Pts',(-2.4513351212562,0.230535148772026,27.5303184906982));
#6707=CARTESIAN_POINT('Ctrl Pts',(-2.44936820280003,0.00220089695502133,
27.5421719646662));
#6708=CARTESIAN_POINT('',(-2.45026626984745,-0.000935076283515541,28.3421725466424));
#6709=CARTESIAN_POINT('Ctrl Pts',(-2.45049902004185,0.00219152320424601,
27.542172503788));
#6710=CARTESIAN_POINT('Ctrl Pts',(-2.45057110097415,-0.0784073286065062,
27.5463547214738));
#6711=CARTESIAN_POINT('Ctrl Pts',(-2.44666247325055,-0.159090238606502,
27.5505369391595));
#6712=CARTESIAN_POINT('Ctrl Pts',(-2.43877499133098,-0.239430139411436,
27.5547191568453));
#6713=CARTESIAN_POINT('Ctrl Pts',(-2.43089124206684,-0.319732020329891,
27.5588993953471));
#6714=CARTESIAN_POINT('Ctrl Pts',(-2.41903242136486,-0.399690743455314,
27.5630796338489));
#6715=CARTESIAN_POINT('Ctrl Pts',(-2.40325239789582,-0.478882200554593,
27.5672598723508));
#6716=CARTESIAN_POINT('Ctrl Pts',(-2.3874748013853,-0.558061478053362,27.5714394679343));
#6717=CARTESIAN_POINT('Ctrl Pts',(-2.36777729279802,-0.63647325944333,27.5756190635179));
#6718=CARTESIAN_POINT('Ctrl Pts',(-2.34426496445741,-0.713703037976942,
27.5797986591014));
#6719=CARTESIAN_POINT('Ctrl Pts',(-2.32074874143595,-0.790945609175494,
27.5839789470107));
#6720=CARTESIAN_POINT('Ctrl Pts',(-2.29341658455421,-0.867005336428038,
27.5881592349201));
#6721=CARTESIAN_POINT('Ctrl Pts',(-2.26242315094726,-0.941483794899246,
27.5923395228294));
#6722=CARTESIAN_POINT('Ctrl Pts',(-2.23139545641689,-1.01604458373739,27.5965244317344));
#6723=CARTESIAN_POINT('Ctrl Pts',(-2.196698593716,-1.08902017892509,27.6007093406394));
#6724=CARTESIAN_POINT('Ctrl Pts',(-2.15853467669294,-1.16003374929961,27.6048942495445));
#6725=CARTESIAN_POINT('Ctrl Pts',(-2.12034575527327,-1.2310938466456,27.6090819003358));
#6726=CARTESIAN_POINT('Ctrl Pts',(-2.07868550646591,-1.30018895778965,27.6132695511272));
#6727=CARTESIAN_POINT('Ctrl Pts',(-2.03379981297051,-1.36697058152731,27.6174572019185));
#6728=CARTESIAN_POINT('Ctrl Pts',(-1.98884110883246,-1.43386083161975,27.6216516643029));
#6729=CARTESIAN_POINT('Ctrl Pts',(-1.94064677863042,-1.49842971071796,27.6258461266873));
#6730=CARTESIAN_POINT('Ctrl Pts',(-1.88950296486415,-1.56036175157223,27.6300405890716));
#6731=CARTESIAN_POINT('Ctrl Pts',(-1.87435517587577,-1.5787048006606,27.6312829061074));
#6732=CARTESIAN_POINT('Ctrl Pts',(-1.85894889207162,-1.59681678924659,27.6325252231432));
#6733=CARTESIAN_POINT('Ctrl Pts',(-1.84329213690865,-1.61469017090299,27.633767540179));
#6734=CARTESIAN_POINT('Ctrl Pts',(-1.78997316716346,-1.67555784660354,27.6379982421193));
#6735=CARTESIAN_POINT('Ctrl Pts',(-1.73353580191242,-1.73389616839656,27.6422289440595));
#6736=CARTESIAN_POINT('Ctrl Pts',(-1.6742493745229,-1.78936840307123,27.6464596459998));
#6737=CARTESIAN_POINT('Ctrl Pts',(-1.61504812541635,-1.84476093940835,27.6506842695855));
#6738=CARTESIAN_POINT('Ctrl Pts',(-1.55300628043507,-1.89729525171571,27.6549088931712));
#6739=CARTESIAN_POINT('Ctrl Pts',(-1.48843239794904,-1.94666875629514,27.6591335167569));
#6740=CARTESIAN_POINT('Ctrl Pts',(-1.42360436543733,-1.99623658522016,27.6633747676251));
#6741=CARTESIAN_POINT('Ctrl Pts',(-1.3562246341688,-2.04261831545966,27.6676160184934));
#6742=CARTESIAN_POINT('Ctrl Pts',(-1.28664173093568,-2.08554628484118,27.6718572693617));
#6743=CARTESIAN_POINT('Ctrl Pts',(-1.21745670452936,-2.12822879099186,27.6760742686487));
#6744=CARTESIAN_POINT('Ctrl Pts',(-1.14609403315353,-2.16749667985583,27.6802912679356));
#6745=CARTESIAN_POINT('Ctrl Pts',(-1.07292669755125,-2.20312926349812,27.6845082672226));
#6746=CARTESIAN_POINT('Ctrl Pts',(-0.999783618521376,-2.23875003415941,
27.688723868482));
#6747=CARTESIAN_POINT('Ctrl Pts',(-0.924837481141474,-2.27073768942765,
27.6929394697414));
#6748=CARTESIAN_POINT('Ctrl Pts',(-0.848485312637826,-2.29891777239594,
27.6971550710009));
#6749=CARTESIAN_POINT('Ctrl Pts',(-0.772135049318076,-2.32709715219834,
27.7013705670702));
#6750=CARTESIAN_POINT('Ctrl Pts',(-0.694379261299073,-2.35146898859246,
27.7055860631395));
#6751=CARTESIAN_POINT('Ctrl Pts',(-0.615633016713064,-2.37190772137804,
27.7098015592088));
#6752=CARTESIAN_POINT('Ctrl Pts',(-0.536052350768313,-2.39256302976379,
27.7140617240744));
#6753=CARTESIAN_POINT('Ctrl Pts',(-0.455460577743858,-2.40920124798699,
27.7183218889399));
#6754=CARTESIAN_POINT('Ctrl Pts',(-0.374297886007632,-2.4217455156416,27.7225820538055));
#6755=CARTESIAN_POINT('Ctrl Pts',(-0.293869244240767,-2.43417633068528,
27.7268036889745));
#6756=CARTESIAN_POINT('Ctrl Pts',(-0.212880443295209,-2.44258696296556,
27.7310253241435));
#6757=CARTESIAN_POINT('Ctrl Pts',(-0.131764318647519,-2.44695492691046,
27.7352469593124));
#6758=CARTESIAN_POINT('Ctrl Pts',(-0.0495377073466007,-2.45138268865368,
27.7395263890263));
#6759=CARTESIAN_POINT('Ctrl Pts',(0.0328192455463651,-2.4516562533755,27.7438058187402));
#6760=CARTESIAN_POINT('Ctrl Pts',(0.114858375165966,-2.44780673331336,27.7480852484541));
#6761=CARTESIAN_POINT('Ctrl Pts',(0.196897504785545,-2.44395721325122,27.752364678168));
#6762=CARTESIAN_POINT('Ctrl Pts',(0.278618329221147,-2.43598472122155,27.7566441078819));
#6763=CARTESIAN_POINT('Ctrl Pts',(0.359582709140937,-2.42397411811407,27.7609235375958));
#6764=CARTESIAN_POINT('Ctrl Pts',(0.439625187255609,-2.41210027387136,27.765154239536));
#6765=CARTESIAN_POINT('Ctrl Pts',(0.519229428312936,-2.39623519297798,27.7693849414763));
#6766=CARTESIAN_POINT('Ctrl Pts',(0.59796650105694,-2.37642300813927,27.7736156434165));
#6767=CARTESIAN_POINT('Ctrl Pts',(0.676590450292641,-2.35663928795868,27.7778402670022));
#6768=CARTESIAN_POINT('Ctrl Pts',(0.754349258430402,-2.33291983907704,27.7820648905878));
#6769=CARTESIAN_POINT('Ctrl Pts',(0.830821468792822,-2.30536026186645,27.7862895141735));
#6770=CARTESIAN_POINT('Ctrl Pts',(0.907594658645635,-2.27769221561246,27.7905307650418));
#6771=CARTESIAN_POINT('Ctrl Pts',(0.983070631995018,-2.24615381785988,27.7947720159101));
#6772=CARTESIAN_POINT('Ctrl Pts',(1.05683565332173,-2.21089317966021,27.7990132667784));
#6773=CARTESIAN_POINT('Ctrl Pts',(1.13017888436282,-2.17583416269497,27.8032302660653));
#6774=CARTESIAN_POINT('Ctrl Pts',(1.20183025301574,-2.13709556008903,27.8074472653523));
#6775=CARTESIAN_POINT('Ctrl Pts',(1.27140227804613,-2.0948714751457,27.8116642646392));
#6776=CARTESIAN_POINT('Ctrl Pts',(1.34095123842816,-2.05266138841028,27.8158798658986));
#6777=CARTESIAN_POINT('Ctrl Pts',(1.40842182686203,-2.00696835508931,27.8200954671581));
#6778=CARTESIAN_POINT('Ctrl Pts',(1.47345241214717,-1.95803172577405,27.8243110684175));
#6779=CARTESIAN_POINT('Ctrl Pts',(1.53848137475138,-1.90909631755397,27.8285265644868));
#6780=CARTESIAN_POINT('Ctrl Pts',(1.6010700843135,-1.85691775476208,27.8327420605561));
#6781=CARTESIAN_POINT('Ctrl Pts',(1.66088825234669,-1.80177702927325,27.8369575566254));
#6782=CARTESIAN_POINT('Ctrl Pts',(1.72134027355368,-1.74605201434518,27.8412177214909));
#6783=CARTESIAN_POINT('Ctrl Pts',(1.77896232133683,-1.68730200333099,27.8454778863565));
#6784=CARTESIAN_POINT('Ctrl Pts',(1.83345145153445,-1.6258554747782,27.8497380512221));
#6785=CARTESIAN_POINT('Ctrl Pts',(1.88744777224637,-1.56496467967213,27.8539596863911));
#6786=CARTESIAN_POINT('Ctrl Pts',(1.93836737087129,-1.50142635194949,27.85818132156));
#6787=CARTESIAN_POINT('Ctrl Pts',(1.98595700024085,-1.43559222733838,27.862402956729));
#6788=CARTESIAN_POINT('Ctrl Pts',(2.03419813568892,-1.36885682795531,27.8666823864429));
#6789=CARTESIAN_POINT('Ctrl Pts',(2.07901716722112,-1.29976271141826,27.8709618161568));
#6790=CARTESIAN_POINT('Ctrl Pts',(2.12019761091784,-1.22870352024331,27.8752412458707));
#6791=CARTESIAN_POINT('Ctrl Pts',(2.16137805461456,-1.15764432906833,27.8795206755846));
#6792=CARTESIAN_POINT('Ctrl Pts',(2.19891974441495,-1.08462052950557,27.8838001052985));
#6793=CARTESIAN_POINT('Ctrl Pts',(2.23265681392579,-1.01004643518541,27.8880795350124));
#6794=CARTESIAN_POINT('Ctrl Pts',(2.26600973592246,-0.936321479612911,27.8923102369527));
#6795=CARTESIAN_POINT('Ctrl Pts',(2.29576972894447,-0.860804072338553,27.8965409388929));
#6796=CARTESIAN_POINT('Ctrl Pts',(2.32174166943258,-0.783878734512165,27.9007716408332));
#6797=CARTESIAN_POINT('Ctrl Pts',(2.34767629538852,-0.707063917229848,27.9049962644189));
#6798=CARTESIAN_POINT('Ctrl Pts',(2.3698335301912,-0.62884562369093,27.9092208880045));
#6799=CARTESIAN_POINT('Ctrl Pts',(2.38806556893476,-0.549629955941546,27.9134455115902));
#6800=CARTESIAN_POINT('Ctrl Pts',(2.40636936537573,-0.470102510996157,27.9176867624585));
#6801=CARTESIAN_POINT('Ctrl Pts',(2.42071680629514,-0.389570256433736,27.9219280133268));
#6802=CARTESIAN_POINT('Ctrl Pts',(2.43100841586237,-0.308461232582512,27.9261692641951));
#6803=CARTESIAN_POINT('Ctrl Pts',(2.44124117774191,-0.227815992211736,27.930386263482));
#6804=CARTESIAN_POINT('Ctrl Pts',(2.44746430597289,-0.146601026615822,27.934603262769));
#6805=CARTESIAN_POINT('Ctrl Pts',(2.44963120743723,-0.0652472033854291,
27.9388202620559));
#6806=CARTESIAN_POINT('Ctrl Pts',(2.45179739052633,0.0160796492728611,27.9430358633154));
#6807=CARTESIAN_POINT('Ctrl Pts',(2.44991000487725,0.0975448036220795,27.9472514645748));
#6808=CARTESIAN_POINT('Ctrl Pts',(2.44397449488418,0.178714628264212,27.9514670658342));
#6809=CARTESIAN_POINT('Ctrl Pts',(2.43803913299742,0.259882427509452,27.9556825619035));
#6810=CARTESIAN_POINT('Ctrl Pts',(2.42805588260075,0.340754447956536,27.9598980579728));
#6811=CARTESIAN_POINT('Ctrl Pts',(2.41408216762736,0.420900864745565,27.9641135540421));
#6812=CARTESIAN_POINT('Ctrl Pts',(2.39996038252952,0.501896539583101,27.9683737189077));
#6813=CARTESIAN_POINT('Ctrl Pts',(2.38176312807834,0.582150661691083,27.9726338837733));
#6814=CARTESIAN_POINT('Ctrl Pts',(2.35960255752585,0.661230686309594,27.9768940486389));
#6815=CARTESIAN_POINT('Ctrl Pts',(2.33764241115584,0.739595496974264,27.9811156838078));
#6816=CARTESIAN_POINT('Ctrl Pts',(2.31179055803483,0.816806935920526,27.9853373189768));
#6817=CARTESIAN_POINT('Ctrl Pts',(2.28220561160531,0.892461649796356,27.9895589541458));
#6818=CARTESIAN_POINT('Ctrl Pts',(2.25221564474001,0.969152083147142,27.9938383838597));
#6819=CARTESIAN_POINT('Ctrl Pts',(2.218389801083,1.0442423942957,27.9981178135736));
#6820=CARTESIAN_POINT('Ctrl Pts',(2.18094183158237,1.11733745003653,28.0023972432875));
#6821=CARTESIAN_POINT('Ctrl Pts',(2.14349386208176,1.19043250577734,28.0066766730014));
#6822=CARTESIAN_POINT('Ctrl Pts',(2.10242406883352,1.26153191406017,28.0109561027153));
#6823=CARTESIAN_POINT('Ctrl Pts',(2.0579909871091,1.33027190715948,28.0152355324292));
#6824=CARTESIAN_POINT('Ctrl Pts',(2.0140638431598,1.3982291915692,28.0194662343694));
#6825=CARTESIAN_POINT('Ctrl Pts',(1.96668442764717,1.46413614849936,28.0236969363097));
#6826=CARTESIAN_POINT('Ctrl Pts',(1.91607038741418,1.52762054204389,28.0279276382499));
#6827=CARTESIAN_POINT('Ctrl Pts',(1.86552906563014,1.59101372598314,28.0321522618356));
#6828=CARTESIAN_POINT('Ctrl Pts',(1.81176263630591,1.65199089856441,28.0363768854213));
#6829=CARTESIAN_POINT('Ctrl Pts',(1.75503250946487,1.7102079232425,28.040601509007));
#6830=CARTESIAN_POINT('Ctrl Pts',(1.69807910406848,1.76865407861167,28.0448427598753));
#6831=CARTESIAN_POINT('Ctrl Pts',(1.6381388796792,1.82431791414242,28.0490840107436));
#6832=CARTESIAN_POINT('Ctrl Pts',(1.57551785703004,1.87688404867735,28.0533252616119));
#6833=CARTESIAN_POINT('Ctrl Pts',(1.51325490299569,1.92914960870578,28.0575422608988));
#6834=CARTESIAN_POINT('Ctrl Pts',(1.44834208503497,1.97835249506572,28.0617592601858));
#6835=CARTESIAN_POINT('Ctrl Pts',(1.38111643225006,2.02422025742478,28.0659762594728));
#6836=CARTESIAN_POINT('Ctrl Pts',(1.31391306623971,2.0700728136172,28.0701918607322));
#6837=CARTESIAN_POINT('Ctrl Pts',(1.244398771907,2.11259217957174,28.0744074619917));
#6838=CARTESIAN_POINT('Ctrl Pts',(1.17294107577154,2.1515481595279,28.0786230632511));
#6839=CARTESIAN_POINT('Ctrl Pts',(1.10148516269026,2.19050316743169,28.0828385593204));
#6840=CARTESIAN_POINT('Ctrl Pts',(1.02808635306628,2.22589474447314,28.0870540553897));
#6841=CARTESIAN_POINT('Ctrl Pts',(0.953137115381867,2.25753845798505,28.091269551459));
#6842=CARTESIAN_POINT('Ctrl Pts',(0.877393690685013,2.28951747879391,28.0955297163246));
#6843=CARTESIAN_POINT('Ctrl Pts',(0.800067224636503,2.31766853265157,28.0997898811902));
#6844=CARTESIAN_POINT('Ctrl Pts',(0.721582103596555,2.34185172839127,28.1040500460557));
#6845=CARTESIAN_POINT('Ctrl Pts',(0.643806816095354,2.36581620696289,28.1082716812247));
#6846=CARTESIAN_POINT('Ctrl Pts',(0.564894218405332,2.38588425469449,28.1124933163937));
#6847=CARTESIAN_POINT('Ctrl Pts',(0.485269308088415,2.40197084674802,28.1167149515627));
#6848=CARTESIAN_POINT('Ctrl Pts',(0.404554325969565,2.41827766561645,28.1209943812765));
#6849=CARTESIAN_POINT('Ctrl Pts',(0.32310786949343,2.43049311709884,28.1252738109904));
#6850=CARTESIAN_POINT('Ctrl Pts',(0.241377877170622,2.43858298411446,28.1295532407043));
#6851=CARTESIAN_POINT('Ctrl Pts',(0.159647884847813,2.44667285113009,28.1338326704182));
#6852=CARTESIAN_POINT('Ctrl Pts',(0.0776348498558789,2.45063717540778,28.1381121001321));
#6853=CARTESIAN_POINT('Ctrl Pts',(-0.0042154132946402,2.45049637426599,
28.1423915298459));
#6854=CARTESIAN_POINT('Ctrl Pts',(-0.0851336875212073,2.45035717635795,
28.1466222317862));
#6855=CARTESIAN_POINT('Ctrl Pts',(-0.166197234216248,2.44620538357499,28.1508529337264));
#6856=CARTESIAN_POINT('Ctrl Pts',(-0.246975256662254,2.43802245120848,28.1550836356667));
#6857=CARTESIAN_POINT('Ctrl Pts',(-0.327637223316661,2.42985127546419,28.1593082592524));
#6858=CARTESIAN_POINT('Ctrl Pts',(-0.408014021674497,2.41766050912256,28.1635328828381));
#6859=CARTESIAN_POINT('Ctrl Pts',(-0.48767478586299,2.40148361502499,28.1677575064237));
#6860=CARTESIAN_POINT('Ctrl Pts',(-0.567649079058921,2.38524305187275,28.171998757292));
#6861=CARTESIAN_POINT('Ctrl Pts',(-0.646901215105209,2.3649849172612,28.1762400081603));
#6862=CARTESIAN_POINT('Ctrl Pts',(-0.725000351671044,2.34079574932903,28.1804812590286));
#6863=CARTESIAN_POINT('Ctrl Pts',(-0.802652915369348,2.31674489567998,28.1846982583155));
#6864=CARTESIAN_POINT('Ctrl Pts',(-0.879165180861529,2.2888079811939,28.1889152576025));
#6865=CARTESIAN_POINT('Ctrl Pts',(-0.95412561193247,2.25712085778642,28.1931322568895));
#6866=CARTESIAN_POINT('Ctrl Pts',(-1.02906119198054,2.22544423935359,28.1973478581489));
#6867=CARTESIAN_POINT('Ctrl Pts',(-1.10244553123049,2.19002006186729,28.2015634594083));
#6868=CARTESIAN_POINT('Ctrl Pts',(-1.17388610765331,2.15103269530209,28.2057790606678));
#6869=CARTESIAN_POINT('Ctrl Pts',(-1.24532490144929,2.11204630157234,28.2099945567371));
#6870=CARTESIAN_POINT('Ctrl Pts',(-1.31481962114464,2.06949711927496,28.2142100528064));
#6871=CARTESIAN_POINT('Ctrl Pts',(-1.38200271650126,2.02361526520807,28.2184255488757));
#6872=CARTESIAN_POINT('Ctrl Pts',(-1.44989770624718,1.97724723177853,28.2226857137413));
#6873=CARTESIAN_POINT('Ctrl Pts',(-1.5154313813222,1.92747573776811,28.2269458786069));
#6874=CARTESIAN_POINT('Ctrl Pts',(-1.57825635937258,1.87458185046693,28.2312060434724));
#6875=CARTESIAN_POINT('Ctrl Pts',(-1.64051313703158,1.82216634498773,28.2354276786414));
#6876=CARTESIAN_POINT('Ctrl Pts',(-1.70010971435821,1.76668506359559,28.2396493138104));
#6877=CARTESIAN_POINT('Ctrl Pts',(-1.75674450736549,1.70844929273338,28.2438709489794));
#6878=CARTESIAN_POINT('Ctrl Pts',(-1.81415463551125,1.64941626920954,28.2481503786932));
#6879=CARTESIAN_POINT('Ctrl Pts',(-1.86852094463015,1.58755313834589,28.2524298084071));
#6880=CARTESIAN_POINT('Ctrl Pts',(-1.91957214723803,1.52321798228224,28.256709238121));
#6881=CARTESIAN_POINT('Ctrl Pts',(-1.9706233498459,1.4588828262186,28.2609886678349));
#6882=CARTESIAN_POINT('Ctrl Pts',(-2.01835921401441,1.39207608219018,28.2652680975488));
#6883=CARTESIAN_POINT('Ctrl Pts',(-2.06255553650031,1.32318362627866,28.2695475272627));
#6884=CARTESIAN_POINT('Ctrl Pts',(-2.10727116745891,1.25348168138597,28.2738772404387));
#6885=CARTESIAN_POINT('Ctrl Pts',(-2.14852584144257,1.1813923810335,28.2782069536148));
#6886=CARTESIAN_POINT('Ctrl Pts',(-2.18606292576872,1.10728457705303,28.2825366667908));
#6887=CARTESIAN_POINT('Ctrl Pts',(-2.22353816353643,1.03329887399521,28.2868592462786));
#6888=CARTESIAN_POINT('Ctrl Pts',(-2.25730779196065,0.957301663987129,28.2911818257663));
#6889=CARTESIAN_POINT('Ctrl Pts',(-2.28715895920242,0.879689800634359,28.2955044052541));
#6890=CARTESIAN_POINT('Ctrl Pts',(-2.31695826439981,0.802212776561693,28.2998194748911));
#6891=CARTESIAN_POINT('Ctrl Pts',(-2.34285250298353,0.723127087240737,28.3041345445282));
#6892=CARTESIAN_POINT('Ctrl Pts',(-2.36467584532766,0.642851768702489,28.3084496141652));
#6893=CARTESIAN_POINT('Ctrl Pts',(-2.38647684186234,0.562658647333804,28.3127602654267));
#6894=CARTESIAN_POINT('Ctrl Pts',(-2.40421511332852,0.481278736729459,28.3170709166881));
#6895=CARTESIAN_POINT('Ctrl Pts',(-2.41777398446114,0.399148105423142,28.3213815679495));
#6896=CARTESIAN_POINT('Ctrl Pts',(-2.43132082051003,0.317090374656657,28.3256883930038));
#6897=CARTESIAN_POINT('Ctrl Pts',(-2.44069556608515,0.23428367808359,28.3299952180582));
#6898=CARTESIAN_POINT('Ctrl Pts',(-2.44583244848935,0.151175010886655,28.3343020431125));
#6899=CARTESIAN_POINT('Ctrl Pts',(-2.4489615618112,0.100549667103463,28.3369255300043));
#6900=CARTESIAN_POINT('Ctrl Pts',(-2.45051917085278,0.0498124829442886,
28.3395490168962));
#6901=CARTESIAN_POINT('Ctrl Pts',(-2.45049982187577,-0.000934337642672194,
28.342172503788));
#6902=CARTESIAN_POINT('',(-2.45279378259028,-0.00178251821640208,29.142172503788));
#6903=CARTESIAN_POINT('Ctrl Pts',(-2.44679612755061,-0.000946051092217225,
28.3421731833771));
#6904=CARTESIAN_POINT('Ctrl Pts',(-2.44799346344638,-0.352013542706997,
28.3603499638112));
#6905=CARTESIAN_POINT('Ctrl Pts',(-2.21301223344718,-1.52018191572573,28.4209120767176));
#6906=CARTESIAN_POINT('Ctrl Pts',(-0.415304599242627,-2.86753353361047,
28.5238595220962));
#6907=CARTESIAN_POINT('Ctrl Pts',(2.18604956098726,-1.90168709135936,28.651015519513));
#6908=CARTESIAN_POINT('Ctrl Pts',(2.78241085774888,0.808341694590506,28.7781715169296));
#6909=CARTESIAN_POINT('Ctrl Pts',(0.826810839185443,2.77697863022819,28.9053275143464));
#6910=CARTESIAN_POINT('Ctrl Pts',(-1.7628525210818,2.22511821664602,29.0266611766324));
#6911=CARTESIAN_POINT('Ctrl Pts',(-2.44705224933042,0.700008483504726,29.1056095064463));
#6912=CARTESIAN_POINT('Ctrl Pts',(-2.45279378259028,-0.00178251821640208,
29.142172503788));
#6913=CARTESIAN_POINT('',(-2.45241907602745,0.00192082108273114,29.942172503788));
#6914=CARTESIAN_POINT('Ctrl Pts',(-2.45279378259028,-0.00178251821640208,
29.142172503788));
#6915=CARTESIAN_POINT('Ctrl Pts',(-2.45370807116707,-0.113536551002519,
29.1479948389186));
#6916=CARTESIAN_POINT('Ctrl Pts',(-2.39595458088149,-1.0378852598289,29.1962025065213));
#6917=CARTESIAN_POINT('Ctrl Pts',(-1.22083214377427,-2.62769772866914,29.2867955065966));
#6918=CARTESIAN_POINT('Ctrl Pts',(1.54828364844088,-2.44909048842879,29.4139515040134));
#6919=CARTESIAN_POINT('Ctrl Pts',(2.89735036164549,-0.0242354782711104,
29.54110750143));
#6920=CARTESIAN_POINT('Ctrl Pts',(1.58903596980293,2.42284773834526,29.6682634988467));
#6921=CARTESIAN_POINT('Ctrl Pts',(-1.17670456466042,2.6477524136598,29.7954194962635));
#6922=CARTESIAN_POINT('Ctrl Pts',(-2.38767422187209,1.06551615028153,29.8867224979106));
#6923=CARTESIAN_POINT('Ctrl Pts',(-2.45349906928597,0.127352511453818,29.9356401670854));
#6924=CARTESIAN_POINT('Ctrl Pts',(-2.45241907602745,0.00192082108273114,
29.942172503788));
#6925=CARTESIAN_POINT('',(-2.44665768414027,0.000722135787914535,30.742172503788));
#6926=CARTESIAN_POINT('Ctrl Pts',(-2.45241907602745,0.00192082108273114,
29.942172503788));
#6927=CARTESIAN_POINT('Ctrl Pts',(-2.44649148908702,-0.686516114889533,
29.9780254995576));
#6928=CARTESIAN_POINT('Ctrl Pts',(-1.78473050610832,-2.19879978302826,30.0562638277996));
#6929=CARTESIAN_POINT('Ctrl Pts',(0.780241187801395,-2.79042114480829,30.1768874885137));
#6930=CARTESIAN_POINT('Ctrl Pts',(2.76849939206588,-0.854773415978033,30.3040434859304));
#6931=CARTESIAN_POINT('Ctrl Pts',(2.21755554772779,1.86485223792129,30.4311994833472));
#6932=CARTESIAN_POINT('Ctrl Pts',(-0.367277704650069,2.87407960296904,30.558355480764));
#6933=CARTESIAN_POINT('Ctrl Pts',(-2.19982864253972,1.54790246893413,30.6620131542442));
#6934=CARTESIAN_POINT('Ctrl Pts',(-2.44761904790825,0.365558552703536,30.7232854952522));
#6935=CARTESIAN_POINT('Ctrl Pts',(-2.44665768414027,0.000722135787914535,
30.742172503788));
#6936=CARTESIAN_POINT('',(-2.45049898092438,-0.00223483524436902,31.5421725268725));
#6937=CARTESIAN_POINT('Ctrl Pts',(-2.44665768414027,0.000722135787914535,
30.742172503788));
#6938=CARTESIAN_POINT('Ctrl Pts',(-2.44546160074793,-0.453190101942719,
30.7656708277245));
#6939=CARTESIAN_POINT('Ctrl Pts',(-2.10644501446377,-1.72751139562769,30.831554484133));
#6940=CARTESIAN_POINT('Ctrl Pts',(-0.053452762941805,-2.89695862564268,
30.9398234730143));
#6941=CARTESIAN_POINT('Ctrl Pts',(2.40669979930934,-1.61338853117316,31.0669794704308));
#6942=CARTESIAN_POINT('Ctrl Pts',(2.65948432735196,1.1499432982076,31.1941354678477));
#6943=CARTESIAN_POINT('Ctrl Pts',(0.473052841258751,2.85857437999996,31.3212914652642));
#6944=CARTESIAN_POINT('Ctrl Pts',(-1.91761420212668,2.02541820437966,31.4373038105778));
#6945=CARTESIAN_POINT('Ctrl Pts',(-2.44440761753277,0.599329367090551,31.510930823419));
#6946=CARTESIAN_POINT('Ctrl Pts',(-2.44976484792678,-0.00223372122999444,
31.542172503788));
#6947=CARTESIAN_POINT('',(-2.4504999619844,0.000431641585035285,32.3421725038399));
#6948=CARTESIAN_POINT('Ctrl Pts',(-2.45049898092438,-0.00223483524436902,
31.5421725268725));
#6949=CARTESIAN_POINT('Ctrl Pts',(-2.45040110829245,-0.109552269678379,
31.5477443490767));
#6950=CARTESIAN_POINT('Ctrl Pts',(-2.44324902256407,-0.216554533994056,
31.5533161712809));
#6951=CARTESIAN_POINT('Ctrl Pts',(-2.42919252957392,-0.322449847669802,
31.5588879934852));
#6952=CARTESIAN_POINT('Ctrl Pts',(-2.41513603658376,-0.428345161345525,
31.5644598156894));
#6953=CARTESIAN_POINT('Ctrl Pts',(-2.39417533386796,-0.533133880352394,
31.5700316378937));
#6954=CARTESIAN_POINT('Ctrl Pts',(-2.36651425439528,-0.63605073205205,31.5756034600979));
#6955=CARTESIAN_POINT('Ctrl Pts',(-2.34551111066838,-0.714195817832348,
31.5798341620375));
#6956=CARTESIAN_POINT('Ctrl Pts',(-2.3205936439755,-0.791446421958622,31.5840648639771));
#6957=CARTESIAN_POINT('Ctrl Pts',(-2.29185503851243,-0.867381537989583,
31.5882955659167));
#6958=CARTESIAN_POINT('Ctrl Pts',(-2.26315772251778,-0.943207556152907,
31.5925201895017));
#6959=CARTESIAN_POINT('Ctrl Pts',(-2.23065033426261,-1.0177214085918,31.5967448130867));
#6960=CARTESIAN_POINT('Ctrl Pts',(-2.1944763240252,-1.09051543468805,31.6009694366717));
#6961=CARTESIAN_POINT('Ctrl Pts',(-2.15815994003323,-1.16359596368338,31.6052106875402));
#6962=CARTESIAN_POINT('Ctrl Pts',(-2.11814813313033,-1.23494264121655,31.6094519384086));
#6963=CARTESIAN_POINT('Ctrl Pts',(-2.07463562739865,-1.30416151742344,31.6136931892771));
#6964=CARTESIAN_POINT('Ctrl Pts',(-2.03137192730004,-1.37298459830609,31.6179101885634));
#6965=CARTESIAN_POINT('Ctrl Pts',(-1.98464770390385,-1.43970374779104,31.6221271878497));
#6966=CARTESIAN_POINT('Ctrl Pts',(-1.93470034788398,-1.50395638696659,31.626344187136));
#6967=CARTESIAN_POINT('Ctrl Pts',(-1.88476955050527,-1.56818772498667,31.6305597883947));
#6968=CARTESIAN_POINT('Ctrl Pts',(-1.83161802763735,-1.62995380963492,31.6347753896535));
#6969=CARTESIAN_POINT('Ctrl Pts',(-1.77552514303334,-1.68892294568356,31.6389909909123));
#6970=CARTESIAN_POINT('Ctrl Pts',(-1.71943365809156,-1.74789061030008,31.643206486981));
#6971=CARTESIAN_POINT('Ctrl Pts',(-1.66040127865333,-1.80406112886422,31.6474219830496));
#6972=CARTESIAN_POINT('Ctrl Pts',(-1.59874512760668,-1.85713873120828,31.6516374791183));
#6973=CARTESIAN_POINT('Ctrl Pts',(-1.53643564748726,-1.9107787614713,31.6558976439846));
#6974=CARTESIAN_POINT('Ctrl Pts',(-1.47144681661139,-1.96125960980886,31.660157808851));
#6975=CARTESIAN_POINT('Ctrl Pts',(-1.4041397835595,-2.00831813172751,31.6644179737174));
#6976=CARTESIAN_POINT('Ctrl Pts',(-1.33744148743178,-2.05495104790201,31.6686396088857));
#6977=CARTESIAN_POINT('Ctrl Pts',(-1.26846718406831,-2.09822309531822,31.672861244054));
#6978=CARTESIAN_POINT('Ctrl Pts',(-1.19759540765003,-2.13792317204701,31.6770828792224));
#6979=CARTESIAN_POINT('Ctrl Pts',(-1.12575339054285,-2.17816674622629,31.6813623089377));
#6980=CARTESIAN_POINT('Ctrl Pts',(-1.05196199707804,-2.21473958837186,31.6856417386531));
#6981=CARTESIAN_POINT('Ctrl Pts',(-0.976637160732151,-2.24747193670512,
31.6899211683685));
#6982=CARTESIAN_POINT('Ctrl Pts',(-0.901312324386287,-2.28020428503837,
31.6942005980838));
#6983=CARTESIAN_POINT('Ctrl Pts',(-0.824454527417686,-2.30909602823866,
31.6984800277992));
#6984=CARTESIAN_POINT('Ctrl Pts',(-0.746494414108302,-2.33403006401055,
31.7027594575145));
#6985=CARTESIAN_POINT('Ctrl Pts',(-0.669421994530779,-2.35868018809575,
31.706990159454));
#6986=CARTESIAN_POINT('Ctrl Pts',(-0.590982356308357,-2.37955503273655,
31.7112208613934));
#6987=CARTESIAN_POINT('Ctrl Pts',(-0.511579914801198,-2.39650500537178,
31.7154515633328));
#6988=CARTESIAN_POINT('Ctrl Pts',(-0.432291552754534,-2.4134306255602,31.7196761869176));
#6989=CARTESIAN_POINT('Ctrl Pts',(-0.352043585654261,-2.42644247676526,
31.7239008105024));
#6990=CARTESIAN_POINT('Ctrl Pts',(-0.271256422911951,-2.43544045359952,
31.7281254340872));
#6991=CARTESIAN_POINT('Ctrl Pts',(-0.19015129785996,-2.44447384469266,31.7323666849557));
#6992=CARTESIAN_POINT('Ctrl Pts',(-0.108503175726638,-2.4494615534512,31.7366079358243));
#6993=CARTESIAN_POINT('Ctrl Pts',(-0.0267486987488107,-2.4503540064887,
31.7408491866928));
#6994=CARTESIAN_POINT('Ctrl Pts',(0.0545383040101661,-2.4512413564566,31.7450661859788));
#6995=CARTESIAN_POINT('Ctrl Pts',(0.135929978927115,-2.44808015204618,31.7492831852649));
#6996=CARTESIAN_POINT('Ctrl Pts',(0.216992958931321,-2.44087367673426,31.753500184551));
#6997=CARTESIAN_POINT('Ctrl Pts',(0.298029064784172,-2.43366959052657,31.7577157858096));
#6998=CARTESIAN_POINT('Ctrl Pts',(0.378736229252866,-2.42242293775469,31.7619313870681));
#6999=CARTESIAN_POINT('Ctrl Pts',(0.458684326233931,-2.40718901186993,31.7661469883267));
#7000=CARTESIAN_POINT('Ctrl Pts',(0.538630428303458,-2.39195546611097,31.7703624843951));
#7001=CARTESIAN_POINT('Ctrl Pts',(0.617817043906377,-2.37273493317112,31.7745779804635));
#7002=CARTESIAN_POINT('Ctrl Pts',(0.695823807960785,-2.34963390303148,31.778793476532));
#7003=CARTESIAN_POINT('Ctrl Pts',(0.774657157628108,-2.32628808669429,31.7830536413986));
#7004=CARTESIAN_POINT('Ctrl Pts',(0.852285033565486,-2.29897916753167,31.7873138062652));
#7005=CARTESIAN_POINT('Ctrl Pts',(0.928290664940497,-2.26786831438343,31.7915739711318));
#7006=CARTESIAN_POINT('Ctrl Pts',(1.00360888769279,-2.23703883339574,31.7957956062999));
#7007=CARTESIAN_POINT('Ctrl Pts',(1.07733369203311,-2.20247616804236,31.800017241468));
#7008=CARTESIAN_POINT('Ctrl Pts',(1.14908264953657,-2.16438428069833,31.8042388766361));
#7009=CARTESIAN_POINT('Ctrl Pts',(1.2218138564265,-2.12577091214711,31.808518306352));
#7010=CARTESIAN_POINT('Ctrl Pts',(1.29251428319697,-2.08353121294873,31.8127977360678));
#7011=CARTESIAN_POINT('Ctrl Pts',(1.36081601004376,-2.03792297126476,31.8170771657837));
#7012=CARTESIAN_POINT('Ctrl Pts',(1.42911773689055,-1.99231472958079,31.8213565954996));
#7013=CARTESIAN_POINT('Ctrl Pts',(1.49502040911961,-1.94333829060324,31.8256360252155));
#7014=CARTESIAN_POINT('Ctrl Pts',(1.55819241617905,-1.89129232118202,31.8299154549314));
#7015=CARTESIAN_POINT('Ctrl Pts',(1.6206451145155,-1.83983897373917,31.8341461568758));
#7016=CARTESIAN_POINT('Ctrl Pts',(1.68066394662085,-1.78519214591414,31.8383768588202));
#7017=CARTESIAN_POINT('Ctrl Pts',(1.73790418615668,-1.72761086177967,31.8426075607646));
#7018=CARTESIAN_POINT('Ctrl Pts',(1.79506218721859,-1.67011230610637,31.8468321843544));
#7019=CARTESIAN_POINT('Ctrl Pts',(1.84944919910022,-1.60968799436825,31.8510568079442));
#7020=CARTESIAN_POINT('Ctrl Pts',(1.90075344280793,-1.54663719069916,31.8552814315341));
#7021=CARTESIAN_POINT('Ctrl Pts',(1.95225960980531,-1.48333823161887,31.8595226824013));
#7022=CARTESIAN_POINT('Ctrl Pts',(2.00065832399735,-1.41739236331834,31.8637639332686));
#7023=CARTESIAN_POINT('Ctrl Pts',(2.04567150290777,-1.34913985642374,31.8680051841358));
#7024=CARTESIAN_POINT('Ctrl Pts',(2.0904272953607,-1.2812776190322,31.8722221834269));
#7025=CARTESIAN_POINT('Ctrl Pts',(2.13183590600085,-1.21113544243133,31.876439182718));
#7026=CARTESIAN_POINT('Ctrl Pts',(2.16966546536988,-1.13907946096017,31.8806561820091));
#7027=CARTESIAN_POINT('Ctrl Pts',(2.20748248341228,-1.06704736762341,31.8848717832727));
#7028=CARTESIAN_POINT('Ctrl Pts',(2.24172259043297,-0.993103140799315,31.8890873845362));
#7029=CARTESIAN_POINT('Ctrl Pts',(2.272199399449,-0.917638348775607,31.8933029857998));
#7030=CARTESIAN_POINT('Ctrl Pts',(2.30267544798981,-0.842175439793632,31.8975184818732));
#7031=CARTESIAN_POINT('Ctrl Pts',(2.32938821208528,-0.765192472678752,31.9017339779466));
#7032=CARTESIAN_POINT('Ctrl Pts',(2.35219963335275,-0.687100527474102,31.90594947402));
#7033=CARTESIAN_POINT('Ctrl Pts',(2.37525277196634,-0.608181094252511,31.9102096388807));
#7034=CARTESIAN_POINT('Ctrl Pts',(2.39432124431858,-0.528129501324468,31.9144698037414));
#7035=CARTESIAN_POINT('Ctrl Pts',(2.40931490965848,-0.447383410619295,31.918729968602));
#7036=CARTESIAN_POINT('Ctrl Pts',(2.42417296962595,-0.367367601900139,31.922951603775));
#7037=CARTESIAN_POINT('Ctrl Pts',(2.43502963113984,-0.286670281456185,31.927173238948));
#7038=CARTESIAN_POINT('Ctrl Pts',(2.44184932582133,-0.205723406509574,31.931394874121));
#7039=CARTESIAN_POINT('Ctrl Pts',(2.44876238268193,-0.123668362210968,31.9356743038255));
#7040=CARTESIAN_POINT('Ctrl Pts',(2.45152708637817,-0.0413573732052278,
31.93995373353));
#7041=CARTESIAN_POINT('Ctrl Pts',(2.45016097810504,0.0407606596040527,31.9442331632345));
#7042=CARTESIAN_POINT('Ctrl Pts',(2.44879486983191,0.12287869241331,31.948512592939));
#7043=CARTESIAN_POINT('Ctrl Pts',(2.44329804777661,0.204803283923386,31.9527920226435));
#7044=CARTESIAN_POINT('Ctrl Pts',(2.4337420804574,0.286093928301343,31.957071452348));
#7045=CARTESIAN_POINT('Ctrl Pts',(2.42429492225696,0.36645895593286,31.9613021542828));
#7046=CARTESIAN_POINT('Ctrl Pts',(2.4108450974072,0.4465066803362,31.9655328562175));
#7047=CARTESIAN_POINT('Ctrl Pts',(2.39342374342147,0.525807031548982,31.9697635581523));
#7048=CARTESIAN_POINT('Ctrl Pts',(2.37602741912777,0.604993449977305,31.9739881817325));
#7049=CARTESIAN_POINT('Ctrl Pts',(2.35467099705921,0.683434177406247,31.9782128053127));
#7050=CARTESIAN_POINT('Ctrl Pts',(2.32943728494601,0.760705058155504,31.982437428893));
#7051=CARTESIAN_POINT('Ctrl Pts',(2.30410425789335,0.838280061929099,31.9866786797626));
#7052=CARTESIAN_POINT('Ctrl Pts',(2.27486341023248,0.914675519389063,31.9909199306323));
#7053=CARTESIAN_POINT('Ctrl Pts',(2.24185026990548,0.989473404051221,31.9951611815019));
#7054=CARTESIAN_POINT('Ctrl Pts',(2.20902589961482,1.06384359236989,31.9993781807835));
#7055=CARTESIAN_POINT('Ctrl Pts',(2.17247244941019,1.13663399850397,32.0035951800651));
#7056=CARTESIAN_POINT('Ctrl Pts',(2.13237221261915,1.20745144699475,32.0078121793466));
#7057=CARTESIAN_POINT('Ctrl Pts',(2.09228526993348,1.27824541795277,32.0120277806007));
#7058=CARTESIAN_POINT('Ctrl Pts',(2.0486541046455,1.34706732579171,32.0162433818548));
#7059=CARTESIAN_POINT('Ctrl Pts',(2.00170701861743,1.41354846454507,32.0204589831089));
#7060=CARTESIAN_POINT('Ctrl Pts',(1.95476110403985,1.4800279444231,32.0246744791729));
#7061=CARTESIAN_POINT('Ctrl Pts',(1.90449970238342,1.54416639208367,32.0288899752369));
#7062=CARTESIAN_POINT('Ctrl Pts',(1.85119368584224,1.60562517029904,32.0331054713009));
#7063=CARTESIAN_POINT('Ctrl Pts',(1.79732282089863,1.66773518630974,32.0373656361729));
#7064=CARTESIAN_POINT('Ctrl Pts',(1.74034273862756,1.72710802884717,32.0416258010449));
#7065=CARTESIAN_POINT('Ctrl Pts',(1.68057260332205,1.78343095604044,32.0458859659169));
#7066=CARTESIAN_POINT('Ctrl Pts',(1.62134304002219,1.839244488407,32.0501076010807));
#7067=CARTESIAN_POINT('Ctrl Pts',(1.55937408609916,1.89206279345411,32.0543292362446));
#7068=CARTESIAN_POINT('Ctrl Pts',(1.4950096556947,1.94162210004409,32.0585508714084));
#7069=CARTESIAN_POINT('Ctrl Pts',(1.42976407049276,1.991859877965,32.0628303011345));
#7070=CARTESIAN_POINT('Ctrl Pts',(1.36205733028204,2.03874846821665,32.0671097308605));
#7071=CARTESIAN_POINT('Ctrl Pts',(1.29227634889257,2.08205957842058,32.0713891605866));
#7072=CARTESIAN_POINT('Ctrl Pts',(1.22249536750309,2.12537068862452,32.0756685903126));
#7073=CARTESIAN_POINT('Ctrl Pts',(1.15064060594837,2.165104138692,32.0799480200387));
#7074=CARTESIAN_POINT('Ctrl Pts',(1.07712117087287,2.20108160531532,32.0842274497648));
#7075=CARTESIAN_POINT('Ctrl Pts',(1.00443886592718,2.23664941398529,32.0884581517012));
#7076=CARTESIAN_POINT('Ctrl Pts',(0.92985624491494,2.26868015883065,32.0926888536377));
#7077=CARTESIAN_POINT('Ctrl Pts',(0.853751750610977,2.29696717397718,32.0969195555742));
#7078=CARTESIAN_POINT('Ctrl Pts',(0.777756597525942,2.32521354846583,32.1011441791561));
#7079=CARTESIAN_POINT('Ctrl Pts',(0.700244345908673,2.34972671501686,32.1053688027379));
#7080=CARTESIAN_POINT('Ctrl Pts',(0.621616440924413,2.37034665194196,32.1095934263197));
#7081=CARTESIAN_POINT('Ctrl Pts',(0.542679071972787,2.39104774488271,32.113834677189));
#7082=CARTESIAN_POINT('Ctrl Pts',(0.462617675086656,2.40782468790357,32.1180759280582));
#7083=CARTESIAN_POINT('Ctrl Pts',(0.381857085610222,2.42056510265047,32.1223171789275));
#7084=CARTESIAN_POINT('Ctrl Pts',(0.301558287351308,2.433232667364,32.1265341782104));
#7085=CARTESIAN_POINT('Ctrl Pts',(0.220568734805544,2.44190966729532,32.1307511774934));
#7086=CARTESIAN_POINT('Ctrl Pts',(0.139317688964832,2.44653649707939,32.1349681767764));
#7087=CARTESIAN_POINT('Ctrl Pts',(0.0580935796242474,2.45116179296812,32.1391837780318));
#7088=CARTESIAN_POINT('Ctrl Pts',(-0.0233913869178665,2.45173955870469,
32.1433993792872));
#7089=CARTESIAN_POINT('Ctrl Pts',(-0.104703613013471,2.4482621190187,32.1476149805426));
#7090=CARTESIAN_POINT('Ctrl Pts',(-0.18601381015834,2.44478476610384,32.1518304766078));
#7091=CARTESIAN_POINT('Ctrl Pts',(-0.267150810837261,2.4372524299078,32.1560459726731));
#7092=CARTESIAN_POINT('Ctrl Pts',(-0.347683249838471,2.42570950605833,32.1602614687383));
#7093=CARTESIAN_POINT('Ctrl Pts',(-0.429069037475522,2.41404426953036,32.1645216336086));
#7094=CARTESIAN_POINT('Ctrl Pts',(-0.509836893019328,2.39828299700287,32.1687817984789));
#7095=CARTESIAN_POINT('Ctrl Pts',(-0.589551077060534,2.37852470610182,32.1730419633491));
#7096=CARTESIAN_POINT('Ctrl Pts',(-0.668544311532325,2.35894511277497,32.177263598514));
#7097=CARTESIAN_POINT('Ctrl Pts',(-0.746502424638695,2.33544070461732,32.1814852336788));
#7098=CARTESIAN_POINT('Ctrl Pts',(-0.823017449620409,2.30815782121161,32.1857068688437));
#7099=CARTESIAN_POINT('Ctrl Pts',(-0.900579972049529,2.28050143272331,32.1899862985667));
#7100=CARTESIAN_POINT('Ctrl Pts',(-0.976659138231037,2.24896251977049,32.1942657282896));
#7101=CARTESIAN_POINT('Ctrl Pts',(-1.0508535298998,2.21374278286732,32.1985451580126));
#7102=CARTESIAN_POINT('Ctrl Pts',(-1.12504792156853,2.17852304596416,32.2028245877356));
#7103=CARTESIAN_POINT('Ctrl Pts',(-1.19735713771539,2.13962277520903,32.2071040174586));
#7104=CARTESIAN_POINT('Ctrl Pts',(-1.26740975649452,2.09728938373856,32.2113834471815));
#7105=CARTESIAN_POINT('Ctrl Pts',(-1.33666472066413,2.05543802171156,32.2156141491495));
#7106=CARTESIAN_POINT('Ctrl Pts',(-1.40397472540036,2.01007394635426,32.2198448511175));
#7107=CARTESIAN_POINT('Ctrl Pts',(-1.46896112141037,1.96140344493039,32.2240755530855));
#7108=CARTESIAN_POINT('Ctrl Pts',(-1.53385414985265,1.91280286962362,32.228300176699));
#7109=CARTESIAN_POINT('Ctrl Pts',(-1.59642983070718,1.86090557927122,32.2325248003124));
#7110=CARTESIAN_POINT('Ctrl Pts',(-1.65633627736508,1.80596245428425,32.2367494239259));
#7111=CARTESIAN_POINT('Ctrl Pts',(-1.71647850345055,1.75080308448089,32.2409906747873));
#7112=CARTESIAN_POINT('Ctrl Pts',(-1.7739300330097,1.69257409850609,32.2452319256486));
#7113=CARTESIAN_POINT('Ctrl Pts',(-1.82836637221471,1.63157183689668,32.24947317651));
#7114=CARTESIAN_POINT('Ctrl Pts',(-1.8824914434803,1.57091838728581,32.2536901758247));
#7115=CARTESIAN_POINT('Ctrl Pts',(-1.93363539988959,1.50752364173452,32.2579071751395));
#7116=CARTESIAN_POINT('Ctrl Pts',(-1.98151572079514,1.44171623360553,32.2621241744542));
#7117=CARTESIAN_POINT('Ctrl Pts',(-2.02938016832626,1.3759306420728,32.2663397757414));
#7118=CARTESIAN_POINT('Ctrl Pts',(-2.07398285556091,1.30773435208733,32.2705553770286));
#7119=CARTESIAN_POINT('Ctrl Pts',(-2.11508257455249,1.23748775865638,32.2747709783158));
#7120=CARTESIAN_POINT('Ctrl Pts',(-2.15618126799898,1.16724291806102,32.2789864744127));
#7121=CARTESIAN_POINT('Ctrl Pts',(-2.19377693307522,1.09494827769197,32.2832019705097));
#7122=CARTESIAN_POINT('Ctrl Pts',(-2.22767334950147,1.02099054741995,32.2874174666066));
#7123=CARTESIAN_POINT('Ctrl Pts',(-2.26192894312335,0.946249137545359,32.2916776314392));
#7124=CARTESIAN_POINT('Ctrl Pts',(-2.29240620797663,0.869809616353677,32.2959377962719));
#7125=CARTESIAN_POINT('Ctrl Pts',(-2.3189524794021,0.792091944331508,32.3001979611045));
#7126=CARTESIAN_POINT('Ctrl Pts',(-2.34525866195077,0.71507716381088,32.3044195963006));
#7127=CARTESIAN_POINT('Ctrl Pts',(-2.36770459988061,0.636807728104529,32.3086412314967));
#7128=CARTESIAN_POINT('Ctrl Pts',(-2.38619245125746,0.557705868322988,32.3128628666928));
#7129=CARTESIAN_POINT('Ctrl Pts',(-2.40493340249762,0.477521099041088,32.3171422963437));
#7130=CARTESIAN_POINT('Ctrl Pts',(-2.41960698558035,0.396481427974036,32.3214217259946));
#7131=CARTESIAN_POINT('Ctrl Pts',(-2.430165449126,0.315033553568883,32.3257011556455));
#7132=CARTESIAN_POINT('Ctrl Pts',(-2.44072391267165,0.233585679163708,32.3299805852964));
#7133=CARTESIAN_POINT('Ctrl Pts',(-2.44716728347151,0.15173009563451,32.3342600149473));
#7134=CARTESIAN_POINT('Ctrl Pts',(-2.44950248378864,0.0699130310692556,
32.3385394445982));
#7135=CARTESIAN_POINT('Ctrl Pts',(-2.45016331335893,0.0467599271480851,
32.3397504643281));
#7136=CARTESIAN_POINT('Ctrl Pts',(-2.45049588145719,0.0235974094165099,
32.340961484058));
#7137=CARTESIAN_POINT('Ctrl Pts',(-2.45049996198422,0.000431642579436891,
32.3421725037879));
#7138=CARTESIAN_POINT('',(-2.45049918758584,0.00199540500337376,33.1421724763606));
#7139=CARTESIAN_POINT('Ctrl Pts',(-2.4504999619844,0.000431641585035285,
32.3421725038399));
#7140=CARTESIAN_POINT('Ctrl Pts',(-2.45051414927913,-0.0801119538513814,
32.3463830220531));
#7141=CARTESIAN_POINT('Ctrl Pts',(-2.44655306968252,-0.160813628721216,
32.3505935402663));
#7142=CARTESIAN_POINT('Ctrl Pts',(-2.43859602483964,-0.241246093515107,
32.3548040584794));
#7143=CARTESIAN_POINT('Ctrl Pts',(-2.43065032934404,-0.321563835319083,
32.3590085711171));
#7144=CARTESIAN_POINT('Ctrl Pts',(-2.41872003130953,-0.401612665834839,
32.3632130837549));
#7145=CARTESIAN_POINT('Ctrl Pts',(-2.40283644220969,-0.480964948815475,
32.3674175963925));
#7146=CARTESIAN_POINT('Ctrl Pts',(-2.38697086816974,-0.56022723097068,32.3716173403003));
#7147=CARTESIAN_POINT('Ctrl Pts',(-2.3671610036448,-0.638794076840536,32.3758170842081));
#7148=CARTESIAN_POINT('Ctrl Pts',(-2.34348982424493,-0.716244157854338,
32.3800168281158));
#7149=CARTESIAN_POINT('Ctrl Pts',(-2.31983319025196,-0.793646647536738,
32.3842139913755));
#7150=CARTESIAN_POINT('Ctrl Pts',(-2.29232008705754,-0.869933285910213,
32.3884111546352));
#7151=CARTESIAN_POINT('Ctrl Pts',(-2.26108403109816,-0.944695323537124,
32.3926083178948));
#7152=CARTESIAN_POINT('Ctrl Pts',(-2.22985735715304,-1.0194349057521,32.3968042205009));
#7153=CARTESIAN_POINT('Ctrl Pts',(-2.19491013178432,-1.09265036308669,32.401000123107));
#7154=CARTESIAN_POINT('Ctrl Pts',(-2.15642442956955,-1.16395185877923,32.4051960257131));
#7155=CARTESIAN_POINT('Ctrl Pts',(-2.1179381978553,-1.23525433546218,32.4093919860478));
#7156=CARTESIAN_POINT('Ctrl Pts',(-2.07591361738323,-1.30464238545099,32.4135879463826));
#7157=CARTESIAN_POINT('Ctrl Pts',(-2.03057852695273,-1.37175110565965,32.4177839067173));
#7158=CARTESIAN_POINT('Ctrl Pts',(-1.98519789814841,-1.43892723550527,32.4219840818272));
#7159=CARTESIAN_POINT('Ctrl Pts',(-1.93650038245503,-1.50381907315001,32.426184256937));
#7160=CARTESIAN_POINT('Ctrl Pts',(-1.88475658813207,-1.56609158528253,32.4303844320469));
#7161=CARTESIAN_POINT('Ctrl Pts',(-1.83298640188451,-1.62839585951265,32.4345867494562));
#7162=CARTESIAN_POINT('Ctrl Pts',(-1.77816716179821,-1.68807780206639,32.4387890668656));
#7163=CARTESIAN_POINT('Ctrl Pts',(-1.72060740200968,-1.74483822119688,32.4429913842749));
#7164=CARTESIAN_POINT('Ctrl Pts',(-1.66294636868909,-1.80169850745935,32.4472010954526));
#7165=CARTESIAN_POINT('Ctrl Pts',(-1.60253553608518,-1.85562669030327,32.4514108066302));
#7166=CARTESIAN_POINT('Ctrl Pts',(-1.53971740739335,-1.90636317509805,32.4556205178079));
#7167=CARTESIAN_POINT('Ctrl Pts',(-1.48960408142772,-1.94683833814125,32.4589788258769));
#7168=CARTESIAN_POINT('Ctrl Pts',(-1.4379594376405,-1.98528303520078,32.4623371339459));
#7169=CARTESIAN_POINT('Ctrl Pts',(-1.3849695681631,-2.02158589856135,32.4656954420149));
#7170=CARTESIAN_POINT('Ctrl Pts',(-1.31821442288667,-2.06731922346827,32.4699261439442));
#7171=CARTESIAN_POINT('Ctrl Pts',(-1.24906605095292,-2.10982850004489,32.4741568458735));
#7172=CARTESIAN_POINT('Ctrl Pts',(-1.17786891945138,-2.14885435955777,32.4783875478028));
#7173=CARTESIAN_POINT('Ctrl Pts',(-1.10677407864559,-2.1878241496443,32.482612171377));
#7174=CARTESIAN_POINT('Ctrl Pts',(-1.03363672858628,-2.22332024065947,32.4868367949513));
#7175=CARTESIAN_POINT('Ctrl Pts',(-0.958830860651012,-2.2551260786624,32.4910614185255));
#7176=CARTESIAN_POINT('Ctrl Pts',(-0.883730571366394,-2.2870570982587,32.4953026693966));
#7177=CARTESIAN_POINT('Ctrl Pts',(-0.806948993604187,-2.31526848609442,
32.4995439202677));
#7178=CARTESIAN_POINT('Ctrl Pts',(-0.728890171634071,-2.33958743536019,
32.5037851711388));
#7179=CARTESIAN_POINT('Ctrl Pts',(-0.651277692293025,-2.36376732816215,
32.5080021704132));
#7180=CARTESIAN_POINT('Ctrl Pts',(-0.572402984222,-2.38409903603608,32.5122191696877));
#7181=CARTESIAN_POINT('Ctrl Pts',(-0.492682124559706,-2.40046132527465,
32.5164361689621));
#7182=CARTESIAN_POINT('Ctrl Pts',(-0.41298769411338,-2.41681819005496,32.5206517702087));
#7183=CARTESIAN_POINT('Ctrl Pts',(-0.3324481243396,-2.42920815602413,32.5248673714553));
#7184=CARTESIAN_POINT('Ctrl Pts',(-0.251491314947697,-2.43756074150079,
32.5290829727019));
#7185=CARTESIAN_POINT('Ctrl Pts',(-0.17053652564392,-2.44591311855819,32.533298468758));
#7186=CARTESIAN_POINT('Ctrl Pts',(-0.089164980138353,-2.45022826877663,
32.5375139648141));
#7187=CARTESIAN_POINT('Ctrl Pts',(-0.00780992149994874,-2.45048755457484,
32.5417294608702));
#7188=CARTESIAN_POINT('Ctrl Pts',(0.07440720289556,-2.45074958785319,32.5459896257503));
#7189=CARTESIAN_POINT('Ctrl Pts',(0.156607004528232,-2.44686927263466,32.5502497906304));
#7190=CARTESIAN_POINT('Ctrl Pts',(0.238343990183245,-2.43888138135981,32.5545099555106));
#7191=CARTESIAN_POINT('Ctrl Pts',(0.319341731307874,-2.43096573406223,32.5587315906656));
#7192=CARTESIAN_POINT('Ctrl Pts',(0.399884538289744,-2.41901664127913,32.5629532258207));
#7193=CARTESIAN_POINT('Ctrl Pts',(0.479547533490022,-2.40311972509146,32.5671748609757));
#7194=CARTESIAN_POINT('Ctrl Pts',(0.560301122686974,-2.3870051786061,32.5714542907184));
#7195=CARTESIAN_POINT('Ctrl Pts',(0.640150148704368,-2.3668340192763,32.5757337204611));
#7196=CARTESIAN_POINT('Ctrl Pts',(0.718668183780573,-2.34274759451835,32.5800131502037));
#7197=CARTESIAN_POINT('Ctrl Pts',(0.797186218856778,-2.3186611697604,32.5842925799464));
#7198=CARTESIAN_POINT('Ctrl Pts',(0.874372824147898,-2.29065970844424,32.5885720096891));
#7199=CARTESIAN_POINT('Ctrl Pts',(0.949824621131082,-2.25893413783873,32.5928514394317));
#7200=CARTESIAN_POINT('Ctrl Pts',(1.02441728808141,-2.22756980966356,32.5970821415528));
#7201=CARTESIAN_POINT('Ctrl Pts',(1.09759503317657,-2.19244781989971,32.6013128436738));
#7202=CARTESIAN_POINT('Ctrl Pts',(1.16895329161688,-2.15371735657631,32.6055435457948));
#7203=CARTESIAN_POINT('Ctrl Pts',(1.2402090278906,-2.11504253826303,32.609768169562));
#7204=CARTESIAN_POINT('Ctrl Pts',(1.30965006399002,-2.07276976282349,32.6139927933291));
#7205=CARTESIAN_POINT('Ctrl Pts',(1.37689184717846,-2.02709622148863,32.6182174170963));
#7206=CARTESIAN_POINT('Ctrl Pts',(1.44439827710164,-1.98124292059051,32.6224586679193));
#7207=CARTESIAN_POINT('Ctrl Pts',(1.50968766811608,-1.93196221120455,32.6266999187423));
#7208=CARTESIAN_POINT('Ctrl Pts',(1.57239597728727,-1.87950023692758,32.6309411695653));
#7209=CARTESIAN_POINT('Ctrl Pts',(1.63474572209043,-1.82733823876064,32.635158169034));
#7210=CARTESIAN_POINT('Ctrl Pts',(1.69454346178162,-1.77203155916156,32.6393751685028));
#7211=CARTESIAN_POINT('Ctrl Pts',(1.75146199910057,-1.71386438078006,32.6435921679715));
#7212=CARTESIAN_POINT('Ctrl Pts',(1.8083616666763,-1.65571648609368,32.6478077694125));
#7213=CARTESIAN_POINT('Ctrl Pts',(1.86238370238937,-1.59471030795587,32.6520233708534));
#7214=CARTESIAN_POINT('Ctrl Pts',(1.91323717824831,-1.53116744667866,32.6562389722944));
#7215=CARTESIAN_POINT('Ctrl Pts',(1.96408938517551,-1.46762617096768,32.6604544685447));
#7216=CARTESIAN_POINT('Ctrl Pts',(2.01177289970693,-1.40154870174325,32.664669964795));
#7217=CARTESIAN_POINT('Ctrl Pts',(2.05603748921055,-1.33328920079658,32.6688854610452));
#7218=CARTESIAN_POINT('Ctrl Pts',(2.10077111682289,-1.26430640595777,32.6731456256955));
#7219=CARTESIAN_POINT('Ctrl Pts',(2.14201265539818,-1.1930954591219,32.6774057903458));
#7220=CARTESIAN_POINT('Ctrl Pts',(2.1795501448686,-1.12004973818276,32.681665954996));
#7221=CARTESIAN_POINT('Ctrl Pts',(2.216748141986,-1.04766464916198,32.6858875903429));
#7222=CARTESIAN_POINT('Ctrl Pts',(2.25030868242107,-0.973478294132603,32.6901092256897));
#7223=CARTESIAN_POINT('Ctrl Pts',(2.28007371977505,-0.897894249002155,32.6943308610366));
#7224=CARTESIAN_POINT('Ctrl Pts',(2.31024623884924,-0.821275462461399,32.6986102903386));
#7225=CARTESIAN_POINT('Ctrl Pts',(2.33651838975215,-0.743220896275271,32.7028897196405));
#7226=CARTESIAN_POINT('Ctrl Pts',(2.35877813836951,-0.664165599794256,32.7071691489425));
#7227=CARTESIAN_POINT('Ctrl Pts',(2.38103788698687,-0.585110303313242,32.7114485782445));
#7228=CARTESIAN_POINT('Ctrl Pts',(2.39928518814752,-0.505054769411128,32.7157280075465));
#7229=CARTESIAN_POINT('Ctrl Pts',(2.41346217146957,-0.424441511736742,32.7200074368484));
#7230=CARTESIAN_POINT('Ctrl Pts',(2.42747772865952,-0.344746156417734,32.7242381384554));
#7231=CARTESIAN_POINT('Ctrl Pts',(2.43756794910877,-0.264205964768421,32.7284688400623));
#7232=CARTESIAN_POINT('Ctrl Pts',(2.44363922756559,-0.183241849757813,32.7326995416692));
#7233=CARTESIAN_POINT('Ctrl Pts',(2.44970178326558,-0.102394057905686,32.7369241649219));
#7234=CARTESIAN_POINT('Ctrl Pts',(2.45175683020018,-0.0211240121449797,
32.7411487881746));
#7235=CARTESIAN_POINT('Ctrl Pts',(2.4497619569373,0.0601382103387006,32.7453734114273));
#7236=CARTESIAN_POINT('Ctrl Pts',(2.44775923205074,0.141720272885431,32.7496146623788));
#7237=CARTESIAN_POINT('Ctrl Pts',(2.44167455622069,0.22329398305791,32.7538559133304));
#7238=CARTESIAN_POINT('Ctrl Pts',(2.43151777934252,0.304420003845395,32.758097164282));
#7239=CARTESIAN_POINT('Ctrl Pts',(2.42141908016349,0.385082136070123,32.7623141632391));
#7240=CARTESIAN_POINT('Ctrl Pts',(2.40729478146787,0.465301218805409,32.7665311621962));
#7241=CARTESIAN_POINT('Ctrl Pts',(2.38920666345568,0.544648298720361,32.7707481611533));
#7242=CARTESIAN_POINT('Ctrl Pts',(2.37112454204265,0.623969073376095,32.7749637620848));
#7243=CARTESIAN_POINT('Ctrl Pts',(2.34908131415745,0.702417966221634,32.7791793630162));
#7244=CARTESIAN_POINT('Ctrl Pts',(2.32318985579329,0.779576259219809,32.7833949639477));
#7245=CARTESIAN_POINT('Ctrl Pts',(2.2972990434737,0.856732626961591,32.7876104596914));
#7246=CARTESIAN_POINT('Ctrl Pts',(2.26756034056709,0.932598018329473,32.7918259554351));
#7247=CARTESIAN_POINT('Ctrl Pts',(2.23413603232489,1.00677030104567,32.7960414511787));
#7248=CARTESIAN_POINT('Ctrl Pts',(2.20035754329814,1.0817285505826,32.8003016164359));
#7249=CARTESIAN_POINT('Ctrl Pts',(2.1628150591435,1.15495714743976,32.8045617816931));
#7250=CARTESIAN_POINT('Ctrl Pts',(2.12172455773923,1.22606490492398,32.8088219469503));
#7251=CARTESIAN_POINT('Ctrl Pts',(2.08100569301125,1.29652953930807,32.8130435818026));
#7252=CARTESIAN_POINT('Ctrl Pts',(2.03680303897295,1.3649111818143,32.8172652166549));
#7253=CARTESIAN_POINT('Ctrl Pts',(1.98937033689326,1.43085845305858,32.8214868515072));
#7254=CARTESIAN_POINT('Ctrl Pts',(1.94128826509763,1.49770856472556,32.8257662819669));
#7255=CARTESIAN_POINT('Ctrl Pts',(1.88988734343297,1.56205675921975,32.8300457124266));
#7256=CARTESIAN_POINT('Ctrl Pts',(1.83547268665345,1.62357330187127,32.8343251428862));
#7257=CARTESIAN_POINT('Ctrl Pts',(1.78105802987395,1.68508984452277,32.8386045733459));
#7258=CARTESIAN_POINT('Ctrl Pts',(1.72363002791167,1.74377443050535,32.8428840038055));
#7259=CARTESIAN_POINT('Ctrl Pts',(1.66352939611642,1.79933882252802,32.8471634342652));
#7260=CARTESIAN_POINT('Ctrl Pts',(1.60411311074725,1.8542705208175,32.8513941362364));
#7261=CARTESIAN_POINT('Ctrl Pts',(1.54186129872075,1.90635936664191,32.8556248382076));
#7262=CARTESIAN_POINT('Ctrl Pts',(1.47707716683848,1.9552987733859,32.8598555401789));
#7263=CARTESIAN_POINT('Ctrl Pts',(1.41238611197482,2.00416786763299,32.8640801637924));
#7264=CARTESIAN_POINT('Ctrl Pts',(1.34517033094913,2.04989623151562,32.868304787406));
#7265=CARTESIAN_POINT('Ctrl Pts',(1.27576845238626,2.0922153583931,32.8725294110195));
#7266=CARTESIAN_POINT('Ctrl Pts',(1.2060934223406,2.13470104462742,32.8767706618804));
#7267=CARTESIAN_POINT('Ctrl Pts',(1.13421539824392,2.17375027803713,32.8810119127414));
#7268=CARTESIAN_POINT('Ctrl Pts',(1.06050908877006,2.20913347777722,32.8852531636023));
#7269=CARTESIAN_POINT('Ctrl Pts',(0.987224233388338,2.24431435570214,32.8894701629094));
#7270=CARTESIAN_POINT('Ctrl Pts',(0.91213236770277,2.27587080780408,32.8936871622165));
#7271=CARTESIAN_POINT('Ctrl Pts',(0.8356275860296,2.3036225358045,32.8979041615237));
#7272=CARTESIAN_POINT('Ctrl Pts',(0.759148167418059,2.3313650634808,32.9021197628003));
#7273=CARTESIAN_POINT('Ctrl Pts',(0.681257199848004,2.35530521342506,32.906335364077));
#7274=CARTESIAN_POINT('Ctrl Pts',(0.602367836105354,2.37531118803953,32.9105509653537));
#7275=CARTESIAN_POINT('Ctrl Pts',(0.523480440910551,2.39531666343945,32.9147664614373));
#7276=CARTESIAN_POINT('Ctrl Pts',(0.443595150134574,2.41138804543011,32.9189819575209));
#7277=CARTESIAN_POINT('Ctrl Pts',(0.363137922722365,2.42344405734502,32.9231974536046));
#7278=CARTESIAN_POINT('Ctrl Pts',(0.281828144578112,2.43562781865068,32.9274576184443));
#7279=CARTESIAN_POINT('Ctrl Pts',(0.199934713508689,2.44371051915757,32.9317177832841));
#7280=CARTESIAN_POINT('Ctrl Pts',(0.117903455469611,2.44766195075797,32.9359779481239));
#7281=CARTESIAN_POINT('Ctrl Pts',(0.0366141022405083,2.4515776449312,32.9401995833));
#7282=CARTESIAN_POINT('Ctrl Pts',(-0.0448101248036766,2.45143655996908,
32.9444212184761));
#7283=CARTESIAN_POINT('Ctrl Pts',(-0.125936422214181,2.44726178974786,32.9486428536521));
#7284=CARTESIAN_POINT('Ctrl Pts',(-0.208173344593542,2.44302986661575,32.9529222833238));
#7285=CARTESIAN_POINT('Ctrl Pts',(-0.290103626129848,2.4346530294107,32.9572017129954));
#7286=CARTESIAN_POINT('Ctrl Pts',(-0.371284847448981,2.4222092832897,32.961481142667));
#7287=CARTESIAN_POINT('Ctrl Pts',(-0.452466068768091,2.4097655371687,32.9657605723387));
#7288=CARTESIAN_POINT('Ctrl Pts',(-0.532897762471851,2.39325504493315,32.9700400020103));
#7289=CARTESIAN_POINT('Ctrl Pts',(-0.612153123806261,2.37280821033101,32.9743194316819));
#7290=CARTESIAN_POINT('Ctrl Pts',(-0.690506065125478,2.35259418815292,32.97855013477));
#7291=CARTESIAN_POINT('Ctrl Pts',(-0.768004043464895,2.32845701957416,32.982780837858));
#7292=CARTESIAN_POINT('Ctrl Pts',(-0.844225133903018,2.30048563857426,32.987011540946));
#7293=CARTESIAN_POINT('Ctrl Pts',(-0.920336715732164,2.27255444470639,32.9912361656848));
#7294=CARTESIAN_POINT('Ctrl Pts',(-0.995174620260639,2.2408001378618,32.9954607904235));
#7295=CARTESIAN_POINT('Ctrl Pts',(-1.06832976081949,2.20536205012859,32.9996854151623));
#7296=CARTESIAN_POINT('Ctrl Pts',(-1.14177280051215,2.16978449721652,33.003926665743));
#7297=CARTESIAN_POINT('Ctrl Pts',(-1.21351934342128,2.13049422503592,33.0081679163237));
#7298=CARTESIAN_POINT('Ctrl Pts',(-1.28317349627679,2.08768197493124,33.0124091669044));
#7299=CARTESIAN_POINT('Ctrl Pts',(-1.35242938860447,2.04511451180084,33.0166261673488));
#7300=CARTESIAN_POINT('Ctrl Pts',(-1.41961635302222,1.99906548255506,33.0208431677933));
#7301=CARTESIAN_POINT('Ctrl Pts',(-1.48436943494468,1.94976860950268,33.0250601682378));
#7302=CARTESIAN_POINT('Ctrl Pts',(-1.54910104979629,1.90048807944796,33.0292757706538));
#7303=CARTESIAN_POINT('Ctrl Pts',(-1.61140001475318,1.84796212527597,33.0334913730699));
#7304=CARTESIAN_POINT('Ctrl Pts',(-1.67093183406871,1.79246675168489,33.0377069754859));
#7305=CARTESIAN_POINT('Ctrl Pts',(-1.73046216787779,1.73697276287822,33.0419224727095));
#7306=CARTESIAN_POINT('Ctrl Pts',(-1.78722515389434,1.67850981988038,33.046137969933));
#7307=CARTESIAN_POINT('Ctrl Pts',(-1.84092183882263,1.61739204689089,33.0503534671565));
#7308=CARTESIAN_POINT('Ctrl Pts',(-1.89518747934265,1.55562668646202,33.0546136306517));
#7309=CARTESIAN_POINT('Ctrl Pts',(-1.94632112062992,1.49115025466911,33.0588737941468));
#7310=CARTESIAN_POINT('Ctrl Pts',(-1.99405598988234,1.42432122753765,33.063133957642));
#7311=CARTESIAN_POINT('Ctrl Pts',(-2.04135916434991,1.35809657500573,33.0673555939475));
#7312=CARTESIAN_POINT('Ctrl Pts',(-2.08532459180849,1.28956213693925,33.071577230253));
#7313=CARTESIAN_POINT('Ctrl Pts',(-2.12573736355962,1.21909429953822,33.0757988665584));
#7314=CARTESIAN_POINT('Ctrl Pts',(-2.16670335345106,1.14766181447089,33.0800782936485));
#7315=CARTESIAN_POINT('Ctrl Pts',(-2.20401846113595,1.07424303692224,33.0843577207385));
#7316=CARTESIAN_POINT('Ctrl Pts',(-2.23750873923386,0.999252166298438,33.0886371478286));
#7317=CARTESIAN_POINT('Ctrl Pts',(-2.27099901733176,0.924261295674634,33.0929165749186));
#7318=CARTESIAN_POINT('Ctrl Pts',(-2.30066434966464,0.847698813084396,33.0971960020087));
#7319=CARTESIAN_POINT('Ctrl Pts',(-2.32638329711352,0.76999415901112,33.1014754290987));
#7320=CARTESIAN_POINT('Ctrl Pts',(-2.35666864530179,0.678493038713086,33.1065146687381));
#7321=CARTESIAN_POINT('Ctrl Pts',(-2.3815763775295,0.585128820235907,33.1115539083775));
#7322=CARTESIAN_POINT('Ctrl Pts',(-2.40091147374684,0.490483786919389,33.1165931480169));
#7323=CARTESIAN_POINT('Ctrl Pts',(-2.4200315925657,0.396891065047913,33.1215763588362));
#7324=CARTESIAN_POINT('Ctrl Pts',(-2.43370224837572,0.302045925225219,33.1265595696555));
#7325=CARTESIAN_POINT('Ctrl Pts',(-2.44178104468291,0.206532273088859,33.1315427804748));
#7326=CARTESIAN_POINT('Ctrl Pts',(-2.44752534295315,0.138618825851275,33.1350860124367));
#7327=CARTESIAN_POINT('Ctrl Pts',(-2.45044351293495,0.0703678339286369,
33.1386292443987));
#7328=CARTESIAN_POINT('Ctrl Pts',(-2.45049918758584,0.00199540500337376,
33.1421724763606));
#7329=CARTESIAN_POINT('',(-2.44727084717605,-0.00140258346811789,33.942172503788));
#7330=CARTESIAN_POINT('Ctrl Pts',(-2.44847586273047,0.00199322861988113,
33.142172503788));
#7331=CARTESIAN_POINT('Ctrl Pts',(-2.44423584572099,-0.553673306700436,
33.1709921446971));
#7332=CARTESIAN_POINT('Ctrl Pts',(-1.98117856145162,-1.93295879325365,33.2421971180786));
#7333=CARTESIAN_POINT('Ctrl Pts',(0.309238185493155,-2.88090186856504,33.355787423932));
#7334=CARTESIAN_POINT('Ctrl Pts',(2.58956571189241,-1.29976110413427,33.4829434213489));
#7335=CARTESIAN_POINT('Ctrl Pts',(2.49480438216511,1.47349276746318,33.6100994187657));
#7336=CARTESIAN_POINT('Ctrl Pts',(0.111868610958372,2.89528823059717,33.7372554161823));
#7337=CARTESIAN_POINT('Ctrl Pts',(-2.051828672412,1.8213500783052,33.8479464445231));
#7338=CARTESIAN_POINT('Ctrl Pts',(-2.44467637437558,0.498983042526859,33.9162521403917));
#7339=CARTESIAN_POINT('Ctrl Pts',(-2.44727084717605,-0.00140258346811789,
33.942172503788));
#7340=CARTESIAN_POINT('',(-2.45356477742091,-0.00152987545416492,34.7421725037879));
#7341=CARTESIAN_POINT('Ctrl Pts',(-2.44727084717605,-0.00140258346811789,
33.942172503788));
#7342=CARTESIAN_POINT('Ctrl Pts',(-2.44891889175687,-0.31925437173569,33.9586374728639));
#7343=CARTESIAN_POINT('Ctrl Pts',(-2.24355252467318,-1.45329455082822,34.0174877744123));
#7344=CARTESIAN_POINT('Ctrl Pts',(-0.530612517065195,-2.84843073781086,
34.1187234084324));
#7345=CARTESIAN_POINT('Ctrl Pts',(2.10758733248769,-1.98834033015572,34.2458794058493));
#7346=CARTESIAN_POINT('Ctrl Pts',(2.81273209537355,0.695553694092942,34.373035403266));
#7347=CARTESIAN_POINT('Ctrl Pts',(0.938155042953724,2.74122592529684,34.5001914006828));
#7348=CARTESIAN_POINT('Ctrl Pts',(-1.70855734209424,2.28836542993453,34.6232371008568));
#7349=CARTESIAN_POINT('Ctrl Pts',(-2.44866265110221,0.732444988893918,34.7038974685585));
#7350=CARTESIAN_POINT('Ctrl Pts',(-2.45356477742091,-0.00152987545416492,
34.7421725037879));
#7351=CARTESIAN_POINT('',(1.07686354780633,-2.20575423999072,34.9999542666628));
#7352=CARTESIAN_POINT('Ctrl Pts',(-2.45356477742091,-0.00152987545416492,
34.7421725037879));
#7353=CARTESIAN_POINT('Ctrl Pts',(-2.4540912092366,-0.0803503087494975,
34.7462828010307));
#7354=CARTESIAN_POINT('Ctrl Pts',(-2.41487118212295,-0.97139961274513,34.7927784307463));
#7355=CARTESIAN_POINT('Ctrl Pts',(-1.3621803363065,-2.52198142046407,34.8787056850368));
#7356=CARTESIAN_POINT('Ctrl Pts',(0.395824670058481,-2.53385348501788,34.9605226420862));
#7357=CARTESIAN_POINT('Ctrl Pts',(1.07686354780633,-2.20575423999072,34.9999542666628));
#7358=CARTESIAN_POINT('',(-1.07508846035141,-2.20207516956602,35.));
#7359=CARTESIAN_POINT('Origin',(0.,0.,35.));
#7360=CARTESIAN_POINT('',(-2.45049860417889,-0.0026155147360495,34.8578274961857));
#7361=CARTESIAN_POINT('Ctrl Pts',(-1.07508846035141,-2.20207516956602,35.));
#7362=CARTESIAN_POINT('Ctrl Pts',(-1.14997613952614,-2.16551380199059,34.9956699954726));
#7363=CARTESIAN_POINT('Ctrl Pts',(-1.22305004349785,-2.12510242184625,34.9913399909452));
#7364=CARTESIAN_POINT('Ctrl Pts',(-1.29390617536955,-2.08104710646841,34.9870099864178));
#7365=CARTESIAN_POINT('Ctrl Pts',(-1.36471943359506,-2.03701844809195,34.9826826018907));
#7366=CARTESIAN_POINT('Ctrl Pts',(-1.43331722252973,-1.9893504704842,34.9783552173635));
#7367=CARTESIAN_POINT('Ctrl Pts',(-1.49932159809749,-1.93829435212467,34.9740278328364));
#7368=CARTESIAN_POINT('Ctrl Pts',(-1.56531940167207,-1.88724331737451,34.9697008791828));
#7369=CARTESIAN_POINT('Ctrl Pts',(-1.62872395639475,-1.83280506987026,34.9653739255293));
#7370=CARTESIAN_POINT('Ctrl Pts',(-1.68918825280508,-1.77527273864759,34.9610469718757));
#7371=CARTESIAN_POINT('Ctrl Pts',(-1.74965116688525,-1.71774172272471,34.9567201171446));
#7372=CARTESIAN_POINT('Ctrl Pts',(-1.80717364164387,-1.65711706240731,34.9523932624135));
#7373=CARTESIAN_POINT('Ctrl Pts',(-1.86144452495553,-1.59372975454218,34.9480664076824));
#7374=CARTESIAN_POINT('Ctrl Pts',(-1.9157272829466,-1.53032857728865,34.9437386062187));
#7375=CARTESIAN_POINT('Ctrl Pts',(-1.96675675199689,-1.46416387957714,34.9394108047551));
#7376=CARTESIAN_POINT('Ctrl Pts',(-2.01426185774394,-1.39560002093649,34.9350830032914));
#7377=CARTESIAN_POINT('Ctrl Pts',(-2.0617888418391,-1.32700458539598,34.9307532086705));
#7378=CARTESIAN_POINT('Ctrl Pts',(-2.10578798686745,-1.25600814742925,34.9264234140496));
#7379=CARTESIAN_POINT('Ctrl Pts',(-2.14603194121717,-1.18300344770235,34.9220936194286));
#7380=CARTESIAN_POINT('Ctrl Pts',(-2.18633590536483,-1.10988988697137,34.9177573684317));
#7381=CARTESIAN_POINT('Ctrl Pts',(-2.22287328548544,-1.03476246431391,34.9134211174348));
#7382=CARTESIAN_POINT('Ctrl Pts',(-2.25546306018371,-0.95803790851235,34.9090848664379));
#7383=CARTESIAN_POINT('Ctrl Pts',(-2.28807781659817,-0.881254539445122,
34.9047452914845));
#7384=CARTESIAN_POINT('Ctrl Pts',(-2.31673878767929,-0.802872004799493,
34.9004057165312));
#7385=CARTESIAN_POINT('Ctrl Pts',(-2.34131425464778,-0.723324139638024,
34.8960661415778));
#7386=CARTESIAN_POINT('Ctrl Pts',(-2.36593829093927,-0.643619061351729,
34.8917179901763));
#7387=CARTESIAN_POINT('Ctrl Pts',(-2.38646057958798,-0.562744471098961,
34.8873698387749));
#7388=CARTESIAN_POINT('Ctrl Pts',(-2.40280007006069,-0.481146623511296,
34.8830216873734));
#7389=CARTESIAN_POINT('Ctrl Pts',(-2.4155486435967,-0.417481470544106,34.8796291257767));
#7390=CARTESIAN_POINT('Ctrl Pts',(-2.42575192533155,-0.353376289000985,
34.87623656418));
#7391=CARTESIAN_POINT('Ctrl Pts',(-2.43339340293186,-0.289044627294339,
34.8728440025833));
#7392=CARTESIAN_POINT('Ctrl Pts',(-2.4446679019399,-0.194127479847733,34.8678385004595));
#7393=CARTESIAN_POINT('Ctrl Pts',(-2.45039627804784,-0.0984857423509142,
34.8628329983358));
#7394=CARTESIAN_POINT('Ctrl Pts',(-2.45049860417835,-0.00261551523903185,
34.857827496212));
#7395=CARTESIAN_POINT('',(-2.45037983021139,-0.00118544631073139,34.0578275478795));
#7396=CARTESIAN_POINT('Ctrl Pts',(-2.45049860417889,-0.0026155147360495,
34.8578274961857));
#7397=CARTESIAN_POINT('Ctrl Pts',(-2.45058303800099,0.0764912707662882,
34.8536972339056));
#7398=CARTESIAN_POINT('Ctrl Pts',(-2.44683277730122,0.155775958000202,34.8495669716254));
#7399=CARTESIAN_POINT('Ctrl Pts',(-2.43922279362101,0.234824217404693,34.8454367093453));
#7400=CARTESIAN_POINT('Ctrl Pts',(-2.43156502720256,0.314368817201754,34.8412805133378));
#7401=CARTESIAN_POINT('Ctrl Pts',(-2.41999881548176,0.393673515189363,34.8371243173304));
#7402=CARTESIAN_POINT('Ctrl Pts',(-2.40455197476298,0.47231350887248,34.8329681213229));
#7403=CARTESIAN_POINT('Ctrl Pts',(-2.38923734093838,0.550280436165396,34.8288474974933));
#7404=CARTESIAN_POINT('Ctrl Pts',(-2.37010832711614,0.627593503657347,34.8247268736638));
#7405=CARTESIAN_POINT('Ctrl Pts',(-2.34724403790772,0.703843502851779,34.8206062498342));
#7406=CARTESIAN_POINT('Ctrl Pts',(-2.32439107691412,0.780055723641504,34.8164876675862));
#7407=CARTESIAN_POINT('Ctrl Pts',(-2.2978066495509,0.855205454128816,34.8123690853382));
#7408=CARTESIAN_POINT('Ctrl Pts',(-2.26762040953671,0.928896080437713,34.8082505030903));
#7409=CARTESIAN_POINT('Ctrl Pts',(-2.23743897407922,1.00257497786646,34.8041325763715));
#7410=CARTESIAN_POINT('Ctrl Pts',(-2.20365704921906,1.07479478108353,34.8000146496527));
#7411=CARTESIAN_POINT('Ctrl Pts',(-2.16645275089669,1.14517803337829,34.7958967229339));
#7412=CARTESIAN_POINT('Ctrl Pts',(-2.12865095884263,1.21669162689593,34.79171266312));
#7413=CARTESIAN_POINT('Ctrl Pts',(-2.08731611560687,1.28630868826316,34.787528603306));
#7414=CARTESIAN_POINT('Ctrl Pts',(-2.04268302315884,1.35366034029909,34.7833445434921));
#7415=CARTESIAN_POINT('Ctrl Pts',(-1.99869892377223,1.42003265721732,34.779221322523));
#7416=CARTESIAN_POINT('Ctrl Pts',(-1.95151221009395,1.48420465471391,34.7750981015539));
#7417=CARTESIAN_POINT('Ctrl Pts',(-1.90138933877843,1.54585537240058,34.7709748805848));
#7418=CARTESIAN_POINT('Ctrl Pts',(-1.85015710989431,1.60887059073297,34.7667604013484));
#7419=CARTESIAN_POINT('Ctrl Pts',(-1.79585756052814,1.6692511875169,34.7625459221121));
#7420=CARTESIAN_POINT('Ctrl Pts',(-1.73881452791423,1.72669461327543,34.7583314428757));
#7421=CARTESIAN_POINT('Ctrl Pts',(-1.68177149530033,1.78413803903396,34.7541169636393));
#7422=CARTESIAN_POINT('Ctrl Pts',(-1.62198542909039,1.838643993989,34.7499024844029));
#7423=CARTESIAN_POINT('Ctrl Pts',(-1.55981354226621,1.8899555453404,34.7456880051665));
#7424=CARTESIAN_POINT('Ctrl Pts',(-1.49730846359926,1.94154208577809,34.7414509396749));
#7425=CARTESIAN_POINT('Ctrl Pts',(-1.43212601463825,1.99011985422216,34.7372138741832));
#7426=CARTESIAN_POINT('Ctrl Pts',(-1.36458746472523,2.03539954336114,34.7329768086916));
#7427=CARTESIAN_POINT('Ctrl Pts',(-1.29714570934954,2.0806143387977,34.7287458156549));
#7428=CARTESIAN_POINT('Ctrl Pts',(-1.22735494169273,2.12254018738515,34.7245148226181));
#7429=CARTESIAN_POINT('Ctrl Pts',(-1.15556958670635,2.16092785170614,34.7202838295813));
#7430=CARTESIAN_POINT('Ctrl Pts',(-1.08363719609896,2.19939414423847,34.7160441703383));
#7431=CARTESIAN_POINT('Ctrl Pts',(-1.0097024079693,2.23430745339174,34.7118045110954));
#7432=CARTESIAN_POINT('Ctrl Pts',(-0.934151230487142,2.26546059965283,34.7075648518524));
#7433=CARTESIAN_POINT('Ctrl Pts',(-0.858890990334782,2.29649377937613,34.7033415189617));
#7434=CARTESIAN_POINT('Ctrl Pts',(-0.782027212945665,2.32379551416278,34.699118186071));
#7435=CARTESIAN_POINT('Ctrl Pts',(-0.703964597663262,2.34720772306944,34.6948948531803));
#7436=CARTESIAN_POINT('Ctrl Pts',(-0.625928348477688,2.37061202436802,34.6906729467445));
#7437=CARTESIAN_POINT('Ctrl Pts',(-0.546694509114701,2.39012927585087,34.6864510403088));
#7438=CARTESIAN_POINT('Ctrl Pts',(-0.466684066711813,2.4056508956782,34.6822291338731));
#7439=CARTESIAN_POINT('Ctrl Pts',(-0.386676329604949,2.42117199069183,34.6780073701875));
#7440=CARTESIAN_POINT('Ctrl Pts',(-0.305892496809424,2.43269763543591,34.673785606502));
#7441=CARTESIAN_POINT('Ctrl Pts',(-0.224763508495889,2.44017040701026,34.6695638428164));
#7442=CARTESIAN_POINT('Ctrl Pts',(-0.143040926436185,2.44769785436161,34.6653111898942));
#7443=CARTESIAN_POINT('Ctrl Pts',(-0.0609685902450196,2.45111281696221,
34.661058536972));
#7444=CARTESIAN_POINT('Ctrl Pts',(0.0210098607397135,2.45040993218516,34.6568058840498));
#7445=CARTESIAN_POINT('Ctrl Pts',(0.10250814005881,2.44971116440899,34.6525781401544));
#7446=CARTESIAN_POINT('Ctrl Pts',(0.183913167396883,2.4449427434225,34.648350396259));
#7447=CARTESIAN_POINT('Ctrl Pts',(0.2647929469091,2.43615166713142,34.6441226523637));
#7448=CARTESIAN_POINT('Ctrl Pts',(0.346387517802885,2.42728289792864,34.639857544928));
#7449=CARTESIAN_POINT('Ctrl Pts',(0.427447035644566,2.41432009501778,34.6355924374924));
#7450=CARTESIAN_POINT('Ctrl Pts',(0.507539056461515,2.39736404331219,34.6313273300567));
#7451=CARTESIAN_POINT('Ctrl Pts',(0.587631077278442,2.3804079916066,34.6270622226211));
#7452=CARTESIAN_POINT('Ctrl Pts',(0.666755155176612,2.35945887307616,34.6227971151854));
#7453=CARTESIAN_POINT('Ctrl Pts',(0.744496864035004,2.33466799983253,34.6185320077498));
#7454=CARTESIAN_POINT('Ctrl Pts',(0.821746605233401,2.31003400901506,34.6142938909084));
#7455=CARTESIAN_POINT('Ctrl Pts',(0.897911870471557,2.28151736349981,34.6100557740671));
#7456=CARTESIAN_POINT('Ctrl Pts',(0.972575452137889,2.24923258910651,34.6058176572258));
#7457=CARTESIAN_POINT('Ctrl Pts',(1.04713463056508,2.21699295901176,34.6015854666087));
#7458=CARTESIAN_POINT('Ctrl Pts',(1.12019587459647,2.18099584830832,34.5973532759916));
#7459=CARTESIAN_POINT('Ctrl Pts',(1.19135785393066,2.14140531284428,34.5931210853744));
#7460=CARTESIAN_POINT('Ctrl Pts',(1.26264068732286,2.1017475409583,34.5888817072477));
#7461=CARTESIAN_POINT('Ctrl Pts',(1.33201735873376,2.05848428635939,34.584642329121));
#7462=CARTESIAN_POINT('Ctrl Pts',(1.39910536548235,2.01182862746271,34.5804029509943));
#7463=CARTESIAN_POINT('Ctrl Pts',(1.46596394810679,1.96533251919509,34.5761780704754));
#7464=CARTESIAN_POINT('Ctrl Pts',(1.53054910463859,1.91546742589171,34.5719531899565));
#7465=CARTESIAN_POINT('Ctrl Pts',(1.59250914367106,1.86248889320824,34.5677283094376));
#7466=CARTESIAN_POINT('Ctrl Pts',(1.65445015555972,1.80952662956166,34.5635047263261));
#7467=CARTESIAN_POINT('Ctrl Pts',(1.7137672992506,1.753453126208,34.5592811432146));
#7468=CARTESIAN_POINT('Ctrl Pts',(1.77014178628731,1.69456434119203,34.5550575601031));
#7469=CARTESIAN_POINT('Ctrl Pts',(1.82651606798102,1.63567577067734,34.5508339923758));
#7470=CARTESIAN_POINT('Ctrl Pts',(1.87994739496282,1.57397227431585,34.5466104246486));
#7471=CARTESIAN_POINT('Ctrl Pts',(1.93015469194864,1.5097857845233,34.5423868569214));
#7472=CARTESIAN_POINT('Ctrl Pts',(1.98068694512054,1.4451838611549,34.5381359530391));
#7473=CARTESIAN_POINT('Ctrl Pts',(2.02795297969414,1.37806705166445,34.5338850491567));
#7474=CARTESIAN_POINT('Ctrl Pts',(2.07170931678843,1.30880508737245,34.5296341452743));
#7475=CARTESIAN_POINT('Ctrl Pts',(2.11524888578472,1.23988624559162,34.5254043002925));
#7476=CARTESIAN_POINT('Ctrl Pts',(2.15531327053484,1.16884388850728,34.5211744553106));
#7477=CARTESIAN_POINT('Ctrl Pts',(2.19170870188478,1.09606715856399,34.5169446103288));
#7478=CARTESIAN_POINT('Ctrl Pts',(2.22837593318399,1.02274693426516,34.5126831769961));
#7479=CARTESIAN_POINT('Ctrl Pts',(2.26131899304487,0.947666762873221,34.5084217436635));
#7480=CARTESIAN_POINT('Ctrl Pts',(2.29038972998756,0.871243441735719,34.5041603103309));
#7481=CARTESIAN_POINT('Ctrl Pts',(2.31946046693025,0.794820120598217,34.4998988769983));
#7482=CARTESIAN_POINT('Ctrl Pts',(2.34465879486285,0.71705411988034,34.4956374436657));
#7483=CARTESIAN_POINT('Ctrl Pts',(2.36588853855451,0.638374242225055,34.4913760103331));
#7484=CARTESIAN_POINT('Ctrl Pts',(2.38693655874852,0.560367852802606,34.4871510542458));
#7485=CARTESIAN_POINT('Ctrl Pts',(2.40416308639464,0.48116882329869,34.4829260981586));
#7486=CARTESIAN_POINT('Ctrl Pts',(2.41743655939156,0.401186653961825,34.4787011420714));
#7487=CARTESIAN_POINT('Ctrl Pts',(2.43069068481461,0.321321067596898,34.474482344331));
#7488=CARTESIAN_POINT('Ctrl Pts',(2.44000312251213,0.240675064453677,34.4702635465906));
#7489=CARTESIAN_POINT('Ctrl Pts',(2.44529243748287,0.159671992500489,34.4660447488501));
#7490=CARTESIAN_POINT('Ctrl Pts',(2.45061171654949,0.0782100362063449,34.4618020515196));
#7491=CARTESIAN_POINT('Ctrl Pts',(2.45186201475039,-0.00361258704432058,
34.457559354189));
#7492=CARTESIAN_POINT('Ctrl Pts',(2.44901297751089,-0.0853562299030711,
34.4533166568584));
#7493=CARTESIAN_POINT('Ctrl Pts',(2.4461852118981,-0.16648955421863,34.4491056365704));
#7494=CARTESIAN_POINT('Ctrl Pts',(2.43931913293496,-0.24754460051366,34.4448946162824));
#7495=CARTESIAN_POINT('Ctrl Pts',(2.42843724804484,-0.328089594940807,34.4406835959944));
#7496=CARTESIAN_POINT('Ctrl Pts',(2.41755909118116,-0.408606995447198,34.4364740183604));
#7497=CARTESIAN_POINT('Ctrl Pts',(2.40266792258095,-0.488614229126138,34.4322644407264));
#7498=CARTESIAN_POINT('Ctrl Pts',(2.38383806368497,-0.567685067732692,34.4280548630924));
#7499=CARTESIAN_POINT('Ctrl Pts',(2.3650088397648,-0.646753239932174,34.4238454274128));
#7500=CARTESIAN_POINT('Ctrl Pts',(2.34224129866315,-0.724884626246403,34.4196359917331));
#7501=CARTESIAN_POINT('Ctrl Pts',(2.31566046996678,-0.801665040919971,34.4154265560534));
#7502=CARTESIAN_POINT('Ctrl Pts',(2.28871480838569,-0.879499298590517,34.4111593441253));
#7503=CARTESIAN_POINT('Ctrl Pts',(2.25785052840493,-0.955944746182242,34.4068921321972));
#7504=CARTESIAN_POINT('Ctrl Pts',(2.22324886302028,-1.03058951240493,34.4026249202691));
#7505=CARTESIAN_POINT('Ctrl Pts',(2.18906615006527,-1.10433048958102,34.3984093751838));
#7506=CARTESIAN_POINT('Ctrl Pts',(2.15123634040796,-1.17631376498225,34.3941938300985));
#7507=CARTESIAN_POINT('Ctrl Pts',(2.10998025654656,-1.24616755172958,34.3899782850132));
#7508=CARTESIAN_POINT('Ctrl Pts',(2.06796570436551,-1.31730555838578,34.3856852396637));
#7509=CARTESIAN_POINT('Ctrl Pts',(2.02239791527187,-1.38623456927327,34.3813921943143));
#7510=CARTESIAN_POINT('Ctrl Pts',(1.97355470503398,-1.45259494568798,34.3770991489648));
#7511=CARTESIAN_POINT('Ctrl Pts',(1.92471149479608,-1.51895532210268,34.3728061036153));
#7512=CARTESIAN_POINT('Ctrl Pts',(1.87259323456035,-1.58274671710294,34.3685130582658));
#7513=CARTESIAN_POINT('Ctrl Pts',(1.81751758542159,-1.64364840421645,34.3642200129163));
#7514=CARTESIAN_POINT('Ctrl Pts',(1.7632259248842,-1.70368317048112,34.3599880780335));
#7515=CARTESIAN_POINT('Ctrl Pts',(1.7058548403839,-1.7611375266858,34.3557561431507));
#7516=CARTESIAN_POINT('Ctrl Pts',(1.64567922433033,-1.81567897509651,34.3515242082678));
#7517=CARTESIAN_POINT('Ctrl Pts',(1.58558996222947,-1.87014215476706,34.3472983463482));
#7518=CARTESIAN_POINT('Ctrl Pts',(1.52270450323097,-1.92170041925766,34.3430724844286));
#7519=CARTESIAN_POINT('Ctrl Pts',(1.45733640531247,-1.97005605294645,34.3388466225091));
#7520=CARTESIAN_POINT('Ctrl Pts',(1.39173504054954,-2.01858424429624,34.3346056805503));
#7521=CARTESIAN_POINT('Ctrl Pts',(1.32363360310567,-2.06388655353515,34.3303647385916));
#7522=CARTESIAN_POINT('Ctrl Pts',(1.25338465788447,-2.10570110637285,34.3261237966329));
#7523=CARTESIAN_POINT('Ctrl Pts',(1.18351173545728,-2.14729183770064,34.3219055552405));
#7524=CARTESIAN_POINT('Ctrl Pts',(1.11151463869165,-2.18543181395312,34.3176873138482));
#7525=CARTESIAN_POINT('Ctrl Pts',(1.0377700097019,-2.2199062270653,34.3134690724558));
#7526=CARTESIAN_POINT('Ctrl Pts',(0.964049845847686,-2.25436920312504,34.3092522304854));
#7527=CARTESIAN_POINT('Ctrl Pts',(0.888583721765571,-2.28516883433822,34.3050353885149));
#7528=CARTESIAN_POINT('Ctrl Pts',(0.811771585361969,-2.31213692137791,34.3008185465444));
#7529=CARTESIAN_POINT('Ctrl Pts',(0.734961421673215,-2.33910431581421,34.2966018128723));
#7530=CARTESIAN_POINT('Ctrl Pts',(0.656805753260624,-2.36224020879375,34.2923850792002));
#7531=CARTESIAN_POINT('Ctrl Pts',(0.577721790458789,-2.38142557784809,34.2881683455281));
#7532=CARTESIAN_POINT('Ctrl Pts',(0.49785086726638,-2.4008018595096,34.283909651359));
#7533=CARTESIAN_POINT('Ctrl Pts',(0.417033536840315,-2.41614842429626,34.27965095719));
#7534=CARTESIAN_POINT('Ctrl Pts',(0.335710518173299,-2.42739545562478,34.2753922630209));
#7535=CARTESIAN_POINT('Ctrl Pts',(0.255071927144433,-2.43854783012409,34.2711694107087));
#7536=CARTESIAN_POINT('Ctrl Pts',(0.173936601210025,-2.44566943717576,34.2669465583965));
#7537=CARTESIAN_POINT('Ctrl Pts',(0.092737889530107,-2.4487445628006,34.2627237060843));
#7538=CARTESIAN_POINT('Ctrl Pts',(0.0105054052777507,-2.45185883905311,
34.2584470909868));
#7539=CARTESIAN_POINT('Ctrl Pts',(-0.0717915981462766,-2.45082287749668,
34.2541704758894));
#7540=CARTESIAN_POINT('Ctrl Pts',(-0.153706531475772,-2.44567466196583,
34.2498938607919));
#7541=CARTESIAN_POINT('Ctrl Pts',(-0.235621464805245,-2.44052644643498,
34.2456172456944));
#7542=CARTESIAN_POINT('Ctrl Pts',(-0.317153850472105,-2.43126609641305,
34.241340630597));
#7543=CARTESIAN_POINT('Ctrl Pts',(-0.397867904257343,-2.41798498356832,
34.2370640154995));
#7544=CARTESIAN_POINT('Ctrl Pts',(-0.477732110699871,-2.40484370905321,
34.232832429363));
#7545=CARTESIAN_POINT('Ctrl Pts',(-0.557093992558343,-2.38771681174341,
34.2286008432265));
#7546=CARTESIAN_POINT('Ctrl Pts',(-0.63552522338495,-2.36665543339995,34.22436925709));
#7547=CARTESIAN_POINT('Ctrl Pts',(-0.713844152186092,-2.34562421186294,
34.2201437299646));
#7548=CARTESIAN_POINT('Ctrl Pts',(-0.791234631374894,-2.32066981764097,
34.2159182028391));
#7549=CARTESIAN_POINT('Ctrl Pts',(-0.86727665140296,-2.29189473142448,34.2116926757137));
#7550=CARTESIAN_POINT('Ctrl Pts',(-0.943597612318161,-2.26301409109365,
34.2074516483124));
#7551=CARTESIAN_POINT('Ctrl Pts',(-1.01855973416004,-2.23028475108662,34.2032106209111));
#7552=CARTESIAN_POINT('Ctrl Pts',(-1.09175191422655,-2.19386143768987,34.1989695935098));
#7553=CARTESIAN_POINT('Ctrl Pts',(-1.16454570854388,-2.15763637674279,34.194751650062));
#7554=CARTESIAN_POINT('Ctrl Pts',(-1.23558835825757,-2.11775765891632,34.1905337066142));
#7555=CARTESIAN_POINT('Ctrl Pts',(-1.30449542205291,-2.07442569012317,34.1863157631664));
#7556=CARTESIAN_POINT('Ctrl Pts',(-1.37337986274379,-2.03110794779103,34.1820992045254));
#7557=CARTESIAN_POINT('Ctrl Pts',(-1.44012971669603,-1.98433945321482,34.1778826458845));
#7558=CARTESIAN_POINT('Ctrl Pts',(-1.50438712146545,-1.93436543568399,34.1736660872435));
#7559=CARTESIAN_POINT('Ctrl Pts',(-1.56864310554956,-1.88439252304298,34.1694496218277));
#7560=CARTESIAN_POINT('Ctrl Pts',(-1.6304063837682,-1.83121451460029,34.1652331564118));
#7561=CARTESIAN_POINT('Ctrl Pts',(-1.68935110363642,-1.77511777035846,34.161016690996));
#7562=CARTESIAN_POINT('Ctrl Pts',(-1.74889122612015,-1.71845439099957,34.1567576349199));
#7563=CARTESIAN_POINT('Ctrl Pts',(-1.80555516479479,-1.65881329779533,34.1524985788438));
#7564=CARTESIAN_POINT('Ctrl Pts',(-1.85904559641062,-1.59652739421104,34.1482395227677));
#7565=CARTESIAN_POINT('Ctrl Pts',(-1.912078472171,-1.53477428273621,34.144016898554));
#7566=CARTESIAN_POINT('Ctrl Pts',(-1.96199168706069,-1.47042184491263,34.1397942743404));
#7567=CARTESIAN_POINT('Ctrl Pts',(-2.0085375323217,-1.40382592626546,34.1355716501267));
#7568=CARTESIAN_POINT('Ctrl Pts',(-2.05568575838159,-1.33636814545953,34.1312943781194));
#7569=CARTESIAN_POINT('Ctrl Pts',(-2.09937856932165,-1.26660881596614,34.1270171061121));
#7570=CARTESIAN_POINT('Ctrl Pts',(-2.1394061252549,-1.19494421678245,34.1227398341048));
#7571=CARTESIAN_POINT('Ctrl Pts',(-2.17943368118814,-1.12327961759877,34.1184625620975));
#7572=CARTESIAN_POINT('Ctrl Pts',(-2.21579582410861,-1.04971021558846,34.1141852900902));
#7573=CARTESIAN_POINT('Ctrl Pts',(-2.24833350072709,-0.974652101782096,
34.1099080180829));
#7574=CARTESIAN_POINT('Ctrl Pts',(-2.28384506994657,-0.892733794117691,
34.1052398101239));
#7575=CARTESIAN_POINT('Ctrl Pts',(-2.31491648604063,-0.808778775978598,
34.1005716021649));
#7576=CARTESIAN_POINT('Ctrl Pts',(-2.34133381517415,-0.723260821503584,
34.0959033942059));
#7577=CARTESIAN_POINT('Ctrl Pts',(-2.36767361785023,-0.637993835021024,
34.0912488859523));
#7578=CARTESIAN_POINT('Ctrl Pts',(-2.38938645150022,-0.551173331584216,
34.0865943776986));
#7579=CARTESIAN_POINT('Ctrl Pts',(-2.40630644908103,-0.463292049479658,
34.081939869445));
#7580=CARTESIAN_POINT('Ctrl Pts',(-2.42314169952809,-0.375850938050761,
34.0773086742108));
#7581=CARTESIAN_POINT('Ctrl Pts',(-2.43523188078036,-0.287359925256168,
34.0726774789767));
#7582=CARTESIAN_POINT('Ctrl Pts',(-2.44246148854258,-0.198323289067031,
34.0680462837425));
#7583=CARTESIAN_POINT('Ctrl Pts',(-2.44777886596267,-0.132836831930789,
34.0646400390643));
#7584=CARTESIAN_POINT('Ctrl Pts',(-2.45046784559981,-0.0670556257196897,
34.061233794386));
#7585=CARTESIAN_POINT('Ctrl Pts',(-2.45049971322092,-0.0011855396130741,
34.0578275497077));
#7586=CARTESIAN_POINT('',(-2.45049908813345,0.00211401446109679,33.2578274733736));
#7587=CARTESIAN_POINT('Ctrl Pts',(-2.44699180045922,-0.00118280948075616,
34.057827496212));
#7588=CARTESIAN_POINT('Ctrl Pts',(-2.44492511997085,0.482062993109739,34.0328023376967));
#7589=CARTESIAN_POINT('Ctrl Pts',(-2.07248525985984,1.78674845601148,33.9653918467091));
#7590=CARTESIAN_POINT('Ctrl Pts',(0.0507853920667545,2.89698596197385,33.8555960232493));
#7591=CARTESIAN_POINT('Ctrl Pts',(2.46316807672906,1.52579262516589,33.7284400258327));
#7592=CARTESIAN_POINT('Ctrl Pts',(2.61640501014275,-1.24485973594507,33.6012840284158));
#7593=CARTESIAN_POINT('Ctrl Pts',(0.36993009926562,-2.87373621598164,33.4741280309992));
#7594=CARTESIAN_POINT('Ctrl Pts',(-1.95817334103329,-1.96722679795361,33.3596425202646));
#7595=CARTESIAN_POINT('Ctrl Pts',(-2.44423543888734,-0.570546915852272,
33.2875423420022));
#7596=CARTESIAN_POINT('Ctrl Pts',(-2.44892925407896,0.00211222005066472,
33.257827496212));
#7597=CARTESIAN_POINT('',(-2.45089796908517,0.000113383330988791,32.457827496212));
#7598=CARTESIAN_POINT('Ctrl Pts',(-2.45049908813345,0.00211401446109679,
33.2578274733736));
#7599=CARTESIAN_POINT('Ctrl Pts',(-2.45041450413369,0.100161127234811,33.2527431029097));
#7600=CARTESIAN_POINT('Ctrl Pts',(-2.44444165697049,0.197950870004684,33.2476587324459));
#7601=CARTESIAN_POINT('Ctrl Pts',(-2.43269561295387,0.294859805187173,33.242574361982));
#7602=CARTESIAN_POINT('Ctrl Pts',(-2.4207837487679,0.39313681425223,33.2374182149124));
#7603=CARTESIAN_POINT('Ctrl Pts',(-2.40293460772991,0.490507975166501,33.2322620678427));
#7604=CARTESIAN_POINT('Ctrl Pts',(-2.37931704861462,0.586345147649234,33.227105920773));
#7605=CARTESIAN_POINT('Ctrl Pts',(-2.36818669111253,0.631510779987266,33.2246759592372));
#7606=CARTESIAN_POINT('Ctrl Pts',(-2.35577585951501,0.676336028494037,33.2222459977015));
#7607=CARTESIAN_POINT('Ctrl Pts',(-2.34210586539719,0.720756800364789,33.2198160361657));
#7608=CARTESIAN_POINT('Ctrl Pts',(-2.31830558535038,0.79809602972413,33.2155853273186));
#7609=CARTESIAN_POINT('Ctrl Pts',(-2.29062567491792,0.874400559717126,33.2113546184715));
#7610=CARTESIAN_POINT('Ctrl Pts',(-2.25917440202268,0.949253006972044,33.2071239096243));
#7611=CARTESIAN_POINT('Ctrl Pts',(-2.22776831532491,1.0239979133502,33.2028992790573));
#7612=CARTESIAN_POINT('Ctrl Pts',(-2.19260180589857,1.09729445521621,33.1986746484902));
#7613=CARTESIAN_POINT('Ctrl Pts',(-2.15383289516444,1.16874039448782,33.1944500179232));
#7614=CARTESIAN_POINT('Ctrl Pts',(-2.11491147791859,1.24046738294985,33.1902087687909));
#7615=CARTESIAN_POINT('Ctrl Pts',(-2.07235939643465,1.31032872450256,33.1859675196587));
#7616=CARTESIAN_POINT('Ctrl Pts',(-2.02638541823373,1.37793772964155,33.1817262705264));
#7617=CARTESIAN_POINT('Ctrl Pts',(-1.98067422462602,1.44516028562803,33.1775092641283));
#7618=CARTESIAN_POINT('Ctrl Pts',(-1.93158041103865,1.51015579536423,33.1732922577301));
#7619=CARTESIAN_POINT('Ctrl Pts',(-1.87935425682599,1.57257045226916,33.1690752513319));
#7620=CARTESIAN_POINT('Ctrl Pts',(-1.82714541628774,1.63496441787365,33.1648596429282));
#7621=CARTESIAN_POINT('Ctrl Pts',(-1.77180659544445,1.69477887331527,33.1606440345245));
#7622=CARTESIAN_POINT('Ctrl Pts',(-1.71362890871323,1.75169238544394,33.1564284261208));
#7623=CARTESIAN_POINT('Ctrl Pts',(-1.65545267334021,1.80860447775178,33.1522129228839));
#7624=CARTESIAN_POINT('Ctrl Pts',(-1.59443804608623,1.86261544619688,33.1479974196469));
#7625=CARTESIAN_POINT('Ctrl Pts',(-1.53091258389673,1.91344111758544,33.1437819164099));
#7626=CARTESIAN_POINT('Ctrl Pts',(-1.46671422046173,1.96480516612865,33.1395217599382));
#7627=CARTESIAN_POINT('Ctrl Pts',(-1.39995188104122,2.01291571941342,33.1352616034664));
#7628=CARTESIAN_POINT('Ctrl Pts',(-1.33099594219616,2.0575227949788,33.1310014469947));
#7629=CARTESIAN_POINT('Ctrl Pts',(-1.26266340285344,2.10172659811871,33.1267798046737));
#7630=CARTESIAN_POINT('Ctrl Pts',(-1.19217720525324,2.14248983358113,33.1225581623527));
#7631=CARTESIAN_POINT('Ctrl Pts',(-1.11992323246884,2.17961515029065,33.1183365200317));
#7632=CARTESIAN_POINT('Ctrl Pts',(-1.0466804974247,2.21724850981954,33.1140571064846));
#7633=CARTESIAN_POINT('Ctrl Pts',(-0.9716216894346,2.2511434269564,33.1097776929375));
#7634=CARTESIAN_POINT('Ctrl Pts',(-0.895168572881708,2.28114521153848,33.1054982793903));
#7635=CARTESIAN_POINT('Ctrl Pts',(-0.818715456328837,2.31114699612055,33.1012188658432));
#7636=CARTESIAN_POINT('Ctrl Pts',(-0.740868517148116,2.33725555424667,33.0969394522961));
#7637=CARTESIAN_POINT('Ctrl Pts',(-0.662062326808542,2.35936934908904,33.092660038749));
#7638=CARTESIAN_POINT('Ctrl Pts',(-0.584153156669579,2.38123143120935,33.0884293361011));
#7639=CARTESIAN_POINT('Ctrl Pts',(-0.505013440062888,2.39927149929197,33.0841986334532));
#7640=CARTESIAN_POINT('Ctrl Pts',(-0.425052711371263,2.41335460356657,33.0799679308054));
#7641=CARTESIAN_POINT('Ctrl Pts',(-0.34520686361132,2.42741747440699,33.0757433064796));
#7642=CARTESIAN_POINT('Ctrl Pts',(-0.264542800566075,2.43753459225269,33.0715186821538));
#7643=CARTESIAN_POINT('Ctrl Pts',(-0.18348426035662,2.44362103776371,33.067294057828));
#7644=CARTESIAN_POINT('Ctrl Pts',(-0.102106707498751,2.44973143698888,33.0630528071407));
#7645=CARTESIAN_POINT('Ctrl Pts',(-0.0203320227278529,2.4517792415305,33.0588115564533));
#7646=CARTESIAN_POINT('Ctrl Pts',(0.0614016513507029,2.44973061523332,33.054570305766));
#7647=CARTESIAN_POINT('Ctrl Pts',(0.142667989344273,2.44769370255361,33.0503533056647));
#7648=CARTESIAN_POINT('Ctrl Pts',(0.223893314766545,2.44160708876418,33.0461363055634));
#7649=CARTESIAN_POINT('Ctrl Pts',(0.304644658920101,2.4314896425425,33.041919305462));
#7650=CARTESIAN_POINT('Ctrl Pts',(0.385369232744089,2.42137555041198,33.037703703362));
#7651=CARTESIAN_POINT('Ctrl Pts',(0.465619676250428,2.40723333725223,33.0334881012619));
#7652=CARTESIAN_POINT('Ctrl Pts',(0.544968130308082,2.38913373149108,33.0292724991619));
#7653=CARTESIAN_POINT('Ctrl Pts',(0.624314604891742,2.37103457725353,33.0250570022268));
#7654=CARTESIAN_POINT('Ctrl Pts',(0.702758681592593,2.34897833118418,33.0208415052916));
#7655=CARTESIAN_POINT('Ctrl Pts',(0.779884097420945,2.32308653402966,33.0166260083565));
#7656=CARTESIAN_POINT('Ctrl Pts',(0.857826726435443,2.29692038998415,33.0123658444378));
#7657=CARTESIAN_POINT('Ctrl Pts',(0.934422118991902,2.26683706757854,33.0081056805191));
#7658=CARTESIAN_POINT('Ctrl Pts',(1.00925957123512,2.2330126215206,33.0038455166005));
#7659=CARTESIAN_POINT('Ctrl Pts',(1.08342021274699,2.19949407508094,32.999623880512));
#7660=CARTESIAN_POINT('Ctrl Pts',(1.15585419266241,2.16230207003995,32.9954022444236));
#7661=CARTESIAN_POINT('Ctrl Pts',(1.2261866659655,2.12165419194751,32.9911806083352));
#7662=CARTESIAN_POINT('Ctrl Pts',(1.29748194996689,2.08044986801926,32.9869011805014));
#7663=CARTESIAN_POINT('Ctrl Pts',(1.36661733968173,2.03569460568112,32.9826217526676));
#7664=CARTESIAN_POINT('Ctrl Pts',(1.43323442601716,1.98765925904801,32.9783423248337));
#7665=CARTESIAN_POINT('Ctrl Pts',(1.49985151235258,1.93962391241489,32.9740628969999));
#7666=CARTESIAN_POINT('Ctrl Pts',(1.56394995326115,1.88830883921173,32.9697834691661));
#7667=CARTESIAN_POINT('Ctrl Pts',(1.62520909562318,1.83402443972366,32.9655040413323));
#7668=CARTESIAN_POINT('Ctrl Pts',(1.68577070373729,1.78035815577412,32.9612733416941));
#7669=CARTESIAN_POINT('Ctrl Pts',(1.74378516371167,1.72358800022147,32.957042642056));
#7670=CARTESIAN_POINT('Ctrl Pts',(1.79891728872159,1.66398522780058,32.9528119424178));
#7671=CARTESIAN_POINT('Ctrl Pts',(1.85397020348703,1.60446808875905,32.9485873211732));
#7672=CARTESIAN_POINT('Ctrl Pts',(1.90614869472641,1.54212675404099,32.9443626999286));
#7673=CARTESIAN_POINT('Ctrl Pts',(1.95515194892122,1.47727150741817,32.940138078684));
#7674=CARTESIAN_POINT('Ctrl Pts',(2.00434810422372,1.41216095838496,32.9358968272353));
#7675=CARTESIAN_POINT('Ctrl Pts',(2.05034361506433,1.34451697771044,32.9316555757866));
#7676=CARTESIAN_POINT('Ctrl Pts',(2.09287281695147,1.27468961793278,32.9274143243379));
#7677=CARTESIAN_POINT('Ctrl Pts',(2.13515880572762,1.20526158211724,32.9231973274699));
#7678=CARTESIAN_POINT('Ctrl Pts',(2.17401777939715,1.13367547293135,32.9189803306019));
#7679=CARTESIAN_POINT('Ctrl Pts',(2.20923118738444,1.06030552704772,32.914763333734));
#7680=CARTESIAN_POINT('Ctrl Pts',(2.24443292114961,0.986959905337576,32.9105477349175));
#7681=CARTESIAN_POINT('Ctrl Pts',(2.27599128825168,0.911832040272801,32.906332136101));
#7682=CARTESIAN_POINT('Ctrl Pts',(2.3037341059364,0.835319950166052,32.9021165372845));
#7683=CARTESIAN_POINT('Ctrl Pts',(2.3314762312292,0.758809769611306,32.8979010436789));
#7684=CARTESIAN_POINT('Ctrl Pts',(2.35540283892995,0.680915870279583,32.8936855500733));
#7685=CARTESIAN_POINT('Ctrl Pts',(2.37539074539078,0.602054031389063,32.8894700564677));
#7686=CARTESIAN_POINT('Ctrl Pts',(2.39559047565151,0.522356446423122,32.885209888755));
#7687=CARTESIAN_POINT('Ctrl Pts',(2.41176739135415,0.441670749723604,32.8809497210424));
#7688=CARTESIAN_POINT('Ctrl Pts',(2.42384715130507,0.360437563400786,32.8766895533297));
#7689=CARTESIAN_POINT('Ctrl Pts',(2.43581764467612,0.279939165888083,32.8724679206506));
#7690=CARTESIAN_POINT('Ctrl Pts',(2.44376482069037,0.198903617470079,32.8682462879715));
#7691=CARTESIAN_POINT('Ctrl Pts',(2.44766867034687,0.117763874776457,32.8640246552924));
#7692=CARTESIAN_POINT('Ctrl Pts',(2.45162597147196,0.0355131675761901,32.8597452200629));
#7693=CARTESIAN_POINT('Ctrl Pts',(2.45142838660174,-0.0468441141031322,
32.8554657848334));
#7694=CARTESIAN_POINT('Ctrl Pts',(2.44710959160658,-0.128859988619679,32.8511863496039));
#7695=CARTESIAN_POINT('Ctrl Pts',(2.44279079661142,-0.210875863136225,32.8469069143744));
#7696=CARTESIAN_POINT('Ctrl Pts',(2.43435090706428,-0.292549849227604,32.8426274791449));
#7697=CARTESIAN_POINT('Ctrl Pts',(2.42187728965222,-0.373444298211699,32.8383480439155));
#7698=CARTESIAN_POINT('Ctrl Pts',(2.4095457158724,-0.453417559621855,32.8341173408624));
#7699=CARTESIAN_POINT('Ctrl Pts',(2.39322547571729,-0.532929756398903,32.8298866378093));
#7700=CARTESIAN_POINT('Ctrl Pts',(2.3729631552908,-0.61155221660324,32.8256559347562));
#7701=CARTESIAN_POINT('Ctrl Pts',(2.35272994617263,-0.690061718240528,32.8214313100445));
#7702=CARTESIAN_POINT('Ctrl Pts',(2.32856602022196,-0.767683575562253,32.8172066853328));
#7703=CARTESIAN_POINT('Ctrl Pts',(2.30056938760177,-0.843996885556813,32.8129820606211));
#7704=CARTESIAN_POINT('Ctrl Pts',(2.27246257512076,-0.920610524165473,32.8087408100326));
#7705=CARTESIAN_POINT('Ctrl Pts',(2.24049289660263,-0.995904824854882,32.8044995594442));
#7706=CARTESIAN_POINT('Ctrl Pts',(2.20481082769516,-1.06946690649041,32.8002583088558));
#7707=CARTESIAN_POINT('Ctrl Pts',(2.16933277775891,-1.14260838302442,32.796041308419));
#7708=CARTESIAN_POINT('Ctrl Pts',(2.13018487983236,-1.21403697269545,32.7918243079822));
#7709=CARTESIAN_POINT('Ctrl Pts',(2.08756345099631,-1.28336631094337,32.7876073075454));
#7710=CARTESIAN_POINT('Ctrl Pts',(2.04495615202774,-1.35267266511054,32.7833917051297));
#7711=CARTESIAN_POINT('Ctrl Pts',(1.99887785229089,-1.41988075401458,32.779176102714));
#7712=CARTESIAN_POINT('Ctrl Pts',(1.94956996752,-1.48463032157641,32.7749605002983));
#7713=CARTESIAN_POINT('Ctrl Pts',(1.90026331305108,-1.54937827354429,32.770745003068));
#7714=CARTESIAN_POINT('Ctrl Pts',(1.84772751638552,-1.61166745680075,32.7665295058376));
#7715=CARTESIAN_POINT('Ctrl Pts',(1.79224545454304,-1.67116919570396,32.7623140086072));
#7716=CARTESIAN_POINT('Ctrl Pts',(1.73617551964589,-1.73130139908245,32.7580538450981));
#7717=CARTESIAN_POINT('Ctrl Pts',(1.67709683077161,-1.78858637106687,32.7537936815891));
#7718=CARTESIAN_POINT('Ctrl Pts',(1.61533959380088,-1.84272305208873,32.7495335180801));
#7719=CARTESIAN_POINT('Ctrl Pts',(1.55414086405891,-1.89637014307751,32.7453118817499));
#7720=CARTESIAN_POINT('Ctrl Pts',(1.49031224568645,-1.94692541421358,32.7410902454197));
#7721=CARTESIAN_POINT('Ctrl Pts',(1.42420691762321,-1.99413763461658,32.7368686090896));
#7722=CARTESIAN_POINT('Ctrl Pts',(1.3571966613759,-2.04199615192372,32.7325891819911));
#7723=CARTESIAN_POINT('Ctrl Pts',(1.28784730742235,-2.08641913142763,32.7283097548926));
#7724=CARTESIAN_POINT('Ctrl Pts',(1.21655372943403,-2.12719234518182,32.7240303277942));
#7725=CARTESIAN_POINT('Ctrl Pts',(1.14526015144572,-2.16796555893602,32.7197509006957));
#7726=CARTESIAN_POINT('Ctrl Pts',(1.07202281661275,-2.20508884355044,32.7154714735972));
#7727=CARTESIAN_POINT('Ctrl Pts',(0.997256979744859,-2.23839870584982,32.7111920464988));
#7728=CARTESIAN_POINT('Ctrl Pts',(0.923342419706714,-2.27132930517074,32.7069613445572));
#7729=CARTESIAN_POINT('Ctrl Pts',(0.847655992323171,-2.30065677971026,32.7027306426156));
#7730=CARTESIAN_POINT('Ctrl Pts',(0.770583328756321,-2.32618820894674,32.6984999406741));
#7731=CARTESIAN_POINT('Ctrl Pts',(0.693621397341056,-2.35168295656406,32.6942753170839));
#7732=CARTESIAN_POINT('Ctrl Pts',(0.615277622969492,-2.37339234556173,32.6900506934937));
#7733=CARTESIAN_POINT('Ctrl Pts',(0.535958946636366,-2.39117089676176,32.6858260699035));
#7734=CARTESIAN_POINT('Ctrl Pts',(0.456328087785067,-2.40901942079971,32.6815848190359));
#7735=CARTESIAN_POINT('Ctrl Pts',(0.375715069952116,-2.42290590555947,32.6773435681684));
#7736=CARTESIAN_POINT('Ctrl Pts',(0.294548495561631,-2.43273332565704,32.6731023173008));
#7737=CARTESIAN_POINT('Ctrl Pts',(0.213846033475075,-2.44250455234474,32.6688853180014));
#7738=CARTESIAN_POINT('Ctrl Pts',(0.132596794480244,-2.44826295159171,32.664668318702));
#7739=CARTESIAN_POINT('Ctrl Pts',(0.0512319056779359,-2.4499643960353,32.6604513194026));
#7740=CARTESIAN_POINT('Ctrl Pts',(-0.0301060089409373,-2.45166527641402,
32.6562357181278));
#7741=CARTESIAN_POINT('Ctrl Pts',(-0.111559032639499,-2.44931186314919,
32.652020116853));
#7742=CARTESIAN_POINT('Ctrl Pts',(-0.192693572261953,-2.44291208135064,
32.6478045155781));
#7743=CARTESIAN_POINT('Ctrl Pts',(-0.273826087424948,-2.43651245923869,
32.6435890194905));
#7744=CARTESIAN_POINT('Ctrl Pts',(-0.35463967077687,-2.42606670698683,32.6393735234028));
#7745=CARTESIAN_POINT('Ctrl Pts',(-0.434704833013202,-2.41163470661603,
32.6351580273152));
#7746=CARTESIAN_POINT('Ctrl Pts',(-0.515618391701819,-2.39704978008393,
32.6308978624624));
#7747=CARTESIAN_POINT('Ctrl Pts',(-0.595767094165784,-2.37839369335156,
32.6266376976097));
#7748=CARTESIAN_POINT('Ctrl Pts',(-0.67471904436235,-2.35578107242052,32.6223775327569));
#7749=CARTESIAN_POINT('Ctrl Pts',(-0.752956939641188,-2.33337296389402,
32.6181558975625));
#7750=CARTESIAN_POINT('Ctrl Pts',(-0.830019217737815,-2.3070798107042,32.613934262368));
#7751=CARTESIAN_POINT('Ctrl Pts',(-0.905503439327968,-2.2770625312813,32.6097126271735));
#7752=CARTESIAN_POINT('Ctrl Pts',(-0.982021045305181,-2.24663431315832,
32.6054331974916));
#7753=CARTESIAN_POINT('Ctrl Pts',(-1.05691661037709,-2.21237943537851,32.6011537678097));
#7754=CARTESIAN_POINT('Ctrl Pts',(-1.12979623069003,-2.1745139059382,32.5968743381278));
#7755=CARTESIAN_POINT('Ctrl Pts',(-1.20267585100298,-2.13664837649788,32.5925949084459));
#7756=CARTESIAN_POINT('Ctrl Pts',(-1.27353913624145,-2.09517249973101,32.588315478764));
#7757=CARTESIAN_POINT('Ctrl Pts',(-1.34202380372876,-2.05034688777909,32.5840360490821));
#7758=CARTESIAN_POINT('Ctrl Pts',(-1.40963924105352,-2.00609021739311,32.5798109353441));
#7759=CARTESIAN_POINT('Ctrl Pts',(-1.47519193949527,-1.9584009273097,32.5755858216061));
#7760=CARTESIAN_POINT('Ctrl Pts',(-1.53831148274827,-1.90749784588209,32.5713607078681));
#7761=CARTESIAN_POINT('Ctrl Pts',(-1.60134028247577,-1.85666794503897,32.5671416683457));
#7762=CARTESIAN_POINT('Ctrl Pts',(-1.66194251379264,-1.8026337186582,32.5629226288233));
#7763=CARTESIAN_POINT('Ctrl Pts',(-1.71977605472221,-1.74565763298652,32.5587035893009));
#7764=CARTESIAN_POINT('Ctrl Pts',(-1.77754248218487,-1.68874766573987,32.554489445802));
#7765=CARTESIAN_POINT('Ctrl Pts',(-1.83254627374902,-1.62890294921535,32.550275302303));
#7766=CARTESIAN_POINT('Ctrl Pts',(-1.88447894375625,-1.56642566390472,32.546061158804));
#7767=CARTESIAN_POINT('Ctrl Pts',(-1.93637859000849,-1.50398810762327,32.5418496950602));
#7768=CARTESIAN_POINT('Ctrl Pts',(-1.98521069363507,-1.43892166303614,32.5376382313165));
#7769=CARTESIAN_POINT('Ctrl Pts',(-2.0307049877932,-1.37156388934377,32.5334267675727));
#7770=CARTESIAN_POINT('Ctrl Pts',(-2.07618439996395,-1.30422814956921,32.5292166814731));
#7771=CARTESIAN_POINT('Ctrl Pts',(-2.11832790992056,-1.23460295530773,32.5250065953735));
#7772=CARTESIAN_POINT('Ctrl Pts',(-2.15690765419008,-1.16305615569336,32.5207965092739));
#7773=CARTESIAN_POINT('Ctrl Pts',(-2.19548669074459,-1.0915106685487,32.5165865004051));
#7774=CARTESIAN_POINT('Ctrl Pts',(-2.23050187128866,-1.01804405729231,32.5123764915362));
#7775=CARTESIAN_POINT('Ctrl Pts',(-2.26177122541205,-0.943048871426129,
32.5081664826673));
#7776=CARTESIAN_POINT('Ctrl Pts',(-2.29307152271146,-0.867979472666756,
32.5039523077052));
#7777=CARTESIAN_POINT('Ctrl Pts',(-2.32061840868368,-0.791378909078912,
32.4997381327431));
#7778=CARTESIAN_POINT('Ctrl Pts',(-2.34427827865547,-0.71365930402688,32.495523957781));
#7779=CARTESIAN_POINT('Ctrl Pts',(-2.36794930498103,-0.635903051799291,
32.4913077957062));
#7780=CARTESIAN_POINT('Ctrl Pts',(-2.38772955051801,-0.557027160022369,
32.4870916336314));
#7781=CARTESIAN_POINT('Ctrl Pts',(-2.40353614312668,-0.477456028010667,
32.4828754715567));
#7782=CARTESIAN_POINT('Ctrl Pts',(-2.41937149873157,-0.397740101720686,
32.4786516374012));
#7783=CARTESIAN_POINT('Ctrl Pts',(-2.43121868415156,-0.317326869841374,
32.4744278032458));
#7784=CARTESIAN_POINT('Ctrl Pts',(-2.43904654596525,-0.23664783247469,32.4702039690903));
#7785=CARTESIAN_POINT('Ctrl Pts',(-2.44669215229249,-0.157847238743247,
32.4660784781309));
#7786=CARTESIAN_POINT('Ctrl Pts',(-2.45050364776331,-0.0787934942721454,
32.4619529871714));
#7787=CARTESIAN_POINT('Ctrl Pts',(-2.45049999737776,0.00011336492003957,
32.457827496212));
#7788=CARTESIAN_POINT('',(-2.45049903342988,-0.00217650160221668,31.657827496212));
#7789=CARTESIAN_POINT('Ctrl Pts',(-2.45453274682372,0.000113551482912981,
32.457827496212));
#7790=CARTESIAN_POINT('Ctrl Pts',(-2.45453682007855,0.00616397536570763,
32.4575116813631));
#7791=CARTESIAN_POINT('Ctrl Pts',(-2.45451638727492,0.0122143709360244,
32.4571958665142));
#7792=CARTESIAN_POINT('Ctrl Pts',(-2.44842902388592,0.830260198165473,32.414494719193));
#7793=CARTESIAN_POINT('Ctrl Pts',(-1.55054418679137,2.44765985374896,32.3297240542486));
#7794=CARTESIAN_POINT('Ctrl Pts',(1.2184054487905,2.62882374300816,32.2025680568319));
#7795=CARTESIAN_POINT('Ctrl Pts',(2.86986248022965,0.398892763100646,32.075412059415));
#7796=CARTESIAN_POINT('Ctrl Pts',(1.88914963708073,-2.19689319950944,31.9482560619984));
#7797=CARTESIAN_POINT('Ctrl Pts',(-0.824246492121587,-2.777740774871,31.8211000645817));
#7798=CARTESIAN_POINT('Ctrl Pts',(-2.31451204546487,-1.28030818469935,31.7242907365184));
#7799=CARTESIAN_POINT('Ctrl Pts',(-2.45124436907125,-0.234112490484375,
31.6698667409274));
#7800=CARTESIAN_POINT('Ctrl Pts',(-2.44926684387645,-0.00218661161304503,
31.6578280778087));
#7801=CARTESIAN_POINT('',(-2.45028716750641,0.000988674573411882,30.8578274549158));
#7802=CARTESIAN_POINT('Ctrl Pts',(-2.45049903342988,-0.00217650160221668,
31.657827496212));
#7803=CARTESIAN_POINT('Ctrl Pts',(-2.45057066460466,0.0784722442460725,
31.6536433021141));
#7804=CARTESIAN_POINT('Ctrl Pts',(-2.44665665890771,0.159202294317996,31.6494591080163));
#7805=CARTESIAN_POINT('Ctrl Pts',(-2.4387596694926,0.239586152471997,31.6452749139184));
#7806=CARTESIAN_POINT('Ctrl Pts',(-2.43086623907027,0.319933783456974,31.6410926055412));
#7807=CARTESIAN_POINT('Ctrl Pts',(-2.41899343344879,0.399935061913178,31.6369102971641));
#7808=CARTESIAN_POINT('Ctrl Pts',(-2.40319591535467,0.47916556890352,31.6327279887869));
#7809=CARTESIAN_POINT('Ctrl Pts',(-2.3874004824536,0.558385617864842,31.6285462324535));
#7810=CARTESIAN_POINT('Ctrl Pts',(-2.36768145903392,0.636834633535598,31.62436447612));
#7811=CARTESIAN_POINT('Ctrl Pts',(-2.34414471162675,0.714097907119433,31.6201827197866));
#7812=CARTESIAN_POINT('Ctrl Pts',(-2.32060357007508,0.79137560521073,31.6160001827488));
#7813=CARTESIAN_POINT('Ctrl Pts',(-2.29324342983352,0.867466669907059,31.6118176457109));
#7814=CARTESIAN_POINT('Ctrl Pts',(-2.26221968959458,0.941972571793139,31.6076351086731));
#7815=CARTESIAN_POINT('Ctrl Pts',(-2.23116118125689,1.01656197194651,31.6034478842939));
#7816=CARTESIAN_POINT('Ctrl Pts',(-2.19643106527826,1.08956222842802,31.5992606599147));
#7817=CARTESIAN_POINT('Ctrl Pts',(-2.15823215230338,1.16059649610187,31.5950734355355));
#7818=CARTESIAN_POINT('Ctrl Pts',(-2.1200075469549,1.23167854102383,31.5908833948528));
#7819=CARTESIAN_POINT('Ctrl Pts',(-2.07830974907221,1.30079156321528,31.5866933541701));
#7820=CARTESIAN_POINT('Ctrl Pts',(-2.0333852848379,1.36758712095598,31.5825033134874));
#7821=CARTESIAN_POINT('Ctrl Pts',(-1.98838819435972,1.43449066241,31.5783064990585));
#7822=CARTESIAN_POINT('Ctrl Pts',(-1.94015431715274,1.49906889049477,31.5741096846297));
#7823=CARTESIAN_POINT('Ctrl Pts',(-1.88897035835881,1.56100648148616,31.5699128702008));
#7824=CARTESIAN_POINT('Ctrl Pts',(-1.87626709970697,1.57637866560742,31.5688712700499));
#7825=CARTESIAN_POINT('Ctrl Pts',(-1.8633822975951,1.59158837468609,31.567829669899));
#7826=CARTESIAN_POINT('Ctrl Pts',(-1.85032066881284,1.60663115635295,31.5667880697481));
#7827=CARTESIAN_POINT('Ctrl Pts',(-1.79726781722405,1.66773092243555,31.5625573678087));
#7828=CARTESIAN_POINT('Ctrl Pts',(-1.74108556238763,1.72631496655015,31.5583266658693));
#7829=CARTESIAN_POINT('Ctrl Pts',(-1.68204176569144,1.78204538339225,31.55409596393));
#7830=CARTESIAN_POINT('Ctrl Pts',(-1.62308279868498,1.83769573095977,31.5498713403452));
#7831=CARTESIAN_POINT('Ctrl Pts',(-1.56127079031439,1.89050027732401,31.5456467167604));
#7832=CARTESIAN_POINT('Ctrl Pts',(-1.49691297561613,1.94015509520039,31.5414220931756));
#7833=CARTESIAN_POINT('Ctrl Pts',(-1.43230186127517,1.99000534462905,31.5371808423071));
#7834=CARTESIAN_POINT('Ctrl Pts',(-1.36512516917725,2.03668066064791,31.5329395914386));
#7835=CARTESIAN_POINT('Ctrl Pts',(-1.2957302547892,2.07991186275378,31.5286983405701));
#7836=CARTESIAN_POINT('Ctrl Pts',(-1.22673214232098,2.12289586772506,31.524481341284));
#7837=CARTESIAN_POINT('Ctrl Pts',(-1.15554150512805,2.16247479059063,31.5202643419979));
#7838=CARTESIAN_POINT('Ctrl Pts',(-1.08253035737813,2.19842631792716,31.5160473427118));
#7839=CARTESIAN_POINT('Ctrl Pts',(-1.00954341442107,2.23436592654581,31.5118317414533));
#7840=CARTESIAN_POINT('Ctrl Pts',(-0.934737576323989,2.26668032243558,31.5076161401948));
#7841=CARTESIAN_POINT('Ctrl Pts',(-0.858509105248948,2.29519331782851,31.5034005389362));
#7842=CARTESIAN_POINT('Ctrl Pts',(-0.782282536270929,2.32370560174864,31.4991850428678));
#7843=CARTESIAN_POINT('Ctrl Pts',(-0.704633840860683,2.34841651185339,31.4949695467994));
#7844=CARTESIAN_POINT('Ctrl Pts',(-0.625977535286773,2.36919867789012,31.490754050731));
#7845=CARTESIAN_POINT('Ctrl Pts',(-0.546487761341621,2.39020105866935,31.4864938858643));
#7846=CARTESIAN_POINT('Ctrl Pts',(-0.465969360420621,2.40719079973597,31.4822337209977));
#7847=CARTESIAN_POINT('Ctrl Pts',(-0.38486218130251,2.42008912054971,31.4779735561311));
#7848=CARTESIAN_POINT('Ctrl Pts',(-0.304488550124137,2.43287078662632,31.473751920963));
#7849=CARTESIAN_POINT('Ctrl Pts',(-0.223537222083068,2.44163475260481,31.4695302857949));
#7850=CARTESIAN_POINT('Ctrl Pts',(-0.142440930413526,2.44635664434745,31.4653086506268));
#7851=CARTESIAN_POINT('Ctrl Pts',(-0.0602344235502362,2.45114317919335,
31.4610292209109));
#7852=CARTESIAN_POINT('Ctrl Pts',(0.0221205514846858,2.45177612534295,31.456749791195));
#7853=CARTESIAN_POINT('Ctrl Pts',(0.104175698326536,2.44828463906429,31.4524703614791));
#7854=CARTESIAN_POINT('Ctrl Pts',(0.186230845168385,2.44479315278564,31.4481909317632));
#7855=CARTESIAN_POINT('Ctrl Pts',(0.267985681418831,2.43717734479116,31.4439115020473));
#7856=CARTESIAN_POINT('Ctrl Pts',(0.349001701606388,2.42552016323836,31.4396320723314));
#7857=CARTESIAN_POINT('Ctrl Pts',(0.42909523193789,2.41399571631889,31.4354013703917));
#7858=CARTESIAN_POINT('Ctrl Pts',(0.508767946089545,2.39847815840009,31.431170668452));
#7859=CARTESIAN_POINT('Ctrl Pts',(0.587590724305905,2.37900975002409,31.4269399665123));
#7860=CARTESIAN_POINT('Ctrl Pts',(0.666300255878092,2.35956931239418,31.4227153429273));
#7861=CARTESIAN_POINT('Ctrl Pts',(0.744161829072512,2.33618940828933,31.4184907193422));
#7862=CARTESIAN_POINT('Ctrl Pts',(0.820753574049774,2.30896379804546,31.4142660957571));
#7863=CARTESIAN_POINT('Ctrl Pts',(0.897646768995757,2.28163103318122,31.4100248448887));
#7864=CARTESIAN_POINT('Ctrl Pts',(0.973259648983094,2.25042229295735,31.4057835940203));
#7865=CARTESIAN_POINT('Ctrl Pts',(1.04717783611404,2.21548388158242,31.4015423431518));
#7866=CARTESIAN_POINT('Ctrl Pts',(1.1206733571401,2.18074524894693,31.3973253438655));
#7867=CARTESIAN_POINT('Ctrl Pts',(1.1924930886288,2.1423196828641,31.3931083445792));
#7868=CARTESIAN_POINT('Ctrl Pts',(1.26224870601945,2.10039959392308,31.3888913452929));
#7869=CARTESIAN_POINT('Ctrl Pts',(1.33198119789673,2.05849340240872,31.3846757440341));
#7870=CARTESIAN_POINT('Ctrl Pts',(1.39965053627575,2.01309522800402,31.3804601427753));
#7871=CARTESIAN_POINT('Ctrl Pts',(1.46489404893623,1.96444284095802,31.3762445415165));
#7872=CARTESIAN_POINT('Ctrl Pts',(1.53013593360256,1.91579166791474,31.3720290454478));
#7873=CARTESIAN_POINT('Ctrl Pts',(1.59295174073313,1.86388672255796,31.3678135493791));
#7874=CARTESIAN_POINT('Ctrl Pts',(1.65300995881143,1.80900755279524,31.3635980533105));
#7875=CARTESIAN_POINT('Ctrl Pts',(1.71370457373299,1.75354686510682,31.3593378884442));
#7876=CARTESIAN_POINT('Ctrl Pts',(1.77158244245977,1.69504886087445,31.3550777235778));
#7877=CARTESIAN_POINT('Ctrl Pts',(1.82633919032043,1.63384069354993,31.3508175587115));
#7878=CARTESIAN_POINT('Ctrl Pts',(1.8806007082956,1.57318610390998,31.3465959235432));
#7879=CARTESIAN_POINT('Ctrl Pts',(1.93179708661286,1.50987058085758,31.3423742883749));
#7880=CARTESIAN_POINT('Ctrl Pts',(1.9796735456331,1.44424475166797,31.3381526532066));
#7881=CARTESIAN_POINT('Ctrl Pts',(2.02820543747765,1.3777204992563,31.3338732234913));
#7882=CARTESIAN_POINT('Ctrl Pts',(2.07332555080609,1.30882261898734,31.329593793776));
#7883=CARTESIAN_POINT('Ctrl Pts',(2.11481568600755,1.23794380495094,31.3253143640606));
#7884=CARTESIAN_POINT('Ctrl Pts',(2.15630582120902,1.16706499091454,31.3210349343453));
#7885=CARTESIAN_POINT('Ctrl Pts',(2.19416581018964,1.09420570863176,31.31675550463));
#7886=CARTESIAN_POINT('Ctrl Pts',(2.22822798017986,1.01977954399154,31.3124760749147));
#7887=CARTESIAN_POINT('Ctrl Pts',(2.26190230088916,0.946200833710374,31.3082453729738));
#7888=CARTESIAN_POINT('Ctrl Pts',(2.2919915486179,0.870814010198756,31.304014671033));
#7889=CARTESIAN_POINT('Ctrl Pts',(2.31829892371577,0.794002739477832,31.2997839690922));
#7890=CARTESIAN_POINT('Ctrl Pts',(2.34456850235438,0.717301825417503,31.2955593455059));
#7891=CARTESIAN_POINT('Ctrl Pts',(2.36706685020385,0.639180964924323,31.2913347219196));
#7892=CARTESIAN_POINT('Ctrl Pts',(2.38564439164342,0.56004561119637,31.2871100983334));
#7893=CARTESIAN_POINT('Ctrl Pts',(2.40429505060736,0.480598796386542,31.2828688474652));
#7894=CARTESIAN_POINT('Ctrl Pts',(2.41899377644315,0.400129917034853,31.2786275965971));
#7895=CARTESIAN_POINT('Ctrl Pts',(2.42963922641231,0.319066575307708,31.2743863457289));
#7896=CARTESIAN_POINT('Ctrl Pts',(2.44022380542717,0.238466755835059,31.2701693464414));
#7897=CARTESIAN_POINT('Ctrl Pts',(2.44680127509927,0.157279719577928,31.2659523471538));
#7898=CARTESIAN_POINT('Ctrl Pts',(2.44932316256167,0.0759361267046567,31.2617353478663));
#7899=CARTESIAN_POINT('Ctrl Pts',(2.45184421396321,-0.00538049898817242,
31.2575197466062));
#7900=CARTESIAN_POINT('Ctrl Pts',(2.45031233873219,-0.0868531137599519,
31.2533041453462));
#7901=CARTESIAN_POINT('Ctrl Pts',(2.44473108895797,-0.168048066583332,31.2490885440861));
#7902=CARTESIAN_POINT('Ctrl Pts',(2.43914997845033,-0.249240993383016,31.2448730480162));
#7903=CARTESIAN_POINT('Ctrl Pts',(2.42951972727157,-0.330155808118384,31.2406575519463));
#7904=CARTESIAN_POINT('Ctrl Pts',(2.41589588316585,-0.410362439438967,31.2364420558764));
#7905=CARTESIAN_POINT('Ctrl Pts',(2.40212767628792,-0.491418966835655,31.2321818910115));
#7906=CARTESIAN_POINT('Ctrl Pts',(2.38428080292077,-0.571751732836788,31.2279217261466));
#7907=CARTESIAN_POINT('Ctrl Pts',(2.36246552773728,-0.650927707393862,31.2236615612818));
#7908=CARTESIAN_POINT('Ctrl Pts',(2.3408475538161,-0.729387600233239,31.2194399261122));
#7909=CARTESIAN_POINT('Ctrl Pts',(2.3153328771864,-0.806711114717247,31.2152182909426));
#7910=CARTESIAN_POINT('Ctrl Pts',(2.28607834965286,-0.882494209186918,31.210996655773));
#7911=CARTESIAN_POINT('Ctrl Pts',(2.25642332516027,-0.959314780636797,31.2067172260605));
#7912=CARTESIAN_POINT('Ctrl Pts',(2.22292547788918,-1.03455198387522,31.202437796348));
#7913=CARTESIAN_POINT('Ctrl Pts',(2.18579683249517,-1.10780975670649,31.1981583666355));
#7914=CARTESIAN_POINT('Ctrl Pts',(2.14866818710117,-1.18106752953774,31.193878936923));
#7915=CARTESIAN_POINT('Ctrl Pts',(2.10790904396655,-1.25234547859705,31.1895995072104));
#7916=CARTESIAN_POINT('Ctrl Pts',(2.06377634851442,-1.32127871144301,31.1853200774979));
#7917=CARTESIAN_POINT('Ctrl Pts',(2.02014617047353,-1.38942703529204,31.1810893755578));
#7918=CARTESIAN_POINT('Ctrl Pts',(1.97305480665064,-1.45554011598604,31.1768586736177));
#7919=CARTESIAN_POINT('Ctrl Pts',(1.92271827747711,-1.51924477140962,31.1726279716777));
#7920=CARTESIAN_POINT('Ctrl Pts',(1.87245406804555,-1.58285790077212,31.1684033480921));
#7921=CARTESIAN_POINT('Ctrl Pts',(1.81895423894421,-1.64406911529902,31.1641787245067));
#7922=CARTESIAN_POINT('Ctrl Pts',(1.7624786959864,-1.70253314099728,31.1599541009211));
#7923=CARTESIAN_POINT('Ctrl Pts',(1.70578087646207,-1.76122726953682,31.1557128500528));
#7924=CARTESIAN_POINT('Ctrl Pts',(1.64608412507255,-1.81715213841931,31.1514715991845));
#7925=CARTESIAN_POINT('Ctrl Pts',(1.58369308339694,-1.86999103409634,31.1472303483161));
#7926=CARTESIAN_POINT('Ctrl Pts',(1.52165879530242,-1.92252779560879,31.1430133490294));
#7927=CARTESIAN_POINT('Ctrl Pts',(1.45696130381112,-1.97201347592064,31.1387963497426));
#7928=CARTESIAN_POINT('Ctrl Pts',(1.38993644591489,-2.01817415658745,31.1345793504558));
#7929=CARTESIAN_POINT('Ctrl Pts',(1.32293380822533,-2.06431953397878,31.1303637491966));
#7930=CARTESIAN_POINT('Ctrl Pts',(1.25360571905293,-2.10714183715016,31.1261481479373));
#7931=CARTESIAN_POINT('Ctrl Pts',(1.18231869690441,-2.14640926874403,31.121932546678));
#7932=CARTESIAN_POINT('Ctrl Pts',(1.11103345355109,-2.18567572051412,31.1177170506089));
#7933=CARTESIAN_POINT('Ctrl Pts',(1.03778978228109,-2.22138725363831,31.1135015545398));
#7934=CARTESIAN_POINT('Ctrl Pts',(0.96297934302438,-2.25335772457644,31.1092860584707));
#7935=CARTESIAN_POINT('Ctrl Pts',(0.887376187502514,-2.2856669652447,31.1050258936049));
#7936=CARTESIAN_POINT('Ctrl Pts',(0.810173301462727,-2.31415518338303,31.1007657287391));
#7937=CARTESIAN_POINT('Ctrl Pts',(0.731794456776513,-2.33868063724639,31.0965055638733));
#7938=CARTESIAN_POINT('Ctrl Pts',(0.654124484453692,-2.36298427849548,31.0922839287045));
#7939=CARTESIAN_POINT('Ctrl Pts',(0.575300209773864,-2.3833964889251,31.0880622935357));
#7940=CARTESIAN_POINT('Ctrl Pts',(0.495746255226477,-2.39983038992945,31.0838406583669));
#7941=CARTESIAN_POINT('Ctrl Pts',(0.415103200256682,-2.41648927244009,31.0795612286526));
#7942=CARTESIAN_POINT('Ctrl Pts',(0.333710824245474,-2.4290600184796,31.0752817989383));
#7943=CARTESIAN_POINT('Ctrl Pts',(0.252016912124409,-2.43750645660751,31.071002369224));
#7944=CARTESIAN_POINT('Ctrl Pts',(0.170323000003344,-2.44595289473541,31.0667229395097));
#7945=CARTESIAN_POINT('Ctrl Pts',(0.0883280451273653,-2.45027506452806,
31.0624435097955));
#7946=CARTESIAN_POINT('Ctrl Pts',(0.00647794685830275,-2.45049143769255,
31.0581640800812));
#7947=CARTESIAN_POINT('Ctrl Pts',(-0.074440164355392,-2.45070534712159,
31.053933378141));
#7948=CARTESIAN_POINT('Ctrl Pts',(-0.155521056560431,-2.44690733381109,
31.0497026762008));
#7949=CARTESIAN_POINT('Ctrl Pts',(-0.236334018065208,-2.43907697334569,
31.0454719742606));
#7950=CARTESIAN_POINT('Ctrl Pts',(-0.317030873580547,-2.43125786295369,
31.041247350675));
#7951=CARTESIAN_POINT('Ctrl Pts',(-0.397460103947968,-2.41941795583632,
31.0370227270894));
#7952=CARTESIAN_POINT('Ctrl Pts',(-0.477190701374035,-2.40358883433131,
31.0327981035038));
#7953=CARTESIAN_POINT('Ctrl Pts',(-0.557235102658854,-2.38769741253546,
31.0285568526355));
#7954=CARTESIAN_POINT('Ctrl Pts',(-0.636574885292314,-2.36778530622874,
31.0243156017671));
#7955=CARTESIAN_POINT('Ctrl Pts',(-0.714778833416086,-2.34393717264357,
31.0200743508988));
#7956=CARTESIAN_POINT('Ctrl Pts',(-0.792535609355393,-2.32022540329891,
31.015857351612));
#7957=CARTESIAN_POINT('Ctrl Pts',(-0.8691690556904,-2.2926226341564,31.0116403523251));
#7958=CARTESIAN_POINT('Ctrl Pts',(-0.944267047302358,-2.26126292000264,
31.0074233530382));
#7959=CARTESIAN_POINT('Ctrl Pts',(-1.01934014228714,-2.22991360228021,31.0032077517788));
#7960=CARTESIAN_POINT('Ctrl Pts',(-1.09287836460301,-2.19480999197966,30.9989921505195));
#7961=CARTESIAN_POINT('Ctrl Pts',(-1.16448839141628,-2.15613474445748,30.9947765492601));
#7962=CARTESIAN_POINT('Ctrl Pts',(-1.23609663137431,-2.11746046198268,30.9905610531909));
#7963=CARTESIAN_POINT('Ctrl Pts',(-1.30577636281149,-2.07521494143544,30.9863455571217));
#7964=CARTESIAN_POINT('Ctrl Pts',(-1.37315903482018,-2.02962669353054,30.9821300610525));
#7965=CARTESIAN_POINT('Ctrl Pts',(-1.44125571600152,-1.98355537740946,30.9778698961868));
#7966=CARTESIAN_POINT('Ctrl Pts',(-1.50700595679883,-1.93407032895756,30.9736097313212));
#7967=CARTESIAN_POINT('Ctrl Pts',(-1.57006115166227,-1.88145109690392,30.9693495664555));
#7968=CARTESIAN_POINT('Ctrl Pts',(-1.6325460640095,-1.82930776264301,30.9651279312866));
#7969=CARTESIAN_POINT('Ctrl Pts',(-1.69238417959032,-1.77408707324614,30.9609062961177));
#7970=CARTESIAN_POINT('Ctrl Pts',(-1.74927255891719,-1.7160989961594,30.9566846609488));
#7971=CARTESIAN_POINT('Ctrl Pts',(-1.80693974500443,-1.65731705735625,30.9524052312348));
#7972=CARTESIAN_POINT('Ctrl Pts',(-1.86157549088736,-1.59569175573528,30.9481258015207));
#7973=CARTESIAN_POINT('Ctrl Pts',(-1.9129069490887,-1.53157998619992,30.9438463718067));
#7974=CARTESIAN_POINT('Ctrl Pts',(-1.96423840729007,-1.46746821666454,30.9395669420926));
#7975=CARTESIAN_POINT('Ctrl Pts',(-2.01226534397574,-1.40087041543376,30.9352875123785));
#7976=CARTESIAN_POINT('Ctrl Pts',(-2.05676187417565,-1.33217147655152,30.9310080826645));
#7977=CARTESIAN_POINT('Ctrl Pts',(-2.10171929271023,-1.26276096444339,30.9266843272642));
#7978=CARTESIAN_POINT('Ctrl Pts',(-2.14323638783552,-1.19095353206572,30.9223605718639));
#7979=CARTESIAN_POINT('Ctrl Pts',(-2.18105535464682,-1.11711583551861,30.9180368164637));
#7980=CARTESIAN_POINT('Ctrl Pts',(-2.21881263121973,-1.04339858290442,30.9137201139663));
#7981=CARTESIAN_POINT('Ctrl Pts',(-2.25288357200986,-0.967658035310448,
30.909403411469));
#7982=CARTESIAN_POINT('Ctrl Pts',(-2.28305401222222,-0.890289069502711,
30.9050867089717));
#7983=CARTESIAN_POINT('Ctrl Pts',(-2.31317310560313,-0.813051777320532,
30.9007773530359));
#7984=CARTESIAN_POINT('Ctrl Pts',(-2.33940475210986,-0.734191988263348,
30.8964679971001));
#7985=CARTESIAN_POINT('Ctrl Pts',(-2.36158169918636,-0.654126996895925,
30.8921586411643));
#7986=CARTESIAN_POINT('Ctrl Pts',(-2.3837364086968,-0.574142289371331,30.8878536063637));
#7987=CARTESIAN_POINT('Ctrl Pts',(-2.40184438315073,-0.49295520152023,30.8835485715631));
#7988=CARTESIAN_POINT('Ctrl Pts',(-2.41578745660414,-0.411000260966004,
30.8792435367625));
#7989=CARTESIAN_POINT('Ctrl Pts',(-2.42971883039785,-0.329114088959626,
30.8749421143249));
#7990=CARTESIAN_POINT('Ctrl Pts',(-2.43949218192722,-0.246461776575417,
30.8706406918873));
#7991=CARTESIAN_POINT('Ctrl Pts',(-2.44504020385128,-0.163488995198076,
30.8663392694497));
#7992=CARTESIAN_POINT('Ctrl Pts',(-2.44869973006771,-0.108759386545377,
30.8635020117038));
#7993=CARTESIAN_POINT('Ctrl Pts',(-2.4505219261096,-0.0538905871457517,
30.8606647539579));
#7994=CARTESIAN_POINT('Ctrl Pts',(-2.4504998008426,0.000987962737408825,
30.857827496212));
#7995=CARTESIAN_POINT('',(-2.45288797253939,0.00174278626405643,30.057827496212));
#7996=CARTESIAN_POINT('Ctrl Pts',(-2.44683799040888,0.00100022143846595,
30.8578267850394));
#7997=CARTESIAN_POINT('Ctrl Pts',(-2.44809241697276,0.348475602492684,30.8398352184422));
#7998=CARTESIAN_POINT('Ctrl Pts',(-2.21640111872538,1.51294853004426,30.7794583193726));
#7999=CARTESIAN_POINT('Ctrl Pts',(-0.427813795401416,2.86569388547629,30.676696087831));
#8000=CARTESIAN_POINT('Ctrl Pts',(2.17773023598689,1.91120828484089,30.5495400904143));
#8001=CARTESIAN_POINT('Ctrl Pts',(2.78591169168837,-0.796192272567481,30.4223840929975));
#8002=CARTESIAN_POINT('Ctrl Pts',(0.838920950119278,-2.77334414168751,30.2952280955807));
#8003=CARTESIAN_POINT('Ctrl Pts',(-1.75708235892424,-2.23196450228063,30.1737092299857));
#8004=CARTESIAN_POINT('Ctrl Pts',(-2.44721005689546,-0.703532279603159,
30.0945756968627));
#8005=CARTESIAN_POINT('Ctrl Pts',(-2.45288797253939,0.00174278626405643,
30.057827496212));
#8006=CARTESIAN_POINT('',(-2.45231819670878,-0.0019531457292471,29.257827496212));
#8007=CARTESIAN_POINT('Ctrl Pts',(-2.45288797253939,0.00174278626405643,
30.057827496212));
#8008=CARTESIAN_POINT('Ctrl Pts',(-2.45375895828535,0.109931172263209,30.0521903643904));
#8009=CARTESIAN_POINT('Ctrl Pts',(-2.39807262124372,1.0306806169693,30.0041679000973));
#8010=CARTESIAN_POINT('Ctrl Pts',(-1.23228707159884,2.62234525986871,29.9137601033299));
#8011=CARTESIAN_POINT('Ctrl Pts',(1.53758168640185,2.45582341515417,29.7866041059142));
#8012=CARTESIAN_POINT('Ctrl Pts',(2.89721695141521,0.0368785196587262,29.6594481084969));
#8013=CARTESIAN_POINT('Ctrl Pts',(1.59959347208367,-2.41589048030868,29.5322921110805));
#8014=CARTESIAN_POINT('Ctrl Pts',(-1.16513924082463,-2.65286197120667,29.4051361136636));
#8015=CARTESIAN_POINT('Ctrl Pts',(-2.38547217171649,-1.07272642830989,29.3136479087075));
#8016=CARTESIAN_POINT('Ctrl Pts',(-2.45344099196259,-0.130954814691625,
29.2645450362236));
#8017=CARTESIAN_POINT('Ctrl Pts',(-2.45231819670878,-0.0019531457292471,
29.257827496212));
#8018=CARTESIAN_POINT('',(-2.44662742701941,-0.000665902842327259,28.4578274962121));
#8019=CARTESIAN_POINT('Ctrl Pts',(-2.45231819670878,-0.0019531457292471,
29.257827496212));
#8020=CARTESIAN_POINT('Ctrl Pts',(-2.4463565458635,0.683000683748745,29.2221597037514));
#8021=CARTESIAN_POINT('Ctrl Pts',(-1.79037424641765,2.19191624501729,29.1441065788186));
#8022=CARTESIAN_POINT('Ctrl Pts',(0.768057079194582,2.79379927909598,29.0236681214135));
#8023=CARTESIAN_POINT('Ctrl Pts',(2.76474296314598,0.866846258871282,28.8965121239966));
#8024=CARTESIAN_POINT('Ctrl Pts',(2.22567210609608,-1.85515761188246,28.76935612658));
#8025=CARTESIAN_POINT('Ctrl Pts',(-0.354732474020897,-2.87565487509438,
28.6422001291633));
#8026=CARTESIAN_POINT('Ctrl Pts',(-2.19633750317876,-1.55513202065881,28.5383572523739));
#8027=CARTESIAN_POINT('Ctrl Pts',(-2.44752200009088,-0.369091194471079,
28.4768997080569));
#8028=CARTESIAN_POINT('Ctrl Pts',(-2.44662742701941,-0.000665902842327259,
28.4578274962121));
#8029=CARTESIAN_POINT('',(-2.45049897433075,0.00224205350688658,27.6578274763058));
#8030=CARTESIAN_POINT('Ctrl Pts',(-2.44662742701941,-0.000665902842327259,
28.4578274962121));
#8031=CARTESIAN_POINT('Ctrl Pts',(-2.44553393612832,0.449682663744117,28.4345143755846));
#8032=CARTESIAN_POINT('Ctrl Pts',(-2.11046025923188,1.72031868191387,28.368815922485));
#8033=CARTESIAN_POINT('Ctrl Pts',(-0.0660938160396643,2.89669772262467,
28.2607321369129));
#8034=CARTESIAN_POINT('Ctrl Pts',(2.39963642723916,1.62387533568544,28.1335761394963));
#8035=CARTESIAN_POINT('Ctrl Pts',(2.66447699381769,-1.13832703481685,28.0064201420796));
#8036=CARTESIAN_POINT('Ctrl Pts',(0.485522390872327,-2.8564828192631,27.8792641446627));
#8037=CARTESIAN_POINT('Ctrl Pts',(-1.91257976242076,-2.03245344355806,27.7630665960403));
#8038=CARTESIAN_POINT('Ctrl Pts',(-2.44444423210955,-0.60282188315779,27.68925437989));
#8039=CARTESIAN_POINT('Ctrl Pts',(-2.44987016120039,0.00224109493129301,
27.657827496212));
#8040=CARTESIAN_POINT('',(-2.45083979799343,-0.000495560851292726,26.8578274467331));
#8041=CARTESIAN_POINT('Ctrl Pts',(-2.45049897433075,0.00224205350688658,
27.6578274763058));
#8042=CARTESIAN_POINT('Ctrl Pts',(-2.45040243215944,0.107759825969181,27.6523482552264));
#8043=CARTESIAN_POINT('Ctrl Pts',(-2.44348655931152,0.21297287842917,27.646869034147));
#8044=CARTESIAN_POINT('Ctrl Pts',(-2.42989259424758,0.317131251094503,27.6413898130676));
#8045=CARTESIAN_POINT('Ctrl Pts',(-2.41629862918364,0.421289623759814,27.6359105919881));
#8046=CARTESIAN_POINT('Ctrl Pts',(-2.39602674806883,0.524393675050337,27.6304313709087));
#8047=CARTESIAN_POINT('Ctrl Pts',(-2.36926728014889,0.625717831946559,27.6249521498292));
#8048=CARTESIAN_POINT('Ctrl Pts',(-2.34860534094122,0.703953825887892,27.620721447889));
#8049=CARTESIAN_POINT('Ctrl Pts',(-2.32402521275331,0.781312427764519,27.6164907459487));
#8050=CARTESIAN_POINT('Ctrl Pts',(-2.2956182417327,0.857372228512266,27.6122600440085));
#8051=CARTESIAN_POINT('Ctrl Pts',(-2.26725208371305,0.93332275225474,27.6080354204228));
#8052=CARTESIAN_POINT('Ctrl Pts',(-2.23507016376297,1.00797774891626,27.6038107968372));
#8053=CARTESIAN_POINT('Ctrl Pts',(-2.19921415187152,1.08092893578072,27.5995861732515));
#8054=CARTESIAN_POINT('Ctrl Pts',(-2.16321701781103,1.15416724408399,27.5953449223832));
#8055=CARTESIAN_POINT('Ctrl Pts',(-2.1235169299542,1.22568784328453,27.5911036715149));
#8056=CARTESIAN_POINT('Ctrl Pts',(-2.0803068914358,1.29509593754467,27.5868624206466));
#8057=CARTESIAN_POINT('Ctrl Pts',(-2.03734392902704,1.36410715453983,27.5826454213597));
#8058=CARTESIAN_POINT('Ctrl Pts',(-1.99091129526616,1.43102956097969,27.5784284220728));
#8059=CARTESIAN_POINT('Ctrl Pts',(-1.94124479636811,1.49549954549433,27.5742114227858));
#8060=CARTESIAN_POINT('Ctrl Pts',(-1.89159476300097,1.55994815679872,27.5699958215264));
#8061=CARTESIAN_POINT('Ctrl Pts',(-1.83871327709317,1.62194559259938,27.565780220267));
#8062=CARTESIAN_POINT('Ctrl Pts',(-1.78287825230751,1.68115894175683,27.5615646190076));
#8063=CARTESIAN_POINT('Ctrl Pts',(-1.72704462074996,1.74037081338824,27.5573491229383));
#8064=CARTESIAN_POINT('Ctrl Pts',(-1.66825791668813,1.79679839888665,27.553133626869));
#8065=CARTESIAN_POINT('Ctrl Pts',(-1.60683396932768,1.85014454705967,27.5489181307998));
#8066=CARTESIAN_POINT('Ctrl Pts',(-1.54475915342195,1.90405596873513,27.5446579659342));
#8067=CARTESIAN_POINT('Ctrl Pts',(-1.47999122643444,1.95481993054553,27.5403978010686));
#8068=CARTESIAN_POINT('Ctrl Pts',(-1.41289018521353,2.0021717145458,27.536137636203));
#8069=CARTESIAN_POINT('Ctrl Pts',(-1.34639601786848,2.04909524050176,27.531916001034));
#8070=CARTESIAN_POINT('Ctrl Pts',(-1.27761119901213,2.09266786159333,27.5276943658651));
#8071=CARTESIAN_POINT('Ctrl Pts',(-1.20691333802824,2.13267682607786,27.5234727306962));
#8072=CARTESIAN_POINT('Ctrl Pts',(-1.13524761730665,2.17323351669346,27.5191933009822));
#8073=CARTESIAN_POINT('Ctrl Pts',(-1.06161652068226,2.21012801679181,27.5149138712683));
#8074=CARTESIAN_POINT('Ctrl Pts',(-0.986435236875301,2.24318875118675,27.5106344415544));
#8075=CARTESIAN_POINT('Ctrl Pts',(-0.911253953068366,2.27624948558168,27.5063550118404));
#8076=CARTESIAN_POINT('Ctrl Pts',(-0.834522963846833,2.30547634084916,27.5020755821265));
#8077=CARTESIAN_POINT('Ctrl Pts',(-0.756672398388362,2.3307503365906,27.4977961524126));
#8078=CARTESIAN_POINT('Ctrl Pts',(-0.679708279253032,2.35573654970048,27.4935654504723));
#8079=CARTESIAN_POINT('Ctrl Pts',(-0.601360480166206,2.37695348549076,27.4893347485321));
#8080=CARTESIAN_POINT('Ctrl Pts',(-0.522032759855261,2.39424978806262,27.4851040465919));
#8081=CARTESIAN_POINT('Ctrl Pts',(-0.442819011650787,2.41152124060689,27.4808794230062));
#8082=CARTESIAN_POINT('Ctrl Pts',(-0.362628588873525,2.42488314889302,27.4766547994205));
#8083=CARTESIAN_POINT('Ctrl Pts',(-0.281881460098939,2.43423357393092,27.4724301758349));
#8084=CARTESIAN_POINT('Ctrl Pts',(-0.20081652660081,2.44362080039184,27.4681889249666));
#8085=CARTESIAN_POINT('Ctrl Pts',(-0.119190946900974,2.4489647525341,27.4639476740983));
#8086=CARTESIAN_POINT('Ctrl Pts',(-0.0374411427535714,2.4502139520518,27.45970642323));
#8087=CARTESIAN_POINT('Ctrl Pts',(0.0438412139151539,2.45145600861459,27.455489423943));
#8088=CARTESIAN_POINT('Ctrl Pts',(0.125245908568656,2.44865000610601,27.4512724246561));
#8089=CARTESIAN_POINT('Ctrl Pts',(0.206339563933992,2.44179733687207,27.4470554253691));
#8090=CARTESIAN_POINT('Ctrl Pts',(0.287406334978518,2.43494693944789,27.4428398241097));
#8091=CARTESIAN_POINT('Ctrl Pts',(0.368161808464795,2.42405257853439,27.4386242228503));
#8092=CARTESIAN_POINT('Ctrl Pts',(0.44817562109846,2.40916767009957,27.4344086215908));
#8093=CARTESIAN_POINT('Ctrl Pts',(0.528187437180859,2.39428313308167,27.4301931255215));
#8094=CARTESIAN_POINT('Ctrl Pts',(0.607457172187924,2.37540833264341,27.4259776294522));
#8095=CARTESIAN_POINT('Ctrl Pts',(0.685564000345778,2.35264792338971,27.421762133383));
#8096=CARTESIAN_POINT('Ctrl Pts',(0.764498474393691,2.32964633728093,27.4175019685174));
#8097=CARTESIAN_POINT('Ctrl Pts',(0.84224478012513,2.30267642571266,27.4132418036518));
#8098=CARTESIAN_POINT('Ctrl Pts',(0.918385447377913,2.27189753731203,27.4089816387862));
#8099=CARTESIAN_POINT('Ctrl Pts',(0.993837484752943,2.24139701870932,27.4047600036172));
#8100=CARTESIAN_POINT('Ctrl Pts',(1.06771240951862,2.20715639802593,27.4005383684483));
#8101=CARTESIAN_POINT('Ctrl Pts',(1.13962690685303,2.1693779668782,27.3963167332793));
#8102=CARTESIAN_POINT('Ctrl Pts',(1.21252591977968,2.13108234579111,27.3920373035654));
#8103=CARTESIAN_POINT('Ctrl Pts',(1.28340999627475,2.08915156679824,27.3877578738515));
#8104=CARTESIAN_POINT('Ctrl Pts',(1.35191009511807,2.04384181010123,27.3834784441376));
#8105=CARTESIAN_POINT('Ctrl Pts',(1.42041019396138,1.99853205340422,27.3791990144237));
#8106=CARTESIAN_POINT('Ctrl Pts',(1.48652595895594,1.949843662644,27.3749195847098));
#8107=CARTESIAN_POINT('Ctrl Pts',(1.54992447940426,1.89807385476526,27.3706401549958));
#8108=CARTESIAN_POINT('Ctrl Pts',(1.61260111190016,1.84689352437498,27.3664094530556));
#8109=CARTESIAN_POINT('Ctrl Pts',(1.67285783685067,1.79250912326261,27.3621787511153));
#8110=CARTESIAN_POINT('Ctrl Pts',(1.7303488008871,1.73517816873904,27.3579480491751));
#8111=CARTESIAN_POINT('Ctrl Pts',(1.7877571662273,1.67792958302206,27.3537234255894));
#8112=CARTESIAN_POINT('Ctrl Pts',(1.84240733600468,1.61774317723485,27.3494988020037));
#8113=CARTESIAN_POINT('Ctrl Pts',(1.89398622828456,1.55491685213983,27.345274178418));
#8114=CARTESIAN_POINT('Ctrl Pts',(1.94576812487976,1.49184325505919,27.3410329275497));
#8115=CARTESIAN_POINT('Ctrl Pts',(1.99445414866917,1.42610921385212,27.3367916766814));
#8116=CARTESIAN_POINT('Ctrl Pts',(2.03976473497208,1.358053782427,27.3325504258131));
#8117=CARTESIAN_POINT('Ctrl Pts',(2.08481623417947,1.29038749370562,27.3283334265262));
#8118=CARTESIAN_POINT('Ctrl Pts',(2.12653053250318,1.2204266812668,27.3241164272392));
#8119=CARTESIAN_POINT('Ctrl Pts',(2.16467416497904,1.1485364641457,27.3198994279523));
#8120=CARTESIAN_POINT('Ctrl Pts',(2.20280515200626,1.07667008020431,27.3156838266928));
#8121=CARTESIAN_POINT('Ctrl Pts',(2.23736760612117,1.00287597228716,27.3114682254334));
#8122=CARTESIAN_POINT('Ctrl Pts',(2.26817343341489,0.927544891609505,27.3072526241739));
#8123=CARTESIAN_POINT('Ctrl Pts',(2.29897849202367,0.852215690636856,27.3030371281046));
#8124=CARTESIAN_POINT('Ctrl Pts',(2.3260269351577,0.775350024024735,27.2988216320353));
#8125=CARTESIAN_POINT('Ctrl Pts',(2.34917891190414,0.697358365451296,27.294606135966));
#8126=CARTESIAN_POINT('Ctrl Pts',(2.37257621468474,0.618540281363256,27.2903459711004));
#8127=CARTESIAN_POINT('Ctrl Pts',(2.39199382957937,0.538572660311562,27.2860858062349));
#8128=CARTESIAN_POINT('Ctrl Pts',(2.40733970685371,0.457892766710145,27.2818256413693));
#8129=CARTESIAN_POINT('Ctrl Pts',(2.42254679325627,0.377942556564998,27.2776040062003));
#8130=CARTESIAN_POINT('Ctrl Pts',(2.4337554932477,0.297293380137397,27.2733823710314));
#8131=CARTESIAN_POINT('Ctrl Pts',(2.4409283538408,0.216377035325058,27.2691607358624));
#8132=CARTESIAN_POINT('Ctrl Pts',(2.44819941150616,0.134352938862447,27.2648813061485));
#8133=CARTESIAN_POINT('Ctrl Pts',(2.45132327236097,0.0520547978091799,27.2606018764346));
#8134=CARTESIAN_POINT('Ctrl Pts',(2.45031551854859,-0.0300684146565806,
27.2563224467207));
#8135=CARTESIAN_POINT('Ctrl Pts',(2.44930776473621,-0.112191627122318,27.2520430170068));
#8136=CARTESIAN_POINT('Ctrl Pts',(2.44416849232606,-0.194139425473974,27.247763587293));
#8137=CARTESIAN_POINT('Ctrl Pts',(2.43496734690492,-0.275470995763323,27.2434841575791));
#8138=CARTESIAN_POINT('Ctrl Pts',(2.42587097042757,-0.355876483230728,27.2392534556388));
#8139=CARTESIAN_POINT('Ctrl Pts',(2.41277058077393,-0.435982137070138,27.2350227536985));
#8140=CARTESIAN_POINT('Ctrl Pts',(2.39569543844949,-0.515357755537185,27.2307920517583));
#8141=CARTESIAN_POINT('Ctrl Pts',(2.37864482840621,-0.594619333081269,27.2265674281726));
#8142=CARTESIAN_POINT('Ctrl Pts',(2.35763090428507,-0.673152507544719,27.2223428045869));
#8143=CARTESIAN_POINT('Ctrl Pts',(2.33273462212481,-0.750532765933785,27.2181181810012));
#8144=CARTESIAN_POINT('Ctrl Pts',(2.30774035312361,-0.828217577710469,27.213876930133));
#8145=CARTESIAN_POINT('Ctrl Pts',(2.27883315349637,-0.904739907102235,27.2096356792647));
#8146=CARTESIAN_POINT('Ctrl Pts',(2.24614672573727,-0.979681140198043,27.2053944283964));
#8147=CARTESIAN_POINT('Ctrl Pts',(2.21364719981109,-1.05419385739942,27.2011774291094));
#8148=CARTESIAN_POINT('Ctrl Pts',(2.1774117357153,-1.12714308017459,27.1969604298225));
#8149=CARTESIAN_POINT('Ctrl Pts',(2.13762090932816,-1.19813484132757,27.1927434305355));
#8150=CARTESIAN_POINT('Ctrl Pts',(2.09784327447047,-1.26910306715864,27.1885278292761));
#8151=CARTESIAN_POINT('Ctrl Pts',(2.05451284518467,-1.33811471469471,27.1843122280166));
#8152=CARTESIAN_POINT('Ctrl Pts',(2.00785631222409,-1.40480008522988,27.1800966267572));
#8153=CARTESIAN_POINT('Ctrl Pts',(1.96120094346449,-1.47148379179286,27.1758811306879));
#8154=CARTESIAN_POINT('Ctrl Pts',(1.91121990353903,-1.53584095633322,27.1716656346186));
#8155=CARTESIAN_POINT('Ctrl Pts',(1.85818258433968,-1.59753176283187,27.1674501385493));
#8156=CARTESIAN_POINT('Ctrl Pts',(1.80458326409292,-1.65987626560309,27.1631899736837));
#8157=CARTESIAN_POINT('Ctrl Pts',(1.74786281182931,-1.71949718877495,27.1589298088181));
#8158=CARTESIAN_POINT('Ctrl Pts',(1.68833902407782,-1.77608040070711,27.1546696439526));
#8159=CARTESIAN_POINT('Ctrl Pts',(1.6293535801594,-1.83215186390235,27.1504480087836));
#8160=CARTESIAN_POINT('Ctrl Pts',(1.56761570131098,-1.88524008226808,27.1462263736146));
#8161=CARTESIAN_POINT('Ctrl Pts',(1.50346814737254,-1.93507978642644,27.1420047384457));
#8162=CARTESIAN_POINT('Ctrl Pts',(1.43844240795877,-1.98560180037837,27.1377253087318));
#8163=CARTESIAN_POINT('Ctrl Pts',(1.37094092201097,-2.03278539840022,27.1334458790179));
#8164=CARTESIAN_POINT('Ctrl Pts',(1.3013496034633,-2.07640060189885,27.129166449304));
#8165=CARTESIAN_POINT('Ctrl Pts',(1.23175828491566,-2.12001580539746,27.1248870195901));
#8166=CARTESIAN_POINT('Ctrl Pts',(1.1600775939914,-2.1600624322741,27.1206075898763));
#8167=CARTESIAN_POINT('Ctrl Pts',(1.08671585527949,-2.19636037568614,27.1163281601624));
#8168=CARTESIAN_POINT('Ctrl Pts',(1.01418945081432,-2.23224501216529,27.1120974582221));
#8169=CARTESIAN_POINT('Ctrl Pts',(0.939747313560539,-2.26460091096603,27.1078667562818));
#8170=CARTESIAN_POINT('Ctrl Pts',(0.863766980855441,-2.29321975675771,27.1036360543416));
#8171=CARTESIAN_POINT('Ctrl Pts',(0.787895810981903,-2.32179748514266,27.0994114307559));
#8172=CARTESIAN_POINT('Ctrl Pts',(0.710491266285224,-2.3466486613437,27.0951868071702));
#8173=CARTESIAN_POINT('Ctrl Pts',(0.631954089816945,-2.36761151339565,27.0909621835846));
#8174=CARTESIAN_POINT('Ctrl Pts',(0.553107806560379,-2.38865687108585,27.0867209327163));
#8175=CARTESIAN_POINT('Ctrl Pts',(0.473120382119022,-2.40578302118066,27.082479681848));
#8176=CARTESIAN_POINT('Ctrl Pts',(0.392416157402072,-2.41887573252736,27.0782384309797));
#8177=CARTESIAN_POINT('Ctrl Pts',(0.312173401513568,-2.43189357941453,27.0740214316927));
#8178=CARTESIAN_POINT('Ctrl Pts',(0.231222484143448,-2.44092391377583,27.0698044324058));
#8179=CARTESIAN_POINT('Ctrl Pts',(0.149992402095245,-2.44590525763238,27.0655874331188));
#8180=CARTESIAN_POINT('Ctrl Pts',(0.0687892495963295,-2.45088495006446,
27.0613718318594));
#8181=CARTESIAN_POINT('Ctrl Pts',(-0.0126924199730705,-2.45181828918591,
27.0571562305999));
#8182=CARTESIAN_POINT('Ctrl Pts',(-0.0940190465854,-2.44869570769403,27.0529406293405));
#8183=CARTESIAN_POINT('Ctrl Pts',(-0.175343643888364,-2.44557320411862,
27.0487251332712));
#8184=CARTESIAN_POINT('Ctrl Pts',(-0.256512741249791,-2.43839500007911,
27.0445096372019));
#8185=CARTESIAN_POINT('Ctrl Pts',(-0.337094783833534,-2.42720360841694,
27.0402941411326));
#8186=CARTESIAN_POINT('Ctrl Pts',(-0.418530700501074,-2.41589362905216,
27.036033976267));
#8187=CARTESIAN_POINT('Ctrl Pts',(-0.499366564979165,-2.40048495620401,
27.0317738114014));
#8188=CARTESIAN_POINT('Ctrl Pts',(-0.579166209922435,-2.38107470510358,
27.0275136465359));
#8189=CARTESIAN_POINT('Ctrl Pts',(-0.65824413253653,-2.36184000380219,27.0232920113669));
#8190=CARTESIAN_POINT('Ctrl Pts',(-0.736304070494887,-2.33867600803522,
27.0190703761979));
#8191=CARTESIAN_POINT('Ctrl Pts',(-0.812937422334597,-2.31172727573301,
27.0148487410289));
#8192=CARTESIAN_POINT('Ctrl Pts',(-0.890619891286033,-2.28440961299101,
27.0105693113151));
#8193=CARTESIAN_POINT('Ctrl Pts',(-0.96683596043162,-2.25320298979247,27.0062898816012));
#8194=CARTESIAN_POINT('Ctrl Pts',(-1.04118333516336,-2.21830735304604,27.0020104518873));
#8195=CARTESIAN_POINT('Ctrl Pts',(-1.11553070989507,-2.18341171629961,26.9977310221734));
#8196=CARTESIAN_POINT('Ctrl Pts',(-1.18800898794173,-2.14482735435103,26.9934515924595));
#8197=CARTESIAN_POINT('Ctrl Pts',(-1.25824567135078,-2.10280005719208,26.9891721627456));
#8198=CARTESIAN_POINT('Ctrl Pts',(-1.32768260398948,-2.06125130431579,26.9849414608054));
#8199=CARTESIAN_POINT('Ctrl Pts',(-1.39518992430469,-2.01618138430327,26.9807107588651));
#8200=CARTESIAN_POINT('Ctrl Pts',(-1.46038808642811,-1.96779493012327,26.9764800569249));
#8201=CARTESIAN_POINT('Ctrl Pts',(-1.52549257673238,-1.91947799396399,26.9722554333392));
#8202=CARTESIAN_POINT('Ctrl Pts',(-1.58829412754739,-1.86785426188774,26.9680308097535));
#8203=CARTESIAN_POINT('Ctrl Pts',(-1.64843976084093,-1.81317307637156,26.9638061861679));
#8204=CARTESIAN_POINT('Ctrl Pts',(-1.70882211544764,-1.75827667652754,26.9595649352996));
#8205=CARTESIAN_POINT('Ctrl Pts',(-1.76652719414015,-1.70029894822672,26.9553236844313));
#8206=CARTESIAN_POINT('Ctrl Pts',(-1.82122921302229,-1.63953481318153,26.951082433563));
#8207=CARTESIAN_POINT('Ctrl Pts',(-1.87561844435622,-1.57911812902039,26.946865434276));
#8208=CARTESIAN_POINT('Ctrl Pts',(-1.92703855155125,-1.5159471662467,26.9426484349891));
#8209=CARTESIAN_POINT('Ctrl Pts',(-1.9752055825826,-1.45034932224431,26.9384314357021));
#8210=CARTESIAN_POINT('Ctrl Pts',(-2.02335664518941,-1.3847732253623,26.9342158344427));
#8211=CARTESIAN_POINT('Ctrl Pts',(-2.06825649825091,-1.3167722195407,26.9300002331833));
#8212=CARTESIAN_POINT('Ctrl Pts',(-2.10966236345032,-1.24670564378333,26.9257846319239));
#8213=CARTESIAN_POINT('Ctrl Pts',(-2.15106719546648,-1.17664081636793,26.9215691358546));
#8214=CARTESIAN_POINT('Ctrl Pts',(-2.18897797729587,-1.10451092242129,26.9173536397853));
#8215=CARTESIAN_POINT('Ctrl Pts',(-2.22319680302907,-1.03070181187448,26.913138143716));
#8216=CARTESIAN_POINT('Ctrl Pts',(-2.25777822280366,-0.956110595480615,
26.9088779788504));
#8217=CARTESIAN_POINT('Ctrl Pts',(-2.28858875983367,-0.879804796272364,
26.9046178139848));
#8218=CARTESIAN_POINT('Ctrl Pts',(-2.31547391831242,-0.802203704563214,
26.9003576491192));
#8219=CARTESIAN_POINT('Ctrl Pts',(-2.34211592258636,-0.725304451073139,
26.8961360139502));
#8220=CARTESIAN_POINT('Ctrl Pts',(-2.36490319402609,-0.647133709268832,
26.8919143787813));
#8221=CARTESIAN_POINT('Ctrl Pts',(-2.38373604912657,-0.568113279280151,
26.8876927436124));
#8222=CARTESIAN_POINT('Ctrl Pts',(-2.40282672761708,-0.488011052875974,
26.8834133138985));
#8223=CARTESIAN_POINT('Ctrl Pts',(-2.41785380712046,-0.407036183878763,
26.8791338841845));
#8224=CARTESIAN_POINT('Ctrl Pts',(-2.42876758743783,-0.325635158131675,
26.8748544544706));
#8225=CARTESIAN_POINT('Ctrl Pts',(-2.43968136775519,-0.244234132384586,
26.8705750247567));
#8226=CARTESIAN_POINT('Ctrl Pts',(-2.44648187352098,-0.16240744421396,26.8662955950428));
#8227=CARTESIAN_POINT('Ctrl Pts',(-2.44917407971559,-0.080601347689007,
26.8620161653289));
#8228=CARTESIAN_POINT('Ctrl Pts',(-2.45005244916336,-0.0539109790342361,
26.86061994229));
#8229=CARTESIAN_POINT('Ctrl Pts',(-2.4504945386623,-0.0272061736956886,
26.859223719251));
#8230=CARTESIAN_POINT('Ctrl Pts',(-2.45049994971379,-0.000496440046205509,
26.857827496212));
#8231=CARTESIAN_POINT('',(-2.45049921122159,-0.00196616437574762,26.0578274962121));
#8232=CARTESIAN_POINT('Ctrl Pts',(-2.4544163928919,-0.000486308122271454,
26.8578269260125));
#8233=CARTESIAN_POINT('Ctrl Pts',(-2.45223809250971,0.784885029909544,26.8168380066458));
#8234=CARTESIAN_POINT('Ctrl Pts',(-1.61768872140475,2.38635253781045,26.7334637548067));
#8235=CARTESIAN_POINT('Ctrl Pts',(1.11139905977937,2.675821036374,26.6077041704954));
#8236=CARTESIAN_POINT('Ctrl Pts',(2.85144128369585,0.514304087493417,26.4805481730787));
#8237=CARTESIAN_POINT('Ctrl Pts',(1.97620912114127,-2.11892038507884,26.3533921756619));
#8238=CARTESIAN_POINT('Ctrl Pts',(-0.711555225186118,-2.80872128383892,
26.2262361782453));
#8239=CARTESIAN_POINT('Ctrl Pts',(-2.28839663859365,-1.34721059041725,26.1277149111577));
#8240=CARTESIAN_POINT('Ctrl Pts',(-2.45037331171153,-0.267128835091938,
26.0715789765424));
#8241=CARTESIAN_POINT('Ctrl Pts',(-2.44838624420166,-0.00198140266975247,
26.0578283743994));
#8242=CARTESIAN_POINT('',(-2.45049957242558,0.00144759872447857,25.2578274962121));
#8243=CARTESIAN_POINT('Ctrl Pts',(-2.45049921122159,-0.00196616437574762,
26.0578274962121));
#8244=CARTESIAN_POINT('Ctrl Pts',(-2.45056435292045,0.0792222060620601,
26.0536206531643));
#8245=CARTESIAN_POINT('Ctrl Pts',(-2.44659036857391,0.160464817053481,26.0494138101165));
#8246=CARTESIAN_POINT('Ctrl Pts',(-2.43858777176841,0.24132950375277,26.0452069670687));
#8247=CARTESIAN_POINT('Ctrl Pts',(-2.43058695487118,0.322176204824771,26.0410010596915));
#8248=CARTESIAN_POINT('Ctrl Pts',(-2.41855935099294,0.402644684117423,26.0367951523142));
#8249=CARTESIAN_POINT('Ctrl Pts',(-2.40256742063308,0.482306996955797,26.032589244937));
#8250=CARTESIAN_POINT('Ctrl Pts',(-2.38657409952559,0.561976237674043,26.0283829717906));
#8251=CARTESIAN_POINT('Ctrl Pts',(-2.36661586067349,0.640838715264166,26.0241766986442));
#8252=CARTESIAN_POINT('Ctrl Pts',(-2.3428061629636,0.718477231914684,26.0199704254978));
#8253=CARTESIAN_POINT('Ctrl Pts',(-2.31897018853183,0.796201431539173,26.0157595102484));
#8254=CARTESIAN_POINT('Ctrl Pts',(-2.29127440516051,0.872698525716211,26.0115485949989));
#8255=CARTESIAN_POINT('Ctrl Pts',(-2.25988184464622,0.947567569220482,26.0073376797495));
#8256=CARTESIAN_POINT('Ctrl Pts',(-2.22847154773062,1.02247891279138,26.003124385386));
#8257=CARTESIAN_POINT('Ctrl Pts',(-2.19336051763349,1.09575995335672,25.9989110910225));
#8258=CARTESIAN_POINT('Ctrl Pts',(-2.15475843919057,1.16703312666651,25.994697796659));
#8259=CARTESIAN_POINT('Ctrl Pts',(-2.11608554478923,1.23843705143533,25.9904767729583));
#8260=CARTESIAN_POINT('Ctrl Pts',(-2.07390905318347,1.30782535253546,25.9862557492577));
#8261=CARTESIAN_POINT('Ctrl Pts',(-2.02848263731192,1.3748485153369,25.982034725557));
#8262=CARTESIAN_POINT('Ctrl Pts',(-1.9922129450324,1.42836164076776,25.9786645448419));
#8263=CARTESIAN_POINT('Ctrl Pts',(-1.95387236655002,1.4803675466132,25.9752943641268));
#8264=CARTESIAN_POINT('Ctrl Pts',(-1.91360765035828,1.5307044164339,25.9719241834117));
#8265=CARTESIAN_POINT('Ctrl Pts',(-1.86306198906733,1.59389399314142,25.9676934814714));
#8266=CARTESIAN_POINT('Ctrl Pts',(-1.80928801626885,1.65469609701548,25.9634627795312));
#8267=CARTESIAN_POINT('Ctrl Pts',(-1.75253974839819,1.71276229532426,25.9592320775909));
#8268=CARTESIAN_POINT('Ctrl Pts',(-1.69587301217369,1.77074506848346,25.9550074540053));
#8269=CARTESIAN_POINT('Ctrl Pts',(-1.63624079006716,1.82599941297201,25.9507828304196));
#8270=CARTESIAN_POINT('Ctrl Pts',(-1.57393781039758,1.87820925857607,25.9465582068339));
#8271=CARTESIAN_POINT('Ctrl Pts',(-1.51138961852615,1.93062459180315,25.9423169559657));
#8272=CARTESIAN_POINT('Ctrl Pts',(-1.44614989728376,1.97997103907197,25.9380757050974));
#8273=CARTESIAN_POINT('Ctrl Pts',(-1.37855486404961,2.02596563070679,25.9338344542291));
#8274=CARTESIAN_POINT('Ctrl Pts',(-1.31134634095089,2.0716972240858,25.9296174549422));
#8275=CARTESIAN_POINT('Ctrl Pts',(-1.24180975659438,2.11411492555232,25.9254004556552));
#8276=CARTESIAN_POINT('Ctrl Pts',(-1.17030785705621,2.1529815999475,25.9211834563683));
#8277=CARTESIAN_POINT('Ctrl Pts',(-1.09882966196187,2.19183538918989,25.9169678551089));
#8278=CARTESIAN_POINT('Ctrl Pts',(-1.02538785381665,2.22714026723881,25.9127522538495));
#8279=CARTESIAN_POINT('Ctrl Pts',(-0.950371267120706,2.25870420919415,25.90853665259));
#8280=CARTESIAN_POINT('Ctrl Pts',(-0.875356552282358,2.29026736354762,25.9043211565208));
#8281=CARTESIAN_POINT('Ctrl Pts',(-0.798767566102965,2.3180895880393,25.9001056604515));
#8282=CARTESIAN_POINT('Ctrl Pts',(-0.721013351052304,2.34202689941946,25.8958901643822));
#8283=CARTESIAN_POINT('Ctrl Pts',(-0.642435226516857,2.36621785850057,25.8916299995166));
#8284=CARTESIAN_POINT('Ctrl Pts',(-0.562667490052483,2.38644092464468,25.887369834651));
#8285=CARTESIAN_POINT('Ctrl Pts',(-0.482146455556506,2.40259964317701,25.8831096697854));
#8286=CARTESIAN_POINT('Ctrl Pts',(-0.402353667767159,2.41861221935501,25.8788880346165));
#8287=CARTESIAN_POINT('Ctrl Pts',(-0.32182162725187,2.4306336612126,25.8746663994475));
#8288=CARTESIAN_POINT('Ctrl Pts',(-0.240981732254135,2.43862216317325,25.8704447642786));
#8289=CARTESIAN_POINT('Ctrl Pts',(-0.159035132209623,2.44672002840604,25.8661653345647));
#8290=CARTESIAN_POINT('Ctrl Pts',(-0.0767726788353745,2.4506736713357,25.8618859048508));
#8291=CARTESIAN_POINT('Ctrl Pts',(0.00535652038182216,2.45049414561419,
25.8576064751368));
#8292=CARTESIAN_POINT('Ctrl Pts',(0.0874857195990188,2.45031461989267,25.8533270454229));
#8293=CARTESIAN_POINT('Ctrl Pts',(0.169481178188457,2.4460020166882,25.849047615709));
#8294=CARTESIAN_POINT('Ctrl Pts',(0.250901402272095,2.43762153262927,25.8447681859951));
#8295=CARTESIAN_POINT('Ctrl Pts',(0.331394534075678,2.42933647304457,25.8405374840548));
#8296=CARTESIAN_POINT('Ctrl Pts',(0.411628226227733,2.4170445801981,25.8363067821146));
#8297=CARTESIAN_POINT('Ctrl Pts',(0.491172003780412,2.40077077471014,25.8320760801743));
#8298=CARTESIAN_POINT('Ctrl Pts',(0.570601498811814,2.38452035020281,25.8278514565886));
#8299=CARTESIAN_POINT('Ctrl Pts',(0.649342596099335,2.36429946752621,25.823626833003));
#8300=CARTESIAN_POINT('Ctrl Pts',(0.726969987829524,2.34018479757372,25.8194022094173));
#8301=CARTESIAN_POINT('Ctrl Pts',(0.804902905615379,2.31597521705126,25.815160958549));
#8302=CARTESIAN_POINT('Ctrl Pts',(0.881712860331046,2.28784118174851,25.8109197076807));
#8303=CARTESIAN_POINT('Ctrl Pts',(0.956979911020769,2.25591216582177,25.8066784568124));
#8304=CARTESIAN_POINT('Ctrl Pts',(1.03181658278257,2.22416572082771,25.8024614575254));
#8305=CARTESIAN_POINT('Ctrl Pts',(1.10512751493269,2.18866776047779,25.7982444582385));
#8306=CARTESIAN_POINT('Ctrl Pts',(1.17651693927947,2.14959487848024,25.7940274589515));
#8307=CARTESIAN_POINT('Ctrl Pts',(1.24788269647031,2.11053494999785,25.7898118576921));
#8308=CARTESIAN_POINT('Ctrl Pts',(1.31732780324429,2.06790267650847,25.7855962564327));
#8309=CARTESIAN_POINT('Ctrl Pts',(1.38448029361734,2.02192100898756,25.7813806551732));
#8310=CARTESIAN_POINT('Ctrl Pts',(1.45163110836222,1.97594048882807,25.7771651591039));
#8311=CARTESIAN_POINT('Ctrl Pts',(1.51648903733628,1.92661100445138,25.7729496630346));
#8312=CARTESIAN_POINT('Ctrl Pts',(1.57871156510025,1.87419850715411,25.7687341669653));
#8313=CARTESIAN_POINT('Ctrl Pts',(1.64159342343222,1.82123062962955,25.7644740020997));
#8314=CARTESIAN_POINT('Ctrl Pts',(1.70178331591786,1.76511431268473,25.7602138372342));
#8315=CARTESIAN_POINT('Ctrl Pts',(1.75896392205096,1.70616416880765,25.7559536723686));
#8316=CARTESIAN_POINT('Ctrl Pts',(1.81562737650644,1.64774718062555,25.7517320371996));
#8317=CARTESIAN_POINT('Ctrl Pts',(1.86933549493996,1.58654781275082,25.7475104020306));
#8318=CARTESIAN_POINT('Ctrl Pts',(1.919819564879,1.52290613246773,25.7432887668617));
#8319=CARTESIAN_POINT('Ctrl Pts',(1.97099476603426,1.45839319216242,25.7390093371478));
#8320=CARTESIAN_POINT('Ctrl Pts',(2.01885668784557,1.39137096474473,25.7347299074339));
#8321=CARTESIAN_POINT('Ctrl Pts',(2.06317147164031,1.32222302529094,25.73045047772));
#8322=CARTESIAN_POINT('Ctrl Pts',(2.10748625543506,1.25307508583716,25.7261710480061));
#8323=CARTESIAN_POINT('Ctrl Pts',(2.14825371448258,1.18180189271072,25.7218916182921));
#8324=CARTESIAN_POINT('Ctrl Pts',(2.18528963332306,1.10880993343799,25.7176121885782));
#8325=CARTESIAN_POINT('Ctrl Pts',(2.2219038422652,1.03664909791454,25.713381486638));
#8326=CARTESIAN_POINT('Ctrl Pts',(2.25500881229822,0.962537041235193,25.7091507846977));
#8327=CARTESIAN_POINT('Ctrl Pts',(2.28439243138472,0.886849180769873,25.7049200827574));
#8328=CARTESIAN_POINT('Ctrl Pts',(2.31373383429575,0.811270062933873,25.7006954591718));
#8329=CARTESIAN_POINT('Ctrl Pts',(2.33936433793749,0.734120067591182,25.6964708355861));
#8330=CARTESIAN_POINT('Ctrl Pts',(2.36111813725174,0.655798286015512,25.6922462120004));
#8331=CARTESIAN_POINT('Ctrl Pts',(2.38295755521612,0.577168245403439,25.6880049611321));
#8332=CARTESIAN_POINT('Ctrl Pts',(2.40088947279089,0.497357598131797,25.6837637102638));
#8333=CARTESIAN_POINT('Ctrl Pts',(2.41479538533874,0.416789511560387,25.6795224593955));
#8334=CARTESIAN_POINT('Ctrl Pts',(2.42862178352172,0.336682115375852,25.6753054601086));
#8335=CARTESIAN_POINT('Ctrl Pts',(2.43846801344614,0.255826381392194,25.6710884608216));
#8336=CARTESIAN_POINT('Ctrl Pts',(2.4442682740133,0.174650664619582,25.6668714615346));
#8337=CARTESIAN_POINT('Ctrl Pts',(2.45006661166717,0.093501859373048,25.6626558602752));
#8338=CARTESIAN_POINT('Ctrl Pts',(2.45182161049298,0.0120337455071861,25.6584402590158));
#8339=CARTESIAN_POINT('Ctrl Pts',(2.44951933141037,-0.0693202354792845,
25.6542246577563));
#8340=CARTESIAN_POINT('Ctrl Pts',(2.44721710977556,-0.150672186473967,25.650009161687));
#8341=CARTESIAN_POINT('Ctrl Pts',(2.44085782576188,-0.231909545407921,25.6457936656177));
#8342=CARTESIAN_POINT('Ctrl Pts',(2.43047963800632,-0.312600350666281,25.6415781695484));
#8343=CARTESIAN_POINT('Ctrl Pts',(2.41999147952684,-0.394146182493485,25.6373180046828));
#8344=CARTESIAN_POINT('Ctrl Pts',(2.40539878471959,-0.47513332618364,25.6330578398173));
#8345=CARTESIAN_POINT('Ctrl Pts',(2.3867942653195,-0.555124657205891,25.6287976749517));
#8346=CARTESIAN_POINT('Ctrl Pts',(2.36835800853611,-0.634392532255847,25.6245760397827));
#8347=CARTESIAN_POINT('Ctrl Pts',(2.3459823911617,-0.712682099639198,25.6203544046137));
#8348=CARTESIAN_POINT('Ctrl Pts',(2.3198078432079,-0.789583320866838,25.6161327694448));
#8349=CARTESIAN_POINT('Ctrl Pts',(2.29327496346407,-0.867537326360603,25.6118533397309));
#8350=CARTESIAN_POINT('Ctrl Pts',(2.26283853301571,-0.944064225088884,25.607573910017));
#8351=CARTESIAN_POINT('Ctrl Pts',(2.2286944316381,-1.01875972652305,25.6032944803032));
#8352=CARTESIAN_POINT('Ctrl Pts',(2.19455033026049,-1.09345522795721,25.5990150505893));
#8353=CARTESIAN_POINT('Ctrl Pts',(2.15669884222795,-1.16631892693866,25.5947356208754));
#8354=CARTESIAN_POINT('Ctrl Pts',(2.11538198855404,-1.23697586577151,25.5904561911616));
#8355=CARTESIAN_POINT('Ctrl Pts',(2.07453558968995,-1.30682826859142,25.5862254892213));
#8356=CARTESIAN_POINT('Ctrl Pts',(2.03014874344254,-1.37478666664726,25.581994787281));
#8357=CARTESIAN_POINT('Ctrl Pts',(1.98242224482002,-1.44046946973643,25.5777640853408));
#8358=CARTESIAN_POINT('Ctrl Pts',(1.93476431604378,-1.50605790471059,25.5735394617551));
#8359=CARTESIAN_POINT('Ctrl Pts',(1.88377653536067,-1.56937686489839,25.5693148381694));
#8360=CARTESIAN_POINT('Ctrl Pts',(1.82970467293873,-1.63007087570639,25.5650902145838));
#8361=CARTESIAN_POINT('Ctrl Pts',(1.7754199943641,-1.69100376613296,25.5608489637155));
#8362=CARTESIAN_POINT('Ctrl Pts',(1.71802714485775,-1.74929059064225,25.5566077128472));
#8363=CARTESIAN_POINT('Ctrl Pts',(1.65781774574641,-1.80460260774728,25.5523664619789));
#8364=CARTESIAN_POINT('Ctrl Pts',(1.5979526255247,-1.85959834931871,25.5481494626919));
#8365=CARTESIAN_POINT('Ctrl Pts',(1.53530342442255,-1.91165289343347,25.543932463405));
#8366=CARTESIAN_POINT('Ctrl Pts',(1.47019465964294,-1.96047900084581,25.539715464118));
#8367=CARTESIAN_POINT('Ctrl Pts',(1.40510747984327,-2.00928892133535,25.5354998628586));
#8368=CARTESIAN_POINT('Ctrl Pts',(1.33756272737899,-2.05487225175624,25.5312842615991));
#8369=CARTESIAN_POINT('Ctrl Pts',(1.26791727466772,-2.09698260235968,25.5270686603397));
#8370=CARTESIAN_POINT('Ctrl Pts',(1.19827355979029,-2.13909190220116,25.5228531642704));
#8371=CARTESIAN_POINT('Ctrl Pts',(1.12652964741628,-2.17772815482706,25.5186376682011));
#8372=CARTESIAN_POINT('Ctrl Pts',(1.05306937206114,-2.21268957326299,25.5144221721318));
#8373=CARTESIAN_POINT('Ctrl Pts',(0.97883068723278,-2.24802145449907,25.5101620072662));
#8374=CARTESIAN_POINT('Ctrl Pts',(0.902839479066593,-2.27959993556317,25.5059018424006));
#8375=CARTESIAN_POINT('Ctrl Pts',(0.82551345853199,-2.30726630014451,25.501641677535));
#8376=CARTESIAN_POINT('Ctrl Pts',(0.74888678842311,-2.33468244515275,25.497420042366));
#8377=CARTESIAN_POINT('Ctrl Pts',(0.670949821353316,-2.35825687574802,25.4931984071971));
#8378=CARTESIAN_POINT('Ctrl Pts',(0.592123330738969,-2.37788565982357,25.4889767720281));
#8379=CARTESIAN_POINT('Ctrl Pts',(0.512217698755994,-2.39778316362452,25.4846973423142));
#8380=CARTESIAN_POINT('Ctrl Pts',(0.431398488927583,-2.41362607529511,25.4804179126003));
#8381=CARTESIAN_POINT('Ctrl Pts',(0.35011166318798,-2.42536019454838,25.4761384828864));
#8382=CARTESIAN_POINT('Ctrl Pts',(0.2688248374484,-2.43709431380164,25.4718590531725));
#8383=CARTESIAN_POINT('Ctrl Pts',(0.187070890347262,-2.44471966028572,25.4675796234586));
#8384=CARTESIAN_POINT('Ctrl Pts',(0.105296103432033,-2.44823670844999,25.4633001937447));
#8385=CARTESIAN_POINT('Ctrl Pts',(0.0244524460301832,-2.45171370970654,
25.4590694918045));
#8386=CARTESIAN_POINT('Ctrl Pts',(-0.0567156527727147,-2.4511886165742,
25.4548387898642));
#8387=CARTESIAN_POINT('Ctrl Pts',(-0.137778655346964,-2.44662365151054,
25.450608087924));
#8388=CARTESIAN_POINT('Ctrl Pts',(-0.218725192691977,-2.44206524504558,
25.4463834643383));
#8389=CARTESIAN_POINT('Ctrl Pts',(-0.299566473306361,-2.43347852000476,
25.4421588407526));
#8390=CARTESIAN_POINT('Ctrl Pts',(-0.379870566370954,-2.42087765134982,
25.4379342171669));
#8391=CARTESIAN_POINT('Ctrl Pts',(-0.460490720457817,-2.40822718816891,
25.4336929662986));
#8392=CARTESIAN_POINT('Ctrl Pts',(-0.540568975281544,-2.39153089546019,
25.4294517154303));
#8393=CARTESIAN_POINT('Ctrl Pts',(-0.619671051722867,-2.37085597151254,
25.4252104645621));
#8394=CARTESIAN_POINT('Ctrl Pts',(-0.698320820460437,-2.35029926731078,
25.4209934652751));
#8395=CARTESIAN_POINT('Ctrl Pts',(-0.776005089679771,-2.32580942701831,
25.4167764659882));
#8396=CARTESIAN_POINT('Ctrl Pts',(-0.852306663366028,-2.29750377618446,
25.4125594667012));
#8397=CARTESIAN_POINT('Ctrl Pts',(-0.928582941411364,-2.26920750929311,
25.4083438654418));
#8398=CARTESIAN_POINT('Ctrl Pts',(-1.00347699853692,-2.23709810560883,25.4041282641824));
#8399=CARTESIAN_POINT('Ctrl Pts',(-1.07658846575323,-2.20134220997261,25.399912662923));
#8400=CARTESIAN_POINT('Ctrl Pts',(-1.14969810864951,-2.16558720653839,25.3956971668537));
#8401=CARTESIAN_POINT('Ctrl Pts',(-1.22102483277604,-2.12618609735331,25.3914816707844));
#8402=CARTESIAN_POINT('Ctrl Pts',(-1.2901911716623,-2.08335234431544,25.3872661747151));
#8403=CARTESIAN_POINT('Ctrl Pts',(-1.36009042004543,-2.04006471060537,25.3830060098496));
#8404=CARTESIAN_POINT('Ctrl Pts',(-1.42778280589333,-1.99327149439715,25.378745844984));
#8405=CARTESIAN_POINT('Ctrl Pts',(-1.49290873360644,-1.94323795843988,25.3744856801184));
#8406=CARTESIAN_POINT('Ctrl Pts',(-1.55744565072549,-1.89365693477338,25.3702640449494));
#8407=CARTESIAN_POINT('Ctrl Pts',(-1.61946202784756,-1.84089431938574,25.3660424097805));
#8408=CARTESIAN_POINT('Ctrl Pts',(-1.67864267155972,-1.78524761061844,25.3618207746115));
#8409=CARTESIAN_POINT('Ctrl Pts',(-1.73863350332392,-1.72883909366943,25.3575413448976));
#8410=CARTESIAN_POINT('Ctrl Pts',(-1.79571002811989,-1.66946727506207,25.3532619151837));
#8411=CARTESIAN_POINT('Ctrl Pts',(-1.84958522757434,-1.60747775597014,25.3489824854698));
#8412=CARTESIAN_POINT('Ctrl Pts',(-1.90346042702879,-1.5454882368782,25.3447030557559));
#8413=CARTESIAN_POINT('Ctrl Pts',(-1.95413404990601,-1.48088144373573,25.340423626042));
#8414=CARTESIAN_POINT('Ctrl Pts',(-2.00136487298623,-1.41403284798367,25.3361441963281));
#8415=CARTESIAN_POINT('Ctrl Pts',(-2.04854588977562,-1.3472547460402,25.3318692793986));
#8416=CARTESIAN_POINT('Ctrl Pts',(-2.09246741364592,-1.27799073561874,25.3275943624691));
#8417=CARTESIAN_POINT('Ctrl Pts',(-2.13286079451398,-1.20658819869298,25.3233194455395));
#8418=CARTESIAN_POINT('Ctrl Pts',(-2.17319329701699,-1.13529327518346,25.3190509714961));
#8419=CARTESIAN_POINT('Ctrl Pts',(-2.21000799855808,-1.06186661759494,25.3147824974527));
#8420=CARTESIAN_POINT('Ctrl Pts',(-2.24307855145268,-0.986685797005798,
25.3105140234094));
#8421=CARTESIAN_POINT('Ctrl Pts',(-2.27709485655374,-0.909354954093692,
25.3061234794762));
#8422=CARTESIAN_POINT('Ctrl Pts',(-2.30714929978556,-0.830168471242618,
25.3017329355431));
#8423=CARTESIAN_POINT('Ctrl Pts',(-2.33304538151715,-0.749566206403059,
25.29734239161));
#8424=CARTESIAN_POINT('Ctrl Pts',(-2.35816409428234,-0.671383523798304,
25.2930836464809));
#8425=CARTESIAN_POINT('Ctrl Pts',(-2.37937041262085,-0.591869318873139,
25.2888249013517));
#8426=CARTESIAN_POINT('Ctrl Pts',(-2.39653373568158,-0.511445308649984,
25.2845661562226));
#8427=CARTESIAN_POINT('Ctrl Pts',(-2.41449380944562,-0.427287878827297,
25.2801097128875));
#8428=CARTESIAN_POINT('Ctrl Pts',(-2.42802622608005,-0.342134607467247,
25.2756532695524));
#8429=CARTESIAN_POINT('Ctrl Pts',(-2.43704040685765,-0.256484512871788,
25.2711968262173));
#8430=CARTESIAN_POINT('Ctrl Pts',(-2.44605458763526,-0.17083441827633,25.2667403828823));
#8431=CARTESIAN_POINT('Ctrl Pts',(-2.45055045587722,-0.0846880646955054,
25.2622839395472));
#8432=CARTESIAN_POINT('Ctrl Pts',(-2.45049957242558,0.00144759872447857,
25.2578274962121));
#8433=CARTESIAN_POINT('',(-2.45049965096235,0.00130791185359291,24.4578274962121));
#8434=CARTESIAN_POINT('Ctrl Pts',(-2.44733420835662,0.00146391743851001,
25.2578265539622));
#8435=CARTESIAN_POINT('Ctrl Pts',(-2.44901787875617,0.315713360581297,25.2415471022785));
#8436=CARTESIAN_POINT('Ctrl Pts',(-2.24674587549421,1.44605613207129,25.1828823181227));
#8437=CARTESIAN_POINT('Ctrl Pts',(-0.543033478857258,2.84610975361437,25.0818322014945));
#8438=CARTESIAN_POINT('Ctrl Pts',(2.09888342822537,1.99747701951716,24.9546762040779));
#8439=CARTESIAN_POINT('Ctrl Pts',(2.81575418359161,-0.683194310844983,24.8275202066611));
#8440=CARTESIAN_POINT('Ctrl Pts',(0.950081915167995,-2.73725600615837,24.7003642092443));
#8441=CARTESIAN_POINT('Ctrl Pts',(-1.70248630229997,-2.29486360804804,24.5771336791462));
#8442=CARTESIAN_POINT('Ctrl Pts',(-2.44889894900063,-0.73622003660141,24.49628848152));
#8443=CARTESIAN_POINT('Ctrl Pts',(-2.45367044800944,0.00128812415959639,
24.4578286163662));
#8444=CARTESIAN_POINT('',(-2.45049903536358,-0.00217432338460381,23.6578274961682));
#8445=CARTESIAN_POINT('Ctrl Pts',(-2.45049965096235,0.00130791185359291,
24.4578274962121));
#8446=CARTESIAN_POINT('Ctrl Pts',(-2.45045953015351,0.0764781366572466,
24.4539024022783));
#8447=CARTESIAN_POINT('Ctrl Pts',(-2.44696089914348,0.151553924908564,24.4499773083446));
#8448=CARTESIAN_POINT('Ctrl Pts',(-2.44002780973264,0.226306291851005,24.4460522144109));
#8449=CARTESIAN_POINT('Ctrl Pts',(-2.43255490964,0.306878881752235,24.4418215124709));
#8450=CARTESIAN_POINT('Ctrl Pts',(-2.4210727636996,0.387232452363853,24.4375908105308));
#8451=CARTESIAN_POINT('Ctrl Pts',(-2.405601950112,0.466936299314313,24.4333601085908));
#8452=CARTESIAN_POINT('Ctrl Pts',(-2.39015336382661,0.546525633767834,24.4291354850053));
#8453=CARTESIAN_POINT('Ctrl Pts',(-2.37072757908059,0.625466645825196,24.4249108614199));
#8454=CARTESIAN_POINT('Ctrl Pts',(-2.34739697382438,0.70333327610751,24.4206862378344));
#8455=CARTESIAN_POINT('Ctrl Pts',(-2.32397454392048,0.78150637404527,24.4164449869661));
#8456=CARTESIAN_POINT('Ctrl Pts',(-2.29661653420305,0.858596142434194,24.4122037360978));
#8457=CARTESIAN_POINT('Ctrl Pts',(-2.26544817732281,0.934181355982198,24.4079624852294));
#8458=CARTESIAN_POINT('Ctrl Pts',(-2.23445804190903,1.0093343713347,24.4037454859427));
#8459=CARTESIAN_POINT('Ctrl Pts',(-2.1997011954864,1.08299955705959,24.3995284866559));
#8460=CARTESIAN_POINT('Ctrl Pts',(-2.16135023163334,1.15477938421956,24.3953114873691));
#8461=CARTESIAN_POINT('Ctrl Pts',(-2.12301198196381,1.22653541479649,24.3910958861099));
#8462=CARTESIAN_POINT('Ctrl Pts',(-2.0810822000198,1.29640691816708,24.3868802848506));
#8463=CARTESIAN_POINT('Ctrl Pts',(-2.03578007432459,1.36401969889843,24.3826646835914));
#8464=CARTESIAN_POINT('Ctrl Pts',(-1.99047907903441,1.43163079251628,24.3784491875222));
#8465=CARTESIAN_POINT('Ctrl Pts',(-1.94180616706901,1.49698288980419,24.3742336914531));
#8466=CARTESIAN_POINT('Ctrl Pts',(-1.8900238220821,1.55973081073696,24.370018195384));
#8467=CARTESIAN_POINT('Ctrl Pts',(-1.837692774166,1.62314362948432,24.3657580305182));
#8468=CARTESIAN_POINT('Ctrl Pts',(-1.78218629962538,1.6838963699139,24.3614978656523));
#8469=CARTESIAN_POINT('Ctrl Pts',(-1.72381579491089,1.74166855492534,24.3572377007865));
#8470=CARTESIAN_POINT('Ctrl Pts',(-1.66597320353632,1.79891823790784,24.3530160656177));
#8471=CARTESIAN_POINT('Ctrl Pts',(-1.60531857067758,1.85324079423695,24.3487944304489));
#8472=CARTESIAN_POINT('Ctrl Pts',(-1.54218923647797,1.9043640956738,24.3445727952801));
#8473=CARTESIAN_POINT('Ctrl Pts',(-1.47819565630826,1.95618727946813,24.3402933655658));
#8474=CARTESIAN_POINT('Ctrl Pts',(-1.41165950364437,2.00472265746796,24.3360139358514));
#8475=CARTESIAN_POINT('Ctrl Pts',(-1.34296197569482,2.04973251470475,24.3317345061371));
#8476=CARTESIAN_POINT('Ctrl Pts',(-1.27426444774527,2.09474237194155,24.3274550764227));
#8477=CARTESIAN_POINT('Ctrl Pts',(-1.20340600096711,2.13622651707175,24.3231756467084));
#8478=CARTESIAN_POINT('Ctrl Pts',(-1.13079124448403,2.17399664475322,24.3188962169941));
#8479=CARTESIAN_POINT('Ctrl Pts',(-1.05900331673324,2.21133670245578,24.3146655150538));
#8480=CARTESIAN_POINT('Ctrl Pts',(-0.985228877900467,2.24518737691167,24.3104348131135));
#8481=CARTESIAN_POINT('Ctrl Pts',(-0.909841187207912,2.27533278094878,24.3062041111732));
#8482=CARTESIAN_POINT('Ctrl Pts',(-0.834561807883372,2.30543487433503,24.3019794875874));
#8483=CARTESIAN_POINT('Ctrl Pts',(-0.757674208128448,2.33184209876887,24.2977548640017));
#8484=CARTESIAN_POINT('Ctrl Pts',(-0.679575786851029,2.35438463296162,24.293530240416));
#8485=CARTESIAN_POINT('Ctrl Pts',(-0.601169985639642,2.37701589010879,24.2892889895477));
#8486=CARTESIAN_POINT('Ctrl Pts',(-0.521544232362832,2.39575175146896,24.2850477386795));
#8487=CARTESIAN_POINT('Ctrl Pts',(-0.441120477794435,2.41046945097224,24.2808064878112));
#8488=CARTESIAN_POINT('Ctrl Pts',(-0.361156588318291,2.42510299429211,24.2765894885242));
#8489=CARTESIAN_POINT('Ctrl Pts',(-0.280404260832229,2.4357641184079,24.2723724892372));
#8490=CARTESIAN_POINT('Ctrl Pts',(-0.199291164988927,2.44238270579313,24.2681554899502));
#8491=CARTESIAN_POINT('Ctrl Pts',(-0.118204959911378,2.44899909897185,24.2639398886908));
#8492=CARTESIAN_POINT('Ctrl Pts',(-0.0367586871396675,2.45157557901672,
24.2597242874313));
#8493=CARTESIAN_POINT('Ctrl Pts',(0.0446143744377594,2.4500938364874,24.2555086861719));
#8494=CARTESIAN_POINT('Ctrl Pts',(0.125985405547148,2.44861213093137,24.2512931901025));
#8495=CARTESIAN_POINT('Ctrl Pts',(0.207282764130744,2.44307241368911,24.2470776940332));
#8496=CARTESIAN_POINT('Ctrl Pts',(0.288074125725909,2.43350848531236,24.2428621979639));
#8497=CARTESIAN_POINT('Ctrl Pts',(0.369721579417327,2.42384321437459,24.2386020330984));
#8498=CARTESIAN_POINT('Ctrl Pts',(0.450851765843265,2.41006798170026,24.2343418682328));
#8499=CARTESIAN_POINT('Ctrl Pts',(0.531026647743397,2.39227108609923,24.2300817033673));
#8500=CARTESIAN_POINT('Ctrl Pts',(0.610476413605104,2.37463514881993,24.2258600681983));
#8501=CARTESIAN_POINT('Ctrl Pts',(0.688987648284235,2.35305018546115,24.2216384330294));
#8502=CARTESIAN_POINT('Ctrl Pts',(0.766148917966809,2.32765248383393,24.2174167978604));
#8503=CARTESIAN_POINT('Ctrl Pts',(0.844366531999536,2.30190708550952,24.2131373681466));
#8504=CARTESIAN_POINT('Ctrl Pts',(0.921196477445402,2.2722439432278,24.2088579384328));
#8505=CARTESIAN_POINT('Ctrl Pts',(0.996232508971911,2.23885484970945,24.2045785087189));
#8506=CARTESIAN_POINT('Ctrl Pts',(1.07126854049844,2.2054657561911,24.2002990790051));
#8507=CARTESIAN_POINT('Ctrl Pts',(1.14451025010084,2.16835099161015,24.1960196492913));
#8508=CARTESIAN_POINT('Ctrl Pts',(1.21558025847346,2.12774878338811,24.1917402195775));
#8509=CARTESIAN_POINT('Ctrl Pts',(1.28584102741354,2.08760889265687,24.1875095176372));
#8510=CARTESIAN_POINT('Ctrl Pts',(1.35424359177118,2.04390963436234,24.183278815697));
#8511=CARTESIAN_POINT('Ctrl Pts',(1.4204043558176,1.99684794513112,24.1790481137567));
#8512=CARTESIAN_POINT('Ctrl Pts',(1.48647006505069,1.94985387059797,24.174823490171));
#8513=CARTESIAN_POINT('Ctrl Pts',(1.55029999500818,1.89950722681738,24.1705988665853));
#8514=CARTESIAN_POINT('Ctrl Pts',(1.61153621068755,1.84605018665333,24.1663742429996));
#8515=CARTESIAN_POINT('Ctrl Pts',(1.67301343999609,1.79238275015581,24.1621329921313));
#8516=CARTESIAN_POINT('Ctrl Pts',(1.73187608249187,1.73558061635585,24.157891741263));
#8517=CARTESIAN_POINT('Ctrl Pts',(1.78779247253049,1.67593207653632,24.1536504903947));
#8518=CARTESIAN_POINT('Ctrl Pts',(1.84338913121596,1.61662460859814,24.1494334911077));
#8519=CARTESIAN_POINT('Ctrl Pts',(1.89607281824978,1.55450354065553,24.1452164918207));
#8520=CARTESIAN_POINT('Ctrl Pts',(1.94555303637773,1.48989047672687,24.1409994925337));
#8521=CARTESIAN_POINT('Ctrl Pts',(1.99501685073089,1.42529883344243,24.1367838912743));
#8522=CARTESIAN_POINT('Ctrl Pts',(2.04127902263956,1.35821720370604,24.1325682900148));
#8523=CARTESIAN_POINT('Ctrl Pts',(2.08408957598101,1.2889999570548,24.1283526887553));
#8524=CARTESIAN_POINT('Ctrl Pts',(2.12689906108861,1.21978443755261,24.124137192686));
#8525=CARTESIAN_POINT('Ctrl Pts',(2.16625685516426,1.14843380318076,24.1199216966167));
#8526=CARTESIAN_POINT('Ctrl Pts',(2.20195731069058,1.07532983400272,24.1157062005473));
#8527=CARTESIAN_POINT('Ctrl Pts',(2.238036060099,1.00145123089103,24.1114460356818));
#8528=CARTESIAN_POINT('Ctrl Pts',(2.27037927363274,0.925782342151553,24.1071858708162));
#8529=CARTESIAN_POINT('Ctrl Pts',(2.29882403061856,0.848739256927979,24.1029257059506));
#8530=CARTESIAN_POINT('Ctrl Pts',(2.32701152811091,0.772392963211155,24.0987040707816));
#8531=CARTESIAN_POINT('Ctrl Pts',(2.35137072031782,0.694697697145301,24.0944824356126));
#8532=CARTESIAN_POINT('Ctrl Pts',(2.37179343710082,0.616073162640177,24.0902608004436));
#8533=CARTESIAN_POINT('Ctrl Pts',(2.3924957426151,0.536372251564608,24.0859813707298));
#8534=CARTESIAN_POINT('Ctrl Pts',(2.4091528752121,0.455716920303052,24.081701941016));
#8535=CARTESIAN_POINT('Ctrl Pts',(2.42170614002903,0.37455256152604,24.0774225113021));
#8536=CARTESIAN_POINT('Ctrl Pts',(2.43425940484595,0.293388202749006,24.0731430815883));
#8537=CARTESIAN_POINT('Ctrl Pts',(2.4427088165426,0.211715311179143,24.0688636518745));
#8538=CARTESIAN_POINT('Ctrl Pts',(2.44705034898911,0.129980150454861,24.0645842221606));
#8539=CARTESIAN_POINT('Ctrl Pts',(2.45134244652859,0.0491756680387825,24.0603535202204));
#8540=CARTESIAN_POINT('Ctrl Pts',(2.45163592503804,-0.0319935986599718,
24.0561228182801));
#8541=CARTESIAN_POINT('Ctrl Pts',(2.44788867719605,-0.113098514823987,24.0518921163399));
#8542=CARTESIAN_POINT('Ctrl Pts',(2.44414681311811,-0.194086905540078,24.0476674927542));
#8543=CARTESIAN_POINT('Ctrl Pts',(2.43637577383816,-0.275010668717048,24.0434428691686));
#8544=CARTESIAN_POINT('Ctrl Pts',(2.42458537776282,-0.355437752551335,24.0392182455829));
#8545=CARTESIAN_POINT('Ctrl Pts',(2.41274857702114,-0.436181381475851,24.0349769947146));
#8546=CARTESIAN_POINT('Ctrl Pts',(2.396860687666,-0.51642393912257,24.0307357438463));
#8547=CARTESIAN_POINT('Ctrl Pts',(2.37698452505334,-0.595730490790041,24.026494492978));
#8548=CARTESIAN_POINT('Ctrl Pts',(2.35722201484881,-0.674583565558943,24.0222774936911));
#8549=CARTESIAN_POINT('Ctrl Pts',(2.33351683191325,-0.752510853870986,24.0180604944042));
#8550=CARTESIAN_POINT('Ctrl Pts',(2.30598208858976,-0.82909399774887,24.0138434951172));
#8551=CARTESIAN_POINT('Ctrl Pts',(2.27845647363606,-0.905651752639155,24.0096278938578));
#8552=CARTESIAN_POINT('Ctrl Pts',(2.24710397669315,-0.980865810720861,24.0054122925984));
#8553=CARTESIAN_POINT('Ctrl Pts',(2.21208719658111,-1.05433414282281,24.001196691339));
#8554=CARTESIAN_POINT('Ctrl Pts',(2.17707129022818,-1.12780064170013,23.9969811952697));
#8555=CARTESIAN_POINT('Ctrl Pts',(2.13839148357112,-1.19952108185924,23.9927656992004));
#8556=CARTESIAN_POINT('Ctrl Pts',(2.09625742106833,-1.26911586335367,23.9885502031312));
#8557=CARTESIAN_POINT('Ctrl Pts',(2.05367689204647,-1.33944809426537,23.9842900382656));
#8558=CARTESIAN_POINT('Ctrl Pts',(2.00756870353918,-1.40760892713529,23.9800298734));
#8559=CARTESIAN_POINT('Ctrl Pts',(1.95819447844173,-1.47323610959015,23.9757697085344));
#8560=CARTESIAN_POINT('Ctrl Pts',(1.90926680270934,-1.53826974801272,23.9715480733654));
#8561=CARTESIAN_POINT('Ctrl Pts',(1.85713227849281,-1.6008150595765,23.9673264381965));
#8562=CARTESIAN_POINT('Ctrl Pts',(1.80208521041733,-1.66055386675505,23.9631048030276));
#8563=CARTESIAN_POINT('Ctrl Pts',(1.74628454329194,-1.72111050329138,23.9588253733136));
#8564=CARTESIAN_POINT('Ctrl Pts',(1.68749133567652,-1.77878286466063,23.9545459435997));
#8565=CARTESIAN_POINT('Ctrl Pts',(1.6260482767155,-1.83328046184716,23.9502665138858));
#8566=CARTESIAN_POINT('Ctrl Pts',(1.56460521775449,-1.88777805903369,23.9459870841718));
#8567=CARTESIAN_POINT('Ctrl Pts',(1.50051273132664,-1.93910063651416,23.9417076544579));
#8568=CARTESIAN_POINT('Ctrl Pts',(1.43414383714884,-1.9870031968691,23.937428224744));
#8569=CARTESIAN_POINT('Ctrl Pts',(1.36853065311727,-2.03436031419173,23.9331975228037));
#8570=CARTESIAN_POINT('Ctrl Pts',(1.30044587424346,-2.07855306101518,23.9289668208635));
#8571=CARTESIAN_POINT('Ctrl Pts',(1.23022750145088,-2.1193136966183,23.9247361189232));
#8572=CARTESIAN_POINT('Ctrl Pts',(1.16011001313893,-2.16001577040363,23.9205114953375));
#8573=CARTESIAN_POINT('Ctrl Pts',(1.08786541773088,-2.19729529471097,23.9162868717519));
#8574=CARTESIAN_POINT('Ctrl Pts',(1.01386228183258,-2.23092660647481,23.9120622481662));
#8575=CARTESIAN_POINT('Ctrl Pts',(0.939567884232503,-2.26469028442799,23.9078209972979));
#8576=CARTESIAN_POINT('Ctrl Pts',(0.863501458712462,-2.29477669322726,23.9035797464296));
#8577=CARTESIAN_POINT('Ctrl Pts',(0.786062688872571,-2.32100316655588,23.8993384955613));
#8578=CARTESIAN_POINT('Ctrl Pts',(0.709066715906454,-2.34707967623679,23.8951214962744));
#8579=CARTESIAN_POINT('Ctrl Pts',(0.630714495145392,-2.36934012240321,23.8909044969874));
#8580=CARTESIAN_POINT('Ctrl Pts',(0.551419004568647,-2.38765310114357,23.8866874977005));
#8581=CARTESIAN_POINT('Ctrl Pts',(0.472149802181747,-2.40596000873086,23.882471896441));
#8582=CARTESIAN_POINT('Ctrl Pts',(0.391938403751396,-2.42032194312577,23.8782562951816));
#8583=CARTESIAN_POINT('Ctrl Pts',(0.311210851255149,-2.43065794715362,23.8740406939222));
#8584=CARTESIAN_POINT('Ctrl Pts',(0.230485313119844,-2.44099369327147,23.8698251978529));
#8585=CARTESIAN_POINT('Ctrl Pts',(0.149244107958652,-2.44730365077036,23.8656097017836));
#8586=CARTESIAN_POINT('Ctrl Pts',(0.0679198912756184,-2.44955855989791,
23.8613942057143));
#8587=CARTESIAN_POINT('Ctrl Pts',(-0.0142660638146256,-2.45183736279141,
23.8571340408487));
#8588=CARTESIAN_POINT('Ctrl Pts',(-0.0965363163014231,-2.44997463881074,
23.8528738759831));
#8589=CARTESIAN_POINT('Ctrl Pts',(-0.178444654041903,-2.44399422164699,
23.8486137111175));
#8590=CARTESIAN_POINT('Ctrl Pts',(-0.259612198056423,-2.43806789245078,
23.8443920759486));
#8591=CARTESIAN_POINT('Ctrl Pts',(-0.340423888303748,-2.42809817162713,
23.8401704407796));
#8592=CARTESIAN_POINT('Ctrl Pts',(-0.420452874624337,-2.41416023292161,
23.8359488056106));
#8593=CARTESIAN_POINT('Ctrl Pts',(-0.501577464582075,-2.40003148264841,
23.8316693758967));
#8594=CARTESIAN_POINT('Ctrl Pts',(-0.581897275366923,-2.38182515070145,
23.8273899461828));
#8595=CARTESIAN_POINT('Ctrl Pts',(-0.660982540191198,-2.35967208136266,
23.8231105164689));
#8596=CARTESIAN_POINT('Ctrl Pts',(-0.740067805015472,-2.33751901202387,
23.818831086755));
#8597=CARTESIAN_POINT('Ctrl Pts',(-0.81791807955301,-2.31141942332912,23.8145516570412));
#8598=CARTESIAN_POINT('Ctrl Pts',(-0.894125423086613,-2.28155428990638,
23.8102722273273));
#8599=CARTESIAN_POINT('Ctrl Pts',(-0.969465030862561,-2.25202921615474,
23.806041525387));
#8600=CARTESIAN_POINT('Ctrl Pts',(-1.04348232106292,-2.21871290277078,23.8018108234467));
#8601=CARTESIAN_POINT('Ctrl Pts',(-1.11576919095807,-2.18174456857552,23.7975801215065));
#8602=CARTESIAN_POINT('Ctrl Pts',(-1.18795220451145,-2.14482934770438,23.7933554979208));
#8603=CARTESIAN_POINT('Ctrl Pts',(-1.2584093248238,-2.10427273670745,23.7891308743351));
#8604=CARTESIAN_POINT('Ctrl Pts',(-1.32675127764851,-2.06026243407437,23.7849062507494));
#8605=CARTESIAN_POINT('Ctrl Pts',(-1.39536221087843,-2.01607891559734,23.7806649998811));
#8606=CARTESIAN_POINT('Ctrl Pts',(-1.46184084931113,-1.96841463423306,23.7764237490129));
#8607=CARTESIAN_POINT('Ctrl Pts',(-1.52581722143069,-1.91750672926734,23.7721824981446));
#8608=CARTESIAN_POINT('Ctrl Pts',(-1.58942777501225,-1.86688991700897,23.7679654988576));
#8609=CARTESIAN_POINT('Ctrl Pts',(-1.65056423310858,-1.81306676722035,23.7637484995706));
#8610=CARTESIAN_POINT('Ctrl Pts',(-1.70889252572217,-1.75631335061,23.7595315002837));
#8611=CARTESIAN_POINT('Ctrl Pts',(-1.7672014812307,-1.69957874899885,23.7553158990242));
#8612=CARTESIAN_POINT('Ctrl Pts',(-1.82270378694922,-1.63991613375571,23.7511002977648));
#8613=CARTESIAN_POINT('Ctrl Pts',(-1.87510071335033,-1.57763987170491,23.7468846965054));
#8614=CARTESIAN_POINT('Ctrl Pts',(-1.92749633231279,-1.5153651636077,23.7426692004361));
#8615=CARTESIAN_POINT('Ctrl Pts',(-1.9767864274444,-1.45047729492946,23.7384537043668));
#8616=CARTESIAN_POINT('Ctrl Pts',(-2.0227121535729,-1.38332418246356,23.7342382082975));
#8617=CARTESIAN_POINT('Ctrl Pts',(-2.06912452394709,-1.31545949331686,23.7299780434319));
#8618=CARTESIAN_POINT('Ctrl Pts',(-2.11210051405413,-1.24528165878774,23.7257178785663));
#8619=CARTESIAN_POINT('Ctrl Pts',(-2.15141857770893,-1.17317873893491,23.7214577137007));
#8620=CARTESIAN_POINT('Ctrl Pts',(-2.19038104173034,-1.10172793084654,23.7172360785318));
#8621=CARTESIAN_POINT('Ctrl Pts',(-2.22575133037728,-1.02838716936309,23.7130144433628));
#8622=CARTESIAN_POINT('Ctrl Pts',(-2.25736154480884,-0.95355603192378,23.7087928081938));
#8623=CARTESIAN_POINT('Ctrl Pts',(-2.28940450576756,-0.877700449841104,
23.7045133784799));
#8624=CARTESIAN_POINT('Ctrl Pts',(-2.31758349228035,-0.800313840879351,
23.700233948766));
#8625=CARTESIAN_POINT('Ctrl Pts',(-2.34177583183151,-0.721828375342686,
23.6959545190522));
#8626=CARTESIAN_POINT('Ctrl Pts',(-2.36596817138266,-0.64334290980602,23.6916750893383));
#8627=CARTESIAN_POINT('Ctrl Pts',(-2.38617380672403,-0.563759079312216,
23.6873956596243));
#8628=CARTESIAN_POINT('Ctrl Pts',(-2.40232402969862,-0.483517844895685,
23.6831162299104));
#8629=CARTESIAN_POINT('Ctrl Pts',(-2.42528233781748,-0.369451123558754,
23.6770328175576));
#8630=CARTESIAN_POINT('Ctrl Pts',(-2.44012249745692,-0.253699812642377,
23.6709494052048));
#8631=CARTESIAN_POINT('Ctrl Pts',(-2.44665526989246,-0.137216035168911,
23.664865992852));
#8632=CARTESIAN_POINT('Ctrl Pts',(-2.44917473836235,-0.0922921980852357,
23.6625198273054));
#8633=CARTESIAN_POINT('Ctrl Pts',(-2.45045903119537,-0.0472596765065585,
23.6601736617587));
#8634=CARTESIAN_POINT('Ctrl Pts',(-2.45049903536283,-0.00217432422771299,
23.6578274962121));
#8635=CARTESIAN_POINT('',(-2.45049999653667,-0.000130283473732951,22.8578274962385));
#8636=CARTESIAN_POINT('Ctrl Pts',(-2.45049903536358,-0.00217432338460544,
23.6578274961682));
#8637=CARTESIAN_POINT('Ctrl Pts',(-2.45057140723685,0.0793899953797731,
23.6535830268485));
#8638=CARTESIAN_POINT('Ctrl Pts',(-2.44656693668155,0.161087169591102,23.6493385575287));
#8639=CARTESIAN_POINT('Ctrl Pts',(-2.43847466509949,0.242469704639374,23.6450940882089));
#8640=CARTESIAN_POINT('Ctrl Pts',(-2.43054759010129,0.32219088704529,23.6409362659851));
#8641=CARTESIAN_POINT('Ctrl Pts',(-2.41869807736882,0.401609652003178,23.6367784437612));
#8642=CARTESIAN_POINT('Ctrl Pts',(-2.40296835781629,0.48030544587134,23.6326206215373));
#8643=CARTESIAN_POINT('Ctrl Pts',(-2.38724644125954,0.558962201348212,23.6284648618721));
#8644=CARTESIAN_POINT('Ctrl Pts',(-2.36764823011024,0.636896227555752,23.6243091022069));
#8645=CARTESIAN_POINT('Ctrl Pts',(-2.34426744405512,0.713694893314566,23.6201533425417));
#8646=CARTESIAN_POINT('Ctrl Pts',(-2.32089060445998,0.790480596170412,23.6159982843302));
#8647=CARTESIAN_POINT('Ctrl Pts',(-2.29373259783618,0.866130860354779,23.6118432261187));
#8648=CARTESIAN_POINT('Ctrl Pts',(-2.26293718669771,0.94024759455191,23.6076881679072));
#8649=CARTESIAN_POINT('Ctrl Pts',(-2.23098851599881,1.01713993164378,23.6033775066228));
#8650=CARTESIAN_POINT('Ctrl Pts',(-2.1951248041455,1.09238108773871,23.5990668453383));
#8651=CARTESIAN_POINT('Ctrl Pts',(-2.15556071890065,1.1655506154314,23.5947561840539));
#8652=CARTESIAN_POINT('Ctrl Pts',(-2.11737709415898,1.23616712964251,23.5905959293214));
#8653=CARTESIAN_POINT('Ctrl Pts',(-2.07574736520934,1.30485380286194,23.586435674589));
#8654=CARTESIAN_POINT('Ctrl Pts',(-2.03090962191127,1.37126086417874,23.5822754198566));
#8655=CARTESIAN_POINT('Ctrl Pts',(-1.98604163029131,1.4377127248547,23.5781123585439));
#8656=CARTESIAN_POINT('Ctrl Pts',(-1.93796161023225,1.50188153438619,23.5739492972312));
#8657=CARTESIAN_POINT('Ctrl Pts',(-1.88694812386953,1.56345035988523,23.5697862359186));
#8658=CARTESIAN_POINT('Ctrl Pts',(-1.83585604644476,1.62511403793661,23.5656167610193));
#8659=CARTESIAN_POINT('Ctrl Pts',(-1.78182181869754,1.68416939772165,23.5614472861201));
#8660=CARTESIAN_POINT('Ctrl Pts',(-1.72516030602709,1.74033679743563,23.5572778112209));
#8661=CARTESIAN_POINT('Ctrl Pts',(-1.71919184832368,1.7462532076002,23.5568386183118));
#8662=CARTESIAN_POINT('Ctrl Pts',(-1.71319426844774,1.75213761220009,23.5563994254028));
#8663=CARTESIAN_POINT('Ctrl Pts',(-1.70716795431091,1.75798971150968,23.5559602324937));
#8664=CARTESIAN_POINT('Ctrl Pts',(-1.64911706508791,1.81436240649869,23.5517295305535));
#8665=CARTESIAN_POINT('Ctrl Pts',(-1.58816176517418,1.86796266208168,23.5474988286132));
#8666=CARTESIAN_POINT('Ctrl Pts',(-1.52459764933914,1.91847654602019,23.5432681266729));
#8667=CARTESIAN_POINT('Ctrl Pts',(-1.46112485764856,1.96891785540664,23.5390435030873));
#8668=CARTESIAN_POINT('Ctrl Pts',(-1.39505105507288,2.01628131296052,23.5348188795016));
#8669=CARTESIAN_POINT('Ctrl Pts',(-1.32670818167451,2.0602901860364,23.5305942559159));
#8670=CARTESIAN_POINT('Ctrl Pts',(-1.2580963242478,2.10447226932974,23.5263530050476));
#8671=CARTESIAN_POINT('Ctrl Pts',(-1.1871978369066,2.14527297494325,23.5221117541793));
#8672=CARTESIAN_POINT('Ctrl Pts',(-1.11438168379101,2.18245359923896,23.5178705033111));
#8673=CARTESIAN_POINT('Ctrl Pts',(-1.04198189530796,2.21942162377061,23.5136535040241));
#8674=CARTESIAN_POINT('Ctrl Pts',(-0.9676867304183,2.25281064046416,23.5094365047371));
#8675=CARTESIAN_POINT('Ctrl Pts',(-0.891885741999468,2.2824307378797,23.5052195054502));
#8676=CARTESIAN_POINT('Ctrl Pts',(-0.816109883266569,2.31204101558496,23.5010039041907));
#8677=CARTESIAN_POINT('Ctrl Pts',(-0.738829625178347,2.3378846861362,23.4967883029313));
#8678=CARTESIAN_POINT('Ctrl Pts',(-0.660454763102909,2.35981985666166,23.4925727016719));
#8679=CARTESIAN_POINT('Ctrl Pts',(-0.582081856682689,2.38175447984798,23.4883572056026));
#8680=CARTESIAN_POINT('Ctrl Pts',(-0.502614848724108,2.39978067261914,23.4841417095333));
#8681=CARTESIAN_POINT('Ctrl Pts',(-0.422477576214879,2.4138067336876,23.4799262134639));
#8682=CARTESIAN_POINT('Ctrl Pts',(-0.341491142553382,2.42798141955705,23.4756660485984));
#8683=CARTESIAN_POINT('Ctrl Pts',(-0.259820629507715,2.43807059611962,23.4714058837328));
#8684=CARTESIAN_POINT('Ctrl Pts',(-0.177910987857276,2.44403312792598,23.4671457188672));
#8685=CARTESIAN_POINT('Ctrl Pts',(-0.0967421517253367,2.4499417335232,23.4629240836983));
#8686=CARTESIAN_POINT('Ctrl Pts',(-0.0153389665478567,2.45179808934017,
23.4587024485293));
#8687=CARTESIAN_POINT('Ctrl Pts',(0.06586532795961,2.44961466532448,23.4544808133603));
#8688=CARTESIAN_POINT('Ctrl Pts',(0.148181316173007,2.44740135004811,23.4502013836464));
#8689=CARTESIAN_POINT('Ctrl Pts',(0.230292433649477,2.44103684580901,23.4459219539326));
#8690=CARTESIAN_POINT('Ctrl Pts',(0.311754480614958,2.43058828142828,23.4416425242187));
#8691=CARTESIAN_POINT('Ctrl Pts',(0.393216527580415,2.42013971704755,23.4373630945048));
#8692=CARTESIAN_POINT('Ctrl Pts',(0.474029032783694,2.40560724381203,23.4330836647909));
#8693=CARTESIAN_POINT('Ctrl Pts',(0.553762120999265,2.38711075640541,23.428804235077));
#8694=CARTESIAN_POINT('Ctrl Pts',(0.632587327526426,2.36882487945665,23.4245735331368));
#8695=CARTESIAN_POINT('Ctrl Pts',(0.710654067120783,2.34659606583175,23.4203428311965));
#8696=CARTESIAN_POINT('Ctrl Pts',(0.787538360381237,2.320502872424,23.4161121292563));
#8697=CARTESIAN_POINT('Ctrl Pts',(0.86431219206763,2.29444716775541,23.4118875056706));
#8698=CARTESIAN_POINT('Ctrl Pts',(0.939906514776988,2.26453825817395,23.4076628820849));
#8699=CARTESIAN_POINT('Ctrl Pts',(1.01390894717371,2.23090539845174,23.4034382584993));
#8700=CARTESIAN_POINT('Ctrl Pts',(1.08820263850347,2.19714016644769,23.399197007631));
#8701=CARTESIAN_POINT('Ctrl Pts',(1.1608914196349,2.15962171520747,23.3949557567627));
#8702=CARTESIAN_POINT('Ctrl Pts',(1.23157483713222,2.11853101713021,23.3907145058944));
#8703=CARTESIAN_POINT('Ctrl Pts',(1.30185408503381,2.07767527671937,23.3864975066075));
#8704=CARTESIAN_POINT('Ctrl Pts',(1.37015043441059,2.03328826709363,23.3822805073205));
#8705=CARTESIAN_POINT('Ctrl Pts',(1.43609330724811,1.98559468746197,23.3780635080335));
#8706=CARTESIAN_POINT('Ctrl Pts',(1.50201431858061,1.93791691929538,23.3738479067741));
#8707=CARTESIAN_POINT('Ctrl Pts',(1.56558302624488,1.88693503031906,23.3696323055147));
#8708=CARTESIAN_POINT('Ctrl Pts',(1.62645826467462,1.83291673658997,23.3654167042552));
#8709=CARTESIAN_POINT('Ctrl Pts',(1.68733198410993,1.77889979075683,23.361201208186));
#8710=CARTESIAN_POINT('Ctrl Pts',(1.7455120208046,1.72184690029657,23.3569857121167));
#8711=CARTESIAN_POINT('Ctrl Pts',(1.80069180584515,1.66206476118175,23.3527702160474));
#8712=CARTESIAN_POINT('Ctrl Pts',(1.856456294213,1.60164915066742,23.3485100511818));
#8713=CARTESIAN_POINT('Ctrl Pts',(1.90915622857819,1.53844645212694,23.3442498863162));
#8714=CARTESIAN_POINT('Ctrl Pts',(1.9585161223792,1.47280849005591,23.3399897214506));
#8715=CARTESIAN_POINT('Ctrl Pts',(2.00742959643023,1.40776416950959,23.3357680862816));
#8716=CARTESIAN_POINT('Ctrl Pts',(2.05306299034284,1.34032888220443,23.3315464511127));
#8717=CARTESIAN_POINT('Ctrl Pts',(2.0951922272049,1.27087362906788,23.3273248159437));
#8718=CARTESIAN_POINT('Ctrl Pts',(2.13789821690709,1.20046752760149,23.3230453862298));
#8719=CARTESIAN_POINT('Ctrl Pts',(2.17700314381538,1.1279861698671,23.3187659565159));
#8720=CARTESIAN_POINT('Ctrl Pts',(2.21232295197123,1.05383936450548,23.314486526802));
#8721=CARTESIAN_POINT('Ctrl Pts',(2.24764276012706,0.979692559143882,23.3102070970881));
#8722=CARTESIAN_POINT('Ctrl Pts',(2.27917732158504,0.903880784271508,23.3059276673742));
#8723=CARTESIAN_POINT('Ctrl Pts',(2.30679469916284,0.826830373120286,23.3016482376603));
#8724=CARTESIAN_POINT('Ctrl Pts',(2.33409761116615,0.750657297325703,23.29741753572));
#8725=CARTESIAN_POINT('Ctrl Pts',(2.35767482651362,0.672987155684556,23.2931868337798));
#8726=CARTESIAN_POINT('Ctrl Pts',(2.37736284503384,0.594218943700571,23.2889561318395));
#8727=CARTESIAN_POINT('Ctrl Pts',(2.39702257728873,0.515563899963611,23.2847315082538));
#8728=CARTESIAN_POINT('Ctrl Pts',(2.4128040983922,0.435814366485919,23.2805068846682));
#8729=CARTESIAN_POINT('Ctrl Pts',(2.42459281212596,0.355387036042603,23.2762822610825));
#8730=CARTESIAN_POINT('Ctrl Pts',(2.43642792390465,0.274643159538683,23.2720410102142));
#8731=CARTESIAN_POINT('Ctrl Pts',(2.4442385709811,0.193216586000986,23.2677997593459));
#8732=CARTESIAN_POINT('Ctrl Pts',(2.44796009702725,0.111541980269029,23.2635585084776));
#8733=CARTESIAN_POINT('Ctrl Pts',(2.45166034329194,0.0303343920291857,23.2593415091907));
#8734=CARTESIAN_POINT('Ctrl Pts',(2.45131808364673,-0.0511179303445025,
23.2551245099037));
#8735=CARTESIAN_POINT('Ctrl Pts',(2.44692160031491,-0.132381765784869,23.2509075106168));
#8736=CARTESIAN_POINT('Ctrl Pts',(2.4425265745135,-0.213618660485914,23.2466919093573));
#8737=CARTESIAN_POINT('Ctrl Pts',(2.4340800192119,-0.294666728329954,23.2424763080979));
#8738=CARTESIAN_POINT('Ctrl Pts',(2.42162230761982,-0.375094187155815,23.2382607068385));
#8739=CARTESIAN_POINT('Ctrl Pts',(2.4091649068798,-0.455519639108869,23.2340452107692));
#8740=CARTESIAN_POINT('Ctrl Pts',(2.39269662110869,-0.535324053419385,23.2298297146999));
#8741=CARTESIAN_POINT('Ctrl Pts',(2.37230932721114,-0.614083631134233,23.2256142186306));
#8742=CARTESIAN_POINT('Ctrl Pts',(2.35170600277696,-0.693677771490152,23.221354053765));
#8743=CARTESIAN_POINT('Ctrl Pts',(2.32710022727633,-0.772204327488093,23.2170938888994));
#8744=CARTESIAN_POINT('Ctrl Pts',(2.29863864811276,-0.84924119977917,23.2128337240338));
#8745=CARTESIAN_POINT('Ctrl Pts',(2.27043448058587,-0.925581336753225,23.2086120888649));
#8746=CARTESIAN_POINT('Ctrl Pts',(2.2384442155249,-1.00045821940249,23.2043904536959));
#8747=CARTESIAN_POINT('Ctrl Pts',(2.20285845685593,-1.07348258908019,23.200168818527));
#8748=CARTESIAN_POINT('Ctrl Pts',(2.16678552612065,-1.14750666859682,23.1958893888131));
#8749=CARTESIAN_POINT('Ctrl Pts',(2.12701815000943,-1.21962669580652,23.1916099590992));
#8750=CARTESIAN_POINT('Ctrl Pts',(2.08380122814361,-1.28946604902462,23.1873305293853));
#8751=CARTESIAN_POINT('Ctrl Pts',(2.04058430627781,-1.3593054022427,23.1830510996714));
#8752=CARTESIAN_POINT('Ctrl Pts',(1.99391817136626,-1.42686371504018,23.1787716699575));
#8753=CARTESIAN_POINT('Ctrl Pts',(1.94408983392752,-1.49179923837616,23.1744922402436));
#8754=CARTESIAN_POINT('Ctrl Pts',(1.89482886740259,-1.55599537265948,23.1702615383033));
#8755=CARTESIAN_POINT('Ctrl Pts',(1.84229209519892,-1.61786962863514,23.1660308363631));
#8756=CARTESIAN_POINT('Ctrl Pts',(1.78672645485823,-1.67706852141161,23.1618001344228));
#8757=CARTESIAN_POINT('Ctrl Pts',(1.7312406470534,-1.7361823616682,23.1575755108371));
#8758=CARTESIAN_POINT('Ctrl Pts',(1.67273492930474,-1.79262813643478,23.1533508872514));
#8759=CARTESIAN_POINT('Ctrl Pts',(1.61149759544756,-1.84608389567396,23.1491262636657));
#8760=CARTESIAN_POINT('Ctrl Pts',(1.55001924355995,-1.89975004620543,23.1448850127975));
#8761=CARTESIAN_POINT('Ctrl Pts',(1.48578801613983,-1.95040221802397,23.1406437619292));
#8762=CARTESIAN_POINT('Ctrl Pts',(1.41913435521906,-1.99775071814203,23.1364025110609));
#8763=CARTESIAN_POINT('Ctrl Pts',(1.35286182164231,-2.04482847832105,23.1321855117739));
#8764=CARTESIAN_POINT('Ctrl Pts',(1.28419486541242,-2.08863997320375,23.127968512487));
#8765=CARTESIAN_POINT('Ctrl Pts',(1.21349137625761,-2.12894079996331,23.1237515132));
#8766=CARTESIAN_POINT('Ctrl Pts',(1.14281132685615,-2.16922826611719,23.1195359119406));
#8767=CARTESIAN_POINT('Ctrl Pts',(1.07009648898759,-2.2060071452667,23.1153203106811));
#8768=CARTESIAN_POINT('Ctrl Pts',(0.995731745286284,-2.23907760951449,23.1111047094217));
#8769=CARTESIAN_POINT('Ctrl Pts',(0.921368857177361,-2.2721472485688,23.1068892133524));
#8770=CARTESIAN_POINT('Ctrl Pts',(0.845356570467875,-2.30150846872244,23.1026737172831));
#8771=CARTESIAN_POINT('Ctrl Pts',(0.768100940560529,-2.32700906640048,23.0984582212138));
#8772=CARTESIAN_POINT('Ctrl Pts',(0.690026684342956,-2.35277987687998,23.0941980563482));
#8773=CARTESIAN_POINT('Ctrl Pts',(0.610683033283608,-2.37460759369635,23.0899378914826));
#8774=CARTESIAN_POINT('Ctrl Pts',(0.530504267227015,-2.39238698216947,23.085677726617));
#8775=CARTESIAN_POINT('Ctrl Pts',(0.451050652338985,-2.41000557065823,23.0814560914481));
#8776=CARTESIAN_POINT('Ctrl Pts',(0.370777441475839,-2.42364874593649,23.0772344562791));
#8777=CARTESIAN_POINT('Ctrl Pts',(0.290115101996816,-2.43326601044633,23.0730128211101));
#8778=CARTESIAN_POINT('Ctrl Pts',(0.208348488222393,-2.44301493612616,23.0687333913963));
#8779=CARTESIAN_POINT('Ctrl Pts',(0.126182504256642,-2.44862685258757,23.0644539616824));
#8780=CARTESIAN_POINT('Ctrl Pts',(0.044066389170475,-2.45010375358789,23.0601745319685));
#8781=CARTESIAN_POINT('Ctrl Pts',(-0.0380497259157154,-2.45158065458821,
23.0558951022546));
#8782=CARTESIAN_POINT('Ctrl Pts',(-0.120115483911881,-2.44892262146589,
23.0516156725407));
#8783=CARTESIAN_POINT('Ctrl Pts',(-0.201688165846101,-2.44218593349434,
23.0473362428268));
#8784=CARTESIAN_POINT('Ctrl Pts',(-0.282332019538064,-2.43552595289466,
23.0431055408866));
#8785=CARTESIAN_POINT('Ctrl Pts',(-0.362797296576456,-2.42485472160483,
23.0388748389463));
#8786=CARTESIAN_POINT('Ctrl Pts',(-0.442653106969058,-2.41018847331296,
23.0346441370061));
#8787=CARTESIAN_POINT('Ctrl Pts',(-0.522394186534937,-2.39554329638437,
23.0304195134204));
#8788=CARTESIAN_POINT('Ctrl Pts',(-0.601527084987009,-2.37691458518828,
23.0261948898347));
#8789=CARTESIAN_POINT('Ctrl Pts',(-0.679625034711575,-2.35437041737134,
23.021970266249));
#8790=CARTESIAN_POINT('Ctrl Pts',(-0.75803036251502,-2.33173752017011,23.0177290153807));
#8791=CARTESIAN_POINT('Ctrl Pts',(-0.835392104466457,-2.30515831837483,
23.0134877645124));
#8792=CARTESIAN_POINT('Ctrl Pts',(-0.911287793776614,-2.27475379039441,
23.0092465136442));
#8793=CARTESIAN_POINT('Ctrl Pts',(-0.986749509586992,-2.2445231162855,23.0050295143572));
#8794=CARTESIAN_POINT('Ctrl Pts',(-1.06076145706714,-2.21051091859256,23.0008125150703));
#8795=CARTESIAN_POINT('Ctrl Pts',(-1.13292438696317,-2.17288577321131,22.9965955157833));
#8796=CARTESIAN_POINT('Ctrl Pts',(-1.20506339326933,-2.13527310138883,22.9923799145239));
#8797=CARTESIAN_POINT('Ctrl Pts',(-1.2753541872375,-2.09405007528642,22.9881643132644));
#8798=CARTESIAN_POINT('Ctrl Pts',(-1.34342038204196,-2.04943209868349,22.983948712005));
#8799=CARTESIAN_POINT('Ctrl Pts',(-1.41148487841883,-2.00481523541447,22.9797332159357));
#8800=CARTESIAN_POINT('Ctrl Pts',(-1.47732449764834,-1.95680384593917,22.9755177198664));
#8801=CARTESIAN_POINT('Ctrl Pts',(-1.54059143022449,-1.90565691957363,22.9713022237972));
#8802=CARTESIAN_POINT('Ctrl Pts',(-1.60452876022909,-1.85396802339049,22.9670420589316));
#8803=CARTESIAN_POINT('Ctrl Pts',(-1.66583816997758,-1.79907703632353,22.962781894066));
#8804=CARTESIAN_POINT('Ctrl Pts',(-1.72419605836845,-1.74129210711664,22.9585217292004));
#8805=CARTESIAN_POINT('Ctrl Pts',(-1.78202614752932,-1.68402979519393,22.9543000940314));
#8806=CARTESIAN_POINT('Ctrl Pts',(-1.83695761709659,-1.62392606598259,22.9500784588624));
#8807=CARTESIAN_POINT('Ctrl Pts',(-1.88871495074073,-1.56131549817724,22.9458568236935));
#8808=CARTESIAN_POINT('Ctrl Pts',(-1.94118084668974,-1.49784778636717,22.9415773939796));
#8809=CARTESIAN_POINT('Ctrl Pts',(-1.99038474476822,-1.4318044752645,22.9372979642657));
#8810=CARTESIAN_POINT('Ctrl Pts',(-2.03608509788774,-1.36356434544157,22.9330185345518));
#8811=CARTESIAN_POINT('Ctrl Pts',(-2.08178545100725,-1.29532421561863,22.9287391048379));
#8812=CARTESIAN_POINT('Ctrl Pts',(-2.12398206323083,-1.22488772157964,22.9244596751239));
#8813=CARTESIAN_POINT('Ctrl Pts',(-2.16248255848491,-1.15265755289616,22.92018024541));
#8814=CARTESIAN_POINT('Ctrl Pts',(-2.20267916262551,-1.07724534122413,22.9157122888027));
#8815=CARTESIAN_POINT('Ctrl Pts',(-2.23898476198766,-0.99962042806452,22.9112443321953));
#8816=CARTESIAN_POINT('Ctrl Pts',(-2.27116419083332,-0.920197515904305,
22.9067763755879));
#8817=CARTESIAN_POINT('Ctrl Pts',(-2.30324859241746,-0.841009143079146,
22.9023216130519));
#8818=CARTESIAN_POINT('Ctrl Pts',(-2.33123095314875,-0.760033706883554,
22.8978668505159));
#8819=CARTESIAN_POINT('Ctrl Pts',(-2.35492280758172,-0.677708506905027,
22.8934120879799));
#8820=CARTESIAN_POINT('Ctrl Pts',(-2.37857232061475,-0.595530436152999,
22.8889652868673));
#8821=CARTESIAN_POINT('Ctrl Pts',(-2.39794647646271,-0.512007771438047,
22.8845184857546));
#8822=CARTESIAN_POINT('Ctrl Pts',(-2.4129051813671,-0.42759658058948,22.8800716846419));
#8823=CARTESIAN_POINT('Ctrl Pts',(-2.42782859230941,-0.343384551726377,
22.8756353754288));
#8824=CARTESIAN_POINT('Ctrl Pts',(-2.4383572374736,-0.258288553180677,22.8711990662157));
#8825=CARTESIAN_POINT('Ctrl Pts',(-2.44440142582957,-0.172777080083969,
22.8667627570026));
#8826=CARTESIAN_POINT('Ctrl Pts',(-2.44845933346359,-0.115366946739541,
22.8637843367479));
#8827=CARTESIAN_POINT('Ctrl Pts',(-2.45049693206645,-0.0577698600959872,
22.8608059164932));
#8828=CARTESIAN_POINT('Ctrl Pts',(-2.45049999653667,-0.000130283473727266,
22.8578274962385));
#8829=CARTESIAN_POINT('',(-2.45049898498603,0.00223037720034039,22.0578274962121));
#8830=CARTESIAN_POINT('Ctrl Pts',(-2.4504999965367,-0.000130282961934726,
22.8578274962121));
#8831=CARTESIAN_POINT('Ctrl Pts',(-2.45050452194915,0.084988469602718,22.8534291395352));
#8832=CARTESIAN_POINT('Ctrl Pts',(-2.44606980392823,0.170029198438209,22.8490307828582));
#8833=CARTESIAN_POINT('Ctrl Pts',(-2.43724598391114,0.254523601870292,22.8446324261812));
#8834=CARTESIAN_POINT('Ctrl Pts',(-2.42839970581659,0.339233057496683,22.840222874961));
#8835=CARTESIAN_POINT('Ctrl Pts',(-2.41514204232535,0.42339300592857,22.8358133237408));
#8836=CARTESIAN_POINT('Ctrl Pts',(-2.39757477354423,0.506542649008293,22.8314037725206));
#8837=CARTESIAN_POINT('Ctrl Pts',(-2.37998497661336,0.589798922642478,22.826988566521));
#8838=CARTESIAN_POINT('Ctrl Pts',(-2.35807465958574,0.672041917853691,22.8225733605213));
#8839=CARTESIAN_POINT('Ctrl Pts',(-2.33199555061119,0.752826010396555,22.8181581545217));
#8840=CARTESIAN_POINT('Ctrl Pts',(-2.30584599539508,0.833828321119468,22.8137310219386));
#8841=CARTESIAN_POINT('Ctrl Pts',(-2.27550527632207,0.913363470995812,22.8093038893556));
#8842=CARTESIAN_POINT('Ctrl Pts',(-2.24117371120737,0.991004866886629,22.8048767567725));
#8843=CARTESIAN_POINT('Ctrl Pts',(-2.21053573284011,1.06029315595121,22.8009259205128));
#8844=CARTESIAN_POINT('Ctrl Pts',(-2.17672019184988,1.12807340583439,22.7969750842531));
#8845=CARTESIAN_POINT('Ctrl Pts',(-2.1398991839799,1.19406102540956,22.7930242479933));
#8846=CARTESIAN_POINT('Ctrl Pts',(-2.10046988365024,1.26472301487648,22.7887935460531));
#8847=CARTESIAN_POINT('Ctrl Pts',(-2.05746265756872,1.33356278892397,22.7845628441128));
#8848=CARTESIAN_POINT('Ctrl Pts',(-2.01107056395171,1.40019478530916,22.7803321421725));
#8849=CARTESIAN_POINT('Ctrl Pts',(-1.96474512300802,1.46673104984992,22.7761075185868));
#8850=CARTESIAN_POINT('Ctrl Pts',(-1.91504473643611,1.53106545800698,22.7718828950011));
#8851=CARTESIAN_POINT('Ctrl Pts',(-1.86220795516667,1.59283765077109,22.7676582714155));
#8852=CARTESIAN_POINT('Ctrl Pts',(-1.80916321877987,1.65485296666434,22.7634170205472));
#8853=CARTESIAN_POINT('Ctrl Pts',(-1.75295757752181,1.71428544075555,22.7591757696789));
#8854=CARTESIAN_POINT('Ctrl Pts',(-1.69387596331198,1.77080051697359,22.7549345188106));
#8855=CARTESIAN_POINT('Ctrl Pts',(-1.63513217928856,1.82699243853532,22.7507175195236));
#8856=CARTESIAN_POINT('Ctrl Pts',(-1.57354556228278,1.88029991050268,22.7465005202367));
#8857=CARTESIAN_POINT('Ctrl Pts',(-1.50943477042091,1.93042920715689,22.7422835209497));
#8858=CARTESIAN_POINT('Ctrl Pts',(-1.44534523268907,1.9805418848526,22.7380679196903));
#8859=CARTESIAN_POINT('Ctrl Pts',(-1.37873354795214,2.02747819333838,22.7338523184308));
#8860=CARTESIAN_POINT('Ctrl Pts',(-1.30995154682697,2.0709845955404,22.7296367171714));
#8861=CARTESIAN_POINT('Ctrl Pts',(-1.24117126199038,2.11448991214531,22.7254212211021));
#8862=CARTESIAN_POINT('Ctrl Pts',(-1.17022116205443,2.15456524494254,22.7212057250328));
#8863=CARTESIAN_POINT('Ctrl Pts',(-1.09748093380322,2.19100110678621,22.7169902289634));
#8864=CARTESIAN_POINT('Ctrl Pts',(-1.02396992593742,2.22782305512183,22.7127300640979));
#8865=CARTESIAN_POINT('Ctrl Pts',(-0.948631052227707,2.26092771178783,22.7084698992323));
#8866=CARTESIAN_POINT('Ctrl Pts',(-0.871878737675352,2.29014796831769,22.7042097343668));
#8867=CARTESIAN_POINT('Ctrl Pts',(-0.795820584848088,2.31910395159665,22.6999880991978));
#8868=CARTESIAN_POINT('Ctrl Pts',(-0.718374921475555,2.34424542806036,22.6957664640288));
#8869=CARTESIAN_POINT('Ctrl Pts',(-0.639960339276593,2.36546000053964,22.6915448288598));
#8870=CARTESIAN_POINT('Ctrl Pts',(-0.560472254771274,2.38696500232232,22.687265399146));
#8871=CARTESIAN_POINT('Ctrl Pts',(-0.479989004804867,2.40443466179886,22.6829859694321));
#8872=CARTESIAN_POINT('Ctrl Pts',(-0.398955367487334,2.41780579549993,22.6787065397183));
#8873=CARTESIAN_POINT('Ctrl Pts',(-0.317921730169778,2.431176929201,22.6744271100044));
#8874=CARTESIAN_POINT('Ctrl Pts',(-0.236338200346401,2.4404495467966,22.6701476802905));
#8875=CARTESIAN_POINT('Ctrl Pts',(-0.154650978361124,2.44561512198709,22.6658682505767));
#8876=CARTESIAN_POINT('Ctrl Pts',(-0.0738938888293157,2.45072187929874,
22.6616375486364));
#8877=CARTESIAN_POINT('Ctrl Pts',(0.00726829076783438,2.45183389960285,
22.6574068466961));
#8878=CARTESIAN_POINT('Ctrl Pts',(0.0884068720686381,2.44890475008136,22.6531761447559));
#8879=CARTESIAN_POINT('Ctrl Pts',(0.169428879553817,2.44597980894175,22.6489515211702));
#8880=CARTESIAN_POINT('Ctrl Pts',(0.250426895264045,2.43902524574514,22.6447268975845));
#8881=CARTESIAN_POINT('Ctrl Pts',(0.330968790351451,2.42804652134453,22.6405022739989));
#8882=CARTESIAN_POINT('Ctrl Pts',(0.411827682403187,2.41702458685676,22.6362610231306));
#8883=CARTESIAN_POINT('Ctrl Pts',(0.492226382121897,2.40194671666979,22.6320197722623));
#8884=CARTESIAN_POINT('Ctrl Pts',(0.571729343457272,2.38287133681823,22.627778521394));
#8885=CARTESIAN_POINT('Ctrl Pts',(0.650777704819028,2.36390503047831,22.623561522107));
#8886=CARTESIAN_POINT('Ctrl Pts',(0.728940086938699,2.34098691574088,22.6193445228201));
#8887=CARTESIAN_POINT('Ctrl Pts',(0.805797012423965,2.31422588023914,22.6151275235331));
#8888=CARTESIAN_POINT('Ctrl Pts',(0.882628458157017,2.28747371660613,22.6109119222737));
#8889=CARTESIAN_POINT('Ctrl Pts',(0.958154867847997,2.25688131498546,22.6066963210142));
#8890=CARTESIAN_POINT('Ctrl Pts',(1.0319725930308,2.22260721163981,22.6024807197548));
#8891=CARTESIAN_POINT('Ctrl Pts',(1.10578847627069,2.18833396352156,22.5982652236855));
#8892=CARTESIAN_POINT('Ctrl Pts',(1.17789533841985,2.15037939316835,22.5940497276162));
#8893=CARTESIAN_POINT('Ctrl Pts',(1.24791148466156,2.10894930627784,22.5898342315469));
#8894=CARTESIAN_POINT('Ctrl Pts',(1.31866954524065,2.06708021242804,22.5855740666813));
#8895=CARTESIAN_POINT('Ctrl Pts',(1.38729189310486,2.0216617408722,22.5813139018157));
#8896=CARTESIAN_POINT('Ctrl Pts',(1.45341365594862,1.97295184804446,22.5770537369501));
#8897=CARTESIAN_POINT('Ctrl Pts',(1.51893740168683,1.92468249624087,22.5728321017811));
#8898=CARTESIAN_POINT('Ctrl Pts',(1.5820052867698,1.87318136532992,22.5686104666122));
#8899=CARTESIAN_POINT('Ctrl Pts',(1.64229618191657,1.81873953628942,22.5643888314432));
#8900=CARTESIAN_POINT('Ctrl Pts',(1.7034124645515,1.76355239397379,22.5601094017293));
#8901=CARTESIAN_POINT('Ctrl Pts',(1.76167479715434,1.70534377668101,22.5558299720154));
#8902=CARTESIAN_POINT('Ctrl Pts',(1.81678924961015,1.64445342667434,22.5515505423015));
#8903=CARTESIAN_POINT('Ctrl Pts',(1.87190370206598,1.58356307666765,22.5472711125876));
#8904=CARTESIAN_POINT('Ctrl Pts',(1.9238700145898,1.51999141522742,22.5429916828737));
#8905=CARTESIAN_POINT('Ctrl Pts',(1.97243944047894,1.45410897240995,22.5387122531598));
#8906=CARTESIAN_POINT('Ctrl Pts',(2.02045583006456,1.38897670075419,22.5344815512196));
#8907=CARTESIAN_POINT('Ctrl Pts',(2.06533293501886,1.32134104863914,22.5302508492793));
#8908=CARTESIAN_POINT('Ctrl Pts',(2.10679961964328,1.25153729975216,22.5260201473391));
#8909=CARTESIAN_POINT('Ctrl Pts',(2.14820672805173,1.18183383964535,22.5217955237534));
#8910=CARTESIAN_POINT('Ctrl Pts',(2.18621291196964,1.10996886568542,22.5175709001677));
#8911=CARTESIAN_POINT('Ctrl Pts',(2.22058880297282,1.03630865002264,22.513346276582));
#8912=CARTESIAN_POINT('Ctrl Pts',(2.25509999068188,0.962358522324323,22.5091050257138));
#8913=CARTESIAN_POINT('Ctrl Pts',(2.2859519663582,0.886599373156029,22.5048637748455));
#8914=CARTESIAN_POINT('Ctrl Pts',(2.3129580423386,0.80942902368347,22.5006225239772));
#8915=CARTESIAN_POINT('Ctrl Pts',(2.33980969688332,0.732699936250112,22.4964055246902));
#8916=CARTESIAN_POINT('Ctrl Pts',(2.36285915913093,0.654576186648453,22.4921885254033));
#8917=CARTESIAN_POINT('Ctrl Pts',(2.38197086714868,0.575469406706372,22.4879715261163));
#8918=CARTESIAN_POINT('Ctrl Pts',(2.40107623921712,0.496388852392389,22.4837559248569));
#8919=CARTESIAN_POINT('Ctrl Pts',(2.41624634033402,0.416326366608874,22.4795403235974));
#8920=CARTESIAN_POINT('Ctrl Pts',(2.42739592099354,0.335707153251063,22.475324722338));
#8921=CARTESIAN_POINT('Ctrl Pts',(2.43854522344221,0.255089951550876,22.4711092262687));
#8922=CARTESIAN_POINT('Ctrl Pts',(2.4456741422628,0.173916510721103,22.4668937301994));
#8923=CARTESIAN_POINT('Ctrl Pts',(2.44874905604841,0.0926191691931757,22.4626782341301));
#8924=CARTESIAN_POINT('Ctrl Pts',(2.45185655264164,0.0104603740362012,22.4584180692645));
#8925=CARTESIAN_POINT('Ctrl Pts',(2.45082358306201,-0.0718244797263049,
22.454157904399));
#8926=CARTESIAN_POINT('Ctrl Pts',(2.44566947993346,-0.153788962289195,22.4498977395334));
#8927=CARTESIAN_POINT('Ctrl Pts',(2.44056199143983,-0.235012143342264,22.4456761043644));
#8928=CARTESIAN_POINT('Ctrl Pts',(2.43140772829698,-0.315920264567787,22.4414544691955));
#8929=CARTESIAN_POINT('Ctrl Pts',(2.41827755582982,-0.396085739417284,22.4372328340265));
#8930=CARTESIAN_POINT('Ctrl Pts',(2.40496763018356,-0.477348686443557,22.4329534043126));
#8931=CARTESIAN_POINT('Ctrl Pts',(2.38757221436306,-0.557848015856419,22.4286739745987));
#8932=CARTESIAN_POINT('Ctrl Pts',(2.36621781198578,-0.637152663214418,22.4243945448848));
#8933=CARTESIAN_POINT('Ctrl Pts',(2.34486340960851,-0.716457310572394,22.4201151151709));
#8934=CARTESIAN_POINT('Ctrl Pts',(2.31955023421842,-0.794566829373144,22.415835685457));
#8935=CARTESIAN_POINT('Ctrl Pts',(2.29045513733628,-0.871071474593132,22.4115562557431));
#8936=CARTESIAN_POINT('Ctrl Pts',(2.26169133209575,-0.94670499882634,22.4073255538029));
#8937=CARTESIAN_POINT('Ctrl Pts',(2.22912314501233,-1.02105450572569,22.4030948518626));
#8938=CARTESIAN_POINT('Ctrl Pts',(2.19288567228929,-1.09371050935262,22.3988641499224));
#8939=CARTESIAN_POINT('Ctrl Pts',(2.15670026284348,-1.16626212629428,22.3946395263367));
#8940=CARTESIAN_POINT('Ctrl Pts',(2.11685624355647,-1.23712465959164,22.390414902751));
#8941=CARTESIAN_POINT('Ctrl Pts',(2.07353737771202,-1.30590696193532,22.3861902791654));
#8942=CARTESIAN_POINT('Ctrl Pts',(2.03004801738204,-1.37495997781279,22.3819490282971));
#8943=CARTESIAN_POINT('Ctrl Pts',(1.98305656789864,-1.44191590929972,22.3777077774288));
#8944=CARTESIAN_POINT('Ctrl Pts',(1.93279642548731,-1.50640241224697,22.3734665265605));
#8945=CARTESIAN_POINT('Ctrl Pts',(1.8828236718605,-1.57052017971494,22.3692495272735));
#8946=CARTESIAN_POINT('Ctrl Pts',(1.82961979357148,-1.63219631202487,22.3650325279866));
#8947=CARTESIAN_POINT('Ctrl Pts',(1.77345747833994,-1.69109397211395,22.3608155286996));
#8948=CARTESIAN_POINT('Ctrl Pts',(1.7173137821445,-1.74997210634027,22.3565999274402));
#8949=CARTESIAN_POINT('Ctrl Pts',(1.6582139173668,-1.80607326123896,22.3523843261808));
#8950=CARTESIAN_POINT('Ctrl Pts',(1.59646922228821,-1.85909555222062,22.3481687249213));
#8951=CARTESIAN_POINT('Ctrl Pts',(1.53472606789922,-1.91211652015918,22.343953228852));
#8952=CARTESIAN_POINT('Ctrl Pts',(1.47033856795391,-1.96205847477121,22.3397377327827));
#8953=CARTESIAN_POINT('Ctrl Pts',(1.403652011213,-2.00865907545748,22.3355222367134));
#8954=CARTESIAN_POINT('Ctrl Pts',(1.33625882157064,-2.05575347158441,22.3312620718478));
#8955=CARTESIAN_POINT('Ctrl Pts',(1.26651794977151,-2.09943498925007,22.3270019069823));
#8956=CARTESIAN_POINT('Ctrl Pts',(1.19481520194442,-2.13947818011835,22.3227417421167));
#8957=CARTESIAN_POINT('Ctrl Pts',(1.12376094665424,-2.17915921317233,22.3185201069477));
#8958=CARTESIAN_POINT('Ctrl Pts',(1.05078060854926,-2.21526731287303,22.3142984717787));
#8959=CARTESIAN_POINT('Ctrl Pts',(0.976272051563283,-2.24763055935276,22.3100768366098));
#8960=CARTESIAN_POINT('Ctrl Pts',(0.900743466087549,-2.28043686143263,22.3057974068959));
#8961=CARTESIAN_POINT('Ctrl Pts',(0.823644965086106,-2.3093948252912,22.301517977182));
#8962=CARTESIAN_POINT('Ctrl Pts',(0.745407459788122,-2.33437742640136,22.2972385474681));
#8963=CARTESIAN_POINT('Ctrl Pts',(0.667169954490138,-2.35936002751151,22.2929591177542));
#8964=CARTESIAN_POINT('Ctrl Pts',(0.587793935911065,-2.38036720367027,22.2886796880403));
#8965=CARTESIAN_POINT('Ctrl Pts',(0.507719649770369,-2.3973258033144,22.2844002583264));
#8966=CARTESIAN_POINT('Ctrl Pts',(0.428557130372018,-2.41409130367664,22.2801695563861));
#8967=CARTESIAN_POINT('Ctrl Pts',(0.348414420808609,-2.42696305918838,22.2759388544458));
#8968=CARTESIAN_POINT('Ctrl Pts',(0.267708942148447,-2.43583295246077,22.2717081525056));
#8969=CARTESIAN_POINT('Ctrl Pts',(0.187119415054472,-2.44469010213714,22.2674835289199));
#8970=CARTESIAN_POINT('Ctrl Pts',(0.105969183031884,-2.44955675817102,22.2632589053342));
#8971=CARTESIAN_POINT('Ctrl Pts',(0.0246865977424086,-2.4503756491387,22.2590342817485));
#8972=CARTESIAN_POINT('Ctrl Pts',(-0.0569158997213511,-2.45119776309921,
22.2547930308803));
#8973=CARTESIAN_POINT('Ctrl Pts',(-0.138651330262343,-2.44794008292565,
22.250551780012));
#8974=CARTESIAN_POINT('Ctrl Pts',(-0.220080279254641,-2.44059724671712,
22.2463105291437));
#8975=CARTESIAN_POINT('Ctrl Pts',(-0.301043615426415,-2.43329639703451,
22.2420935298567));
#8976=CARTESIAN_POINT('Ctrl Pts',(-0.381703497640066,-2.42195702478502,
22.2378765305698));
#8977=CARTESIAN_POINT('Ctrl Pts',(-0.461629091239207,-2.40662602664429,
22.2336595312828));
#8978=CARTESIAN_POINT('Ctrl Pts',(-0.541528187755521,-2.39130011106484,
22.2294439300234));
#8979=CARTESIAN_POINT('Ctrl Pts',(-0.620693022701401,-2.37198528500518,
22.2252283287639));
#8980=CARTESIAN_POINT('Ctrl Pts',(-0.698701222103427,-2.34877986457462,
22.2210127275045));
#8981=CARTESIAN_POINT('Ctrl Pts',(-0.776707474999328,-2.32557502317926,
22.2167972314352));
#8982=CARTESIAN_POINT('Ctrl Pts',(-0.853556704287774,-2.29847991407358,
22.2125817353659));
#8983=CARTESIAN_POINT('Ctrl Pts',(-0.928841401710857,-2.26764280707254,
22.2083662392966));
#8984=CARTESIAN_POINT('Ctrl Pts',(-1.00492384078945,-2.23647893984489,22.2041060744311));
#8985=CARTESIAN_POINT('Ctrl Pts',(-1.07940793955795,-2.20149346835282,22.1998459095655));
#8986=CARTESIAN_POINT('Ctrl Pts',(-1.15189527062315,-2.16288870160164,22.1955857446999));
#8987=CARTESIAN_POINT('Ctrl Pts',(-1.22372701323972,-2.1246330832985,22.1913641095309));
#8988=CARTESIAN_POINT('Ctrl Pts',(-1.29359758931343,-2.08282366793479,22.187142474362));
#8989=CARTESIAN_POINT('Ctrl Pts',(-1.36114704767515,-2.03770188315298,22.182920839193));
#8990=CARTESIAN_POINT('Ctrl Pts',(-1.42962126387374,-1.99196237729536,22.1786414094791));
#8991=CARTESIAN_POINT('Ctrl Pts',(-1.49570993162519,-1.94281941724681,22.1743619797652));
#8992=CARTESIAN_POINT('Ctrl Pts',(-1.55907295365847,-1.89056652228126,22.1700825500513));
#8993=CARTESIAN_POINT('Ctrl Pts',(-1.62243597569174,-1.83831362731572,22.1658031203375));
#8994=CARTESIAN_POINT('Ctrl Pts',(-1.68307303386764,-1.78295117658067,22.1615236906235));
#8995=CARTESIAN_POINT('Ctrl Pts',(-1.74068427121121,-1.72480970485381,22.1572442609096));
#8996=CARTESIAN_POINT('Ctrl Pts',(-1.7968404183609,-1.66813671547985,22.1530729169877));
#8997=CARTESIAN_POINT('Ctrl Pts',(-1.85034552545501,-1.60859737264155,22.1489015730657));
#8998=CARTESIAN_POINT('Ctrl Pts',(-1.90088679305711,-1.54647329429935,22.1447302291437));
#8999=CARTESIAN_POINT('Ctrl Pts',(-1.95136270988548,-1.48442954351477,22.1405642788449));
#9000=CARTESIAN_POINT('Ctrl Pts',(-1.9988820873696,-1.41980805190629,22.1363983285462));
#9001=CARTESIAN_POINT('Ctrl Pts',(-2.04316834329864,-1.35292770351644,22.1322323782474));
#9002=CARTESIAN_POINT('Ctrl Pts',(-2.08741180346071,-1.286111984564,22.1280704536905));
#9003=CARTESIAN_POINT('Ctrl Pts',(-2.12842807668247,-1.21704213571679,22.1239085291337));
#9004=CARTESIAN_POINT('Ctrl Pts',(-2.16598137453372,-1.14606934134589,22.1197466045769));
#9005=CARTESIAN_POINT('Ctrl Pts',(-2.20351064303067,-1.07514196057431,22.1155873431246));
#9006=CARTESIAN_POINT('Ctrl Pts',(-2.23758111056645,-1.00231447313506,22.1114280816724));
#9007=CARTESIAN_POINT('Ctrl Pts',(-2.26800165933677,-0.927964828668443,
22.1072688202201));
#9008=CARTESIAN_POINT('Ctrl Pts',(-2.29842423865581,-0.853610221419062,
22.1031092811403));
#9009=CARTESIAN_POINT('Ctrl Pts',(-2.32519621322486,-0.777733690127223,
22.0989497420605));
#9010=CARTESIAN_POINT('Ctrl Pts',(-2.34817408744077,-0.700734404087374,
22.0947902029807));
#9011=CARTESIAN_POINT('Ctrl Pts',(-2.37115120639363,-0.62373764894816,22.0906308006213));
#9012=CARTESIAN_POINT('Ctrl Pts',(-2.39033434371215,-0.545618674233663,
22.086471398262));
#9013=CARTESIAN_POINT('Ctrl Pts',(-2.40563014694972,-0.466791009003669,
22.0823119959027));
#9014=CARTESIAN_POINT('Ctrl Pts',(-2.42094168019324,-0.387882278423694,
22.0781483160678));
#9015=CARTESIAN_POINT('Ctrl Pts',(-2.43235781015019,-0.308263874393964,
22.073984636233));
#9016=CARTESIAN_POINT('Ctrl Pts',(-2.43983664962305,-0.228357993414225,
22.0698209563982));
#9017=CARTESIAN_POINT('Ctrl Pts',(-2.44701757026806,-0.151635155269717,
22.0658231363361));
#9018=CARTESIAN_POINT('Ctrl Pts',(-2.45056895731558,-0.0746477053578802,
22.0618253162741));
#9019=CARTESIAN_POINT('Ctrl Pts',(-2.45049898498603,0.00223037720034039,
22.0578274962121));
#9020=CARTESIAN_POINT('',(-2.45061844109802,-0.00106435975836244,21.2578274962121));
#9021=CARTESIAN_POINT('Ctrl Pts',(-2.45086617389337,0.00223071140564801,
22.0578274962121));
#9022=CARTESIAN_POINT('Ctrl Pts',(-2.45251442784572,0.180067490317817,22.0485810853057));
#9023=CARTESIAN_POINT('Ctrl Pts',(-2.35363098083641,1.17128616743177,21.996949341927));
#9024=CARTESIAN_POINT('Ctrl Pts',(-1.00509393446104,2.71753790621056,21.9029322660762));
#9025=CARTESIAN_POINT('Ctrl Pts',(1.7406206758319,2.31634750235136,21.7757762686594));
#9026=CARTESIAN_POINT('Ctrl Pts',(2.88987924261423,-0.209341949658435,21.6486202712428));
#9027=CARTESIAN_POINT('Ctrl Pts',(1.38860903771261,-2.54302792536034,21.5214642738259));
#9028=CARTESIAN_POINT('Ctrl Pts',(-1.38626047639343,-2.54430893964709,21.3943082764093));
#9029=CARTESIAN_POINT('Ctrl Pts',(-2.42529371805448,-0.93243122202057,21.306429350538));
#9030=CARTESIAN_POINT('Ctrl Pts',(-2.45429856883823,-0.060650494243286,
21.2609357571389));
#9031=CARTESIAN_POINT('Ctrl Pts',(-2.45397390661175,-0.00106581711394382,
21.2578274962121));
#9032=CARTESIAN_POINT('',(-2.45049945194367,-0.00163890932682275,20.457827496242));
#9033=CARTESIAN_POINT('Ctrl Pts',(-2.45049976887328,-0.00106430821629522,
21.2578274962121));
#9034=CARTESIAN_POINT('Ctrl Pts',(-2.45053457116059,0.0790656726311988,
21.2536415436539));
#9035=CARTESIAN_POINT('Ctrl Pts',(-2.44663482555755,0.159355808442185,21.2494555910958));
#9036=CARTESIAN_POINT('Ctrl Pts',(-2.43877965671865,0.239382614187571,21.2452696385376));
#9037=CARTESIAN_POINT('Ctrl Pts',(-2.43054835629895,0.323241369260646,21.2408832486642));
#9038=CARTESIAN_POINT('Ctrl Pts',(-2.41797325303175,0.406810428677306,21.2364968587908));
#9039=CARTESIAN_POINT('Ctrl Pts',(-2.40109181530039,0.48960018841653,21.2321104689173));
#9040=CARTESIAN_POINT('Ctrl Pts',(-2.38502088583582,0.56841506250072,21.2279346775315));
#9041=CARTESIAN_POINT('Ctrl Pts',(-2.36504768720049,0.646523207223542,21.2237588861456));
#9042=CARTESIAN_POINT('Ctrl Pts',(-2.3412575617958,0.723507622167163,21.2195830947598));
#9043=CARTESIAN_POINT('Ctrl Pts',(-2.31747992244979,0.80045163245106,21.2154094950049));
#9044=CARTESIAN_POINT('Ctrl Pts',(-2.28988947121437,0.876272629653963,21.21123589525));
#9045=CARTESIAN_POINT('Ctrl Pts',(-2.25862197796156,0.950566678707497,21.2070622954951));
#9046=CARTESIAN_POINT('Ctrl Pts',(-2.22736082903793,1.02484565313069,21.2028895425843));
#9047=CARTESIAN_POINT('Ctrl Pts',(-2.1924243042169,1.09759785649143,21.1987167896735));
#9048=CARTESIAN_POINT('Ctrl Pts',(-2.15399652100067,1.1684388034968,21.1945440367627));
#9049=CARTESIAN_POINT('Ctrl Pts',(-2.11556416357238,1.23928818298218,21.1903707871525));
#9050=CARTESIAN_POINT('Ctrl Pts',(-2.07363995182196,1.30822543773707,21.1861975375423));
#9051=CARTESIAN_POINT('Ctrl Pts',(-2.02845344465825,1.37489158585471,21.1820242879321));
#9052=CARTESIAN_POINT('Ctrl Pts',(-1.98321910359144,1.44162830596983,21.1778466205691));
#9053=CARTESIAN_POINT('Ctrl Pts',(-1.93471584461374,1.50608872883422,21.1736689532061));
#9054=CARTESIAN_POINT('Ctrl Pts',(-1.88321550237887,1.56794439365683,21.1694912858431));
#9055=CARTESIAN_POINT('Ctrl Pts',(-1.8316833021961,1.62983832219696,21.1653110341884));
#9056=CARTESIAN_POINT('Ctrl Pts',(-1.77715065342666,1.68912393887092,21.1611307825337));
#9057=CARTESIAN_POINT('Ctrl Pts',(-1.71992671606892,1.74550919257172,21.1569505308789));
#9058=CARTESIAN_POINT('Ctrl Pts',(-1.66261026310704,1.8019856059524,21.1527635208898));
#9059=CARTESIAN_POINT('Ctrl Pts',(-1.60259419652624,1.85555198760815,21.1485765109006));
#9060=CARTESIAN_POINT('Ctrl Pts',(-1.5402206393873,1.90595661860531,21.1443895009114));
#9061=CARTESIAN_POINT('Ctrl Pts',(-1.51840549222494,1.92358563470292,21.1429250944662));
#9062=CARTESIAN_POINT('Ctrl Pts',(-1.49630221864538,1.94082828205214,21.141460688021));
#9063=CARTESIAN_POINT('Ctrl Pts',(-1.47392622329026,1.95767508496617,21.1399962815758));
#9064=CARTESIAN_POINT('Ctrl Pts',(-1.40928148802951,2.00634586349842,21.1357655796355));
#9065=CARTESIAN_POINT('Ctrl Pts',(-1.34210184128882,2.05190276253568,21.1315348776953));
#9066=CARTESIAN_POINT('Ctrl Pts',(-1.27271981542071,2.09407127897678,21.127304175755));
#9067=CARTESIAN_POINT('Ctrl Pts',(-1.20343747243289,2.13617921086268,21.1230795521694));
#9068=CARTESIAN_POINT('Ctrl Pts',(-1.13195942866314,2.17490818912302,21.1188549285837));
#9069=CARTESIAN_POINT('Ctrl Pts',(-1.05864962455588,2.21002516330192,21.114630304998));
#9070=CARTESIAN_POINT('Ctrl Pts',(-0.985051287563485,2.24528035094355,21.1103890541297));
#9071=CARTESIAN_POINT('Ctrl Pts',(-0.909607119530442,2.27689475581923,21.1061478032615));
#9072=CARTESIAN_POINT('Ctrl Pts',(-0.832713038729248,2.30467768790569,21.1019065523932));
#9073=CARTESIAN_POINT('Ctrl Pts',(-0.756258640255835,2.33230175647332,21.0976895531062));
#9074=CARTESIAN_POINT('Ctrl Pts',(-0.678371307079352,2.35613789064809,21.0934725538192));
#9075=CARTESIAN_POINT('Ctrl Pts',(-0.599461283012908,2.37604638426284,21.0892555545323));
#9076=CARTESIAN_POINT('Ctrl Pts',(-0.520577419345773,2.39594827777642,21.0850399532728));
#9077=CARTESIAN_POINT('Ctrl Pts',(-0.440671988646477,2.41192500280039,21.0808243520134));
#9078=CARTESIAN_POINT('Ctrl Pts',(-0.360169313484261,2.42388702616774,21.076608750754));
#9079=CARTESIAN_POINT('Ctrl Pts',(-0.279668647071809,2.43584875105169,21.0723932546847));
#9080=CARTESIAN_POINT('Ctrl Pts',(-0.198571225996181,2.44379590617561,21.0681777586154));
#9081=CARTESIAN_POINT('Ctrl Pts',(-0.117309027646915,2.4476905118974,21.0639622625461));
#9082=CARTESIAN_POINT('Ctrl Pts',(-0.0351857480572538,2.45162638615479,
21.0597020976805));
#9083=CARTESIAN_POINT('Ctrl Pts',(0.0471053385266302,2.45142327603031,21.0554419328149));
#9084=CARTESIAN_POINT('Ctrl Pts',(0.129117630039666,2.44709601111459,21.0511817679493));
#9085=CARTESIAN_POINT('Ctrl Pts',(0.210388187650214,2.4428078827604,21.0469601327804));
#9086=CARTESIAN_POINT('Ctrl Pts',(0.291384511414774,2.43447000829635,21.0427384976114));
#9087=CARTESIAN_POINT('Ctrl Pts',(0.371678321881904,2.42214893741963,21.0385168624424));
#9088=CARTESIAN_POINT('Ctrl Pts',(0.453071361451193,2.40965919003349,21.0342374327285));
#9089=CARTESIAN_POINT('Ctrl Pts',(0.533742022627232,2.39307645947121,21.0299580030146));
#9090=CARTESIAN_POINT('Ctrl Pts',(0.613257987154518,2.37252289582023,21.0256785733008));
#9091=CARTESIAN_POINT('Ctrl Pts',(0.692773951681803,2.35196933216924,21.0213991435869));
#9092=CARTESIAN_POINT('Ctrl Pts',(0.771134770927176,2.32744514445989,21.017119713873));
#9093=CARTESIAN_POINT('Ctrl Pts',(0.847928937232249,2.29912304311974,21.0128402841591));
#9094=CARTESIAN_POINT('Ctrl Pts',(0.923848685915814,2.27112343169884,21.0086095822188));
#9095=CARTESIAN_POINT('Ctrl Pts',(0.998522848093135,2.23930668313396,21.0043788802785));
#9096=CARTESIAN_POINT('Ctrl Pts',(1.0715405962618,2.20380375727126,21.0001481783383));
#9097=CARTESIAN_POINT('Ctrl Pts',(1.14445343801784,2.16835183934407,20.9959235547526));
#9098=CARTESIAN_POINT('Ctrl Pts',(1.21571417750784,2.12922446394462,20.9916989311669));
#9099=CARTESIAN_POINT('Ctrl Pts',(1.28492983413974,2.08660144046188,20.9874743075812));
#9100=CARTESIAN_POINT('Ctrl Pts',(1.35441790990188,2.04381066119166,20.9832330567129));
#9101=CARTESIAN_POINT('Ctrl Pts',(1.4218443249558,1.99749682266795,20.9789918058446));
#9102=CARTESIAN_POINT('Ctrl Pts',(1.48683440038694,1.94788955431924,20.9747505549763));
#9103=CARTESIAN_POINT('Ctrl Pts',(1.55145286089868,1.8985659416042,20.9705335556894));
#9104=CARTESIAN_POINT('Ctrl Pts',(1.61366239489633,1.84598674570367,20.9663165564024));
#9105=CARTESIAN_POINT('Ctrl Pts',(1.6731234325085,1.79042124361586,20.9620995571155));
#9106=CARTESIAN_POINT('Ctrl Pts',(1.73256475748587,1.73487416270761,20.957883955856));
#9107=CARTESIAN_POINT('Ctrl Pts',(1.78925905601964,1.67634305891218,20.9536683545966));
#9108=CARTESIAN_POINT('Ctrl Pts',(1.84290131916034,1.61513621030459,20.9494527533371));
#9109=CARTESIAN_POINT('Ctrl Pts',(1.89654224378802,1.55393088896597,20.9452372572678));
#9110=CARTESIAN_POINT('Ctrl Pts',(1.94713097873232,1.49005030602837,20.9410217611985));
#9111=CARTESIAN_POINT('Ctrl Pts',(1.99440171464731,1.42383708710367,20.9368062651292));
#9112=CARTESIAN_POINT('Ctrl Pts',(2.04217334697813,1.35692225092259,20.9325461002637));
#9113=CARTESIAN_POINT('Ctrl Pts',(2.08655594974683,1.28762543457208,20.9282859353981));
#9114=CARTESIAN_POINT('Ctrl Pts',(2.12732019539462,1.21633015101419,20.9240257705325));
#9115=CARTESIAN_POINT('Ctrl Pts',(2.16771576187937,1.14567967481268,20.9198041353635));
#9116=CARTESIAN_POINT('Ctrl Pts',(2.20455800040299,1.07306718226124,20.9155825001946));
#9117=CARTESIAN_POINT('Ctrl Pts',(2.23767098755545,0.998888783325058,20.9113608650256));
#9118=CARTESIAN_POINT('Ctrl Pts',(2.27123729432136,0.923694875791697,20.9070814353117));
#9119=CARTESIAN_POINT('Ctrl Pts',(2.30097129047062,0.846892323748042,20.9028020055978));
#9120=CARTESIAN_POINT('Ctrl Pts',(2.32674161238323,0.768910735524134,20.898522575884));
#9121=CARTESIAN_POINT('Ctrl Pts',(2.35251193429585,0.690929147300226,20.8942431461701));
#9122=CARTESIAN_POINT('Ctrl Pts',(2.37431851482032,0.611769013259261,20.8899637164562));
#9123=CARTESIAN_POINT('Ctrl Pts',(2.39208376642678,0.531869819032303,20.8856842867423));
#9124=CARTESIAN_POINT('Ctrl Pts',(2.40964673379992,0.452880397861552,20.8814535848021));
#9125=CARTESIAN_POINT('Ctrl Pts',(2.42332603911261,0.37287156964722,20.8772228828618));
#9126=CARTESIAN_POINT('Ctrl Pts',(2.43300936096408,0.292259643914732,20.8729921809216));
#9127=CARTESIAN_POINT('Ctrl Pts',(2.44267877054647,0.211763535338661,20.8687675573359));
#9128=CARTESIAN_POINT('Ctrl Pts',(2.44836354387018,0.130666507954962,20.8645429337503));
#9129=CARTESIAN_POINT('Ctrl Pts',(2.45000209268374,0.0493963140860758,20.8603183101646));
#9130=CARTESIAN_POINT('Ctrl Pts',(2.45164709050126,-0.0321937431872997,
20.8560770592963));
#9131=CARTESIAN_POINT('Ctrl Pts',(2.44921384221654,-0.113957869725936,20.851835808428));
#9132=CARTESIAN_POINT('Ctrl Pts',(2.44269255489614,-0.19545672732079,20.8475945575597));
#9133=CARTESIAN_POINT('Ctrl Pts',(2.43620855646406,-0.276489572355669,20.8433775582728));
#9134=CARTESIAN_POINT('Ctrl Pts',(2.425683180625,-0.357259705605165,20.8391605589858));
#9135=CARTESIAN_POINT('Ctrl Pts',(2.41115897688995,-0.437335841388503,20.8349435596989));
#9136=CARTESIAN_POINT('Ctrl Pts',(2.39663958824617,-0.517385430181111,20.8307279584394));
#9137=CARTESIAN_POINT('Ctrl Pts',(2.37812408725206,-0.596741021166517,20.82651235718));
#9138=CARTESIAN_POINT('Ctrl Pts',(2.35570652555985,-0.67497927037408,20.8222967559206));
#9139=CARTESIAN_POINT('Ctrl Pts',(2.33328952324378,-0.753215567335034,20.8180812598513));
#9140=CARTESIAN_POINT('Ctrl Pts',(2.30697078296014,-0.83033413118005,20.813865763782));
#9141=CARTESIAN_POINT('Ctrl Pts',(2.27689445744093,-0.905925979136689,20.8096502677127));
#9142=CARTESIAN_POINT('Ctrl Pts',(2.24649943318818,-0.982318823418311,20.8053901028471));
#9143=CARTESIAN_POINT('Ctrl Pts',(2.21226688043535,-1.05715194788155,20.8011299379815));
#9144=CARTESIAN_POINT('Ctrl Pts',(2.17439507993339,-1.13002490519522,20.7968697731159));
#9145=CARTESIAN_POINT('Ctrl Pts',(2.13686579880114,-1.2022387863869,20.792648137947));
#9146=CARTESIAN_POINT('Ctrl Pts',(2.09576312380993,-1.2725274392583,20.788426502778));
#9147=CARTESIAN_POINT('Ctrl Pts',(2.05132484037468,-1.34052849625131,20.7842048676091));
#9148=CARTESIAN_POINT('Ctrl Pts',(2.00627819305501,-1.40946049350526,20.7799254378951));
#9149=CARTESIAN_POINT('Ctrl Pts',(1.95780420739424,-1.47604138597227,20.7756460081812));
#9150=CARTESIAN_POINT('Ctrl Pts',(1.90619295800774,-1.53992813366134,20.7713665784673));
#9151=CARTESIAN_POINT('Ctrl Pts',(1.85458170862125,-1.6038148813504,20.7670871487534));
#9152=CARTESIAN_POINT('Ctrl Pts',(1.79983357142897,-1.66500716231496,20.7628077190395));
#9153=CARTESIAN_POINT('Ctrl Pts',(1.74227604047368,-1.72320180152858,20.7585282893256));
#9154=CARTESIAN_POINT('Ctrl Pts',(1.6853738889797,-1.78073380684068,20.7542975873853));
#9155=CARTESIAN_POINT('Ctrl Pts',(1.62551200269765,-1.83555251310833,20.7500668854451));
#9156=CARTESIAN_POINT('Ctrl Pts',(1.56297958485594,-1.88733809035995,20.7458361835048));
#9157=CARTESIAN_POINT('Ctrl Pts',(1.50053700889227,-1.93904926598637,20.7416115599191));
#9158=CARTESIAN_POINT('Ctrl Pts',(1.43543187664608,-1.98773567326295,20.7373869363334));
#9159=CARTESIAN_POINT('Ctrl Pts',(1.36799047949149,-2.03311394122923,20.7331623127477));
#9160=CARTESIAN_POINT('Ctrl Pts',(1.30028364634082,-2.07867080908024,20.7289210618795));
#9161=CARTESIAN_POINT('Ctrl Pts',(1.23022245239336,-2.12089310400238,20.7246798110112));
#9162=CARTESIAN_POINT('Ctrl Pts',(1.15817097254333,-2.1595347296022,20.7204385601429));
#9163=CARTESIAN_POINT('Ctrl Pts',(1.08653148490456,-2.19795540139495,20.7162215608559));
#9164=CARTESIAN_POINT('Ctrl Pts',(1.01292482457161,-2.23283601945659,20.712004561569));
#9165=CARTESIAN_POINT('Ctrl Pts',(0.937736635034463,-2.26397885443178,20.707787562282));
#9166=CARTESIAN_POINT('Ctrl Pts',(0.862573372027066,-2.29511136487586,20.7035719610226));
#9167=CARTESIAN_POINT('Ctrl Pts',(0.785830050330809,-2.32250837516431,20.6993563597631));
#9168=CARTESIAN_POINT('Ctrl Pts',(0.707913520252535,-2.34601975649048,20.6951407585037));
#9169=CARTESIAN_POINT('Ctrl Pts',(0.629998934392989,-2.36953055114694,20.6909252624344));
#9170=CARTESIAN_POINT('Ctrl Pts',(0.550911643902007,-2.38915577630415,20.6867097663651));
#9171=CARTESIAN_POINT('Ctrl Pts',(0.471073550119092,-2.40479520133798,20.6824942702958));
#9172=CARTESIAN_POINT('Ctrl Pts',(0.390389465380692,-2.42060034691324,20.6782341054303));
#9173=CARTESIAN_POINT('Ctrl Pts',(0.30893904342235,-2.43233461074544,20.6739739405647));
#9174=CARTESIAN_POINT('Ctrl Pts',(0.227166314897859,-2.43994789193862,20.6697137756991));
#9175=CARTESIAN_POINT('Ctrl Pts',(0.146133153625253,-2.44749231724854,20.6654921405301));
#9176=CARTESIAN_POINT('Ctrl Pts',(0.0647839647791666,-2.45099004336908,
20.6612705053612));
#9177=CARTESIAN_POINT('Ctrl Pts',(-0.0164478485492509,-2.45044480008796,
20.6570488701922));
#9178=CARTESIAN_POINT('Ctrl Pts',(-0.0987917323190438,-2.44989209237989,
20.6527694404783));
#9179=CARTESIAN_POINT('Ctrl Pts',(-0.181014508631477,-2.44518490819373,
20.6484900107644));
#9180=CARTESIAN_POINT('Ctrl Pts',(-0.262670714200303,-2.43638140402965,
20.6442105810505));
#9181=CARTESIAN_POINT('Ctrl Pts',(-0.34432691976913,-2.42757789986558,20.6399311513366));
#9182=CARTESIAN_POINT('Ctrl Pts',(-0.425416080387844,-2.41467821747542,
20.6356517216227));
#9183=CARTESIAN_POINT('Ctrl Pts',(-0.505505990217785,-2.39779355738853,
20.6313722919088));
#9184=CARTESIAN_POINT('Ctrl Pts',(-0.584683955406296,-2.38110115466991,
20.6271415899686));
#9185=CARTESIAN_POINT('Ctrl Pts',(-0.663183129487585,-2.3604513204164,20.6229108880283));
#9186=CARTESIAN_POINT('Ctrl Pts',(-0.740578034953068,-2.33591404468252,
20.618680186088));
#9187=CARTESIAN_POINT('Ctrl Pts',(-0.817861745235176,-2.31141202226226,
20.6144555625024));
#9188=CARTESIAN_POINT('Ctrl Pts',(-0.894043898284959,-2.28303379019962,
20.6102309389167));
#9189=CARTESIAN_POINT('Ctrl Pts',(-0.968709589820252,-2.25090026002715,
20.606006315331));
#9190=CARTESIAN_POINT('Ctrl Pts',(-1.04366915074491,-2.2186402586375,20.6017650644627));
#9191=CARTESIAN_POINT('Ctrl Pts',(-1.11709982321976,-2.18259543340949,20.5975238135944));
#9192=CARTESIAN_POINT('Ctrl Pts',(-1.18859758538988,-2.1429386435466,20.5932825627261));
#9193=CARTESIAN_POINT('Ctrl Pts',(-1.25968652152083,-2.10350861222599,20.5890655634391));
#9194=CARTESIAN_POINT('Ctrl Pts',(-1.32886418144608,-2.06050803863655,20.5848485641522));
#9195=CARTESIAN_POINT('Ctrl Pts',(-1.39575553076863,-2.01415410242831,20.5806315648652));
#9196=CARTESIAN_POINT('Ctrl Pts',(-1.46262470414545,-1.96781553356404,20.5764159636058));
#9197=CARTESIAN_POINT('Ctrl Pts',(-1.52720869015642,-1.91812607443359,20.5722003623463));
#9198=CARTESIAN_POINT('Ctrl Pts',(-1.58916099330204,-1.86534650597879,20.5679847610869));
#9199=CARTESIAN_POINT('Ctrl Pts',(-1.65111175057791,-1.81256825451034,20.5637692650176));
#9200=CARTESIAN_POINT('Ctrl Pts',(-1.71043060224588,-1.75670034944357,20.5595537689482));
#9201=CARTESIAN_POINT('Ctrl Pts',(-1.76680485627142,-1.69804324145639,20.5553382728789));
#9202=CARTESIAN_POINT('Ctrl Pts',(-1.82377647061365,-1.63876458327385,20.5510781080133));
#9203=CARTESIAN_POINT('Ctrl Pts',(-1.87774036455432,-1.57663759770729,20.5468179431478));
#9204=CARTESIAN_POINT('Ctrl Pts',(-1.92841401193213,-1.51200848165075,20.5425577782822));
#9205=CARTESIAN_POINT('Ctrl Pts',(-1.97862935773705,-1.44796388293363,20.5383361431132));
#9206=CARTESIAN_POINT('Ctrl Pts',(-2.02561351182713,-1.38146265077644,20.5341145079442));
#9207=CARTESIAN_POINT('Ctrl Pts',(-2.06913496048165,-1.31287119143982,20.5298928727753));
#9208=CARTESIAN_POINT('Ctrl Pts',(-2.11325222147361,-1.24334070918508,20.5256134430614));
#9209=CARTESIAN_POINT('Ctrl Pts',(-2.15381100610034,-1.17166276615519,20.5213340133475));
#9210=CARTESIAN_POINT('Ctrl Pts',(-2.19061903077653,-1.09824337557742,20.5170545836337));
#9211=CARTESIAN_POINT('Ctrl Pts',(-2.22742705545273,-1.02482398499965,20.5127751539198));
#9212=CARTESIAN_POINT('Ctrl Pts',(-2.26048418261629,-0.949663622312802,
20.5084957242059));
#9213=CARTESIAN_POINT('Ctrl Pts',(-2.28964990358769,-0.873185873111157,
20.5042162944921));
#9214=CARTESIAN_POINT('Ctrl Pts',(-2.32256423751074,-0.786878588700953,
20.4993868380648));
#9215=CARTESIAN_POINT('Ctrl Pts',(-2.35062682283035,-0.698624244658884,
20.4945573816374));
#9216=CARTESIAN_POINT('Ctrl Pts',(-2.37363404666454,-0.608943070011404,
20.4897279252101));
#9217=CARTESIAN_POINT('Ctrl Pts',(-2.3965458373727,-0.519633889608201,20.4849185011921));
#9218=CARTESIAN_POINT('Ctrl Pts',(-2.4144439916773,-0.428909874618249,20.480109077174));
#9219=CARTESIAN_POINT('Ctrl Pts',(-2.42717418291953,-0.337306590165269,
20.475299653156));
#9220=CARTESIAN_POINT('Ctrl Pts',(-2.43981461087043,-0.246349219992158,
20.4705241414116));
#9221=CARTESIAN_POINT('Ctrl Pts',(-2.44735958946865,-0.154525137022721,
20.4657486296672));
#9222=CARTESIAN_POINT('Ctrl Pts',(-2.44970596636031,-0.0623773066003385,
20.4609731179229));
#9223=CARTESIAN_POINT('Ctrl Pts',(-2.45022115121845,-0.0421447654798911,
20.4599245773626));
#9224=CARTESIAN_POINT('Ctrl Pts',(-2.450485903419,-0.0218966818199169,20.4588760368023));
#9225=CARTESIAN_POINT('Ctrl Pts',(-2.45049945194367,-0.00163890932682414,
20.457827496242));
#9226=CARTESIAN_POINT('',(-2.45049932159731,0.0018234174231849,19.6578274961832));
#9227=CARTESIAN_POINT('Ctrl Pts',(-2.45049945194405,-0.0016389087485609,
20.4578274962121));
#9228=CARTESIAN_POINT('Ctrl Pts',(-2.45055421052199,0.0802362202531978,
20.4535896465835));
#9229=CARTESIAN_POINT('Ctrl Pts',(-2.44650126866439,0.16213599296622,20.4493517969549));
#9230=CARTESIAN_POINT('Ctrl Pts',(-2.43835979033716,0.243622213410317,20.4451139473264));
#9231=CARTESIAN_POINT('Ctrl Pts',(-2.43021791027475,0.325112454731139,20.4408758885843));
#9232=CARTESIAN_POINT('Ctrl Pts',(-2.41798713907075,0.406188647605483,20.4366378298422));
#9233=CARTESIAN_POINT('Ctrl Pts',(-2.40173848544128,0.486418027575255,20.4323997711001));
#9234=CARTESIAN_POINT('Ctrl Pts',(-2.38548424781655,0.566674979089633,20.4281602559111));
#9235=CARTESIAN_POINT('Ctrl Pts',(-2.36520947641849,0.646084091095377,20.4239207407222));
#9236=CARTESIAN_POINT('Ctrl Pts',(-2.34103593495705,0.724224413589979,20.4196812255333));
#9237=CARTESIAN_POINT('Ctrl Pts',(-2.31683056137721,0.802467632551038,20.4154361276808));
#9238=CARTESIAN_POINT('Ctrl Pts',(-2.28871630842795,0.87943828998129,20.4111910298283));
#9239=CARTESIAN_POINT('Ctrl Pts',(-2.25686416502691,0.9547326278165,20.4069459319758));
#9240=CARTESIAN_POINT('Ctrl Pts',(-2.22498765302891,1.03008456985588,20.4026975863959));
#9241=CARTESIAN_POINT('Ctrl Pts',(-2.18936775799366,1.10375722819108,20.398449240816));
#9242=CARTESIAN_POINT('Ctrl Pts',(-2.15022167574432,1.17537100319827,20.3942008952361));
#9243=CARTESIAN_POINT('Ctrl Pts',(-2.11100646739711,1.24711123736905,20.3899450477165));
#9244=CARTESIAN_POINT('Ctrl Pts',(-2.06825288420797,1.31678494324426,20.3856892001968));
#9245=CARTESIAN_POINT('Ctrl Pts',(-2.02222143977409,1.38404143670557,20.3814333526771));
#9246=CARTESIAN_POINT('Ctrl Pts',(-2.00645504894317,1.4070776932226,20.3799756674765));
#9247=CARTESIAN_POINT('Ctrl Pts',(-1.99030445808792,1.42983066454623,20.3785179822759));
#9248=CARTESIAN_POINT('Ctrl Pts',(-1.9737811738493,1.45228720567182,20.3770602970754));
#9249=CARTESIAN_POINT('Ctrl Pts',(-1.92582494114561,1.51746378294222,20.3728295951351));
#9250=CARTESIAN_POINT('Ctrl Pts',(-1.8745467411694,1.58038502095646,20.3685988931949));
#9251=CARTESIAN_POINT('Ctrl Pts',(-1.82018633211609,1.6406925264588,20.3643681912547));
#9252=CARTESIAN_POINT('Ctrl Pts',(-1.7659040240129,1.70091338666983,20.360143567669));
#9253=CARTESIAN_POINT('Ctrl Pts',(-1.70854861038468,1.75852762992404,20.3559189440833));
#9254=CARTESIAN_POINT('Ctrl Pts',(-1.64840183330696,1.81320755732769,20.3516943204977));
#9255=CARTESIAN_POINT('Ctrl Pts',(-1.58801833041419,1.86810269410764,20.3474530696294));
#9256=CARTESIAN_POINT('Ctrl Pts',(-1.52482172567997,1.92003998548779,20.3432118187611));
#9257=CARTESIAN_POINT('Ctrl Pts',(-1.45913655136706,1.96872313301404,20.3389705678928));
#9258=CARTESIAN_POINT('Ctrl Pts',(-1.39382696656726,2.01712790905287,20.3347535686059));
#9259=CARTESIAN_POINT('Ctrl Pts',(-1.3260575717552,2.06231537510799,20.3305365693189));
#9260=CARTESIAN_POINT('Ctrl Pts',(-1.25618125472393,2.10403396010621,20.326319570032));
#9261=CARTESIAN_POINT('Ctrl Pts',(-1.18632810322037,2.14573871448086,20.3221039687726));
#9262=CARTESIAN_POINT('Ctrl Pts',(-1.11436981557281,2.1839766333117,20.3178883675131));
#9263=CARTESIAN_POINT('Ctrl Pts',(-1.04068716598189,2.21854016699283,20.3136727662537));
#9264=CARTESIAN_POINT('Ctrl Pts',(-0.967006354963416,2.25310283822452,20.3094572701844));
#9265=CARTESIAN_POINT('Ctrl Pts',(-0.891601689049961,2.28399111007847,20.3052417741152));
#9266=CARTESIAN_POINT('Ctrl Pts',(-0.814876071396342,2.31104462057003,20.3010262780459));
#9267=CARTESIAN_POINT('Ctrl Pts',(-0.737337443617486,2.33838479904322,20.2967661131803));
#9268=CARTESIAN_POINT('Ctrl Pts',(-0.658450154465879,2.36180828715304,20.2925059483147));
#9269=CARTESIAN_POINT('Ctrl Pts',(-0.578646273070949,2.38120111302282,20.2882457834491));
#9270=CARTESIAN_POINT('Ctrl Pts',(-0.499564152321246,2.40041854669026,20.2840241482801));
#9271=CARTESIAN_POINT('Ctrl Pts',(-0.41958242575381,2.41567790543055,20.2798025131112));
#9272=CARTESIAN_POINT('Ctrl Pts',(-0.339130454732167,2.42692002024648,20.2755808779422));
#9273=CARTESIAN_POINT('Ctrl Pts',(-0.257577089375796,2.43831604057163,20.2713014482283));
#9274=CARTESIAN_POINT('Ctrl Pts',(-0.175540999427799,2.44558394767251,20.2670220185144));
#9275=CARTESIAN_POINT('Ctrl Pts',(-0.0934713727955725,2.44871667460074,
20.2627425888004));
#9276=CARTESIAN_POINT('Ctrl Pts',(-0.0114017461633575,2.45184940152897,
20.2584631590865));
#9277=CARTESIAN_POINT('Ctrl Pts',(0.0707009274014986,2.4508470197602,20.2541837293726));
#9278=CARTESIAN_POINT('Ctrl Pts',(0.152392883928499,2.44575686831867,20.2499042996586));
#9279=CARTESIAN_POINT('Ctrl Pts',(0.233154654090854,2.44072467594271,20.2456735977184));
#9280=CARTESIAN_POINT('Ctrl Pts',(0.313818783241487,2.43167844720005,20.2414428957781));
#9281=CARTESIAN_POINT('Ctrl Pts',(0.393954141627136,2.41862572224287,20.2372121938379));
#9282=CARTESIAN_POINT('Ctrl Pts',(0.473974367552768,2.40559175045987,20.2329875702522));
#9283=CARTESIAN_POINT('Ctrl Pts',(0.55346687639895,2.38856278878805,20.2287629466665));
#9284=CARTESIAN_POINT('Ctrl Pts',(0.632003614358155,2.3675982939338,20.2245383230808));
#9285=CARTESIAN_POINT('Ctrl Pts',(0.710849457379773,2.34655128697554,20.2202970722125));
#9286=CARTESIAN_POINT('Ctrl Pts',(0.788731516291807,2.32153773094163,20.2160558213442));
#9287=CARTESIAN_POINT('Ctrl Pts',(0.865224970328303,2.29267005928031,20.2118145704759));
#9288=CARTESIAN_POINT('Ctrl Pts',(0.94128103283111,2.26396745370656,20.207597571189));
#9289=CARTESIAN_POINT('Ctrl Pts',(1.01596388804184,2.23145485462087,20.203380571902));
#9290=CARTESIAN_POINT('Ctrl Pts',(1.08887096805654,2.19529275153078,20.1991635726151));
#9291=CARTESIAN_POINT('Ctrl Pts',(1.1617538777791,2.15914263696905,20.1949479713556));
#9292=CARTESIAN_POINT('Ctrl Pts',(1.23286176508385,2.11934562752412,20.1907323700962));
#9293=CARTESIAN_POINT('Ctrl Pts',(1.3018139754152,2.07610949215442,20.1865167688368));
#9294=CARTESIAN_POINT('Ctrl Pts',(1.37076446521094,2.03287443563788,20.1823012727675));
#9295=CARTESIAN_POINT('Ctrl Pts',(1.43755899154895,1.98620067179806,20.1780857766982));
#9296=CARTESIAN_POINT('Ctrl Pts',(1.50184459234321,1.9363401226152,20.1738702806289));
#9297=CARTESIAN_POINT('Ctrl Pts',(1.56681138471229,1.88595123449486,20.1696101157633));
#9298=CARTESIAN_POINT('Ctrl Pts',(1.6292153714371,1.83230790661776,20.1653499508977));
#9299=CARTESIAN_POINT('Ctrl Pts',(1.68872680245974,1.77571169863075,20.1610897860321));
#9300=CARTESIAN_POINT('Ctrl Pts',(1.74770000140563,1.71962735691947,20.1568681508632));
#9301=CARTESIAN_POINT('Ctrl Pts',(1.80383247632666,1.66064371619445,20.1526465156942));
#9302=CARTESIAN_POINT('Ctrl Pts',(1.85684201911466,1.59908973045611,20.1484248805252));
#9303=CARTESIAN_POINT('Ctrl Pts',(1.91057726705718,1.5366930654117,20.1441454508113));
#9304=CARTESIAN_POINT('Ctrl Pts',(1.96110312556303,1.47165553663225,20.1398660210974));
#9305=CARTESIAN_POINT('Ctrl Pts',(2.00817045738786,1.40435097610058,20.1355865913835));
#9306=CARTESIAN_POINT('Ctrl Pts',(2.05523778921268,1.3370464155689,20.1313071616696));
#9307=CARTESIAN_POINT('Ctrl Pts',(2.09884638929285,1.2674752737451,20.1270277319558));
#9308=CARTESIAN_POINT('Ctrl Pts',(2.13879579919847,1.19603627843431,20.1227483022419));
#9309=CARTESIAN_POINT('Ctrl Pts',(2.17829032470766,1.12541072403142,20.1185176003016));
#9310=CARTESIAN_POINT('Ctrl Pts',(2.21435715494338,1.05269401520267,20.1142868983613));
#9311=CARTESIAN_POINT('Ctrl Pts',(2.24676921058953,0.978252709859208,20.1100561964211));
#9312=CARTESIAN_POINT('Ctrl Pts',(2.27913469903013,0.903918356188484,20.1058315728354));
#9313=CARTESIAN_POINT('Ctrl Pts',(2.30785565738889,0.827864749770065,20.1016069492497));
#9314=CARTESIAN_POINT('Ctrl Pts',(2.33275032093671,0.750483970628084,20.097382325664));
#9315=CARTESIAN_POINT('Ctrl Pts',(2.35774296495488,0.672798636049037,20.0931410747957));
#9316=CARTESIAN_POINT('Ctrl Pts',(2.37887889886291,0.593776073551608,20.0888998239274));
#9317=CARTESIAN_POINT('Ctrl Pts',(2.39602264893294,0.513834327191517,20.0846585730591));
#9318=CARTESIAN_POINT('Ctrl Pts',(2.41306837060006,0.434349689788944,20.0804415737722));
#9319=CARTESIAN_POINT('Ctrl Pts',(2.42616734086377,0.35395681112558,20.0762245744852));
#9320=CARTESIAN_POINT('Ctrl Pts',(2.4352365374527,0.273081044115823,20.0720075751983));
#9321=CARTESIAN_POINT('Ctrl Pts',(2.44430272740455,0.192232089192166,20.0677919739388));
#9322=CARTESIAN_POINT('Ctrl Pts',(2.44934174488293,0.110901025627287,20.0635763726794));
#9323=CARTESIAN_POINT('Ctrl Pts',(2.45032218231688,0.0295203801778828,20.0593607714199));
#9324=CARTESIAN_POINT('Ctrl Pts',(2.45130259528638,-0.0518582346140824,
20.0551452753506));
#9325=CARTESIAN_POINT('Ctrl Pts',(2.44822462504784,-0.133285963790905,20.0509297792814));
#9326=CARTESIAN_POINT('Ctrl Pts',(2.44110897904662,-0.214329658278944,20.0467142832121));
#9327=CARTESIAN_POINT('Ctrl Pts',(2.43391793329733,-0.296232118667681,20.0424541183465));
#9328=CARTESIAN_POINT('Ctrl Pts',(2.42260315950338,-0.377741873168812,20.0381939534809));
#9329=CARTESIAN_POINT('Ctrl Pts',(2.40723966561878,-0.458418413975253,20.0339337886153));
#9330=CARTESIAN_POINT('Ctrl Pts',(2.39201512193373,-0.538365301648864,20.0297121534464));
#9331=CARTESIAN_POINT('Ctrl Pts',(2.3728149691518,-0.617493544060195,20.0254905182774));
#9332=CARTESIAN_POINT('Ctrl Pts',(2.34976298701067,-0.695387773026463,20.0212688831084));
#9333=CARTESIAN_POINT('Ctrl Pts',(2.32639542127129,-0.7743483806195,20.0169894533946));
#9334=CARTESIAN_POINT('Ctrl Pts',(2.29906992801853,-0.852040464810376,20.0127100236807));
#9335=CARTESIAN_POINT('Ctrl Pts',(2.2679659234488,-0.928052164522561,20.0084305939668));
#9336=CARTESIAN_POINT('Ctrl Pts',(2.23686191887908,-1.00406386423475,20.0041511642529));
#9337=CARTESIAN_POINT('Ctrl Pts',(2.20197967069622,-1.07839476317502,19.999871734539));
#9338=CARTESIAN_POINT('Ctrl Pts',(2.16354588173339,-1.15066044845319,19.9955923048252));
#9339=CARTESIAN_POINT('Ctrl Pts',(2.12554971953235,-1.22210327970913,19.9913616028849));
#9340=CARTESIAN_POINT('Ctrl Pts',(2.08393960868889,-1.29179642615623,19.9871309009447));
#9341=CARTESIAN_POINT('Ctrl Pts',(2.03890079209262,-1.35935051035563,19.9829001990044));
#9342=CARTESIAN_POINT('Ctrl Pts',(1.99392668388306,-1.42680753792399,19.9786755754187));
#9343=CARTESIAN_POINT('Ctrl Pts',(1.94553390923085,-1.49213122321285,19.9744509518331));
#9344=CARTESIAN_POINT('Ctrl Pts',(1.8939537027883,-1.55495646938893,19.9702263282474));
#9345=CARTESIAN_POINT('Ctrl Pts',(1.84217048685805,-1.61802898330433,19.9659850773791));
#9346=CARTESIAN_POINT('Ctrl Pts',(1.78717491795345,-1.67858293021693,19.9617438265108));
#9347=CARTESIAN_POINT('Ctrl Pts',(1.72924512267815,-1.73627807556676,19.9575025756425));
#9348=CARTESIAN_POINT('Ctrl Pts',(1.67164657145925,-1.7936433185945,19.9532855763556));
#9349=CARTESIAN_POINT('Ctrl Pts',(1.6111475916028,-1.84818203326638,19.9490685770686));
#9350=CARTESIAN_POINT('Ctrl Pts',(1.5480608525303,-1.89959412687636,19.9448515777817));
#9351=CARTESIAN_POINT('Ctrl Pts',(1.48499502809192,-1.95098917625259,19.9406359765222));
#9352=CARTESIAN_POINT('Ctrl Pts',(1.41934350830166,-1.99925936940489,19.9364203752628));
#9353=CARTESIAN_POINT('Ctrl Pts',(1.35145293885315,-2.04414412507171,19.9322047740033));
#9354=CARTESIAN_POINT('Ctrl Pts',(1.28356406344963,-2.08902776074799,19.927989277934));
#9355=CARTESIAN_POINT('Ctrl Pts',(1.21343663801125,-2.13052587132057,19.9237737818647));
#9356=CARTESIAN_POINT('Ctrl Pts',(1.14144604713651,-2.16842135469019,19.9195582857954));
#9357=CARTESIAN_POINT('Ctrl Pts',(1.06869262005342,-2.20671839118635,19.9152981209298));
#9358=CARTESIAN_POINT('Ctrl Pts',(0.994036728184708,-2.24133575668633,19.9110379560643));
#9359=CARTESIAN_POINT('Ctrl Pts',(0.91788934197804,-2.27209801854654,19.9067777911987));
#9360=CARTESIAN_POINT('Ctrl Pts',(0.84243064641623,-2.30258206098238,19.9025561560297));
#9361=CARTESIAN_POINT('Ctrl Pts',(0.765507791155449,-2.32928035591837,19.8983345208607));
#9362=CARTESIAN_POINT('Ctrl Pts',(0.687537015936515,-2.35207208684537,19.8941128856918));
#9363=CARTESIAN_POINT('Ctrl Pts',(0.608498814165895,-2.37517583850939,19.8898334559779));
#9364=CARTESIAN_POINT('Ctrl Pts',(0.528384264145614,-2.39426513924351,19.885554026264));
#9365=CARTESIAN_POINT('Ctrl Pts',(0.447636779228395,-2.40926784809868,19.8812745965501));
#9366=CARTESIAN_POINT('Ctrl Pts',(0.366889294311188,-2.42427055695384,19.8769951668362));
#9367=CARTESIAN_POINT('Ctrl Pts',(0.285509369436723,-2.43518667361799,19.8727157371223));
#9368=CARTESIAN_POINT('Ctrl Pts',(0.203942942233879,-2.4419986745109,19.8684363074084));
#9369=CARTESIAN_POINT('Ctrl Pts',(0.123305272054182,-2.4487331104805,19.8642056054682));
#9370=CARTESIAN_POINT('Ctrl Pts',(0.0421820279329571,-2.45148179185811,
19.8599749035279));
#9371=CARTESIAN_POINT('Ctrl Pts',(-0.0389991254238726,-2.45018964943863,
19.8557442015877));
#9372=CARTESIAN_POINT('Ctrl Pts',(-0.120063643801093,-2.44889936347225,
19.851519578002));
#9373=CARTESIAN_POINT('Ctrl Pts',(-0.201185445118751,-2.44357979119285,
19.8472949544163));
#9374=CARTESIAN_POINT('Ctrl Pts',(-0.281932378287597,-2.4342276771233,19.8430703308306));
#9375=CARTESIAN_POINT('Ctrl Pts',(-0.362997115410038,-2.42483875498304,
19.8388290799624));
#9376=CARTESIAN_POINT('Ctrl Pts',(-0.443683554332948,-2.41138544090157,
19.8345878290941));
#9377=CARTESIAN_POINT('Ctrl Pts',(-0.523555059252396,-2.39391736489195,
19.8303465782258));
#9378=CARTESIAN_POINT('Ctrl Pts',(-0.60296985685637,-2.37654917178937,19.8261295789388));
#9379=CARTESIAN_POINT('Ctrl Pts',(-0.681578555905265,-2.3552121055536,19.8219125796519));
#9380=CARTESIAN_POINT('Ctrl Pts',(-0.758959568270084,-2.33000657160689,
19.8176955803649));
#9381=CARTESIAN_POINT('Ctrl Pts',(-0.836314927136413,-2.30480939384611,
19.8134799791055));
#9382=CARTESIAN_POINT('Ctrl Pts',(-0.91244296571893,-2.27574643908791,19.8092643778461));
#9383=CARTESIAN_POINT('Ctrl Pts',(-0.986936920276588,-2.24296807052507,
19.8050487765866));
#9384=CARTESIAN_POINT('Ctrl Pts',(-1.06142901601773,-2.21019051986716,19.8008332805173));
#9385=CARTESIAN_POINT('Ctrl Pts',(-1.13428668356631,-2.1736979280292,19.796617784448));
#9386=CARTESIAN_POINT('Ctrl Pts',(-1.20512415503052,-2.13368836078795,19.7924022883788));
#9387=CARTESIAN_POINT('Ctrl Pts',(-1.27671224386715,-2.09325483888524,19.7881421235132));
#9388=CARTESIAN_POINT('Ctrl Pts',(-1.34623663860387,-2.04922958793333,19.7838819586476));
#9389=CARTESIAN_POINT('Ctrl Pts',(-1.4133273386569,-2.00186315311636,19.779621793782));
#9390=CARTESIAN_POINT('Ctrl Pts',(-1.47981125836186,-1.95492510884805,19.775400158613));
#9391=CARTESIAN_POINT('Ctrl Pts',(-1.54390499578219,-1.90470641275385,19.7711785234441));
#9392=CARTESIAN_POINT('Ctrl Pts',(-1.60528161640228,-1.85149161003794,19.7669568882751));
#9393=CARTESIAN_POINT('Ctrl Pts',(-1.66749848818512,-1.7975482921414,19.7626774585612));
#9394=CARTESIAN_POINT('Ctrl Pts',(-1.72692292784109,-1.74052655506609,19.7583980288473));
#9395=CARTESIAN_POINT('Ctrl Pts',(-1.78325421308252,-1.6807601439597,19.7541185991334));
#9396=CARTESIAN_POINT('Ctrl Pts',(-1.83958549832394,-1.62099373285332,19.7498391694195));
#9397=CARTESIAN_POINT('Ctrl Pts',(-1.89282336092224,-1.55848306367117,19.7455597397056));
#9398=CARTESIAN_POINT('Ctrl Pts',(-1.94271163188047,-1.49359357435559,19.7412803099917));
#9399=CARTESIAN_POINT('Ctrl Pts',(-1.99209745832981,-1.42935761275235,19.7370439801071));
#9400=CARTESIAN_POINT('Ctrl Pts',(-2.03838923801735,-1.36254563061871,19.7328076502224));
#9401=CARTESIAN_POINT('Ctrl Pts',(-2.08130749356317,-1.29348728916746,19.7285713203378));
#9402=CARTESIAN_POINT('Ctrl Pts',(-2.12416473962921,-1.22452711604652,19.7243410125125));
#9403=CARTESIAN_POINT('Ctrl Pts',(-2.16365774029283,-1.15332731247133,19.7201107046873));
#9404=CARTESIAN_POINT('Ctrl Pts',(-2.19954791923169,-1.08024960125128,19.715880396862));
#9405=CARTESIAN_POINT('Ctrl Pts',(-2.23539796364597,-1.00725360985776,19.7116548196176));
#9406=CARTESIAN_POINT('Ctrl Pts',(-2.26765298492923,-0.932384294427066,
19.7074292423732));
#9407=CARTESIAN_POINT('Ctrl Pts',(-2.29611906075015,-0.856030086422113,
19.7032036651288));
#9408=CARTESIAN_POINT('Ctrl Pts',(-2.32456236915016,-0.779736947192605,
19.6989814675386));
#9409=CARTESIAN_POINT('Ctrl Pts',(-2.34922259155874,-0.701961707256178,
19.6947592699485));
#9410=CARTESIAN_POINT('Ctrl Pts',(-2.36995348616866,-0.623113732313,19.6905370723584));
#9411=CARTESIAN_POINT('Ctrl Pts',(-2.39067451838713,-0.544303268032445,
19.6863168834113));
#9412=CARTESIAN_POINT('Ctrl Pts',(-2.40746982107492,-0.464421530264314,
19.6820966944641));
#9413=CARTESIAN_POINT('Ctrl Pts',(-2.42024309441003,-0.383892711523121,
19.677876505517));
#9414=CARTESIAN_POINT('Ctrl Pts',(-2.43301721239596,-0.303358567699503,
19.6736560375038));
#9415=CARTESIAN_POINT('Ctrl Pts',(-2.44176868987403,-0.222177713514921,
19.6694355694907));
#9416=CARTESIAN_POINT('Ctrl Pts',(-2.44645260879298,-0.140783105982285,
19.6652151014775));
#9417=CARTESIAN_POINT('Ctrl Pts',(-2.4491855556258,-0.0932914352864258,
19.6627525663891));
#9418=CARTESIAN_POINT('Ctrl Pts',(-2.45053470395958,-0.0457271215581164,
19.6602900313006));
#9419=CARTESIAN_POINT('Ctrl Pts',(-2.45049932159773,0.00182341686532293,
19.6578274962121));
#9420=CARTESIAN_POINT('',(-2.45075211844691,0.000775521760612707,18.8578274962121));
#9421=CARTESIAN_POINT('Ctrl Pts',(-2.45049932159731,0.00182341742318767,
19.6578274961832));
#9422=CARTESIAN_POINT('Ctrl Pts',(-2.45042940194533,0.095788769285848,19.6529612426404));
#9423=CARTESIAN_POINT('Ctrl Pts',(-2.44495079787585,0.189533578803116,19.6480949890976));
#9424=CARTESIAN_POINT('Ctrl Pts',(-2.43416311526941,0.282489253356498,19.6432287355548));
#9425=CARTESIAN_POINT('Ctrl Pts',(-2.42327182879274,0.376337665302642,19.6383157469791));
#9426=CARTESIAN_POINT('Ctrl Pts',(-2.40696909967135,0.469381553086519,19.6334027584035));
#9427=CARTESIAN_POINT('Ctrl Pts',(-2.38540708047696,0.561055532376605,19.6284897698279));
#9428=CARTESIAN_POINT('Ctrl Pts',(-2.3643914766168,0.650406349462673,19.6237012840769));
#9429=CARTESIAN_POINT('Ctrl Pts',(-2.33838008968937,0.738455789770857,19.618912798326));
#9430=CARTESIAN_POINT('Ctrl Pts',(-2.30755712572132,0.824700164625154,19.614124312575));
#9431=CARTESIAN_POINT('Ctrl Pts',(-2.28032455570944,0.900898416642212,19.6098936106347));
#9432=CARTESIAN_POINT('Ctrl Pts',(-2.24926248145931,0.975889639658068,19.6056629086945));
#9433=CARTESIAN_POINT('Ctrl Pts',(-2.2144977131412,1.04926170638807,19.6014322067542));
#9434=CARTESIAN_POINT('Ctrl Pts',(-2.17978289222936,1.12252835764708,19.5972075831685));
#9435=CARTESIAN_POINT('Ctrl Pts',(-2.14137614001205,1.19418005603882,19.5929829595828));
#9436=CARTESIAN_POINT('Ctrl Pts',(-2.09945329369666,1.2638220276551,19.5887583359971));
#9437=CARTESIAN_POINT('Ctrl Pts',(-2.05736544735254,1.33373809629311,19.5845170851289));
#9438=CARTESIAN_POINT('Ctrl Pts',(-2.01173392995358,1.40162813757825,19.5802758342606));
#9439=CARTESIAN_POINT('Ctrl Pts',(-1.96278458077779,1.46711517593574,19.5760345833923));
#9440=CARTESIAN_POINT('Ctrl Pts',(-1.91411512523693,1.5322277577271,19.5718175841053));
#9441=CARTESIAN_POINT('Ctrl Pts',(-1.86216595908345,1.59496436663864,19.5676005848184));
#9442=CARTESIAN_POINT('Ctrl Pts',(-1.80720292120841,1.65498273452499,19.5633835855314));
#9443=CARTESIAN_POINT('Ctrl Pts',(-1.75225810478283,1.71498120500937,19.5591679842719));
#9444=CARTESIAN_POINT('Ctrl Pts',(-1.6943017146434,1.77226288130959,19.5549523830125));
#9445=CARTESIAN_POINT('Ctrl Pts',(-1.63363893730656,1.82651966113587,19.550736781753));
#9446=CARTESIAN_POINT('Ctrl Pts',(-1.57297767366264,1.8807750871154,19.5465212856837));
#9447=CARTESIAN_POINT('Ctrl Pts',(-1.50961050445397,1.93200545746552,19.5423057896144));
#9448=CARTESIAN_POINT('Ctrl Pts',(-1.44387735729821,1.97994152112671,19.5380902935451));
#9449=CARTESIAN_POINT('Ctrl Pts',(-1.37744767988608,2.02838553123738,19.5338301286795));
#9450=CARTESIAN_POINT('Ctrl Pts',(-1.30860196654172,2.07346470535285,19.529569963814));
#9451=CARTESIAN_POINT('Ctrl Pts',(-1.23772139805673,2.1149458600145,19.5253097989484));
#9452=CARTESIAN_POINT('Ctrl Pts',(-1.16748188617039,2.15605185165922,19.5210881637794));
#9453=CARTESIAN_POINT('Ctrl Pts',(-1.09524462393809,2.19362448211211,19.5168665286104));
#9454=CARTESIAN_POINT('Ctrl Pts',(-1.02140392707162,2.22748384231237,19.5126448934415));
#9455=CARTESIAN_POINT('Ctrl Pts',(-0.94655234477819,2.26180674003659,19.5083654637276));
#9456=CARTESIAN_POINT('Ctrl Pts',(-0.870053552590683,2.29231374449871,19.5040860340137));
#9457=CARTESIAN_POINT('Ctrl Pts',(-0.792335812248403,2.31886916634567,19.4998066042998));
#9458=CARTESIAN_POINT('Ctrl Pts',(-0.714618071906124,2.34542458819263,19.495527174586));
#9459=CARTESIAN_POINT('Ctrl Pts',(-0.635681873070141,2.36802835533124,19.4912477448721));
#9460=CARTESIAN_POINT('Ctrl Pts',(-0.555965896586985,2.38659845215575,19.4869683151582));
#9461=CARTESIAN_POINT('Ctrl Pts',(-0.477157606948763,2.40495710036807,19.482737613218));
#9462=CARTESIAN_POINT('Ctrl Pts',(-0.397290797063172,2.41944256428239,19.4785069112777));
#9463=CARTESIAN_POINT('Ctrl Pts',(-0.316780622573661,2.42993832990919,19.4742762093374));
#9464=CARTESIAN_POINT('Ctrl Pts',(-0.236386119051856,2.44041901600877,19.4700515857518));
#9465=CARTESIAN_POINT('Ctrl Pts',(-0.155350543957463,2.44692132847501,19.4658269621661));
#9466=CARTESIAN_POINT('Ctrl Pts',(-0.0741010067707996,2.44937936849226,
19.4616023385804));
#9467=CARTESIAN_POINT('Ctrl Pts',(0.00746831251923698,2.45184708286871,
19.4573610877121));
#9468=CARTESIAN_POINT('Ctrl Pts',(0.0892528195595222,2.4502385139366,19.4531198368438));
#9469=CARTESIAN_POINT('Ctrl Pts',(0.170813297239063,2.4445394387259,19.4488785859755));
#9470=CARTESIAN_POINT('Ctrl Pts',(0.251907410013752,2.43887295097353,19.4446615866886));
#9471=CARTESIAN_POINT('Ctrl Pts',(0.332779579893849,2.4291626419863,19.4404445874016));
#9472=CARTESIAN_POINT('Ctrl Pts',(0.412998114036378,2.41544670978318,19.4362275881146));
#9473=CARTESIAN_POINT('Ctrl Pts',(0.493190053979881,2.40173532471166,19.4320119868552));
#9474=CARTESIAN_POINT('Ctrl Pts',(0.572728330459702,2.3840210318284,19.4277963855957));
#9475=CARTESIAN_POINT('Ctrl Pts',(0.65118867256248,2.36239360876343,19.4235807843363));
#9476=CARTESIAN_POINT('Ctrl Pts',(0.729647056877126,2.34076672535851,19.419365288267));
#9477=CARTESIAN_POINT('Ctrl Pts',(0.807027112241932,2.3152270305395,19.4151497921977));
#9478=CARTESIAN_POINT('Ctrl Pts',(0.882918422963899,2.28591454529493,19.4109342961284));
#9479=CARTESIAN_POINT('Ctrl Pts',(0.959613903217039,2.25629145522232,19.4066741312628));
#9480=CARTESIAN_POINT('Ctrl Pts',(1.03478844276865,2.2228153026946,19.4024139663972));
#9481=CARTESIAN_POINT('Ctrl Pts',(1.10803961507543,2.18568032004305,19.3981538015317));
#9482=CARTESIAN_POINT('Ctrl Pts',(1.18062829061635,2.1488811928479,19.3939321663627));
#9483=CARTESIAN_POINT('Ctrl Pts',(1.25132787185725,2.10848943841322,19.3897105311937));
#9484=CARTESIAN_POINT('Ctrl Pts',(1.3197736117042,2.06473917574333,19.3854888960248));
#9485=CARTESIAN_POINT('Ctrl Pts',(1.38915637955753,2.02038996825234,19.3812094663109));
#9486=CARTESIAN_POINT('Ctrl Pts',(1.45622272539394,1.97258988683397,19.376930036597));
#9487=CARTESIAN_POINT('Ctrl Pts',(1.52062670138999,1.92162553194419,19.3726506068831));
#9488=CARTESIAN_POINT('Ctrl Pts',(1.58503067738604,1.87066117705441,19.3683711771692));
#9489=CARTESIAN_POINT('Ctrl Pts',(1.64677195782055,1.81653292134733,19.3640917474553));
#9490=CARTESIAN_POINT('Ctrl Pts',(1.70554408044883,1.75956518482435,19.3598123177414));
#9491=CARTESIAN_POINT('Ctrl Pts',(1.76364699365454,1.70324611206166,19.3555816158012));
#9492=CARTESIAN_POINT('Ctrl Pts',(1.8190665934253,1.64394009257529,19.351350913861));
#9493=CARTESIAN_POINT('Ctrl Pts',(1.87148014956442,1.58193308954151,19.3471202119207));
#9494=CARTESIAN_POINT('Ctrl Pts',(1.92381840184534,1.5200151735094,19.342895588335));
#9495=CARTESIAN_POINT('Ctrl Pts',(1.97315889030848,1.45540433311514,19.3386709647494));
#9496=CARTESIAN_POINT('Ctrl Pts',(2.01921496789646,1.38842398546802,19.3344463411637));
#9497=CARTESIAN_POINT('Ctrl Pts',(2.06545231309397,1.32118001642413,19.3302050902954));
#9498=CARTESIAN_POINT('Ctrl Pts',(2.10837899763103,1.2515481785876,19.3259638394271));
#9499=CARTESIAN_POINT('Ctrl Pts',(2.14774526609153,1.17989004656427,19.3217225885588));
#9500=CARTESIAN_POINT('Ctrl Pts',(2.18688643721838,1.10864165757942,19.3175055892719));
#9501=CARTESIAN_POINT('Ctrl Pts',(2.22250757270791,1.03539049603139,19.3132885899849));
#9502=CARTESIAN_POINT('Ctrl Pts',(2.25440706421273,0.960520191785537,19.309071590698));
#9503=CARTESIAN_POINT('Ctrl Pts',(2.28629598033826,0.885674708683485,19.3048559894386));
#9504=CARTESIAN_POINT('Ctrl Pts',(2.31446552046429,0.809211576346526,19.3006403881792));
#9505=CARTESIAN_POINT('Ctrl Pts',(2.33876146051008,0.7315361104093,19.2964247869197));
#9506=CARTESIAN_POINT('Ctrl Pts',(2.36305679430942,0.653862582675529,19.2922092908504));
#9507=CARTESIAN_POINT('Ctrl Pts',(2.3834785824084,0.574977225666107,19.2879937947812));
#9508=CARTESIAN_POINT('Ctrl Pts',(2.39992234458836,0.495300908484432,19.2837782987119));
#9509=CARTESIAN_POINT('Ctrl Pts',(2.4165403503333,0.414780314585646,19.2795181338463));
#9510=CARTESIAN_POINT('Ctrl Pts',(2.42909540951884,0.333452369365408,19.2752579689807));
#9511=CARTESIAN_POINT('Ctrl Pts',(2.43753294594085,0.251760575652595,19.2709978041151));
#9512=CARTESIAN_POINT('Ctrl Pts',(2.44589417176715,0.170807617202951,19.2667761689461));
#9513=CARTESIAN_POINT('Ctrl Pts',(2.45021209118132,0.0894978380503747,19.2625545337772));
#9514=CARTESIAN_POINT('Ctrl Pts',(2.45048606309993,0.00826465686051566,
19.2583328986082));
#9515=CARTESIAN_POINT('Ctrl Pts',(2.45076378571743,-0.0740806134972785,
19.2540534688943));
#9516=CARTESIAN_POINT('Ctrl Pts',(2.44688602179809,-0.156346678642749,19.2497740391804));
#9517=CARTESIAN_POINT('Ctrl Pts',(2.4389064325815,-0.238087511458697,19.2454946094665));
#9518=CARTESIAN_POINT('Ctrl Pts',(2.4309268433649,-0.319828344274645,19.2412151797526));
#9519=CARTESIAN_POINT('Ctrl Pts',(2.4188455658135,-0.401043469149177,19.2369357500387));
#9520=CARTESIAN_POINT('Ctrl Pts',(2.40276943619433,-0.481299580812578,19.2326563203248));
#9521=CARTESIAN_POINT('Ctrl Pts',(2.38687635760244,-0.560641855375045,19.2284256183845));
#9522=CARTESIAN_POINT('Ctrl Pts',(2.36701920340031,-0.639345282321367,19.2241949164443));
#9523=CARTESIAN_POINT('Ctrl Pts',(2.34326366932798,-0.716983699959484,19.219964214504));
#9524=CARTESIAN_POINT('Ctrl Pts',(2.31954226542159,-0.794510572554247,19.2157395909183));
#9525=CARTESIAN_POINT('Ctrl Pts',(2.29193374025496,-0.87097503381822,19.2115149673326));
#9526=CARTESIAN_POINT('Ctrl Pts',(2.26055481508318,-0.945960981227155,19.207290343747));
#9527=CARTESIAN_POINT('Ctrl Pts',(2.22905238867009,-1.02124205848949,19.2030490928787));
#9528=CARTESIAN_POINT('Ctrl Pts',(2.19374991270444,-1.0950324933475,19.1988078420104));
#9529=CARTESIAN_POINT('Ctrl Pts',(2.15481616321522,-1.16692654128117,19.1945665911421));
#9530=CARTESIAN_POINT('Ctrl Pts',(2.11610503790499,-1.23840949720328,19.1903495918551));
#9531=CARTESIAN_POINT('Ctrl Pts',(2.07380427750137,-1.30801728147344,19.1861325925682));
#9532=CARTESIAN_POINT('Ctrl Pts',(2.02812726855209,-1.37537268860314,19.1819155932812));
#9533=CARTESIAN_POINT('Ctrl Pts',(1.98246540253054,-1.44270576594186,19.1776999920218));
#9534=CARTESIAN_POINT('Ctrl Pts',(1.93342977151758,-1.50778756438723,19.1734843907623));
#9535=CARTESIAN_POINT('Ctrl Pts',(1.8812776489379,-1.57026897619697,19.1692687895029));
#9536=CARTESIAN_POINT('Ctrl Pts',(1.82912682768837,-1.63274882893412,19.1650532934336));
#9537=CARTESIAN_POINT('Ctrl Pts',(1.77385996832874,-1.69262806770863,19.1608377973643));
#9538=CARTESIAN_POINT('Ctrl Pts',(1.71577435289581,-1.74959098647225,19.156622301295));
#9539=CARTESIAN_POINT('Ctrl Pts',(1.65707324299192,-1.8071575032401,19.1523621364294));
#9540=CARTESIAN_POINT('Ctrl Pts',(1.59549361899203,-1.86174517669218,19.1481019715638));
#9541=CARTESIAN_POINT('Ctrl Pts',(1.53137881103256,-1.91306800378881,19.1438418066982));
#9542=CARTESIAN_POINT('Ctrl Pts',(1.46784386891811,-1.96392665801415,19.1396201715293));
#9543=CARTESIAN_POINT('Ctrl Pts',(1.40181983312291,-2.01157905891122,19.1353985363603));
#9544=CARTESIAN_POINT('Ctrl Pts',(1.33367075656057,-2.05579000948423,19.1311769011913));
#9545=CARTESIAN_POINT('Ctrl Pts',(1.26458871333723,-2.10060621173513,19.1268974714774));
#9546=CARTESIAN_POINT('Ctrl Pts',(1.1933234328532,-2.14188577477813,19.1226180417635));
#9547=CARTESIAN_POINT('Ctrl Pts',(1.12027896859355,-2.17943233033902,19.1183386120496));
#9548=CARTESIAN_POINT('Ctrl Pts',(1.04723450433389,-2.21697888589991,19.1140591823357));
#9549=CARTESIAN_POINT('Ctrl Pts',(0.972411330325981,-2.25079229162899,19.1097797526218));
#9550=CARTESIAN_POINT('Ctrl Pts',(0.896231593655689,-2.28072777431534,19.105500322908));
#9551=CARTESIAN_POINT('Ctrl Pts',(0.82091927839707,-2.31032239629796,19.1012696209677));
#9552=CARTESIAN_POINT('Ctrl Pts',(0.743997881582165,-2.33623831222196,19.0970389190274));
#9553=CARTESIAN_POINT('Ctrl Pts',(0.66586127031152,-2.35830002728642,19.0928082170871));
#9554=CARTESIAN_POINT('Ctrl Pts',(0.587836919851385,-2.38033004573678,19.0885835935015));
#9555=CARTESIAN_POINT('Ctrl Pts',(0.508601266211257,-2.39851673566438,19.0843589699158));
#9556=CARTESIAN_POINT('Ctrl Pts',(0.428567344988989,-2.41273294850655,19.0801343463301));
#9557=CARTESIAN_POINT('Ctrl Pts',(0.348218426087391,-2.4270051135498,19.0758930954618));
#9558=CARTESIAN_POINT('Ctrl Pts',(0.267065384156518,-2.43727530688736,19.0716518445935));
#9559=CARTESIAN_POINT('Ctrl Pts',(0.185540729295466,-2.44346575334554,19.0674105937252));
#9560=CARTESIAN_POINT('Ctrl Pts',(0.104482234503321,-2.44962080267199,19.0631935944383));
#9561=CARTESIAN_POINT('Ctrl Pts',(0.0230568334204954,-2.45174259914225,
19.0589765951513));
#9562=CARTESIAN_POINT('Ctrl Pts',(-0.058302805595985,-2.4498063255816,19.0547595958643));
#9563=CARTESIAN_POINT('Ctrl Pts',(-0.139635472112221,-2.447870693938,19.0505439946049));
#9564=CARTESIAN_POINT('Ctrl Pts',(-0.22090195529595,-2.44187967493441,19.0463283933455));
#9565=CARTESIAN_POINT('Ctrl Pts',(-0.301669449306597,-2.43186056207075,
19.042112792086));
#9566=CARTESIAN_POINT('Ctrl Pts',(-0.382434927959681,-2.42184169920983,
19.0378972960167));
#9567=CARTESIAN_POINT('Ctrl Pts',(-0.462700980805989,-2.40779500065838,
19.0336817999474));
#9568=CARTESIAN_POINT('Ctrl Pts',(-0.542041223593945,-2.38979948153078,
19.0294663038781));
#9569=CARTESIAN_POINT('Ctrl Pts',(-0.622222181942375,-2.37161327590641,
19.0252061390125));
#9570=CARTESIAN_POINT('Ctrl Pts',(-0.701457116994926,-2.34939415684086,
19.020945974147));
#9571=CARTESIAN_POINT('Ctrl Pts',(-0.779319686541284,-2.32327593629538,
19.0166858092814));
#9572=CARTESIAN_POINT('Ctrl Pts',(-0.856478053016731,-2.29739393362997,
19.0124641741124));
#9573=CARTESIAN_POINT('Ctrl Pts',(-0.932288362691395,-2.26768330319229,
19.0082425389434));
#9574=CARTESIAN_POINT('Ctrl Pts',(-1.00635576936152,-2.23432278676846,19.0040209037745));
#9575=CARTESIAN_POINT('Ctrl Pts',(-1.08143716513512,-2.20050556203445,18.9997414740606));
#9576=CARTESIAN_POINT('Ctrl Pts',(-1.15472713540503,-2.16293798578523,18.9954620443467));
#9577=CARTESIAN_POINT('Ctrl Pts',(-1.22584182272403,-2.12185345291814,18.9911826146329));
#9578=CARTESIAN_POINT('Ctrl Pts',(-1.29695651004303,-2.08076892005105,18.986903184919));
#9579=CARTESIAN_POINT('Ctrl Pts',(-1.3658955380855,-2.03616775203834,18.9826237552051));
#9580=CARTESIAN_POINT('Ctrl Pts',(-1.43230863225199,-1.98832649028685,18.9783443254913));
#9581=CARTESIAN_POINT('Ctrl Pts',(-1.49744651369067,-1.94140383934044,18.9741470660679));
#9582=CARTESIAN_POINT('Ctrl Pts',(-1.5604081629043,-1.89118166509442,18.9699498066445));
#9583=CARTESIAN_POINT('Ctrl Pts',(-1.62083593804614,-1.83789039715052,18.9657525472211));
#9584=CARTESIAN_POINT('Ctrl Pts',(-1.68117667131845,-1.78467589145015,18.9615613336484));
#9585=CARTESIAN_POINT('Ctrl Pts',(-1.73899042455984,-1.7284013784966,18.9573701200757));
#9586=CARTESIAN_POINT('Ctrl Pts',(-1.79394951889508,-1.66933980173484,18.953178906503));
#9587=CARTESIAN_POINT('Ctrl Pts',(-1.84884541218041,-1.61034614373532,18.9489925126804));
#9588=CARTESIAN_POINT('Ctrl Pts',(-1.90089284763804,-1.54857213380597,18.9448061188577));
#9589=CARTESIAN_POINT('Ctrl Pts',(-1.949799360154,-1.48432904207357,18.9406197250351));
#9590=CARTESIAN_POINT('Ctrl Pts',(-1.99867561180049,-1.42012570070802,18.9364359215406));
#9591=CARTESIAN_POINT('Ctrl Pts',(-2.04441451086891,-1.35345668447874,18.9322521180462));
#9592=CARTESIAN_POINT('Ctrl Pts',(-2.08676327369891,-1.28466699558345,18.9280683145517));
#9593=CARTESIAN_POINT('Ctrl Pts',(-2.12909933263273,-1.21589794240471,18.9238857661259));
#9594=CARTESIAN_POINT('Ctrl Pts',(-2.16804702656787,-1.1450098823527,18.9197032177001));
#9595=CARTESIAN_POINT('Ctrl Pts',(-2.20339726727572,-1.07237620850235,18.9155206692743));
#9596=CARTESIAN_POINT('Ctrl Pts',(-2.23874817182224,-0.999741170671455,
18.9113380423049));
#9597=CARTESIAN_POINT('Ctrl Pts',(-2.27050128388473,-0.925360880408144,
18.9071554153354));
#9598=CARTESIAN_POINT('Ctrl Pts',(-2.29849448721695,-0.849631297818818,
18.902972788366));
#9599=CARTESIAN_POINT('Ctrl Pts',(-2.32651476312664,-0.773828476201883,
18.8987861163256));
#9600=CARTESIAN_POINT('Ctrl Pts',(-2.35076770707159,-0.6966742020151,18.8945994442852));
#9601=CARTESIAN_POINT('Ctrl Pts',(-2.37114045908617,-0.618581581753452,
18.8904127722448));
#9602=CARTESIAN_POINT('Ctrl Pts',(-2.39152389618695,-0.540448003531031,
18.8862239043817));
#9603=CARTESIAN_POINT('Ctrl Pts',(-2.40802299471504,-0.461375563097046,
18.8820350365187));
#9604=CARTESIAN_POINT('Ctrl Pts',(-2.42057614060227,-0.38178711024209,18.8778461686556));
#9605=CARTESIAN_POINT('Ctrl Pts',(-2.4331498751215,-0.302068122987079,18.8736504305577));
#9606=CARTESIAN_POINT('Ctrl Pts',(-2.44176468746064,-0.221831904193627,
18.8694546924599));
#9607=CARTESIAN_POINT('Ctrl Pts',(-2.44641093600418,-0.141505414027701,
18.8652589543621));
#9608=CARTESIAN_POINT('Ctrl Pts',(-2.44915406890085,-0.0940808659040406,
18.8627818016454));
#9609=CARTESIAN_POINT('Ctrl Pts',(-2.45051487676998,-0.0466248548202002,
18.8603046489288));
#9610=CARTESIAN_POINT('Ctrl Pts',(-2.45049987730867,0.000775441940834045,
18.8578274962121));
#9611=CARTESIAN_POINT('',(-2.45034175952418,-0.00225396745384549,18.0578274962121));
#9612=CARTESIAN_POINT('Ctrl Pts',(-2.45424115301751,0.000776625838913008,
18.8578274962121));
#9613=CARTESIAN_POINT('Ctrl Pts',(-2.45441689260005,0.0431881474040568,
18.8556144401662));
#9614=CARTESIAN_POINT('Ctrl Pts',(-2.45341292665042,0.0855911761083251,
18.8534013841204));
#9615=CARTESIAN_POINT('Ctrl Pts',(-2.40888053683753,0.93884568070453,18.8088029956023));
#9616=CARTESIAN_POINT('Ctrl Pts',(-1.43961464987565,2.51450507031629,18.7240323306577));
#9617=CARTESIAN_POINT('Ctrl Pts',(1.33466462877634,2.57174968017351,18.5968763332411));
#9618=CARTESIAN_POINT('Ctrl Pts',(2.8848211319999,0.270246415603432,18.4697203358243));
#9619=CARTESIAN_POINT('Ctrl Pts',(1.78908804275333,-2.27912045843473,18.3425643384076));
#9620=CARTESIAN_POINT('Ctrl Pts',(-0.947554210610886,-2.73813204698707,
18.2154083409909));
#9621=CARTESIAN_POINT('Ctrl Pts',(-2.34155166386826,-1.2062176413868,18.1204960602591));
#9622=CARTESIAN_POINT('Ctrl Pts',(-2.45213219889459,-0.19741509474636,18.0679691119994));
#9623=CARTESIAN_POINT('Ctrl Pts',(-2.45034175952418,-0.00225396745384549,
18.0578274962121));
#9624=CARTESIAN_POINT('',(-2.45013024099823,0.000414097004077804,17.2578274769431));
#9625=CARTESIAN_POINT('Ctrl Pts',(-2.45034175952418,-0.00225396745384549,
18.0578274962121));
#9626=CARTESIAN_POINT('Ctrl Pts',(-2.44464933131434,0.618230995521739,18.0255837795272));
#9627=CARTESIAN_POINT('Ctrl Pts',(-1.89007728857131,2.06341743069497,17.9509547303701));
#9628=CARTESIAN_POINT('Ctrl Pts',(0.540405443485623,2.84660992154335,17.8339403487407));
#9629=CARTESIAN_POINT('Ctrl Pts',(2.68589061564201,1.08683839166205,17.7067843513239));
#9630=CARTESIAN_POINT('Ctrl Pts',(2.36794055168644,-1.6697555606909,17.5796283539071));
#9631=CARTESIAN_POINT('Ctrl Pts',(-0.121828482878495,-2.89488927414131,
17.4524723564905));
#9632=CARTESIAN_POINT('Ctrl Pts',(-2.12790075727867,-1.68857036130835,17.3452054039253));
#9633=CARTESIAN_POINT('Ctrl Pts',(-2.44587085179714,-0.434202241831305,
17.2803237838326));
#9634=CARTESIAN_POINT('Ctrl Pts',(-2.44652391920135,0.000413115175876,17.2578274962121));
#9635=CARTESIAN_POINT('',(-2.45049912112546,0.00207541883864715,16.4578274962121));
#9636=CARTESIAN_POINT('Ctrl Pts',(-2.45049996499496,0.000414197662163056,
17.2578274749676));
#9637=CARTESIAN_POINT('Ctrl Pts',(-2.45048532431696,0.0870322165542004,
17.2533512807253));
#9638=CARTESIAN_POINT('Ctrl Pts',(-2.4458738856359,0.17353746902709,17.2488750864831));
#9639=CARTESIAN_POINT('Ctrl Pts',(-2.43672683137172,0.259446717599513,17.2443988922408));
#9640=CARTESIAN_POINT('Ctrl Pts',(-2.42754837478303,0.345650897198139,17.2399073309853));
#9641=CARTESIAN_POINT('Ctrl Pts',(-2.41380320604947,0.431254610299297,17.2354157697298));
#9642=CARTESIAN_POINT('Ctrl Pts',(-2.39560398952621,0.51578268230535,17.2309242084743));
#9643=CARTESIAN_POINT('Ctrl Pts',(-2.37737168473939,0.600464436043839,17.2264244810452));
#9644=CARTESIAN_POINT('Ctrl Pts',(-2.35466927232697,0.684066288710046,17.221924753616));
#9645=CARTESIAN_POINT('Ctrl Pts',(-2.32765907930525,0.76612887984193,17.2174250261868));
#9646=CARTESIAN_POINT('Ctrl Pts',(-2.30057021386121,0.848430494175921,17.2129121924294));
#9647=CARTESIAN_POINT('Ctrl Pts',(-2.26914861576148,0.9291835360433,17.208399358672));
#9648=CARTESIAN_POINT('Ctrl Pts',(-2.23360485339684,1.00794821736143,17.2038865249145));
#9649=CARTESIAN_POINT('Ctrl Pts',(-2.2185714769549,1.04126205432774,17.2019778038287));
#9650=CARTESIAN_POINT('Ctrl Pts',(-2.20280124227922,1.07422051047322,17.2000690827428));
#9651=CARTESIAN_POINT('Ctrl Pts',(-2.18631246248532,1.10679178998643,17.198160361657));
#9652=CARTESIAN_POINT('Ctrl Pts',(-2.14976489501516,1.17898640053239,17.1939296597167));
#9653=CARTESIAN_POINT('Ctrl Pts',(-2.10956882614381,1.24950456864096,17.1896989577765));
#9654=CARTESIAN_POINT('Ctrl Pts',(-2.06590160807849,1.31795326007363,17.1854682558362));
#9655=CARTESIAN_POINT('Ctrl Pts',(-2.02229712779015,1.38630360957091,17.1812436322506));
#9656=CARTESIAN_POINT('Ctrl Pts',(-1.97523165093694,1.45258999872321,17.1770190086649));
#9657=CARTESIAN_POINT('Ctrl Pts',(-1.92492900182796,1.51644274139237,17.1727943850792));
#9658=CARTESIAN_POINT('Ctrl Pts',(-1.87442837144425,1.58054679582369,17.1685531342109));
#9659=CARTESIAN_POINT('Ctrl Pts',(-1.82066524674829,1.64219758258882,17.1643118833426));
#9660=CARTESIAN_POINT('Ctrl Pts',(-1.76391083588777,1.70104932704426,17.1600706324743));
#9661=CARTESIAN_POINT('Ctrl Pts',(-1.70748094820539,1.75956455571421,17.1558536331874));
#9662=CARTESIAN_POINT('Ctrl Pts',(-1.64809421610665,1.81531232708092,17.1516366339004));
#9663=CARTESIAN_POINT('Ctrl Pts',(-1.5860571931162,1.86798630352697,17.1474196346135));
#9664=CARTESIAN_POINT('Ctrl Pts',(-1.52404073675602,1.92064281739751,17.143204033354));
#9665=CARTESIAN_POINT('Ctrl Pts',(-1.45937608854198,1.97022725920215,17.1389884320946));
#9666=CARTESIAN_POINT('Ctrl Pts',(-1.39240456823114,2.01647210949446,17.1347728308352));
#9667=CARTESIAN_POINT('Ctrl Pts',(-1.32543471903273,2.0627158058583,17.1305573347659));
#9668=CARTESIAN_POINT('Ctrl Pts',(-1.2561584954922,2.10561981303298,17.1263418386966));
#9669=CARTESIAN_POINT('Ctrl Pts',(-1.18494682731833,2.14495950228162,17.1221263426273));
#9670=CARTESIAN_POINT('Ctrl Pts',(-1.11298057665956,2.18471604794199,17.1178661777617));
#9671=CARTESIAN_POINT('Ctrl Pts',(-1.03903803618435,2.2208320401469,17.1136060128961));
#9672=CARTESIAN_POINT('Ctrl Pts',(-0.963526554606486,2.2531237934406,17.1093458480305));
#9673=CARTESIAN_POINT('Ctrl Pts',(-0.888698012437882,2.28512349431449,17.1051242128616));
#9674=CARTESIAN_POINT('Ctrl Pts',(-0.812329257027663,2.31336774702246,17.1009025776926));
#9675=CARTESIAN_POINT('Ctrl Pts',(-0.7348340068149,2.3377273648628,17.0966809425236));
#9676=CARTESIAN_POINT('Ctrl Pts',(-0.656277840028052,2.36242046794558,17.0924015128097));
#9677=CARTESIAN_POINT('Ctrl Pts',(-0.576564580054757,2.3831216445284,17.0881220830958));
#9678=CARTESIAN_POINT('Ctrl Pts',(-0.496136095112703,2.39974982552897,17.0838426533819));
#9679=CARTESIAN_POINT('Ctrl Pts',(-0.415707610170649,2.41637800652954,17.079563223668));
#9680=CARTESIAN_POINT('Ctrl Pts',(-0.334564395092556,2.42893318165386,17.0752837939541));
#9681=CARTESIAN_POINT('Ctrl Pts',(-0.25315194338759,2.43738883716962,17.0710043642402));
#9682=CARTESIAN_POINT('Ctrl Pts',(-0.172666495461915,2.44574821227059,17.0667736623));
#9683=CARTESIAN_POINT('Ctrl Pts',(-0.0916151872469946,2.45013243657524,
17.0625429603597));
#9684=CARTESIAN_POINT('Ctrl Pts',(-0.0104244858216357,2.45047782689323,
17.0583122584195));
#9685=CARTESIAN_POINT('Ctrl Pts',(0.0706495669060399,2.45082272098037,17.0540876348338));
#9686=CARTESIAN_POINT('Ctrl Pts',(0.151862153987194,2.44714030358705,17.0498630112481));
#9687=CARTESIAN_POINT('Ctrl Pts',(0.232781277887563,2.43941860423033,17.0456383876624));
#9688=CARTESIAN_POINT('Ctrl Pts',(0.314018883450085,2.43166651379264,17.0413971367941));
#9689=CARTESIAN_POINT('Ctrl Pts',(0.394960238835914,2.41984322854111,17.0371558859258));
#9690=CARTESIAN_POINT('Ctrl Pts',(0.475167796108238,2.40398956227801,17.0329146350575));
#9691=CARTESIAN_POINT('Ctrl Pts',(0.554916724509232,2.38822654768556,17.0286976357706));
#9692=CARTESIAN_POINT('Ctrl Pts',(0.633939762958023,2.3684792097371,17.0244806364836));
#9693=CARTESIAN_POINT('Ctrl Pts',(0.711813384088354,2.34483943079962,17.0202636371967));
#9694=CARTESIAN_POINT('Ctrl Pts',(0.789661188409645,2.32120748896602,17.0160480359372));
#9695=CARTESIAN_POINT('Ctrl Pts',(0.86635988747163,2.29368580369924,17.0118324346778));
#9696=CARTESIAN_POINT('Ctrl Pts',(0.94149976772727,2.26241650395534,17.0076168334184));
#9697=CARTESIAN_POINT('Ctrl Pts',(1.01663777304888,2.2311479844612,17.0034013373491));
#9698=CARTESIAN_POINT('Ctrl Pts',(1.09021660795131,2.19613221609753,16.9991858412798));
#9699=CARTESIAN_POINT('Ctrl Pts',(1.16184658839562,2.15755944414828,16.9949703452105));
#9700=CARTESIAN_POINT('Ctrl Pts',(1.23423558390045,2.11857794229777,16.9907101803449));
#9701=CARTESIAN_POINT('Ctrl Pts',(1.30463374341828,2.07596382114797,16.9864500154793));
#9702=CARTESIAN_POINT('Ctrl Pts',(1.37266608860103,2.02996011271274,16.9821898506137));
#9703=CARTESIAN_POINT('Ctrl Pts',(1.44008313702819,1.98437247008371,16.9779682154447));
#9704=CARTESIAN_POINT('Ctrl Pts',(1.5051766538526,1.93545663745896,16.9737465802758));
#9705=CARTESIAN_POINT('Ctrl Pts',(1.56761403231892,1.88349050851784,16.9695249451068));
#9706=CARTESIAN_POINT('Ctrl Pts',(1.63090618381286,1.83081295884671,16.9652455153929));
#9707=CARTESIAN_POINT('Ctrl Pts',(1.6914685570292,1.77500129807699,16.960966085679));
#9708=CARTESIAN_POINT('Ctrl Pts',(1.7489937598395,1.71638313847535,16.9566866559651));
#9709=CARTESIAN_POINT('Ctrl Pts',(1.80651896264979,1.65776497887372,16.9524072262512));
#9710=CARTESIAN_POINT('Ctrl Pts',(1.86100671849099,1.5963407309012,16.9481277965373));
#9711=CARTESIAN_POINT('Ctrl Pts',(1.91219354027981,1.53247059172833,16.9438483668235));
#9712=CARTESIAN_POINT('Ctrl Pts',(1.96279752275777,1.46932771059958,16.9396176648832));
#9713=CARTESIAN_POINT('Ctrl Pts',(2.01036573076263,1.40355688444311,16.9353869629429));
#9714=CARTESIAN_POINT('Ctrl Pts',(2.05461372784441,1.33548218983006,16.9311562610027));
#9715=CARTESIAN_POINT('Ctrl Pts',(2.09879815272956,1.2675052998219,16.926931637417));
#9716=CARTESIAN_POINT('Ctrl Pts',(2.13967158933008,1.19723150186897,16.9227070138313));
#9717=CARTESIAN_POINT('Ctrl Pts',(2.17699008478969,1.12501752018686,16.9184823902457));
#9718=CARTESIAN_POINT('Ctrl Pts',(2.21445545846413,1.05251931856005,16.9142411393774));
#9719=CARTESIAN_POINT('Ctrl Pts',(2.24833755111596,0.978065998396562,16.9099998885091));
#9720=CARTESIAN_POINT('Ctrl Pts',(2.27843378362012,0.902047528491999,16.9057586376408));
#9721=CARTESIAN_POINT('Ctrl Pts',(2.30835792509426,0.826463734149699,16.9015416383538));
#9722=CARTESIAN_POINT('Ctrl Pts',(2.33453921131335,0.749333077380558,16.8973246390669));
#9723=CARTESIAN_POINT('Ctrl Pts',(2.35682559033526,0.671061388205926,16.8931076397799));
#9724=CARTESIAN_POINT('Ctrl Pts',(2.37910458093497,0.59281564780859,16.8888920385205));
#9725=CARTESIAN_POINT('Ctrl Pts',(2.3974911012804,0.513430073128373,16.8846764372611));
#9726=CARTESIAN_POINT('Ctrl Pts',(2.41188282359256,0.433326084212761,16.8804608360016));
#9727=CARTESIAN_POINT('Ctrl Pts',(2.42627418679409,0.353224094098535,16.8762453399323));
#9728=CARTESIAN_POINT('Ctrl Pts',(2.43667086898234,0.272404183314324,16.872029843863));
#9729=CARTESIAN_POINT('Ctrl Pts',(2.44302184075596,0.191296982697953,16.8678143477938));
#9730=CARTESIAN_POINT('Ctrl Pts',(2.44944010953561,0.109330343248744,16.8635541829282));
#9731=CARTESIAN_POINT('Ctrl Pts',(2.4517263641234,0.027070771010427,16.8592940180626));
#9732=CARTESIAN_POINT('Ctrl Pts',(2.44988191779351,-0.0550348877385224,
16.855033853197));
#9733=CARTESIAN_POINT('Ctrl Pts',(2.44805415296768,-0.136397968154888,16.850812218028));
#9734=CARTESIAN_POINT('Ctrl Pts',(2.44217019982957,-0.217609443387193,16.8465905828591));
#9735=CARTESIAN_POINT('Ctrl Pts',(2.43228362234313,-0.29823921687362,16.8423689476901));
#9736=CARTESIAN_POINT('Ctrl Pts',(2.42226169676907,-0.379972818824617,16.8380895179762));
#9737=CARTESIAN_POINT('Ctrl Pts',(2.40812680941319,-0.461108184029412,16.8338100882623));
#9738=CARTESIAN_POINT('Ctrl Pts',(2.38998797701349,-0.54120949708128,16.8295306585485));
#9739=CARTESIAN_POINT('Ctrl Pts',(2.37184914461379,-0.621310810133148,16.8252512288346));
#9740=CARTESIAN_POINT('Ctrl Pts',(2.34970656253396,-0.700377616281152,16.8209717991207));
#9741=CARTESIAN_POINT('Ctrl Pts',(2.3237204142266,-0.777993371762617,16.8166923694068));
#9742=CARTESIAN_POINT('Ctrl Pts',(2.29803015748355,-0.854725354588237,16.8124616674665));
#9743=CARTESIAN_POINT('Ctrl Pts',(2.26848683192545,-0.930327787757224,16.8082309655263));
#9744=CARTESIAN_POINT('Ctrl Pts',(2.23520891010395,-1.00438607028967,16.804000263586));
#9745=CARTESIAN_POINT('Ctrl Pts',(2.20197879949943,-1.07833795144781,16.7997756400003));
#9746=CARTESIAN_POINT('Ctrl Pts',(2.1650249379799,-1.15074966746851,16.7955510164147));
#9747=CARTESIAN_POINT('Ctrl Pts',(2.12451516514688,-1.22122297843635,16.791326392829));
#9748=CARTESIAN_POINT('Ctrl Pts',(2.08384595386266,-1.29197365841333,16.7870851419607));
#9749=CARTESIAN_POINT('Ctrl Pts',(2.03959293116551,-1.36077019225043,16.7828438910924));
#9750=CARTESIAN_POINT('Ctrl Pts',(1.99197428751592,-1.42723112629855,16.7786026402241));
#9751=CARTESIAN_POINT('Ctrl Pts',(1.94462792849306,-1.49331203501978,16.7743856409372));
#9752=CARTESIAN_POINT('Ctrl Pts',(1.89395460707311,-1.55708359967046,16.7701686416502));
#9753=CARTESIAN_POINT('Ctrl Pts',(1.84021320517683,-1.61819826025516,16.7659516423633));
#9754=CARTESIAN_POINT('Ctrl Pts',(1.78648961973098,-1.67929265999287,16.7617360411038));
#9755=CARTESIAN_POINT('Ctrl Pts',(1.72970028052916,-1.7377315558649,16.7575204398444));
#9756=CARTESIAN_POINT('Ctrl Pts',(1.67014409817489,-1.7932007532152,16.7533048385849));
#9757=CARTESIAN_POINT('Ctrl Pts',(1.61058940190117,-1.84866856646579,16.7490893425156));
#9758=CARTESIAN_POINT('Ctrl Pts',(1.54826834079983,-1.90116651235793,16.7448738464464));
#9759=CARTESIAN_POINT('Ctrl Pts',(1.48351534306502,-1.9504185389015,16.7406583503771));
#9760=CARTESIAN_POINT('Ctrl Pts',(1.41807620106221,-2.00019245627457,16.7363981855115));
#9761=CARTESIAN_POINT('Ctrl Pts',(1.35015365218003,-2.04665094891283,16.7321380206459));
#9762=CARTESIAN_POINT('Ctrl Pts',(1.28012409681095,-2.08955319309271,16.7278778557803));
#9763=CARTESIAN_POINT('Ctrl Pts',(1.21072790132531,-2.13206742166647,16.7236562206113));
#9764=CARTESIAN_POINT('Ctrl Pts',(1.13926310063498,-2.17108929855924,16.7194345854424));
#9765=CARTESIAN_POINT('Ctrl Pts',(1.06612030182457,-2.20643099870299,16.7152129502734));
#9766=CARTESIAN_POINT('Ctrl Pts',(0.991976171870441,-2.24225652973101,16.7109335205595));
#9767=CARTESIAN_POINT('Ctrl Pts',(0.916108207728543,-2.27430016473768,16.7066540908456));
#9768=CARTESIAN_POINT('Ctrl Pts',(0.838941847434141,-2.30241760474154,16.7023746611317));
#9769=CARTESIAN_POINT('Ctrl Pts',(0.761775487139728,-2.33053504474541,16.6980952314178));
#9770=CARTESIAN_POINT('Ctrl Pts',(0.683311218800301,-2.35472620779242,16.6938158017039));
#9771=CARTESIAN_POINT('Ctrl Pts',(0.603985979936841,-2.37490024759772,16.68953637199));
#9772=CARTESIAN_POINT('Ctrl Pts',(0.525563978780598,-2.39484457547628,16.6853056700498));
#9773=CARTESIAN_POINT('Ctrl Pts',(0.446005557894124,-2.4109378551966,16.6810749681095));
#9774=CARTESIAN_POINT('Ctrl Pts',(0.365723438613278,-2.42305522356567,16.6768442661693));
#9775=CARTESIAN_POINT('Ctrl Pts',(0.285556662647657,-2.43515518261058,16.6726196425836));
#9776=CARTESIAN_POINT('Ctrl Pts',(0.204668709249403,-2.44329050640891,16.6683950189979));
#9777=CARTESIAN_POINT('Ctrl Pts',(0.123485271971944,-2.44738669556039,16.6641703954122));
#9778=CARTESIAN_POINT('Ctrl Pts',(0.0419823127471129,-2.45149900650196,
16.6599291445439));
#9779=CARTESIAN_POINT('Ctrl Pts',(-0.0398180013639428,-2.45154020316717,
16.6556878936756));
#9780=CARTESIAN_POINT('Ctrl Pts',(-0.12147682943596,-2.44748720730266,16.6514466428074));
#9781=CARTESIAN_POINT('Ctrl Pts',(-0.202668730232951,-2.44345738657254,
16.6472296435204));
#9782=CARTESIAN_POINT('Ctrl Pts',(-0.283720289483871,-2.43538009094091,
16.6430126442334));
#9783=CARTESIAN_POINT('Ctrl Pts',(-0.364199131769119,-2.42328480423136,
16.6387956449465));
#9784=CARTESIAN_POINT('Ctrl Pts',(-0.444651293557495,-2.41119352737397,
16.634580043687));
#9785=CARTESIAN_POINT('Ctrl Pts',(-0.524530655895172,-2.39508697373133,
16.6303644424276));
#9786=CARTESIAN_POINT('Ctrl Pts',(-0.603411223519619,-2.37504634593318,
16.6261488411682));
#9787=CARTESIAN_POINT('Ctrl Pts',(-0.682289822870212,-2.35500621820045,
16.6219333450989));
#9788=CARTESIAN_POINT('Ctrl Pts',(-0.760169226586095,-2.33103232705722,
16.6177178490296));
#9789=CARTESIAN_POINT('Ctrl Pts',(-0.836636278493729,-2.30325638770593,
16.6135023529603));
#9790=CARTESIAN_POINT('Ctrl Pts',(-0.913913600677536,-2.27518612527708,
16.6092421880947));
#9791=CARTESIAN_POINT('Ctrl Pts',(-0.989748000477595,-2.24323290960423,
16.6049820232291));
#9792=CARTESIAN_POINT('Ctrl Pts',(-1.0637332159051,-2.20758281733216,16.6007218583635));
#9793=CARTESIAN_POINT('Ctrl Pts',(-1.13704929574873,-2.17225515090111,16.5965002231946));
#9794=CARTESIAN_POINT('Ctrl Pts',(-1.20854912200698,-2.13329748850999,16.5922785880256));
#9795=CARTESIAN_POINT('Ctrl Pts',(-1.27786330003798,-2.09093654528683,16.5880569528566));
#9796=CARTESIAN_POINT('Ctrl Pts',(-1.34812639506825,-2.04799567714397,16.5837775231427));
#9797=CARTESIAN_POINT('Ctrl Pts',(-1.41614313681786,-2.00155791913127,16.5794980934288));
#9798=CARTESIAN_POINT('Ctrl Pts',(-1.48156186764036,-1.95190283629949,16.5752186637149));
#9799=CARTESIAN_POINT('Ctrl Pts',(-1.54698059846286,-1.90224775346771,16.570939234001));
#9800=CARTESIAN_POINT('Ctrl Pts',(-1.60980098518759,-1.84937571182599,16.5666598042871));
#9801=CARTESIAN_POINT('Ctrl Pts',(-1.6697100849671,-1.79360488462737,16.5623803745733));
#9802=CARTESIAN_POINT('Ctrl Pts',(-1.73069629536528,-1.73683134915223,16.5580240046415));
#9803=CARTESIAN_POINT('Ctrl Pts',(-1.78892059448119,-1.67681583650999,16.5536676347098));
#9804=CARTESIAN_POINT('Ctrl Pts',(-1.84401397873806,-1.61386576152375,16.5493112647781));
#9805=CARTESIAN_POINT('Ctrl Pts',(-1.89663132731389,-1.5537448217212,16.5451506811016));
#9806=CARTESIAN_POINT('Ctrl Pts',(-1.9463927235685,-1.49094779758312,16.5409900974251));
#9807=CARTESIAN_POINT('Ctrl Pts',(-1.99301105788362,-1.4257830035295,16.5368295137486));
#9808=CARTESIAN_POINT('Ctrl Pts',(-2.03958588784661,-1.360679021433,16.5326728127397));
#9809=CARTESIAN_POINT('Ctrl Pts',(-2.08302319534392,-1.2932120399579,16.5285161117308));
#9810=CARTESIAN_POINT('Ctrl Pts',(-2.1230755050836,-1.22372409051796,16.524359410722));
#9811=CARTESIAN_POINT('Ctrl Pts',(-2.16310357207443,-1.15427820054769,16.5202052256693));
#9812=CARTESIAN_POINT('Ctrl Pts',(-2.19975046767778,-1.0828141848471,16.5160510406167));
#9813=CARTESIAN_POINT('Ctrl Pts',(-2.23281243012162,-1.0097023828309,16.5118968555641));
#9814=CARTESIAN_POINT('Ctrl Pts',(-2.265865219138,-0.936610866537691,16.5077438231386));
#9815=CARTESIAN_POINT('Ctrl Pts',(-2.29533485359459,-0.861872909497991,
16.5035907907131));
#9816=CARTESIAN_POINT('Ctrl Pts',(-2.32106460665767,-0.785881251666621,
16.4994377582876));
#9817=CARTESIAN_POINT('Ctrl Pts',(-2.34680682649795,-0.709852773774594,
16.495282713603));
#9818=CARTESIAN_POINT('Ctrl Pts',(-2.36880538969035,-0.632569836508239,
16.4911276689184));
#9819=CARTESIAN_POINT('Ctrl Pts',(-2.38695297832093,-0.55444181776344,16.4869726242338));
#9820=CARTESIAN_POINT('Ctrl Pts',(-2.40510579337019,-0.476291298523169,
16.4828163829162));
#9821=CARTESIAN_POINT('Ctrl Pts',(-2.41940533677263,-0.397295685264642,
16.4786601415986));
#9822=CARTESIAN_POINT('Ctrl Pts',(-2.42979556890757,-0.317873785199594,
16.474503900281));
#9823=CARTESIAN_POINT('Ctrl Pts',(-2.4401976646121,-0.238361201189751,16.470342913366));
#9824=CARTESIAN_POINT('Ctrl Pts',(-2.44668150234325,-0.158421837288515,
16.4661819264511));
#9825=CARTESIAN_POINT('Ctrl Pts',(-2.44924304161787,-0.0784778509289605,
16.4620209395362));
#9826=CARTESIAN_POINT('Ctrl Pts',(-2.4501035481908,-0.051621996556521,16.4606231250948));
#9827=CARTESIAN_POINT('Ctrl Pts',(-2.45052185378628,-0.0247656044411454,
16.4592253106535));
#9828=CARTESIAN_POINT('Ctrl Pts',(-2.45049912112546,0.00207541883864715,
16.4578274962121));
#9829=CARTESIAN_POINT('',(-2.45049951066269,-0.00154862581067043,15.6578274962121));
#9830=CARTESIAN_POINT('Ctrl Pts',(-2.45186148920186,0.00207657267883799,
16.4578274962121));
#9831=CARTESIAN_POINT('Ctrl Pts',(-2.45316840210371,0.146834273666068,16.4502931231936));
#9832=CARTESIAN_POINT('Ctrl Pts',(-2.37555074445045,1.1045405278822,16.4003734177029));
#9833=CARTESIAN_POINT('Ctrl Pts',(-1.11386916294639,2.67479374468711,16.3080683797398));
#9834=CARTESIAN_POINT('Ctrl Pts',(1.64579100316184,2.38465889860411,16.180912382323));
#9835=CARTESIAN_POINT('Ctrl Pts',(2.89597065474372,-0.0926285897766665,
16.0537563849064));
#9836=CARTESIAN_POINT('Ctrl Pts',(1.49003463575844,-2.48495933025483,15.9266003874895));
#9837=CARTESIAN_POINT('Ctrl Pts',(-1.28252584789195,-2.59814424893407,15.7994443900729));
#9838=CARTESIAN_POINT('Ctrl Pts',(-2.4072097803276,-0.998919564647339,15.7098534263137));
#9839=CARTESIAN_POINT('Ctrl Pts',(-2.45396548163378,-0.0940230492670492,
15.6626477950268));
#9840=CARTESIAN_POINT('Ctrl Pts',(-2.45328308412766,-0.00155038492700349,
15.6578274962121));
#9841=CARTESIAN_POINT('',(-2.45039354441706,-0.00121703784683746,14.8578275494461));
#9842=CARTESIAN_POINT('Ctrl Pts',(-2.45049951066269,-0.00154862581067043,
15.6578274962121));
#9843=CARTESIAN_POINT('Ctrl Pts',(-2.4505500210209,0.0783774655743783,15.6536564556925));
#9844=CARTESIAN_POINT('Ctrl Pts',(-2.44668598205683,0.158458895275208,15.6494854151729));
#9845=CARTESIAN_POINT('Ctrl Pts',(-2.43888821404384,0.238274063628554,15.6453143746533));
#9846=CARTESIAN_POINT('Ctrl Pts',(-2.43108444750479,0.318150630752134,15.6411401255111));
#9847=CARTESIAN_POINT('Ctrl Pts',(-2.4193408568407,0.397760046304294,15.6369658763688));
#9848=CARTESIAN_POINT('Ctrl Pts',(-2.40369055215463,0.47667806692,15.6327916272266));
#9849=CARTESIAN_POINT('Ctrl Pts',(-2.38808610712666,0.555364836226782,15.628629609772));
#9850=CARTESIAN_POINT('Ctrl Pts',(-2.36859787333269,0.633363780969156,15.6244675923174));
#9851=CARTESIAN_POINT('Ctrl Pts',(-2.34531045813541,0.71025988550718,15.6203055748628));
#9852=CARTESIAN_POINT('Ctrl Pts',(-2.32203341019351,0.787121756896235,15.6161454102844));
#9853=CARTESIAN_POINT('Ctrl Pts',(-2.2949606750716,0.86288130469108,15.611985245706));
#9854=CARTESIAN_POINT('Ctrl Pts',(-2.26422727925668,0.937136637780155,15.6078250811276));
#9855=CARTESIAN_POINT('Ctrl Pts',(-2.23349754837517,1.01138311597885,15.6036654126456));
#9856=CARTESIAN_POINT('Ctrl Pts',(-2.19910820756072,1.08412529377227,15.5995057441636));
#9857=CARTESIAN_POINT('Ctrl Pts',(-2.16124259240274,1.15498082528857,15.5953460756816));
#9858=CARTESIAN_POINT('Ctrl Pts',(-2.12315117743551,1.22625888171129,15.5911616023114));
#9859=CARTESIAN_POINT('Ctrl Pts',(-2.08154210565964,1.29562727592304,15.5869771289412));
#9860=CARTESIAN_POINT('Ctrl Pts',(-2.03664817295185,1.36272318157867,15.582792655571));
#9861=CARTESIAN_POINT('Ctrl Pts',(-1.99196174743556,1.42950895884714,15.5786275235297));
#9862=CARTESIAN_POINT('Ctrl Pts',(-1.94402109266039,1.49404285456839,15.5744623914884));
#9863=CARTESIAN_POINT('Ctrl Pts',(-1.89309724305004,1.55599906116821,15.5702972594471));
#9864=CARTESIAN_POINT('Ctrl Pts',(-1.8418186862252,1.61838682024552,15.5661031154125));
#9865=CARTESIAN_POINT('Ctrl Pts',(-1.78751554941219,1.6781604800788,15.5619089713778));
#9866=CARTESIAN_POINT('Ctrl Pts',(-1.73050189298285,1.73502548926025,15.5577148273432));
#9867=CARTESIAN_POINT('Ctrl Pts',(-1.67348823655352,1.79189049844169,15.5535206833086));
#9868=CARTESIAN_POINT('Ctrl Pts',(-1.61376446905625,1.8458465818398,15.549326539274));
#9869=CARTESIAN_POINT('Ctrl Pts',(-1.55167630420393,1.89664200548549,15.5451323952393));
#9870=CARTESIAN_POINT('Ctrl Pts',(-1.48904695305643,1.94788018319229,15.5409016932991));
#9871=CARTESIAN_POINT('Ctrl Pts',(-1.42375917604961,1.99610924247822,15.5366709913588));
#9872=CARTESIAN_POINT('Ctrl Pts',(-1.35613416485738,2.04104149318591,15.5324402894186));
#9873=CARTESIAN_POINT('Ctrl Pts',(-1.28860631219869,2.0859091886128,15.5282156658329));
#9874=CARTESIAN_POINT('Ctrl Pts',(-1.21874827851875,2.1274892274372,15.5239910422472));
#9875=CARTESIAN_POINT('Ctrl Pts',(-1.14691430973519,2.16553407179953,15.5197664186615));
#9876=CARTESIAN_POINT('Ctrl Pts',(-1.07479761666251,2.20372865314228,15.5155251677933));
#9877=CARTESIAN_POINT('Ctrl Pts',(-1.00068976864277,2.2383598521934,15.511283916925));
#9878=CARTESIAN_POINT('Ctrl Pts',(-0.924978671719191,2.26922116746354,15.5070426660567));
#9879=CARTESIAN_POINT('Ctrl Pts',(-0.849700492791331,2.29990601694076,15.5028256667697));
#9880=CARTESIAN_POINT('Ctrl Pts',(-0.772837785029555,2.3268638009232,15.4986086674828));
#9881=CARTESIAN_POINT('Ctrl Pts',(-0.694794824440917,2.34993838258158,15.4943916681958));
#9882=CARTESIAN_POINT('Ctrl Pts',(-0.616777736800977,2.37300531451136,15.4901760669364));
#9883=CARTESIAN_POINT('Ctrl Pts',(-0.537581618971362,2.39219146885349,15.485960465677));
#9884=CARTESIAN_POINT('Ctrl Pts',(-0.457626837639022,2.40739027319471,15.4817448644175));
#9885=CARTESIAN_POINT('Ctrl Pts',(-0.377674051385011,2.4225886982865,15.4775293683482));
#9886=CARTESIAN_POINT('Ctrl Pts',(-0.296963096348684,2.43379988541402,15.473313872279));
#9887=CARTESIAN_POINT('Ctrl Pts',(-0.215924066860775,2.44096846504626,15.4690983762097));
#9888=CARTESIAN_POINT('Ctrl Pts',(-0.134026320903873,2.44821300532893,15.4648382113441));
#9889=CARTESIAN_POINT('Ctrl Pts',(-0.0517939874893621,2.45132869563443,
15.4605780464785));
#9890=CARTESIAN_POINT('Ctrl Pts',(0.0303260965828464,2.45031234291999,15.4563178816129));
#9891=CARTESIAN_POINT('Ctrl Pts',(0.11170347185729,2.44930518228214,15.452096246444));
#9892=CARTESIAN_POINT('Ctrl Pts',(0.192970154550172,2.44424051071898,15.447874611275));
#9893=CARTESIAN_POINT('Ctrl Pts',(0.27369552980105,2.43516755213413,15.443652976106));
#9894=CARTESIAN_POINT('Ctrl Pts',(0.355526042312747,2.42597038397371,15.4393735463921));
#9895=CARTESIAN_POINT('Ctrl Pts',(0.436799825927911,2.41265443022054,15.4350941166783));
#9896=CARTESIAN_POINT('Ctrl Pts',(0.517079988014912,2.39532430706042,15.4308146869644));
#9897=CARTESIAN_POINT('Ctrl Pts',(0.5973601501019,2.37799418390031,15.4265352572505));
#9898=CARTESIAN_POINT('Ctrl Pts',(0.676646233962757,2.35665008210104,15.4222558275366));
#9899=CARTESIAN_POINT('Ctrl Pts',(0.754520101635884,2.33144797630729,15.4179763978227));
#9900=CARTESIAN_POINT('Ctrl Pts',(0.831507257655783,2.30653283456915,15.4137456958824));
#9901=CARTESIAN_POINT('Ctrl Pts',(0.907403777978826,2.27775342892995,15.4095149939422));
#9902=CARTESIAN_POINT('Ctrl Pts',(0.981793887963674,2.24522404484657,15.4052842920019));
#9903=CARTESIAN_POINT('Ctrl Pts',(1.05607711982931,2.21274139653747,15.4010596684163));
#9904=CARTESIAN_POINT('Ctrl Pts',(1.12885781728258,2.17651965477312,15.3968350448306));
#9905=CARTESIAN_POINT('Ctrl Pts',(1.19973606806946,2.13672263454414,15.3926104212449));
#9906=CARTESIAN_POINT('Ctrl Pts',(1.27089328162873,2.09676898111705,15.3883691703766));
#9907=CARTESIAN_POINT('Ctrl Pts',(1.34013258959538,2.05321199180259,15.3841279195084));
#9908=CARTESIAN_POINT('Ctrl Pts',(1.4070703573616,2.00626599917217,15.3798866686401));
#9909=CARTESIAN_POINT('Ctrl Pts',(1.47362537325352,1.95958844493266,15.3756696693531));
#9910=CARTESIAN_POINT('Ctrl Pts',(1.53790471347362,1.90956080874419,15.3714526700662));
#9911=CARTESIAN_POINT('Ctrl Pts',(1.59955822498862,1.85643845437204,15.3672356707792));
#9912=CARTESIAN_POINT('Ctrl Pts',(1.66119129701568,1.80333371122259,15.3630200695198));
#9913=CARTESIAN_POINT('Ctrl Pts',(1.72019991700277,1.7471365906119,15.3588044682603));
#9914=CARTESIAN_POINT('Ctrl Pts',(1.77626689188751,1.6881428194274,15.3545888670009));
#9915=CARTESIAN_POINT('Ctrl Pts',(1.8323324677565,1.62915052028977,15.3503733709316));
#9916=CARTESIAN_POINT('Ctrl Pts',(1.8854562248713,1.5673620471762,15.3461578748623));
#9917=CARTESIAN_POINT('Ctrl Pts',(1.93535875271642,1.50310902741084,15.341942378793));
#9918=CARTESIAN_POINT('Ctrl Pts',(1.98579006431885,1.43817516131008,15.3376822139274));
#9919=CARTESIAN_POINT('Ctrl Pts',(2.03293116385478,1.37072457999735,15.3334220490618));
#9920=CARTESIAN_POINT('Ctrl Pts',(2.07653744401255,1.30113123612256,15.3291618841962));
#9921=CARTESIAN_POINT('Ctrl Pts',(2.11974934113627,1.23216730695611,15.3249402490273));
#9922=CARTESIAN_POINT('Ctrl Pts',(2.15948992514981,1.16109965892827,15.3207186138583));
#9923=CARTESIAN_POINT('Ctrl Pts',(2.19556744143376,1.08831698512703,15.3164969786893));
#9924=CARTESIAN_POINT('Ctrl Pts',(2.23213886198761,1.01453791032408,15.3122175489754));
#9925=CARTESIAN_POINT('Ctrl Pts',(2.26494596294879,0.938996950216263,15.3079381192615));
#9926=CARTESIAN_POINT('Ctrl Pts',(2.29384016231614,0.862118066012683,15.3036586895476));
#9927=CARTESIAN_POINT('Ctrl Pts',(2.3227343616835,0.785239181809103,15.2993792598337));
#9928=CARTESIAN_POINT('Ctrl Pts',(2.34771557258479,0.707022860765963,15.2950998301198));
#9929=CARTESIAN_POINT('Ctrl Pts',(2.36868854703008,0.627905102040517,15.2908204004059));
#9930=CARTESIAN_POINT('Ctrl Pts',(2.38942271247052,0.549688218547485,15.2865896984657));
#9931=CARTESIAN_POINT('Ctrl Pts',(2.40631748587874,0.470296136967602,15.2823589965254));
#9932=CARTESIAN_POINT('Ctrl Pts',(2.41924384829611,0.390140298458688,15.2781282945852));
#9933=CARTESIAN_POINT('Ctrl Pts',(2.43215163908745,0.310099621834392,15.2739036709995));
#9934=CARTESIAN_POINT('Ctrl Pts',(2.44110226899643,0.229297822829221,15.2696790474138));
#9935=CARTESIAN_POINT('Ctrl Pts',(2.44601694947692,0.148159822055846,15.2654544238281));
#9936=CARTESIAN_POINT('Ctrl Pts',(2.45095097316745,0.066702478164027,15.2612131729599));
#9937=CARTESIAN_POINT('Ctrl Pts',(2.45181708829446,-0.0150932609085146,
15.2569719220916));
#9938=CARTESIAN_POINT('Ctrl Pts',(2.44858779225843,-0.096788809285944,15.2527306712233));
#9939=CARTESIAN_POINT('Ctrl Pts',(2.44537696142003,-0.178017220420699,15.2485136719363));
#9940=CARTESIAN_POINT('Ctrl Pts',(2.4381174462129,-0.259146114168169,15.2442966726494));
#9941=CARTESIAN_POINT('Ctrl Pts',(2.4268343686435,-0.339742839763735,15.2400796733624));
#9942=CARTESIAN_POINT('Ctrl Pts',(2.41555503166114,-0.42031284578157,15.235864072103));
#9943=CARTESIAN_POINT('Ctrl Pts',(2.40025484563934,-0.500350573794205,15.2316484708435));
#9944=CARTESIAN_POINT('Ctrl Pts',(2.38101071310185,-0.579429231308029,15.2274328695841));
#9945=CARTESIAN_POINT('Ctrl Pts',(2.36176706075519,-0.658505915605031,15.2232173735148));
#9946=CARTESIAN_POINT('Ctrl Pts',(2.33857976857895,-0.736623125368398,15.2190018774455));
#9947=CARTESIAN_POINT('Ctrl Pts',(2.31157637857764,-0.813366397143319,15.2147863813762));
#9948=CARTESIAN_POINT('Ctrl Pts',(2.2842868516882,-0.890922866111946,15.2105262165106));
#9949=CARTESIAN_POINT('Ctrl Pts',(2.25310001776086,-0.96707564396322,15.206266051645));
#9950=CARTESIAN_POINT('Ctrl Pts',(2.218197847003,-1.04141661286502,15.2020058867794));
#9951=CARTESIAN_POINT('Ctrl Pts',(2.18361133774962,-1.11508522868453,15.1977842516105));
#9952=CARTESIAN_POINT('Ctrl Pts',(2.1453767009966,-1.18697429020506,15.1935626164415));
#9953=CARTESIAN_POINT('Ctrl Pts',(2.10371691515927,-1.25671213524529,15.1893409812725));
#9954=CARTESIAN_POINT('Ctrl Pts',(2.0614868033065,-1.32740469732228,15.1850615515586));
#9955=CARTESIAN_POINT('Ctrl Pts',(2.01573732590765,-1.39588628495882,15.1807821218447));
#9956=CARTESIAN_POINT('Ctrl Pts',(1.96674448748316,-1.4618024390986,15.1765026921308));
#9957=CARTESIAN_POINT('Ctrl Pts',(1.91775164905867,-1.52771859323837,15.1722232624169));
#9958=CARTESIAN_POINT('Ctrl Pts',(1.8655158122392,-1.59106897703662,15.1679438327031));
#9959=CARTESIAN_POINT('Ctrl Pts',(1.81035197820612,-1.65153745492047,15.1636644029892));
#9960=CARTESIAN_POINT('Ctrl Pts',(1.75581626777774,-1.71131740781391,15.1594337010489));
#9961=CARTESIAN_POINT('Ctrl Pts',(1.69821380838738,-1.76850562913858,15.1552029991086));
#9962=CARTESIAN_POINT('Ctrl Pts',(1.63782066989113,-1.82277088611744,15.1509722971684));
#9963=CARTESIAN_POINT('Ctrl Pts',(1.57751429971735,-1.87695817885346,15.1467476735827));
#9964=CARTESIAN_POINT('Ctrl Pts',(1.51442555639587,-1.92823053948142,15.142523049997));
#9965=CARTESIAN_POINT('Ctrl Pts',(1.44886903807624,-1.97629166888494,15.1382984264114));
#9966=CARTESIAN_POINT('Ctrl Pts',(1.38305450227046,-2.0245419573852,15.1340571755431));
#9967=CARTESIAN_POINT('Ctrl Pts',(1.31475304428415,-2.06955533231734,15.1298159246748));
#9968=CARTESIAN_POINT('Ctrl Pts',(1.24431851825873,-2.11107121507504,15.1255746738065));
#9969=CARTESIAN_POINT('Ctrl Pts',(1.17428673866117,-2.15234970894942,15.1213576745196));
#9970=CARTESIAN_POINT('Ctrl Pts',(1.10214662337587,-2.19017036109005,15.1171406752326));
#9971=CARTESIAN_POINT('Ctrl Pts',(1.02827552813991,-2.22432005076351,15.1129236759457));
#9972=CARTESIAN_POINT('Ctrl Pts',(0.954428922788017,-2.25845841906779,15.1087080746862));
#9973=CARTESIAN_POINT('Ctrl Pts',(0.878852898870565,-2.28892804667559,15.1044924734268));
#9974=CARTESIAN_POINT('Ctrl Pts',(0.801947921324733,-2.31556251945028,15.1002768721674));
#9975=CARTESIAN_POINT('Ctrl Pts',(0.72504486275666,-2.34219632762611,15.0960613760981));
#9976=CARTESIAN_POINT('Ctrl Pts',(0.646813356299004,-2.36499502006823,15.0918458800287));
#9977=CARTESIAN_POINT('Ctrl Pts',(0.567670917971575,-2.38384143325208,15.0876303839594));
#9978=CARTESIAN_POINT('Ctrl Pts',(0.487689860085084,-2.40288754928875,15.0833702190939));
#9979=CARTESIAN_POINT('Ctrl Pts',(0.406778917865914,-2.41789700011409,15.0791100542283));
#9980=CARTESIAN_POINT('Ctrl Pts',(0.325379740277694,-2.42880181871984,15.0748498893627));
#9981=CARTESIAN_POINT('Ctrl Pts',(0.244716751479458,-2.43960801218648,15.0706282541937));
#9982=CARTESIAN_POINT('Ctrl Pts',(0.163574796900046,-2.44638354323397,15.0664066190248));
#9983=CARTESIAN_POINT('Ctrl Pts',(0.0823870774699844,-2.44911466033462,
15.0621849838558));
#9984=CARTESIAN_POINT('Ctrl Pts',(8.78912479101573E-5,-2.45188316666093,
15.0579055541419));
#9985=CARTESIAN_POINT('Ctrl Pts',(-0.082257827778794,-2.45049569217384,
15.053626124428));
#9986=CARTESIAN_POINT('Ctrl Pts',(-0.164202633374892,-2.44499238141814,
15.0493466947141));
#9987=CARTESIAN_POINT('Ctrl Pts',(-0.246147438970991,-2.43948907066244,
15.0450672650002));
#9988=CARTESIAN_POINT('Ctrl Pts',(-0.327690851599183,-2.42987004615082,
15.0407878352863));
#9989=CARTESIAN_POINT('Ctrl Pts',(-0.408396532527029,-2.41622898795207,
15.0365084055725));
#9990=CARTESIAN_POINT('Ctrl Pts',(-0.488183257328885,-2.40274325381295,
15.0322777036322));
#9991=CARTESIAN_POINT('Ctrl Pts',(-0.567451338534771,-2.38527593323865,
15.0280470016919));
#9992=CARTESIAN_POINT('Ctrl Pts',(-0.645772822204954,-2.36387980068815,
15.0238162997517));
#9993=CARTESIAN_POINT('Ctrl Pts',(-0.723981779453858,-2.34251440849282,
15.019591676166));
#9994=CARTESIAN_POINT('Ctrl Pts',(-0.801246395387222,-2.31723153636678,
15.0153670525803));
#9995=CARTESIAN_POINT('Ctrl Pts',(-0.87714722712885,-2.28813526521929,15.0111424289946));
#9996=CARTESIAN_POINT('Ctrl Pts',(-0.953346789527534,-2.25892447690515,
15.0069011781263));
#9997=CARTESIAN_POINT('Ctrl Pts',(-1.02817134162219,-2.22587028670684,15.002659927258));
#9998=CARTESIAN_POINT('Ctrl Pts',(-1.10121021916515,-2.1891291198114,14.9984186763898));
#9999=CARTESIAN_POINT('Ctrl Pts',(-1.17383145853143,-2.1525980398514,14.9942016771028));
#10000=CARTESIAN_POINT('Ctrl Pts',(-1.24468696936429,-2.11242224432306,
14.9899846778158));
#10001=CARTESIAN_POINT('Ctrl Pts',(-1.3133932639374,-2.0688036118114,14.9857676785289));
#10002=CARTESIAN_POINT('Ctrl Pts',(-1.38207678087082,-2.02519943983061,
14.9815520772695));
#10003=CARTESIAN_POINT('Ctrl Pts',(-1.44861210416253,-1.97815494650574,
14.97733647601));
#10004=CARTESIAN_POINT('Ctrl Pts',(-1.51264250341415,-1.92791672716043,
14.9731208747506));
#10005=CARTESIAN_POINT('Ctrl Pts',(-1.57667130494187,-1.87767976138849,
14.9689053786813));
#10006=CARTESIAN_POINT('Ctrl Pts',(-1.63819494148964,-1.8242495159687,14.964689882612));
#10007=CARTESIAN_POINT('Ctrl Pts',(-1.69688885882355,-1.76791358691552,
14.9604743865427));
#10008=CARTESIAN_POINT('Ctrl Pts',(-1.7562047163974,-1.7109807036493,14.9562142216771));
#10009=CARTESIAN_POINT('Ctrl Pts',(-1.81263016772042,-1.65108051476925,
14.9519540568115));
#10010=CARTESIAN_POINT('Ctrl Pts',(-1.86586895503826,-1.58854754182065,
14.9476938919459));
#10011=CARTESIAN_POINT('Ctrl Pts',(-1.91862624119627,-1.52658012831694,
14.943472256777));
#10012=CARTESIAN_POINT('Ctrl Pts',(-1.9682540353506,-1.46202777234666,14.939250621608));
#10013=CARTESIAN_POINT('Ctrl Pts',(-2.01450623568521,-1.39524724561112,
14.935028986439));
#10014=CARTESIAN_POINT('Ctrl Pts',(-2.06139163258072,-1.32755248777827,
14.9307495567251));
#10015=CARTESIAN_POINT('Ctrl Pts',(-2.10480805075351,-1.25756850989386,
14.9264701270112));
#10016=CARTESIAN_POINT('Ctrl Pts',(-2.14454698933919,-1.18569324047842,
14.9221906972973));
#10017=CARTESIAN_POINT('Ctrl Pts',(-2.18428592792488,-1.11381797106297,
14.9179112675834));
#10018=CARTESIAN_POINT('Ctrl Pts',(-2.22034723029976,-1.04005187962091,
14.9136318378696));
#10019=CARTESIAN_POINT('Ctrl Pts',(-2.25257341972762,-0.964812540723137,
14.9093524081557));
#10020=CARTESIAN_POINT('Ctrl Pts',(-2.28784259062658,-0.882468672303579,
14.9046688901658));
#10021=CARTESIAN_POINT('Ctrl Pts',(-2.31863234322746,-0.798096502575592,
14.899985372176));
#10022=CARTESIAN_POINT('Ctrl Pts',(-2.3447298650929,-0.712174213055641,
14.8953018541861));
#10023=CARTESIAN_POINT('Ctrl Pts',(-2.3707485750078,-0.626511400403514,
14.8906324799602));
#10024=CARTESIAN_POINT('Ctrl Pts',(-2.39210319657218,-0.539308069372384,
14.8859631057343));
#10025=CARTESIAN_POINT('Ctrl Pts',(-2.40862911253215,-0.451061024987314,
14.8812937315084));
#10026=CARTESIAN_POINT('Ctrl Pts',(-2.42506955792523,-0.363270386463663,
14.8766485068705));
#10027=CARTESIAN_POINT('Ctrl Pts',(-2.4367309933493,-0.274447073716981,
14.8720032822326));
#10028=CARTESIAN_POINT('Ctrl Pts',(-2.44349925207793,-0.185099041311885,
14.8673580575947));
#10029=CARTESIAN_POINT('Ctrl Pts',(-2.44812801520219,-0.123994569068216,
14.8641812221087));
#10030=CARTESIAN_POINT('Ctrl Pts',(-2.45046918747776,-0.062645071709354,
14.8610043866226));
#10031=CARTESIAN_POINT('Ctrl Pts',(-2.4504996977374,-0.00121712321269822,
14.8578275511366));
#10032=CARTESIAN_POINT('',(-2.450499106739,0.00209233634422269,14.0578274722887));
#10033=CARTESIAN_POINT('Ctrl Pts',(-2.44705070124995,-0.00121434961548067,
14.8578274962121));
#10034=CARTESIAN_POINT('Ctrl Pts',(-2.44487279928209,0.485573530690027,
14.8326171343877));
#10035=CARTESIAN_POINT('Ctrl Pts',(-2.06824721923167,1.79388671502831,14.765021440091));
#10036=CARTESIAN_POINT('Ctrl Pts',(0.0634192762513089,2.89675751214696,
14.6550404133223));
#10037=CARTESIAN_POINT('Ctrl Pts',(2.46980661816694,1.51501859976684,14.5278844159054));
#10038=CARTESIAN_POINT('Ctrl Pts',(2.61094584679872,-1.25625947712439,14.4007284184888));
#10039=CARTESIAN_POINT('Ctrl Pts',(0.357387405644541,-2.87532612603628,
14.2735724210721));
#10040=CARTESIAN_POINT('Ctrl Pts',(-1.96297980716343,-1.9601448883806,14.1592721136464));
#10041=CARTESIAN_POINT('Ctrl Pts',(-2.44422976160869,-0.567055827848684,
14.0873571386931));
#10042=CARTESIAN_POINT('Ctrl Pts',(-2.44883291810884,0.00209045259362897,
14.0578274962121));
#10043=CARTESIAN_POINT('',(-2.45089304864667,0.000179724721355419,13.2578274962121));
#10044=CARTESIAN_POINT('Ctrl Pts',(-2.450499106739,0.00209233634422269,
14.0578274722887));
#10045=CARTESIAN_POINT('Ctrl Pts',(-2.45041577647118,0.0996869450801318,
14.0527672681355));
#10046=CARTESIAN_POINT('Ctrl Pts',(-2.44449835478114,0.197027745386937,
14.0477070639824));
#10047=CARTESIAN_POINT('Ctrl Pts',(-2.43286032705182,0.293497664483561,
14.0426468598292));
#10048=CARTESIAN_POINT('Ctrl Pts',(-2.42106460921774,0.39127470812082,14.0375180921581));
#10049=CARTESIAN_POINT('Ctrl Pts',(-2.40339228844355,0.488157094540066,
14.032389324487));
#10050=CARTESIAN_POINT('Ctrl Pts',(-2.38001045809076,0.583524180628866,
14.0272605568159));
#10051=CARTESIAN_POINT('Ctrl Pts',(-2.36785304147166,0.63311043541895,14.0245938466234));
#10052=CARTESIAN_POINT('Ctrl Pts',(-2.354152852917,0.682287388051048,14.021927136431));
#10053=CARTESIAN_POINT('Ctrl Pts',(-2.33893842772714,0.730970096037636,
14.0192604262385));
#10054=CARTESIAN_POINT('Ctrl Pts',(-2.31480093488946,0.808204595578842,
14.0150297242983));
#10055=CARTESIAN_POINT('Ctrl Pts',(-2.28678837606431,0.884387484301744,
14.010799022358));
#10056=CARTESIAN_POINT('Ctrl Pts',(-2.25501083799085,0.959101856188274,
14.0065683204177));
#10057=CARTESIAN_POINT('Ctrl Pts',(-2.22327895549577,1.03370888408064,14.0023436968321));
#10058=CARTESIAN_POINT('Ctrl Pts',(-2.18779301727481,1.106851161095,13.9981190732464));
#10059=CARTESIAN_POINT('Ctrl Pts',(-2.14871279704752,1.17812714331018,13.9938944496607));
#10060=CARTESIAN_POINT('Ctrl Pts',(-2.10947876480526,1.24968365368974,13.9896531987924));
#10061=CARTESIAN_POINT('Ctrl Pts',(-2.06662223866416,1.3193586940769,13.9854119479241));
#10062=CARTESIAN_POINT('Ctrl Pts',(-2.0203536715087,1.38676648792121,13.9811706970558));
#10063=CARTESIAN_POINT('Ctrl Pts',(-1.97434966920793,1.45378884226998,13.9769536977689));
#10064=CARTESIAN_POINT('Ctrl Pts',(-1.92497280611315,1.51856942078425,13.9727366984819));
#10065=CARTESIAN_POINT('Ctrl Pts',(-1.87247490186335,1.58075551300378,13.968519699195));
#10066=CARTESIAN_POINT('Ctrl Pts',(-1.81999440181729,1.6429209891733,13.9643040979356));
#10067=CARTESIAN_POINT('Ctrl Pts',(-1.76439521510269,1.70249333203805,13.9600884966761));
#10068=CARTESIAN_POINT('Ctrl Pts',(-1.70596985481517,1.75915238238815,13.9558728954167));
#10069=CARTESIAN_POINT('Ctrl Pts',(-1.64754595239124,1.81581001894866,13.9516573993474));
#10070=CARTESIAN_POINT('Ctrl Pts',(-1.58629635121681,1.86955418454522,13.9474419032781));
#10071=CARTESIAN_POINT('Ctrl Pts',(-1.52254984401921,1.92010213855333,13.9432264072088));
#10072=CARTESIAN_POINT('Ctrl Pts',(-1.45812785766163,1.9711857154687,13.9389662423432));
#10073=CARTESIAN_POINT('Ctrl Pts',(-1.39115610371203,2.01900462760382,13.9347060774777));
#10074=CARTESIAN_POINT('Ctrl Pts',(-1.32200604904638,2.06331050893577,13.9304459126121));
#10075=CARTESIAN_POINT('Ctrl Pts',(-1.2534813999018,2.10721567991493,13.9262242774431));
#10076=CARTESIAN_POINT('Ctrl Pts',(-1.18281813218952,2.14767092939085,13.9220026422742));
#10077=CARTESIAN_POINT('Ctrl Pts',(-1.11040298547042,2.18448059269438,13.9177810071052));
#10078=CARTESIAN_POINT('Ctrl Pts',(-1.03699646922666,2.22179418342283,13.9135015773913));
#10079=CARTESIAN_POINT('Ctrl Pts',(-0.961790195746483,2.25536141382249,
13.9092221476774));
#10080=CARTESIAN_POINT('Ctrl Pts',(-0.88520660629556,2.28502943398344,13.9049427179635));
#10081=CARTESIAN_POINT('Ctrl Pts',(-0.808623016844648,2.31469745414439,
13.9006632882497));
#10082=CARTESIAN_POINT('Ctrl Pts',(-0.730662597778344,2.34046617228505,
13.8963838585358));
#10083=CARTESIAN_POINT('Ctrl Pts',(-0.651760365548603,2.36223594839719,
13.8921044288219));
#10084=CARTESIAN_POINT('Ctrl Pts',(-0.573756554456367,2.38375784271352,
13.8878737268816));
#10085=CARTESIAN_POINT('Ctrl Pts',(-0.494538886439511,2.4014523915938,13.8836430249414));
#10086=CARTESIAN_POINT('Ctrl Pts',(-0.414517480633836,2.4151864334351,13.8794123230011));
#10087=CARTESIAN_POINT('Ctrl Pts',(-0.334611043569813,2.42890074323731,
13.8751876994154));
#10088=CARTESIAN_POINT('Ctrl Pts',(-0.253903616583601,2.43866576896866,
13.8709630758297));
#10089=CARTESIAN_POINT('Ctrl Pts',(-0.172819304132251,2.44439844095009,
13.8667384522441));
#10090=CARTESIAN_POINT('Ctrl Pts',(-0.0914158598692677,2.45015367559426,
13.8624972013758));
#10091=CARTESIAN_POINT('Ctrl Pts',(-0.0096330145461995,2.45184462109823,
13.8582559505075));
#10092=CARTESIAN_POINT('Ctrl Pts',(0.0720909456151732,2.44943935331339,
13.8540146996392));
#10093=CARTESIAN_POINT('Ctrl Pts',(0.153347606074584,2.44704783891148,13.8497977003522));
#10094=CARTESIAN_POINT('Ctrl Pts',(0.234545583426512,2.44060684242901,13.8455807010653));
#10095=CARTESIAN_POINT('Ctrl Pts',(0.315251995562358,2.43013712150034,13.8413637017783));
#10096=CARTESIAN_POINT('Ctrl Pts',(0.395931651756961,2.41967087151321,13.8371481005189));
#10097=CARTESIAN_POINT('Ctrl Pts',(0.476119605525095,2.4051786091569,13.8329324992594));
#10098=CARTESIAN_POINT('Ctrl Pts',(0.555388310547285,2.38673292902818,13.828716898));
#10099=CARTESIAN_POINT('Ctrl Pts',(0.634655037610613,2.3682877091668,13.8245014019307));
#10100=CARTESIAN_POINT('Ctrl Pts',(0.713002108820923,2.34588937412897,13.8202859058614));
#10101=CARTESIAN_POINT('Ctrl Pts',(0.790013795593493,2.31966127975012,13.8160704097921));
#10102=CARTESIAN_POINT('Ctrl Pts',(0.867841523774046,2.2931552637731,13.8118102449265));
#10103=CARTESIAN_POINT('Ctrl Pts',(0.944304934860477,2.26273798332441,13.8075500800609));
#10104=CARTESIAN_POINT('Ctrl Pts',(1.01899409668334,2.2285872836675,13.8032899151953));
#10105=CARTESIAN_POINT('Ctrl Pts',(1.09300775630467,2.19474544907535,13.7990682800263));
#10106=CARTESIAN_POINT('Ctrl Pts',(1.16527874189591,2.15723772646233,13.7948466448574));
#10107=CARTESIAN_POINT('Ctrl Pts',(1.23543316153471,2.1162833348539,13.7906250096884));
#10108=CARTESIAN_POINT('Ctrl Pts',(1.30654800115186,2.07476827413718,13.7863455799745));
#10109=CARTESIAN_POINT('Ctrl Pts',(1.37548747002716,2.02971173012123,13.7820661502606));
#10110=CARTESIAN_POINT('Ctrl Pts',(1.44189434374329,1.98138611872626,13.7777867205467));
#10111=CARTESIAN_POINT('Ctrl Pts',(1.50830121745942,1.93306050733129,13.7735072908328));
#10112=CARTESIAN_POINT('Ctrl Pts',(1.57217515553177,1.88146618777257,13.7692278611189));
#10113=CARTESIAN_POINT('Ctrl Pts',(1.63319686181335,1.8269149571239,13.764948431405));
#10114=CARTESIAN_POINT('Ctrl Pts',(1.69352374376336,1.77298487466464,13.7607177294648));
#10115=CARTESIAN_POINT('Ctrl Pts',(1.75128995276369,1.71596206270458,13.7564870275245));
#10116=CARTESIAN_POINT('Ctrl Pts',(1.80616148883633,1.65611923672317,13.7522563255843));
#10117=CARTESIAN_POINT('Ctrl Pts',(1.86095418960994,1.5963623884165,13.7480317019986));
#10118=CARTESIAN_POINT('Ctrl Pts',(1.91286016552321,1.53379391262591,13.7438070784129));
#10119=CARTESIAN_POINT('Ctrl Pts',(1.96157995994131,1.46872540345588,13.7395824548272));
#10120=CARTESIAN_POINT('Ctrl Pts',(2.01049150583125,1.40340079750728,13.7353412039589));
#10121=CARTESIAN_POINT('Ctrl Pts',(2.05619138227933,1.33555675297525,13.7310999530907));
#10122=CARTESIAN_POINT('Ctrl Pts',(2.0984154554648,1.26554447818575,13.7268587022224));
#10123=CARTESIAN_POINT('Ctrl Pts',(2.14039809031595,1.19593253538064,13.7226417029354));
#10124=CARTESIAN_POINT('Ctrl Pts',(2.17894432091395,1.1241774932692,13.7184247036485));
#10125=CARTESIAN_POINT('Ctrl Pts',(2.21383723189433,1.05065453916997,13.7142077043615));
#10126=CARTESIAN_POINT('Ctrl Pts',(2.24871857511137,0.977155959538485,13.7099921031021));
#10127=CARTESIAN_POINT('Ctrl Pts',(2.27994880462262,0.901891051630504,13.7057765018427));
#10128=CARTESIAN_POINT('Ctrl Pts',(2.30735747623917,0.825258581805236,13.7015609005832));
#10129=CARTESIAN_POINT('Ctrl Pts',(2.33476546393858,0.74862802415801,13.6973454045139));
#10130=CARTESIAN_POINT('Ctrl Pts',(2.35835192774053,0.670630410700876,13.6931299084446));
#10131=CARTESIAN_POINT('Ctrl Pts',(2.37799549961099,0.591682054679605,13.6889144123753));
#10132=CARTESIAN_POINT('Ctrl Pts',(2.39784722129248,0.511897135659761,13.6846542475098));
#10133=CARTESIAN_POINT('Ctrl Pts',(2.4136718605078,0.431141671581015,13.6803940826442));
#10134=CARTESIAN_POINT('Ctrl Pts',(2.42539699986736,0.349856603531223,13.6761339177786));
#10135=CARTESIAN_POINT('Ctrl Pts',(2.43701609495948,0.269306692244254,13.6719122826096));
#10136=CARTESIAN_POINT('Ctrl Pts',(2.44460956275511,0.188237192055988,13.6676906474407));
#10137=CARTESIAN_POINT('Ctrl Pts',(2.44815928378303,0.107081143190291,13.6634690122717));
#10138=CARTESIAN_POINT('Ctrl Pts',(2.45175760079408,0.0248140611052921,
13.6591895825578));
#10139=CARTESIAN_POINT('Ctrl Pts',(2.45120061758858,-0.0575414626753487,
13.6549101528439));
#10140=CARTESIAN_POINT('Ctrl Pts',(2.44652396436944,-0.139537599829008,
13.6506307231301));
#10141=CARTESIAN_POINT('Ctrl Pts',(2.4418473111503,-0.221533736982679,13.6463512934162));
#10142=CARTESIAN_POINT('Ctrl Pts',(2.43305110558808,-0.303170006760965,
13.6420718637023));
#10143=CARTESIAN_POINT('Ctrl Pts',(2.4202246227017,-0.384009147896767,13.6377924339884));
#10144=CARTESIAN_POINT('Ctrl Pts',(2.40754418870418,-0.463927813260419,
13.6335617320481));
#10145=CARTESIAN_POINT('Ctrl Pts',(2.39087714044234,-0.543368013967231,
13.6293310301079));
#10146=CARTESIAN_POINT('Ctrl Pts',(2.37027193396235,-0.621901285631722,
13.6251003281676));
#10147=CARTESIAN_POINT('Ctrl Pts',(2.3496963314944,-0.700321726593826,13.6208757045819));
#10148=CARTESIAN_POINT('Ctrl Pts',(2.32519392503057,-0.777837380340297,
13.6166510809963));
#10149=CARTESIAN_POINT('Ctrl Pts',(2.29686456028875,-0.854027775713154,
13.6124264574106));
#10150=CARTESIAN_POINT('Ctrl Pts',(2.26842369677213,-0.930518041408317,
13.6081852065423));
#10151=CARTESIAN_POINT('Ctrl Pts',(2.23612576042997,-1.00567212575424,13.603943955674));
#10152=CARTESIAN_POINT('Ctrl Pts',(2.20012302712488,-1.07907780790583,13.5997027048057));
#10153=CARTESIAN_POINT('Ctrl Pts',(2.164326158373,-1.1520637544826,13.5954857055188));
#10154=CARTESIAN_POINT('Ctrl Pts',(2.12486695278486,-1.22332081768395,13.5912687062318));
#10155=CARTESIAN_POINT('Ctrl Pts',(2.0819434113731,-1.29246349342646,13.5870517069449));
#10156=CARTESIAN_POINT('Ctrl Pts',(2.03903410005436,-1.36158324685933,13.5828361056854));
#10157=CARTESIAN_POINT('Ctrl Pts',(1.99266297873596,-1.42858961003027,13.578620504426));
#10158=CARTESIAN_POINT('Ctrl Pts',(1.94307303273131,-1.49312338387434,13.5744049031666));
#10159=CARTESIAN_POINT('Ctrl Pts',(1.89348432412387,-1.5576555474341,13.5701894070973));
#10160=CARTESIAN_POINT('Ctrl Pts',(1.84067723475027,-1.61971487623792,13.565973911028));
#10161=CARTESIAN_POINT('Ctrl Pts',(1.78493607301241,-1.67897393227502,13.5617584149587));
#10162=CARTESIAN_POINT('Ctrl Pts',(1.72860425941355,-1.73886091694939,13.5574982500931));
#10163=CARTESIAN_POINT('Ctrl Pts',(1.66927614260114,-1.79588756633691,13.5532380852275));
#10164=CARTESIAN_POINT('Ctrl Pts',(1.60728323947942,-1.84975426424392,13.5489779203619));
#10165=CARTESIAN_POINT('Ctrl Pts',(1.54585101131401,-1.90313378205489,13.5447562851929));
#10166=CARTESIAN_POINT('Ctrl Pts',(1.48180241256323,-1.95341003501791,13.540534650024));
#10167=CARTESIAN_POINT('Ctrl Pts',(1.4154917149567,-2.00033333594402,13.536313014855));
#10168=CARTESIAN_POINT('Ctrl Pts',(1.34827321825363,-2.0478990208553,13.5320335851411));
#10169=CARTESIAN_POINT('Ctrl Pts',(1.2787306347668,-2.09201898923083,13.5277541554272));
#10170=CARTESIAN_POINT('Ctrl Pts',(1.2072597701414,-2.13248073787271,13.5234747257133));
#10171=CARTESIAN_POINT('Ctrl Pts',(1.135788905516,-2.1729424865146,13.5191952959994));
#10172=CARTESIAN_POINT('Ctrl Pts',(1.06239022765311,-2.20974585407236,13.5149158662855));
#10173=CARTESIAN_POINT('Ctrl Pts',(0.987479701805409,-2.24272916075979,
13.5106364365716));
#10174=CARTESIAN_POINT('Ctrl Pts',(0.913422145486526,-2.27533690266182,
13.5064057346314));
#10175=CARTESIAN_POINT('Ctrl Pts',(0.837608461737434,-2.3043338221964,13.5021750326911));
#10176=CARTESIAN_POINT('Ctrl Pts',(0.760425119891014,-2.32952868345482,
13.4979443307509));
#10177=CARTESIAN_POINT('Ctrl Pts',(0.683352669269241,-2.35468734663017,
13.4937197071652));
#10178=CARTESIAN_POINT('Ctrl Pts',(0.604914907103674,-2.37605465728748,
13.4894950835795));
#10179=CARTESIAN_POINT('Ctrl Pts',(0.525519405338082,-2.39348691339917,
13.4852704599938));
#10180=CARTESIAN_POINT('Ctrl Pts',(0.445811418585593,-2.41098777942203,
13.4810292091255));
#10181=CARTESIAN_POINT('Ctrl Pts',(0.365138571434227,-2.42452235803849,
13.4767879582572));
#10182=CARTESIAN_POINT('Ctrl Pts',(0.283929885616584,-2.43399549507672,
13.4725467073889));
#10183=CARTESIAN_POINT('Ctrl Pts',(0.203185553149003,-2.44341446447419,
13.468329708102));
#10184=CARTESIAN_POINT('Ctrl Pts',(0.121911959836887,-2.44881825868415,
13.464112708815));
#10185=CARTESIAN_POINT('Ctrl Pts',(0.0405404212323698,-2.45016463206992,
13.4598957095281));
#10186=CARTESIAN_POINT('Ctrl Pts',(-0.0408041409269525,-2.45151055910344,
13.4556801082686));
#10187=CARTESIAN_POINT('Ctrl Pts',(-0.122246119268457,-2.4488017288125,
13.4514645070092));
#10188=CARTESIAN_POINT('Ctrl Pts',(-0.203351959348853,-2.44204795829832,
13.4472489057498));
#10189=CARTESIAN_POINT('Ctrl Pts',(-0.284455775629077,-2.43529435630815,
13.4430334096805));
#10190=CARTESIAN_POINT('Ctrl Pts',(-0.365223006958241,-2.42449605444568,
13.4388179136112));
#10191=CARTESIAN_POINT('Ctrl Pts',(-0.44522442942863,-2.40971480832068,
13.4346024175419));
#10192=CARTESIAN_POINT('Ctrl Pts',(-0.526073573539391,-2.39477693520299,
13.4303422526763));
#10193=CARTESIAN_POINT('Ctrl Pts',(-0.606140103294735,-2.37577127820813,
13.4260820878107));
#10194=CARTESIAN_POINT('Ctrl Pts',(-0.684992626946587,-2.3528143469107,
13.4218219229451));
#10195=CARTESIAN_POINT('Ctrl Pts',(-0.763131994204292,-2.33006504222541,
13.4176002877761));
#10196=CARTESIAN_POINT('Ctrl Pts',(-0.840078802224773,-2.30343585993608,
13.4133786526072));
#10197=CARTESIAN_POINT('Ctrl Pts',(-0.915431317714254,-2.27308947306259,
13.4091570174382));
#10198=CARTESIAN_POINT('Ctrl Pts',(-0.991815415556953,-2.24232764156884,
13.4048775877243));
#10199=CARTESIAN_POINT('Ctrl Pts',(-1.06656078941694,-2.20774626487551,
13.4005981580104));
#10200=CARTESIAN_POINT('Ctrl Pts',(-1.13927448176671,-2.16956306780771,
13.3963187282965));
#10201=CARTESIAN_POINT('Ctrl Pts',(-1.21198817411647,-2.13137987073991,
13.3920392985826));
#10202=CARTESIAN_POINT('Ctrl Pts',(-1.2826697959722,-2.08959515933193,13.3877598688687));
#10203=CARTESIAN_POINT('Ctrl Pts',(-1.3509582053218,-2.04447112414769,13.3834804391548));
#10204=CARTESIAN_POINT('Ctrl Pts',(-1.4183296521778,-1.99995300508036,13.3792584727291));
#10205=CARTESIAN_POINT('Ctrl Pts',(-1.48362752635937,-1.95201570998192,
13.3750365063033));
#10206=CARTESIAN_POINT('Ctrl Pts',(-1.54648268776746,-1.90087915092873,
13.3708145398775));
#10207=CARTESIAN_POINT('Ctrl Pts',(-1.60924745713495,-1.84981613138795,
13.3665986450639));
#10208=CARTESIAN_POINT('Ctrl Pts',(-1.66957613039138,-1.79556327676153,
13.3623827502502));
#10209=CARTESIAN_POINT('Ctrl Pts',(-1.72712802140429,-1.73838403342877,
13.3581668554366));
#10210=CARTESIAN_POINT('Ctrl Pts',(-1.78461321438406,-1.68127105626034,
13.3539558465075));
#10211=CARTESIAN_POINT('Ctrl Pts',(-1.83932769036507,-1.6212387574476,13.3497448375783));
#10212=CARTESIAN_POINT('Ctrl Pts',(-1.89096455202603,-1.55859016838327,
13.3455338286492));
#10213=CARTESIAN_POINT('Ctrl Pts',(-1.94256868566732,-1.49598128669443,
13.3413254887045));
#10214=CARTESIAN_POINT('Ctrl Pts',(-1.99109878021877,-1.43075976556846,
13.3371171487599));
#10215=CARTESIAN_POINT('Ctrl Pts',(-2.03628630091438,-1.36326385953286,
13.3329088088152));
#10216=CARTESIAN_POINT('Ctrl Pts',(-2.08145918883159,-1.29578981025374,
13.3287018316297));
#10217=CARTESIAN_POINT('Ctrl Pts',(-2.12329139246497,-1.22604322647744,
13.3244948544441));
#10218=CARTESIAN_POINT('Ctrl Pts',(-2.16155690934293,-1.15439247124704,
13.3202878772586));
#10219=CARTESIAN_POINT('Ctrl Pts',(-2.19982189664581,-1.08274270762626,
13.3160809582955));
#10220=CARTESIAN_POINT('Ctrl Pts',(-2.23452007640637,-1.00918923771928,
13.3118740393323));
#10221=CARTESIAN_POINT('Ctrl Pts',(-2.26547144885606,-0.934124919064908,
13.3076671203692));
#10222=CARTESIAN_POINT('Ctrl Pts',(-2.29645345916556,-0.858986296433364,
13.3034560370998));
#10223=CARTESIAN_POINT('Ctrl Pts',(-2.32368107498482,-0.782334270582736,
13.2992449538305));
#10224=CARTESIAN_POINT('Ctrl Pts',(-2.34702275463093,-0.704581038096152,
13.2950338705611));
#10225=CARTESIAN_POINT('Ctrl Pts',(-2.37037558795451,-0.626790651707603,
13.2908207750516));
#10226=CARTESIAN_POINT('Ctrl Pts',(-2.38983867445933,-0.547898464757276,
13.2866076795421));
#10227=CARTESIAN_POINT('Ctrl Pts',(-2.4053312616335,-0.46832870060312,13.2823945840326));
#10228=CARTESIAN_POINT('Ctrl Pts',(-2.42085181559001,-0.388615299350151,
13.2781738831616));
#10229=CARTESIAN_POINT('Ctrl Pts',(-2.43238748256562,-0.30822234053528,
13.2739531822907));
#10230=CARTESIAN_POINT('Ctrl Pts',(-2.43990926163131,-0.227580853776741,
13.2697324814198));
#10231=CARTESIAN_POINT('Ctrl Pts',(-2.4469812836525,-0.151761241794422,
13.2657641530172));
#10232=CARTESIAN_POINT('Ctrl Pts',(-2.45050555932682,-0.0757222904314883,
13.2617958246147));
#10233=CARTESIAN_POINT('Ctrl Pts',(-2.45049999341142,0.000179695898497237,
13.2578274962121));
#10234=CARTESIAN_POINT('',(-2.45049902004184,-0.00219152320485761,12.4578274962121));
#10235=CARTESIAN_POINT('Ctrl Pts',(-2.45452289746772,0.000179990899257165,
13.2578274962121));
#10236=CARTESIAN_POINT('Ctrl Pts',(-2.45453302561943,0.00977866883437539,
13.2573264780541));
#10237=CARTESIAN_POINT('Ctrl Pts',(-2.45448160011236,0.0193772351782657,
13.2568254598961));
#10238=CARTESIAN_POINT('Ctrl Pts',(-2.44478267249261,0.840936583347449,
13.2139391092659));
#10239=CARTESIAN_POINT('Ctrl Pts',(-1.53984848482298,2.45440272420173,13.1291684443213));
#10240=CARTESIAN_POINT('Ctrl Pts',(1.22986534347375,2.62348190878122,13.0020124469047));
#10241=CARTESIAN_POINT('Ctrl Pts',(2.87157581782199,0.386365644539962,12.8748564494879));
#10242=CARTESIAN_POINT('Ctrl Pts',(1.87954498804306,-2.20511603474788,12.7477004520711));
#10243=CARTESIAN_POINT('Ctrl Pts',(-0.836359972883942,-2.7741175325747,
12.6205444546545));
#10244=CARTESIAN_POINT('Ctrl Pts',(-2.31723869397904,-1.27307296623665,
12.5239203157511));
#10245=CARTESIAN_POINT('Ctrl Pts',(-2.4513350646012,-0.230535143793987,
12.4696815093198));
#10246=CARTESIAN_POINT('Ctrl Pts',(-2.44936814623945,-0.00220089742423947,
12.4578280353609));
#10247=CARTESIAN_POINT('',(-2.45026621721638,0.000935076449264825,11.6578274533481));
#10248=CARTESIAN_POINT('Ctrl Pts',(-2.45049902004184,-0.00219152320485761,
12.4578274962121));
#10249=CARTESIAN_POINT('Ctrl Pts',(-2.45057110097417,0.078407328605816,
12.4536452785263));
#10250=CARTESIAN_POINT('Ctrl Pts',(-2.4466624732506,0.159090238605734,12.4494630608406));
#10251=CARTESIAN_POINT('Ctrl Pts',(-2.43877499133106,0.239430139410592,
12.4452808431548));
#10252=CARTESIAN_POINT('Ctrl Pts',(-2.43089124206696,0.319732020328914,
12.441100604653));
#10253=CARTESIAN_POINT('Ctrl Pts',(-2.41903242136504,0.399690743454207,
12.4369203661511));
#10254=CARTESIAN_POINT('Ctrl Pts',(-2.40325239789606,0.478882200553359,
12.4327401276493));
#10255=CARTESIAN_POINT('Ctrl Pts',(-2.38747480138559,0.558061478052139,
12.4285605320658));
#10256=CARTESIAN_POINT('Ctrl Pts',(-2.36777729279835,0.636473259442116,
12.4243809364822));
#10257=CARTESIAN_POINT('Ctrl Pts',(-2.34426496445777,0.71370303797574,12.4202013408987));
#10258=CARTESIAN_POINT('Ctrl Pts',(-2.32074874143639,0.790945609174209,
12.4160210529893));
#10259=CARTESIAN_POINT('Ctrl Pts',(-2.29341658455472,0.867005336426674,
12.41184076508));
#10260=CARTESIAN_POINT('Ctrl Pts',(-2.26242315094786,0.941483794897807,
12.4076604771707));
#10261=CARTESIAN_POINT('Ctrl Pts',(-2.23139545641759,1.01604458373585,12.4034755682657));
#10262=CARTESIAN_POINT('Ctrl Pts',(-2.1966985937168,1.08902017892346,12.3992906593607));
#10263=CARTESIAN_POINT('Ctrl Pts',(-2.15853467669386,1.1600337492979,12.3951057504556));
#10264=CARTESIAN_POINT('Ctrl Pts',(-2.12034575527428,1.23109384664386,12.3909180996643));
#10265=CARTESIAN_POINT('Ctrl Pts',(-2.07868550646702,1.30018895778788,12.3867304488729));
#10266=CARTESIAN_POINT('Ctrl Pts',(-2.03379981297172,1.36697058152551,12.3825427980816));
#10267=CARTESIAN_POINT('Ctrl Pts',(-1.98884110883373,1.43386083161799,12.3783483356972));
#10268=CARTESIAN_POINT('Ctrl Pts',(-1.94064677863175,1.49842971071624,12.3741538733129));
#10269=CARTESIAN_POINT('Ctrl Pts',(-1.88950296486554,1.56036175157056,12.3699594109285));
#10270=CARTESIAN_POINT('Ctrl Pts',(-1.87435517587672,1.57870480065947,12.3687170938927));
#10271=CARTESIAN_POINT('Ctrl Pts',(-1.85894889207212,1.59681678924601,12.3674747768568));
#10272=CARTESIAN_POINT('Ctrl Pts',(-1.8432921369087,1.61469017090294,12.366232459821));
#10273=CARTESIAN_POINT('Ctrl Pts',(-1.78997316716356,1.67555784660342,12.3620017578807));
#10274=CARTESIAN_POINT('Ctrl Pts',(-1.73353580191259,1.73389616839639,12.3577710559405));
#10275=CARTESIAN_POINT('Ctrl Pts',(-1.67424937452314,1.789368403071,12.3535403540002));
#10276=CARTESIAN_POINT('Ctrl Pts',(-1.61504812541672,1.84476093940802,12.3493157304146));
#10277=CARTESIAN_POINT('Ctrl Pts',(-1.55300628043559,1.89729525171528,12.3450911068289));
#10278=CARTESIAN_POINT('Ctrl Pts',(-1.48843239794972,1.94666875629462,12.3408664832432));
#10279=CARTESIAN_POINT('Ctrl Pts',(-1.42360436543798,1.9962365852197,12.3366252323749));
#10280=CARTESIAN_POINT('Ctrl Pts',(-1.35622463416943,2.04261831545925,12.3323839815066));
#10281=CARTESIAN_POINT('Ctrl Pts',(-1.28664173093628,2.08554628484081,12.3281427306383));
#10282=CARTESIAN_POINT('Ctrl Pts',(-1.21745670452995,2.12822879099152,12.3239257313514));
#10283=CARTESIAN_POINT('Ctrl Pts',(-1.14609403315411,2.16749667985552,12.3197087320644));
#10284=CARTESIAN_POINT('Ctrl Pts',(-1.07292669755181,2.20312926349785,12.3154917327775));
#10285=CARTESIAN_POINT('Ctrl Pts',(-0.999783618522003,2.23875003415913,
12.311276131518));
#10286=CARTESIAN_POINT('Ctrl Pts',(-0.924837481142166,2.27073768942736,
12.3070605302586));
#10287=CARTESIAN_POINT('Ctrl Pts',(-0.84848531263859,2.29891777239565,12.3028449289992));
#10288=CARTESIAN_POINT('Ctrl Pts',(-0.772135049318726,2.32709715219813,
12.2986294329299));
#10289=CARTESIAN_POINT('Ctrl Pts',(-0.694379261299608,2.3514689885923,12.2944139368606));
#10290=CARTESIAN_POINT('Ctrl Pts',(-0.615633016713481,2.37190772137793,
12.2901984407913));
#10291=CARTESIAN_POINT('Ctrl Pts',(-0.536052350768697,2.3925630297637,12.2859382759257));
#10292=CARTESIAN_POINT('Ctrl Pts',(-0.455460577744214,2.40920124798693,
12.2816781110601));
#10293=CARTESIAN_POINT('Ctrl Pts',(-0.374297886007959,2.42174551564155,
12.2774179461945));
#10294=CARTESIAN_POINT('Ctrl Pts',(-0.293869244241128,2.43417633068524,
12.2731963110256));
#10295=CARTESIAN_POINT('Ctrl Pts',(-0.212880443295602,2.44258696296552,
12.2689746758566));
#10296=CARTESIAN_POINT('Ctrl Pts',(-0.131764318647952,2.44695492691043,
12.2647530406876));
#10297=CARTESIAN_POINT('Ctrl Pts',(-0.0495377073469863,2.45138268865367,
12.2604736109737));
#10298=CARTESIAN_POINT('Ctrl Pts',(0.0328192455460188,2.45165625337551,
12.2561941812598));
#10299=CARTESIAN_POINT('Ctrl Pts',(0.11485837516566,2.44780673331338,12.2519147515459));
#10300=CARTESIAN_POINT('Ctrl Pts',(0.196897504785295,2.44395721325124,12.247635321832));
#10301=CARTESIAN_POINT('Ctrl Pts',(0.278618329220953,2.43598472122157,12.2433558921182));
#10302=CARTESIAN_POINT('Ctrl Pts',(0.35958270914079,2.42397411811409,12.2390764624043));
#10303=CARTESIAN_POINT('Ctrl Pts',(0.439625187255648,2.41210027387136,12.234845760464));
#10304=CARTESIAN_POINT('Ctrl Pts',(0.519229428313152,2.39623519297794,12.2306150585238));
#10305=CARTESIAN_POINT('Ctrl Pts',(0.597966501057326,2.37642300813918,12.2263843565835));
#10306=CARTESIAN_POINT('Ctrl Pts',(0.676590450293147,2.35663928795854,12.2221597329978));
#10307=CARTESIAN_POINT('Ctrl Pts',(0.754349258431024,2.33291983907684,12.2179351094121));
#10308=CARTESIAN_POINT('Ctrl Pts',(0.830821468793549,2.30536026186619,12.2137104858265));
#10309=CARTESIAN_POINT('Ctrl Pts',(0.907594658646335,2.27769221561218,12.2094692349582));
#10310=CARTESIAN_POINT('Ctrl Pts',(0.98307063199569,2.24615381785958,12.2052279840899));
#10311=CARTESIAN_POINT('Ctrl Pts',(1.05683565332237,2.2108931796599,12.2009867332216));
#10312=CARTESIAN_POINT('Ctrl Pts',(1.13017888436362,2.17583416269456,12.1967697339346));
#10313=CARTESIAN_POINT('Ctrl Pts',(1.20183025301668,2.13709556008851,12.1925527346477));
#10314=CARTESIAN_POINT('Ctrl Pts',(1.2714022780472,2.09487147514505,12.1883357353607));
#10315=CARTESIAN_POINT('Ctrl Pts',(1.34095123842937,2.0526613884095,12.1841201341013));
#10316=CARTESIAN_POINT('Ctrl Pts',(1.40842182686337,2.00696835508838,12.1799045328419));
#10317=CARTESIAN_POINT('Ctrl Pts',(1.47345241214861,1.95803172577296,12.1756889315824));
#10318=CARTESIAN_POINT('Ctrl Pts',(1.53848137475285,1.90909631755279,12.1714734355131));
#10319=CARTESIAN_POINT('Ctrl Pts',(1.60107008431499,1.8569177547608,12.1672579394439));
#10320=CARTESIAN_POINT('Ctrl Pts',(1.66088825234819,1.80177702927187,12.1630424433746));
#10321=CARTESIAN_POINT('Ctrl Pts',(1.72134027355505,1.74605201434383,12.158782278509));
#10322=CARTESIAN_POINT('Ctrl Pts',(1.77896232133806,1.68730200332968,12.1545221136434));
#10323=CARTESIAN_POINT('Ctrl Pts',(1.83345145153556,1.62585547477694,12.1502619487778));
#10324=CARTESIAN_POINT('Ctrl Pts',(1.88744777224751,1.56496467967076,12.1460403136088));
#10325=CARTESIAN_POINT('Ctrl Pts',(1.93836737087246,1.50142635194799,12.1418186784399));
#10326=CARTESIAN_POINT('Ctrl Pts',(1.98595700024202,1.43559222733676,12.1375970432709));
#10327=CARTESIAN_POINT('Ctrl Pts',(2.0341981356899,1.36885682795383,12.133317613557));
#10328=CARTESIAN_POINT('Ctrl Pts',(2.07901716722194,1.29976271141695,12.1290381838431));
#10329=CARTESIAN_POINT('Ctrl Pts',(2.1201976109185,1.22870352024216,12.1247587541292));
#10330=CARTESIAN_POINT('Ctrl Pts',(2.16137805461507,1.15764432906738,12.1204793244153));
#10331=CARTESIAN_POINT('Ctrl Pts',(2.19891974441531,1.08462052950482,12.1161998947014));
#10332=CARTESIAN_POINT('Ctrl Pts',(2.23265681392604,1.01004643518486,12.1119204649876));
#10333=CARTESIAN_POINT('Ctrl Pts',(2.26600973592268,0.936321479612382,12.1076897630473));
#10334=CARTESIAN_POINT('Ctrl Pts',(2.29576972894466,0.860804072338048,12.103459061107));
#10335=CARTESIAN_POINT('Ctrl Pts',(2.32174166943275,0.783878734511687,12.0992283591668));
#10336=CARTESIAN_POINT('Ctrl Pts',(2.3476762953887,0.707063917229259,12.0950037355811));
#10337=CARTESIAN_POINT('Ctrl Pts',(2.36983353019139,0.628845623690227,12.0907791119954));
#10338=CARTESIAN_POINT('Ctrl Pts',(2.38806556893495,0.549629955940727,12.0865544884097));
#10339=CARTESIAN_POINT('Ctrl Pts',(2.40636936537588,0.470102510995376,12.0823132375414));
#10340=CARTESIAN_POINT('Ctrl Pts',(2.42071680629526,0.389570256432995,12.0780719866732));
#10341=CARTESIAN_POINT('Ctrl Pts',(2.43100841586246,0.308461232581811,12.0738307358049));
#10342=CARTESIAN_POINT('Ctrl Pts',(2.44124117774198,0.227815992210994,12.0696137365179));
#10343=CARTESIAN_POINT('Ctrl Pts',(2.44746430597294,0.14660102661504,12.0653967372309));
#10344=CARTESIAN_POINT('Ctrl Pts',(2.44963120743725,0.0652472033846067,
12.061179737944));
#10345=CARTESIAN_POINT('Ctrl Pts',(2.45179739052633,-0.0160796492736131,
12.0569641366846));
#10346=CARTESIAN_POINT('Ctrl Pts',(2.44991000487722,-0.0975448036227609,
12.0527485354251));
#10347=CARTESIAN_POINT('Ctrl Pts',(2.44397449488414,-0.178714628264822,
12.0485329341657));
#10348=CARTESIAN_POINT('Ctrl Pts',(2.43803913299736,-0.259882427510101,
12.0443174380964));
#10349=CARTESIAN_POINT('Ctrl Pts',(2.42805588260066,-0.34075444795722,12.0401019420271));
#10350=CARTESIAN_POINT('Ctrl Pts',(2.41408216762724,-0.420900864746285,
12.0358864459578));
#10351=CARTESIAN_POINT('Ctrl Pts',(2.39996038252938,-0.501896539583761,
12.0316262810922));
#10352=CARTESIAN_POINT('Ctrl Pts',(2.38176312807819,-0.582150661691685,
12.0273661162266));
#10353=CARTESIAN_POINT('Ctrl Pts',(2.3596025575257,-0.661230686310136,12.023105951361));
#10354=CARTESIAN_POINT('Ctrl Pts',(2.33764241115569,-0.739595496974737,
12.0188843161921));
#10355=CARTESIAN_POINT('Ctrl Pts',(2.31179055803468,-0.816806935920933,
12.0146626810231));
#10356=CARTESIAN_POINT('Ctrl Pts',(2.28220561160518,-0.892461649796697,
12.0104410458541));
#10357=CARTESIAN_POINT('Ctrl Pts',(2.25221564473989,-0.969152083147433,
12.0061616161402));
#10358=CARTESIAN_POINT('Ctrl Pts',(2.21838980108288,-1.04424239429594,12.0018821864263));
#10359=CARTESIAN_POINT('Ctrl Pts',(2.18094183158227,-1.11733745003672,11.9976027567124));
#10360=CARTESIAN_POINT('Ctrl Pts',(2.14349386208166,-1.1904325057775,11.9933233269985));
#10361=CARTESIAN_POINT('Ctrl Pts',(2.10242406883344,-1.26153191406031,11.9890438972846));
#10362=CARTESIAN_POINT('Ctrl Pts',(2.05799098710902,-1.33027190715959,11.9847644675708));
#10363=CARTESIAN_POINT('Ctrl Pts',(2.01406384315971,-1.39822919156933,11.9805337656305));
#10364=CARTESIAN_POINT('Ctrl Pts',(1.96668442764706,-1.46413614849952,11.9763030636902));
#10365=CARTESIAN_POINT('Ctrl Pts',(1.91607038741404,-1.52762054204406,11.97207236175));
#10366=CARTESIAN_POINT('Ctrl Pts',(1.86552906563004,-1.59101372598326,11.9678477381643));
#10367=CARTESIAN_POINT('Ctrl Pts',(1.81176263630584,-1.65199089856448,11.9636231145786));
#10368=CARTESIAN_POINT('Ctrl Pts',(1.75503250946484,-1.71020792324253,11.9593984909929));
#10369=CARTESIAN_POINT('Ctrl Pts',(1.69807910406844,-1.7686540786117,11.9551572401246));
#10370=CARTESIAN_POINT('Ctrl Pts',(1.63813887967917,-1.82431791414245,11.9509159892564));
#10371=CARTESIAN_POINT('Ctrl Pts',(1.57551785703001,-1.87688404867738,11.9466747383881));
#10372=CARTESIAN_POINT('Ctrl Pts',(1.51325490299575,-1.92914960870573,11.9424577391011));
#10373=CARTESIAN_POINT('Ctrl Pts',(1.44834208503512,-1.9783524950656,11.9382407398142));
#10374=CARTESIAN_POINT('Ctrl Pts',(1.38111643225032,-2.02422025742461,11.9340237405272));
#10375=CARTESIAN_POINT('Ctrl Pts',(1.31391306624008,-2.07007281361697,11.9298081392678));
#10376=CARTESIAN_POINT('Ctrl Pts',(1.24439877190748,-2.11259217957145,11.9255925380083));
#10377=CARTESIAN_POINT('Ctrl Pts',(1.17294107577213,-2.15154815952758,11.9213769367489));
#10378=CARTESIAN_POINT('Ctrl Pts',(1.10148516269089,-2.19050316743138,11.9171614406796));
#10379=CARTESIAN_POINT('Ctrl Pts',(1.02808635306695,-2.22589474447284,11.9129459446103));
#10380=CARTESIAN_POINT('Ctrl Pts',(0.953137115382562,-2.25753845798476,
11.908730448541));
#10381=CARTESIAN_POINT('Ctrl Pts',(0.87739369068565,-2.28951747879367,11.9044702836754));
#10382=CARTESIAN_POINT('Ctrl Pts',(0.800067224637078,-2.31766853265137,
11.9002101188099));
#10383=CARTESIAN_POINT('Ctrl Pts',(0.721582103597065,-2.34185172839111,
11.8959499539443));
#10384=CARTESIAN_POINT('Ctrl Pts',(0.643806816095898,-2.36581620696274,
11.8917283187753));
#10385=CARTESIAN_POINT('Ctrl Pts',(0.564894218405914,-2.38588425469436,
11.8875066836064));
#10386=CARTESIAN_POINT('Ctrl Pts',(0.485269308089031,-2.40197084674789,
11.8832850484374));
#10387=CARTESIAN_POINT('Ctrl Pts',(0.404554325970041,-2.41827766561638,
11.8790056187235));
#10388=CARTESIAN_POINT('Ctrl Pts',(0.323107869493765,-2.4304931170988,11.8747261890096));
#10389=CARTESIAN_POINT('Ctrl Pts',(0.241377877170814,-2.43858298411444,
11.8704467592957));
#10390=CARTESIAN_POINT('Ctrl Pts',(0.159647884847869,-2.44667285113009,
11.8661673295818));
#10391=CARTESIAN_POINT('Ctrl Pts',(0.0776348498557966,-2.45063717540779,
11.861887899868));
#10392=CARTESIAN_POINT('Ctrl Pts',(-0.00421541329485567,-2.45049637426599,
11.8576084701541));
#10393=CARTESIAN_POINT('Ctrl Pts',(-0.0851336875214292,-2.45035717635794,
11.8533777682138));
#10394=CARTESIAN_POINT('Ctrl Pts',(-0.166197234216478,-2.44620538357498,
11.8491470662736));
#10395=CARTESIAN_POINT('Ctrl Pts',(-0.246975256662488,-2.43802245120846,
11.8449163643333));
#10396=CARTESIAN_POINT('Ctrl Pts',(-0.327637223317059,-2.42985127546414,
11.8406917407476));
#10397=CARTESIAN_POINT('Ctrl Pts',(-0.408014021675053,-2.41766050912247,
11.836467117162));
#10398=CARTESIAN_POINT('Ctrl Pts',(-0.487674785863702,-2.40148361502484,
11.8322424935763));
#10399=CARTESIAN_POINT('Ctrl Pts',(-0.567649079059602,-2.38524305187259,
11.828001242708));
#10400=CARTESIAN_POINT('Ctrl Pts',(-0.646901215105861,-2.36498491726102,
11.8237599918397));
#10401=CARTESIAN_POINT('Ctrl Pts',(-0.725000351671659,-2.34079574932884,
11.8195187409714));
#10402=CARTESIAN_POINT('Ctrl Pts',(-0.802652915369833,-2.31674489567981,
11.8153017416845));
#10403=CARTESIAN_POINT('Ctrl Pts',(-0.879165180861883,-2.28880798119376,
11.8110847423975));
#10404=CARTESIAN_POINT('Ctrl Pts',(-0.954125611932698,-2.25712085778632,
11.8068677431105));
#10405=CARTESIAN_POINT('Ctrl Pts',(-1.02906119198066,-2.22544423935353,
11.8026521418511));
#10406=CARTESIAN_POINT('Ctrl Pts',(-1.1024455312305,-2.19002006186729,11.7984365405917));
#10407=CARTESIAN_POINT('Ctrl Pts',(-1.17388610765322,-2.15103269530214,
11.7942209393323));
#10408=CARTESIAN_POINT('Ctrl Pts',(-1.24532490144898,-2.11204630157251,
11.790005443263));
#10409=CARTESIAN_POINT('Ctrl Pts',(-1.31481962114412,-2.06949711927528,
11.7857899471937));
#10410=CARTESIAN_POINT('Ctrl Pts',(-1.38200271650055,-2.02361526520856,
11.7815744511244));
#10411=CARTESIAN_POINT('Ctrl Pts',(-1.44989770624654,-1.97724723177901,
11.7773142862588));
#10412=CARTESIAN_POINT('Ctrl Pts',(-1.51543138132163,-1.92747573776857,
11.7730541213932));
#10413=CARTESIAN_POINT('Ctrl Pts',(-1.57825635937206,-1.87458185046736,
11.7687939565276));
#10414=CARTESIAN_POINT('Ctrl Pts',(-1.64051313703101,-1.82216634498823,
11.7645723213587));
#10415=CARTESIAN_POINT('Ctrl Pts',(-1.7001097143576,-1.76668506359617,11.7603506861897));
#10416=CARTESIAN_POINT('Ctrl Pts',(-1.75674450736484,-1.70844929273405,
11.7561290510207));
#10417=CARTESIAN_POINT('Ctrl Pts',(-1.81415463551072,-1.64941626921013,
11.7518496213068));
#10418=CARTESIAN_POINT('Ctrl Pts',(-1.86852094462973,-1.5875531383464,11.7475701915929));
#10419=CARTESIAN_POINT('Ctrl Pts',(-1.91957214723769,-1.52321798228266,
11.743290761879));
#10420=CARTESIAN_POINT('Ctrl Pts',(-1.97062334984566,-1.45888282621893,
11.7390113321651));
#10421=CARTESIAN_POINT('Ctrl Pts',(-2.01835921401425,-1.39207608219041,
11.7347319024512));
#10422=CARTESIAN_POINT('Ctrl Pts',(-2.06255553650021,-1.3231836262788,11.7304524727373));
#10423=CARTESIAN_POINT('Ctrl Pts',(-2.10727116745882,-1.25348168138612,
11.7261227595613));
#10424=CARTESIAN_POINT('Ctrl Pts',(-2.14852584144248,-1.18139238103366,
11.7217930463853));
#10425=CARTESIAN_POINT('Ctrl Pts',(-2.18606292576863,-1.1072845770532,11.7174633332092));
#10426=CARTESIAN_POINT('Ctrl Pts',(-2.22353816353652,-1.03329887399503,
11.7131407537215));
#10427=CARTESIAN_POINT('Ctrl Pts',(-2.25730779196089,-0.957301663986588,
11.7088181742337));
#10428=CARTESIAN_POINT('Ctrl Pts',(-2.28715895920277,-0.879689800633441,
11.7044955947459));
#10429=CARTESIAN_POINT('Ctrl Pts',(-2.31695826440011,-0.802212776560814,
11.7001805251089));
#10430=CARTESIAN_POINT('Ctrl Pts',(-2.34285250298379,-0.723127087239894,
11.6958654554718));
#10431=CARTESIAN_POINT('Ctrl Pts',(-2.36467584532787,-0.642851768701699,
11.6915503858348));
#10432=CARTESIAN_POINT('Ctrl Pts',(-2.38647684186266,-0.562658647332512,
11.6872397345734));
#10433=CARTESIAN_POINT('Ctrl Pts',(-2.40421511332889,-0.481278736727669,
11.6829290833119));
#10434=CARTESIAN_POINT('Ctrl Pts',(-2.41777398446152,-0.39914810542084,
11.6786184320505));
#10435=CARTESIAN_POINT('Ctrl Pts',(-2.43132082051032,-0.317090374654447,
11.6743116069961));
#10436=CARTESIAN_POINT('Ctrl Pts',(-2.44069556608535,-0.234283678081487,
11.6700047819418));
#10437=CARTESIAN_POINT('Ctrl Pts',(-2.44583244848948,-0.151175010884661,
11.6656979568875));
#10438=CARTESIAN_POINT('Ctrl Pts',(-2.44896156181122,-0.100549667102359,
11.6630744699957));
#10439=CARTESIAN_POINT('Ctrl Pts',(-2.45051917085277,-0.0498124829440769,
11.6604509831039));
#10440=CARTESIAN_POINT('Ctrl Pts',(-2.45049982187577,0.000934337641984426,
11.6578274962121));
#10441=CARTESIAN_POINT('',(-2.4527937259461,0.00178251817473156,10.8578274962121));
#10442=CARTESIAN_POINT('Ctrl Pts',(-2.44679607104562,0.000946051269979937,
11.6578268166126));
#10443=CARTESIAN_POINT('Ctrl Pts',(-2.44799340688633,0.35201353471065,11.6396500361819));
#10444=CARTESIAN_POINT('Ctrl Pts',(-2.21301218228035,1.52018188066365,11.5790879232791));
#10445=CARTESIAN_POINT('Ctrl Pts',(-0.415304589651594,2.8675334673887,11.4761404779038));
#10446=CARTESIAN_POINT('Ctrl Pts',(2.18604951050344,1.90168704744197,11.348984480487));
#10447=CARTESIAN_POINT('Ctrl Pts',(2.7824107934927,-0.808341675923911,11.2218284830704));
#10448=CARTESIAN_POINT('Ctrl Pts',(0.826810820091264,-2.77697856609673,
11.0946724856537));
#10449=CARTESIAN_POINT('Ctrl Pts',(-1.76285248037032,-2.22511816526007,
10.9733388233675));
#10450=CARTESIAN_POINT('Ctrl Pts',(-2.44705219281867,-0.700008467339178,
10.8943904935537));
#10451=CARTESIAN_POINT('Ctrl Pts',(-2.4527937259461,0.00178251817473156,
10.8578274962121));
#10452=CARTESIAN_POINT('',(-2.45241901939193,-0.00192082103873892,10.0578274962121));
#10453=CARTESIAN_POINT('Ctrl Pts',(-2.4527937259461,0.00178251817473156,
10.8578274962121));
#10454=CARTESIAN_POINT('Ctrl Pts',(-2.45370801450179,0.113536548380269,
10.8520051610814));
#10455=CARTESIAN_POINT('Ctrl Pts',(-2.39595452555011,1.03788523585881,10.8037974934788));
#10456=CARTESIAN_POINT('Ctrl Pts',(-1.22083211557998,2.62769766798767,10.7132044934033));
#10457=CARTESIAN_POINT('Ctrl Pts',(1.54828361268476,2.44909043186913,10.5860484959867));
#10458=CARTESIAN_POINT('Ctrl Pts',(2.89735029473491,0.0242354777121154,
10.4588924985699));
#10459=CARTESIAN_POINT('Ctrl Pts',(1.58903593310591,-2.42284768239323,10.3317365011533));
#10460=CARTESIAN_POINT('Ctrl Pts',(-1.17670453748705,-2.64775235251303,
10.2045805037364));
#10461=CARTESIAN_POINT('Ctrl Pts',(-2.3876741667315,-1.06551612567497,10.1132775020894));
#10462=CARTESIAN_POINT('Ctrl Pts',(-2.45349901262548,-0.127352508512948,
10.0643598329146));
#10463=CARTESIAN_POINT('Ctrl Pts',(-2.45241901939193,-0.00192082103873892,
10.0578274962121));
#10464=CARTESIAN_POINT('',(-2.4466576276378,-0.000722135771627219,9.25782749621205));
#10465=CARTESIAN_POINT('Ctrl Pts',(-2.45241901939193,-0.00192082103873892,
10.0578274962121));
#10466=CARTESIAN_POINT('Ctrl Pts',(-2.44649143258849,0.686516099035135,
10.0219745004424));
#10467=CARTESIAN_POINT('Ctrl Pts',(-1.78473046489226,2.19879973224981,9.94373617220041));
#10468=CARTESIAN_POINT('Ctrl Pts',(0.780241169782797,2.79042108036697,9.8231125114863));
#10469=CARTESIAN_POINT('Ctrl Pts',(2.76849932813169,0.854773396237229,9.6959565140695));
#10470=CARTESIAN_POINT('Ctrl Pts',(2.21755549651571,-1.86485219485422,9.56880051665281));
#10471=CARTESIAN_POINT('Ctrl Pts',(-0.367277696167932,-2.87407953659603,
9.44164451923604));
#10472=CARTESIAN_POINT('Ctrl Pts',(-2.19982859173748,-1.5479024331872,9.33798684575582));
#10473=CARTESIAN_POINT('Ctrl Pts',(-2.44761899138352,-0.36555854426161,
9.27671450474781));
#10474=CARTESIAN_POINT('Ctrl Pts',(-2.4466576276378,-0.000722135771627219,
9.25782749621205));
#10475=CARTESIAN_POINT('',(-2.45049898092435,0.0022348352783145,8.45782747312582));
#10476=CARTESIAN_POINT('Ctrl Pts',(-2.4466576276378,-0.000722135771627219,
9.25782749621205));
#10477=CARTESIAN_POINT('Ctrl Pts',(-2.44546154427314,0.453190091476666,
9.23432917227556));
#10478=CARTESIAN_POINT('Ctrl Pts',(-2.10644496581795,1.72751135573376,9.16844551586685));
#10479=CARTESIAN_POINT('Ctrl Pts',(-0.0534527617077329,2.89695855874034,
9.06017652698584));
#10480=CARTESIAN_POINT('Ctrl Pts',(2.40669974372965,1.61338849391436,8.93302052956913));
#10481=CARTESIAN_POINT('Ctrl Pts',(2.65948426593449,-1.14994327165152,8.80586453215237));
#10482=CARTESIAN_POINT('Ctrl Pts',(0.473052830333179,-2.85857431398534,
8.67870853473567));
#10483=CARTESIAN_POINT('Ctrl Pts',(-1.91761415784133,-2.0254181576049,8.56269618942219));
#10484=CARTESIAN_POINT('Ctrl Pts',(-2.4444075610822,-0.599329353249913,
8.48906917658101));
#10485=CARTESIAN_POINT('Ctrl Pts',(-2.44976479135255,0.00223372117810497,
8.45782749621206));
#10486=CARTESIAN_POINT('',(-2.4504999619844,-0.000431641586564807,7.65782749616008));
#10487=CARTESIAN_POINT('Ctrl Pts',(-2.45049898092435,0.0022348352783145,
8.45782747312582));
#10488=CARTESIAN_POINT('Ctrl Pts',(-2.45040110829094,0.109552269706613,
8.45225565092188));
#10489=CARTESIAN_POINT('Ctrl Pts',(-2.44324902256183,0.216554534016528,
8.44668382871794));
#10490=CARTESIAN_POINT('Ctrl Pts',(-2.42919252957169,0.322449847686588,
8.441112006514));
#10491=CARTESIAN_POINT('Ctrl Pts',(-2.41513603658154,0.428345161356646,
8.43554018431006));
#10492=CARTESIAN_POINT('Ctrl Pts',(-2.39417533386648,0.53313388035792,8.42996836210611));
#10493=CARTESIAN_POINT('Ctrl Pts',(-2.36651425439525,0.636050732052167,
8.42439653990217));
#10494=CARTESIAN_POINT('Ctrl Pts',(-2.34551111066831,0.714195817832587,
8.42016583796257));
#10495=CARTESIAN_POINT('Ctrl Pts',(-2.32059364397539,0.791446421958971,
8.41593513602298));
#10496=CARTESIAN_POINT('Ctrl Pts',(-2.29185503851226,0.867381537990035,
8.41170443408338));
#10497=CARTESIAN_POINT('Ctrl Pts',(-2.26315772251752,0.943207556153543,
8.40747981049835));
#10498=CARTESIAN_POINT('Ctrl Pts',(-2.23065033426224,1.01772140859261,8.40325518691333));
#10499=CARTESIAN_POINT('Ctrl Pts',(-2.19447632402472,1.09051543468901,8.3990305633283));
#10500=CARTESIAN_POINT('Ctrl Pts',(-2.15815994003272,1.16359596368433,8.39478931245985));
#10501=CARTESIAN_POINT('Ctrl Pts',(-2.11814813312979,1.23494264121746,8.39054806159139));
#10502=CARTESIAN_POINT('Ctrl Pts',(-2.0746356273981,1.30416151742431,8.38630681072294));
#10503=CARTESIAN_POINT('Ctrl Pts',(-2.03137192729937,1.37298459830708,8.38208981143663));
#10504=CARTESIAN_POINT('Ctrl Pts',(-1.98464770390307,1.43970374779213,8.37787281215031));
#10505=CARTESIAN_POINT('Ctrl Pts',(-1.93470034788306,1.50395638696777,8.373655812864));
#10506=CARTESIAN_POINT('Ctrl Pts',(-1.8847695505042,1.56818772498797,8.3694402116052));
#10507=CARTESIAN_POINT('Ctrl Pts',(-1.83161802763612,1.62995380963631,8.3652246103464));
#10508=CARTESIAN_POINT('Ctrl Pts',(-1.77552514303193,1.68892294568504,8.3610090090876));
#10509=CARTESIAN_POINT('Ctrl Pts',(-1.71943365809002,1.7478906103016,8.35679351301894));
#10510=CARTESIAN_POINT('Ctrl Pts',(-1.66040127865167,1.80406112886576,8.35257801695027));
#10511=CARTESIAN_POINT('Ctrl Pts',(-1.59874512760487,1.85713873120984,8.3483625208816));
#10512=CARTESIAN_POINT('Ctrl Pts',(-1.53643564748553,1.91077876147268,8.34410235601526));
#10513=CARTESIAN_POINT('Ctrl Pts',(-1.47144681660976,1.96125960981008,8.33984219114891));
#10514=CARTESIAN_POINT('Ctrl Pts',(-1.40413978355796,2.00831813172858,8.33558202628256));
#10515=CARTESIAN_POINT('Ctrl Pts',(-1.3374414874301,2.05495104790311,8.33136039111421));
#10516=CARTESIAN_POINT('Ctrl Pts',(-1.26846718406647,2.09822309531934,8.32713875594585));
#10517=CARTESIAN_POINT('Ctrl Pts',(-1.19759540764804,2.13792317204813,8.3229171207775));
#10518=CARTESIAN_POINT('Ctrl Pts',(-1.12575339054113,2.17816674622717,8.31863769106215));
#10519=CARTESIAN_POINT('Ctrl Pts',(-1.05196199707661,2.21473958837252,8.31435826134681));
#10520=CARTESIAN_POINT('Ctrl Pts',(-0.976637160731033,2.2474719367056,8.31007883163147));
#10521=CARTESIAN_POINT('Ctrl Pts',(-0.901312324385457,2.28020428503868,
8.30579940191612));
#10522=CARTESIAN_POINT('Ctrl Pts',(-0.824454527417156,2.30909602823884,
8.30151997220078));
#10523=CARTESIAN_POINT('Ctrl Pts',(-0.746494414108079,2.33403006401062,
8.29724054248544));
#10524=CARTESIAN_POINT('Ctrl Pts',(-0.669421994530714,2.35868018809576,
8.29300984054604));
#10525=CARTESIAN_POINT('Ctrl Pts',(-0.590982356308454,2.37955503273652,
8.28877913860664));
#10526=CARTESIAN_POINT('Ctrl Pts',(-0.511579914801459,2.39650500537172,
8.28454843666723));
#10527=CARTESIAN_POINT('Ctrl Pts',(-0.43229155275501,2.4134306255601,8.28032381308242));
#10528=CARTESIAN_POINT('Ctrl Pts',(-0.352043585654955,2.42644247676516,
8.27609918949761));
#10529=CARTESIAN_POINT('Ctrl Pts',(-0.271256422912863,2.43544045359941,
8.2718745659128));
#10530=CARTESIAN_POINT('Ctrl Pts',(-0.190151297860828,2.44447384469259,
8.26763331504429));
#10531=CARTESIAN_POINT('Ctrl Pts',(-0.108503175727459,2.44946155345117,
8.26339206417579));
#10532=CARTESIAN_POINT('Ctrl Pts',(-0.0267486987495833,2.4503540064887,
8.25915081330729));
#10533=CARTESIAN_POINT('Ctrl Pts',(0.0545383040092322,2.45124135645662,
8.25493381402122));
#10534=CARTESIAN_POINT('Ctrl Pts',(0.13592997892602,2.44808015204624,8.25071681473515));
#10535=CARTESIAN_POINT('Ctrl Pts',(0.216992958930068,2.44087367673437,8.24649981544908));
#10536=CARTESIAN_POINT('Ctrl Pts',(0.298029064782754,2.43366959052674,8.24228421419053));
#10537=CARTESIAN_POINT('Ctrl Pts',(0.378736229251284,2.42242293775493,8.23806861293197));
#10538=CARTESIAN_POINT('Ctrl Pts',(0.45868432623219,2.40718901187026,8.23385301167342));
#10539=CARTESIAN_POINT('Ctrl Pts',(0.538630428301518,2.3919554661114,8.22963751560502));
#10540=CARTESIAN_POINT('Ctrl Pts',(0.617817043904243,2.37273493317166,8.22542201953661));
#10541=CARTESIAN_POINT('Ctrl Pts',(0.695823807958463,2.34963390303217,8.22120652346821));
#10542=CARTESIAN_POINT('Ctrl Pts',(0.774657157626014,2.32628808669499,8.21694635860158));
#10543=CARTESIAN_POINT('Ctrl Pts',(0.852285033563614,2.29897916753237,8.21268619373496));
#10544=CARTESIAN_POINT('Ctrl Pts',(0.928290664938836,2.26786831438411,8.20842602886833));
#10545=CARTESIAN_POINT('Ctrl Pts',(1.00360888769098,2.23703883339655,8.20420439370026));
#10546=CARTESIAN_POINT('Ctrl Pts',(1.07733369203115,2.20247616804331,8.19998275853218));
#10547=CARTESIAN_POINT('Ctrl Pts',(1.14908264953447,2.16438428069944,8.19576112336411));
#10548=CARTESIAN_POINT('Ctrl Pts',(1.22181385642477,2.12577091214812,8.19148169364821));
#10549=CARTESIAN_POINT('Ctrl Pts',(1.29251428319559,2.0835312129496,8.18720226393231));
#10550=CARTESIAN_POINT('Ctrl Pts',(1.3608160100427,2.03792297126546,8.18292283421641));
#10551=CARTESIAN_POINT('Ctrl Pts',(1.42911773688982,1.99231472958133,8.17864340450051));
#10552=CARTESIAN_POINT('Ctrl Pts',(1.49502040911919,1.94333829060359,8.17436397478461));
#10553=CARTESIAN_POINT('Ctrl Pts',(1.55819241617889,1.89129232118215,8.17008454506871));
#10554=CARTESIAN_POINT('Ctrl Pts',(1.62064511451561,1.8398389737391,8.16585384312429));
#10555=CARTESIAN_POINT('Ctrl Pts',(1.68066394662119,1.78519214591384,8.16162314117987));
#10556=CARTESIAN_POINT('Ctrl Pts',(1.73790418615722,1.72761086177912,8.15739243923545));
#10557=CARTESIAN_POINT('Ctrl Pts',(1.79506218721933,1.67011230610558,8.1531678156456));
#10558=CARTESIAN_POINT('Ctrl Pts',(1.84944919910114,1.60968799436721,8.14894319205576));
#10559=CARTESIAN_POINT('Ctrl Pts',(1.900753442809,1.54663719069785,8.14471856846591));
#10560=CARTESIAN_POINT('Ctrl Pts',(1.9522596098063,1.48333823161757,8.14047731759866));
#10561=CARTESIAN_POINT('Ctrl Pts',(2.00065832399826,1.41739236331705,8.13623606673141));
#10562=CARTESIAN_POINT('Ctrl Pts',(2.0456715029086,1.34913985642248,8.13199481586416));
#10563=CARTESIAN_POINT('Ctrl Pts',(2.09042729536166,1.28127761903066,8.12777781657305));
#10564=CARTESIAN_POINT('Ctrl Pts',(2.13183590600191,1.2111354424295,8.12356081728193));
#10565=CARTESIAN_POINT('Ctrl Pts',(2.169665465371,1.13907946095803,8.11934381799081));
#10566=CARTESIAN_POINT('Ctrl Pts',(2.20748248341347,1.06704736762096,8.11512821672722));
#10567=CARTESIAN_POINT('Ctrl Pts',(2.24172259043421,0.993103140796551,8.11091261546363));
#10568=CARTESIAN_POINT('Ctrl Pts',(2.27219939945024,0.917638348772516,8.10669701420004));
#10569=CARTESIAN_POINT('Ctrl Pts',(2.30267544799107,0.842175439790226,8.10248151812661));
#10570=CARTESIAN_POINT('Ctrl Pts',(2.32938821208652,0.765192472675022,8.09826602205318));
#10571=CARTESIAN_POINT('Ctrl Pts',(2.35219963335394,0.687100527470042,8.09405052597975));
#10572=CARTESIAN_POINT('Ctrl Pts',(2.37525277196729,0.608181094248742,8.0897903611191));
#10573=CARTESIAN_POINT('Ctrl Pts',(2.39432124431933,0.528129501321001,8.08553019625845));
#10574=CARTESIAN_POINT('Ctrl Pts',(2.40931490965907,0.447383410616135,8.0812700313978));
#10575=CARTESIAN_POINT('Ctrl Pts',(2.42417296962649,0.36736760189666,8.07704839622479));
#10576=CARTESIAN_POINT('Ctrl Pts',(2.43502963114029,0.286670281452381,8.07282676105177));
#10577=CARTESIAN_POINT('Ctrl Pts',(2.44184932582168,0.20572340650544,8.06860512587876));
#10578=CARTESIAN_POINT('Ctrl Pts',(2.44876238268208,0.123668362207468,8.06432569617429));
#10579=CARTESIAN_POINT('Ctrl Pts',(2.4515270863782,0.0413573732023643,8.06004626646982));
#10580=CARTESIAN_POINT('Ctrl Pts',(2.450160978105,-0.0407606596062904,8.05576683676536));
#10581=CARTESIAN_POINT('Ctrl Pts',(2.44879486983181,-0.122878692414948,
8.05148740706089));
#10582=CARTESIAN_POINT('Ctrl Pts',(2.4432980477765,-0.204803283924434,8.04720797735643));
#10583=CARTESIAN_POINT('Ctrl Pts',(2.43374208045734,-0.286093928301824,
8.04292854765196));
#10584=CARTESIAN_POINT('Ctrl Pts',(2.4242949222569,-0.366458955933194,8.03869784571719));
#10585=CARTESIAN_POINT('Ctrl Pts',(2.41084509740716,-0.446506680336389,
8.03446714378243));
#10586=CARTESIAN_POINT('Ctrl Pts',(2.39342374342146,-0.525807031549031,
8.03023644184766));
#10587=CARTESIAN_POINT('Ctrl Pts',(2.37602741912779,-0.604993449977247,
8.02601181826745));
#10588=CARTESIAN_POINT('Ctrl Pts',(2.35467099705926,-0.683434177406085,
8.02178719468725));
#10589=CARTESIAN_POINT('Ctrl Pts',(2.32943728494609,-0.760705058155243,
8.01756257110704));
#10590=CARTESIAN_POINT('Ctrl Pts',(2.30410425789343,-0.83828006192888,8.01332132023738));
#10591=CARTESIAN_POINT('Ctrl Pts',(2.27486341023255,-0.914675519388884,
8.00908006936772));
#10592=CARTESIAN_POINT('Ctrl Pts',(2.24185026990555,-0.989473404051081,
8.00483881849806));
#10593=CARTESIAN_POINT('Ctrl Pts',(2.20902589961493,-1.06384359236965,8.0006218192165));
#10594=CARTESIAN_POINT('Ctrl Pts',(2.17247244941037,-1.13663399850362,7.99640481993494));
#10595=CARTESIAN_POINT('Ctrl Pts',(2.1323722126194,-1.20745144699431,7.99218782065338));
#10596=CARTESIAN_POINT('Ctrl Pts',(2.09228526993381,-1.27824541795222,7.9879722193993));
#10597=CARTESIAN_POINT('Ctrl Pts',(2.04865410464592,-1.34706732579106,7.98375661814521));
#10598=CARTESIAN_POINT('Ctrl Pts',(2.00170701861795,-1.41354846454433,7.97954101689113));
#10599=CARTESIAN_POINT('Ctrl Pts',(1.95476110404048,-1.48002794442226,7.97532552082713));
#10600=CARTESIAN_POINT('Ctrl Pts',(1.90449970238417,-1.54416639208273,7.97111002476313));
#10601=CARTESIAN_POINT('Ctrl Pts',(1.85119368584312,-1.60562517029803,7.96689452869914));
#10602=CARTESIAN_POINT('Ctrl Pts',(1.79732282089945,-1.66773518630887,7.96263436382715));
#10603=CARTESIAN_POINT('Ctrl Pts',(1.74034273862831,-1.72710802884643,7.95837419895515));
#10604=CARTESIAN_POINT('Ctrl Pts',(1.68057260332271,-1.78343095603982,7.95411403408316));
#10605=CARTESIAN_POINT('Ctrl Pts',(1.62134304002295,-1.83924448840633,7.94989239891933));
#10606=CARTESIAN_POINT('Ctrl Pts',(1.55937408610003,-1.89206279345339,7.9456707637555));
#10607=CARTESIAN_POINT('Ctrl Pts',(1.49500965569569,-1.94162210004332,7.94144912859166));
#10608=CARTESIAN_POINT('Ctrl Pts',(1.42976407049358,-1.99185987796442,7.93716969886559));
#10609=CARTESIAN_POINT('Ctrl Pts',(1.36205733028268,-2.03874846821623,7.93289026913952));
#10610=CARTESIAN_POINT('Ctrl Pts',(1.29227634889301,-2.08205957842031,7.92861083941345));
#10611=CARTESIAN_POINT('Ctrl Pts',(1.22249536750335,-2.12537068862438,7.92433140968737));
#10612=CARTESIAN_POINT('Ctrl Pts',(1.15064060594843,-2.16510413869198,7.9200519799613));
#10613=CARTESIAN_POINT('Ctrl Pts',(1.07712117087272,-2.20108160531539,7.91577255023523));
#10614=CARTESIAN_POINT('Ctrl Pts',(1.00443886592732,-2.23664941398521,7.91154184829876));
#10615=CARTESIAN_POINT('Ctrl Pts',(0.929856244915385,-2.26868015883045,
7.90731114636229));
#10616=CARTESIAN_POINT('Ctrl Pts',(0.853751750611722,-2.2969671739769,7.90308044442583));
#10617=CARTESIAN_POINT('Ctrl Pts',(0.777756597526991,-2.32521354846546,
7.89885582084401));
#10618=CARTESIAN_POINT('Ctrl Pts',(0.700244345910027,-2.34972671501645,
7.89463119726219));
#10619=CARTESIAN_POINT('Ctrl Pts',(0.621616440926069,-2.37034665194153,
7.89040657368037));
#10620=CARTESIAN_POINT('Ctrl Pts',(0.542679071974386,-2.39104774488235,
7.88616532281112));
#10621=CARTESIAN_POINT('Ctrl Pts',(0.462617675088182,-2.40782468790328,
7.88192407194188));
#10622=CARTESIAN_POINT('Ctrl Pts',(0.381857085611667,-2.42056510265024,
7.87768282107263));
#10623=CARTESIAN_POINT('Ctrl Pts',(0.30155828735309,-2.43323266736377,7.87346582178968));
#10624=CARTESIAN_POINT('Ctrl Pts',(0.220568734807663,-2.44190966729512,
7.86924882250672));
#10625=CARTESIAN_POINT('Ctrl Pts',(0.139317688967278,-2.44653649707925,
7.86503182322376));
#10626=CARTESIAN_POINT('Ctrl Pts',(0.0580935796269779,-2.45116179296804,
7.86081622196837));
#10627=CARTESIAN_POINT('Ctrl Pts',(-0.0233913869148578,-2.45173955870471,
7.85660062071298));
#10628=CARTESIAN_POINT('Ctrl Pts',(-0.104703613010195,-2.44826211901884,
7.85238501945759));
#10629=CARTESIAN_POINT('Ctrl Pts',(-0.186013810154746,-2.4447847661041,
7.84816952339237));
#10630=CARTESIAN_POINT('Ctrl Pts',(-0.26715081083336,-2.43725242990822,
7.84395402732716));
#10631=CARTESIAN_POINT('Ctrl Pts',(-0.347683249834275,-2.42570950605893,
7.83973853126194));
#10632=CARTESIAN_POINT('Ctrl Pts',(-0.429069037471752,-2.41404426953105,
7.83547836639165));
#10633=CARTESIAN_POINT('Ctrl Pts',(-0.509836893015987,-2.3982829970036,
7.83121820152137));
#10634=CARTESIAN_POINT('Ctrl Pts',(-0.589551077057614,-2.37852470610255,
7.82695803665108));
#10635=CARTESIAN_POINT('Ctrl Pts',(-0.668544311529168,-2.35894511277586,
7.82273640148625));
#10636=CARTESIAN_POINT('Ctrl Pts',(-0.74650242463531,-2.33544070461839,
7.81851476632141));
#10637=CARTESIAN_POINT('Ctrl Pts',(-0.82301744961681,-2.30815782121289,
7.81429313115658));
#10638=CARTESIAN_POINT('Ctrl Pts',(-0.900579972046674,-2.28050143272446,
7.81001370143357));
#10639=CARTESIAN_POINT('Ctrl Pts',(-0.976659138228902,-2.24896251977144,
7.80573427171055));
#10640=CARTESIAN_POINT('Ctrl Pts',(-1.05085352989834,-2.21374278286801,
7.80145484198754));
#10641=CARTESIAN_POINT('Ctrl Pts',(-1.12504792156778,-2.17852304596457,
7.79717541226452));
#10642=CARTESIAN_POINT('Ctrl Pts',(-1.19735713771531,-2.13962277520911,
7.79289598254151));
#10643=CARTESIAN_POINT('Ctrl Pts',(-1.26740975649506,-2.09728938373824,
7.78861655281849));
#10644=CARTESIAN_POINT('Ctrl Pts',(-1.33666472066548,-2.05543802171072,
7.78438585085046));
#10645=CARTESIAN_POINT('Ctrl Pts',(-1.40397472540247,-2.01007394635283,
7.78015514888243));
#10646=CARTESIAN_POINT('Ctrl Pts',(-1.46896112141315,-1.9614034449283,7.7759244469144));
#10647=CARTESIAN_POINT('Ctrl Pts',(-1.53385414985612,-1.91280286962088,
7.77169982330086));
#10648=CARTESIAN_POINT('Ctrl Pts',(-1.59642983071125,-1.86090557926777,
7.76747519968733));
#10649=CARTESIAN_POINT('Ctrl Pts',(-1.65633627736967,-1.80596245428004,
7.7632505760738));
#10650=CARTESIAN_POINT('Ctrl Pts',(-1.71647850345477,-1.75080308447673,
7.75900932521246));
#10651=CARTESIAN_POINT('Ctrl Pts',(-1.77393003301355,-1.69257409850204,
7.75476807435113));
#10652=CARTESIAN_POINT('Ctrl Pts',(-1.8283663722182,-1.63157183689277,7.75052682348979));
#10653=CARTESIAN_POINT('Ctrl Pts',(-1.88249144348427,-1.5709183872811,7.74630982417498));
#10654=CARTESIAN_POINT('Ctrl Pts',(-1.93363539989396,-1.50752364172897,
7.74209282486016));
#10655=CARTESIAN_POINT('Ctrl Pts',(-1.98151572079982,-1.44171623359909,
7.73787582554535));
#10656=CARTESIAN_POINT('Ctrl Pts',(-2.02938016833126,-1.37593064206547,
7.73366022425811));
#10657=CARTESIAN_POINT('Ctrl Pts',(-2.07398285556615,-1.30773435207906,
7.72944462297087));
#10658=CARTESIAN_POINT('Ctrl Pts',(-2.11508257455789,-1.23748775864715,
7.72522902168364));
#10659=CARTESIAN_POINT('Ctrl Pts',(-2.15618126800456,-1.16724291805077,
7.72101352558664));
#10660=CARTESIAN_POINT('Ctrl Pts',(-2.19377693308089,-1.09494827768069,
7.71679802948964));
#10661=CARTESIAN_POINT('Ctrl Pts',(-2.22767334950713,-1.02099054740761,
7.71258253339264));
#10662=CARTESIAN_POINT('Ctrl Pts',(-2.26192894312803,-0.946249137534035,
7.70832236856007));
#10663=CARTESIAN_POINT('Ctrl Pts',(-2.29240620798047,-0.869809616343446,
7.70406220372749));
#10664=CARTESIAN_POINT('Ctrl Pts',(-2.3189524794052,-0.792091944322416,
7.69980203889492));
#10665=CARTESIAN_POINT('Ctrl Pts',(-2.34525866195388,-0.715077163800797,
7.69558040369877));
#10666=CARTESIAN_POINT('Ctrl Pts',(-2.36770459988362,-0.63680772809343,
7.69135876850262));
#10667=CARTESIAN_POINT('Ctrl Pts',(-2.3861924512603,-0.557705868310855,
7.68713713330648));
#10668=CARTESIAN_POINT('Ctrl Pts',(-2.4049334024995,-0.477521099031188,
7.68285770365569));
#10669=CARTESIAN_POINT('Ctrl Pts',(-2.41960698558152,-0.396481427966423,
7.6785782740049));
#10670=CARTESIAN_POINT('Ctrl Pts',(-2.43016544912669,-0.315033553563563,
7.67429884435412));
#10671=CARTESIAN_POINT('Ctrl Pts',(-2.44072391267186,-0.233585679160702,
7.67001941470333));
#10672=CARTESIAN_POINT('Ctrl Pts',(-2.44716728347148,-0.151730095633827,
7.66573998505254));
#10673=CARTESIAN_POINT('Ctrl Pts',(-2.44950248378859,-0.0699130310708557,
7.66146055540175));
#10674=CARTESIAN_POINT('Ctrl Pts',(-2.4501633133589,-0.0467599271495813,
7.66024953567185));
#10675=CARTESIAN_POINT('Ctrl Pts',(-2.45049588145717,-0.0235974094178985,
7.65903851594195));
#10676=CARTESIAN_POINT('Ctrl Pts',(-2.45049996198422,-0.000431642580974575,
7.65782749621206));
#10677=CARTESIAN_POINT('',(-2.45049918758584,-0.00199540500347388,6.85782752364025));
#10678=CARTESIAN_POINT('Ctrl Pts',(-2.4504999619844,-0.000431641586563175,
7.65782749616008));
#10679=CARTESIAN_POINT('Ctrl Pts',(-2.45051414927918,0.0801119538488336,
7.65361697794695));
#10680=CARTESIAN_POINT('Ctrl Pts',(-2.44655306968272,0.160813628717667,
7.64940645973383));
#10681=CARTESIAN_POINT('Ctrl Pts',(-2.43859602484009,0.241246093510585,
7.64519594152071));
#10682=CARTESIAN_POINT('Ctrl Pts',(-2.43065032934474,0.321563835313509,
7.64099142888307));
#10683=CARTESIAN_POINT('Ctrl Pts',(-2.41872003131059,0.401612665828241,
7.63678691624544));
#10684=CARTESIAN_POINT('Ctrl Pts',(-2.40283644221121,0.480964948807892,
7.6325824036078));
#10685=CARTESIAN_POINT('Ctrl Pts',(-2.38697086817172,0.560227230962065,
7.62838265970011));
#10686=CARTESIAN_POINT('Ctrl Pts',(-2.36716100364736,0.638794076830931,
7.62418291579242));
#10687=CARTESIAN_POINT('Ctrl Pts',(-2.34348982424815,0.716244157843789,
7.61998317188473));
#10688=CARTESIAN_POINT('Ctrl Pts',(-2.31983319025584,0.793646647525318,
7.61578600862513));
#10689=CARTESIAN_POINT('Ctrl Pts',(-2.29232008706215,0.869933285897969,
7.61158884536554));
#10690=CARTESIAN_POINT('Ctrl Pts',(-2.26108403110359,0.944695323524109,
7.60739168210594));
#10691=CARTESIAN_POINT('Ctrl Pts',(-2.22985735715928,1.01943490573837,7.60319577949991));
#10692=CARTESIAN_POINT('Ctrl Pts',(-2.19491013179145,1.0926503630723,7.59899987689388));
#10693=CARTESIAN_POINT('Ctrl Pts',(-2.15642442957764,1.16395185876424,7.59480397428786));
#10694=CARTESIAN_POINT('Ctrl Pts',(-2.11793819786441,1.2352543354465,7.59060801395317));
#10695=CARTESIAN_POINT('Ctrl Pts',(-2.07591361739344,1.30464238543468,7.58641205361848));
#10696=CARTESIAN_POINT('Ctrl Pts',(-2.03057852696413,1.37175110564278,7.58221609328379));
#10697=CARTESIAN_POINT('Ctrl Pts',(-1.98519789816097,1.43892723548788,7.57801591817401));
#10698=CARTESIAN_POINT('Ctrl Pts',(-1.93650038246883,1.50381907313217,7.57381574306422));
#10699=CARTESIAN_POINT('Ctrl Pts',(-1.8847565881472,1.56609158526432,7.56961556795444));
#10700=CARTESIAN_POINT('Ctrl Pts',(-1.83298640190095,1.62839585949408,7.56541325054514));
#10701=CARTESIAN_POINT('Ctrl Pts',(-1.77816716181604,1.68807780204755,7.56121093313585));
#10702=CARTESIAN_POINT('Ctrl Pts',(-1.72060740202897,1.74483822117786,7.55700861572656));
#10703=CARTESIAN_POINT('Ctrl Pts',(-1.6629463687098,1.80169850744017,7.55279890454897));
#10704=CARTESIAN_POINT('Ctrl Pts',(-1.60253553610739,1.85562669028403,7.54858919337138));
#10705=CARTESIAN_POINT('Ctrl Pts',(-1.53971740741712,1.90636317507885,7.5443794821938));
#10706=CARTESIAN_POINT('Ctrl Pts',(-1.48960408144351,1.94683833812953,7.5410211741242));
#10707=CARTESIAN_POINT('Ctrl Pts',(-1.43795943764779,1.98528303519585,7.53766286605461));
#10708=CARTESIAN_POINT('Ctrl Pts',(-1.38496956816147,2.02158589856247,7.53430455798502));
#10709=CARTESIAN_POINT('Ctrl Pts',(-1.31821442288576,2.06731922346882,7.53007385605578));
#10710=CARTESIAN_POINT('Ctrl Pts',(-1.24906605095274,2.10982850004496,7.52584315412654));
#10711=CARTESIAN_POINT('Ctrl Pts',(-1.17786891945196,2.14885435955745,7.52161245219729));
#10712=CARTESIAN_POINT('Ctrl Pts',(-1.10677407864698,2.18782414964356,7.5173878286231));
#10713=CARTESIAN_POINT('Ctrl Pts',(-1.03363672858851,2.2233202406584,7.51316320504892));
#10714=CARTESIAN_POINT('Ctrl Pts',(-0.958830860654071,2.2551260786611,7.50893858147472));
#10715=CARTESIAN_POINT('Ctrl Pts',(-0.883730571369413,2.28705709825754,
7.50469733060362));
#10716=CARTESIAN_POINT('Ctrl Pts',(-0.806948993607136,2.3152684860934,7.50045607973252));
#10717=CARTESIAN_POINT('Ctrl Pts',(-0.728890171636918,2.3395874353593,7.49621482886142));
#10718=CARTESIAN_POINT('Ctrl Pts',(-0.651277692296751,2.3637673281611,7.49199782958701));
#10719=CARTESIAN_POINT('Ctrl Pts',(-0.572402984226607,2.38409903603495,
7.4877808303126));
#10720=CARTESIAN_POINT('Ctrl Pts',(-0.492682124565188,2.40046132527353,
7.48356383103818));
#10721=CARTESIAN_POINT('Ctrl Pts',(-0.412987694119799,2.41681819005383,
7.47934822979166));
#10722=CARTESIAN_POINT('Ctrl Pts',(-0.332448124346945,2.42920815602309,
7.47513262854513));
#10723=CARTESIAN_POINT('Ctrl Pts',(-0.251491314955957,2.43756074149994,
7.4709170272986));
#10724=CARTESIAN_POINT('Ctrl Pts',(-0.170536525653001,2.44591311855753,
7.46670153124256));
#10725=CARTESIAN_POINT('Ctrl Pts',(-0.0891649801482384,2.45022826877624,
7.46248603518651));
#10726=CARTESIAN_POINT('Ctrl Pts',(-0.00780992151061345,2.4504875545748,
7.45827053913046));
#10727=CARTESIAN_POINT('Ctrl Pts',(0.0744072028859268,2.45074958785351,
7.45401037425028));
#10728=CARTESIAN_POINT('Ctrl Pts',(0.156607004519655,2.44686927263525,7.4497502093701));
#10729=CARTESIAN_POINT('Ctrl Pts',(0.238343990175726,2.43888138136054,7.44549004448992));
#10730=CARTESIAN_POINT('Ctrl Pts',(0.319341731299578,2.43096573406329,7.44126840933491));
#10731=CARTESIAN_POINT('Ctrl Pts',(0.399884538280696,2.4190166412806,7.43704677417991));
#10732=CARTESIAN_POINT('Ctrl Pts',(0.479547533480251,2.40311972509341,7.4328251390249));
#10733=CARTESIAN_POINT('Ctrl Pts',(0.560301122679176,2.387005178608,7.42854570928213));
#10734=CARTESIAN_POINT('Ctrl Pts',(0.640150148698512,2.36683401927795,7.42426627953936));
#10735=CARTESIAN_POINT('Ctrl Pts',(0.718668183776595,2.34274759451957,7.41998684979659));
#10736=CARTESIAN_POINT('Ctrl Pts',(0.797186218854677,2.31866116976119,7.41570742005382));
#10737=CARTESIAN_POINT('Ctrl Pts',(0.874372824147611,2.29065970844442,7.41142799031106));
#10738=CARTESIAN_POINT('Ctrl Pts',(0.94982462113251,2.25893413783813,7.40714856056829));
#10739=CARTESIAN_POINT('Ctrl Pts',(1.02441728808841,2.22756980966057,7.40291785844694));
#10740=CARTESIAN_POINT('Ctrl Pts',(1.09759503318878,2.19244781989382,7.39868715632559));
#10741=CARTESIAN_POINT('Ctrl Pts',(1.16895329163391,2.15371735656707,7.39445645420424));
#10742=CARTESIAN_POINT('Ctrl Pts',(1.24020902791233,2.11504253825051,7.39023183043679));
#10743=CARTESIAN_POINT('Ctrl Pts',(1.30965006401606,2.07276976280726,7.38600720666934));
#10744=CARTESIAN_POINT('Ctrl Pts',(1.37689184720839,2.0270962214683,7.38178258290188));
#10745=CARTESIAN_POINT('Ctrl Pts',(1.44439827712931,1.98124292057027,7.37754133207895));
#10746=CARTESIAN_POINT('Ctrl Pts',(1.50968766814146,1.93196221118463,7.37330008125602));
#10747=CARTESIAN_POINT('Ctrl Pts',(1.57239597731041,1.87950023690821,7.36905883043309));
#10748=CARTESIAN_POINT('Ctrl Pts',(1.63474572211708,1.82733823873704,7.36484183096403));
#10749=CARTESIAN_POINT('Ctrl Pts',(1.69454346181136,1.77203155913337,7.36062483149498));
#10750=CARTESIAN_POINT('Ctrl Pts',(1.75146199913296,1.71386438074696,7.35640783202593));
#10751=CARTESIAN_POINT('Ctrl Pts',(1.80836166671137,1.65571648605564,7.35219223058466));
#10752=CARTESIAN_POINT('Ctrl Pts',(1.86238370242667,1.59471030791258,7.3479766291434));
#10753=CARTESIAN_POINT('Ctrl Pts',(1.91323717828737,1.53116744662985,7.34376102770214));
#10754=CARTESIAN_POINT('Ctrl Pts',(1.9640893852163,1.46762617091338,7.33954553145153));
#10755=CARTESIAN_POINT('Ctrl Pts',(2.011772899749,1.40154870168318,7.33533003520092));
#10756=CARTESIAN_POINT('Ctrl Pts',(2.05603748925338,1.33328920073053,7.33111453895032));
#10757=CARTESIAN_POINT('Ctrl Pts',(2.10077111685933,1.26430640589672,7.32685437430042));
#10758=CARTESIAN_POINT('Ctrl Pts',(2.14201265542884,1.19309545906634,7.32259420965052));
#10759=CARTESIAN_POINT('Ctrl Pts',(2.17955014489416,1.12004973813302,7.31833404500063));
#10760=CARTESIAN_POINT('Ctrl Pts',(2.21674814201247,1.04766464910641,7.31411240965347));
#10761=CARTESIAN_POINT('Ctrl Pts',(2.25030868244795,0.973478294070949,7.3098907743063));
#10762=CARTESIAN_POINT('Ctrl Pts',(2.28007371980181,0.897894248934212,7.30566913895914));
#10763=CARTESIAN_POINT('Ctrl Pts',(2.31024623886864,0.821275462405448,7.30138970965788));
#10764=CARTESIAN_POINT('Ctrl Pts',(2.33651838976551,0.743220896231788,7.29711028035661));
#10765=CARTESIAN_POINT('Ctrl Pts',(2.35877813837818,0.664165599763462,7.29283085105534));
#10766=CARTESIAN_POINT('Ctrl Pts',(2.38103788699085,0.585110303295135,7.28855142175408));
#10767=CARTESIAN_POINT('Ctrl Pts',(2.39928518814817,0.505054769405927,7.28427199245281));
#10768=CARTESIAN_POINT('Ctrl Pts',(2.41346217146823,0.424441511744397,7.27999256315154));
#10769=CARTESIAN_POINT('Ctrl Pts',(2.42747772865689,0.344746156434165,7.2757618615451));
#10770=CARTESIAN_POINT('Ctrl Pts',(2.43756794910575,0.264205964793622,7.27153115993865));
#10771=CARTESIAN_POINT('Ctrl Pts',(2.44363922756305,0.183241849791682,7.26730045833221));
#10772=CARTESIAN_POINT('Ctrl Pts',(2.44970178326352,0.102394057948189,7.26307583508002));
#10773=CARTESIAN_POINT('Ctrl Pts',(2.45175683019946,0.0211240121960097,
7.25885121182784));
#10774=CARTESIAN_POINT('Ctrl Pts',(2.44976195693876,-0.060138210279318,
7.25462658857565));
#10775=CARTESIAN_POINT('Ctrl Pts',(2.44775923205409,-0.141720272829519,
7.25038533762395));
#10776=CARTESIAN_POINT('Ctrl Pts',(2.44167455622559,-0.223293983005645,
7.24614408667225));
#10777=CARTESIAN_POINT('Ctrl Pts',(2.4315177793486,-0.304420003796851,7.24190283572055));
#10778=CARTESIAN_POINT('Ctrl Pts',(2.4214190801722,-0.38508213601366,7.23768583676393));
#10779=CARTESIAN_POINT('Ctrl Pts',(2.40729478148,-0.465301218741227,7.23346883780732));
#10780=CARTESIAN_POINT('Ctrl Pts',(2.38920666347201,-0.544648298648727,
7.2292518388507));
#10781=CARTESIAN_POINT('Ctrl Pts',(2.37112454206316,-0.623969073297096,
7.22503623791971));
#10782=CARTESIAN_POINT('Ctrl Pts',(2.34908131418291,-0.702417966135538,
7.22082063698871));
#10783=CARTESIAN_POINT('Ctrl Pts',(2.32318985582445,-0.779576259126962,
7.21660503605771));
#10784=CARTESIAN_POINT('Ctrl Pts',(2.29729904351051,-0.856732626862104,
7.21238954031452));
#10785=CARTESIAN_POINT('Ctrl Pts',(2.2675603406103,-0.932598018223689,7.20817404457134));
#10786=CARTESIAN_POINT('Ctrl Pts',(2.23413603237521,-1.006770300934,7.20395854882816));
#10787=CARTESIAN_POINT('Ctrl Pts',(2.20035754334729,-1.08172855048354,7.19969838357038));
#10788=CARTESIAN_POINT('Ctrl Pts',(2.16281505919034,-1.15495714735286,7.1954382183126));
#10789=CARTESIAN_POINT('Ctrl Pts',(2.12172455778278,-1.22606490484862,7.19117805305482));
#10790=CARTESIAN_POINT('Ctrl Pts',(2.08100569306159,-1.29652953922673,7.18695641820299));
#10791=CARTESIAN_POINT('Ctrl Pts',(2.03680303903082,-1.36491118172741,7.18273478335116));
#10792=CARTESIAN_POINT('Ctrl Pts',(1.98937033695942,-1.4308584529666,7.17851314849933));
#10793=CARTESIAN_POINT('Ctrl Pts',(1.94128826515444,-1.49770856465308,7.17423371803858));
#10794=CARTESIAN_POINT('Ctrl Pts',(1.88988734347876,-1.56205675916543,7.16995428757782));
#10795=CARTESIAN_POINT('Ctrl Pts',(1.83547268668684,-1.62357330183351,7.16567485711707));
#10796=CARTESIAN_POINT('Ctrl Pts',(1.78105802989493,-1.6850898445016,7.16139542665632));
#10797=CARTESIAN_POINT('Ctrl Pts',(1.72363002791887,-1.74377443049916,7.15711599619557));
#10798=CARTESIAN_POINT('Ctrl Pts',(1.66352939610883,-1.79933882253504,7.15283656573482));
#10799=CARTESIAN_POINT('Ctrl Pts',(1.60411311074133,-1.85427052082251,7.14860586376366));
#10800=CARTESIAN_POINT('Ctrl Pts',(1.54186129871659,-1.90635936664518,7.14437516179251));
#10801=CARTESIAN_POINT('Ctrl Pts',(1.47707716683612,-1.95529877338768,7.14014445982135));
#10802=CARTESIAN_POINT('Ctrl Pts',(1.4123861119746,-2.00416786763303,7.13591983620791));
#10803=CARTESIAN_POINT('Ctrl Pts',(1.34517033095112,-2.04989623151421,7.13169521259446));
#10804=CARTESIAN_POINT('Ctrl Pts',(1.27576845239048,-2.09221535839053,7.12747058898102));
#10805=CARTESIAN_POINT('Ctrl Pts',(1.20609342234507,-2.13470104462489,7.12322933812006));
#10806=CARTESIAN_POINT('Ctrl Pts',(1.13421539824854,-2.17375027803472,7.11898808725911));
#10807=CARTESIAN_POINT('Ctrl Pts',(1.06050908877473,-2.20913347777498,7.11474683639815));
#10808=CARTESIAN_POINT('Ctrl Pts',(0.987224233395099,-2.24431435569908,
7.11052983709113));
#10809=CARTESIAN_POINT('Ctrl Pts',(0.912132367711619,-2.27587080780046,
7.10631283778411));
#10810=CARTESIAN_POINT('Ctrl Pts',(0.835627586040501,-2.30362253580054,
7.10209583847709));
#10811=CARTESIAN_POINT('Ctrl Pts',(0.759148167431046,-2.3313650634765,7.09788023720051));
#10812=CARTESIAN_POINT('Ctrl Pts',(0.681257199863043,-2.35530521342064,
7.09366463592394));
#10813=CARTESIAN_POINT('Ctrl Pts',(0.602367836122385,-2.37531118803521,
7.08944903464736));
#10814=CARTESIAN_POINT('Ctrl Pts',(0.523480440929719,-2.39531666343519,
7.08523353856384));
#10815=CARTESIAN_POINT('Ctrl Pts',(0.443595150155823,-2.41138804542613,
7.08101804248031));
#10816=CARTESIAN_POINT('Ctrl Pts',(0.363137922745616,-2.42344405734153,
7.07680254639679));
#10817=CARTESIAN_POINT('Ctrl Pts',(0.281828144599183,-2.43562781864832,
7.0725423815569));
#10818=CARTESIAN_POINT('Ctrl Pts',(0.199934713527443,-2.44371051915612,
7.06828221671701));
#10819=CARTESIAN_POINT('Ctrl Pts',(0.11790345548595,-2.44766195075719,7.06402205187711));
#10820=CARTESIAN_POINT('Ctrl Pts',(0.0366141022588304,-2.45157764493086,
7.05980041670116));
#10821=CARTESIAN_POINT('Ctrl Pts',(-0.0448101247834487,-2.45143655996938,
7.0555787815252));
#10822=CARTESIAN_POINT('Ctrl Pts',(-0.125936422192143,-2.44726178974899,
7.05135714634924));
#10823=CARTESIAN_POINT('Ctrl Pts',(-0.208173344576256,-2.44302986661738,
7.04707771667738));
#10824=CARTESIAN_POINT('Ctrl Pts',(-0.290103626117359,-2.43465302941235,
7.04279828700552));
#10825=CARTESIAN_POINT('Ctrl Pts',(-0.371284847441249,-2.42220928329088,
7.03851885733366));
#10826=CARTESIAN_POINT('Ctrl Pts',(-0.452466068765136,-2.40976553716941,
7.0342394276618));
#10827=CARTESIAN_POINT('Ctrl Pts',(-0.532897762473629,-2.39325504493292,
7.02995999798993));
#10828=CARTESIAN_POINT('Ctrl Pts',(-0.612153123812642,-2.37280821032936,
7.02568056831807));
#10829=CARTESIAN_POINT('Ctrl Pts',(-0.690506065164704,-2.35259418814258,
7.02144986522828));
#10830=CARTESIAN_POINT('Ctrl Pts',(-0.768004043535359,-2.32845701955206,
7.01721916213848));
#10831=CARTESIAN_POINT('Ctrl Pts',(-0.844225134002871,-2.30048563853762,
7.01298845904869));
#10832=CARTESIAN_POINT('Ctrl Pts',(-0.920336715861448,-2.27255444465519,
7.00876383430817));
#10833=CARTESIAN_POINT('Ctrl Pts',(-0.995174620417518,-2.24080013779327,
7.00453920956766));
#10834=CARTESIAN_POINT('Ctrl Pts',(-1.06832976100188,-2.20536205004023,
7.00031458482714));
#10835=CARTESIAN_POINT('Ctrl Pts',(-1.14177280068195,-2.16978449712677,
6.9960733342469));
#10836=CARTESIAN_POINT('Ctrl Pts',(-1.21351934357818,-2.13049422494611,
6.99183208366666));
#10837=CARTESIAN_POINT('Ctrl Pts',(-1.28317349642087,-2.08768197484268,
6.98759083308642));
#10838=CARTESIAN_POINT('Ctrl Pts',(-1.35242938877218,-2.04511451169118,
6.98337383264018));
#10839=CARTESIAN_POINT('Ctrl Pts',(-1.41961635321147,-1.99906548242192,
6.97915683219393));
#10840=CARTESIAN_POINT('Ctrl Pts',(-1.4843694351532,-1.94976860934393,6.97493983174769));
#10841=CARTESIAN_POINT('Ctrl Pts',(-1.54910105002411,-1.90048807926359,
6.97072422932985));
#10842=CARTESIAN_POINT('Ctrl Pts',(-1.61140001499802,-1.84796212506383,
6.966508626912));
#10843=CARTESIAN_POINT('Ctrl Pts',(-1.6709318343281,-1.79246675144308,6.96229302449416));
#10844=CARTESIAN_POINT('Ctrl Pts',(-1.73046216815164,-1.73697276260684,
6.95807752726888));
#10845=CARTESIAN_POINT('Ctrl Pts',(-1.78722515418016,-1.67850981957754,
6.9538620300436));
#10846=CARTESIAN_POINT('Ctrl Pts',(-1.8409218391178,-1.61739204655492,6.94964653281833));
#10847=CARTESIAN_POINT('Ctrl Pts',(-1.8951874795977,-1.55562668614899,6.94538636932524));
#10848=CARTESIAN_POINT('Ctrl Pts',(-1.94632112084788,-1.49115025438227,
6.94112620583216));
#10849=CARTESIAN_POINT('Ctrl Pts',(-1.99405599006674,-1.42432122727949,
6.93686604233908));
#10850=CARTESIAN_POINT('Ctrl Pts',(-2.04135916454392,-1.358096574716,6.93264440603186));
#10851=CARTESIAN_POINT('Ctrl Pts',(-2.08532459200953,-1.2895621366162,6.92842276972465));
#10852=CARTESIAN_POINT('Ctrl Pts',(-2.12573736376488,-1.21909429918032,
6.92420113341743));
#10853=CARTESIAN_POINT('Ctrl Pts',(-2.16670335360515,-1.14766181417434,
6.91992170633141));
#10854=CARTESIAN_POINT('Ctrl Pts',(-2.20401846124588,-1.07424303669084,
6.9156422792454));
#10855=CARTESIAN_POINT('Ctrl Pts',(-2.23750873930705,-0.999252166134541,
6.91136285215939));
#10856=CARTESIAN_POINT('Ctrl Pts',(-2.27099901736822,-0.924261295578242,
6.90708342507337));
#10857=CARTESIAN_POINT('Ctrl Pts',(-2.30066434967179,-0.847698813057868,
6.90280399798736));
#10858=CARTESIAN_POINT('Ctrl Pts',(-2.32638329709889,-0.769994159055309,
6.89852457090134));
#10859=CARTESIAN_POINT('Ctrl Pts',(-2.3566686452367,-0.67849303891555,6.89348533127081));
#10860=CARTESIAN_POINT('Ctrl Pts',(-2.38157637743318,-0.585128820600957,
6.88844609164027));
#10861=CARTESIAN_POINT('Ctrl Pts',(-2.40091147363867,-0.490483787448861,
6.88340685200973));
#10862=CARTESIAN_POINT('Ctrl Pts',(-2.42003159244815,-0.396891065728579,
6.87842364119861));
#10863=CARTESIAN_POINT('Ctrl Pts',(-2.43370224826641,-0.302045926058559,
6.8734404303875));
#10864=CARTESIAN_POINT('Ctrl Pts',(-2.44178104459956,-0.206532274074234,
6.86845721957638));
#10865=CARTESIAN_POINT('Ctrl Pts',(-2.44752534292489,-0.138618826511733,
6.86491398759767));
#10866=CARTESIAN_POINT('Ctrl Pts',(-2.45044351293468,-0.0703678342595561,
6.86137075561896));
#10867=CARTESIAN_POINT('Ctrl Pts',(-2.45049918758584,-0.00199540500347388,
6.85782752364025));
#10868=CARTESIAN_POINT('',(-2.44727079087888,0.00140258600070248,6.05782749621206));
#10869=CARTESIAN_POINT('Ctrl Pts',(-2.44847580618664,-0.00199322855914286,
6.85782749621206));
#10870=CARTESIAN_POINT('Ctrl Pts',(-2.44423578927424,0.553673293985754,
6.82900785530291));
#10871=CARTESIAN_POINT('Ctrl Pts',(-1.98117851569519,1.93295874884265,6.75780288192152));
#10872=CARTESIAN_POINT('Ctrl Pts',(0.309238178351472,2.88090180145063,6.64421257606786));
#10873=CARTESIAN_POINT('Ctrl Pts',(2.5895656520796,1.29976107516381,6.51705657865114));
#10874=CARTESIAN_POINT('Ctrl Pts',(2.4948043245916,-1.47349273530034,6.38990058123439));
#10875=CARTESIAN_POINT('Ctrl Pts',(0.111868608253771,-2.89528816042125,
6.26274458381766));
#10876=CARTESIAN_POINT('Ctrl Pts',(-2.05182862477049,-1.82135004090711,
6.15205355547688));
#10877=CARTESIAN_POINT('Ctrl Pts',(-2.44467631807943,-0.498983029647765,
6.08374785960835));
#10878=CARTESIAN_POINT('Ctrl Pts',(-2.44727079087888,0.00140258600070248,
6.05782749621206));
#10879=CARTESIAN_POINT('Ctrl Pts',(-2.44727079087888,0.00140258600070248,
6.05782749621206));
#10880=CARTESIAN_POINT('Ctrl Pts',(-2.44891883545906,0.31925436769618,6.0413625271361));
#10881=CARTESIAN_POINT('Ctrl Pts',(-2.24355247310808,1.45329452179378,5.98251222558789));
#10882=CARTESIAN_POINT('Ctrl Pts',(-0.530612503065825,2.84843065415222,
5.88127659156747));
#10883=CARTESIAN_POINT('Ctrl Pts',(2.10758727991065,1.98834031509364,5.75412059415071));
#10884=CARTESIAN_POINT('Ctrl Pts',(2.812732038963,-0.695553730705045,5.62696459673398));
#10885=CARTESIAN_POINT('Ctrl Pts',(0.938155002898276,-2.7412257732876,5.49980859931725));
#10886=CARTESIAN_POINT('Ctrl Pts',(-1.70855726544326,-2.28836551633789,
5.37676289914326));
#10887=CARTESIAN_POINT('Ctrl Pts',(-2.448662628639,-0.732444886033958,5.29610253144154));
#10888=CARTESIAN_POINT('Ctrl Pts',(-2.45356474526275,0.00152995343032009,
5.25782749621206));
#10889=CARTESIAN_POINT('Origin',(0.,0.,3.52095488139519));
#10890=CARTESIAN_POINT('',(-1.13766281679009,-1.63852094212837,5.));
#10891=CARTESIAN_POINT('',(-1.99474929467261,-0.00167746926262795,6.47978083014939));
#10892=CARTESIAN_POINT('Ctrl Pts',(-1.99474929622187,-0.00167562595544705,
6.47978072236948));
#10893=CARTESIAN_POINT('Ctrl Pts',(-1.99483545784495,0.100895497651632,
6.47378329174917));
#10894=CARTESIAN_POINT('Ctrl Pts',(-1.98701043932826,0.203310863465348,
6.4676806320529));
#10895=CARTESIAN_POINT('Ctrl Pts',(-1.96937497030234,0.317421448938346,
6.46052004982015));
#10896=CARTESIAN_POINT('Ctrl Pts',(-1.96727993673741,0.330157217431481,
6.45971591010473));
#10897=CARTESIAN_POINT('Ctrl Pts',(-1.963773434283,0.350253645291977,6.45843877103503));
#10898=CARTESIAN_POINT('Ctrl Pts',(-1.96244380023555,0.357628362555231,
6.45796834281405));
#10899=CARTESIAN_POINT('Ctrl Pts',(-1.96011217704298,0.370155872022657,
6.45716614897992));
#10900=CARTESIAN_POINT('Ctrl Pts',(-1.9591313376779,0.375312559156564,6.4568350552308));
#10901=CARTESIAN_POINT('Ctrl Pts',(-1.95726986988266,0.384892924240948,
6.4562182546167));
#10902=CARTESIAN_POINT('Ctrl Pts',(-1.95639456720463,0.389317612686523,
6.45593271890036));
#10903=CARTESIAN_POINT('Ctrl Pts',(-1.95454910215499,0.398483106474347,
6.45533984795679));
#10904=CARTESIAN_POINT('Ctrl Pts',(-1.95357668142963,0.403223421909805,
6.45503244234779));
#10905=CARTESIAN_POINT('Ctrl Pts',(-1.95131894196877,0.414029460517692,
6.45432988210507));
#10906=CARTESIAN_POINT('Ctrl Pts',(-1.9500225755942,0.420092800105781,6.45393437629805));
#10907=CARTESIAN_POINT('Ctrl Pts',(-1.94596819471851,0.438632668434363,
6.45272101625882));
#10908=CARTESIAN_POINT('Ctrl Pts',(-1.94311859336475,0.451088630052562,
6.45190023447609));
#10909=CARTESIAN_POINT('Ctrl Pts',(-1.91673115779224,0.561539097367733,
6.44457117467772));
#10910=CARTESIAN_POINT('Ctrl Pts',(-1.88592180806099,0.65763034597248,6.43782599008551));
#10911=CARTESIAN_POINT('Ctrl Pts',(-1.83102027101028,0.792732209204058,
6.42781686022865));
#10912=CARTESIAN_POINT('Ctrl Pts',(-1.81263947984916,0.833904925648595,
6.42469358502988));
#10913=CARTESIAN_POINT('Ctrl Pts',(-1.77596335178935,0.909104539903885,
6.41887035459788));
#10914=CARTESIAN_POINT('Ctrl Pts',(-1.75804329577687,0.943292440308809,
6.41617538920016));
#10915=CARTESIAN_POINT('Ctrl Pts',(-1.6931828168785,1.05875684170231,6.40693979961625));
#10916=CARTESIAN_POINT('Ctrl Pts',(-1.64150169914192,1.13723770495279,6.40042327456305));
#10917=CARTESIAN_POINT('Ctrl Pts',(-1.57107855529992,1.22931954274143,6.3927050128987));
#10918=CARTESIAN_POINT('Ctrl Pts',(-1.55738454599874,1.24662257378676,6.39125157235773));
#10919=CARTESIAN_POINT('Ctrl Pts',(-1.54002211389152,1.26782805436302,6.38947009772506));
#10920=CARTESIAN_POINT('Ctrl Pts',(-1.53662202572881,1.27194686930946,6.38912406516935));
#10921=CARTESIAN_POINT('Ctrl Pts',(-1.53123558281951,1.27841880232028,6.38858039218694));
#10922=CARTESIAN_POINT('Ctrl Pts',(-1.52926028282817,1.28078102417959,6.38838196522768));
#10923=CARTESIAN_POINT('Ctrl Pts',(-1.52554376976702,1.28520467246108,6.38801041412956));
#10924=CARTESIAN_POINT('Ctrl Pts',(-1.52380386401095,1.28726711591932,6.38783720203768));
#10925=CARTESIAN_POINT('Ctrl Pts',(-1.51982425555209,1.29196507559292,6.38744267825979));
#10926=CARTESIAN_POINT('Ctrl Pts',(-1.51758188462613,1.29459829607974,6.38722156597914));
#10927=CARTESIAN_POINT('Ctrl Pts',(-1.51068680961063,1.30265266346664,6.38654525043112));
#10928=CARTESIAN_POINT('Ctrl Pts',(-1.50601175842704,1.30805473339989,6.38609166184389));
#10929=CARTESIAN_POINT('Ctrl Pts',(-1.46849566989697,1.35093720225692,6.38249004175736));
#10930=CARTESIAN_POINT('Ctrl Pts',(-1.43428646804993,1.38720371466403,6.37943807103119));
#10931=CARTESIAN_POINT('Ctrl Pts',(-1.38618047241073,1.43451809404303,6.37538544944971));
#10932=CARTESIAN_POINT('Ctrl Pts',(-1.37344580270871,1.44671528620066,6.37433393248397));
#10933=CARTESIAN_POINT('Ctrl Pts',(-1.30422033565708,1.51128101896889,6.36872016674912));
#10934=CARTESIAN_POINT('Ctrl Pts',(-1.24489149383222,1.56051503964148,6.36426581366972));
#10935=CARTESIAN_POINT('Ctrl Pts',(-1.10458100944215,1.66384482259954,6.3541587884084));
#10936=CARTESIAN_POINT('Ctrl Pts',(-1.02219467798493,1.71569079889588,6.34850760007928));
#10937=CARTESIAN_POINT('Ctrl Pts',(-0.902002049954595,1.77958820547176,
6.34032786939562));
#10938=CARTESIAN_POINT('Ctrl Pts',(-0.867116258291207,1.79684473030039,
6.33796194397986));
#10939=CARTESIAN_POINT('Ctrl Pts',(-0.809148149437407,1.8234377342857,6.33402825651246));
#10940=CARTESIAN_POINT('Ctrl Pts',(-0.786355536221787,1.83338233401351,
6.33248104399878));
#10941=CARTESIAN_POINT('Ctrl Pts',(-0.755949547503772,1.84597740904105,
6.33041388425508));
#10942=CARTESIAN_POINT('Ctrl Pts',(-0.748496865557286,1.84901183128992,
6.32990696939371));
#10943=CARTESIAN_POINT('Ctrl Pts',(-0.736829242274105,1.85368030250194,
6.32911290575315));
#10944=CARTESIAN_POINT('Ctrl Pts',(-0.732626702307686,1.85534528071483,
6.32882680122559));
#10945=CARTESIAN_POINT('Ctrl Pts',(-0.723928664410519,1.85875714184884,
6.32823444029299));
#10946=CARTESIAN_POINT('Ctrl Pts',(-0.719432421645852,1.86050203266296,
6.32792811927288));
#10947=CARTESIAN_POINT('Ctrl Pts',(-0.709279634326413,1.86439979459841,
6.32723614944195));
#10948=CARTESIAN_POINT('Ctrl Pts',(-0.703619550282622,1.86654325449338,
6.32685018844351));
#10949=CARTESIAN_POINT('Ctrl Pts',(-0.689120847414753,1.87195855883133,
6.32586098253435));
#10950=CARTESIAN_POINT('Ctrl Pts',(-0.680268713248486,1.87519355295221,
6.32525651476466));
#10951=CARTESIAN_POINT('Ctrl Pts',(-0.628244223989518,1.89378893971041,
6.3217007059215));
#10952=CARTESIAN_POINT('Ctrl Pts',(-0.58457894865682,1.90771964158041,6.31870241676991));
#10953=CARTESIAN_POINT('Ctrl Pts',(-0.410651896070864,1.95667629777106,
6.30669462949979));
#10954=CARTESIAN_POINT('Ctrl Pts',(-0.277474502821969,1.97995323086137,
6.29732692835705));
#10955=CARTESIAN_POINT('Ctrl Pts',(-0.0671962521706056,1.99506558345611,
6.28261850168907));
#10956=CARTESIAN_POINT('Ctrl Pts',(0.00885162920110615,1.99617757585605,
6.27732407312693));
#10957=CARTESIAN_POINT('Ctrl Pts',(0.115373037623233,1.99164610082271,6.2700756496008));
#10958=CARTESIAN_POINT('Ctrl Pts',(0.14593287779101,1.98964040498711,6.26801596116497));
#10959=CARTESIAN_POINT('Ctrl Pts',(0.19404508037269,1.98536812464061,6.26481644041901));
#10960=CARTESIAN_POINT('Ctrl Pts',(0.211633251299721,1.98357039289723,6.26365595607929));
#10961=CARTESIAN_POINT('Ctrl Pts',(0.234087125333168,1.98097325174916,6.26218810326669));
#10962=CARTESIAN_POINT('Ctrl Pts',(0.238976276339238,1.98038939276991,6.26186932122211));
#10963=CARTESIAN_POINT('Ctrl Pts',(0.246827286499457,1.97942233284843,6.26135881036512));
#10964=CARTESIAN_POINT('Ctrl Pts',(0.249790495085022,1.97905057792708,6.26116644657866));
#10965=CARTESIAN_POINT('Ctrl Pts',(0.255450902701729,1.97832752518511,6.26079961078503));
#10966=CARTESIAN_POINT('Ctrl Pts',(0.258148185381015,1.97797736970302,6.26062507957087));
#10967=CARTESIAN_POINT('Ctrl Pts',(0.264380546801473,1.97715533230295,6.26022242311067));
#10968=CARTESIAN_POINT('Ctrl Pts',(0.267915081921974,1.97667948614402,6.25999452395423));
#10969=CARTESIAN_POINT('Ctrl Pts',(0.278992644397972,1.97515788154757,6.25928164912899));
#10970=CARTESIAN_POINT('Ctrl Pts',(0.286531083075442,1.97407839144626,6.25879853859943));
#10971=CARTESIAN_POINT('Ctrl Pts',(0.367182079548968,1.9620575955819,6.25364968208958));
#10972=CARTESIAN_POINT('Ctrl Pts',(0.439648080560575,1.94710169364371,6.24919673160379));
#10973=CARTESIAN_POINT('Ctrl Pts',(0.649999597695964,1.89134069608987,6.2363481732548));
#10974=CARTESIAN_POINT('Ctrl Pts',(0.784491178788448,1.83963174432793,6.22820483318484));
#10975=CARTESIAN_POINT('Ctrl Pts',(0.960232980314657,1.74925403133659,6.21648535583192));
#10976=CARTESIAN_POINT('Ctrl Pts',(1.00717766616614,1.72265188078188,6.21324263821359));
#10977=CARTESIAN_POINT('Ctrl Pts',(1.07076977977223,1.68312749457902,6.20865138836919));
#10978=CARTESIAN_POINT('Ctrl Pts',(1.08837961537673,1.67179419998456,6.20735799507431));
#10979=CARTESIAN_POINT('Ctrl Pts',(1.11462089798262,1.65431555613821,6.20539535499746));
#10980=CARTESIAN_POINT('Ctrl Pts',(1.123387494083,1.64837502918241,6.20473362988915));
#10981=CARTESIAN_POINT('Ctrl Pts',(1.13937934459163,1.63735161293312,6.2035151157058));
#10982=CARTESIAN_POINT('Ctrl Pts',(1.14661896801578,1.63228996609139,6.20295913405017));
#10983=CARTESIAN_POINT('Ctrl Pts',(1.15817270784372,1.62409727327752,6.2020647204416));
#10984=CARTESIAN_POINT('Ctrl Pts',(1.16250836543807,1.62099669143672,6.20172745823199));
#10985=CARTESIAN_POINT('Ctrl Pts',(1.16683711738787,1.61787474917985,6.20138908820981));
#10986=CARTESIAN_POINT('Ctrl Pts',(1.1668427251728,1.61787070474099,6.20138864985752));
#10987=CARTESIAN_POINT('Ctrl Pts',(1.16685395790826,1.61786260339434,6.20138777180559));
#10988=CARTESIAN_POINT('Ctrl Pts',(1.16685958274033,1.61785854657172,6.20138733211519));
#10989=CARTESIAN_POINT('Ctrl Pts',(1.1668708493223,1.61785042063543,6.20138645140633));
#10990=CARTESIAN_POINT('Ctrl Pts',(1.16687649115576,1.61784635146123,6.20138601038133));
#10991=CARTESIAN_POINT('Ctrl Pts',(1.16688779196573,1.61783820065853,6.20138512698563));
#10992=CARTESIAN_POINT('Ctrl Pts',(1.16689345090486,1.61783411905672,6.20138468461783));
#10993=CARTESIAN_POINT('Ctrl Pts',(1.16690478602028,1.61782594333011,6.20138379852913));
#10994=CARTESIAN_POINT('Ctrl Pts',(1.1669104621646,1.61782184922808,6.20138335481071));
#10995=CARTESIAN_POINT('Ctrl Pts',(1.16692183156641,1.61781364858965,6.20138246603039));
#10996=CARTESIAN_POINT('Ctrl Pts',(1.1669275249085,1.61780954199195,6.20138202096186));
#10997=CARTESIAN_POINT('Ctrl Pts',(1.1669389288723,1.61780131624126,6.20138112946828));
#10998=CARTESIAN_POINT('Ctrl Pts',(1.16694463948499,1.6177971970945,6.20138068304391));
#10999=CARTESIAN_POINT('Ctrl Pts',(1.16695607815501,1.61778894612584,6.20137978882569));
#11000=CARTESIAN_POINT('Ctrl Pts',(1.1669618061394,1.61778481435627,6.20137934103752));
#11001=CARTESIAN_POINT('Ctrl Pts',(1.16697327957827,1.61777653812278,6.20137844408965));
#11002=CARTESIAN_POINT('Ctrl Pts',(1.16697902500957,1.6177723936753,6.20137799493174));
#11003=CARTESIAN_POINT('Ctrl Pts',(1.16699053327574,1.61776409213312,6.20137709524955));
#11004=CARTESIAN_POINT('Ctrl Pts',(1.16699629617251,1.61775993499349,6.20137664472041));
#11005=CARTESIAN_POINT('Ctrl Pts',(1.16700783944966,1.61775160800842,6.20137574228943));
#11006=CARTESIAN_POINT('Ctrl Pts',(1.16701361984161,1.61774743815436,6.20137529038668));
#11007=CARTESIAN_POINT('Ctrl Pts',(1.16702519843997,1.61773908550089,6.20137438518255));
#11008=CARTESIAN_POINT('Ctrl Pts',(1.16703099650494,1.61773490280323,6.20137393189223));
#11009=CARTESIAN_POINT('Ctrl Pts',(1.16704261023854,1.6177265246138,6.20137302392938));
#11010=CARTESIAN_POINT('Ctrl Pts',(1.16704842595355,1.61772232908827,6.20137256925323));
#11011=CARTESIAN_POINT('Ctrl Pts',(1.16706007514067,1.61771392513151,6.20137165850668));
#11012=CARTESIAN_POINT('Ctrl Pts',(1.16706590858467,1.61770971672027,6.20137120243846));
#11013=CARTESIAN_POINT('Ctrl Pts',(1.16707759338638,1.61770128687824,6.2013702888955));
#11014=CARTESIAN_POINT('Ctrl Pts',(1.16708344468417,1.61769706549038,6.20136983142542));
#11015=CARTESIAN_POINT('Ctrl Pts',(1.1670951650322,1.61768860981056,6.20136891509127));
#11016=CARTESIAN_POINT('Ctrl Pts',(1.1671010341701,1.61768437545507,6.20136845622033));
#11017=CARTESIAN_POINT('Ctrl Pts',(1.16711279038519,1.61767589370429,6.20136753706982));
#11018=CARTESIAN_POINT('Ctrl Pts',(1.16711867746088,1.6176716463098,6.20136707679033));
#11019=CARTESIAN_POINT('Ctrl Pts',(1.16713046958509,1.61766313845594,6.20136615482004));
#11020=CARTESIAN_POINT('Ctrl Pts',(1.16713637463946,1.61765887799204,6.20136569312876));
#11021=CARTESIAN_POINT('Ctrl Pts',(1.16714820292851,1.61765034384878,6.20136476831859));
#11022=CARTESIAN_POINT('Ctrl Pts',(1.16715412610175,1.61764607021344,6.20136430520449));
#11023=CARTESIAN_POINT('Ctrl Pts',(1.16716599042766,1.61763750987132,6.20136337756433));
#11024=CARTESIAN_POINT('Ctrl Pts',(1.167171931674,1.61763322309665,6.20136291303093));
#11025=CARTESIAN_POINT('Ctrl Pts',(1.1671838324892,1.6176246362274,6.2013619825253));
#11026=CARTESIAN_POINT('Ctrl Pts',(1.16718979197073,1.61762033619553,6.20136151655988));
#11027=CARTESIAN_POINT('Ctrl Pts',(1.16720172917041,1.61761172287293,6.20136058319685));
#11028=CARTESIAN_POINT('Ctrl Pts',(1.16720770690673,1.6176074095688,6.20136011579781));
#11029=CARTESIAN_POINT('Ctrl Pts',(1.1672196807526,1.61759876960217,6.20135917955681));
#11030=CARTESIAN_POINT('Ctrl Pts',(1.16722567684419,1.61759444295234,6.20135871071624));
#11031=CARTESIAN_POINT('Ctrl Pts',(1.16723768734518,1.61758577633339,6.20135777159645));
#11032=CARTESIAN_POINT('Ctrl Pts',(1.16724370180057,1.61758143633077,6.20135730131362));
#11033=CARTESIAN_POINT('Ctrl Pts',(1.16725574926075,1.61757274283819,6.20135635929115));
#11034=CARTESIAN_POINT('Ctrl Pts',(1.16726178219903,1.61756838939591,6.20135588755669));
#11035=CARTESIAN_POINT('Ctrl Pts',(1.16727386665867,1.61755966899877,6.20135494262827));
#11036=CARTESIAN_POINT('Ctrl Pts',(1.16727991815537,1.61755530206138,6.20135446943622));
#11037=CARTESIAN_POINT('Ctrl Pts',(1.1672920396957,1.61754655469914,6.20135352159538));
#11038=CARTESIAN_POINT('Ctrl Pts',(1.16729810977938,1.61754217424508,6.20135304694344));
#11039=CARTESIAN_POINT('Ctrl Pts',(1.16731026860616,1.61753339976737,6.20135209617397));
#11040=CARTESIAN_POINT('Ctrl Pts',(1.16731635733521,1.61752900575354,6.20135162005752));
#11041=CARTESIAN_POINT('Ctrl Pts',(1.1673285537123,1.617520203968,6.20135066633867));
#11042=CARTESIAN_POINT('Ctrl Pts',(1.16733466126203,1.61751579626691,6.20135018874394));
#11043=CARTESIAN_POINT('Ctrl Pts',(1.16734689496726,1.61750696733194,6.20134923209296));
#11044=CARTESIAN_POINT('Ctrl Pts',(1.16735302125991,1.61750254599875,6.20134875302597));
#11045=CARTESIAN_POINT('Ctrl Pts',(1.16736529280305,1.6174936895445,6.20134779340287));
#11046=CARTESIAN_POINT('Ctrl Pts',(1.16737143798602,1.61748925447185,6.20134731285203));
#11047=CARTESIAN_POINT('Ctrl Pts',(1.16738374734558,1.61748037051186,6.20134635025837));
#11048=CARTESIAN_POINT('Ctrl Pts',(1.16738991148429,1.61747592165153,6.2013458682185));
#11049=CARTESIAN_POINT('Ctrl Pts',(1.1674022588263,1.61746701006401,6.20134490264118));
#11050=CARTESIAN_POINT('Ctrl Pts',(1.1674084420091,1.61746254735126,6.20134441910532));
#11051=CARTESIAN_POINT('Ctrl Pts',(1.16742082737896,1.61745360810143,6.20134345054065));
#11052=CARTESIAN_POINT('Ctrl Pts',(1.1674270296184,1.6174491315262,6.20134296550774));
#11053=CARTESIAN_POINT('Ctrl Pts',(1.16743945331582,1.61744016439574,6.20134199393218));
#11054=CARTESIAN_POINT('Ctrl Pts',(1.16744567472654,1.61743567387429,6.20134150739319));
#11055=CARTESIAN_POINT('Ctrl Pts',(1.16745813680016,1.61742667882607,6.20134053280279));
#11056=CARTESIAN_POINT('Ctrl Pts',(1.16746437744894,1.61742217430916,6.20134004475245));
#11057=CARTESIAN_POINT('Ctrl Pts',(1.16747687802406,1.61741315125073,6.20133906713729));
#11058=CARTESIAN_POINT('Ctrl Pts',(1.16748313795783,1.61740863270348,6.20133857757186));
#11059=CARTESIAN_POINT('Ctrl Pts',(1.16749567725866,1.61739958147092,6.20133759691427));
#11060=CARTESIAN_POINT('Ctrl Pts',(1.16750195658278,1.61739504881626,6.20133710582545));
#11061=CARTESIAN_POINT('Ctrl Pts',(1.16751453465434,1.61738596937503,6.20133612212178));
#11062=CARTESIAN_POINT('Ctrl Pts',(1.16752083341089,1.61738142258154,6.20133562950621));
#11063=CARTESIAN_POINT('Ctrl Pts',(1.16753345051829,1.61737231473819,6.20133464273561));
#11064=CARTESIAN_POINT('Ctrl Pts',(1.16753976884214,1.61736775370747,6.20133414858267));
#11065=CARTESIAN_POINT('Ctrl Pts',(1.16755242488283,1.61735861753395,6.20133315875302));
#11066=CARTESIAN_POINT('Ctrl Pts',(1.16755876272582,1.61735404229972,6.20133266306642));
#11067=CARTESIAN_POINT('Ctrl Pts',(1.16757145817837,1.61734487744844,6.20133167014016));
#11068=CARTESIAN_POINT('Ctrl Pts',(1.16757781570674,1.61734028788965,6.20133117290683));
#11069=CARTESIAN_POINT('Ctrl Pts',(1.16759055051545,1.6173310943987,6.20133017688818));
#11070=CARTESIAN_POINT('Ctrl Pts',(1.16759692778888,1.61732649047118,6.20132967810338));
#11071=CARTESIAN_POINT('Ctrl Pts',(1.16760970206933,1.617317268255,6.20132867898318));
#11072=CARTESIAN_POINT('Ctrl Pts',(1.167616099105,1.61731264994529,6.2013281786455));
#11073=CARTESIAN_POINT('Ctrl Pts',(1.17154924071912,1.61447310142397,6.20102054973219));
#11074=CARTESIAN_POINT('Ctrl Pts',(1.17546561882557,1.61162390058299,6.20071287055676));
#11075=CARTESIAN_POINT('Ctrl Pts',(1.18439653130153,1.60507670837164,6.20000809586637));
#11076=CARTESIAN_POINT('Ctrl Pts',(1.18940417405175,1.60136944282339,6.1996106413179));
#11077=CARTESIAN_POINT('Ctrl Pts',(1.20475020153467,1.5898967570584,6.19838553768148));
#11078=CARTESIAN_POINT('Ctrl Pts',(1.21503035429342,1.58205435155071,6.19755487840136));
#11079=CARTESIAN_POINT('Ctrl Pts',(1.31283042549924,1.5059302549315,6.18955479129185));
#11080=CARTESIAN_POINT('Ctrl Pts',(1.39456791579108,1.43056716216406,6.18209546318093));
#11081=CARTESIAN_POINT('Ctrl Pts',(1.58017988328052,1.22833265497639,6.16317566618876));
#11082=CARTESIAN_POINT('Ctrl Pts',(1.67551834430475,1.09471829609673,6.15153291966259));
#11083=CARTESIAN_POINT('Ctrl Pts',(1.7655876895568,0.928640282536424,6.13891008189978));
#11084=CARTESIAN_POINT('Ctrl Pts',(1.77726939827769,0.906082943360314,6.13723293126986));
#11085=CARTESIAN_POINT('Ctrl Pts',(1.79097575625745,0.878330356717615,6.13522003300546));
#11086=CARTESIAN_POINT('Ctrl Pts',(1.79341303610973,0.873343036116761,6.13486026386835));
#11087=CARTESIAN_POINT('Ctrl Pts',(1.79719015755045,0.865531553428992,6.13429990467391));
#11088=CARTESIAN_POINT('Ctrl Pts',(1.79854421010301,0.862714354240172,6.13409844678299));
#11089=CARTESIAN_POINT('Ctrl Pts',(1.80105219526685,0.857464751667521,6.13372424413561));
#11090=CARTESIAN_POINT('Ctrl Pts',(1.80220781380114,0.855033219496038,6.1335513975929));
#11091=CARTESIAN_POINT('Ctrl Pts',(1.8048076775525,0.849534169211961,6.1331615678815));
#11092=CARTESIAN_POINT('Ctrl Pts',(1.80624902283492,0.846465312659504,6.13294476585074));
#11093=CARTESIAN_POINT('Ctrl Pts',(1.81046795662747,0.837422677624703,6.13230810352624));
#11094=CARTESIAN_POINT('Ctrl Pts',(1.81322381793899,0.831438724117706,6.13188956369581));
#11095=CARTESIAN_POINT('Ctrl Pts',(1.83181961182467,0.790528438261178,6.12904626848214));
#11096=CARTESIAN_POINT('Ctrl Pts',(1.8466803477236,0.755162540750613,6.1266781007164));
#11097=CARTESIAN_POINT('Ctrl Pts',(1.89084654305761,0.640937872351519,6.11924502511665));
#11098=CARTESIAN_POINT('Ctrl Pts',(1.91619033775963,0.560641539955537,6.11433854531592));
#11099=CARTESIAN_POINT('Ctrl Pts',(1.96058035079472,0.381184061292047,6.10360402756647));
#11100=CARTESIAN_POINT('Ctrl Pts',(1.97732676532404,0.281699036557145,6.09779666075204));
#11101=CARTESIAN_POINT('Ctrl Pts',(1.99114965917706,0.130309267377016,6.08876253496379));
#11102=CARTESIAN_POINT('Ctrl Pts',(1.99384125902702,0.0790815978831233,
6.08567371482998));
#11103=CARTESIAN_POINT('Ctrl Pts',(1.99498302481693,-0.00280721763638021,
6.08064711494166));
#11104=CARTESIAN_POINT('Ctrl Pts',(1.99470486916856,-0.0334286616570386,
6.07874777226864));
#11105=CARTESIAN_POINT('Ctrl Pts',(1.99344266254815,-0.0727301800558009,
6.07628010080449));
#11106=CARTESIAN_POINT('Ctrl Pts',(1.99310632073564,-0.0814279947685661,
6.07573210282954));
#11107=CARTESIAN_POINT('Ctrl Pts',(1.99247203792964,-0.0954526117014155,
6.07484535865277));
#11108=CARTESIAN_POINT('Ctrl Pts',(1.99220963197063,-0.100780972377443,
6.07450772827141));
#11109=CARTESIAN_POINT('Ctrl Pts',(1.99166829518422,-0.110943268996255,
6.07386237673639));
#11110=CARTESIAN_POINT('Ctrl Pts',(1.99139313192672,-0.115777374358363,
6.07355477602906));
#11111=CARTESIAN_POINT('Ctrl Pts',(1.99072381174659,-0.126826866884556,
6.07285025763432));
#11112=CARTESIAN_POINT('Ctrl Pts',(1.99031814327962,-0.133041481862757,
6.07245298136447));
#11113=CARTESIAN_POINT('Ctrl Pts',(1.98898144361166,-0.15214237476871,6.07122870810039));
#11114=CARTESIAN_POINT('Ctrl Pts',(1.98795432907092,-0.165021385584337,
6.07039870557162));
#11115=CARTESIAN_POINT('Ctrl Pts',(1.97696042151785,-0.287809682854197,
6.06244099233957));
#11116=CARTESIAN_POINT('Ctrl Pts',(1.95801560505594,-0.396704365877378,
6.05502683770449));
#11117=CARTESIAN_POINT('Ctrl Pts',(1.8867623249582,-0.669876521328289,6.03557328451888));
#11118=CARTESIAN_POINT('Ctrl Pts',(1.82201671894246,-0.829977488385105,
6.02330309043042));
#11119=CARTESIAN_POINT('Ctrl Pts',(1.72839140978783,-0.99601080332654,6.01066247690451));
#11120=CARTESIAN_POINT('Ctrl Pts',(1.7190168608733,-1.01210448053465,6.00943901982118));
#11121=CARTESIAN_POINT('Ctrl Pts',(1.70683388478276,-1.0323617532933,6.00790362057498));
#11122=CARTESIAN_POINT('Ctrl Pts',(1.70423366156926,-1.03664860391784,6.00757896282793));
#11123=CARTESIAN_POINT('Ctrl Pts',(1.70004853827431,-1.04349008966061,6.00706131406208));
#11124=CARTESIAN_POINT('Ctrl Pts',(1.69847399970036,-1.04605098936168,6.00686765633956));
#11125=CARTESIAN_POINT('Ctrl Pts',(1.69546722034032,-1.05091666194025,6.00649993024281));
#11126=CARTESIAN_POINT('Ctrl Pts',(1.69403608376109,-1.05322204334525,6.00632579623812));
#11127=CARTESIAN_POINT('Ctrl Pts',(1.69073469092016,-1.05851603515985,6.00592613158815));
#11128=CARTESIAN_POINT('Ctrl Pts',(1.688861213966,-1.06150261054767,6.00570081641614));
#11129=CARTESIAN_POINT('Ctrl Pts',(1.68287712720233,-1.07098610806003,6.00498579225285));
#11130=CARTESIAN_POINT('Ctrl Pts',(1.67873680853298,-1.07746433871588,6.0044980082182));
#11131=CARTESIAN_POINT('Ctrl Pts',(1.6117139351783,-1.18100879320996,5.99670930202907));
#11132=CARTESIAN_POINT('Ctrl Pts',(1.5405331982177,-1.27246596508619,5.98993339891934));
#11133=CARTESIAN_POINT('Ctrl Pts',(1.39203827205014,-1.43240140596483,5.97724958093508));
#11134=CARTESIAN_POINT('Ctrl Pts',(1.31657262010389,-1.5020585693946,5.97134753588054));
#11135=CARTESIAN_POINT('Ctrl Pts',(1.19402730263821,-1.59881148846721,5.96208572494271));
#11136=CARTESIAN_POINT('Ctrl Pts',(1.15064883809481,-1.63030854400094,5.95886328055533));
#11137=CARTESIAN_POINT('Ctrl Pts',(1.07975006847105,-1.67754781485643,5.95363852429944));
#11138=CARTESIAN_POINT('Ctrl Pts',(1.05303102294477,-1.69444751214884,5.95167866524807));
#11139=CARTESIAN_POINT('Ctrl Pts',(1.01837345362023,-1.71523192659664,5.94914290784695));
#11140=CARTESIAN_POINT('Ctrl Pts',(1.01079429292872,-1.71970926218264,5.94858876091558));
#11141=CARTESIAN_POINT('Ctrl Pts',(0.998555281127256,-1.72683051116412,
5.94769442636926));
#11142=CARTESIAN_POINT('Ctrl Pts',(0.99391392276094,-1.72950610781894,5.94735538930819));
#11143=CARTESIAN_POINT('Ctrl Pts',(0.985060923621533,-1.73456217632846,
5.9467089028518));
#11144=CARTESIAN_POINT('Ctrl Pts',(0.980851284860299,-1.73694609101891,
5.94640158050069));
#11145=CARTESIAN_POINT('Ctrl Pts',(0.971237109139491,-1.74234449418348,
5.94569987388336));
#11146=CARTESIAN_POINT('Ctrl Pts',(0.965827153216209,-1.74534918204492,
5.94530514167649));
#11147=CARTESIAN_POINT('Ctrl Pts',(0.949258326623996,-1.75445087862507,
5.94409653074269));
#11148=CARTESIAN_POINT('Ctrl Pts',(0.938055234607965,-1.76046630770092,
5.94327975810114));
#11149=CARTESIAN_POINT('Ctrl Pts',(0.840544929354676,-1.81162881203009,
5.93617328324466));
#11150=CARTESIAN_POINT('Ctrl Pts',(0.751109280151451,-1.85049841027218,
5.92966293700355));
#11151=CARTESIAN_POINT('Ctrl Pts',(0.525554038086432,-1.92947479610904,
5.91328536835762));
#11152=CARTESIAN_POINT('Ctrl Pts',(0.387310899573127,-1.9619038431194,5.90326336716052));
#11153=CARTESIAN_POINT('Ctrl Pts',(0.206893570312868,-1.98439922626238,
5.89079553690071));
#11154=CARTESIAN_POINT('Ctrl Pts',(0.166838072108192,-1.98816768296259,
5.88806818306347));
#11155=CARTESIAN_POINT('Ctrl Pts',(0.105295543908531,-1.99208437002136,
5.88396548495557));
#11156=CARTESIAN_POINT('Ctrl Pts',(0.0838759409859687,-1.99310115347258,
5.88255381144328));
#11157=CARTESIAN_POINT('Ctrl Pts',(0.0571860680969412,-1.99393705497265,
5.88081840913506));
#11158=CARTESIAN_POINT('Ctrl Pts',(0.0519283722696119,-1.99408090890421,
5.88047768902073));
#11159=CARTESIAN_POINT('Ctrl Pts',(0.0436093249084487,-1.99427559849121,
5.87994045021108));
#11160=CARTESIAN_POINT('Ctrl Pts',(0.0405483666366889,-1.99434018317582,
5.87974317577479));
#11161=CARTESIAN_POINT('Ctrl Pts',(0.0347847264327985,-1.99444851813789,
5.8793724863747));
#11162=CARTESIAN_POINT('Ctrl Pts',(0.0320821370276298,-1.99449382181939,
5.879198989199));
#11163=CARTESIAN_POINT('Ctrl Pts',(0.02588912740067,-1.99458504464769,5.87880214247683));
#11164=CARTESIAN_POINT('Ctrl Pts',(0.0223986785255345,-1.99462729523678,
5.87857900052784));
#11165=CARTESIAN_POINT('Ctrl Pts',(0.0116086709578286,-1.99472957760531,
5.87789077700168));
#11166=CARTESIAN_POINT('Ctrl Pts',(0.00430877727809598,-1.99475870405667,
5.87742739161974));
#11167=CARTESIAN_POINT('Ctrl Pts',(-0.0574059456853493,-1.99466615903818,
5.8735274262474));
#11168=CARTESIAN_POINT('Ctrl Pts',(-0.111800270555511,-1.99235801181298,
5.87020546836019));
#11169=CARTESIAN_POINT('Ctrl Pts',(-0.333123715251099,-1.97387152039378,
5.85691551669195));
#11170=CARTESIAN_POINT('Ctrl Pts',(-0.497789386475864,-1.93890519574217,
5.84750129925474));
#11171=CARTESIAN_POINT('Ctrl Pts',(-0.7046252326072,-1.86685993061634,5.83448494191983));
#11172=CARTESIAN_POINT('Ctrl Pts',(-0.75242932728827,-1.8481104459472,5.83139301507024));
#11173=CARTESIAN_POINT('Ctrl Pts',(-0.82753015280353,-1.81525769025027,
5.82636173799532));
#11174=CARTESIAN_POINT('Ctrl Pts',(-0.855317663129843,-1.8023313156661,
5.82446087641621));
#11175=CARTESIAN_POINT('Ctrl Pts',(-0.890605838408203,-1.78491587097732,
5.82199130850308));
#11176=CARTESIAN_POINT('Ctrl Pts',(-0.898390967220353,-1.78101013248547,
5.82144295189787));
#11177=CARTESIAN_POINT('Ctrl Pts',(-0.910905679881658,-1.77462866537391,
5.82055564037865));
#11178=CARTESIAN_POINT('Ctrl Pts',(-0.915651399804231,-1.77218468866558,
5.82021780205387));
#11179=CARTESIAN_POINT('Ctrl Pts',(-0.924685447948449,-1.76748631018066,
5.81957206063025));
#11180=CARTESIAN_POINT('Ctrl Pts',(-0.928975490992635,-1.76523527349147,
5.81926427807812));
#11181=CARTESIAN_POINT('Ctrl Pts',(-0.938764552515327,-1.76005326826835,
5.81855935272324));
#11182=CARTESIAN_POINT('Ctrl Pts',(-0.944258101465469,-1.75711212748711,
5.81816185118607));
#11183=CARTESIAN_POINT('Ctrl Pts',(-0.961105159534676,-1.74799071293887,
5.81693691282452));
#11184=CARTESIAN_POINT('Ctrl Pts',(-0.972412267543258,-1.7417258765555,
5.81610646916056));
#11185=CARTESIAN_POINT('Ctrl Pts',(-1.07975177043433,-1.68088212742121,
5.80814191946065));
#11186=CARTESIAN_POINT('Ctrl Pts',(-1.17113885925422,-1.6185348036098,5.8007209948428));
#11187=CARTESIAN_POINT('Ctrl Pts',(-1.39056148198761,-1.44048651914965,
5.78124908575034));
#11188=CARTESIAN_POINT('Ctrl Pts',(-1.5096311177695,-1.31517204783432,5.76896716401717));
#11189=CARTESIAN_POINT('Ctrl Pts',(-1.62200127168785,-1.16124036202486,
5.75633143902411));
#11190=CARTESIAN_POINT('Ctrl Pts',(-1.63266265342924,-1.14620243575778,
5.7551207358907));
#11191=CARTESIAN_POINT('Ctrl Pts',(-1.64594760561904,-1.12690239535459,
5.7535989366099));
#11192=CARTESIAN_POINT('Ctrl Pts',(-1.64876526123938,-1.12277586531809,
5.75327539657764));
#11193=CARTESIAN_POINT('Ctrl Pts',(-1.65325141030606,-1.11615247799598,
5.75275907754486));
#11194=CARTESIAN_POINT('Ctrl Pts',(-1.65492979963592,-1.11366239874826,
5.75256563814905));
#11195=CARTESIAN_POINT('Ctrl Pts',(-1.65811370318259,-1.10891562747181,
5.75219818172789));
#11196=CARTESIAN_POINT('Ctrl Pts',(-1.65962021823812,-1.10665968248471,
5.75202409980606));
#11197=CARTESIAN_POINT('Ctrl Pts',(-1.66307633079417,-1.10146136498175,
5.75162423141542));
#11198=CARTESIAN_POINT('Ctrl Pts',(-1.66502272186826,-1.09851688959549,
5.75139866201532));
#11199=CARTESIAN_POINT('Ctrl Pts',(-1.67021088471961,-1.09062283577806,
5.75079635040621));
#11200=CARTESIAN_POINT('Ctrl Pts',(-1.67343849847667,-1.08566392741619,
5.75042053910547));
#11201=CARTESIAN_POINT('Ctrl Pts',(-1.69643246002242,-1.04998980684191,
5.74773465461568));
#11202=CARTESIAN_POINT('Ctrl Pts',(-1.71537543318536,-1.01874884927788,
5.74547618279619));
#11203=CARTESIAN_POINT('Ctrl Pts',(-1.73957576146082,-0.97624635636358,
5.74250236399689));
#11204=CARTESIAN_POINT('Ctrl Pts',(-1.74560028333231,-0.965432774010427,
5.74175409617249));
#11205=CARTESIAN_POINT('Ctrl Pts',(-1.75892721409724,-0.940979256898706,
5.74007907521559));
#11206=CARTESIAN_POINT('Ctrl Pts',(-1.76617242179207,-0.927308957514271,
5.73915448839903));
#11207=CARTESIAN_POINT('Ctrl Pts',(-1.82286021482552,-0.817275045846243,
5.73179549247975));
#11208=CARTESIAN_POINT('Ctrl Pts',(-1.86454090950103,-0.717110462915257,
5.72559352667216));
#11209=CARTESIAN_POINT('Ctrl Pts',(-1.9364905485362,-0.494732056815316,
5.7119848237207));
#11210=CARTESIAN_POINT('Ctrl Pts',(-1.96375246862011,-0.37205501291752,
5.70456309050233));
#11211=CARTESIAN_POINT('Ctrl Pts',(-1.98093268101575,-0.234738892788047,
5.69592602231359));
#11212=CARTESIAN_POINT('Ctrl Pts',(-1.98242070417028,-0.221821489984438,
5.69511063144308));
#11213=CARTESIAN_POINT('Ctrl Pts',(-1.98443584273738,-0.202684227298421,
5.69389799127785));
#11214=CARTESIAN_POINT('Ctrl Pts',(-1.98506024343091,-0.196474778144652,
5.69350380762331));
#11215=CARTESIAN_POINT('Ctrl Pts',(-1.98611713431289,-0.185444645870438,
5.69280228346871));
#11216=CARTESIAN_POINT('Ctrl Pts',(-1.9865612396156,-0.180625104769318,
5.69249531120944));
#11217=CARTESIAN_POINT('Ctrl Pts',(-1.98745671334991,-0.170504202616952,
5.69184972126438));
#11218=CARTESIAN_POINT('Ctrl Pts',(-1.98790441989601,-0.165202563546381,
5.69151099085031));
#11219=CARTESIAN_POINT('Ctrl Pts',(-1.98902458286963,-0.151273449951201,
5.69061955969116));
#11220=CARTESIAN_POINT('Ctrl Pts',(-1.98966211143803,-0.142643353541211,
5.69006576557676));
#11221=CARTESIAN_POINT('Ctrl Pts',(-1.99226996191,-0.103912833767429,5.68757354836504));
#11222=CARTESIAN_POINT('Ctrl Pts',(-1.99361342319119,-0.0737755451558504,
5.68561558193784));
#11223=CARTESIAN_POINT('Ctrl Pts',(-1.99537187113631,0.00661805718719807,
5.68033950854938));
#11224=CARTESIAN_POINT('Ctrl Pts',(-1.99457189737183,0.0568764910081049,
5.67698549523901));
#11225=CARTESIAN_POINT('Ctrl Pts',(-1.9865115335522,0.20685853291375,5.66681389434118));
#11226=CARTESIAN_POINT('Ctrl Pts',(-1.97365340446702,0.306116713493541,
5.65985890814608));
#11227=CARTESIAN_POINT('Ctrl Pts',(-1.92840220335123,0.524923220974854,
5.64426807745429));
#11228=CARTESIAN_POINT('Ctrl Pts',(-1.89221036520727,0.643293764795097,
5.63565180152835));
#11229=CARTESIAN_POINT('Ctrl Pts',(-1.84242786372121,0.76455489259417,5.62709355044145));
#11230=CARTESIAN_POINT('Ctrl Pts',(-1.83951949558784,0.771526180106602,
5.62660257780486));
#11231=CARTESIAN_POINT('Ctrl Pts',(-1.83520622005182,0.781701945461527,
5.62588762401942));
#11232=CARTESIAN_POINT('Ctrl Pts',(-1.83383241346844,0.784919410784791,
5.62566181379824));
#11233=CARTESIAN_POINT('Ctrl Pts',(-1.83138003864552,0.790621307558209,
5.62526210580802));
#11234=CARTESIAN_POINT('Ctrl Pts',(-1.83030486868632,0.793107171775505,
5.62508800300706));
#11235=CARTESIAN_POINT('Ctrl Pts',(-1.82802060912128,0.798359147287296,
5.62472051122588));
#11236=CARTESIAN_POINT('Ctrl Pts',(-1.8268103061763,0.801124697518659,5.62452719827139));
#11237=CARTESIAN_POINT('Ctrl Pts',(-1.82355024617195,0.808528152580744,
5.62401019855294));
#11238=CARTESIAN_POINT('Ctrl Pts',(-1.82148905811442,0.813161045769863,
5.62368720496686));
#11239=CARTESIAN_POINT('Ctrl Pts',(-1.81152010643198,0.835339965892331,
5.6221432648916));
#11240=CARTESIAN_POINT('Ctrl Pts',(-1.80337602822225,0.852779527207339,
5.62093622002811));
#11241=CARTESIAN_POINT('Ctrl Pts',(-1.77994018711997,0.901126743211738,
5.6176020687051));
#11242=CARTESIAN_POINT('Ctrl Pts',(-1.7640970070584,0.931760976963422,5.61550343545838));
#11243=CARTESIAN_POINT('Ctrl Pts',(-1.70343175402551,1.04196234640266,5.60795017858878));
#11244=CARTESIAN_POINT('Ctrl Pts',(-1.65395328902846,1.11884138760937,5.60266975725423));
#11245=CARTESIAN_POINT('Ctrl Pts',(-1.50577979388946,1.3176440410781,5.58829082130289));
#11246=CARTESIAN_POINT('Ctrl Pts',(-1.39773334261183,1.43174396083351,5.57916958180672));
#11247=CARTESIAN_POINT('Ctrl Pts',(-1.26781432937435,1.54007540644937,5.56860584625756));
#11248=CARTESIAN_POINT('Ctrl Pts',(-1.2580887150382,1.54803042763973,5.56781760471203));
#11249=CARTESIAN_POINT('Ctrl Pts',(-1.24348388755124,1.55974784225511,5.56663736881999));
#11250=CARTESIAN_POINT('Ctrl Pts',(-1.23866121644361,1.56358047426879,5.56624819599186));
#11251=CARTESIAN_POINT('Ctrl Pts',(-1.23002062631253,1.57038218682327,5.5655518760555));
#11252=CARTESIAN_POINT('Ctrl Pts',(-1.22620949982333,1.57335984940326,5.56524507391428));
#11253=CARTESIAN_POINT('Ctrl Pts',(-1.21813833384278,1.57961877573058,5.56459599596803));
#11254=CARTESIAN_POINT('Ctrl Pts',(-1.21387578636663,1.58289672795081,5.5642535925637));
#11255=CARTESIAN_POINT('Ctrl Pts',(-1.20253516152739,1.59154506310076,5.56334361166134));
#11256=CARTESIAN_POINT('Ctrl Pts',(-1.19543443150329,1.59688541177246,5.56277486167977));
#11257=CARTESIAN_POINT('Ctrl Pts',(-1.16224158948563,1.62150377362716,5.56012068537297));
#11258=CARTESIAN_POINT('Ctrl Pts',(-1.13571862007832,1.64018993119354,5.55801252110072));
#11259=CARTESIAN_POINT('Ctrl Pts',(-1.06256816321573,1.68910128390786,5.55222805203436));
#11260=CARTESIAN_POINT('Ctrl Pts',(-1.01511720125407,1.71803677821077,5.54850685440975));
#11261=CARTESIAN_POINT('Ctrl Pts',(-0.875385112120838,1.79543397851492,
5.53764413397983));
#11262=CARTESIAN_POINT('Ctrl Pts',(-0.780437447968371,1.83869422144671,
5.5303680973131));
#11263=CARTESIAN_POINT('Ctrl Pts',(-0.611572399718526,1.90018774754922,
5.51783870096188));
#11264=CARTESIAN_POINT('Ctrl Pts',(-0.539173674083609,1.92198531499819,
5.51259214251872));
#11265=CARTESIAN_POINT('Ctrl Pts',(-0.429794959507707,1.94824741977908,
5.50499226884686));
#11266=CARTESIAN_POINT('Ctrl Pts',(-0.393645728192932,1.95587197569543,
5.50253269657453));
#11267=CARTESIAN_POINT('Ctrl Pts',(-0.351452381912605,1.96355395879441,
5.49973784430294));
#11268=CARTESIAN_POINT('Ctrl Pts',(-0.345597025245524,1.96459299198573,
5.49935167914772));
#11269=CARTESIAN_POINT('Ctrl Pts',(-0.336245698468212,1.96620928342696,
5.49873773953017));
#11270=CARTESIAN_POINT('Ctrl Pts',(-0.332752741792645,1.96680342924189,
5.49850903711937));
#11271=CARTESIAN_POINT('Ctrl Pts',(-0.326573498945125,1.96783757503372,
5.49810556661486));
#11272=CARTESIAN_POINT('Ctrl Pts',(-0.323887882895573,1.96828138526332,
5.49793058443278));
#11273=CARTESIAN_POINT('Ctrl Pts',(-0.318225880966407,1.96920515438684,
5.49756246719589));
#11274=CARTESIAN_POINT('Ctrl Pts',(-0.315249324177963,1.96968386176064,
5.49736940377541));
#11275=CARTESIAN_POINT('Ctrl Pts',(-0.307321234758452,1.97094047186723,
5.49685637041444));
#11276=CARTESIAN_POINT('Ctrl Pts',(-0.302367795855993,1.97170646961303,
5.49653706724388));
#11277=CARTESIAN_POINT('Ctrl Pts',(-0.27917130355343,1.97520409404567,5.49504736914465));
#11278=CARTESIAN_POINT('Ctrl Pts',(-0.260893088809021,1.97770136387354,
5.49388963222285));
#11279=CARTESIAN_POINT('Ctrl Pts',(-0.0705787679143973,2.00101860196148,
5.48197768228276));
#11280=CARTESIAN_POINT('Ctrl Pts',(0.10346290506844,1.99959272592379,5.47224164547537));
#11281=CARTESIAN_POINT('Ctrl Pts',(0.382160446189852,1.96077901704428,5.4557602292599));
#11282=CARTESIAN_POINT('Ctrl Pts',(0.487768397941316,1.93720882792712,5.44930870388769));
#11283=CARTESIAN_POINT('Ctrl Pts',(0.603264906900256,1.90138515958882,5.44175975933388));
#11284=CARTESIAN_POINT('Ctrl Pts',(0.615551939787139,1.89744298201715,5.44095043083739));
#11285=CARTESIAN_POINT('Ctrl Pts',(0.633717973541987,1.89141956481533,5.43974423864212));
#11286=CARTESIAN_POINT('Ctrl Pts',(0.639627023229914,1.88942946676524,5.43935036908409));
#11287=CARTESIAN_POINT('Ctrl Pts',(0.65011984886831,1.88584074369298,5.43864821945197));
#11288=CARTESIAN_POINT('Ctrl Pts',(0.654707322726424,1.88425302158516,5.43834030120745));
#11289=CARTESIAN_POINT('Ctrl Pts',(0.664343589367101,1.88087847579217,5.43769150455605));
#11290=CARTESIAN_POINT('Ctrl Pts',(0.669391066148478,1.87908803547684,5.43735050840611));
#11291=CARTESIAN_POINT('Ctrl Pts',(0.682669996322445,1.87431744287109,5.43645033017658));
#11292=CARTESIAN_POINT('Ctrl Pts',(0.690889076515815,1.87130341752442,5.43589002667382));
#11293=CARTESIAN_POINT('Ctrl Pts',(0.728088131141798,1.85738364583677,5.43333966573404));
#11294=CARTESIAN_POINT('Ctrl Pts',(0.756830266421681,1.8458586358357,5.4313290387166));
#11295=CARTESIAN_POINT('Ctrl Pts',(0.833110702010663,1.81319061908548,5.42588104560036));
#11296=CARTESIAN_POINT('Ctrl Pts',(0.880106935472394,1.79085026163924,5.42240501771151));
#11297=CARTESIAN_POINT('Ctrl Pts',(1.01590787719392,1.71965811697747,5.41200705733227));
#11298=CARTESIAN_POINT('Ctrl Pts',(1.10192098641263,1.66585104109242,5.40494875447953));
#11299=CARTESIAN_POINT('Ctrl Pts',(1.27978105537475,1.53476486151793,5.38953352226989));
#11300=CARTESIAN_POINT('Ctrl Pts',(1.36952528585145,1.45524925078667,5.38120156160177));
#11301=CARTESIAN_POINT('Ctrl Pts',(1.4563208046089,1.36315974014363,5.37293880354485));
#11302=CARTESIAN_POINT('Ctrl Pts',(1.46100720748692,1.35813574655702,5.37249201682164));
#11303=CARTESIAN_POINT('Ctrl Pts',(1.46801666512753,1.35054308544168,5.37182291036847));
#11304=CARTESIAN_POINT('Ctrl Pts',(1.47035908023618,1.34799248155751,5.37159916502835));
#11305=CARTESIAN_POINT('Ctrl Pts',(1.47440298705309,1.34356607864765,5.3712126653243));
#11306=CARTESIAN_POINT('Ctrl Pts',(1.47610756099954,1.34169312603902,5.37104967820269));
#11307=CARTESIAN_POINT('Ctrl Pts',(1.47965736587697,1.33777771639469,5.37071011568917));
#11308=CARTESIAN_POINT('Ctrl Pts',(1.48150191182836,1.33573471326586,5.37053359575939));
#11309=CARTESIAN_POINT('Ctrl Pts',(1.48594598782051,1.33079196323776,5.37010810759617));
#11310=CARTESIAN_POINT('Ctrl Pts',(1.48854125963519,1.32788841667238,5.36985946312305));
#11311=CARTESIAN_POINT('Ctrl Pts',(1.49755825512467,1.31774069925689,5.36899491600126));
#11312=CARTESIAN_POINT('Ctrl Pts',(1.50393586374513,1.31045725029181,5.36838226164647));
#11313=CARTESIAN_POINT('Ctrl Pts',(1.58871287782516,1.21220488086934,5.36021786304469));
#11314=CARTESIAN_POINT('Ctrl Pts',(1.65880757784344,1.11436793531017,5.35322296340594));
#11315=CARTESIAN_POINT('Ctrl Pts',(1.80218643627317,0.870437635295791,5.33681810773762));
#11316=CARTESIAN_POINT('Ctrl Pts',(1.86718634175054,0.720517499326425,5.3274514031093));
#11317=CARTESIAN_POINT('Ctrl Pts',(1.91918146435512,0.544251907777537,5.31608306181147));
#11318=CARTESIAN_POINT('Ctrl Pts',(1.92479874774447,0.524039464253312,5.31477555087322));
#11319=CARTESIAN_POINT('Ctrl Pts',(1.93206145943059,0.496212303706111,5.31296865518706));
#11320=CARTESIAN_POINT('Ctrl Pts',(1.93398275399293,0.488670479801494,5.31247826591798));
#11321=CARTESIAN_POINT('Ctrl Pts',(1.93696840268202,0.476657208407773,5.31169598204464));
#11322=CARTESIAN_POINT('Ctrl Pts',(1.93806153561012,0.47219293823856,5.31140502477862));
#11323=CARTESIAN_POINT('Ctrl Pts',(1.94026996437983,0.463037021388265,5.31080775817177));
#11324=CARTESIAN_POINT('Ctrl Pts',(1.94138369444478,0.458345031737235,5.31050140023966));
#11325=CARTESIAN_POINT('Ctrl Pts',(1.94391282647574,0.447515539170537,5.30979362066193));
#11326=CARTESIAN_POINT('Ctrl Pts',(1.9453161887259,0.441375304135935,5.30939181219178));
#11327=CARTESIAN_POINT('Ctrl Pts',(1.94961948984479,0.422127498653317,5.30813062931188));
#11328=CARTESIAN_POINT('Ctrl Pts',(1.95241615617427,0.408997455557157,5.30726793375808));
#11329=CARTESIAN_POINT('Ctrl Pts',(1.97852886095199,0.280025220012113,5.29876928998424));
#11330=CARTESIAN_POINT('Ctrl Pts',(1.9916362901664,0.162377204889784,5.29080067566583));
#11331=CARTESIAN_POINT('Ctrl Pts',(1.99800674982891,-0.124534297934065,
5.27095624988362));
#11332=CARTESIAN_POINT('Ctrl Pts',(1.98030586717885,-0.293141627222418,
5.25892010931736));
#11333=CARTESIAN_POINT('Ctrl Pts',(1.93840789848359,-0.470949176563014,
5.24687145907564));
#11334=CARTESIAN_POINT('Ctrl Pts',(1.93510062495414,-0.484359272753008,
5.24596728793283));
#11335=CARTESIAN_POINT('Ctrl Pts',(1.93051728763558,-0.502146717549188,
5.24477499731521));
#11336=CARTESIAN_POINT('Ctrl Pts',(1.92936522179259,-0.506555195162452,
5.24448007376748));
#11337=CARTESIAN_POINT('Ctrl Pts',(1.9274611372099,-0.513740599195335,5.24400036109387));
#11338=CARTESIAN_POINT('Ctrl Pts',(1.92671820698699,-0.516519883296295,
5.24381505114184));
#11339=CARTESIAN_POINT('Ctrl Pts',(1.92527391553418,-0.521876467056921,
5.24345837663292));
#11340=CARTESIAN_POINT('Ctrl Pts',(1.92457338752335,-0.524453975952867,
5.24328696443752));
#11341=CARTESIAN_POINT('Ctrl Pts',(1.92292667021037,-0.530465143650162,
5.2428876873275));
#11342=CARTESIAN_POINT('Ctrl Pts',(1.92197645257756,-0.533897709164933,
5.24266005640868));
#11343=CARTESIAN_POINT('Ctrl Pts',(1.91888779659482,-0.544940058709323,
5.24192891573797));
#11344=CARTESIAN_POINT('Ctrl Pts',(1.9167132845712,-0.552539802410515,5.24142745428522));
#11345=CARTESIAN_POINT('Ctrl Pts',(1.91151335971188,-0.570312969131404,
5.24025834960125));
#11346=CARTESIAN_POINT('Ctrl Pts',(1.90845178423322,-0.580475671742746,
5.23959266082213));
#11347=CARTESIAN_POINT('Ctrl Pts',(1.87068735171775,-0.702303050702932,
5.2316410010785));
#11348=CARTESIAN_POINT('Ctrl Pts',(1.82630652852721,-0.810748357969191,
5.22484274320764));
#11349=CARTESIAN_POINT('Ctrl Pts',(1.70020098125594,-1.05514084716902,5.20888758195758));
#11350=CARTESIAN_POINT('Ctrl Pts',(1.61130655733755,-1.18646086427432,5.19975982712934));
#11351=CARTESIAN_POINT('Ctrl Pts',(1.49392963985225,-1.32198872595641,5.18866484035132));
#11352=CARTESIAN_POINT('Ctrl Pts',(1.47974913353996,-1.33784244504943,5.18733865547572));
#11353=CARTESIAN_POINT('Ctrl Pts',(1.45996548697671,-1.35926103996997,5.18550606602541));
#11354=CARTESIAN_POINT('Ctrl Pts',(1.45457845909306,-1.36502428601496,5.18500879675367));
#11355=CARTESIAN_POINT('Ctrl Pts',(1.44595760576161,-1.37413821996671,5.1842156901674));
#11356=CARTESIAN_POINT('Ctrl Pts',(1.44274595093105,-1.37750984232699,5.18392080436705));
#11357=CARTESIAN_POINT('Ctrl Pts',(1.43614150503355,-1.38439481166425,5.18331557104669));
#11358=CARTESIAN_POINT('Ctrl Pts',(1.43274755925192,-1.38790700257863,5.18300517469529));
#11359=CARTESIAN_POINT('Ctrl Pts',(1.42489262242761,-1.39597608959126,5.18228820973392));
#11360=CARTESIAN_POINT('Ctrl Pts',(1.42042262837544,-1.4005241102549,5.18188125028765));
#11361=CARTESIAN_POINT('Ctrl Pts',(1.40636206078448,-1.41469355945827,5.18060432756427));
#11362=CARTESIAN_POINT('Ctrl Pts',(1.39669511952127,-1.42423833721886,5.17973101045326));
#11363=CARTESIAN_POINT('Ctrl Pts',(1.30073769388706,-1.51706663215664,5.17110534393398));
#11364=CARTESIAN_POINT('Ctrl Pts',(1.20721596881097,-1.5924917593615,5.16301494691285));
#11365=CARTESIAN_POINT('Ctrl Pts',(1.03649139783089,-1.70645929303209,5.14882714055206));
#11366=CARTESIAN_POINT('Ctrl Pts',(0.962508099534142,-1.7492556571168,5.14284667789002));
#11367=CARTESIAN_POINT('Ctrl Pts',(0.806752962026177,-1.82647295016002,
5.13078516638235));
#11368=CARTESIAN_POINT('Ctrl Pts',(0.724955751690994,-1.86045610765889,
5.12472186470645));
#11369=CARTESIAN_POINT('Ctrl Pts',(0.633851438582407,-1.89138032493641,
5.11843943049738));
#11370=CARTESIAN_POINT('Ctrl Pts',(0.626525452757398,-1.89381969613309,
5.11793748685206));
#11371=CARTESIAN_POINT('Ctrl Pts',(0.615744047215548,-1.89734022675981,
5.11720374107812));
#11372=CARTESIAN_POINT('Ctrl Pts',(0.612299663329723,-1.89845457953319,
5.11697006703781));
#11373=CARTESIAN_POINT('Ctrl Pts',(0.606254466106184,-1.90039220333834,
5.11656126657632));
#11374=CARTESIAN_POINT('Ctrl Pts',(0.603655021873108,-1.90121950833504,
5.11638591013217));
#11375=CARTESIAN_POINT('Ctrl Pts',(0.601037949391743,-1.90204651524843,
5.11620979154589));
#11376=CARTESIAN_POINT('Ctrl Pts',(0.601022058580757,-1.9020515365986,5.1162087221732));
#11377=CARTESIAN_POINT('Ctrl Pts',(0.600990694950365,-1.90206144678514,
5.11620661158774));
#11378=CARTESIAN_POINT('Ctrl Pts',(0.60097522218867,-1.90206633561466,5.11620557037802));
#11379=CARTESIAN_POINT('Ctrl Pts',(0.600944682111629,-1.90207598475756,
5.11620351527187));
#11380=CARTESIAN_POINT('Ctrl Pts',(0.600929614755258,-1.90208074509464,
5.11620250137189));
#11381=CARTESIAN_POINT('Ctrl Pts',(0.600899873110135,-1.90209014119548,
5.11620050004993));
#11382=CARTESIAN_POINT('Ctrl Pts',(0.600885198870916,-1.90209477695374,
5.11619951263054));
#11383=CARTESIAN_POINT('Ctrl Pts',(0.60085623164982,-1.90210392765807,5.11619756347288));
#11384=CARTESIAN_POINT('Ctrl Pts',(0.600841938685225,-1.90210844260827,
5.11619660173507));
#11385=CARTESIAN_POINT('Ctrl Pts',(0.600813722868489,-1.90211735524549,
5.1161947031886));
#11386=CARTESIAN_POINT('Ctrl Pts',(0.60079979989473,-1.90212175297998,5.1161937663711));
#11387=CARTESIAN_POINT('Ctrl Pts',(0.600772312851441,-1.90213043475296,
5.11619191690914));
#11388=CARTESIAN_POINT('Ctrl Pts',(0.600758748826103,-1.90213471878604,
5.11619100426704));
#11389=CARTESIAN_POINT('Ctrl Pts',(0.600731969096899,-1.90214317652406,
5.116189202442));
#11390=CARTESIAN_POINT('Ctrl Pts',(0.600718753420697,-1.90214735022836,
5.11618831326034));
#11391=CARTESIAN_POINT('Ctrl Pts',(0.600692660210878,-1.90215559054751,
5.11618655766958));
#11392=CARTESIAN_POINT('Ctrl Pts',(0.600679782674728,-1.90215965717082,
5.11618569125976));
#11393=CARTESIAN_POINT('Ctrl Pts',(0.600654355845628,-1.90216768647689,
5.11618398054502));
#11394=CARTESIAN_POINT('Ctrl Pts',(0.600641806564661,-1.90217164916312,
5.11618313624037));
#11395=CARTESIAN_POINT('Ctrl Pts',(0.600617026788357,-1.90217947360295,
5.11618146909812));
#11396=CARTESIAN_POINT('Ctrl Pts',(0.600604796270744,-1.90218333537046,
5.11618064625853));
#11397=CARTESIAN_POINT('Ctrl Pts',(0.60058064469499,-1.90219096093795,5.11617902141746));
#11398=CARTESIAN_POINT('Ctrl Pts',(0.600568723688315,-1.90219472472817,
5.11617821941899));
#11399=CARTESIAN_POINT('Ctrl Pts',(0.600545182366988,-1.90220215712849,
5.11617663566894));
#11400=CARTESIAN_POINT('Ctrl Pts',(0.600533562023444,-1.90220582575386,
5.11617585391498));
#11401=CARTESIAN_POINT('Ctrl Pts',(0.600510613391981,-1.90221307056931,
5.11617431007164));
#11402=CARTESIAN_POINT('Ctrl Pts',(0.60049928511379,-1.90221664676213,5.11617354798249));
#11403=CARTESIAN_POINT('Ctrl Pts',(0.6004769123105,-1.90222370935077,5.11617204290899));
#11404=CARTESIAN_POINT('Ctrl Pts',(0.600465867800263,-1.9022271957474,5.11617129992523));
#11405=CARTESIAN_POINT('Ctrl Pts',(0.600445699975258,-1.90223356188791,
5.11616994321385));
#11406=CARTESIAN_POINT('Ctrl Pts',(0.600436576677637,-1.90223644166018,
5.11616932948501));
#11407=CARTESIAN_POINT('Ctrl Pts',(0.600418357611893,-1.90224219237026,
5.11616810388953));
#11408=CARTESIAN_POINT('Ctrl Pts',(0.600409282098518,-1.9022450569159,5.11616749338542));
#11409=CARTESIAN_POINT('Ctrl Pts',(0.600391183907054,-1.90225076918808,
5.11616627594166));
#11410=CARTESIAN_POINT('Ctrl Pts',(0.600382162085712,-1.90225361664507,
5.11616566905957));
#11411=CARTESIAN_POINT('Ctrl Pts',(0.600364171034225,-1.90225929481953,
5.11616445884324));
#11412=CARTESIAN_POINT('Ctrl Pts',(0.600355202502612,-1.90226212531738,
5.11616385555593));
#11413=CARTESIAN_POINT('Ctrl Pts',(0.600337317392383,-1.90226776977743,
5.11616265248605));
#11414=CARTESIAN_POINT('Ctrl Pts',(0.600328401643277,-1.90227058347869,
5.11616205275922));
#11415=CARTESIAN_POINT('Ctrl Pts',(0.600310621472889,-1.90227619454529,
5.11616085676806));
#11416=CARTESIAN_POINT('Ctrl Pts',(0.600301757969406,-1.90227899162183,
5.11616026056541));
#11417=CARTESIAN_POINT('Ctrl Pts',(0.600284081898186,-1.90228456956512,
5.11615907159608));
#11418=CARTESIAN_POINT('Ctrl Pts',(0.600275270187719,-1.90228735016216,
5.11615847888701));
#11419=CARTESIAN_POINT('Ctrl Pts',(0.600257697194919,-1.90229289530902,
5.1161572968705));
#11420=CARTESIAN_POINT('Ctrl Pts',(0.60024893679643,-1.90229565958073,5.11615670762247));
#11421=CARTESIAN_POINT('Ctrl Pts',(0.60023146591235,-1.90230117224184,5.11615553249323));
#11422=CARTESIAN_POINT('Ctrl Pts',(0.600222756322408,-1.90230392034941,
5.11615494667221));
#11423=CARTESIAN_POINT('Ctrl Pts',(0.600205386767657,-1.9023094007753,5.11615377837747));
#11424=CARTESIAN_POINT('Ctrl Pts',(0.600196727611904,-1.90231213283914,
5.11615319595811));
#11425=CARTESIAN_POINT('Ctrl Pts',(0.600179458215574,-1.90231758140383,
5.11615203441879));
#11426=CARTESIAN_POINT('Ctrl Pts',(0.600170848970063,-1.90232029759151,
5.1161514553657));
#11427=CARTESIAN_POINT('Ctrl Pts',(0.600153678969677,-1.90232571454005,
5.11615030053019));
#11428=CARTESIAN_POINT('Ctrl Pts',(0.600145119203757,-1.90232841498967,
5.11614972481423));
#11429=CARTESIAN_POINT('Ctrl Pts',(0.600128047579786,-1.90233380064812,
5.11614857661364));
#11430=CARTESIAN_POINT('Ctrl Pts',(0.600119536776585,-1.90233648552493,
5.1161480041999));
#11431=CARTESIAN_POINT('Ctrl Pts',(0.600102562850611,-1.90234184011168,
5.11614686258828));
#11432=CARTESIAN_POINT('Ctrl Pts',(0.600094100646314,-1.90234450953262,
5.11614629345213));
#11433=CARTESIAN_POINT('Ctrl Pts',(0.6000772233725,-1.90234983338188,5.11614515835884));
#11434=CARTESIAN_POINT('Ctrl Pts',(0.600068809326611,-1.90235248748803,
5.11614459247049));
#11435=CARTESIAN_POINT('Ctrl Pts',(0.600052027743847,-1.90235778090719,
5.11614346383058));
#11436=CARTESIAN_POINT('Ctrl Pts',(0.600043661332126,-1.90236041986602,
5.11614290115464));
#11437=CARTESIAN_POINT('Ctrl Pts',(0.600026974885705,-1.90236568303423,
5.1161417789305));
#11438=CARTESIAN_POINT('Ctrl Pts',(0.600018655807818,-1.90236830694254,
5.11614121944661));
#11439=CARTESIAN_POINT('Ctrl Pts',(0.600002063280902,-1.90237354024771,
5.11614010355611));
#11440=CARTESIAN_POINT('Ctrl Pts',(0.599993791007381,-1.90237614927453,
5.11613954722852));
#11441=CARTESIAN_POINT('Ctrl Pts',(0.599977291810429,-1.90238135290666,
5.11613843763172));
#11442=CARTESIAN_POINT('Ctrl Pts',(0.599969065966349,-1.90238394717224,
5.11613788443506));
#11443=CARTESIAN_POINT('Ctrl Pts',(0.599952659172731,-1.90238912142755,
5.11613678106935));
#11444=CARTESIAN_POINT('Ctrl Pts',(0.599944479340818,-1.90239170106549,
5.11613623097543));
#11445=CARTESIAN_POINT('Ctrl Pts',(0.59992816411756,-1.90239684621061,5.11613513378452));
#11446=CARTESIAN_POINT('Ctrl Pts',(0.599920029875086,-1.90239941135615,
5.11613458676476));
#11447=CARTESIAN_POINT('Ctrl Pts',(0.599903805442814,-1.90240452764074,
5.11613349569595));
#11448=CARTESIAN_POINT('Ctrl Pts',(0.599895716395943,-1.90240707842002,
5.11613295172373));
#11449=CARTESIAN_POINT('Ctrl Pts',(0.599879581920754,-1.90241216611084,
5.11613186672067));
#11450=CARTESIAN_POINT('Ctrl Pts',(0.599871537665024,-1.90241470265329,
5.11613132576865));
#11451=CARTESIAN_POINT('Ctrl Pts',(0.599855492353792,-1.90241976200422,
5.11613024677773));
#11452=CARTESIAN_POINT('Ctrl Pts',(0.599847492490544,-1.90242228443741,
5.11612970881897));
#11453=CARTESIAN_POINT('Ctrl Pts',(0.599831519207564,-1.90242732085509,
5.11612863468762));
#11454=CARTESIAN_POINT('Ctrl Pts',(0.59982354691347,-1.90242983448462,5.1161280985906));
#11455=CARTESIAN_POINT('Ctrl Pts',(0.599807709929055,-1.90243482770856,
5.11612703364043));
#11456=CARTESIAN_POINT('Ctrl Pts',(0.599799797274981,-1.90243732242556,
5.11612650156182));
#11457=CARTESIAN_POINT('Ctrl Pts',(0.599784015155897,-1.90244229813457,
5.1161254403166));
#11458=CARTESIAN_POINT('Ctrl Pts',(0.599776145716583,-1.90244477911908,
5.11612491115167));
#11459=CARTESIAN_POINT('Ctrl Pts',(0.599760449674114,-1.90244972747614,
5.11612385570993));
#11460=CARTESIAN_POINT('Ctrl Pts',(0.599752623068072,-1.90245219485019,
5.11612332943289));
#11461=CARTESIAN_POINT('Ctrl Pts',(0.596769037986115,-1.90339276371807,
5.11592270850813));
#11462=CARTESIAN_POINT('Ctrl Pts',(0.593791058305956,-1.9043238897484,5.11572301614141));
#11463=CARTESIAN_POINT('Ctrl Pts',(0.585581761738283,-1.90686956446533,
5.11517401788902));
#11464=CARTESIAN_POINT('Ctrl Pts',(0.580345916025022,-1.90846958450192,
5.11482553044147));
#11465=CARTESIAN_POINT('Ctrl Pts',(0.553245875734745,-1.91662923651127,
5.1130300607523));
#11466=CARTESIAN_POINT('Ctrl Pts',(0.531275809044089,-1.92283508105358,
5.11160219131275));
#11467=CARTESIAN_POINT('Ctrl Pts',(0.4668949383013,-1.93983283296633,5.1074854205176));
#11468=CARTESIAN_POINT('Ctrl Pts',(0.424227876943702,-1.94960855766813,
5.10484156992936));
#11469=CARTESIAN_POINT('Ctrl Pts',(0.255799354590592,-1.98240620660087,
5.09461338342289));
#11470=CARTESIAN_POINT('Ctrl Pts',(0.128266004044852,-1.99472262025498,
5.0873011150277));
#11471=CARTESIAN_POINT('Ctrl Pts',(-0.0970385373153938,-1.99477079400317,
5.07401678910656));
#11472=CARTESIAN_POINT('Ctrl Pts',(-0.194361689752754,-1.98764856573406,
5.06816093898525));
#11473=CARTESIAN_POINT('Ctrl Pts',(-0.303437260793348,-1.97157739253857,
5.06127508079671));
#11474=CARTESIAN_POINT('Ctrl Pts',(-0.316089124841791,-1.96958859644474,
5.06047156146571));
#11475=CARTESIAN_POINT('Ctrl Pts',(-0.334904997509748,-1.96644489316413,
5.05926903272429));
#11476=CARTESIAN_POINT('Ctrl Pts',(-0.341084297102048,-1.96538250120667,
5.0588728979646));
#11477=CARTESIAN_POINT('Ctrl Pts',(-0.352102615806268,-1.96343462075366,
5.05816433847337));
#11478=CARTESIAN_POINT('Ctrl Pts',(-0.356943582300218,-1.96256032783435,
5.05785226520953));
#11479=CARTESIAN_POINT('Ctrl Pts',(-0.367156895998506,-1.96067673441863,
5.05719222777742));
#11480=CARTESIAN_POINT('Ctrl Pts',(-0.372528419594711,-1.95966324117194,
5.05684413480996));
#11481=CARTESIAN_POINT('Ctrl Pts',(-0.386758480432933,-1.95691770747346,
5.0559194023487));
#11482=CARTESIAN_POINT('Ctrl Pts',(-0.395609464360333,-1.95514761165191,
5.05534157407363));
#11483=CARTESIAN_POINT('Ctrl Pts',(-0.436684424850211,-1.94664275471185,
5.05264743723274));
#11484=CARTESIAN_POINT('Ctrl Pts',(-0.468748965751537,-1.93917134262347,
5.05050807205476));
#11485=CARTESIAN_POINT('Ctrl Pts',(-0.555096263771183,-1.91678473440005,
5.04464375120731));
#11486=CARTESIAN_POINT('Ctrl Pts',(-0.608953148288937,-1.90036066774255,
5.04087326678573));
#11487=CARTESIAN_POINT('Ctrl Pts',(-0.830828305511239,-1.82229748065257,
5.02487353074236));
#11488=CARTESIAN_POINT('Ctrl Pts',(-0.990790867277254,-1.74049751837718,
5.01210349646804));
#11489=CARTESIAN_POINT('Ctrl Pts',(-1.13766281679009,-1.63852094212837,
5.));
#11490=CARTESIAN_POINT('',(1.16034898466907,-1.62253437445173,5.));
#11491=CARTESIAN_POINT('Origin',(0.,0.,5.));
#11492=CARTESIAN_POINT('',(-1.99474961218969,0.00124385252382927,5.52095488142951));
#11493=CARTESIAN_POINT('Ctrl Pts',(1.16034898466907,-1.62253437445173,5.00000000000001));
#11494=CARTESIAN_POINT('Ctrl Pts',(1.21844063257987,-1.58099036420922,5.00455858344228));
#11495=CARTESIAN_POINT('Ctrl Pts',(1.2743420855766,-1.53629197585398,5.00911716688455));
#11496=CARTESIAN_POINT('Ctrl Pts',(1.32770815537402,-1.48869695259086,5.01367575032681));
#11497=CARTESIAN_POINT('Ctrl Pts',(1.38306156050821,-1.43932950591443,5.01840409395556));
#11498=CARTESIAN_POINT('Ctrl Pts',(1.43568659918061,-1.38684571252913,5.02313243758431));
#11499=CARTESIAN_POINT('Ctrl Pts',(1.48523547325909,-1.33157919459296,5.02786078121306));
#11500=CARTESIAN_POINT('Ctrl Pts',(1.53297087618727,-1.27833541153662,5.03241606914843));
#11501=CARTESIAN_POINT('Ctrl Pts',(1.57785107762913,-1.22250944870469,5.03697135708381));
#11502=CARTESIAN_POINT('Ctrl Pts',(1.61960376883367,-1.16443599844722,5.04152664501918));
#11503=CARTESIAN_POINT('Ctrl Pts',(1.66135728082582,-1.1063614065635,5.04608202250385));
#11504=CARTESIAN_POINT('Ctrl Pts',(1.6999828936299,-1.04603961018101,5.05063739998851));
#11505=CARTESIAN_POINT('Ctrl Pts',(1.73525066685647,-0.983835700548712,
5.05519277747318));
#11506=CARTESIAN_POINT('Ctrl Pts',(1.77052858039765,-0.921613905828823,
5.05974946473605));
#11507=CARTESIAN_POINT('Ctrl Pts',(1.80244651005969,-0.857509319488621,
5.06430615199893));
#11508=CARTESIAN_POINT('Ctrl Pts',(1.83082032737691,-0.79191192146824,5.0688628392618));
#11509=CARTESIAN_POINT('Ctrl Pts',(1.85920990629121,-0.726278084228345,
5.07342205775507));
#11510=CARTESIAN_POINT('Ctrl Pts',(1.88405127804513,-0.659150205705004,
5.07798127624833));
#11511=CARTESIAN_POINT('Ctrl Pts',(1.90520884064975,-0.590937252176608,
5.0825404947416));
#11512=CARTESIAN_POINT('Ctrl Pts',(1.92639922177238,-0.522618490238898,
5.08710678525904));
#11513=CARTESIAN_POINT('Ctrl Pts',(1.94389425381641,-0.453211730812403,
5.09167307577648));
#11514=CARTESIAN_POINT('Ctrl Pts',(1.95760863540901,-0.383139652179284,
5.09623936629392));
#11515=CARTESIAN_POINT('Ctrl Pts',(1.97133530670789,-0.313004780684608,
5.10080974874718));
#11516=CARTESIAN_POINT('Ctrl Pts',(1.98127451558112,-0.242203854129323,
5.10538013120044));
#11517=CARTESIAN_POINT('Ctrl Pts',(1.98739272978761,-0.171165709437767,
5.10995051365369));
#11518=CARTESIAN_POINT('Ctrl Pts',(1.99352228814312,-0.0999958486486999,
5.114529370328));
#11519=CARTESIAN_POINT('Ctrl Pts',(1.99581669271177,-0.0285883473734132,
5.1191082270023));
#11520=CARTESIAN_POINT('Ctrl Pts',(1.99429447824322,0.0426274154575889,
5.12368708367661));
#11521=CARTESIAN_POINT('Ctrl Pts',(1.9939100714607,0.0606116238725119,5.12484338825665));
#11522=CARTESIAN_POINT('Ctrl Pts',(1.99328252909201,0.0785836332191591,
5.12599969283669));
#11523=CARTESIAN_POINT('Ctrl Pts',(1.99241266991592,0.0965366006161332,
5.12715599741674));
#11524=CARTESIAN_POINT('Ctrl Pts',(1.98909632330557,0.16498246427945,5.13156441992923));
#11525=CARTESIAN_POINT('Ctrl Pts',(1.98224070223774,0.233421908887211,5.13597284244173));
#11526=CARTESIAN_POINT('Ctrl Pts',(1.97184014003056,0.301453188180601,5.14038126495422));
#11527=CARTESIAN_POINT('Ctrl Pts',(1.96145700103407,0.369370500239447,5.14478230239726));
#11528=CARTESIAN_POINT('Ctrl Pts',(1.94754077282591,0.4368805132556,5.14918333984031));
#11529=CARTESIAN_POINT('Ctrl Pts',(1.93013775644399,0.503582966003958,5.15358437728335));
#11530=CARTESIAN_POINT('Ctrl Pts',(1.9127587100587,0.570193546312947,5.1579793529696));
#11531=CARTESIAN_POINT('Ctrl Pts',(1.89190253429834,0.635998292760284,5.16237432865586));
#11532=CARTESIAN_POINT('Ctrl Pts',(1.86766684366622,0.700605540636004,5.16676930434212));
#11533=CARTESIAN_POINT('Ctrl Pts',(1.84344930507931,0.76516439898147,5.17116098827991));
#11534=CARTESIAN_POINT('Ctrl Pts',(1.81585744398091,0.828527069005353,5.1755526722177));
#11535=CARTESIAN_POINT('Ctrl Pts',(1.78503868383535,0.890317055723046,5.1799443561555));
#11536=CARTESIAN_POINT('Ctrl Pts',(1.7542319931214,0.952082843867704,5.18433432019513));
#11537=CARTESIAN_POINT('Ctrl Pts',(1.72020113315709,1.01227672231106,5.18872428423476));
#11538=CARTESIAN_POINT('Ctrl Pts',(1.68314085352376,1.07054398774609,5.19311424827439));
#11539=CARTESIAN_POINT('Ctrl Pts',(1.64608184473292,1.12880925512505,5.19750406177677));
#11540=CARTESIAN_POINT('Ctrl Pts',(1.60599389321954,1.18514761905863,5.20189387527914));
#11541=CARTESIAN_POINT('Ctrl Pts',(1.56311569278322,1.23923238074012,5.20628368878152));
#11542=CARTESIAN_POINT('Ctrl Pts',(1.52019395217665,1.29337206216423,5.21067795986899));
#11543=CARTESIAN_POINT('Ctrl Pts',(1.47447661880384,1.34525317987349,5.21507223095646));
#11544=CARTESIAN_POINT('Ctrl Pts',(1.42624270807061,1.39458212385481,5.21946650204393));
#11545=CARTESIAN_POINT('Ctrl Pts',(1.37798275764808,1.44393769869305,5.22386314543446));
#11546=CARTESIAN_POINT('Ctrl Pts',(1.32720389605377,1.49073801954655,5.22825978882499));
#11547=CARTESIAN_POINT('Ctrl Pts',(1.27421986522253,1.53472841166516,5.23265643221552));
#11548=CARTESIAN_POINT('Ctrl Pts',(1.22114023463785,1.57879817620174,5.23706100852503));
#11549=CARTESIAN_POINT('Ctrl Pts',(1.16584789491828,1.62004759307619,5.24146558483455));
#11550=CARTESIAN_POINT('Ctrl Pts',(1.10868660112007,1.65826462996617,5.24587016114406));
#11551=CARTESIAN_POINT('Ctrl Pts',(1.0721680575412,1.68268028668746,5.2486841057072));
#11552=CARTESIAN_POINT('Ctrl Pts',(1.03488724876347,1.70585917353192,5.25149805027034));
#11553=CARTESIAN_POINT('Ctrl Pts',(0.996938583639457,1.72775606581223,5.25431199483347));
#11554=CARTESIAN_POINT('Ctrl Pts',(0.936781371479421,1.76246758966287,5.25877273303172));
#11555=CARTESIAN_POINT('Ctrl Pts',(0.874692054691213,1.79410108641791,5.26323347122997));
#11556=CARTESIAN_POINT('Ctrl Pts',(0.81101789861186,1.82243725012172,5.26769420942822));
#11557=CARTESIAN_POINT('Ctrl Pts',(0.747439221880839,1.85073092376972,5.27214825875296));
#11558=CARTESIAN_POINT('Ctrl Pts',(0.682280865182101,1.87573688187796,5.27660230807769));
#11559=CARTESIAN_POINT('Ctrl Pts',(0.615915837290236,1.89728101341764,5.28105635740243));
#11560=CARTESIAN_POINT('Ctrl Pts',(0.549629308337894,1.91879966178444,5.28550513831758));
#11561=CARTESIAN_POINT('Ctrl Pts',(0.482139405117496,1.93686446734296,5.28995391923274));
#11562=CARTESIAN_POINT('Ctrl Pts',(0.413838670673521,1.95134956303456,5.2944027001479));
#11563=CARTESIAN_POINT('Ctrl Pts',(0.345581263020212,1.9658254700591,5.29884865896457));
#11564=CARTESIAN_POINT('Ctrl Pts',(0.276514520753651,1.97672607152122,5.30329461778123));
#11565=CARTESIAN_POINT('Ctrl Pts',(0.20704423956589,1.98397586814018,5.3077405765979));
#11566=CARTESIAN_POINT('Ctrl Pts',(0.137594622853645,1.99122350825075,5.31218521292953));
#11567=CARTESIAN_POINT('Ctrl Pts',(0.0677421904907084,1.99482244894574,
5.31662984926117));
#11568=CARTESIAN_POINT('Ctrl Pts',(-0.00210077107298254,1.99474889378611,
5.32107448559281));
#11569=CARTESIAN_POINT('Ctrl Pts',(-0.0719464861410047,1.99467533572662,
5.32551929715076));
#11570=CARTESIAN_POINT('Ctrl Pts',(-0.14178224182859,1.99092899721851,5.32996410870872));
#11571=CARTESIAN_POINT('Ctrl Pts',(-0.211196141989236,1.98353819023201,
5.33440892026668));
#11572=CARTESIAN_POINT('Ctrl Pts',(-0.280681757242118,1.97613974742036,
5.33885832398947));
#11573=CARTESIAN_POINT('Ctrl Pts',(-0.349744160958529,1.96508937225319,
5.34330772771225));
#11574=CARTESIAN_POINT('Ctrl Pts',(-0.417977924856529,1.95046712785236,
5.34775713143504));
#11575=CARTESIAN_POINT('Ctrl Pts',(-0.486250650610277,1.93583653406928,
5.35220907579191));
#11576=CARTESIAN_POINT('Ctrl Pts',(-0.553693323397087,1.91763013788569,
5.35666102014877));
#11577=CARTESIAN_POINT('Ctrl Pts',(-0.619914716242915,1.89597819267139,
5.36111296450564));
#11578=CARTESIAN_POINT('Ctrl Pts',(-0.686249234273024,1.87428925970755,
5.36557251406385));
#11579=CARTESIAN_POINT('Ctrl Pts',(-0.751357852414863,1.84914320335359,
5.37003206362206));
#11580=CARTESIAN_POINT('Ctrl Pts',(-0.814869132399808,1.82071850091166,
5.37449161318027));
#11581=CARTESIAN_POINT('Ctrl Pts',(-0.847987482030452,1.80589626407684,
5.37681707287025));
#11582=CARTESIAN_POINT('Ctrl Pts',(-0.88067189007166,1.79018327490047,5.37914253256023));
#11583=CARTESIAN_POINT('Ctrl Pts',(-0.912872628507629,1.77360963197136,
5.38146799225021));
#11584=CARTESIAN_POINT('Ctrl Pts',(-0.974655985131309,1.74180988633263,
5.38592983729844));
#11585=CARTESIAN_POINT('Ctrl Pts',(-1.03489322914811,1.70671752778341,5.39039168234667));
#11586=CARTESIAN_POINT('Ctrl Pts',(-1.09321210451729,1.66850677464519,5.3948535273949));
#11587=CARTESIAN_POINT('Ctrl Pts',(-1.15144567010817,1.63035191680429,5.39930884558525));
#11588=CARTESIAN_POINT('Ctrl Pts',(-1.20776603278464,1.5890879845105,5.40376416377559));
#11589=CARTESIAN_POINT('Ctrl Pts',(-1.26182512641187,1.54493524552185,5.40821948196593));
#11590=CARTESIAN_POINT('Ctrl Pts',(-1.31582315400275,1.50083238218932,5.41266976735598));
#11591=CARTESIAN_POINT('Ctrl Pts',(-1.36756461026547,1.45384750082595,5.41712005274602));
#11592=CARTESIAN_POINT('Ctrl Pts',(-1.41673151392217,1.40424334784246,5.42157033813607));
#11593=CARTESIAN_POINT('Ctrl Pts',(-1.46586884463928,1.35466903079556,5.4260179467657));
#11594=CARTESIAN_POINT('Ctrl Pts',(-1.51243435264932,1.30247891342531,5.43046555539534));
#11595=CARTESIAN_POINT('Ctrl Pts',(-1.55614533347603,1.24797406367311,5.43491316402498));
#11596=CARTESIAN_POINT('Ctrl Pts',(-1.59984472482338,1.1934836652743,5.43935959342076));
#11597=CARTESIAN_POINT('Ctrl Pts',(-1.64069078681985,1.13668013322742,5.44380602281655));
#11598=CARTESIAN_POINT('Ctrl Pts',(-1.67844085819717,1.07789788386208,5.44825245221233));
#11599=CARTESIAN_POINT('Ctrl Pts',(-1.71619361699196,1.01911144980415,5.45269919814823));
#11600=CARTESIAN_POINT('Ctrl Pts',(-1.75084968610701,0.958346430253622,
5.45714594408413));
#11601=CARTESIAN_POINT('Ctrl Pts',(-1.78221049605736,0.895965016193699,
5.46159269002003));
#11602=CARTESIAN_POINT('Ctrl Pts',(-1.8136051237754,0.833516333457627,5.46604423108148));
#11603=CARTESIAN_POINT('Ctrl Pts',(-1.84169718062978,0.769448213746021,
5.47049577214293));
#11604=CARTESIAN_POINT('Ctrl Pts',(-1.86633515606672,0.704145331397873,
5.47494731320438));
#11605=CARTESIAN_POINT('Ctrl Pts',(-1.89098784905164,0.638803440231542,
5.47940151340352));
#11606=CARTESIAN_POINT('Ctrl Pts',(-1.91218220563635,0.572225782930733,
5.48385571360267));
#11607=CARTESIAN_POINT('Ctrl Pts',(-1.92981663893441,0.504812145844266,
5.48830991380181));
#11608=CARTESIAN_POINT('Ctrl Pts',(-1.94748182379731,0.437280950410659,
5.49277188139692));
#11609=CARTESIAN_POINT('Ctrl Pts',(-1.9615745946863,0.368911342533814,5.49723384899204));
#11610=CARTESIAN_POINT('Ctrl Pts',(-1.97204464136655,0.300112470513115,
5.50169581658715));
#11611=CARTESIAN_POINT('Ctrl Pts',(-1.97746364796756,0.264504077063874,
5.50400520761375));
#11612=CARTESIAN_POINT('Ctrl Pts',(-1.98191304825906,0.22878076537244,5.50631459864035));
#11613=CARTESIAN_POINT('Ctrl Pts',(-1.98539134842953,0.192999368084864,
5.50862398966694));
#11614=CARTESIAN_POINT('Ctrl Pts',(-1.9915820919786,0.12931496950562,5.5127342869097));
#11615=CARTESIAN_POINT('Ctrl Pts',(-1.99470965376256,0.0653246187217622,
5.51684458415246));
#11616=CARTESIAN_POINT('Ctrl Pts',(-1.99474961218935,0.00124385305840679,
5.52095488139522));
#11617=CARTESIAN_POINT('',(-1.99474967239247,0.00114323669999672,6.32095488134804));
#11618=CARTESIAN_POINT('Ctrl Pts',(-1.99474961218969,0.00124385252382661,
5.52095488142951));
#11619=CARTESIAN_POINT('Ctrl Pts',(-1.9947923012447,-0.067216012531803,
5.52534606483161));
#11620=CARTESIAN_POINT('Ctrl Pts',(-1.99130645198071,-0.135821349700975,
5.52973724823371));
#11621=CARTESIAN_POINT('Ctrl Pts',(-1.9842735171274,-0.204171917086737,
5.5341284316358));
#11622=CARTESIAN_POINT('Ctrl Pts',(-1.97725128635011,-0.272418455402859,
5.5385129316885));
#11623=CARTESIAN_POINT('Ctrl Pts',(-1.96669273659649,-0.340410496159951,
5.54289743174119));
#11624=CARTESIAN_POINT('Ctrl Pts',(-1.95263133344811,-0.40774800813326,
5.54728193179388));
#11625=CARTESIAN_POINT('Ctrl Pts',(-1.93858172148399,-0.475029054261563,
5.55166275522572));
#11626=CARTESIAN_POINT('Ctrl Pts',(-1.92103517909631,-0.541656167923529,
5.55604357865757));
#11627=CARTESIAN_POINT('Ctrl Pts',(-1.90007676440551,-0.607236240573879,
5.56042440208941));
#11628=CARTESIAN_POINT('Ctrl Pts',(-1.87912834776242,-0.672785028763785,
5.56480313568372));
#11629=CARTESIAN_POINT('Ctrl Pts',(-1.85477143901977,-0.737287286775999,
5.56918186927803));
#11630=CARTESIAN_POINT('Ctrl Pts',(-1.82714130271717,-0.800363806281255,
5.57356060287234));
#11631=CARTESIAN_POINT('Ctrl Pts',(-1.79951436007353,-0.863433035019276,
5.57793883034602));
#11632=CARTESIAN_POINT('Ctrl Pts',(-1.76861514440305,-0.925076391265085,
5.5823170578197));
#11633=CARTESIAN_POINT('Ctrl Pts',(-1.73462677544328,-0.984935283363958,
5.58669528529339));
#11634=CARTESIAN_POINT('Ctrl Pts',(-1.70060673917722,-1.04484994659657,
5.59107759200579));
#11635=CARTESIAN_POINT('Ctrl Pts',(-1.66349205160161,-1.10297638629838,
5.59545989871818));
#11636=CARTESIAN_POINT('Ctrl Pts',(-1.62351090162258,-1.15898227545232,
5.59984220543058));
#11637=CARTESIAN_POINT('Ctrl Pts',(-1.58351074586159,-1.21501478804552,
5.60422659535384));
#11638=CARTESIAN_POINT('Ctrl Pts',(-1.54064173061988,-1.26892434962013,
5.6086109852771));
#11639=CARTESIAN_POINT('Ctrl Pts',(-1.49517250870967,-1.32041157663012,
5.61299537520035));
#11640=CARTESIAN_POINT('Ctrl Pts',(-1.44962193118818,-1.37199092694133,
5.61738760987457));
#11641=CARTESIAN_POINT('Ctrl Pts',(-1.40146221209025,-1.42113892980289,
5.6217798445488));
#11642=CARTESIAN_POINT('Ctrl Pts',(-1.3509984143541,-1.46759355644289,5.62617207922302));
#11643=CARTESIAN_POINT('Ctrl Pts',(-1.31420229917125,-1.50146634979783,
5.62937471517657));
#11644=CARTESIAN_POINT('Ctrl Pts',(-1.27618192583642,-1.53390795235667,
5.63257735113012));
#11645=CARTESIAN_POINT('Ctrl Pts',(-1.23706539739349,-1.56483122574663,
5.63577998708368));
#11646=CARTESIAN_POINT('Ctrl Pts',(-1.18264856416134,-1.60785003845923,
5.64023532383071));
#11647=CARTESIAN_POINT('Ctrl Pts',(-1.1258777518735,-1.64811182099942,5.64469066057773));
#11648=CARTESIAN_POINT('Ctrl Pts',(-1.06706373825887,-1.6853493824703,5.64914599732476));
#11649=CARTESIAN_POINT('Ctrl Pts',(-1.00833802735375,-1.72253103587825,
5.65359464487847));
#11650=CARTESIAN_POINT('Ctrl Pts',(-0.947575613746329,-1.75669722063681,
5.65804329243219));
#11651=CARTESIAN_POINT('Ctrl Pts',(-0.885119358305062,-1.78762168370537,
5.6624919399859));
#11652=CARTESIAN_POINT('Ctrl Pts',(-0.822736679037341,-1.81850971641728,
5.66693534684015));
#11653=CARTESIAN_POINT('Ctrl Pts',(-0.75866455749729,-1.84616339634459,
5.6713787536944));
#11654=CARTESIAN_POINT('Ctrl Pts',(-0.693272231122471,-1.87040134090373,
5.67582216054865));
#11655=CARTESIAN_POINT('Ctrl Pts',(-0.627921132954196,-1.89462400405234,
5.68026276594735));
#11656=CARTESIAN_POINT('Ctrl Pts',(-0.56125193886616,-1.91543503440923,
5.68470337134605));
#11657=CARTESIAN_POINT('Ctrl Pts',(-0.493654338107925,-1.93270094866413,
5.68914397674475));
#11658=CARTESIAN_POINT('Ctrl Pts',(-0.426076423290402,-1.94996183469671,
5.69358328893935));
#11659=CARTESIAN_POINT('Ctrl Pts',(-0.357571112320087,-1.96367953317274,
5.69802260113395));
#11660=CARTESIAN_POINT('Ctrl Pts',(-0.288542033082598,-1.97377077130161,
5.70246191332854));
#11661=CARTESIAN_POINT('Ctrl Pts',(-0.219509639122772,-1.98386249400383,
5.70690143869544));
#11662=CARTESIAN_POINT('Ctrl Pts',(-0.149953911393263,-1.99032734221718,
5.71134096406233));
#11663=CARTESIAN_POINT('Ctrl Pts',(-0.0802856487958224,-1.9931336576099,
5.71578048942923));
#11664=CARTESIAN_POINT('Ctrl Pts',(-0.0105438244567896,-1.9959429361517,
5.7202247024287));
#11665=CARTESIAN_POINT('Ctrl Pts',(0.0593102821093654,-1.99508595175291,
5.72466891542818));
#11666=CARTESIAN_POINT('Ctrl Pts',(0.128864772078434,-1.99058318917275,
5.72911312842766));
#11667=CARTESIAN_POINT('Ctrl Pts',(0.198459756193018,-1.9860778051152,5.73355992881737));
#11668=CARTESIAN_POINT('Ctrl Pts',(0.267754290470471,-1.977922475244,5.73800672920708));
#11669=CARTESIAN_POINT('Ctrl Pts',(0.336343287961951,-1.96618939961107,
5.74245352959679));
#11670=CARTESIAN_POINT('Ctrl Pts',(0.405051579770993,-1.95443591707176,
5.74690806414266));
#11671=CARTESIAN_POINT('Ctrl Pts',(0.473051408038398,-1.93909237483016,
5.75136259868854));
#11672=CARTESIAN_POINT('Ctrl Pts',(0.539950309985821,-1.92028154843143,
5.75581713323441));
#11673=CARTESIAN_POINT('Ctrl Pts',(0.575587653455228,-1.91026093730329,
5.75819008365642));
#11674=CARTESIAN_POINT('Ctrl Pts',(0.610912875599195,-1.89925723901571,
5.76056303407842));
#11675=CARTESIAN_POINT('Ctrl Pts',(0.645869037961982,-1.88729455790612,
5.76293598450042));
#11676=CARTESIAN_POINT('Ctrl Pts',(0.711495626231272,-1.86483585836044,
5.76739095409096));
#11677=CARTESIAN_POINT('Ctrl Pts',(0.776078710937367,-1.83890579026429,
5.7718459236815));
#11678=CARTESIAN_POINT('Ctrl Pts',(0.839225447637288,-1.80962101295768,
5.77630089327204));
#11679=CARTESIAN_POINT('Ctrl Pts',(0.902277588112757,-1.78038010536647,
5.78074918914791));
#11680=CARTESIAN_POINT('Ctrl Pts',(0.963897210932753,-1.74779466727024,
5.78519748502378));
#11681=CARTESIAN_POINT('Ctrl Pts',(1.02370852762626,-1.71203049416921,5.78964578089965));
#11682=CARTESIAN_POINT('Ctrl Pts',(1.08344971310567,-1.6763082560233,5.79408886096674));
#11683=CARTESIAN_POINT('Ctrl Pts',(1.1413863857378,-1.63741493552949,5.79853194103383));
#11684=CARTESIAN_POINT('Ctrl Pts',(1.19716620747039,-1.59556279543958,5.80297502110093));
#11685=CARTESIAN_POINT('Ctrl Pts',(1.25291105510323,-1.5537368967552,5.80741531534475));
#11686=CARTESIAN_POINT('Ctrl Pts',(1.30650134413439,-1.50895615180086,5.81185560958857));
#11687=CARTESIAN_POINT('Ctrl Pts',(1.35761394400723,-1.46147594627388,5.81629590383239));
#11688=CARTESIAN_POINT('Ctrl Pts',(1.408711843642,-1.41400939629028,5.82073492102549));
#11689=CARTESIAN_POINT('Ctrl Pts',(1.45733311043558,-1.36384525986239,5.82517393821859));
#11690=CARTESIAN_POINT('Ctrl Pts',(1.50318929080677,-1.31127781896281,5.82961295541169));
#11691=CARTESIAN_POINT('Ctrl Pts',(1.54904784572592,-1.25870765598936,5.83405220246823));
#11692=CARTESIAN_POINT('Ctrl Pts',(1.59214071008936,-1.20373431177558,5.83849144952477));
#11693=CARTESIAN_POINT('Ctrl Pts',(1.63221895130854,-1.14668603265639,5.84293069658131));
#11694=CARTESIAN_POINT('Ctrl Pts',(1.67233976145668,-1.08957715995656,5.84737465876473));
#11695=CARTESIAN_POINT('Ctrl Pts',(1.70943927566257,-1.03038935471185,5.85181862094815));
#11696=CARTESIAN_POINT('Ctrl Pts',(1.74331181171396,-0.969480009922113,
5.85626258313157));
#11697=CARTESIAN_POINT('Ctrl Pts',(1.77720418540061,-0.908534993242815,
5.86070914794565));
#11698=CARTESIAN_POINT('Ctrl Pts',(1.80786560417123,-0.845866869904689,
5.86515571275973));
#11699=CARTESIAN_POINT('Ctrl Pts',(1.83513756064359,-0.781855290968285,
5.86960227757381));
#11700=CARTESIAN_POINT('Ctrl Pts',(1.86245711540089,-0.717731991357304,
5.8740566030654));
#11701=CARTESIAN_POINT('Ctrl Pts',(1.88637523117278,-0.652261015143535,
5.87851092855698));
#11702=CARTESIAN_POINT('Ctrl Pts',(1.90678276159614,-0.585838768416548,
5.88296525404856));
#11703=CARTESIAN_POINT('Ctrl Pts',(1.91766648320351,-0.550414529083512,
5.88534083000476));
#11704=CARTESIAN_POINT('Ctrl Pts',(1.92755255690717,-0.514719928244699,
5.88771640596095));
#11705=CARTESIAN_POINT('Ctrl Pts',(1.93643040487919,-0.478816091583604,
5.89009198191715));
#11706=CARTESIAN_POINT('Ctrl Pts',(1.95307244233698,-0.411512281417537,
5.89454513589899));
#11707=CARTESIAN_POINT('Ctrl Pts',(1.96623450191741,-0.343205993838856,
5.89899828988084));
#11708=CARTESIAN_POINT('Ctrl Pts',(1.97580171301588,-0.274290272054082,
5.90345144386268));
#11709=CARTESIAN_POINT('Ctrl Pts',(1.98535451082555,-0.205478373859169,
5.90789788903527));
#11710=CARTESIAN_POINT('Ctrl Pts',(1.99132314210793,-0.136059344847672,
5.91234433420785));
#11711=CARTESIAN_POINT('Ctrl Pts',(1.9936432686362,-0.0664385424402738,
5.91679077938043));
#11712=CARTESIAN_POINT('Ctrl Pts',(1.99596065109929,0.00309991789794359,
5.92123196564356));
#11713=CARTESIAN_POINT('Ctrl Pts',(1.99463808295563,0.0728391905275966,
5.92567315190669));
#11714=CARTESIAN_POINT('Ctrl Pts',(1.98966298447894,0.142368432927878,5.93011433816982));
#11715=CARTESIAN_POINT('Ctrl Pts',(1.98469103545918,0.211853660248919,5.93455271296602));
#11716=CARTESIAN_POINT('Ctrl Pts',(1.97607117780648,0.281128633700857,5.93899108776222));
#11717=CARTESIAN_POINT('Ctrl Pts',(1.9638429012161,0.349783678640308,5.94342946255843));
#11718=CARTESIAN_POINT('Ctrl Pts',(1.95161820583892,0.418418617037978,5.94786653751762));
#11719=CARTESIAN_POINT('Ctrl Pts',(1.93578727518894,0.486433505382848,5.95230361247682));
#11720=CARTESIAN_POINT('Ctrl Pts',(1.91644108088272,0.55342673047576,5.95674068743601));
#11721=CARTESIAN_POINT('Ctrl Pts',(1.89709397134644,0.62042312488517,5.96117797230441));
#11722=CARTESIAN_POINT('Ctrl Pts',(1.87423140617596,0.686397290190647,5.96561525717282));
#11723=CARTESIAN_POINT('Ctrl Pts',(1.84799431799466,0.750962424598896,5.97005254204122));
#11724=CARTESIAN_POINT('Ctrl Pts',(1.82172945025819,0.815595919897694,5.97449452506054));
#11725=CARTESIAN_POINT('Ctrl Pts',(1.79208311290496,0.87881695194219,5.97893650807985));
#11726=CARTESIAN_POINT('Ctrl Pts',(1.75924416903776,0.940259281372236,5.98337849109917));
#11727=CARTESIAN_POINT('Ctrl Pts',(1.72638607747854,1.00173743652206,5.98782306414462));
#11728=CARTESIAN_POINT('Ctrl Pts',(1.69033192755659,1.0614344054251,5.99226763719007));
#11729=CARTESIAN_POINT('Ctrl Pts',(1.65131484610172,1.11901154665359,5.99671221023552));
#11730=CARTESIAN_POINT('Ctrl Pts',(1.61222962352486,1.17668924309682,6.00116454547596));
#11731=CARTESIAN_POINT('Ctrl Pts',(1.57017143564818,1.23223933126419,6.0056168807164));
#11732=CARTESIAN_POINT('Ctrl Pts',(1.52541422963819,1.28535558913373,6.01006921595683));
#11733=CARTESIAN_POINT('Ctrl Pts',(1.50135933304927,1.31390308358541,6.01246213708252));
#11734=CARTESIAN_POINT('Ctrl Pts',(1.47652545867745,1.34174817175601,6.01485505820821));
#11735=CARTESIAN_POINT('Ctrl Pts',(1.4509593153368,1.3688479198718,6.01724797933389));
#11736=CARTESIAN_POINT('Ctrl Pts',(1.40336940591118,1.41929254662303,6.02170226475804));
#11737=CARTESIAN_POINT('Ctrl Pts',(1.35305152644983,1.46735223801887,6.0261565501822));
#11738=CARTESIAN_POINT('Ctrl Pts',(1.30027421093083,1.51271760050851,6.03061083560635));
#11739=CARTESIAN_POINT('Ctrl Pts',(1.24757620065672,1.55801479524185,6.03505842784815));
#11740=CARTESIAN_POINT('Ctrl Pts',(1.1924264574792,1.6006253800914,6.03950602008996));
#11741=CARTESIAN_POINT('Ctrl Pts',(1.13513120857,1.64027580053795,6.04395361233177));
#11742=CARTESIAN_POINT('Ctrl Pts',(1.07790348008118,1.67987949436915,6.04839596324373));
#11743=CARTESIAN_POINT('Ctrl Pts',(1.0185356681765,1.71652967510947,6.0528383141557));
#11744=CARTESIAN_POINT('Ctrl Pts',(0.957366616645845,1.74999334965367,6.05728066506767));
#11745=CARTESIAN_POINT('Ctrl Pts',(0.896236136705961,1.7834359228872,6.0617202147503));
#11746=CARTESIAN_POINT('Ctrl Pts',(0.833307098785434,1.81369574159731,6.06615976443293));
#11747=CARTESIAN_POINT('Ctrl Pts',(0.768945538335652,1.84058423376212,6.07059931411557));
#11748=CARTESIAN_POINT('Ctrl Pts',(0.704602699117713,1.86746490471047,6.07503757243984));
#11749=CARTESIAN_POINT('Ctrl Pts',(0.638828615998939,1.89097600724552,6.07947583076412));
#11750=CARTESIAN_POINT('Ctrl Pts',(0.572010404389035,1.91097662460081,6.0839140890884));
#11751=CARTESIAN_POINT('Ctrl Pts',(0.505188931272009,1.93097821821921,6.08835256405138));
#11752=CARTESIAN_POINT('Ctrl Pts',(0.437323698104091,1.94746884838247,6.09279103901437));
#11753=CARTESIAN_POINT('Ctrl Pts',(0.368816404675191,1.96035762608318,6.09722951397736));
#11754=CARTESIAN_POINT('Ctrl Pts',(0.300236563836182,1.97326005265826,6.10167268916783));
#11755=CARTESIAN_POINT('Ctrl Pts',(0.231013787655493,1.98255292298725,6.10611586435829));
#11756=CARTESIAN_POINT('Ctrl Pts',(0.161558428550818,1.98819678016644,6.11055903954876));
#11757=CARTESIAN_POINT('Ctrl Pts',(0.0920625359450201,1.99384393104815,
6.11500480773492));
#11758=CARTESIAN_POINT('Ctrl Pts',(0.0223342797007121,1.99583781617353,
6.11945057592108));
#11759=CARTESIAN_POINT('Ctrl Pts',(-0.0472152311563271,1.99419113538468,
6.12389634410723));
#11760=CARTESIAN_POINT('Ctrl Pts',(-0.116886046268897,1.99254158254994,
6.12834986634649));
#11761=CARTESIAN_POINT('Ctrl Pts',(-0.186377005639694,1.9872388259532,6.13280338858574));
#11762=CARTESIAN_POINT('Ctrl Pts',(-0.255282160080176,1.97834743693943,
6.137256910825));
#11763=CARTESIAN_POINT('Ctrl Pts',(-0.292142099617515,1.9735911010149,6.13963926613354));
#11764=CARTESIAN_POINT('Ctrl Pts',(-0.32883457540803,1.96780872561293,6.14202162144208));
#11765=CARTESIAN_POINT('Ctrl Pts',(-0.365299029972776,1.96101610936804,
6.14440397675062));
#11766=CARTESIAN_POINT('Ctrl Pts',(-0.433474361558249,1.94831637560385,
6.14885811887486));
#11767=CARTESIAN_POINT('Ctrl Pts',(-0.50112157463356,1.93203206395733,6.15331226099909));
#11768=CARTESIAN_POINT('Ctrl Pts',(-0.567835177170299,1.91222142391198,
6.15776640312333));
#11769=CARTESIAN_POINT('Ctrl Pts',(-0.634448541320298,1.89244054970933,
6.16221385281898));
#11770=CARTESIAN_POINT('Ctrl Pts',(-0.700130613620823,1.86914400129941,
6.16666130251463));
#11771=CARTESIAN_POINT('Ctrl Pts',(-0.764485625150959,1.84244112292294,
6.17110875221028));
#11772=CARTESIAN_POINT('Ctrl Pts',(-0.828764820816398,1.81576970288617,
6.17555096241896));
#11773=CARTESIAN_POINT('Ctrl Pts',(-0.891719610835551,1.78570010983387,
6.17999317262764));
#11774=CARTESIAN_POINT('Ctrl Pts',(-0.952970668561464,1.75239107146821,
6.18443538283632));
#11775=CARTESIAN_POINT('Ctrl Pts',(-1.01418311864234,1.71910302838946,6.18887479303988));
#11776=CARTESIAN_POINT('Ctrl Pts',(-1.07369353773084,1.68257982395457,6.19331420324345));
#11777=CARTESIAN_POINT('Ctrl Pts',(-1.13114522433883,1.64302709775446,6.19775361344701));
#11778=CARTESIAN_POINT('Ctrl Pts',(-1.18858021774735,1.60348586402023,6.20219173373266));
#11779=CARTESIAN_POINT('Ctrl Pts',(-1.24395726316132,1.560917133434,6.2066298540183));
#11780=CARTESIAN_POINT('Ctrl Pts',(-1.29694831277892,1.51557006980209,6.21106797430394));
#11781=CARTESIAN_POINT('Ctrl Pts',(-1.3499419688548,1.47022077569484,6.21550631288637));
#11782=CARTESIAN_POINT('Ctrl Pts',(-1.40054902575009,1.42209319732952,6.21994465146879));
#11783=CARTESIAN_POINT('Ctrl Pts',(-1.44847560118041,1.3714758456805,6.22438299005121));
#11784=CARTESIAN_POINT('Ctrl Pts',(-1.49645296876867,1.32080485021286,6.22882603234534));
#11785=CARTESIAN_POINT('Ctrl Pts',(-1.54174384764662,1.26763917104718,6.23326907463948));
#11786=CARTESIAN_POINT('Ctrl Pts',(-1.58409291328415,1.2123024394032,6.23771211693362));
#11787=CARTESIAN_POINT('Ctrl Pts',(-1.6264667111397,1.15693339063269,6.24215775400261));
#11788=CARTESIAN_POINT('Ctrl Pts',(-1.66589499939298,1.09939116969751,6.2466033910716));
#11789=CARTESIAN_POINT('Ctrl Pts',(-1.70216589599974,1.04002828086327,6.2510490281406));
#11790=CARTESIAN_POINT('Ctrl Pts',(-1.73850009042253,0.980561795438689,
6.25550242347155));
#11791=CARTESIAN_POINT('Ctrl Pts',(-1.77166566112311,0.9192687301121,6.2599558188025));
#11792=CARTESIAN_POINT('Ctrl Pts',(-1.80149713174049,0.856525333443663,
6.26440921413346));
#11793=CARTESIAN_POINT('Ctrl Pts',(-1.81746380226121,0.822943243079948,
6.26679280081142));
#11794=CARTESIAN_POINT('Ctrl Pts',(-1.83247618130686,0.788946008594228,
6.26917638748939));
#11795=CARTESIAN_POINT('Ctrl Pts',(-1.84651473762329,0.75459319254815,6.27155997416736));
#11796=CARTESIAN_POINT('Ctrl Pts',(-1.87590422211887,0.682676142688478,
6.276549973291));
#11797=CARTESIAN_POINT('Ctrl Pts',(-1.90112125185148,0.608959762926832,
6.28153997241463));
#11798=CARTESIAN_POINT('Ctrl Pts',(-1.92196856688165,0.533914216348369,
6.28652997153827));
#11799=CARTESIAN_POINT('Ctrl Pts',(-1.94274065878641,0.459139455746603,
6.29150196530585));
#11800=CARTESIAN_POINT('Ctrl Pts',(-1.95917436280922,0.383045343934298,
6.29647395907343));
#11801=CARTESIAN_POINT('Ctrl Pts',(-1.97112115201587,0.306119203212767,
6.30144595284101));
#11802=CARTESIAN_POINT('Ctrl Pts',(-1.98299656103722,0.229652684075272,
6.30638823972833));
#11803=CARTESIAN_POINT('Ctrl Pts',(-1.99043838878741,0.152364307798669,
6.31133052661565));
#11804=CARTESIAN_POINT('Ctrl Pts',(-1.99334890400618,0.0747509825847146,
6.31627281350298));
#11805=CARTESIAN_POINT('Ctrl Pts',(-1.9942679947044,0.0502420280178952,
6.31783350278466));
#11806=CARTESIAN_POINT('Ctrl Pts',(-1.99473559789568,0.0257007914548224,
6.31939419206635));
#11807=CARTESIAN_POINT('Ctrl Pts',(-1.99474967239247,0.00114323669999672,
6.32095488134804));
#11808=CARTESIAN_POINT('',(-1.99475051923913,-0.000231578174347214,7.92279770353672));
#11809=CARTESIAN_POINT('Ctrl Pts',(-1.99474972256478,0.00105205880370748,
6.31944091739086));
#11810=CARTESIAN_POINT('Ctrl Pts',(-1.99477744461827,-0.0515101728021833,
6.32260645846605));
#11811=CARTESIAN_POINT('Ctrl Pts',(-1.99272763490246,-0.104049755308175,
6.32582344761956));
#11812=CARTESIAN_POINT('Ctrl Pts',(-1.98792329969081,-0.165118817176486,
6.32964937505444));
#11813=CARTESIAN_POINT('Ctrl Pts',(-1.98718416083469,-0.173788309031887,
6.33019453377832));
#11814=CARTESIAN_POINT('Ctrl Pts',(-1.98586247174082,-0.188177734492508,
6.33110285450026));
#11815=CARTESIAN_POINT('Ctrl Pts',(-1.98531186365345,-0.193900539832301,
6.33146501686582));
#11816=CARTESIAN_POINT('Ctrl Pts',(-1.98427511807121,-0.204208415796533,
6.3321190244032));
#11817=CARTESIAN_POINT('Ctrl Pts',(-1.98379780732684,-0.208794349402572,
6.33241059083647));
#11818=CARTESIAN_POINT('Ctrl Pts',(-1.982790989217,-0.218152492191368,6.33300681262577));
#11819=CARTESIAN_POINT('Ctrl Pts',(-1.98226014254585,-0.222924523958921,
6.33331150826404));
#11820=CARTESIAN_POINT('Ctrl Pts',(-1.9810783692691,-0.233209944863012,
6.33396968410619));
#11821=CARTESIAN_POINT('Ctrl Pts',(-1.98042164592977,-0.238722614918188,
6.33432334478309));
#11822=CARTESIAN_POINT('Ctrl Pts',(-1.97858702868945,-0.253593976284769,
6.33527986739594));
#11823=CARTESIAN_POINT('Ctrl Pts',(-1.97736576347493,-0.262947080739622,
6.3358840932835));
#11824=CARTESIAN_POINT('Ctrl Pts',(-1.97128705934792,-0.307061623973,6.33874669531897));
#11825=CARTESIAN_POINT('Ctrl Pts',(-1.96557928455428,-0.341697712851584,
6.34103177104202));
#11826=CARTESIAN_POINT('Ctrl Pts',(-1.95340752322231,-0.405085067763132,
6.3452860522495));
#11827=CARTESIAN_POINT('Ctrl Pts',(-1.94721438490059,-0.433878851796861,
6.34724637621284));
#11828=CARTESIAN_POINT('Ctrl Pts',(-1.89984439107361,-0.632606107181402,
6.36096895098833));
#11829=CARTESIAN_POINT('Ctrl Pts',(-1.8371160572075,-0.796610341711909,
6.37337363602623));
#11830=CARTESIAN_POINT('Ctrl Pts',(-1.72340193659099,-1.00647675563919,
6.38978603019156));
#11831=CARTESIAN_POINT('Ctrl Pts',(-1.69027884995545,-1.06116397510046,
6.39410779554719));
#11832=CARTESIAN_POINT('Ctrl Pts',(-1.65071104264968,-1.1199235205728,6.3987274612763));
#11833=CARTESIAN_POINT('Ctrl Pts',(-1.64680819589923,-1.12565465735264,
6.39917776919579));
#11834=CARTESIAN_POINT('Ctrl Pts',(-1.64093774469943,-1.13417924194797,
6.39984701510508));
#11835=CARTESIAN_POINT('Ctrl Pts',(-1.63899277010808,-1.1369880979177,6.40006744238022));
#11836=CARTESIAN_POINT('Ctrl Pts',(-1.63564679302806,-1.141793799642,6.40044440039165));
#11837=CARTESIAN_POINT('Ctrl Pts',(-1.63424933839479,-1.14379308122026,
6.40060117123368));
#11838=CARTESIAN_POINT('Ctrl Pts',(-1.63133409071118,-1.14794755773208,
6.40092682568418));
#11839=CARTESIAN_POINT('Ctrl Pts',(-1.62981569806856,-1.15010230038321,
6.40109566637637));
#11840=CARTESIAN_POINT('Ctrl Pts',(-1.62560067317879,-1.15605870876959,
6.40156224462036));
#11841=CARTESIAN_POINT('Ctrl Pts',(-1.62289495892478,-1.15985397361839,
6.4018593636531));
#11842=CARTESIAN_POINT('Ctrl Pts',(-1.61217612655929,-1.17477817502841,
6.403027201273));
#11843=CARTESIAN_POINT('Ctrl Pts',(-1.60406140500754,-1.18583416101091,
6.40389117972435));
#11844=CARTESIAN_POINT('Ctrl Pts',(-1.5938215077739,-1.19948814263535,6.40495792865003));
#11845=CARTESIAN_POINT('Ctrl Pts',(-1.59180319962261,-1.20216528687708,
6.4051670745444));
#11846=CARTESIAN_POINT('Ctrl Pts',(-1.47625948307019,-1.35462476567131,
6.4170777417854));
#11847=CARTESIAN_POINT('Ctrl Pts',(-1.34212455588771,-1.48764105505261,
6.42754694131136));
#11848=CARTESIAN_POINT('Ctrl Pts',(-1.1382817295954,-1.63942572172107,6.4424914233546));
#11849=CARTESIAN_POINT('Ctrl Pts',(-1.08330577784576,-1.67626055422912,
6.44643440691091));
#11850=CARTESIAN_POINT('Ctrl Pts',(-1.00592310602849,-1.72270953433397,
6.45194659419272));
#11851=CARTESIAN_POINT('Ctrl Pts',(-0.985018140549544,-1.73474742327056,
6.4534319114796));
#11852=CARTESIAN_POINT('Ctrl Pts',(-0.953627321074768,-1.75207311154907,
6.45565957665956));
#11853=CARTESIAN_POINT('Ctrl Pts',(-0.943304310780017,-1.75765247525431,
6.45639172496357));
#11854=CARTESIAN_POINT('Ctrl Pts',(-0.926732750150575,-1.76642100763935,
6.45756666211685));
#11855=CARTESIAN_POINT('Ctrl Pts',(-0.920515458518767,-1.76966891113723,
6.4580073874649));
#11856=CARTESIAN_POINT('Ctrl Pts',(-0.90865641228606,-1.77578465465829,
6.45884794560778));
#11857=CARTESIAN_POINT('Ctrl Pts',(-0.903017876892885,-1.77865857539385,
6.45924755939515));
#11858=CARTESIAN_POINT('Ctrl Pts',(-0.893087651142748,-1.78366054965695,
6.45995130503853));
#11859=CARTESIAN_POINT('Ctrl Pts',(-0.888801771785937,-1.78580007807172,
6.46025503192961));
#11860=CARTESIAN_POINT('Ctrl Pts',(-0.880410575884844,-1.78995130682423,
6.46084969044561));
#11861=CARTESIAN_POINT('Ctrl Pts',(-0.87630596547766,-1.79196437387208,
6.46114057199418));
#11862=CARTESIAN_POINT('Ctrl Pts',(-0.865417544050263,-1.79725813951197,
6.46191222343387));
#11863=CARTESIAN_POINT('Ctrl Pts',(-0.858622051765832,-1.80051451402988,
6.46239383521247));
#11864=CARTESIAN_POINT('Ctrl Pts',(-0.834466616022044,-1.81192186209441,
6.46410597416705));
#11865=CARTESIAN_POINT('Ctrl Pts',(-0.817008205454793,-1.81986068617312,
6.46534378488314));
#11866=CARTESIAN_POINT('Ctrl Pts',(-0.629741323994729,-1.90177836965273,
6.47862903756359));
#11867=CARTESIAN_POINT('Ctrl Pts',(-0.450563654349494,-1.95199815661323,
6.49153662801257));
#11868=CARTESIAN_POINT('Ctrl Pts',(-0.168979054343724,-1.99004403633932,
6.51132612211482));
#11869=CARTESIAN_POINT('Ctrl Pts',(-0.070003666522376,-1.99597935232476,
6.51816336057112));
#11870=CARTESIAN_POINT('Ctrl Pts',(0.0386265208164566,-1.99439915239692,
6.52528083487543));
#11871=CARTESIAN_POINT('Ctrl Pts',(0.0482383789861798,-1.99418982420783,
6.52590722540753));
#11872=CARTESIAN_POINT('Ctrl Pts',(0.0617504707858433,-1.99379780304654,
6.52678268373903));
#11873=CARTESIAN_POINT('Ctrl Pts',(0.065652062648478,-1.99367314456987,
6.52703487209125));
#11874=CARTESIAN_POINT('Ctrl Pts',(0.07231851905358,-1.99344055592961,6.52746472190555));
#11875=CARTESIAN_POINT('Ctrl Pts',(0.0750835592791098,-1.99333832494506,
6.52764270090586));
#11876=CARTESIAN_POINT('Ctrl Pts',(0.0803838822548329,-1.99313131338395,
6.52798326590869));
#11877=CARTESIAN_POINT('Ctrl Pts',(0.0829191791686259,-1.99302744858703,
6.52814590389593));
#11878=CARTESIAN_POINT('Ctrl Pts',(0.0889351559742316,-1.99276948974236,
6.52853121365268));
#11879=CARTESIAN_POINT('Ctrl Pts',(0.0924156585639026,-1.99261111301622,
6.52875364571643));
#11880=CARTESIAN_POINT('Ctrl Pts',(0.102843906927676,-1.99210920430587,
6.52941868495274));
#11881=CARTESIAN_POINT('Ctrl Pts',(0.109790378816801,-1.9917384434692,6.52985980603651));
#11882=CARTESIAN_POINT('Ctrl Pts',(0.230485184815082,-1.98466312924971,
6.53749388010856));
#11883=CARTESIAN_POINT('Ctrl Pts',(0.343474201183392,-1.96825935870635,
6.54417709211632));
#11884=CARTESIAN_POINT('Ctrl Pts',(0.554848976247106,-1.91880175393996,
6.55679790705072));
#11885=CARTESIAN_POINT('Ctrl Pts',(0.653263445867949,-1.8875655122907,6.56272897672596));
#11886=CARTESIAN_POINT('Ctrl Pts',(0.799135076962752,-1.82848501768097,
6.57205969138134));
#11887=CARTESIAN_POINT('Ctrl Pts',(0.848592900520164,-1.80606304426536,
6.57532230788499));
#11888=CARTESIAN_POINT('Ctrl Pts',(0.915859545877599,-1.7721939235694,6.57993984516027));
#11889=CARTESIAN_POINT('Ctrl Pts',(0.934495546409145,-1.76243809354769,
6.58123889245969));
#11890=CARTESIAN_POINT('Ctrl Pts',(0.962306301824172,-1.74731422744665,
6.58320935682907));
#11891=CARTESIAN_POINT('Ctrl Pts',(0.971598492456417,-1.74216439825661,
6.58387317856972));
#11892=CARTESIAN_POINT('Ctrl Pts',(0.98857238525353,-1.73257925497255,6.58509605647586));
#11893=CARTESIAN_POINT('Ctrl Pts',(0.9962665290319,-1.72816643720659,6.58565430312171));
#11894=CARTESIAN_POINT('Ctrl Pts',(1.00853840649026,-1.72101896438434,6.58655110633162));
#11895=CARTESIAN_POINT('Ctrl Pts',(1.01313511018971,-1.71831697912146,6.5868884784308));
#11896=CARTESIAN_POINT('Ctrl Pts',(1.01772689524567,-1.71559305467304,6.58722696322272));
#11897=CARTESIAN_POINT('Ctrl Pts',(1.01773290126574,-1.71558949175785,6.5872274059608));
#11898=CARTESIAN_POINT('Ctrl Pts',(1.01774493154419,-1.71558235502268,6.58722829278647));
#11899=CARTESIAN_POINT('Ctrl Pts',(1.0177509557751,-1.71557878121873,6.58722873687205));
#11900=CARTESIAN_POINT('Ctrl Pts',(1.01776302226643,-1.71557162282909,6.58722962637739));
#11901=CARTESIAN_POINT('Ctrl Pts',(1.0177690646568,-1.71556803816607,6.58723007180674));
#11902=CARTESIAN_POINT('Ctrl Pts',(1.01778116774478,-1.71556085789276,6.58723096402014));
#11903=CARTESIAN_POINT('Ctrl Pts',(1.0177872283856,-1.71555726231589,6.58723141080001));
#11904=CARTESIAN_POINT('Ctrl Pts',(1.01779936826458,-1.71555006004202,6.58723230573588));
#11905=CARTESIAN_POINT('Ctrl Pts',(1.01780544734149,-1.7155464534404,6.58723275388001));
#11906=CARTESIAN_POINT('Ctrl Pts',(1.01781762374053,-1.71553922932512,6.58723365151848));
#11907=CARTESIAN_POINT('Ctrl Pts',(1.01782372116222,-1.71553561175213,6.58723410102017));
#11908=CARTESIAN_POINT('Ctrl Pts',(1.01783593461551,-1.71552836547692,6.58723500140071));
#11909=CARTESIAN_POINT('Ctrl Pts',(1.01784205054153,-1.71552473683709,6.58723545227179));
#11910=CARTESIAN_POINT('Ctrl Pts',(1.01785430099153,-1.7155174684345,6.58723635539026));
#11911=CARTESIAN_POINT('Ctrl Pts',(1.01786043549049,-1.71551382868632,6.58723680763582));
#11912=CARTESIAN_POINT('Ctrl Pts',(1.01787272299974,-1.71550653811761,6.58723771349691));
#11913=CARTESIAN_POINT('Ctrl Pts',(1.01787887607784,-1.71550288725659,6.58723816711746));
#11914=CARTESIAN_POINT('Ctrl Pts',(1.01789120095963,-1.71549557433426,6.58723907574439));
#11915=CARTESIAN_POINT('Ctrl Pts',(1.01789737274825,-1.71549191228163,6.58723953074967));
#11916=CARTESIAN_POINT('Ctrl Pts',(1.01790973488439,-1.71548457707418,6.5872404421338));
#11917=CARTESIAN_POINT('Ctrl Pts',(1.01791592533307,-1.71548090385907,6.58724089852013));
#11918=CARTESIAN_POINT('Ctrl Pts',(1.01792832521644,-1.71547354607239,6.5872418126979));
#11919=CARTESIAN_POINT('Ctrl Pts',(1.0179345345215,-1.71546986157747,6.58724227047981));
#11920=CARTESIAN_POINT('Ctrl Pts',(1.01794697194665,-1.71546248133181,6.58724318743618));
#11921=CARTESIAN_POINT('Ctrl Pts',(1.01795320009879,-1.71545878556177,6.58724364661302));
#11922=CARTESIAN_POINT('Ctrl Pts',(1.01796567538871,-1.71545138266381,6.5872445663719));
#11923=CARTESIAN_POINT('Ctrl Pts',(1.01797192249516,-1.71544767555419,6.58724502695164));
#11924=CARTESIAN_POINT('Ctrl Pts',(1.01798443565261,-1.7154402500006,6.58724594951333));
#11925=CARTESIAN_POINT('Ctrl Pts',(1.0179907017328,-1.71543653153903,6.58724641149744));
#11926=CARTESIAN_POINT('Ctrl Pts',(1.0180032530666,-1.71542908314486,6.58724733688481));
#11927=CARTESIAN_POINT('Ctrl Pts',(1.01800953826952,-1.71542535324207,6.58724780028434));
#11928=CARTESIAN_POINT('Ctrl Pts',(1.01802212759982,-1.71541788211236,6.58724872848423));
#11929=CARTESIAN_POINT('Ctrl Pts',(1.0180284318443,-1.71541414081568,6.58724919329324));
#11930=CARTESIAN_POINT('Ctrl Pts',(1.01804105978887,-1.71540664658209,6.5872501243513));
#11931=CARTESIAN_POINT('Ctrl Pts',(1.01804738333042,-1.71540289373901,6.58725059058867));
#11932=CARTESIAN_POINT('Ctrl Pts',(1.01806004947274,-1.71539537664701,6.58725152447429));
#11933=CARTESIAN_POINT('Ctrl Pts',(1.01806639220496,-1.71539161231981,6.58725199213225));
#11934=CARTESIAN_POINT('Ctrl Pts',(1.01807909713451,-1.71538407201784,6.58725292888899));
#11935=CARTESIAN_POINT('Ctrl Pts',(1.01808545923271,-1.71538029610161,6.5872533979805));
#11936=CARTESIAN_POINT('Ctrl Pts',(1.01809820282943,-1.71537273265916,6.58725433759963));
#11937=CARTESIAN_POINT('Ctrl Pts',(1.0181045843219,-1.71536894513624,6.58725480812682));
#11938=CARTESIAN_POINT('Ctrl Pts',(1.01811736682391,-1.71536135841022,6.58725575062599));
#11939=CARTESIAN_POINT('Ctrl Pts',(1.01812376780242,-1.71535755922525,6.5872562225957));
#11940=CARTESIAN_POINT('Ctrl Pts',(1.01813658926401,-1.71534994918168,6.58725716797902));
#11941=CARTESIAN_POINT('Ctrl Pts',(1.01814300976267,-1.71534613831354,6.5872576413938));
#11942=CARTESIAN_POINT('Ctrl Pts',(1.01815587046537,-1.71533850478353,6.58725858968213));
#11943=CARTESIAN_POINT('Ctrl Pts',(1.01816231062961,-1.71533468214499,6.58725906455277));
#11944=CARTESIAN_POINT('Ctrl Pts',(1.01817521039148,-1.71532702523475,6.58726001573281));
#11945=CARTESIAN_POINT('Ctrl Pts',(1.01818167012497,-1.7153231908821,6.58726049205225));
#11946=CARTESIAN_POINT('Ctrl Pts',(1.01819460961073,-1.71531551019526,6.58726144617312));
#11947=CARTESIAN_POINT('Ctrl Pts',(1.01820108917981,-1.7153116639695,6.58726192396105));
#11948=CARTESIAN_POINT('Ctrl Pts',(1.01821406800295,-1.71530395973367,6.58726288099435));
#11949=CARTESIAN_POINT('Ctrl Pts',(1.01822056734699,-1.71530010166988,6.58726336024637));
#11950=CARTESIAN_POINT('Ctrl Pts',(1.01823358593542,-1.71529237362922,6.58726432022377));
#11951=CARTESIAN_POINT('Ctrl Pts',(1.01824010515381,-1.71528850366748,6.58726480094725));
#11952=CARTESIAN_POINT('Ctrl Pts',(1.01825316354293,-1.71528075179914,6.58726576387146));
#11953=CARTESIAN_POINT('Ctrl Pts',(1.01825970266175,-1.71527686992306,6.58726624606838));
#11954=CARTESIAN_POINT('Ctrl Pts',(1.02242340091638,-1.71280510396838,6.58757328055461));
#11955=CARTESIAN_POINT('Ctrl Pts',(1.0265715439348,-1.71032213323363,6.58788038147212));
#11956=CARTESIAN_POINT('Ctrl Pts',(1.03598579856819,-1.70464041706431,6.58858013785632));
#11957=CARTESIAN_POINT('Ctrl Pts',(1.04124617837504,-1.70143231453255,6.58897313421463));
#11958=CARTESIAN_POINT('Ctrl Pts',(1.05720190257521,-1.69159982630021,6.59017130689509));
#11959=CARTESIAN_POINT('Ctrl Pts',(1.06784935454139,-1.68489868511379,6.59097930486818));
#11960=CARTESIAN_POINT('Ctrl Pts',(1.20950777495385,-1.59386163002618,6.60184464060991));
#11961=CARTESIAN_POINT('Ctrl Pts',(1.33023408679994,-1.49457731321874,6.61249972469336));
#11962=CARTESIAN_POINT('Ctrl Pts',(1.50166672770224,-1.31621559577668,6.62974270148864));
#11963=CARTESIAN_POINT('Ctrl Pts',(1.56054694475119,-1.24584145932417,6.63616419091552));
#11964=CARTESIAN_POINT('Ctrl Pts',(1.63469017815413,-1.14368311722831,6.64477894588772));
#11965=CARTESIAN_POINT('Ctrl Pts',(1.65426947702844,-1.11517525407169,6.64711285809053));
#11966=CARTESIAN_POINT('Ctrl Pts',(1.68359869975836,-1.06999757466042,6.65068759613698));
#11967=CARTESIAN_POINT('Ctrl Pts',(1.69386392789966,-1.05367189086545,6.65195505129884));
#11968=CARTESIAN_POINT('Ctrl Pts',(1.70652987241577,-1.03286451614205,6.65353747910869));
#11969=CARTESIAN_POINT('Ctrl Pts',(1.70915197346041,-1.02851973590306,6.65386611384148));
#11970=CARTESIAN_POINT('Ctrl Pts',(1.71330806898991,-1.02157336679463,6.65438862007934));
#11971=CARTESIAN_POINT('Ctrl Pts',(1.71485276292102,-1.0189782553177,6.65458317988249));
#11972=CARTESIAN_POINT('Ctrl Pts',(1.71777250611696,-1.01404759507408,6.65495160330142));
#11973=CARTESIAN_POINT('Ctrl Pts',(1.7191486720879,-1.01171278097614,6.65512553678619));
#11974=CARTESIAN_POINT('Ctrl Pts',(1.72229150130787,-1.00635570342453,6.65552342332095));
#11975=CARTESIAN_POINT('Ctrl Pts',(1.72405496824476,-1.00333159235627,6.65574716747327));
#11976=CARTESIAN_POINT('Ctrl Pts',(1.72959916945345,-0.993766248438064,
6.65645219698094));
#11977=CARTESIAN_POINT('Ctrl Pts',(1.73335076322023,-0.987208073068833,
6.65693163291302));
#11978=CARTESIAN_POINT('Ctrl Pts',(1.7975572137286,-0.873474105764137,6.66518099619098));
#11979=CARTESIAN_POINT('Ctrl Pts',(1.84801506115116,-0.760933180365182,
6.67235561461449));
#11980=CARTESIAN_POINT('Ctrl Pts',(1.92011243192427,-0.549736608298843,
6.68531074385638));
#11981=CARTESIAN_POINT('Ctrl Pts',(1.94526936378461,-0.452733932616914,
6.69108317192942));
#11982=CARTESIAN_POINT('Ctrl Pts',(1.97199907273376,-0.304617246401701,
6.70003379705962));
#11983=CARTESIAN_POINT('Ctrl Pts',(1.97907069257955,-0.254657856555056,
6.70307389550469));
#11984=CARTESIAN_POINT('Ctrl Pts',(1.98734264182223,-0.174390859627053,
6.70802810825));
#11985=CARTESIAN_POINT('Ctrl Pts',(1.98975893393945,-0.144229604993428,
6.70990520348969));
#11986=CARTESIAN_POINT('Ctrl Pts',(1.99198379047747,-0.105372108024621,
6.71234787109334));
#11987=CARTESIAN_POINT('Ctrl Pts',(1.99242287791246,-0.0967149131407915,
6.71289362678897));
#11988=CARTESIAN_POINT('Ctrl Pts',(1.99304068217451,-0.0827331927704075,
6.71377764369478));
#11989=CARTESIAN_POINT('Ctrl Pts',(1.99325452252908,-0.0774102674565435,
6.71411480202458));
#11990=CARTESIAN_POINT('Ctrl Pts',(1.99362210987647,-0.0672451882657548,
6.71475985265493));
#11991=CARTESIAN_POINT('Ctrl Pts',(1.99377954458275,-0.0624031990861622,
6.71506762702889));
#11992=CARTESIAN_POINT('Ctrl Pts',(1.99409953282732,-0.0513187172266358,
6.71577339458607));
#11993=CARTESIAN_POINT('Ctrl Pts',(1.99425041397984,-0.0450759629419817,
6.71617175061494));
#11994=CARTESIAN_POINT('Ctrl Pts',(1.99462511715923,-0.0258319168961299,
6.71740246806978));
#11995=CARTESIAN_POINT('Ctrl Pts',(1.99475112292412,-0.0128292717293726,
6.71823788038833));
#11996=CARTESIAN_POINT('Ctrl Pts',(1.9947388541967,0.128286842604169,6.72734782198812));
#11997=CARTESIAN_POINT('Ctrl Pts',(1.98238600886794,0.256076005755822,6.73601469384028));
#11998=CARTESIAN_POINT('Ctrl Pts',(1.92826886430591,0.533605755829806,6.75561488815851));
#11999=CARTESIAN_POINT('Ctrl Pts',(1.88110249869077,0.68147895752933,6.766588682889));
#12000=CARTESIAN_POINT('Ctrl Pts',(1.80985798105033,0.838909550587931,6.77804094487477));
#12001=CARTESIAN_POINT('Ctrl Pts',(1.80217138918023,0.855297308823046,6.7792294736845));
#12002=CARTESIAN_POINT('Ctrl Pts',(1.79209328911896,0.876044435110608,6.78072746105763));
#12003=CARTESIAN_POINT('Ctrl Pts',(1.78990740758255,0.880501949323029,6.7810489044153));
#12004=CARTESIAN_POINT('Ctrl Pts',(1.78637598200101,0.88763584091704,6.78156265246885));
#12005=CARTESIAN_POINT('Ctrl Pts',(1.78504102913085,0.89031739270955,6.78175560640357));
#12006=CARTESIAN_POINT('Ctrl Pts',(1.78248373307362,0.895425421542024,6.78212284322593));
#12007=CARTESIAN_POINT('Ctrl Pts',(1.78126248785867,0.897852378535421,6.78229718825098));
#12008=CARTESIAN_POINT('Ctrl Pts',(1.77843517971906,0.903442559927139,6.78269846193021));
#12009=CARTESIAN_POINT('Ctrl Pts',(1.77682563488174,0.906603999137742,6.78292516938992));
#12010=CARTESIAN_POINT('Ctrl Pts',(1.7724843988219,0.915075008697134,6.78353206370028));
#12011=CARTESIAN_POINT('Ctrl Pts',(1.76973726086726,0.920376686624943,6.78391129962796));
#12012=CARTESIAN_POINT('Ctrl Pts',(1.74953795691009,0.958934318166979,6.78666560948518));
#12013=CARTESIAN_POINT('Ctrl Pts',(1.73117213129009,0.991706399218336,6.78898616812232));
#12014=CARTESIAN_POINT('Ctrl Pts',(1.66830589966521,1.09681002703077,6.79642544126453));
#12015=CARTESIAN_POINT('Ctrl Pts',(1.62010955898059,1.16682657540779,6.80137882115103));
#12016=CARTESIAN_POINT('Ctrl Pts',(1.50528263557822,1.31274692867956,6.81216106285884));
#12017=CARTESIAN_POINT('Ctrl Pts',(1.43706274274468,1.38709403816706,6.81796951597042));
#12018=CARTESIAN_POINT('Ctrl Pts',(1.32607580268801,1.49103403342782,6.82700590066267));
#12019=CARTESIAN_POINT('Ctrl Pts',(1.28729359631978,1.52464229070176,6.83009591377815));
#12020=CARTESIAN_POINT('Ctrl Pts',(1.22335770152675,1.57586854469316,6.83512432904677));
#12021=CARTESIAN_POINT('Ctrl Pts',(1.19901728102899,1.59446641119766,6.837024267462));
#12022=CARTESIAN_POINT('Ctrl Pts',(1.16722155833814,1.61762084333542,6.83949265876285));
#12023=CARTESIAN_POINT('Ctrl Pts',(1.1601504069946,1.62269972216716,6.8400407708087));
#12024=CARTESIAN_POINT('Ctrl Pts',(1.14869230958585,1.63081636324019,6.84092768801521));
#12025=CARTESIAN_POINT('Ctrl Pts',(1.1443259729406,1.63388313519194,6.84126537702318));
#12026=CARTESIAN_POINT('Ctrl Pts',(1.13597343610338,1.63969977931773,6.84191083315588));
#12027=CARTESIAN_POINT('Ctrl Pts',(1.1319894179478,1.64245273015748,6.84221847978438));
#12028=CARTESIAN_POINT('Ctrl Pts',(1.12285832735404,1.64871329673649,6.84292309309018));
#12029=CARTESIAN_POINT('Ctrl Pts',(1.11770479145757,1.65221135326027,6.84332041835098));
#12030=CARTESIAN_POINT('Ctrl Pts',(1.10181042283158,1.66289154877919,6.84454480659798));
#12031=CARTESIAN_POINT('Ctrl Pts',(1.09101629209933,1.66999339764401,6.8453748750289));
#12032=CARTESIAN_POINT('Ctrl Pts',(0.987393192092796,1.73673734789289,6.8533312104813));
#12033=CARTESIAN_POINT('Ctrl Pts',(0.889851419589409,1.78867518848476,6.86074375154518));
#12034=CARTESIAN_POINT('Ctrl Pts',(0.630523920453439,1.90027829728847,6.88019768047408));
#12035=CARTESIAN_POINT('Ctrl Pts',(0.464388405942447,1.94755291589205,6.89247013574457));
#12036=CARTESIAN_POINT('Ctrl Pts',(0.275845800696351,1.97567276133391,6.90511150412131));
#12037=CARTESIAN_POINT('Ctrl Pts',(0.257404482929136,1.97815994281335,6.90633384367969));
#12038=CARTESIAN_POINT('Ctrl Pts',(0.233953680755479,1.98098923890008,6.90786808080435));
#12039=CARTESIAN_POINT('Ctrl Pts',(0.228974786452716,1.98157090155009,6.90819266838026));
#12040=CARTESIAN_POINT('Ctrl Pts',(0.221006445941902,1.98247137455274,6.90871025032497));
#12041=CARTESIAN_POINT('Ctrl Pts',(0.21801842097341,1.98280220104763,6.90890391085958));
#12042=CARTESIAN_POINT('Ctrl Pts',(0.212331536604923,1.98341882777876,6.90927166533526));
#12043=CARTESIAN_POINT('Ctrl Pts',(0.209632875255926,1.98370587172527,6.90944582481277));
#12044=CARTESIAN_POINT('Ctrl Pts',(0.203425952773704,1.98435326532506,6.90984558718963));
#12045=CARTESIAN_POINT('Ctrl Pts',(0.199917318455736,1.98470981912138,6.91007097438661));
#12046=CARTESIAN_POINT('Ctrl Pts',(0.188751890948206,1.98581456126663,6.91078639524413));
#12047=CARTESIAN_POINT('Ctrl Pts',(0.181091590339512,1.98652777191804,6.91127450121112));
#12048=CARTESIAN_POINT('Ctrl Pts',(0.0585558306538583,1.99722174846652,
6.91904154560142));
#12049=CARTESIAN_POINT('Ctrl Pts',(-0.0569880609261623,1.9972692312399,
6.925798700472));
#12050=CARTESIAN_POINT('Ctrl Pts',(-0.274174718596705,1.97848259156458,
6.93846928754536));
#12051=CARTESIAN_POINT('Ctrl Pts',(-0.375606069714301,1.96175541427916,
6.94437674922504));
#12052=CARTESIAN_POINT('Ctrl Pts',(-0.546187912683751,1.91990474241444,
6.95479462237053));
#12053=CARTESIAN_POINT('Ctrl Pts',(-0.616062822790427,1.89863642479476,
6.95920524830631));
#12054=CARTESIAN_POINT('Ctrl Pts',(-0.700140637813496,1.86791435743031,
6.96477102059672));
#12055=CARTESIAN_POINT('Ctrl Pts',(-0.715599497257305,1.86204680203107,
6.96580525195011));
#12056=CARTESIAN_POINT('Ctrl Pts',(-0.737388336406335,1.85346523907365,
6.9672791772467));
#12057=CARTESIAN_POINT('Ctrl Pts',(-0.743780236237131,1.85090948168201,
6.9677135547612));
#12058=CARTESIAN_POINT('Ctrl Pts',(-0.754743830501469,1.84645980164953,
6.96846209750261));
#12059=CARTESIAN_POINT('Ctrl Pts',(-0.75932197194156,1.84458184719259,6.96877572113332));
#12060=CARTESIAN_POINT('Ctrl Pts',(-0.768043538058219,1.84096628790879,
6.96937521434914));
#12061=CARTESIAN_POINT('Ctrl Pts',(-0.772188177967852,1.83923167840067,
6.96966098075384));
#12062=CARTESIAN_POINT('Ctrl Pts',(-0.78184452241162,1.83515192391297,6.97032883639506));
#12063=CARTESIAN_POINT('Ctrl Pts',(-0.787351571854947,1.83279593574103,
6.97071129301806));
#12064=CARTESIAN_POINT('Ctrl Pts',(-0.806243720121482,1.82461276525473,
6.97202880811448));
#12065=CARTESIAN_POINT('Ctrl Pts',(-0.819575156000233,1.81866358191567,
6.97296802383439));
#12066=CARTESIAN_POINT('Ctrl Pts',(-0.930510687918328,1.76769087960372,
6.98086496092724));
#12067=CARTESIAN_POINT('Ctrl Pts',(-1.02437783155736,1.71499982243722,6.9880919074526));
#12068=CARTESIAN_POINT('Ctrl Pts',(-1.25623949497343,1.55899788585439,7.00734832448742));
#12069=CARTESIAN_POINT('Ctrl Pts',(-1.38592543961186,1.44493033539489,7.01961954560327));
#12070=CARTESIAN_POINT('Ctrl Pts',(-1.51166442290954,1.30163191360699,7.03226239542534));
#12071=CARTESIAN_POINT('Ctrl Pts',(-1.52376125153095,1.28744967909363,7.03348688447422));
#12072=CARTESIAN_POINT('Ctrl Pts',(-1.53885912746847,1.26923808039028,7.0350234177662));
#12073=CARTESIAN_POINT('Ctrl Pts',(-1.54204568694168,1.26536469826562,7.03534819782987));
#12074=CARTESIAN_POINT('Ctrl Pts',(-1.5471191920912,1.25915003445405,7.03586601183961));
#12075=CARTESIAN_POINT('Ctrl Pts',(-1.54901548589635,1.25681646573801,7.03605971301805));
#12076=CARTESIAN_POINT('Ctrl Pts',(-1.55261313177231,1.25236871157321,7.0364274949243));
#12077=CARTESIAN_POINT('Ctrl Pts',(-1.55431542511603,1.25025536831757,7.03660164139576));
#12078=CARTESIAN_POINT('Ctrl Pts',(-1.55821927877015,1.2453885617818,7.03700130685573));
#12079=CARTESIAN_POINT('Ctrl Pts',(-1.5604178545082,1.24263273349234,7.03722661048264));
#12080=CARTESIAN_POINT('Ctrl Pts',(-1.56738662798207,1.23384999036367,7.03794150362382));
#12081=CARTESIAN_POINT('Ctrl Pts',(-1.57212937496593,1.22780123524641,7.03842916944329));
#12082=CARTESIAN_POINT('Ctrl Pts',(-1.64775113496999,1.13019891928993,7.04622590443198));
#12083=CARTESIAN_POINT('Ctrl Pts',(-1.71057367642031,1.03265662672429,7.05300881891232));
#12084=CARTESIAN_POINT('Ctrl Pts',(-1.81237929514299,0.839531986095422,
7.06569672327122));
#12085=CARTESIAN_POINT('Ctrl Pts',(-1.85311402592373,0.745318816234449,
7.07159587099584));
#12086=CARTESIAN_POINT('Ctrl Pts',(-1.90382021315251,0.597795063367899,
7.08084994018711));
#12087=CARTESIAN_POINT('Ctrl Pts',(-1.9191679968745,0.546519776918832,7.0840675044448));
#12088=CARTESIAN_POINT('Ctrl Pts',(-1.94026607927825,0.464103544249463,
7.08928498010321));
#12089=CARTESIAN_POINT('Ctrl Pts',(-1.94736888644038,0.43333451757863,7.09124259108606));
#12090=CARTESIAN_POINT('Ctrl Pts',(-1.95551325494937,0.393792961562603,
7.09377581024684));
#12091=CARTESIAN_POINT('Ctrl Pts',(-1.95723127799705,0.38516322162594,7.09432972066377));
#12092=CARTESIAN_POINT('Ctrl Pts',(-1.95990318425386,0.371262389593682,
7.09522375683155));
#12093=CARTESIAN_POINT('Ctrl Pts',(-1.96089304246371,0.365998263219489,
7.09556273333203));
#12094=CARTESIAN_POINT('Ctrl Pts',(-1.9627365468652,0.355972210274397,7.0962091591243));
#12095=CARTESIAN_POINT('Ctrl Pts',(-1.96359409667029,0.351211033044341,
7.09651648161124));
#12096=CARTESIAN_POINT('Ctrl Pts',(-1.96550931660985,0.340351288999826,
7.09721826504437));
#12097=CARTESIAN_POINT('Ctrl Pts',(-1.96655593439504,0.334250847526576,
7.09761307429341));
#12098=CARTESIAN_POINT('Ctrl Pts',(-1.96966706715817,0.31559637624988,7.09882219456842));
#12099=CARTESIAN_POINT('Ctrl Pts',(-1.97163985158742,0.303027575170243,
7.09963940331373));
#12100=CARTESIAN_POINT('Ctrl Pts',(-1.9877290618664,0.193704402903063,7.10677064894761));
#12101=CARTESIAN_POINT('Ctrl Pts',(-1.99483182184317,0.0960674158499719,
7.11330712457486));
#12102=CARTESIAN_POINT('Ctrl Pts',(-1.9945866700246,-0.194289774984962,
7.13320902369089));
#12103=CARTESIAN_POINT('Ctrl Pts',(-1.9665315913241,-0.385843753873489,
7.14703282624318));
#12104=CARTESIAN_POINT('Ctrl Pts',(-1.90798583330162,-0.582035259283457,
7.16050168284247));
#12105=CARTESIAN_POINT('Ctrl Pts',(-1.90440764541565,-0.593638375583651,
7.16129512512014));
#12106=CARTESIAN_POINT('Ctrl Pts',(-1.89938014469388,-0.609427794194555,
7.16236986835138));
#12107=CARTESIAN_POINT('Ctrl Pts',(-1.89802260062614,-0.613642712680085,
7.1626562810746));
#12108=CARTESIAN_POINT('Ctrl Pts',(-1.89584893660257,-0.620315305104654,
7.16310888888343));
#12109=CARTESIAN_POINT('Ctrl Pts',(-1.89504205724023,-0.622775938555268,
7.16327562102889));
#12110=CARTESIAN_POINT('Ctrl Pts',(-1.89337435221628,-0.62782846675722,
7.1636176100584));
#12111=CARTESIAN_POINT('Ctrl Pts',(-1.89251299685581,-0.630420159979779,
7.1637928313699));
#12112=CARTESIAN_POINT('Ctrl Pts',(-1.8904715829434,-0.636520588967075,
7.16420481309576));
#12113=CARTESIAN_POINT('Ctrl Pts',(-1.88928706785623,-0.640027844601951,
7.16444131035098));
#12114=CARTESIAN_POINT('Ctrl Pts',(-1.88537086808901,-0.651517794793943,
7.16521497170818));
#12115=CARTESIAN_POINT('Ctrl Pts',(-1.88259825426532,-0.659486592935013,
7.16574977148564));
#12116=CARTESIAN_POINT('Ctrl Pts',(-1.84700096143439,-0.759742994455694,
7.1724586506003));
#12117=CARTESIAN_POINT('Ctrl Pts',(-1.80746730943883,-0.849523101789957,
7.17826050963938));
#12118=CARTESIAN_POINT('Ctrl Pts',(-1.72508194445567,-1.00455938966159,
7.18850896035907));
#12119=CARTESIAN_POINT('Ctrl Pts',(-1.68470758033952,-1.07089113462028,
7.19297744615205));
#12120=CARTESIAN_POINT('Ctrl Pts',(-1.57257247560681,-1.23301790181466,
7.20447462146601));
#12121=CARTESIAN_POINT('Ctrl Pts',(-1.49588371763748,-1.32500682946709,
7.21157044691108));
#12122=CARTESIAN_POINT('Ctrl Pts',(-1.40224357760754,-1.41877042545384,
7.21984136981117));
#12123=CARTESIAN_POINT('Ctrl Pts',(-1.39296748642958,-1.42787889545759,
7.22065663746208));
#12124=CARTESIAN_POINT('Ctrl Pts',(-1.37910531737959,-1.44122693392285,
7.22186937015431));
#12125=CARTESIAN_POINT('Ctrl Pts',(-1.37458716874236,-1.44553680879389,
7.22226377534085));
#12126=CARTESIAN_POINT('Ctrl Pts',(-1.3665277547429,-1.45315275454438,7.22296582116136));
#12127=CARTESIAN_POINT('Ctrl Pts',(-1.36299452494478,-1.45646728655837,
7.22327309401369));
#12128=CARTESIAN_POINT('Ctrl Pts',(-1.35555046928034,-1.46339976483327,
7.22391944718087));
#12129=CARTESIAN_POINT('Ctrl Pts',(-1.35163715840075,-1.46701497524824,
7.22425864082987));
#12130=CARTESIAN_POINT('Ctrl Pts',(-1.34131760137602,-1.47647208657606,
7.22515159113617));
#12131=CARTESIAN_POINT('Ctrl Pts',(-1.33488772411706,-1.48228792421194,
7.22570644482831));
#12132=CARTESIAN_POINT('Ctrl Pts',(-1.30583911040822,-1.50822016130144,
7.22820654577537));
#12133=CARTESIAN_POINT('Ctrl Pts',(-1.28280317585141,-1.52786114609097,
7.23017145725435));
#12134=CARTESIAN_POINT('Ctrl Pts',(-1.22018484864454,-1.57883639412306,
7.23546966910293));
#12135=CARTESIAN_POINT('Ctrl Pts',(-1.17984700709602,-1.60920344953893,
7.23883919118132));
#12136=CARTESIAN_POINT('Ctrl Pts',(-1.05616927384214,-1.69515867901641,
7.24904047659767));
#12137=CARTESIAN_POINT('Ctrl Pts',(-0.969754322193277,-1.74603256559661,
7.25600943872138));
#12138=CARTESIAN_POINT('Ctrl Pts',(-0.769562514334622,-1.84442805855687,
7.27157312375087));
#12139=CARTESIAN_POINT('Ctrl Pts',(-0.65444006442421,-1.88834768232673,
7.28014732982795));
#12140=CARTESIAN_POINT('Ctrl Pts',(-0.528717325381184,-1.92341951351136,
7.28866878727077));
#12141=CARTESIAN_POINT('Ctrl Pts',(-0.521428903465127,-1.92540814846505,
7.28915982412871));
#12142=CARTESIAN_POINT('Ctrl Pts',(-0.510746864418605,-1.92825762214947,
7.28987497815223));
#12143=CARTESIAN_POINT('Ctrl Pts',(-0.507362108399073,-1.92915098121202,
7.29010092298121));
#12144=CARTESIAN_POINT('Ctrl Pts',(-0.501352673830008,-1.93072017763888,
7.29050087953229));
#12145=CARTESIAN_POINT('Ctrl Pts',(-0.498728951708093,-1.93139958086799,
7.29067509653724));
#12146=CARTESIAN_POINT('Ctrl Pts',(-0.493178541450453,-1.93282477481158,
7.29104278676217));
#12147=CARTESIAN_POINT('Ctrl Pts',(-0.490251549938585,-1.93356926484485,
7.29123618407431));
#12148=CARTESIAN_POINT('Ctrl Pts',(-0.482401561484502,-1.93554696464492,
7.29175354268274));
#12149=CARTESIAN_POINT('Ctrl Pts',(-0.477475489111115,-1.93676804949092,
7.2920768093821));
#12150=CARTESIAN_POINT('Ctrl Pts',(-0.45380645602142,-1.94253938509753,
7.29362363067294));
#12151=CARTESIAN_POINT('Ctrl Pts',(-0.435002038710527,-1.9468366278307,
7.29483322377454));
#12152=CARTESIAN_POINT('Ctrl Pts',(-0.382311522558341,-1.95807602382593,
7.2981763187303));
#12153=CARTESIAN_POINT('Ctrl Pts',(-0.348301574264663,-1.96441088430794,
7.30028117018476));
#12154=CARTESIAN_POINT('Ctrl Pts',(-0.223538339647063,-1.98430743217364,
7.30786615025344));
#12155=CARTESIAN_POINT('Ctrl Pts',(-0.132039425032454,-1.99248920695555,
7.31317080884233));
#12156=CARTESIAN_POINT('Ctrl Pts',(0.115340367407889,-1.99748769174982,
7.32752115855705));
#12157=CARTESIAN_POINT('Ctrl Pts',(0.270785521303748,-1.9824042001089,7.33659109858792));
#12158=CARTESIAN_POINT('Ctrl Pts',(0.435177562778028,-1.94674246144229,
7.34709544743529));
#12159=CARTESIAN_POINT('Ctrl Pts',(0.447442143776204,-1.94396019474529,
7.34788438196233));
#12160=CARTESIAN_POINT('Ctrl Pts',(0.465674161534954,-1.93964251621462,
7.34906533275389));
#12161=CARTESIAN_POINT('Ctrl Pts',(0.471662282310595,-1.93819508963639,
7.34945451977796));
#12162=CARTESIAN_POINT('Ctrl Pts',(0.482337316233643,-1.93556235946276,
7.35015071420359));
#12163=CARTESIAN_POINT('Ctrl Pts',(0.487026826562608,-1.93438770765701,
7.35045737589868));
#12164=CARTESIAN_POINT('Ctrl Pts',(0.496918666775499,-1.93187169979591,
7.35110599939883));
#12165=CARTESIAN_POINT('Ctrl Pts',(0.502119932709991,-1.93052635260604,
7.35144808813377));
#12166=CARTESIAN_POINT('Ctrl Pts',(0.515895166759187,-1.92690384754689,
7.35235686498088));
#12167=CARTESIAN_POINT('Ctrl Pts',(0.524459411377618,-1.92459049732045,
7.35292472175721));
#12168=CARTESIAN_POINT('Ctrl Pts',(0.564159956717498,-1.91358202795201,
7.35557061230818));
#12169=CARTESIAN_POINT('Ctrl Pts',(0.59509586627981,-1.90418836792565,7.35767123299051));
#12170=CARTESIAN_POINT('Ctrl Pts',(0.678283802698345,-1.87670328919761,
7.3634298160512));
#12171=CARTESIAN_POINT('Ctrl Pts',(0.730030982862083,-1.85718550045609,
7.36713222951314));
#12172=CARTESIAN_POINT('Ctrl Pts',(0.876531237683069,-1.79485981503344,
7.37795721683183));
#12173=CARTESIAN_POINT('Ctrl Pts',(0.968832756592229,-1.74676518811115,
7.38521460075528));
#12174=CARTESIAN_POINT('Ctrl Pts',(1.11743386317596,-1.65392076745725,7.3974335506059));
#12175=CARTESIAN_POINT('Ctrl Pts',(1.17584254626516,-1.61291904942451,7.40238922845445));
#12176=CARTESIAN_POINT('Ctrl Pts',(1.23889348613665,-1.56340935694367,7.40782663950981));
#12177=CARTESIAN_POINT('Ctrl Pts',(1.24581779177863,-1.55789727578309,7.4084250027478));
#12178=CARTESIAN_POINT('Ctrl Pts',(1.27878078056078,-1.53129683297923,7.41127852426397));
#12179=CARTESIAN_POINT('Ctrl Pts',(1.30432389837575,-1.50959920871224,7.41350492517378));
#12180=CARTESIAN_POINT('Ctrl Pts',(1.33361065375467,-1.48342288584133,7.41606386009804));
#12181=CARTESIAN_POINT('Ctrl Pts',(1.33789470271329,-1.4795602726768,7.41643833875314));
#12182=CARTESIAN_POINT('Ctrl Pts',(1.34474229004939,-1.47333224405047,7.41703707194208));
#12183=CARTESIAN_POINT('Ctrl Pts',(1.34731644456302,-1.47097862889667,7.41726218735919));
#12184=CARTESIAN_POINT('Ctrl Pts',(1.35187856928799,-1.46678533962336,7.41766120282715));
#12185=CARTESIAN_POINT('Ctrl Pts',(1.35386897879026,-1.46494835651323,7.417835304758));
#12186=CARTESIAN_POINT('Ctrl Pts',(1.35807607523794,-1.461049657063,7.41820332760344));
#12187=CARTESIAN_POINT('Ctrl Pts',(1.36029180606423,-1.45898695305727,7.41839717038853));
#12188=CARTESIAN_POINT('Ctrl Pts',(1.36623266375402,-1.45343109549215,7.41891698177227));
#12189=CARTESIAN_POINT('Ctrl Pts',(1.36994911795889,-1.44992863839659,7.41924224425486));
#12190=CARTESIAN_POINT('Ctrl Pts',(1.3878943416308,-1.4328861246421,7.42081344153227));
#12191=CARTESIAN_POINT('Ctrl Pts',(1.40193665605217,-1.41915010929218,7.42204487728735));
#12192=CARTESIAN_POINT('Ctrl Pts',(1.44077374141241,-1.380020997941,7.42546427423165));
#12193=CARTESIAN_POINT('Ctrl Pts',(1.46509806120008,-1.35416945541063,7.427621975579));
#12194=CARTESIAN_POINT('Ctrl Pts',(1.55230838588195,-1.2563810260175,7.43548021356458));
#12195=CARTESIAN_POINT('Ctrl Pts',(1.61069559112383,-1.1806001642617,7.44099283948859));
#12196=CARTESIAN_POINT('Ctrl Pts',(1.66907656893195,-1.09238988289051,7.44712921610931));
#12197=CARTESIAN_POINT('Ctrl Pts',(1.67465777629022,-1.08381436634872,7.44772295023516));
#12198=CARTESIAN_POINT('Ctrl Pts',(1.75550845940798,-0.957471749850599,
7.45643372225907));
#12199=CARTESIAN_POINT('Ctrl Pts',(1.81825156134243,-0.832174999067098,
7.46464528927353));
#12200=CARTESIAN_POINT('Ctrl Pts',(1.87192306876504,-0.689273735359299,
7.47417382146523));
#12201=CARTESIAN_POINT('Ctrl Pts',(1.87634509248304,-0.677143514376843,
7.47498354721903));
#12202=CARTESIAN_POINT('Ctrl Pts',(1.88272469071956,-0.659100957884343,
7.47618959778913));
#12203=CARTESIAN_POINT('Ctrl Pts',(1.88477289524618,-0.653220839874413,
7.47658291199912));
#12204=CARTESIAN_POINT('Ctrl Pts',(1.88836494851416,-0.642750987722597,
7.47728372835545));
#12205=CARTESIAN_POINT('Ctrl Pts',(1.88991968551728,-0.638165019890582,
7.47759086734001));
#12206=CARTESIAN_POINT('Ctrl Pts',(1.8931527342253,-0.62851314025626,7.47823766626295));
#12207=CARTESIAN_POINT('Ctrl Pts',(1.89482744306627,-0.623446070378056,
7.47857744230303));
#12208=CARTESIAN_POINT('Ctrl Pts',(1.89918202328465,-0.610091039795128,
7.47947357806876));
#12209=CARTESIAN_POINT('Ctrl Pts',(1.90182795345701,-0.601792211534336,
7.48003104910718));
#12210=CARTESIAN_POINT('Ctrl Pts',(1.91354541720835,-0.56419178736214,7.4825598149577));
#12211=CARTESIAN_POINT('Ctrl Pts',(1.92199428672097,-0.534701995675028,
7.48455133157076));
#12212=CARTESIAN_POINT('Ctrl Pts',(1.9427742309293,-0.455300257242834,7.48993876774639));
#12213=CARTESIAN_POINT('Ctrl Pts',(1.95386073223267,-0.405089515106551,
7.49337242930983));
#12214=CARTESIAN_POINT('Ctrl Pts',(1.98092517562932,-0.255228144499492,
7.50369486797471));
#12215=CARTESIAN_POINT('Ctrl Pts',(1.99129584600062,-0.154736879579646,
7.51072053506725));
#12216=CARTESIAN_POINT('Ctrl Pts',(1.99728343870076,0.0667645588387559,
7.52618018596327));
#12217=CARTESIAN_POINT('Ctrl Pts',(1.98958588043622,0.187493772365523,7.5345905543698));
#12218=CARTESIAN_POINT('Ctrl Pts',(1.9699624920002,0.313563755208486,7.54292108234574));
#12219=CARTESIAN_POINT('Ctrl Pts',(1.96887450474531,0.320324267453869,7.54336636866715));
#12220=CARTESIAN_POINT('Ctrl Pts',(1.96718493119378,0.330488966526171,7.54403357140755));
#12221=CARTESIAN_POINT('Ctrl Pts',(1.96660928693717,0.333897324762621,7.5442569030128));
#12222=CARTESIAN_POINT('Ctrl Pts',(1.9655969214408,0.339798038862502,7.54464284884334));
#12223=CARTESIAN_POINT('Ctrl Pts',(1.9651643145003,0.342291077860937,7.54480569452101));
#12224=CARTESIAN_POINT('Ctrl Pts',(1.96424766385382,0.347514556546481,7.54514643121397));
#12225=CARTESIAN_POINT('Ctrl Pts',(1.96376266922329,0.35024481589118,7.54532426513538));
#12226=CARTESIAN_POINT('Ctrl Pts',(1.96257545985934,0.356848175993785,7.54575374694498));
#12227=CARTESIAN_POINT('Ctrl Pts',(1.96186746631204,0.360720253969869,7.54600506650521));
#12228=CARTESIAN_POINT('Ctrl Pts',(1.95935382546153,0.374241245638005,7.54688091734196));
#12229=CARTESIAN_POINT('Ctrl Pts',(1.95748838278438,0.383879100728014,7.54750213571959));
#12230=CARTESIAN_POINT('Ctrl Pts',(1.95279076986144,0.407224348149123,7.54900022816679));
#12231=CARTESIAN_POINT('Ctrl Pts',(1.949885291655,0.420916659710581,7.54987329915693));
#12232=CARTESIAN_POINT('Ctrl Pts',(1.93825608032229,0.473013595745383,7.55317779078762));
#12233=CARTESIAN_POINT('Ctrl Pts',(1.92853936526036,0.511189615960492,7.55556315091296));
#12234=CARTESIAN_POINT('Ctrl Pts',(1.89056007024004,0.643840770926139,7.5638031914185));
#12235=CARTESIAN_POINT('Ctrl Pts',(1.8564304918077,0.736489261720345,7.56947642422971));
#12236=CARTESIAN_POINT('Ctrl Pts',(1.75703781313496,0.954896110597521,7.58340853372254));
#12237=CARTESIAN_POINT('Ctrl Pts',(1.68498903147929,1.07694575235569,7.59170649840494));
#12238=CARTESIAN_POINT('Ctrl Pts',(1.59295945706711,1.20069731000528,7.60133334543289));
#12239=CARTESIAN_POINT('Ctrl Pts',(1.58516403279668,1.21097020557984,7.60214211985005));
#12240=CARTESIAN_POINT('Ctrl Pts',(1.57345963234088,1.2260877137306,7.60334702318699));
#12241=CARTESIAN_POINT('Ctrl Pts',(1.56962659733869,1.23099091786586,7.60374014991941));
#12242=CARTESIAN_POINT('Ctrl Pts',(1.56277078898525,1.23967675967138,7.60444075552367));
#12243=CARTESIAN_POINT('Ctrl Pts',(1.55975705724399,1.24346649696526,7.60474787202841));
#12244=CARTESIAN_POINT('Ctrl Pts',(1.55339176571419,1.25141123600155,7.60539474970155));
#12245=CARTESIAN_POINT('Ctrl Pts',(1.5500372696955,1.25556382594476,7.60573462745199));
#12246=CARTESIAN_POINT('Ctrl Pts',(1.54116098470617,1.26646214973071,7.60663131863999));
#12247=CARTESIAN_POINT('Ctrl Pts',(1.5356116211114,1.27318518000599,7.60718924588464));
#12248=CARTESIAN_POINT('Ctrl Pts',(1.51029214535424,1.30345326850397,7.60972303946187));
#12249=CARTESIAN_POINT('Ctrl Pts',(1.49002428157141,1.32657463127274,7.6117192262284));
#12250=CARTESIAN_POINT('Ctrl Pts',(1.43435084715314,1.38720025305192,7.61712237488871));
#12251=CARTESIAN_POINT('Ctrl Pts',(1.39801357631594,1.42381324897596,7.62056735014991));
#12252=CARTESIAN_POINT('Ctrl Pts',(1.28641579991935,1.5278634208877,7.63091109378776));
#12253=CARTESIAN_POINT('Ctrl Pts',(1.2074099424394,1.591034307249,7.63794668903852));
#12254=CARTESIAN_POINT('Ctrl Pts',(1.02458663839534,1.71572751954561,7.65338634756665));
#12255=CARTESIAN_POINT('Ctrl Pts',(0.91926443509452,1.77438970039164,7.66176633229916));
#12256=CARTESIAN_POINT('Ctrl Pts',(0.803008397587063,1.82599349694093,7.67007150315024));
#12257=CARTESIAN_POINT('Ctrl Pts',(0.796716196827393,1.82874767053753,7.67051817345978));
#12258=CARTESIAN_POINT('Ctrl Pts',(0.787231246477696,1.83284110384073,7.67118709766611));
#12259=CARTESIAN_POINT('Ctrl Pts',(0.784049111713108,1.83420460642279,7.67141077677652));
#12260=CARTESIAN_POINT('Ctrl Pts',(0.77853380724305,1.8365508658078,7.67179715877749));
#12261=CARTESIAN_POINT('Ctrl Pts',(0.776202299677492,1.83753747223605,7.67196009435165));
#12262=CARTESIAN_POINT('Ctrl Pts',(0.771368718279766,1.83957202125561,7.6722970451981));
#12263=CARTESIAN_POINT('Ctrl Pts',(0.768866380526226,1.84061930065361,7.67247101785099));
#12264=CARTESIAN_POINT('Ctrl Pts',(0.762844891113841,1.84312499463655,7.67288855335545));
#12265=CARTESIAN_POINT('Ctrl Pts',(0.759323659112666,1.84457844914495,7.6731318151839));
#12266=CARTESIAN_POINT('Ctrl Pts',(0.751798009799821,1.84765960046673,7.67364983723874));
#12267=CARTESIAN_POINT('Ctrl Pts',(0.74779241287204,1.84928438992299,7.67392442546535));
#12268=CARTESIAN_POINT('Ctrl Pts',(0.736741427233352,1.85372522192481,7.67467894707545));
#12269=CARTESIAN_POINT('Ctrl Pts',(0.729685119287649,1.85651414212947,7.67515733607856));
#12270=CARTESIAN_POINT('Ctrl Pts',(0.666922456711792,1.88090720403825,7.67938382986364));
#12271=CARTESIAN_POINT('Ctrl Pts',(0.610281647414656,1.90004085858221,7.68299927293976));
#12272=CARTESIAN_POINT('Ctrl Pts',(0.430727789222,1.951834785073,7.69409530373554));
#12273=CARTESIAN_POINT('Ctrl Pts',(0.305502023434583,1.9753118591386,7.70132961021421));
#12274=CARTESIAN_POINT('Ctrl Pts',(0.074688402749332,1.9960949308181,7.71491414429359));
#12275=CARTESIAN_POINT('Ctrl Pts',(-0.0300741819228045,1.99726419872849,
7.72117046548653));
#12276=CARTESIAN_POINT('Ctrl Pts',(-0.147248343016588,1.98934923586138,
7.72850192178656));
#12277=CARTESIAN_POINT('Ctrl Pts',(-0.160051361091155,1.98836012992434,
7.72930730650042));
#12278=CARTESIAN_POINT('Ctrl Pts',(-0.179033273300147,1.98670915086992,
7.73050812074171));
#12279=CARTESIAN_POINT('Ctrl Pts',(-0.185220237068421,1.98614189459371,
7.7309005779782));
#12280=CARTESIAN_POINT('Ctrl Pts',(-0.196222715304694,1.98508126797529,
7.73160043109354));
#12281=CARTESIAN_POINT('Ctrl Pts',(-0.201039295273785,1.98459925313573,
7.73190746743925));
#12282=CARTESIAN_POINT('Ctrl Pts',(-0.211169396991009,1.98354823622688,
7.73255462794128));
#12283=CARTESIAN_POINT('Ctrl Pts',(-0.216482474760609,1.98297540500871,
7.73289487040154));
#12284=CARTESIAN_POINT('Ctrl Pts',(-0.230481798875473,1.9814091300373,7.73379355535302));
#12285=CARTESIAN_POINT('Ctrl Pts',(-0.239163851510388,1.98037992524209,
7.73435312062968));
#12286=CARTESIAN_POINT('Ctrl Pts',(-0.278598851162377,1.9754420421766,7.73690506007576));
#12287=CARTESIAN_POINT('Ctrl Pts',(-0.309263450472154,1.97087404980394,
7.73891811286941));
#12288=CARTESIAN_POINT('Ctrl Pts',(-0.391207133474379,1.95670779418995,
7.74437813661366));
#12289=CARTESIAN_POINT('Ctrl Pts',(-0.44223403973368,1.94581003048356,7.74786411260748));
#12290=CARTESIAN_POINT('Ctrl Pts',(-0.595433162492025,1.90675411245586,
7.75858722276122));
#12291=CARTESIAN_POINT('Ctrl Pts',(-0.695838376719188,1.87244684474971,
7.76597842956949));
#12292=CARTESIAN_POINT('Ctrl Pts',(-0.897946628224816,1.78487872210169,
7.78134165407321));
#12293=CARTESIAN_POINT('Ctrl Pts',(-0.998769818620894,1.7304813526263,7.78928449099847));
#12294=CARTESIAN_POINT('Ctrl Pts',(-1.10075106228303,1.66356022475537,7.79725028667874));
#12295=CARTESIAN_POINT('Ctrl Pts',(-1.10709229512563,1.65934691282602,7.79774525247533));
#12296=CARTESIAN_POINT('Ctrl Pts',(-1.11636798956632,1.6531070107846,7.79846856928922));
#12297=CARTESIAN_POINT('Ctrl Pts',(-1.11932129240937,1.65110875537549,7.79869876244862));
#12298=CARTESIAN_POINT('Ctrl Pts',(-1.12445516726062,1.6476149824771,7.79909871353418));
#12299=CARTESIAN_POINT('Ctrl Pts',(-1.12663814375659,1.6461230352043,7.7992687114782));
#12300=CARTESIAN_POINT('Ctrl Pts',(-1.12882584223643,1.6446214702738,7.79943900766025));
#12301=CARTESIAN_POINT('Ctrl Pts',(-1.12883350313277,1.64461621200567,7.79943960400361));
#12302=CARTESIAN_POINT('Ctrl Pts',(-1.12884878447753,1.64460572307439,7.79944079354019));
#12303=CARTESIAN_POINT('Ctrl Pts',(-1.12885639273591,1.64460050077967,7.79944138578447));
#12304=CARTESIAN_POINT('Ctrl Pts',(-1.12887155391961,1.64459009401593,7.79944256596414));
#12305=CARTESIAN_POINT('Ctrl Pts',(-1.12887910629555,1.64458490992518,7.79944315385677));
#12306=CARTESIAN_POINT('Ctrl Pts',(-1.1288941564389,1.64457457907543,7.79944432538958));
#12307=CARTESIAN_POINT('Ctrl Pts',(-1.1289016535973,1.64456943273561,7.79944490898237));
#12308=CARTESIAN_POINT('Ctrl Pts',(-1.12891659392282,1.64455917696735,7.79944607196355));
#12309=CARTESIAN_POINT('Ctrl Pts',(-1.12892403648006,1.64455406795867,7.79944665130449));
#12310=CARTESIAN_POINT('Ctrl Pts',(-1.12893886834671,1.64454388634561,7.79944780583991));
#12311=CARTESIAN_POINT('Ctrl Pts',(-1.12894625698808,1.64453881420089,7.7994483809824));
#12312=CARTESIAN_POINT('Ctrl Pts',(-1.12896098144157,1.64452870603161,7.79944952715351));
#12313=CARTESIAN_POINT('Ctrl Pts',(-1.12896831670578,1.64452367038424,7.7994500981395));
#12314=CARTESIAN_POINT('Ctrl Pts',(-1.12898293515746,1.64451363469618,7.79945123605625));
#12315=CARTESIAN_POINT('Ctrl Pts',(-1.12899021768419,1.64450863511014,7.79945180293558));
#12316=CARTESIAN_POINT('Ctrl Pts',(-1.12900473129285,1.64449867111398,7.79945293268822));
#12317=CARTESIAN_POINT('Ctrl Pts',(-1.12901196169899,1.64449370716885,7.79945349550894));
#12318=CARTESIAN_POINT('Ctrl Pts',(-1.12902637157479,1.64448381410851,7.79945461718396));
#12319=CARTESIAN_POINT('Ctrl Pts',(-1.12903355041035,1.64447888542969,7.79945517598891));
#12320=CARTESIAN_POINT('Ctrl Pts',(-1.12904785782266,1.64446906243968,7.79945628968519));
#12321=CARTESIAN_POINT('Ctrl Pts',(-1.12905498568997,1.64446416861658,7.79945684452129));
#12322=CARTESIAN_POINT('Ctrl Pts',(-1.1290691917274,1.64445441495536,7.79945795032362));
#12323=CARTESIAN_POINT('Ctrl Pts',(-1.12907626917904,1.64444955561151,7.79945850123392));
#12324=CARTESIAN_POINT('Ctrl Pts',(-1.12909037504845,1.64443987045622,7.7994595992363));
#12325=CARTESIAN_POINT('Ctrl Pts',(-1.12909740268166,1.64443504518442,7.79946014626732));
#12326=CARTESIAN_POINT('Ctrl Pts',(-1.12911140940098,1.64442542784179,7.79946123654905));
#12327=CARTESIAN_POINT('Ctrl Pts',(-1.12911838773864,1.64442063628581,7.79946177974152));
#12328=CARTESIAN_POINT('Ctrl Pts',(-1.12913229651027,1.64441108593581,7.79946286239626));
#12329=CARTESIAN_POINT('Ctrl Pts',(-1.12913922613612,1.6444063276976,7.79946340179564));
#12330=CARTESIAN_POINT('Ctrl Pts',(-1.12915303793578,1.64439684367569,7.7994644768994));
#12331=CARTESIAN_POINT('Ctrl Pts',(-1.12915991935299,1.64439211841245,7.79946501254489));
#12332=CARTESIAN_POINT('Ctrl Pts',(-1.1291736353442,1.64438269992505,7.79946608018829));
#12333=CARTESIAN_POINT('Ctrl Pts',(-1.12918046910672,1.64437800725904,7.79946661212303));
#12334=CARTESIAN_POINT('Ctrl Pts',(-1.12919409029006,1.64436865362434,7.79946767238401));
#12335=CARTESIAN_POINT('Ctrl Pts',(-1.12920087691404,1.64436399320373,7.79946820064823));
#12336=CARTESIAN_POINT('Ctrl Pts',(-1.12921440430238,1.64435470373135,7.79946925360569));
#12337=CARTESIAN_POINT('Ctrl Pts',(-1.12922114426384,1.64435007523182,7.79946977823644));
#12338=CARTESIAN_POINT('Ctrl Pts',(-1.12923457904166,1.64434084911344,7.79947082398263));
#12339=CARTESIAN_POINT('Ctrl Pts',(-1.12924127293075,1.64433625213223,7.79947134502589));
#12340=CARTESIAN_POINT('Ctrl Pts',(-1.12925461583179,1.64432708886894,7.79947238361798));
#12341=CARTESIAN_POINT('Ctrl Pts',(-1.12926126403854,1.64432252314068,7.79947290110413));
#12342=CARTESIAN_POINT('Ctrl Pts',(-1.12927451638761,1.64431342182757,7.79947393264529));
#12343=CARTESIAN_POINT('Ctrl Pts',(-1.12928111951491,1.64430888694064,7.79947444662129));
#12344=CARTESIAN_POINT('Ctrl Pts',(-1.12929428204093,1.6442998470819,7.79947547116831));
#12345=CARTESIAN_POINT('Ctrl Pts',(-1.12930084054295,1.64429534272677,7.79947598166954));
#12346=CARTESIAN_POINT('Ctrl Pts',(-1.12931391423852,1.64428636364544,7.79947699929973));
#12347=CARTESIAN_POINT('Ctrl Pts',(-1.12932042855701,1.64428188952106,7.79947750636059));
#12348=CARTESIAN_POINT('Ctrl Pts',(-1.12933341448615,1.64427297049101,7.79947851715683));
#12349=CARTESIAN_POINT('Ctrl Pts',(-1.12933988513022,1.64426852625001,7.79947902081697));
#12350=CARTESIAN_POINT('Ctrl Pts',(-1.12935278414045,1.64425966669371,7.79948002484528));
#12351=CARTESIAN_POINT('Ctrl Pts',(-1.12935921155788,1.6442552520308,7.79948052513959));
#12352=CARTESIAN_POINT('Ctrl Pts',(-1.129372024619,1.64424645128663,7.79948152247549));
#12353=CARTESIAN_POINT('Ctrl Pts',(-1.12937840927727,1.64424206588296,7.79948201944037));
#12354=CARTESIAN_POINT('Ctrl Pts',(-1.12939113730432,1.64423332332683,7.79948301015514));
#12355=CARTESIAN_POINT('Ctrl Pts',(-1.12939747967533,1.64422896686044,7.79948350382736));
#12356=CARTESIAN_POINT('Ctrl Pts',(-1.12941012345138,1.64422028195881,7.79948448798199));
#12357=CARTESIAN_POINT('Ctrl Pts',(-1.12941642390336,1.64421595417894,7.79948497839023));
#12358=CARTESIAN_POINT('Ctrl Pts',(-1.12942898457574,1.64420732614796,7.79948595607408));
#12359=CARTESIAN_POINT('Ctrl Pts',(-1.12943524365278,1.64420302668297,7.7994864432607));
#12360=CARTESIAN_POINT('Ctrl Pts',(-1.12944772185695,1.64419445509034,7.79948741452328));
#12361=CARTESIAN_POINT('Ctrl Pts',(-1.12945393996183,1.64419018366563,7.79948789851966));
#12362=CARTESIAN_POINT('Ctrl Pts',(-1.12946633655248,1.64418166792836,7.79948886342754));
#12363=CARTESIAN_POINT('Ctrl Pts',(-1.12947251404302,1.64417742430017,7.79948934426156));
#12364=CARTESIAN_POINT('Ctrl Pts',(-1.12948483010306,1.6441689636784,7.79949030289906));
#12365=CARTESIAN_POINT('Ctrl Pts',(-1.1294909674934,1.64416474749555,7.79949078061075));
#12366=CARTESIAN_POINT('Ctrl Pts',(-1.12950320365697,1.64415634155764,7.79949173302728));
#12367=CARTESIAN_POINT('Ctrl Pts',(-1.129509301343,1.64415215255014,7.79949220764749));
#12368=CARTESIAN_POINT('Ctrl Pts',(-1.12952145844548,1.6441438007261,7.79949315390811));
#12369=CARTESIAN_POINT('Ctrl Pts',(-1.12952751680522,1.6441396386362,7.79949362546628));
#12370=CARTESIAN_POINT('Ctrl Pts',(-1.12953959574272,1.64413134031427,7.79949456564078));
#12371=CARTESIAN_POINT('Ctrl Pts',(-1.12954561519649,1.6441272048551,7.79949503416964));
#12372=CARTESIAN_POINT('Ctrl Pts',(-1.1295576167294,1.64411895951666,7.79949596831725));
#12373=CARTESIAN_POINT('Ctrl Pts',(-1.12956359766323,1.6441148504249,7.79949643384687));
#12374=CARTESIAN_POINT('Ctrl Pts',(-1.12957553990149,1.64410664563144,7.79949736337723));
#12375=CARTESIAN_POINT('Ctrl Pts',(-1.12958150011876,1.64410255067646,7.7994978272935));
#12376=CARTESIAN_POINT('Ctrl Pts',(-1.12959331502839,1.64409443317423,7.7994987469112));
#12377=CARTESIAN_POINT('Ctrl Pts',(-1.12959922053442,1.6440903757152,7.79949920656787));
#12378=CARTESIAN_POINT('Ctrl Pts',(-1.12961099424549,1.64408228633193,7.7995001229769));
#12379=CARTESIAN_POINT('Ctrl Pts',(-1.12961686242387,1.64407825442658,7.79950057972719));
#12380=CARTESIAN_POINT('Ctrl Pts',(-1.1321026690405,1.6423702879494,7.79969406254519));
#12381=CARTESIAN_POINT('Ctrl Pts',(-1.13457876906356,1.64066073064219,7.7998867032622));
#12382=CARTESIAN_POINT('Ctrl Pts',(-1.13967656474752,1.63712403371453,7.80028315440653));
#12383=CARTESIAN_POINT('Ctrl Pts',(-1.1422977591648,1.63529618227094,7.80048691606186));
#12384=CARTESIAN_POINT('Ctrl Pts',(-1.14887621928734,1.63068525484135,7.80099811394823));
#12385=CARTESIAN_POINT('Ctrl Pts',(-1.15282780041494,1.6278940479461,7.80130501243175));
#12386=CARTESIAN_POINT('Ctrl Pts',(-1.1640207951718,1.61992665889257,7.80217394976679));
#12387=CARTESIAN_POINT('Ctrl Pts',(-1.17123787698936,1.6147162704329,7.80273379357753));
#12388=CARTESIAN_POINT('Ctrl Pts',(-1.24450432988161,1.56107170669042,7.80841548203265));
#12389=CARTESIAN_POINT('Ctrl Pts',(-1.30755434317338,1.50865530586343,7.81329181922092));
#12390=CARTESIAN_POINT('Ctrl Pts',(-1.44818887621015,1.3762792306951,7.82460687486772));
#12391=CARTESIAN_POINT('Ctrl Pts',(-1.52265231535625,1.2934163807026,7.83096862600547));
#12392=CARTESIAN_POINT('Ctrl Pts',(-1.59495836704808,1.19800153550023,7.83801163344411));
#12393=CARTESIAN_POINT('Ctrl Pts',(-1.60005083122588,1.19119150737489,7.8385128050549));
#12394=CARTESIAN_POINT('Ctrl Pts',(-1.62756465856201,1.15390315248315,7.84124956555442));
#12395=CARTESIAN_POINT('Ctrl Pts',(-1.64915803002073,1.1228253570584,7.84350391461993));
#12396=CARTESIAN_POINT('Ctrl Pts',(-1.69851187560312,1.04729637387332,7.84894666167827));
#12397=CARTESIAN_POINT('Ctrl Pts',(-1.72542882828057,1.00233073420163,7.8521589330171));
#12398=CARTESIAN_POINT('Ctrl Pts',(-1.75526152709308,0.947724318018689,
7.85605225274669));
#12399=CARTESIAN_POINT('Ctrl Pts',(-1.75991572893285,0.939053264177024,
7.85667022954452));
#12400=CARTESIAN_POINT('Ctrl Pts',(-1.76738783374599,0.924881613775711,
7.85767998412094));
#12401=CARTESIAN_POINT('Ctrl Pts',(-1.77024470947094,0.919401664979605,
7.85807038084249));
#12402=CARTESIAN_POINT('Ctrl Pts',(-1.77529200205676,0.909609401506133,
7.85876792543009));
#12403=CARTESIAN_POINT('Ctrl Pts',(-1.77749229614253,0.905302210509712,
7.85907472247838));
#12404=CARTESIAN_POINT('Ctrl Pts',(-1.78209865543059,0.896203488400793,
7.85972278901815));
#12405=CARTESIAN_POINT('Ctrl Pts',(-1.78450110669329,0.891410180328937,
7.86006418220649));
#12406=CARTESIAN_POINT('Ctrl Pts',(-1.79080568035827,0.878703829739025,
7.86096915678257));
#12407=CARTESIAN_POINT('Ctrl Pts',(-1.79467464395518,0.870774553714571,
7.86153388946256));
#12408=CARTESIAN_POINT('Ctrl Pts',(-1.81225485171914,0.834129780455785,
7.86414396085249));
#12409=CARTESIAN_POINT('Ctrl Pts',(-1.82532968640814,0.805115817549437,
7.86621114827469));
#12410=CARTESIAN_POINT('Ctrl Pts',(-1.85873901079451,0.725976562968527,
7.87185508999053));
#12411=CARTESIAN_POINT('Ctrl Pts',(-1.87773676530586,0.67531951160803,7.87547415614104));
#12412=CARTESIAN_POINT('Ctrl Pts',(-1.92440635302603,0.533606801034589,
7.8856092143321));
#12413=CARTESIAN_POINT('Ctrl Pts',(-1.94765785277755,0.441250752980717,
7.89223205196852));
#12414=CARTESIAN_POINT('Ctrl Pts',(-1.98454972412004,0.232778735486161,
7.90700343017225));
#12415=CARTESIAN_POINT('Ctrl Pts',(-1.99476344435805,0.116390624358837,
7.91513345943431));
#12416=CARTESIAN_POINT('Ctrl Pts',(-1.99474998671859,-0.000230187268986486,
7.92279853500751));
#12417=CARTESIAN_POINT('',(-1.99474934551713,-0.00070464336927533,9.51915475821937));
#12418=CARTESIAN_POINT('Ctrl Pts',(-1.99474998656462,-0.000231517709445007,
7.92279862245266));
#12419=CARTESIAN_POINT('Ctrl Pts',(-1.99474919835786,-0.00702268470821122,
7.92324498174364));
#12420=CARTESIAN_POINT('Ctrl Pts',(-1.9947137291373,-0.0138139320109587,
7.92368967326531));
#12421=CARTESIAN_POINT('Ctrl Pts',(-1.99458019797554,-0.0267402687567622,
7.92453274020215));
#12422=CARTESIAN_POINT('Ctrl Pts',(-1.99448851188337,-0.0328753170553419,
7.92493143649948));
#12423=CARTESIAN_POINT('Ctrl Pts',(-1.99431154685697,-0.0419225873353665,
7.9255171731148));
#12424=CARTESIAN_POINT('Ctrl Pts',(-1.99424819438127,-0.0448351282615908,
7.92570539763462));
#12425=CARTESIAN_POINT('Ctrl Pts',(-1.99411820777729,-0.0502640251753199,
7.92605559865818));
#12426=CARTESIAN_POINT('Ctrl Pts',(-1.99405319072349,-0.0527804088123176,
7.92621766454593));
#12427=CARTESIAN_POINT('Ctrl Pts',(-1.99390931282479,-0.0579686071675126,
7.92655126521432));
#12428=CARTESIAN_POINT('Ctrl Pts',(-1.9938298451588,-0.060640381030368,
7.92672276224302));
#12429=CARTESIAN_POINT('Ctrl Pts',(-1.99363054664146,-0.0669164489115221,
7.92712492753491));
#12430=CARTESIAN_POINT('Ctrl Pts',(-1.99350631081618,-0.0705206130981336,
7.92735534875611));
#12431=CARTESIAN_POINT('Ctrl Pts',(-1.99307033130641,-0.0822450767397962,
7.92810324740931));
#12432=CARTESIAN_POINT('Ctrl Pts',(-1.99271873610237,-0.0903639440833199,
7.92861854138705));
#12433=CARTESIAN_POINT('Ctrl Pts',(-1.99112077054334,-0.122691678963774,
7.93066076785591));
#12434=CARTESIAN_POINT('Ctrl Pts',(-1.98948272109989,-0.146880213706721,
7.93216743237205));
#12435=CARTESIAN_POINT('Ctrl Pts',(-1.96990370952836,-0.374386901190947,
7.94618719422936));
#12436=CARTESIAN_POINT('Ctrl Pts',(-1.92129704506945,-0.573870850494195,
7.9574542476288));
#12437=CARTESIAN_POINT('Ctrl Pts',(-1.82542117175168,-0.805630745843469,
7.97241777499219));
#12438=CARTESIAN_POINT('Ctrl Pts',(-1.80608487406229,-0.848092158331292,
7.97523691016454));
#12439=CARTESIAN_POINT('Ctrl Pts',(-1.77684988749654,-0.906746435730694,
7.97926637794183));
#12440=CARTESIAN_POINT('Ctrl Pts',(-1.76818095249556,-0.923537061250847,
7.98043587306774));
#12441=CARTESIAN_POINT('Ctrl Pts',(-1.75256448426842,-0.9527580954185,7.98250096788063));
#12442=CARTESIAN_POINT('Ctrl Pts',(-1.74571986294223,-0.965242147521277,
7.98339295341556));
#12443=CARTESIAN_POINT('Ctrl Pts',(-1.73556681296389,-0.983299232066698,
7.98469781058864));
#12444=CARTESIAN_POINT('Ctrl Pts',(-1.73236382907274,-0.988931293951964,
7.98510690084292));
#12445=CARTESIAN_POINT('Ctrl Pts',(-1.72670129708155,-0.99877624631566,
7.98582573690936));
#12446=CARTESIAN_POINT('Ctrl Pts',(-1.72425361484388,-1.00299592748575,
7.98613505222859));
#12447=CARTESIAN_POINT('Ctrl Pts',(-1.71947348729546,-1.01116741736087,
7.98673642439877));
#12448=CARTESIAN_POINT('Ctrl Pts',(-1.71714283365613,-1.01512024297024,
7.98702841475435));
#12449=CARTESIAN_POINT('Ctrl Pts',(-1.71090263653403,-1.02562073265587,
7.98780699131351));
#12450=CARTESIAN_POINT('Ctrl Pts',(-1.70696917877913,-1.0321540287064,7.98829444805345));
#12451=CARTESIAN_POINT('Ctrl Pts',(-1.69271464262985,-1.05552582146159,
7.9900492905339));
#12452=CARTESIAN_POINT('Ctrl Pts',(-1.68218136141572,-1.07223292328785,
7.99132444840849));
#12453=CARTESIAN_POINT('Ctrl Pts',(-1.66884153951536,-1.09271107114892,
7.99291382923818));
#12454=CARTESIAN_POINT('Ctrl Pts',(-1.66626718369475,-1.09663268278067,
7.99321941368867));
#12455=CARTESIAN_POINT('Ctrl Pts',(-1.66090678184472,-1.10473592887662,
7.99385337348201));
#12456=CARTESIAN_POINT('Ctrl Pts',(-1.65811872343561,-1.10891618653504,
7.99418182144609));
#12457=CARTESIAN_POINT('Ctrl Pts',(-1.54641487542538,-1.27503549262519,
8.00729026365598));
#12458=CARTESIAN_POINT('Ctrl Pts',(-1.41435187244186,-1.42010220360328,
8.02102892779902));
#12459=CARTESIAN_POINT('Ctrl Pts',(-1.21893814355199,-1.58003710125661,
8.03852744183577));
#12460=CARTESIAN_POINT('Ctrl Pts',(-1.17292969788131,-1.6144857948274,8.04246923023262));
#12461=CARTESIAN_POINT('Ctrl Pts',(-1.11059261661262,-1.65708702467915,
8.04752320495543));
#12462=CARTESIAN_POINT('Ctrl Pts',(-1.09555200119732,-1.66706905417847,
8.04872166226926));
#12463=CARTESIAN_POINT('Ctrl Pts',(-1.07361269850618,-1.68120435789523,
8.05043747729061));
#12464=CARTESIAN_POINT('Ctrl Pts',(-1.06682156507247,-1.68552189923614,
8.05096418717117));
#12465=CARTESIAN_POINT('Ctrl Pts',(-1.05618823450231,-1.69219214897676,
8.05178181791416));
#12466=CARTESIAN_POINT('Ctrl Pts',(-1.05236396941016,-1.69457308269347,
8.05207446212659));
#12467=CARTESIAN_POINT('Ctrl Pts',(-1.04593049403554,-1.69854829581648,
8.05256435595975));
#12468=CARTESIAN_POINT('Ctrl Pts',(-1.04332564768817,-1.70014955364336,
8.0527620474876));
#12469=CARTESIAN_POINT('Ctrl Pts',(-1.03823511504251,-1.70326271392913,
8.05314708246664));
#12470=CARTESIAN_POINT('Ctrl Pts',(-1.03574978391139,-1.70477517936031,
8.05333446225131));
#12471=CARTESIAN_POINT('Ctrl Pts',(-1.0310057685985,-1.70764797882935,8.0536909700158));
#12472=CARTESIAN_POINT('Ctrl Pts',(-1.02874770181923,-1.7090092687151,8.05386015889986));
#12473=CARTESIAN_POINT('Ctrl Pts',(-1.02344977615187,-1.71218885201387,
8.05425594981016));
#12474=CARTESIAN_POINT('Ctrl Pts',(-1.02040774598619,-1.71400354190723,
8.05448231577532));
#12475=CARTESIAN_POINT('Ctrl Pts',(-1.01067197355746,-1.7197762050327,8.05520398229661));
#12476=CARTESIAN_POINT('Ctrl Pts',(-1.00395981102077,-1.72370320419505,
8.05569730724738));
#12477=CARTESIAN_POINT('Ctrl Pts',(-0.902753986074565,-1.78212267676023,
8.0630751798442));
#12478=CARTESIAN_POINT('Ctrl Pts',(-0.803953758096544,-1.82882250889825,
8.06949343634463));
#12479=CARTESIAN_POINT('Ctrl Pts',(-0.629559763123477,-1.8943707784932,
8.08033655778919));
#12480=CARTESIAN_POINT('Ctrl Pts',(-0.555788473304771,-1.91731198279,8.084785291036));
#12481=CARTESIAN_POINT('Ctrl Pts',(-0.454905773957928,-1.94237077750035,
8.09086659107214));
#12482=CARTESIAN_POINT('Ctrl Pts',(-0.428811250243471,-1.9482978100742,
8.09243907652897));
#12483=CARTESIAN_POINT('Ctrl Pts',(-0.346881013560604,-1.96518148219439,
8.09738878169408));
#12484=CARTESIAN_POINT('Ctrl Pts',(-0.290694259826521,-1.97427474120783,
8.10080208088731));
#12485=CARTESIAN_POINT('Ctrl Pts',(-0.201428744960775,-1.98482818203363,
8.10630827741049));
#12486=CARTESIAN_POINT('Ctrl Pts',(-0.168569171068974,-1.98788849989265,
8.10835258875764));
#12487=CARTESIAN_POINT('Ctrl Pts',(-0.126736832157239,-1.99073985135108,
8.11098304894076));
#12488=CARTESIAN_POINT('Ctrl Pts',(-0.117819566576094,-1.99128750458934,
8.11154537490469));
#12489=CARTESIAN_POINT('Ctrl Pts',(-0.10352060763326,-1.99206929103457,
8.11244974942427));
#12490=CARTESIAN_POINT('Ctrl Pts',(-0.0981410516170769,-1.99234156447808,
8.11279060004348));
#12491=CARTESIAN_POINT('Ctrl Pts',(-0.0879340962046485,-1.99281672561594,
8.11343849411302));
#12492=CARTESIAN_POINT('Ctrl Pts',(-0.0831069257959719,-1.99302386974665,
8.11374540174689));
#12493=CARTESIAN_POINT('Ctrl Pts',(-0.0721477659788656,-1.9934542666989,
8.11444333136067));
#12494=CARTESIAN_POINT('Ctrl Pts',(-0.066015425865769,-1.99366676646652,
8.11483468753223));
#12495=CARTESIAN_POINT('Ctrl Pts',(-0.0501893533174395,-1.99414207830848,
8.11584684511366));
#12496=CARTESIAN_POINT('Ctrl Pts',(-0.0404945990617473,-1.9943625000474,
8.11646896763902));
#12497=CARTESIAN_POINT('Ctrl Pts',(0.0192962539183146,-1.995285775576,8.12031909035055));
#12498=CARTESIAN_POINT('Ctrl Pts',(0.0693984906723488,-1.99417170078574,
8.1236035006446));
#12499=CARTESIAN_POINT('Ctrl Pts',(0.157490198662347,-1.9888892159616,8.12948643175581));
#12500=CARTESIAN_POINT('Ctrl Pts',(0.195502802759619,-1.98551299168738,
8.13206050013074));
#12501=CARTESIAN_POINT('Ctrl Pts',(0.353603103501263,-1.96688671612717,
8.14290707675554));
#12502=CARTESIAN_POINT('Ctrl Pts',(0.472267963639652,-1.94181288727138,
8.15140849277079));
#12503=CARTESIAN_POINT('Ctrl Pts',(0.666995965587714,-1.88175251228524,
8.16556739914724));
#12504=CARTESIAN_POINT('Ctrl Pts',(0.744491046033528,-1.85246115360052,
8.17125478951414));
#12505=CARTESIAN_POINT('Ctrl Pts',(0.828106081501254,-1.81475836849115,
8.17729682884523));
#12506=CARTESIAN_POINT('Ctrl Pts',(0.836237958919359,-1.81102559375437,
8.17788338092407));
#12507=CARTESIAN_POINT('Ctrl Pts',(0.848743913290462,-1.80518279142026,
8.17878348906329));
#12508=CARTESIAN_POINT('Ctrl Pts',(0.853135743192,-1.80311135142817,8.17909921553368));
#12509=CARTESIAN_POINT('Ctrl Pts',(0.860411922989664,-1.79964694990149,
8.17962162341749));
#12510=CARTESIAN_POINT('Ctrl Pts',(0.863300530292969,-1.79826305535526,
8.17982883999635));
#12511=CARTESIAN_POINT('Ctrl Pts',(0.868898882039267,-1.79556435876297,
8.18023008086414));
#12512=CARTESIAN_POINT('Ctrl Pts',(0.87160900456911,-1.79425036634199,8.18042415384803));
#12513=CARTESIAN_POINT('Ctrl Pts',(0.876673319000713,-1.79178077110302,
8.18078648815098));
#12514=CARTESIAN_POINT('Ctrl Pts',(0.879028181403468,-1.79062667698948,
8.18095483752522));
#12515=CARTESIAN_POINT('Ctrl Pts',(0.884450720555287,-1.7879558708462,8.18134219662372));
#12516=CARTESIAN_POINT('Ctrl Pts',(0.887516769138473,-1.78643590932066,
8.18156100046291));
#12517=CARTESIAN_POINT('Ctrl Pts',(0.896806920125838,-1.78180059344639,
8.18222335731854));
#12518=CARTESIAN_POINT('Ctrl Pts',(0.903018725144317,-1.77866050506421,
8.18266539126806));
#12519=CARTESIAN_POINT('Ctrl Pts',(0.949219373216593,-1.75500149881257,
8.18594765862068));
#12520=CARTESIAN_POINT('Ctrl Pts',(0.988524499290065,-1.73316696214508,
8.18870991705859));
#12521=CARTESIAN_POINT('Ctrl Pts',(1.17079741718341,-1.62369139993394,8.20153503873979));
#12522=CARTESIAN_POINT('Ctrl Pts',(1.30308454601846,-1.51957919992771,8.21094222012277));
#12523=CARTESIAN_POINT('Ctrl Pts',(1.46158788443693,-1.35873700728124,8.22429201143942));
#12524=CARTESIAN_POINT('Ctrl Pts',(1.50055068185925,-1.31558056302475,8.22777573484626));
#12525=CARTESIAN_POINT('Ctrl Pts',(1.55891495756934,-1.2449634990721,8.23338540779656));
#12526=CARTESIAN_POINT('Ctrl Pts',(1.57960303742029,-1.21860740033364,8.23546039011382));
#12527=CARTESIAN_POINT('Ctrl Pts',(1.60498204194526,-1.18454246710169,8.23812518954213));
#12528=CARTESIAN_POINT('Ctrl Pts',(1.61029857038343,-1.17730485487386,8.23869040722485));
#12529=CARTESIAN_POINT('Ctrl Pts',(1.61873149171826,-1.16566077635638,8.23959833417471));
#12530=CARTESIAN_POINT('Ctrl Pts',(1.62187923050394,-1.16127707655951,8.23993982858464));
#12531=CARTESIAN_POINT('Ctrl Pts',(1.62781016057328,-1.15294621279992,8.24058823902225));
#12532=CARTESIAN_POINT('Ctrl Pts',(1.63059688608532,-1.14900160264908,8.24089501617111));
#12533=CARTESIAN_POINT('Ctrl Pts',(1.63688136977162,-1.14003700741539,8.24159168032751));
#12534=CARTESIAN_POINT('Ctrl Pts',(1.64037039961539,-1.13501099010945,8.2419818968755));
#12535=CARTESIAN_POINT('Ctrl Pts',(1.6506119211806,-1.12011201199589,8.24313760703068));
#12536=CARTESIAN_POINT('Ctrl Pts',(1.65729870030194,-1.11019441602274,8.2439055781069));
#12537=CARTESIAN_POINT('Ctrl Pts',(1.70571082979594,-1.03697912895236,8.24956610100389));
#12538=CARTESIAN_POINT('Ctrl Pts',(1.74388153957281,-0.971416387937629,
8.25459007936603));
#12539=CARTESIAN_POINT('Ctrl Pts',(1.80497645631379,-0.851218525839171,
8.26372797321559));
#12540=CARTESIAN_POINT('Ctrl Pts',(1.82937581102105,-0.797431070722207,
8.26779211780525));
#12541=CARTESIAN_POINT('Ctrl Pts',(1.8887550277339,-0.649403382013918,8.27886396084816));
#12542=CARTESIAN_POINT('Ctrl Pts',(1.9190598748867,-0.55347067261022,8.28592632842845));
#12543=CARTESIAN_POINT('Ctrl Pts',(1.95193545864888,-0.413356824994963,
8.29581951877102));
#12544=CARTESIAN_POINT('Ctrl Pts',(1.96047756787429,-0.37073459189691,8.29877347965395));
#12545=CARTESIAN_POINT('Ctrl Pts',(1.97133790974497,-0.305558174233478,
8.30317515152615));
#12546=CARTESIAN_POINT('Ctrl Pts',(1.9746754281152,-0.283189007121508,8.3046653631025));
#12547=CARTESIAN_POINT('Ctrl Pts',(1.97833151175884,-0.255461594712451,
8.30648332639868));
#12548=CARTESIAN_POINT('Ctrl Pts',(1.97900970236519,-0.250153545529075,
8.30683003181563));
#12549=CARTESIAN_POINT('Ctrl Pts',(1.9800447757931,-0.241784499837728,8.30737452503285));
#12550=CARTESIAN_POINT('Ctrl Pts',(1.98041593330107,-0.238725344173639,
8.30757310324985));
#12551=CARTESIAN_POINT('Ctrl Pts',(1.9810987587589,-0.232986158452578,8.30794478724546));
#12552=CARTESIAN_POINT('Ctrl Pts',(1.98141207480238,-0.230306387072146,
8.30811798165558));
#12553=CARTESIAN_POINT('Ctrl Pts',(1.98211423392382,-0.224193363413962,
8.30851226908235));
#12554=CARTESIAN_POINT('Ctrl Pts',(1.98249959365815,-0.220759738421593,
8.3087331636315));
#12555=CARTESIAN_POINT('Ctrl Pts',(1.98365243526449,-0.210241201841807,
8.30940814395487));
#12556=CARTESIAN_POINT('Ctrl Pts',(1.98439088432201,-0.203153067406235,
8.30986062437608));
#12557=CARTESIAN_POINT('Ctrl Pts',(1.98994114960749,-0.146957375157954,
8.31343027016316));
#12558=CARTESIAN_POINT('Ctrl Pts',(1.99296780040644,-0.0976858818530874,
8.31645327444844));
#12559=CARTESIAN_POINT('Ctrl Pts',(1.99451998299925,-0.0336649519246329,
8.3203011941513));
#12560=CARTESIAN_POINT('Ctrl Pts',(1.9947138020683,-0.0189777777130987,
8.32117848838709));
#12561=CARTESIAN_POINT('Ctrl Pts',(1.99486315799158,0.0504767434801115,
8.32530672653474));
#12562=CARTESIAN_POINT('Ctrl Pts',(1.9927254450652,0.105226956036382,8.32850142798983));
#12563=CARTESIAN_POINT('Ctrl Pts',(1.98018545881007,0.261236509058774,8.33759394038254));
#12564=CARTESIAN_POINT('Ctrl Pts',(1.96428684639156,0.361877236430052,8.34345376848755));
#12565=CARTESIAN_POINT('Ctrl Pts',(1.92864216957015,0.511984217938865,8.35261311640273));
#12566=CARTESIAN_POINT('Ctrl Pts',(1.91448811627231,0.562603826910618,8.35577507977248));
#12567=CARTESIAN_POINT('Ctrl Pts',(1.88878231313883,0.642261770431691,8.36091023176004));
#12568=CARTESIAN_POINT('Ctrl Pts',(1.87851806472765,0.671690792713433,8.36284281731794));
#12569=CARTESIAN_POINT('Ctrl Pts',(1.86449153788505,0.709066702808122,8.36534792026673));
#12570=CARTESIAN_POINT('Ctrl Pts',(1.86136004999609,0.717246850263437,8.3658993342113));
#12571=CARTESIAN_POINT('Ctrl Pts',(1.85623016925888,0.730387374603764,8.36679030446632));
#12572=CARTESIAN_POINT('Ctrl Pts',(1.85426550304053,0.735360864863523,8.36712872581784));
#12573=CARTESIAN_POINT('Ctrl Pts',(1.85048463770983,0.744820509920601,8.36777472869912));
#12574=CARTESIAN_POINT('Ctrl Pts',(1.84867206084681,0.749308078939836,8.36808218612897));
#12575=CARTESIAN_POINT('Ctrl Pts',(1.84449796102807,0.759534956826287,8.36878516797642));
#12576=CARTESIAN_POINT('Ctrl Pts',(1.8421259579232,0.765269908322834,8.36918104506223));
#12577=CARTESIAN_POINT('Ctrl Pts',(1.83477734615351,0.782804996250314,8.37039663610397));
#12578=CARTESIAN_POINT('Ctrl Pts',(1.82971390730288,0.79456817002563,8.37121929320982));
#12579=CARTESIAN_POINT('Ctrl Pts',(1.78312360124049,0.899997554589512,8.37865871515974));
#12580=CARTESIAN_POINT('Ctrl Pts',(1.73455774807666,0.990367994491398,8.38552067686724));
#12581=CARTESIAN_POINT('Ctrl Pts',(1.60645029012431,1.19018971634929,8.40182385625274));
#12582=CARTESIAN_POINT('Ctrl Pts',(1.52229322252373,1.29609212985326,8.41136305929429));
#12583=CARTESIAN_POINT('Ctrl Pts',(1.39927749418973,1.42223542577928,8.42345559862231));
#12584=CARTESIAN_POINT('Ctrl Pts',(1.36954868653589,1.45088523872937,8.42625671105926));
#12585=CARTESIAN_POINT('Ctrl Pts',(1.32277093468428,1.4932451421116,8.43045705871768));
#12586=CARTESIAN_POINT('Ctrl Pts',(1.30635126125194,1.50763075048331,8.4318945924608));
#12587=CARTESIAN_POINT('Ctrl Pts',(1.28566244582949,1.52516478469197,8.43365719966969));
#12588=CARTESIAN_POINT('Ctrl Pts',(1.28161330237793,1.5285689025361,8.43399990147263));
#12589=CARTESIAN_POINT('Ctrl Pts',(1.27519441749139,1.53392182740926,8.43453952770088));
#12590=CARTESIAN_POINT('Ctrl Pts',(1.27283367601301,1.53588131329318,8.43473721941486));
#12591=CARTESIAN_POINT('Ctrl Pts',(1.26838664679261,1.53955518518983,8.43510815487782));
#12592=CARTESIAN_POINT('Ctrl Pts',(1.26630142340231,1.54127076115827,8.43528148317324));
#12593=CARTESIAN_POINT('Ctrl Pts',(1.26152339202232,1.54518554912742,8.43567727277348));
#12594=CARTESIAN_POINT('Ctrl Pts',(1.25882831884873,1.54738195477544,8.43589952983252));
#12595=CARTESIAN_POINT('Ctrl Pts',(1.25050661791335,1.55412776709656,8.43658280770704));
#12596=CARTESIAN_POINT('Ctrl Pts',(1.24486088992064,1.55865367754036,8.4370421651381));
#12597=CARTESIAN_POINT('Ctrl Pts',(1.19807788950323,1.59574102996418,8.44081526606513));
#12598=CARTESIAN_POINT('Ctrl Pts',(1.15569117061557,1.62670190499935,8.44402244164942));
#12599=CARTESIAN_POINT('Ctrl Pts',(1.05512066905209,1.69424428359257,8.45128273539682));
#12600=CARTESIAN_POINT('Ctrl Pts',(0.996170117816534,1.72956338474557,8.4552871836776));
#12601=CARTESIAN_POINT('Ctrl Pts',(0.846411451135171,1.80908614897429,8.46513389694844));
#12602=CARTESIAN_POINT('Ctrl Pts',(0.753851595048748,1.84957068237211,8.47094876518043));
#12603=CARTESIAN_POINT('Ctrl Pts',(0.610060098383983,1.89986895498957,8.48000046845443));
#12604=CARTESIAN_POINT('Ctrl Pts',(0.560853055406495,1.91497222164778,8.48309942273978));
#12605=CARTESIAN_POINT('Ctrl Pts',(0.481448291601828,1.93602101458039,8.48814111088676));
#12606=CARTESIAN_POINT('Ctrl Pts',(0.451600521548301,1.9432001016132,8.49004511829261));
#12607=CARTESIAN_POINT('Ctrl Pts',(0.413084316541226,1.95152884204975,8.49251808416927));
#12608=CARTESIAN_POINT('Ctrl Pts',(0.40455656351681,1.95331447979062,8.49306660735261));
#12609=CARTESIAN_POINT('Ctrl Pts',(0.3907865517942,1.95610375975275,8.493954027109));
#12610=CARTESIAN_POINT('Ctrl Pts',(0.385551420483809,1.95714234261121,8.49429180517637));
#12611=CARTESIAN_POINT('Ctrl Pts',(0.375558802752016,1.95908310071585,8.4949373234207));
#12612=CARTESIAN_POINT('Ctrl Pts',(0.370802069172672,1.9599889884009,8.4952449426467));
#12613=CARTESIAN_POINT('Ctrl Pts',(0.359922145165043,1.96201997215704,8.49594934072553));
#12614=CARTESIAN_POINT('Ctrl Pts',(0.353796915157029,1.96313373540777,8.49634647740351));
#12615=CARTESIAN_POINT('Ctrl Pts',(0.334958041792395,1.96646821504985,8.49756972961547));
#12616=CARTESIAN_POINT('Ctrl Pts',(0.322228179310622,1.96859419840775,8.49839884256805));
#12617=CARTESIAN_POINT('Ctrl Pts',(0.17002543558183,1.99249738076289,8.50834383411671));
#12618=CARTESIAN_POINT('Ctrl Pts',(0.0286703205075798,1.99952930955107,
8.51794241227215));
#12619=CARTESIAN_POINT('Ctrl Pts',(-0.210506504120044,1.98605295207319,
8.53460073779848));
#12620=CARTESIAN_POINT('Ctrl Pts',(-0.308253603338334,1.97324599557256,
8.54151624800528));
#12621=CARTESIAN_POINT('Ctrl Pts',(-0.461585935940137,1.94148036013177,
8.5522492392706));
#12622=CARTESIAN_POINT('Ctrl Pts',(-0.517978582685788,1.92720191624104,
8.55616880575215));
#12623=CARTESIAN_POINT('Ctrl Pts',(-0.580203651643638,1.90851717021064,
8.56040474559539));
#12624=CARTESIAN_POINT('Ctrl Pts',(-0.586724945791023,1.90652246449761,
8.56084756144487));
#12625=CARTESIAN_POINT('Ctrl Pts',(-0.596476185128885,1.90348502504609,
8.56150788968686));
#12626=CARTESIAN_POINT('Ctrl Pts',(-0.599713822617182,1.90246745343574,
8.56172683405279));
#12627=CARTESIAN_POINT('Ctrl Pts',(-0.605271364915361,1.90070515168517,
8.56210212663698));
#12628=CARTESIAN_POINT('Ctrl Pts',(-0.607592510685936,1.8999644312538,8.56225870893541));
#12629=CARTESIAN_POINT('Ctrl Pts',(-0.612431897141488,1.89841031833551,
8.56258482913751));
#12630=CARTESIAN_POINT('Ctrl Pts',(-0.614949867764217,1.89759617035238,
8.56275432120036));
#12631=CARTESIAN_POINT('Ctrl Pts',(-0.621947430236766,1.89531822281732,
8.56322483628384));
#12632=CARTESIAN_POINT('Ctrl Pts',(-0.62642350324943,1.8938435435362,8.56352522298788));
#12633=CARTESIAN_POINT('Ctrl Pts',(-0.644327565861596,1.88787448163442,
8.56472457188317));
#12634=CARTESIAN_POINT('Ctrl Pts',(-0.657713158802765,1.88325290351226,
8.56561631395642));
#12635=CARTESIAN_POINT('Ctrl Pts',(-0.78716585736158,1.83700877640986,8.57420279605515));
#12636=CARTESIAN_POINT('Ctrl Pts',(-0.899204661235883,1.78484488547056,
8.58134932864037));
#12637=CARTESIAN_POINT('Ctrl Pts',(-1.07576225874995,1.68176725401699,8.59320782759595));
#12638=CARTESIAN_POINT('Ctrl Pts',(-1.14324302575928,1.63664296192731,8.59790231384253));
#12639=CARTESIAN_POINT('Ctrl Pts',(-1.25290082780132,1.5532161200711,8.60605640141695));
#12640=CARTESIAN_POINT('Ctrl Pts',(-1.29652772255488,1.51698908462148,8.60945757932838));
#12641=CARTESIAN_POINT('Ctrl Pts',(-1.36295167933405,1.45687110856619,8.61494594452384));
#12642=CARTESIAN_POINT('Ctrl Pts',(-1.38680132096748,1.434187089192,8.61698494925403));
#12643=CARTESIAN_POINT('Ctrl Pts',(-1.41639142011538,1.4046147446235,8.61960946504547));
#12644=CARTESIAN_POINT('Ctrl Pts',(-1.42266243464717,1.3982627895587,8.62017128627684));
#12645=CARTESIAN_POINT('Ctrl Pts',(-1.43264775950447,1.38801187108157,8.62107504074794));
#12646=CARTESIAN_POINT('Ctrl Pts',(-1.43638932989371,1.38413953383203,8.62141577899471));
#12647=CARTESIAN_POINT('Ctrl Pts',(-1.44345859753185,1.37676366444645,8.62206358356379));
#12648=CARTESIAN_POINT('Ctrl Pts',(-1.44678933840303,1.37326309210471,8.62237051460594));
#12649=CARTESIAN_POINT('Ctrl Pts',(-1.4543229337111,1.36528753614966,8.62306866814696));
#12650=CARTESIAN_POINT('Ctrl Pts',(-1.45851789878658,1.36080519892093,8.62346022565939));
#12651=CARTESIAN_POINT('Ctrl Pts',(-1.46929254426302,1.3491853902312,8.62447324254151));
#12652=CARTESIAN_POINT('Ctrl Pts',(-1.47584087316181,1.34201919114791,8.62509602677348));
#12653=CARTESIAN_POINT('Ctrl Pts',(-1.51597328106713,1.29745110171667,8.62895756103816));
#12654=CARTESIAN_POINT('Ctrl Pts',(-1.54818324441548,1.25884162454708,8.63225310633331));
#12655=CARTESIAN_POINT('Ctrl Pts',(-1.58164999819233,1.21549624204324,8.63590407090433));
#12656=CARTESIAN_POINT('Ctrl Pts',(-1.58438928193606,1.21192344394325,8.63620465163962));
#12657=CARTESIAN_POINT('Ctrl Pts',(-1.7025774672363,1.05668717812211,8.64924935851054));
#12658=CARTESIAN_POINT('Ctrl Pts',(-1.79569805930562,0.889271865546751,
8.66282020358993));
#12659=CARTESIAN_POINT('Ctrl Pts',(-1.88362460343772,0.658883452183352,
8.67970186574406));
#12660=CARTESIAN_POINT('Ctrl Pts',(-1.90139572804824,0.605693548269844,
8.68347600624639));
#12661=CARTESIAN_POINT('Ctrl Pts',(-1.9187777646919,0.5453121310817,8.68757229660485));
#12662=CARTESIAN_POINT('Ctrl Pts',(-1.92061818691374,0.538794222212334,
8.68801204673621));
#12663=CARTESIAN_POINT('Ctrl Pts',(-1.92332844537685,0.529005394061882,
8.68866871405302));
#12664=CARTESIAN_POINT('Ctrl Pts',(-1.92422318826357,0.525741512444485,
8.68888704017161));
#12665=CARTESIAN_POINT('Ctrl Pts',(-1.92574748824871,0.520125085498782,
8.68926163709257));
#12666=CARTESIAN_POINT('Ctrl Pts',(-1.92638104583876,0.517773656662664,
8.68941813947184));
#12667=CARTESIAN_POINT('Ctrl Pts',(-1.92769521524748,0.512860356998419,
8.68974445796068));
#12668=CARTESIAN_POINT('Ctrl Pts',(-1.92837502451171,0.510298298752017,
8.68991422698065));
#12669=CARTESIAN_POINT('Ctrl Pts',(-1.93025483735156,0.503156279105541,
8.69038640768047));
#12670=CARTESIAN_POINT('Ctrl Pts',(-1.93144365521974,0.498573350816465,
8.69068817547325));
#12671=CARTESIAN_POINT('Ctrl Pts',(-1.93616370910622,0.480107140939406,
8.69189934263267));
#12672=CARTESIAN_POINT('Ctrl Pts',(-1.93956177019794,0.466189814427429,
8.69280134190122));
#12673=CARTESIAN_POINT('Ctrl Pts',(-1.97718139401264,0.304575808395203,
8.70316365221341));
#12674=CARTESIAN_POINT('Ctrl Pts',(-1.99461257593291,0.153453720322189,
8.71179798766024));
#12675=CARTESIAN_POINT('Ctrl Pts',(-1.9948712195267,-0.133668063256788,
8.72848308371536));
#12676=CARTESIAN_POINT('Ctrl Pts',(-1.98119470638394,-0.268771511709406,
8.73645960938413));
#12677=CARTESIAN_POINT('Ctrl Pts',(-1.95133019285738,-0.414132864749555,
8.74572228903352));
#12678=CARTESIAN_POINT('Ctrl Pts',(-1.94859819806634,-0.426802766026727,
8.74653511835288));
#12679=CARTESIAN_POINT('Ctrl Pts',(-1.94436908514981,-0.445528131973983,
8.7477449112978));
#12680=CARTESIAN_POINT('Ctrl Pts',(-1.94296668538109,-0.451604820314016,
8.74813883678131));
#12681=CARTESIAN_POINT('Ctrl Pts',(-1.94042451116146,-0.462389164508565,
8.74884034143957));
#12682=CARTESIAN_POINT('Ctrl Pts',(-1.93929603772199,-0.467099454472853,
8.74914755486349));
#12683=CARTESIAN_POINT('Ctrl Pts',(-1.93688937959648,-0.476985869411982,
8.74979410163906));
#12684=CARTESIAN_POINT('Ctrl Pts',(-1.93560757738012,-0.482161066336755,
8.75013354953625));
#12685=CARTESIAN_POINT('Ctrl Pts',(-1.93218260533877,-0.495755400451982,
8.75102789131757));
#12686=CARTESIAN_POINT('Ctrl Pts',(-1.93000517328316,-0.504165711438824,
8.75158388846695));
#12687=CARTESIAN_POINT('Ctrl Pts',(-1.91994969820836,-0.541984929848783,
8.75409647391396));
#12688=CARTESIAN_POINT('Ctrl Pts',(-1.91145427515081,-0.571224029081828,
8.75607296827559));
#12689=CARTESIAN_POINT('Ctrl Pts',(-1.88698279356925,-0.648777507387629,
8.76140996467395));
#12690=CARTESIAN_POINT('Ctrl Pts',(-1.86982252687338,-0.696691679811968,
8.76480734494315));
#12691=CARTESIAN_POINT('Ctrl Pts',(-1.81338344907362,-0.837115270440164,
8.77506133297987));
#12692=CARTESIAN_POINT('Ctrl Pts',(-1.76892982573233,-0.927364797288488,
8.78205501589821));
#12693=CARTESIAN_POINT('Ctrl Pts',(-1.655881647942,-1.11890972469254,8.79757326434299));
#12694=CARTESIAN_POINT('Ctrl Pts',(-1.58437979116762,-1.21805214954246,
8.80607587102078));
#12695=CARTESIAN_POINT('Ctrl Pts',(-1.49928347115201,-1.3157636743316,8.81453558878648));
#12696=CARTESIAN_POINT('Ctrl Pts',(-1.49427466625688,-1.32144928007537,
8.81502809347339));
#12697=CARTESIAN_POINT('Ctrl Pts',(-1.48690171831705,-1.32972295103032,
8.81574497790965));
#12698=CARTESIAN_POINT('Ctrl Pts',(-1.4845630329989,-1.33233345974091,8.81597119772909));
#12699=CARTESIAN_POINT('Ctrl Pts',(-1.48040331329187,-1.33695210871287,
8.81637146659798));
#12700=CARTESIAN_POINT('Ctrl Pts',(-1.47858505316461,-1.33896271490548,
8.81654572205943));
#12701=CARTESIAN_POINT('Ctrl Pts',(-1.47473391977586,-1.3432038325526,8.81691330412691));
#12702=CARTESIAN_POINT('Ctrl Pts',(-1.47270008733336,-1.34543343313088,
8.81710655555436));
#12703=CARTESIAN_POINT('Ctrl Pts',(-1.4672394448791,-1.35139247642033,8.81762311138456));
#12704=CARTESIAN_POINT('Ctrl Pts',(-1.46380344945119,-1.35511352906802,
8.81794572494267));
#12705=CARTESIAN_POINT('Ctrl Pts',(-1.44729277991712,-1.37285788345148,
8.81948465836798));
#12706=CARTESIAN_POINT('Ctrl Pts',(-1.43403000936744,-1.3867058653566,8.82068718836113));
#12707=CARTESIAN_POINT('Ctrl Pts',(-1.39649112352568,-1.42478645771653,
8.82400573882597));
#12708=CARTESIAN_POINT('Ctrl Pts',(-1.37178574784152,-1.44858829811479,
8.82609361627723));
#12709=CARTESIAN_POINT('Ctrl Pts',(-1.27943561048134,-1.53307819133598,
8.83361080412467));
#12710=CARTESIAN_POINT('Ctrl Pts',(-1.20827651075083,-1.58976549836233,
8.83886715203368));
#12711=CARTESIAN_POINT('Ctrl Pts',(-1.00427656197088,-1.73064050114208,
8.85324523900114));
#12712=CARTESIAN_POINT('Ctrl Pts',(-0.864994015592043,-1.80429043552511,
8.86238813070886));
#12713=CARTESIAN_POINT('Ctrl Pts',(-0.706829196491486,-1.86536250943538,
8.87297601545846));
#12714=CARTESIAN_POINT('Ctrl Pts',(-0.695089226714996,-1.86976890552744,
8.87376268101761));
#12715=CARTESIAN_POINT('Ctrl Pts',(-0.677527657379335,-1.87617208685013,
8.87494088959773));
#12716=CARTESIAN_POINT('Ctrl Pts',(-0.671736943825578,-1.87825315197675,
8.87532962284469));
#12717=CARTESIAN_POINT('Ctrl Pts',(-0.661380480805454,-1.88192103595676,
8.87602531193258));
#12718=CARTESIAN_POINT('Ctrl Pts',(-0.656818398393524,-1.88351812224486,
8.876331923984));
#12719=CARTESIAN_POINT('Ctrl Pts',(-0.647169572322146,-1.88685664919923,
8.87698076170768));
#12720=CARTESIAN_POINT('Ctrl Pts',(-0.642081510127311,-1.88859413410776,
8.87732311553629));
#12721=CARTESIAN_POINT('Ctrl Pts',(-0.628562330140101,-1.89314975243665,
8.87823334129869));
#12722=CARTESIAN_POINT('Ctrl Pts',(-0.620119367098661,-1.89593210699305,
8.87880238854272));
#12723=CARTESIAN_POINT('Ctrl Pts',(-0.580702202905509,-1.90863046183729,
8.88146206344512));
#12724=CARTESIAN_POINT('Ctrl Pts',(-0.549508575655639,-1.9178439472601,
8.88357556558254));
#12725=CARTESIAN_POINT('Ctrl Pts',(-0.464265935569141,-1.94077125358747,
8.88937853642262));
#12726=CARTESIAN_POINT('Ctrl Pts',(-0.409847888416812,-1.95298737070563,
8.89311330066537));
#12727=CARTESIAN_POINT('Ctrl Pts',(-0.252367966201468,-1.98146775926962,
8.9039984746494));
#12728=CARTESIAN_POINT('Ctrl Pts',(-0.148451749659453,-1.99194952987044,
8.9112833732864));
#12729=CARTESIAN_POINT('Ctrl Pts',(0.0322676069675566,-1.99595513025144,
8.9238876027556));
#12730=CARTESIAN_POINT('Ctrl Pts',(0.108777153001586,-1.9932504154117,8.92919992888788));
#12731=CARTESIAN_POINT('Ctrl Pts',(0.220691514846194,-1.98282918575057,
8.93678782057855));
#12732=CARTESIAN_POINT('Ctrl Pts',(0.256342683274169,-1.97853611292099,
8.93917699825019));
#12733=CARTESIAN_POINT('Ctrl Pts',(0.297687922397998,-1.97242088751557,
8.94190050405145));
#12734=CARTESIAN_POINT('Ctrl Pts',(0.303510950166099,-1.97153325153051,
8.94228298133976));
#12735=CARTESIAN_POINT('Ctrl Pts',(0.312811277746774,-1.9700733703544,8.94289201048762));
#12736=CARTESIAN_POINT('Ctrl Pts',(0.316291085565656,-1.9695176896198,8.94311947017718));
#12737=CARTESIAN_POINT('Ctrl Pts',(0.322447807500711,-1.96851780200896,
8.94352115199808));
#12738=CARTESIAN_POINT('Ctrl Pts',(0.325125307925283,-1.96807735109432,
8.94369558562817));
#12739=CARTESIAN_POINT('Ctrl Pts',(0.33076873336208,-1.96713717204483,8.94406270022442));
#12740=CARTESIAN_POINT('Ctrl Pts',(0.33373442177827,-1.96663620037476,8.94425530925021));
#12741=CARTESIAN_POINT('Ctrl Pts',(0.341646133624258,-1.96528132180977,
8.94476833043426));
#12742=CARTESIAN_POINT('Ctrl Pts',(0.346590126967151,-1.9644154447779,8.94508806817207));
#12743=CARTESIAN_POINT('Ctrl Pts',(0.36991525599551,-1.96023954780605,8.94659277420059));
#12744=CARTESIAN_POINT('Ctrl Pts',(0.388253323196731,-1.95669001108131,
8.94776468420938));
#12745=CARTESIAN_POINT('Ctrl Pts',(0.574893587595598,-1.91783635127253,
8.95960375346688));
#12746=CARTESIAN_POINT('Ctrl Pts',(0.73803417500281,-1.8611617396097,8.96926487394913));
#12747=CARTESIAN_POINT('Ctrl Pts',(0.990543753951332,-1.73493888711216,
8.98577814694247));
#12748=CARTESIAN_POINT('Ctrl Pts',(1.08491556362824,-1.67754073427017,8.99235467400632));
#12749=CARTESIAN_POINT('Ctrl Pts',(1.18449948715099,-1.60504064125372,9.00004366418073));
#12750=CARTESIAN_POINT('Ctrl Pts',(1.19487045727827,-1.59733499083669,9.0008539606765));
#12751=CARTESIAN_POINT('Ctrl Pts',(1.21012883357632,-1.58576623823173,9.00206069960659));
#12752=CARTESIAN_POINT('Ctrl Pts',(1.21507432048008,-1.58198000949722,9.00245412638088));
#12753=CARTESIAN_POINT('Ctrl Pts',(1.22383322436455,-1.57520895507257,9.00315506948077));
#12754=CARTESIAN_POINT('Ctrl Pts',(1.2276536741217,-1.57223327433851,9.00346222216824));
#12755=CARTESIAN_POINT('Ctrl Pts',(1.23566077676945,-1.56594970459861,9.00410897452413));
#12756=CARTESIAN_POINT('Ctrl Pts',(1.2398450628347,-1.56263887441444,9.00444869000707));
#12757=CARTESIAN_POINT('Ctrl Pts',(1.25082171125663,-1.55388172254456,9.00534449447386));
#12758=CARTESIAN_POINT('Ctrl Pts',(1.2575917298175,-1.54840769764214,9.00590169328192));
#12759=CARTESIAN_POINT('Ctrl Pts',(1.28801826757867,-1.52347457808038,9.00842746164429));
#12760=CARTESIAN_POINT('Ctrl Pts',(1.31125940703234,-1.50351735659395,9.01041619430015));
#12761=CARTESIAN_POINT('Ctrl Pts',(1.37217632382544,-1.44872086972475,9.01579427062109));
#12762=CARTESIAN_POINT('Ctrl Pts',(1.40898076916794,-1.4129516827679,9.01922119512866));
#12763=CARTESIAN_POINT('Ctrl Pts',(1.51389345210909,-1.30281115691842,9.0295309384371));
#12764=CARTESIAN_POINT('Ctrl Pts',(1.57778463103721,-1.22465613256173,9.03655068356465));
#12765=CARTESIAN_POINT('Ctrl Pts',(1.6841844803214,-1.07227998251384,9.04951722788825));
#12766=CARTESIAN_POINT('Ctrl Pts',(1.72837192207188,-0.999496918901939,
9.05544466567372));
#12767=CARTESIAN_POINT('Ctrl Pts',(1.78509575959843,-0.890986942673127,
9.06372090870368));
#12768=CARTESIAN_POINT('Ctrl Pts',(1.80147845757624,-0.857379970392465,
9.06621085083126));
#12769=CARTESIAN_POINT('Ctrl Pts',(1.81936916166936,-0.817899117130282,
9.06903581628544));
#12770=CARTESIAN_POINT('Ctrl Pts',(1.8218057928042,-0.812457240554516,9.06942302624669));
#12771=CARTESIAN_POINT('Ctrl Pts',(1.82565220465214,-0.803762500479012,
9.07003813861911));
#12772=CARTESIAN_POINT('Ctrl Pts',(1.82707775378387,-0.800516715398479,
9.07026697715849));
#12773=CARTESIAN_POINT('Ctrl Pts',(1.829580404173,-0.794777004369244,9.07067023727668));
#12774=CARTESIAN_POINT('Ctrl Pts',(1.83066107256199,-0.792284658297716,
9.07084487601038));
#12775=CARTESIAN_POINT('Ctrl Pts',(1.83292318661552,-0.787038204325411,
9.07121150347618));
#12776=CARTESIAN_POINT('Ctrl Pts',(1.83410351565088,-0.784283645926796,
9.07140342378063));
#12777=CARTESIAN_POINT('Ctrl Pts',(1.83722497722179,-0.776953441193756,
9.07191265672301));
#12778=CARTESIAN_POINT('Ctrl Pts',(1.83915523892175,-0.772373145013534,
9.07222931236446));
#12779=CARTESIAN_POINT('Ctrl Pts',(1.84805788817394,-0.75102553755355,9.07369822586326));
#12780=CARTESIAN_POINT('Ctrl Pts',(1.85481850208658,-0.734170073418918,
9.07483816773641));
#12781=CARTESIAN_POINT('Ctrl Pts',(1.91739535033485,-0.571769873827472,
9.08565359998278));
#12782=CARTESIAN_POINT('Ctrl Pts',(1.95620832368073,-0.420225514296504,
9.09449394386143));
#12783=CARTESIAN_POINT('Ctrl Pts',(1.99386873050268,-0.139996348203782,
9.11095368171462));
#12784=CARTESIAN_POINT('Ctrl Pts',(1.99873350416568,-0.0129990598037182,
9.11845430159421));
#12785=CARTESIAN_POINT('Ctrl Pts',(1.99077256562081,0.126575313573216,9.12717997152477));
#12786=CARTESIAN_POINT('Ctrl Pts',(1.98990498202591,0.139552383661874,9.12799558985713));
#12787=CARTESIAN_POINT('Ctrl Pts',(1.98843306153819,0.158746732133081,9.12920874484194));
#12788=CARTESIAN_POINT('Ctrl Pts',(1.98792631274059,0.16497132736871,9.12960321850335));
#12789=CARTESIAN_POINT('Ctrl Pts',(1.98697456266756,0.176020229321791,9.1303053411172));
#12790=CARTESIAN_POINT('Ctrl Pts',(1.98654119889403,0.180845509307262,9.13061262199557));
#12791=CARTESIAN_POINT('Ctrl Pts',(1.98559442483017,0.190973088244688,9.13125894617887));
#12792=CARTESIAN_POINT('Ctrl Pts',(1.98507734474336,0.196274997973149,9.13159810264342));
#12793=CARTESIAN_POINT('Ctrl Pts',(1.9836631766378,0.210197734220782,9.13249085130298));
#12794=CARTESIAN_POINT('Ctrl Pts',(1.98273113542377,0.218814822415026,9.13304553963666));
#12795=CARTESIAN_POINT('Ctrl Pts',(1.97829470653264,0.25747303655343,9.13554384709906));
#12796=CARTESIAN_POINT('Ctrl Pts',(1.97416367201117,0.287436844290733,9.13750709589638));
#12797=CARTESIAN_POINT('Ctrl Pts',(1.96133343722684,0.367070485823468,9.14279974935694));
#12798=CARTESIAN_POINT('Ctrl Pts',(1.95142995828625,0.416521297994372,9.14616528229606));
#12799=CARTESIAN_POINT('Ctrl Pts',(1.9163036686025,0.56287421998384,9.15635900505328));
#12800=CARTESIAN_POINT('Ctrl Pts',(1.8856512087182,0.658303379924851,9.16332441021045));
#12801=CARTESIAN_POINT('Ctrl Pts',(1.8016335613901,0.865038322893551,9.17889434919384));
#12802=CARTESIAN_POINT('Ctrl Pts',(1.74483771688556,0.974537625131619,9.1874785853881));
#12803=CARTESIAN_POINT('Ctrl Pts',(1.67422003688979,1.08446848562963,9.19600888768589));
#12804=CARTESIAN_POINT('Ctrl Pts',(1.67010103560599,1.09080115673942,9.19649989473049));
#12805=CARTESIAN_POINT('Ctrl Pts',(1.66402078775315,1.10003392410547,9.19721501329284));
#12806=CARTESIAN_POINT('Ctrl Pts',(1.66208778584233,1.10295240553285,9.19744095222803));
#12807=CARTESIAN_POINT('Ctrl Pts',(1.65864457729324,1.10812141664551,9.19784090185988));
#12808=CARTESIAN_POINT('Ctrl Pts',(1.65713745643808,1.1103739724224,9.19801511781593));
#12809=CARTESIAN_POINT('Ctrl Pts',(1.65394112508214,1.11513023405453,9.19838280980742));
#12810=CARTESIAN_POINT('Ctrl Pts',(1.65225082263892,1.1176331703769,9.19857620991978));
#12811=CARTESIAN_POINT('Ctrl Pts',(1.6477048579684,1.12433181131501,9.19909358407897));
#12812=CARTESIAN_POINT('Ctrl Pts',(1.64483883290656,1.1285205075816,9.19941686345561));
#12813=CARTESIAN_POINT('Ctrl Pts',(1.63100345231419,1.14857624347236,9.20096383887248));
#12814=CARTESIAN_POINT('Ctrl Pts',(1.6198198580537,1.16429521298118,9.20217357005242));
#12815=CARTESIAN_POINT('Ctrl Pts',(1.58794877964815,1.20774288668222,9.20551714559542));
#12816=CARTESIAN_POINT('Ctrl Pts',(1.56676467253656,1.23510038531111,9.20762232956163));
#12817=CARTESIAN_POINT('Ctrl Pts',(1.48681524806204,1.33297871826151,9.21520971605896));
#12818=CARTESIAN_POINT('Ctrl Pts',(1.42391110370231,1.39997546068546,9.22051632014442));
#12819=CARTESIAN_POINT('Ctrl Pts',(1.24253094788149,1.56823430375081,9.23486528437918));
#12820=CARTESIAN_POINT('Ctrl Pts',(1.11647736803299,1.66033460837213,9.24393197198401));
#12821=CARTESIAN_POINT('Ctrl Pts',(0.970053344998273,1.74303829056393,9.25443311532393));
#12822=CARTESIAN_POINT('Ctrl Pts',(0.959036299165654,1.74912416363821,9.25522267219396));
#12823=CARTESIAN_POINT('Ctrl Pts',(0.942540368423959,1.75803390008944,9.25640437510974));
#12824=CARTESIAN_POINT('Ctrl Pts',(0.937104648719312,1.76093736854443,9.25679368656554));
#12825=CARTESIAN_POINT('Ctrl Pts',(0.927493503402662,1.76601402031382,9.25748194073597));
#12826=CARTESIAN_POINT('Ctrl Pts',(0.923323656768331,1.76819771039007,9.25778050870269));
#12827=CARTESIAN_POINT('Ctrl Pts',(0.914513441564125,1.77277183382422,9.25841128068376));
#12828=CARTESIAN_POINT('Ctrl Pts',(0.909871347485943,1.77515884916593,9.25874360236748));
#12829=CARTESIAN_POINT('Ctrl Pts',(0.900363143603138,1.78000097711915,9.25942424183463));
#12830=CARTESIAN_POINT('Ctrl Pts',(0.895496237024818,1.7824544194457,9.2597726148598));
#12831=CARTESIAN_POINT('Ctrl Pts',(0.883476063557577,1.78845221886334,9.26063299412145));
#12832=CARTESIAN_POINT('Ctrl Pts',(0.876311505848276,1.79197361466987,9.26114579746332));
#12833=CARTESIAN_POINT('Ctrl Pts',(0.856414242517697,1.80160530181083,9.26256997678239));
#12834=CARTESIAN_POINT('Ctrl Pts',(0.843637685815049,1.80762342768383,9.26348451933301));
#12835=CARTESIAN_POINT('Ctrl Pts',(0.727697535552327,1.86073764447368,9.27178508870476));
#12836=CARTESIAN_POINT('Ctrl Pts',(0.620774059034965,1.89908402303756,9.27946973697872));
#12837=CARTESIAN_POINT('Ctrl Pts',(0.378259191255245,1.9633797100866,9.2968442164919));
#12838=CARTESIAN_POINT('Ctrl Pts',(0.242041533444697,1.98478138891175,9.30657394376062));
#12839=CARTESIAN_POINT('Ctrl Pts',(0.0689674952153302,1.99387855063382,
9.31827295996429));
#12840=CARTESIAN_POINT('Ctrl Pts',(0.0331840629342068,1.99479507753941,
9.3206544067323));
#12841=CARTESIAN_POINT('Ctrl Pts',(-0.00849179740224064,1.99474060462243,
9.32337011611159));
#12842=CARTESIAN_POINT('Ctrl Pts',(-0.0143763629121435,1.99470687386591,
9.32375222428513));
#12843=CARTESIAN_POINT('Ctrl Pts',(-0.0237828037088323,1.99461132721786,
9.32436077871265));
#12844=CARTESIAN_POINT('Ctrl Pts',(-0.027304757952857,1.99456622328742,
9.32458813060584));
#12845=CARTESIAN_POINT('Ctrl Pts',(-0.0335395130969901,1.99446986068405,
9.32498968934213));
#12846=CARTESIAN_POINT('Ctrl Pts',(-0.0362523491747951,1.99442239549463,
9.32516410724176));
#12847=CARTESIAN_POINT('Ctrl Pts',(-0.0419730986466469,1.99431062596545,
9.32553126135294));
#12848=CARTESIAN_POINT('Ctrl Pts',(-0.0449809581585582,1.99424505202991,
9.32572392534565));
#12849=CARTESIAN_POINT('Ctrl Pts',(-0.0530102869146406,1.99405183059469,
9.32623724891666));
#12850=CARTESIAN_POINT('Ctrl Pts',(-0.0580314830086291,1.99391201960316,
9.32655723267571));
#12851=CARTESIAN_POINT('Ctrl Pts',(-0.0817614403357396,1.99316156307402,
9.32806483499531));
#12852=CARTESIAN_POINT('Ctrl Pts',(-0.100462285256823,1.99230653773857,
9.32923933419196));
#12853=CARTESIAN_POINT('Ctrl Pts',(-0.290792935676209,1.98091749373384,
9.34107958778681));
#12854=CARTESIAN_POINT('Ctrl Pts',(-0.460413968350718,1.94849484637778,
9.35073996135217));
#12855=CARTESIAN_POINT('Ctrl Pts',(-0.728487792859784,1.86023718996438,
9.36724926830924));
#12856=CARTESIAN_POINT('Ctrl Pts',(-0.830131529611602,1.81715528857856,
9.37382236719202));
#12857=CARTESIAN_POINT('Ctrl Pts',(-0.939139766533037,1.75988958651772,
9.38150842976427));
#12858=CARTESIAN_POINT('Ctrl Pts',(-0.950531170106828,1.75376319379863,
9.38231959699395));
#12859=CARTESIAN_POINT('Ctrl Pts',(-0.967320904204017,1.74452189973883,
9.38352738591893));
#12860=CARTESIAN_POINT('Ctrl Pts',(-0.972765669432981,1.74149170004331,
9.38392098423441));
#12861=CARTESIAN_POINT('Ctrl Pts',(-0.982303824636207,1.73612470014121,
9.38461391685686));
#12862=CARTESIAN_POINT('Ctrl Pts',(-0.986403317301261,1.73379879839836,
9.3849128577992));
#12863=CARTESIAN_POINT('Ctrl Pts',(-0.994992166194602,1.72888547933815,
9.38554154195178));
#12864=CARTESIAN_POINT('Ctrl Pts',(-0.999479755345363,1.72629505857907,
9.38587139206675));
#12865=CARTESIAN_POINT('Ctrl Pts',(-1.00862211214142,1.72097011643965,9.38654620432678));
#12866=CARTESIAN_POINT('Ctrl Pts',(-1.01327597049019,1.71823412649641,9.38689121791251));
#12867=CARTESIAN_POINT('Ctrl Pts',(-1.02467637512553,1.71146943733045,9.38774011828662));
#12868=CARTESIAN_POINT('Ctrl Pts',(-1.03141028804542,1.70741972679024,9.38824476885135));
#12869=CARTESIAN_POINT('Ctrl Pts',(-1.04991221388023,1.69614345309387,9.38964035162478));
#12870=CARTESIAN_POINT('Ctrl Pts',(-1.06162920438432,1.68883441662369,9.39053429347277));
#12871=CARTESIAN_POINT('Ctrl Pts',(-1.09871092132302,1.66516452479977,9.3933963495681));
#12872=CARTESIAN_POINT('Ctrl Pts',(-1.12377963745658,1.64835000736031,9.39538099027834));
#12873=CARTESIAN_POINT('Ctrl Pts',(-1.22435274191833,1.57753109530907,9.4035512462473));
#12874=CARTESIAN_POINT('Ctrl Pts',(-1.29641730826499,1.51886220450217,9.40990353934877));
#12875=CARTESIAN_POINT('Ctrl Pts',(-1.47601735423118,1.35052491548672,9.42699261916796));
#12876=CARTESIAN_POINT('Ctrl Pts',(-1.57544451244576,1.23309569234885,9.4378580140116));
#12877=CARTESIAN_POINT('Ctrl Pts',(-1.66832843679843,1.09357693157464,9.4489163625842));
#12878=CARTESIAN_POINT('Ctrl Pts',(-1.6760917629886,1.08164074839177,9.44984863238098));
#12879=CARTESIAN_POINT('Ctrl Pts',(-1.68625943703765,1.06563548181358,9.4510793946607));
#12880=CARTESIAN_POINT('Ctrl Pts',(-1.68877785517966,1.06163987588282,9.45138506057795));
#12881=CARTESIAN_POINT('Ctrl Pts',(-1.69268628132033,1.05538984711988,9.45186067535815));
#12882=CARTESIAN_POINT('Ctrl Pts',(-1.69408600998909,1.0531415704141,9.45203125909392));
#12883=CARTESIAN_POINT('Ctrl Pts',(-1.69676457596883,1.04882003695711,9.45235816754792));
#12884=CARTESIAN_POINT('Ctrl Pts',(-1.69804407830334,1.04674724953077,9.45251453386157));
#12885=CARTESIAN_POINT('Ctrl Pts',(-1.7010947871771,1.0417848024119,9.45288786339674));
#12886=CARTESIAN_POINT('Ctrl Pts',(-1.70286242713999,1.03889297049726,9.4531045902612));
#12887=CARTESIAN_POINT('Ctrl Pts',(-1.70815289171911,1.03018807141602,9.45375453280931));
#12888=CARTESIAN_POINT('Ctrl Pts',(-1.71165342847114,1.02436141473171,9.45418631194267));
#12889=CARTESIAN_POINT('Ctrl Pts',(-1.74429471793887,0.969395349991002,
9.45823004829396));
#12890=CARTESIAN_POINT('Ctrl Pts',(-1.77134473905288,0.919037881446591,
9.46171423789622));
#12891=CARTESIAN_POINT('Ctrl Pts',(-1.89070386374988,0.671923166784247,
9.47811141932761));
#12892=CARTESIAN_POINT('Ctrl Pts',(-1.95260856510629,0.462140879230423,
9.49014102357731));
#12893=CARTESIAN_POINT('Ctrl Pts',(-1.98309007296206,0.217355166525072,
9.5052788696862));
#12894=CARTESIAN_POINT('Ctrl Pts',(-1.9860741270961,0.188146027176488,9.507098884177));
#12895=CARTESIAN_POINT('Ctrl Pts',(-1.98916000412274,0.149526392237284,
9.50952751948987));
#12896=CARTESIAN_POINT('Ctrl Pts',(-1.98984156330218,0.14016494601869,9.51011793694034));
#12897=CARTESIAN_POINT('Ctrl Pts',(-1.99082037726254,0.125269689495495,
9.51106022337514));
#12898=CARTESIAN_POINT('Ctrl Pts',(-1.99116069055567,0.11973876985399,9.51141073964354));
#12899=CARTESIAN_POINT('Ctrl Pts',(-1.99175253953599,0.109418396779451,
9.51206597844657));
#12900=CARTESIAN_POINT('Ctrl Pts',(-1.99200985747923,0.104629304441112,
9.51237051722645));
#12901=CARTESIAN_POINT('Ctrl Pts',(-1.9924808427591,0.0952310036940479,
9.51296911607559));
#12902=CARTESIAN_POINT('Ctrl Pts',(-1.99269579357922,0.0906218874647015,
9.51326313387955));
#12903=CARTESIAN_POINT('Ctrl Pts',(-1.99314311743561,0.080257422717421,
9.51392532354307));
#12904=CARTESIAN_POINT('Ctrl Pts',(-1.99336655655012,0.0745017486757097,
9.514293773342));
#12905=CARTESIAN_POINT('Ctrl Pts',(-1.99391674533475,0.058546648621588,
9.51531716629216));
#12906=CARTESIAN_POINT('Ctrl Pts',(-1.99419015815151,0.0483456728499656,
9.51597377308197));
#12907=CARTESIAN_POINT('Ctrl Pts',(-1.99463292918793,0.0251946012443252,
9.51746929279413));
#12908=CARTESIAN_POINT('Ctrl Pts',(-1.9947544595798,0.0122442029112117,
9.51830966718299));
#12909=CARTESIAN_POINT('Ctrl Pts',(-1.99474987500506,-0.000706163778629118,
9.51915393760047));
#12910=CARTESIAN_POINT('',(-1.99474947325114,0.00144964281281663,11.1209548814577));
#12911=CARTESIAN_POINT('Ctrl Pts',(-1.99474987552157,-0.000704703254848296,
9.51915384238488));
#12912=CARTESIAN_POINT('Ctrl Pts',(-1.99466554320306,-0.239417779555123,
9.53471620625515));
#12913=CARTESIAN_POINT('Ctrl Pts',(-1.95172253893193,-0.476180383039018,
9.55181752929714));
#12914=CARTESIAN_POINT('Ctrl Pts',(-1.85711043663534,-0.728791549331281,
9.57016584446524));
#12915=CARTESIAN_POINT('Ctrl Pts',(-1.84551239464581,-0.757681017506495,
9.572260448041));
#12916=CARTESIAN_POINT('Ctrl Pts',(-1.82619143527078,-0.802728078959297,
9.57550810023716));
#12917=CARTESIAN_POINT('Ctrl Pts',(-1.81891942338838,-0.819072471240963,
9.57668252470648));
#12918=CARTESIAN_POINT('Ctrl Pts',(-1.80935781572755,-0.839807300489132,
9.57816536550759));
#12919=CARTESIAN_POINT('Ctrl Pts',(-1.80727069380295,-0.844289433714375,
9.57848547770938));
#12920=CARTESIAN_POINT('Ctrl Pts',(-1.80389427003971,-0.851470475472302,
9.57899760630593));
#12921=CARTESIAN_POINT('Ctrl Pts',(-1.80261554217607,-0.854174288701194,
9.57919026479088));
#12922=CARTESIAN_POINT('Ctrl Pts',(-1.80016304159989,-0.859329957174259,
9.57955729176092));
#12923=CARTESIAN_POINT('Ctrl Pts',(-1.79899035278767,-0.861782259212724,
9.57973172094026));
#12924=CARTESIAN_POINT('Ctrl Pts',(-1.79627169415799,-0.867437728713526,
9.5801336587595));
#12925=CARTESIAN_POINT('Ctrl Pts',(-1.79472216805457,-0.870639163144749,
9.58036094380133));
#12926=CARTESIAN_POINT('Ctrl Pts',(-1.78972313568337,-0.880897473015252,
9.58108850393134));
#12927=CARTESIAN_POINT('Ctrl Pts',(-1.7862404533854,-0.887938234317444,
9.58158675765473));
#12928=CARTESIAN_POINT('Ctrl Pts',(-1.7394767457496,-0.981089403425853,
9.58816650883814));
#12929=CARTESIAN_POINT('Ctrl Pts',(-1.69004532862152,-1.06398683709094,
9.59388492219143));
#12930=CARTESIAN_POINT('Ctrl Pts',(-1.55225840726779,-1.26106112652312,
9.60793369624107));
#12931=CARTESIAN_POINT('Ctrl Pts',(-1.45716866178045,-1.36983199556655,
9.6161427170153));
#12932=CARTESIAN_POINT('Ctrl Pts',(-1.32243864423323,-1.49389142264357,
9.62714637822894));
#12933=CARTESIAN_POINT('Ctrl Pts',(-1.29291237014169,-1.51951731184371,
9.62952262909124));
#12934=CARTESIAN_POINT('Ctrl Pts',(-1.24976377664027,-1.55479750889399,
9.63296009969196));
#12935=CARTESIAN_POINT('Ctrl Pts',(-1.23674270864199,-1.56517482665475,
9.63399303997714));
#12936=CARTESIAN_POINT('Ctrl Pts',(-1.216504699627,-1.58089355894691,9.63559269079468));
#12937=CARTESIAN_POINT('Ctrl Pts',(-1.20937885742552,-1.58635144402778,
9.6361548450625));
#12938=CARTESIAN_POINT('Ctrl Pts',(-1.19753658951515,-1.595295607261,9.63708742078457));
#12939=CARTESIAN_POINT('Ctrl Pts',(-1.1928411412951,-1.59880954720163,9.63745676081658));
#12940=CARTESIAN_POINT('Ctrl Pts',(-1.18369864920448,-1.60558883548575,
9.63817511783331));
#12941=CARTESIAN_POINT('Ctrl Pts',(-1.17925341583401,-1.60885654457168,
9.63852403884496));
#12942=CARTESIAN_POINT('Ctrl Pts',(-1.17477102588897,-1.61212301022304,
9.63887553491039));
#12943=CARTESIAN_POINT('Ctrl Pts',(-1.17474733180471,-1.61214027608537,
9.63887739292243));
#12944=CARTESIAN_POINT('Ctrl Pts',(-1.17469921836505,-1.61217533469059,
9.63888116580047));
#12945=CARTESIAN_POINT('Ctrl Pts',(-1.1746747995976,-1.61219312695551,9.63888308061977));
#12946=CARTESIAN_POINT('Ctrl Pts',(-1.17462520819229,-1.61222925905361,
9.63888696935317));
#12947=CARTESIAN_POINT('Ctrl Pts',(-1.17460003606027,-1.61224759846515,
9.63888894322695));
#12948=CARTESIAN_POINT('Ctrl Pts',(-1.17454890766215,-1.61228484674399,
9.63889295244054));
#12949=CARTESIAN_POINT('Ctrl Pts',(-1.17452295192947,-1.61230375516576,
9.63889498773782));
#12950=CARTESIAN_POINT('Ctrl Pts',(-1.17447022457372,-1.61234216442608,
9.63889912228646));
#12951=CARTESIAN_POINT('Ctrl Pts',(-1.1744434534398,-1.61236166484722,9.63890122149873));
#12952=CARTESIAN_POINT('Ctrl Pts',(-1.17438906180464,-1.61240128230557,
9.63890548650019));
#12953=CARTESIAN_POINT('Ctrl Pts',(-1.17436144176037,-1.61242139894434,
9.63890765225274));
#12954=CARTESIAN_POINT('Ctrl Pts',(-1.17430531706245,-1.61246227430653,
9.6389120530958));
#12955=CARTESIAN_POINT('Ctrl Pts',(-1.17427681281601,-1.61248303266288,
9.63891428815353));
#12956=CARTESIAN_POINT('Ctrl Pts',(-1.17421888240189,-1.61252521841843,
9.63891883053004));
#12957=CARTESIAN_POINT('Ctrl Pts',(-1.17418945666586,-1.61254664542746,
9.63892113781408));
#12958=CARTESIAN_POINT('Ctrl Pts',(-1.1741296440476,-1.61259019682035,9.63892582771611));
#12959=CARTESIAN_POINT('Ctrl Pts',(-1.17409925752153,-1.61261232086323,
9.63892821030521));
#12960=CARTESIAN_POINT('Ctrl Pts',(-1.17403748176703,-1.61265729633212,
9.63893305407281));
#12961=CARTESIAN_POINT('Ctrl Pts',(-1.17400609289531,-1.61268014741046,
9.63893551522229));
#12962=CARTESIAN_POINT('Ctrl Pts',(-1.17394226856811,-1.61272660862848,
9.63894051954815));
#12963=CARTESIAN_POINT('Ctrl Pts',(-1.17390983343254,-1.61275021844041,
9.6389430626983));
#12964=CARTESIAN_POINT('Ctrl Pts',(-1.1738438701572,-1.61279823062703,9.63894823466178));
#12965=CARTESIAN_POINT('Ctrl Pts',(-1.17381034230115,-1.61282263269283,
9.63895086345162));
#12966=CARTESIAN_POINT('Ctrl Pts',(-1.17374214439206,-1.61287226487909,
9.6389562105478));
#12967=CARTESIAN_POINT('Ctrl Pts',(-1.17370747461191,-1.61289749469037,
9.63895892883141));
#12968=CARTESIAN_POINT('Ctrl Pts',(-1.17363694074604,-1.61294881995159,
9.63896445899669));
#12969=CARTESIAN_POINT('Ctrl Pts',(-1.17360107690588,-1.61297491510326,
9.63896727085768));
#12970=CARTESIAN_POINT('Ctrl Pts',(-1.17352809965376,-1.61302801089418,
9.63897299250648));
#12971=CARTESIAN_POINT('Ctrl Pts',(-1.17349098645414,-1.61305501124951,
9.63897590227609));
#12972=CARTESIAN_POINT('Ctrl Pts',(-1.17341545188838,-1.61310995968244,
9.63898182433144));
#12973=CARTESIAN_POINT('Ctrl Pts',(-1.17337703067473,-1.61313790750888,
9.63898483660355));
#12974=CARTESIAN_POINT('Ctrl Pts',(-1.17329881764629,-1.61319479587265,
9.63899096855377));
#12975=CARTESIAN_POINT('Ctrl Pts',(-1.17325902602441,-1.61322373611755,
9.63899408821495));
#12976=CARTESIAN_POINT('Ctrl Pts',(-1.17317800601289,-1.61328265697803,
9.6390004401253));
#12977=CARTESIAN_POINT('Ctrl Pts',(-1.17313677771917,-1.61331263735867,
9.63900367236497));
#12978=CARTESIAN_POINT('Ctrl Pts',(-1.17305281379804,-1.61337368930207,
9.63901025495861));
#12979=CARTESIAN_POINT('Ctrl Pts',(-1.17301007826626,-1.61340476061573,
9.63901360530295));
#12980=CARTESIAN_POINT('Ctrl Pts',(-1.17292302472627,-1.61346804851192,
9.63902042999041));
#12981=CARTESIAN_POINT('Ctrl Pts',(-1.17287870678803,-1.61350026484818,
9.63902390432572));
#12982=CARTESIAN_POINT('Ctrl Pts',(-1.17278840833128,-1.61356590042513,
9.6390309832679));
#12983=CARTESIAN_POINT('Ctrl Pts',(-1.17274242784303,-1.61359931943089,
9.63903458786986));
#12984=CARTESIAN_POINT('Ctrl Pts',(-1.17264871880393,-1.6136674218278,9.63904193403896));
#12985=CARTESIAN_POINT('Ctrl Pts',(-1.17260099025469,-1.61370210498551,
9.63904567560322));
#12986=CARTESIAN_POINT('Ctrl Pts',(-1.17250685220924,-1.61377050639584,
9.63905305525199));
#12987=CARTESIAN_POINT('Ctrl Pts',(-1.17246044299194,-1.61380422462264,
9.63905669331673));
#12988=CARTESIAN_POINT('Ctrl Pts',(-1.16858269558852,-1.61662131384445,
9.63936067076246));
#12989=CARTESIAN_POINT('Ctrl Pts',(-1.16474148675107,-1.61939101430458,
9.63966153659612));
#12990=CARTESIAN_POINT('Ctrl Pts',(-1.15581418950967,-1.62577983999472,
9.64036022324365));
#12991=CARTESIAN_POINT('Ctrl Pts',(-1.15072092402591,-1.62938880637796,
9.64075843089691));
#12992=CARTESIAN_POINT('Ctrl Pts',(-1.13497590430505,-1.64043470664046,
9.64198821857783));
#12993=CARTESIAN_POINT('Ctrl Pts',(-1.12426854242503,-1.64779141924634,
9.64282284271778));
#12994=CARTESIAN_POINT('Ctrl Pts',(-1.00620397309347,-1.72722365243542,
9.65200895816982));
#12995=CARTESIAN_POINT('Ctrl Pts',(-0.892174803386398,-1.78878740911501,
9.66076061035555));
#12996=CARTESIAN_POINT('Ctrl Pts',(-0.679955527685574,-1.87799841786487,
9.67672343276998));
#12997=CARTESIAN_POINT('Ctrl Pts',(-0.584063729278959,-1.90999663084407,
9.68382099476163));
#12998=CARTESIAN_POINT('Ctrl Pts',(-0.44141227310467,-1.94584474734148,
9.6939505215032));
#12999=CARTESIAN_POINT('Ctrl Pts',(-0.396282315762313,-1.9555350975074,
9.69709320179769));
#13000=CARTESIAN_POINT('Ctrl Pts',(-0.327664431831805,-1.96779533980772,
9.7017413691947));
#13001=CARTESIAN_POINT('Ctrl Pts',(-0.3044021385221,-1.97152781837762,9.70329479251749));
#13002=CARTESIAN_POINT('Ctrl Pts',(-0.275710468961657,-1.97561147326816,
9.70517892479128));
#13003=CARTESIAN_POINT('Ctrl Pts',(-0.270339816057213,-1.97635354669309,
9.70553023774412));
#13004=CARTESIAN_POINT('Ctrl Pts',(-0.261896428185398,-1.97748512401847,
9.70608032898307));
#13005=CARTESIAN_POINT('Ctrl Pts',(-0.258825747960257,-1.97788937691783,
9.70627992465509));
#13006=CARTESIAN_POINT('Ctrl Pts',(-0.253080572335661,-1.97863211681487,
9.70665248638472));
#13007=CARTESIAN_POINT('Ctrl Pts',(-0.250406362052425,-1.97897233021321,
9.70682554572711));
#13008=CARTESIAN_POINT('Ctrl Pts',(-0.244326510445079,-1.9797332885553,
9.70721819472701));
#13009=CARTESIAN_POINT('Ctrl Pts',(-0.240920475976034,-1.98015066654216,
9.70743759226989));
#13010=CARTESIAN_POINT('Ctrl Pts',(-0.230783831719392,-1.98136627689524,
9.70808888482382));
#13011=CARTESIAN_POINT('Ctrl Pts',(-0.224050127246862,-1.98213900720012,
9.70851936736008));
#13012=CARTESIAN_POINT('Ctrl Pts',(-0.174984724614378,-1.98751630645788,
9.71164118067062));
#13013=CARTESIAN_POINT('Ctrl Pts',(-0.13251555437737,-1.99079907950381,
9.714262569465));
#13014=CARTESIAN_POINT('Ctrl Pts',(-0.0196481404712469,-1.99589498881153,
9.72109233456169));
#13015=CARTESIAN_POINT('Ctrl Pts',(0.0507980067771298,-1.99534553709103,
9.72521540036741));
#13016=CARTESIAN_POINT('Ctrl Pts',(0.176301232370485,-1.98771401109925,
9.73252892190659));
#13017=CARTESIAN_POINT('Ctrl Pts',(0.231366847896893,-1.98205916045819,
9.73572662113803));
#13018=CARTESIAN_POINT('Ctrl Pts',(0.402190215102142,-1.95730029580344,
9.74576944574804));
#13019=CARTESIAN_POINT('Ctrl Pts',(0.516529115322381,-1.93027818773817,
9.75268493805949));
#13020=CARTESIAN_POINT('Ctrl Pts',(0.641459484615225,-1.88885246677057,
9.76082929595517));
#13021=CARTESIAN_POINT('Ctrl Pts',(0.655044776703003,-1.88418423607092,
9.76172273408732));
#13022=CARTESIAN_POINT('Ctrl Pts',(0.676190539915999,-1.87666171634797,
9.76312617672897));
#13023=CARTESIAN_POINT('Ctrl Pts',(0.683786269615503,-1.87390746257725,
9.76363290336428));
#13024=CARTESIAN_POINT('Ctrl Pts',(0.696515014871994,-1.86920425331903,
9.76448653250431));
#13025=CARTESIAN_POINT('Ctrl Pts',(0.701657140527358,-1.86728009755925,
9.7648326106423));
#13026=CARTESIAN_POINT('Ctrl Pts',(0.711702382026279,-1.86347387004959,
9.76551112530169));
#13027=CARTESIAN_POINT('Ctrl Pts',(0.716606141283242,-1.86159361364236,
9.76584349898133));
#13028=CARTESIAN_POINT('Ctrl Pts',(0.721510347196118,-1.8596909370812,9.76617706461301));
#13029=CARTESIAN_POINT('Ctrl Pts',(0.721518314365015,-1.85968784601311,
9.76617760651293));
#13030=CARTESIAN_POINT('Ctrl Pts',(0.721534265834445,-1.85968165711234,
9.76617869148417));
#13031=CARTESIAN_POINT('Ctrl Pts',(0.721542250180477,-1.85967855926174,
9.7661792345586));
#13032=CARTESIAN_POINT('Ctrl Pts',(0.721558236253706,-1.85967235669838,
9.76618032189585));
#13033=CARTESIAN_POINT('Ctrl Pts',(0.721566237917644,-1.85966925200989,
9.76618086615439));
#13034=CARTESIAN_POINT('Ctrl Pts',(0.721582258588347,-1.85966303578485,
9.76618195585731));
#13035=CARTESIAN_POINT('Ctrl Pts',(0.721590277609264,-1.85965992424254,
9.76618250130267));
#13036=CARTESIAN_POINT('Ctrl Pts',(0.721606333131996,-1.85965369425549,
9.76618359338865));
#13037=CARTESIAN_POINT('Ctrl Pts',(0.721614369605373,-1.85965057582153,
9.76618414002736));
#13038=CARTESIAN_POINT('Ctrl Pts',(0.72163046010647,-1.85964433202189,9.76618523450508));
#13039=CARTESIAN_POINT('Ctrl Pts',(0.721638514110968,-1.85964120666497,
9.76618578234253));
#13040=CARTESIAN_POINT('Ctrl Pts',(0.721654639746199,-1.85963494899073,
9.76618687922267));
#13041=CARTESIAN_POINT('Ctrl Pts',(0.721662711354995,-1.85963181668166,
9.76618742826387));
#13042=CARTESIAN_POINT('Ctrl Pts',(0.72167887236349,-1.85962554503842,9.76618852756278));
#13043=CARTESIAN_POINT('Ctrl Pts',(0.721686961720999,-1.85962240572037,
9.76618907781761));
#13044=CARTESIAN_POINT('Ctrl Pts',(0.721703158011983,-1.85961612014178,
9.76619017952918));
#13045=CARTESIAN_POINT('Ctrl Pts',(0.721711265073703,-1.85961297383121,
9.76619073099466));
#13046=CARTESIAN_POINT('Ctrl Pts',(0.721727497148056,-1.85960667412127,
9.76619183515306));
#13047=CARTESIAN_POINT('Ctrl Pts',(0.721735622082283,-1.85960352075206,
9.76619238784066));
#13048=CARTESIAN_POINT('Ctrl Pts',(0.721751889945942,-1.85959720690685,
9.76619349444638));
#13049=CARTESIAN_POINT('Ctrl Pts',(0.721760032849961,-1.85959404644044,
9.76619404836278));
#13050=CARTESIAN_POINT('Ctrl Pts',(0.721776336582764,-1.85958771842734,
9.76619515742133));
#13051=CARTESIAN_POINT('Ctrl Pts',(0.721784497484633,-1.85958455085201,
9.76619571256846));
#13052=CARTESIAN_POINT('Ctrl Pts',(0.721800837377344,-1.85957820855654,
9.76619682409971));
#13053=CARTESIAN_POINT('Ctrl Pts',(0.721809016376319,-1.85957503383295,
9.76619738048439));
#13054=CARTESIAN_POINT('Ctrl Pts',(0.721825392549674,-1.85956867720658,
9.76619849449663));
#13055=CARTESIAN_POINT('Ctrl Pts',(0.721833589715874,-1.85956549530669,
9.76619905212366));
#13056=CARTESIAN_POINT('Ctrl Pts',(0.72185000242863,-1.85955912424732,9.76620016863459));
#13057=CARTESIAN_POINT('Ctrl Pts',(0.721858217910648,-1.85955593511261,
9.76620072751412));
#13058=CARTESIAN_POINT('Ctrl Pts',(0.721874667083772,-1.85954954964924,
9.76620184651844));
#13059=CARTESIAN_POINT('Ctrl Pts',(0.721882900847955,-1.85954635329194,
9.76620240664823));
#13060=CARTESIAN_POINT('Ctrl Pts',(0.721899387034375,-1.85953995320825,
9.76620352818366));
#13061=CARTESIAN_POINT('Ctrl Pts',(0.721907639313324,-1.85953674953721,
9.76620408957957));
#13062=CARTESIAN_POINT('Ctrl Pts',(0.726328966596836,-1.85782028336506,
9.76650487069316));
#13063=CARTESIAN_POINT('Ctrl Pts',(0.730735897212822,-1.85609132881169,
9.76680561656221));
#13064=CARTESIAN_POINT('Ctrl Pts',(0.740907818592239,-1.85205877565358,
9.76750199343696));
#13065=CARTESIAN_POINT('Ctrl Pts',(0.746668269512591,-1.84974392768006,
9.76789800166783));
#13066=CARTESIAN_POINT('Ctrl Pts',(0.764287970526054,-1.84256770165359,
9.7691143891054));
#13067=CARTESIAN_POINT('Ctrl Pts',(0.776111065680874,-1.83761895888335,
9.76993771707991));
#13068=CARTESIAN_POINT('Ctrl Pts',(0.881362334053054,-1.79236745889032,
9.77733215885068));
#13069=CARTESIAN_POINT('Ctrl Pts',(0.971611860087501,-1.74509173243757,
9.78414492592111));
#13070=CARTESIAN_POINT('Ctrl Pts',(1.17301994279952,-1.61910640238618,9.80045741338772));
#13071=CARTESIAN_POINT('Ctrl Pts',(1.28052117720835,-1.53549473839281,9.81006263172157));
#13072=CARTESIAN_POINT('Ctrl Pts',(1.42220211559756,-1.39999778009519,9.82351572832756));
#13073=CARTESIAN_POINT('Ctrl Pts',(1.46381375293885,-1.35643044474564,9.82757977430909));
#13074=CARTESIAN_POINT('Ctrl Pts',(1.50790516056004,-1.30587008931015,9.83195398429804));
#13075=CARTESIAN_POINT('Ctrl Pts',(1.51238920605761,-1.30067426980741,9.83239966016945));
#13076=CARTESIAN_POINT('Ctrl Pts',(1.51905615678763,-1.29286794856655,9.83306340158647));
#13077=CARTESIAN_POINT('Ctrl Pts',(1.52125928513371,-1.29027490393425,9.83328292075334));
#13078=CARTESIAN_POINT('Ctrl Pts',(1.52502932801671,-1.28581454845004,9.83365886170635));
#13079=CARTESIAN_POINT('Ctrl Pts',(1.52659946094424,-1.28394999529047,9.83381551989977));
#13080=CARTESIAN_POINT('Ctrl Pts',(1.52986447479925,-1.28005829279767,9.83414146230983));
#13081=CARTESIAN_POINT('Ctrl Pts',(1.53155874009731,-1.27803066083866,9.83431070183287));
#13082=CARTESIAN_POINT('Ctrl Pts',(1.53625081250909,-1.27239263794878,9.83477969726562));
#13083=CARTESIAN_POINT('Ctrl Pts',(1.53923994051465,-1.26877499606804,9.83507882373492));
#13084=CARTESIAN_POINT('Ctrl Pts',(1.55110244070676,-1.25431458613355,9.83626747254976));
#13085=CARTESIAN_POINT('Ctrl Pts',(1.55987449940735,-1.24338869028923,9.83714993568137));
#13086=CARTESIAN_POINT('Ctrl Pts',(1.66552277798042,-1.10892219239282,9.84783381853443));
#13087=CARTESIAN_POINT('Ctrl Pts',(1.74761783588492,-0.974434457931812,
9.85674701638314));
#13088=CARTESIAN_POINT('Ctrl Pts',(1.86696717975537,-0.714251545226549,
9.87339736341441));
#13089=CARTESIAN_POINT('Ctrl Pts',(1.90929294823105,-0.591874242693872,
9.88102353686478));
#13090=CARTESIAN_POINT('Ctrl Pts',(1.94271215935481,-0.452865558979571,
9.88993906177004));
#13091=CARTESIAN_POINT('Ctrl Pts',(1.94579656278178,-0.439424020398143,
9.89080337107382));
#13092=CARTESIAN_POINT('Ctrl Pts',(1.95010701342335,-0.419703591321184,
9.89207507303935));
#13093=CARTESIAN_POINT('Ctrl Pts',(1.95144267175982,-0.413448867042847,
9.89247895315575));
#13094=CARTESIAN_POINT('Ctrl Pts',(1.95374141545631,-0.402424797314688,
9.89319178354887));
#13095=CARTESIAN_POINT('Ctrl Pts',(1.95471717913912,-0.397658125598284,
9.89350032570075));
#13096=CARTESIAN_POINT('Ctrl Pts',(1.95658428145294,-0.388364264390364,
9.89410255710767));
#13097=CARTESIAN_POINT('Ctrl Pts',(1.95747737150352,-0.38383745485089,9.89439618825226));
#13098=CARTESIAN_POINT('Ctrl Pts',(1.95982977919919,-0.371692038995564,
9.89518482250007));
#13099=CARTESIAN_POINT('Ctrl Pts',(1.96126036414179,-0.364068010841824,
9.89568073804258));
#13100=CARTESIAN_POINT('Ctrl Pts',(1.96632284253102,-0.336192438968879,
9.89749723045264));
#13101=CARTESIAN_POINT('Ctrl Pts',(1.9696857203306,-0.315893949686496,9.89882630947225));
#13102=CARTESIAN_POINT('Ctrl Pts',(1.99777278921564,-0.128417222707487,
9.91116424253305));
#13103=CARTESIAN_POINT('Ctrl Pts',(2.00146629835545,0.0411853431269605,
9.92287128180867));
#13104=CARTESIAN_POINT('Ctrl Pts',(1.97677137018671,0.275378882401097,9.93929848210391));
#13105=CARTESIAN_POINT('Ctrl Pts',(1.96648131641869,0.341190042158797,9.94393224434978));
#13106=CARTESIAN_POINT('Ctrl Pts',(1.94587602771992,0.44021519068582,9.95083519303516));
#13107=CARTESIAN_POINT('Ctrl Pts',(1.93795336962955,0.47387758460321,9.95316897863299));
#13108=CARTESIAN_POINT('Ctrl Pts',(1.92425515378727,0.525967175611622,9.95674354955565));
#13109=CARTESIAN_POINT('Ctrl Pts',(1.91908079659945,0.544544149766249,9.95801096037916));
#13110=CARTESIAN_POINT('Ctrl Pts',(1.91220526349812,0.567912268300645,9.95959334549513));
#13111=CARTESIAN_POINT('Ctrl Pts',(1.91075429606123,0.572775117906503,9.95992198052444));
#13112=CARTESIAN_POINT('Ctrl Pts',(1.90841023020851,0.580523105905471,9.96044448957));
#13113=CARTESIAN_POINT('Ctrl Pts',(1.90752912185515,0.583411803812091,9.96063905186045));
#13114=CARTESIAN_POINT('Ctrl Pts',(1.90584483789668,0.588889091467024,9.96100748168583));
#13115=CARTESIAN_POINT('Ctrl Pts',(1.90504295701879,0.591478013272316,9.96118141908379));
#13116=CARTESIAN_POINT('Ctrl Pts',(1.90319319811501,0.597407288855301,9.96157931704202));
#13117=CARTESIAN_POINT('Ctrl Pts',(1.90214180251372,0.600746520352626,9.96180306868883));
#13118=CARTESIAN_POINT('Ctrl Pts',(1.89879349967892,0.611283809058716,9.962508131235));
#13119=CARTESIAN_POINT('Ctrl Pts',(1.89646444997975,0.618471700228498,9.96298759254051));
#13120=CARTESIAN_POINT('Ctrl Pts',(1.85548622121049,0.742530034692208,9.97123980166891));
#13121=CARTESIAN_POINT('Ctrl Pts',(1.80613460102611,0.85560960852316,9.97841682517459));
#13122=CARTESIAN_POINT('Ctrl Pts',(1.69833631411699,1.05104361143335,9.9913735853075));
#13123=CARTESIAN_POINT('Ctrl Pts',(1.64348820989429,1.13489393037237,9.99714519583903));
#13124=CARTESIAN_POINT('Ctrl Pts',(1.55189005821547,1.25427558029602,10.0060938429019));
#13125=CARTESIAN_POINT('Ctrl Pts',(1.51969245447149,1.29309870041465,10.0091327791738));
#13126=CARTESIAN_POINT('Ctrl Pts',(1.46588350917848,1.35319176825916,10.0140852685697));
#13127=CARTESIAN_POINT('Ctrl Pts',(1.44519755200979,1.37526226814515,10.0159618368398));
#13128=CARTESIAN_POINT('Ctrl Pts',(1.41794905463334,1.40304068640936,10.0184039171176));
#13129=CARTESIAN_POINT('Ctrl Pts',(1.4118392752602,1.40918861273704,10.0189496248935));
#13130=CARTESIAN_POINT('Ctrl Pts',(1.40191004236041,1.41905044799409,10.0198335870101));
#13131=CARTESIAN_POINT('Ctrl Pts',(1.39811539350248,1.42278926281316,10.0201707387771));
#13132=CARTESIAN_POINT('Ctrl Pts',(1.39084122867069,1.42989919586673,10.0208157921251));
#13133=CARTESIAN_POINT('Ctrl Pts',(1.38736431390615,1.43327293057874,10.0211235758412));
#13134=CARTESIAN_POINT('Ctrl Pts',(1.37937738156402,1.44096655177306,10.0218293864971));
#13135=CARTESIAN_POINT('Ctrl Pts',(1.37485931587067,1.44527797471506,10.0222277763976));
#13136=CARTESIAN_POINT('Ctrl Pts',(1.36087010217768,1.45850240713906,10.0234586782001));
#13137=CARTESIAN_POINT('Ctrl Pts',(1.35133212525532,1.46734392034201,10.0242942422111));
#13138=CARTESIAN_POINT('Ctrl Pts',(1.2516033751738,1.55799340231525,10.0329945744169));
#13139=CARTESIAN_POINT('Ctrl Pts',(1.15420554333993,1.63145767517632,10.0412116130469));
#13140=CARTESIAN_POINT('Ctrl Pts',(0.955808788950157,1.75440273624483,10.0573597662389));
#13141=CARTESIAN_POINT('Ctrl Pts',(0.85611063822225,1.80515196118373,10.0652254429485));
#13142=CARTESIAN_POINT('Ctrl Pts',(0.71208958779295,1.86383424100899,10.0759188473012));
#13143=CARTESIAN_POINT('Ctrl Pts',(0.670951447758556,1.87903548601276,10.0788999464845));
#13144=CARTESIAN_POINT('Ctrl Pts',(0.607753655898465,1.90004754720504,10.0833372034989));
#13145=CARTESIAN_POINT('Ctrl Pts',(0.586041892350024,1.90685610314944,10.0848366269482));
#13146=CARTESIAN_POINT('Ctrl Pts',(0.559074648536351,1.91480856649511,10.0866642501847));
#13147=CARTESIAN_POINT('Ctrl Pts',(0.553925856333002,1.91630437463869,10.0870116401075));
#13148=CARTESIAN_POINT('Ctrl Pts',(0.545806142506566,1.91862782415021,10.0875569651969));
#13149=CARTESIAN_POINT('Ctrl Pts',(0.542839272955747,1.91946935293457,10.087755694763));
#13150=CARTESIAN_POINT('Ctrl Pts',(0.537273423296608,1.92103412481024,10.0881275080933));
#13151=CARTESIAN_POINT('Ctrl Pts',(0.53467495742286,1.92175896773887,10.0883006811837));
#13152=CARTESIAN_POINT('Ctrl Pts',(0.528748479295534,1.92339921008778,10.0886947192377));
#13153=CARTESIAN_POINT('Ctrl Pts',(0.52541956356879,1.92431124259613,10.0889153866973));
#13154=CARTESIAN_POINT('Ctrl Pts',(0.515227879912795,1.92707506869052,10.0895889895652));
#13155=CARTESIAN_POINT('Ctrl Pts',(0.508357473466802,1.92889884945905,10.090040329153));
#13156=CARTESIAN_POINT('Ctrl Pts',(0.454202445240981,1.94296510412912,10.0935774106964));
#13157=CARTESIAN_POINT('Ctrl Pts',(0.406487882822977,1.95350499579497,10.0965709042129));
#13158=CARTESIAN_POINT('Ctrl Pts',(0.336081173830721,1.96636546643905,10.1008732233337));
#13159=CARTESIAN_POINT('Ctrl Pts',(0.313663461052419,1.97006573369058,10.1022262492787));
#13160=CARTESIAN_POINT('Ctrl Pts',(0.185685916817995,1.98894974472243,10.1098787485907));
#13161=CARTESIAN_POINT('Ctrl Pts',(0.0791032665448506,1.99603225096116,
10.1159843263449));
#13162=CARTESIAN_POINT('Ctrl Pts',(-0.145651283860061,1.99292917366836,
10.1290965099994));
#13163=CARTESIAN_POINT('Ctrl Pts',(-0.263368743202459,1.98081093067287,
10.1361096641252));
#13164=CARTESIAN_POINT('Ctrl Pts',(-0.392556735101928,1.95578852129427,
10.1443182708401));
#13165=CARTESIAN_POINT('Ctrl Pts',(-0.405773520362426,1.95308918543334,
10.1451638948004));
#13166=CARTESIAN_POINT('Ctrl Pts',(-0.425158849545157,1.94892475296259,
10.1464131620989));
#13167=CARTESIAN_POINT('Ctrl Pts',(-0.431349601427333,1.94756392960523,
10.1468134689344));
#13168=CARTESIAN_POINT('Ctrl Pts',(-0.442272711072371,1.94510822444996,
10.1475222097685));
#13169=CARTESIAN_POINT('Ctrl Pts',(-0.447007775440067,1.94402551521184,
10.1478302509018));
#13170=CARTESIAN_POINT('Ctrl Pts',(-0.45625125632837,1.94187636490389,10.148433189329));
#13171=CARTESIAN_POINT('Ctrl Pts',(-0.460760008225332,1.94081148999511,
10.1487280344726));
#13172=CARTESIAN_POINT('Ctrl Pts',(-0.472901669886414,1.93789918402654,
10.1495240596415));
#13173=CARTESIAN_POINT('Ctrl Pts',(-0.480527385301628,1.93602238258862,
10.1500261833138));
#13174=CARTESIAN_POINT('Ctrl Pts',(-0.50851484841694,1.92895871252512,10.1518771668622));
#13175=CARTESIAN_POINT('Ctrl Pts',(-0.528804771385689,1.92349539205547,
10.1532349184836));
#13176=CARTESIAN_POINT('Ctrl Pts',(-0.702168362297694,1.87386475707725,
10.1649768033311));
#13177=CARTESIAN_POINT('Ctrl Pts',(-0.849498418499253,1.81183389701955,
10.1759728743808));
#13178=CARTESIAN_POINT('Ctrl Pts',(-1.05351265350642,1.69553846678368,10.1923575302063));
#13179=CARTESIAN_POINT('Ctrl Pts',(-1.11699491278831,1.65440714573147,10.1976313981587));
#13180=CARTESIAN_POINT('Ctrl Pts',(-1.20588764102468,1.58935754766939,10.2051488853783));
#13181=CARTESIAN_POINT('Ctrl Pts',(-1.23324955553266,1.56822136492417,10.2074821561844));
#13182=CARTESIAN_POINT('Ctrl Pts',(-1.27499573129756,1.53420505111607,10.211056028605));
#13183=CARTESIAN_POINT('Ctrl Pts',(-1.28976490938993,1.52181004083861,10.2123232438763));
#13184=CARTESIAN_POINT('Ctrl Pts',(-1.30819190486062,1.50588420923139,10.2139054204633));
#13185=CARTESIAN_POINT('Ctrl Pts',(-1.31201847140064,1.50255144458737,10.2142340382317));
#13186=CARTESIAN_POINT('Ctrl Pts',(-1.31810208535009,1.49721193406086,10.2147565262599));
#13187=CARTESIAN_POINT('Ctrl Pts',(-1.32036733301462,1.49521462977877,10.214951084699));
#13188=CARTESIAN_POINT('Ctrl Pts',(-1.32465691210462,1.49141509093844,10.215319511586));
#13189=CARTESIAN_POINT('Ctrl Pts',(-1.32668208130511,1.48961389745618,10.2154934498785));
#13190=CARTESIAN_POINT('Ctrl Pts',(-1.3313148060788,1.48547659220756,10.2158913555569));
#13191=CARTESIAN_POINT('Ctrl Pts',(-1.33391988421804,1.48313774202744,10.2161151140011));
#13192=CARTESIAN_POINT('Ctrl Pts',(-1.34212809986904,1.47572925083891,10.2168202194162));
#13193=CARTESIAN_POINT('Ctrl Pts',(-1.34770867950719,1.4706345493704,10.2172997164733));
#13194=CARTESIAN_POINT('Ctrl Pts',(-1.44350882101068,1.38217204215057,10.2255358500459));
#13195=CARTESIAN_POINT('Ctrl Pts',(-1.52588224592425,1.29066286106292,10.2326992282234));
#13196=CARTESIAN_POINT('Ctrl Pts',(-1.65917091336927,1.11184906702836,10.2456466970642));
#13197=CARTESIAN_POINT('Ctrl Pts',(-1.71288827551406,1.0271655423483,10.2514228947977));
#13198=CARTESIAN_POINT('Ctrl Pts',(-1.78379974316823,0.894225624335424,
10.2603824399163));
#13199=CARTESIAN_POINT('Ctrl Pts',(-1.80587763974001,0.848755771137132,
10.2634277057106));
#13200=CARTESIAN_POINT('Ctrl Pts',(-1.83839196520735,0.774764665366407,
10.2683896100349));
#13201=CARTESIAN_POINT('Ctrl Pts',(-1.84994557992173,0.746757324311987,
10.2702690821462));
#13202=CARTESIAN_POINT('Ctrl Pts',(-1.86398024679475,0.710408623386117,
10.272714432388));
#13203=CARTESIAN_POINT('Ctrl Pts',(-1.86705115963712,0.702298181752679,
10.2732604399878));
#13204=CARTESIAN_POINT('Ctrl Pts',(-1.87192324935163,0.689172910640475,
10.2741447703062));
#13205=CARTESIAN_POINT('Ctrl Pts',(-1.87375741381474,0.68417037753718,10.2744819887589));
#13206=CARTESIAN_POINT('Ctrl Pts',(-1.87722090588861,0.674605589668786,
10.2751270912739));
#13207=CARTESIAN_POINT('Ctrl Pts',(-1.87885370165126,0.670044624057689,
10.2754348571419));
#13208=CARTESIAN_POINT('Ctrl Pts',(-1.88255262331098,0.65959241844588,10.2761405157749));
#13209=CARTESIAN_POINT('Ctrl Pts',(-1.88460773089371,0.653697359025662,
10.276538770948));
#13210=CARTESIAN_POINT('Ctrl Pts',(-1.89085516959573,0.635502286251923,
10.277768849074));
#13211=CARTESIAN_POINT('Ctrl Pts',(-1.89495494095966,0.623171073353046,
10.2786037182227));
#13212=CARTESIAN_POINT('Ctrl Pts',(-1.93511572345898,0.498314238767923,
10.2870706469722));
#13213=CARTESIAN_POINT('Ctrl Pts',(-1.96122463182681,0.382856144628593,
10.2950333271179));
#13214=CARTESIAN_POINT('Ctrl Pts',(-1.98887519146185,0.177185738021458,
10.3093737644185));
#13215=CARTESIAN_POINT('Ctrl Pts',(-1.99481690562072,0.0878868247181338,
10.3156443863969));
#13216=CARTESIAN_POINT('Ctrl Pts',(-1.99468269327559,-0.0899240165370003,
10.3279929204652));
#13217=CARTESIAN_POINT('Ctrl Pts',(-1.98873717572502,-0.178252210388867,
10.3340578020223));
#13218=CARTESIAN_POINT('Ctrl Pts',(-1.97590266073967,-0.27367445741639,
10.3403469262823));
#13219=CARTESIAN_POINT('Ctrl Pts',(-1.97481170461867,-0.281438749290134,
10.3408567158645));
#13220=CARTESIAN_POINT('Ctrl Pts',(-1.97315972090685,-0.292713015128034,
10.3415939420188));
#13221=CARTESIAN_POINT('Ctrl Pts',(-1.97263506392022,-0.296228119035658,
10.3418233676241));
#13222=CARTESIAN_POINT('Ctrl Pts',(-1.97169260976568,-0.302428837693241,
10.3422273018549));
#13223=CARTESIAN_POINT('Ctrl Pts',(-1.97127871501168,-0.305115023190094,
10.3424020300434));
#13224=CARTESIAN_POINT('Ctrl Pts',(-1.97039760539452,-0.310756806331503,
10.3427684601465));
#13225=CARTESIAN_POINT('Ctrl Pts',(-1.96992923106563,-0.313712194388884,
10.3429600951018));
#13226=CARTESIAN_POINT('Ctrl Pts',(-1.96866837529435,-0.321553874444086,
10.3434677587129));
#13227=CARTESIAN_POINT('Ctrl Pts',(-1.96786434615075,-0.32643832873687,
10.3437831375364));
#13228=CARTESIAN_POINT('Ctrl Pts',(-1.96406090146752,-0.349019339251954,
10.345237484841));
#13229=CARTESIAN_POINT('Ctrl Pts',(-1.96084078798335,-0.366678581940024,
10.3463644327846));
#13230=CARTESIAN_POINT('Ctrl Pts',(-1.95135781817718,-0.414979787523451,
10.3494242008028));
#13231=CARTESIAN_POINT('Ctrl Pts',(-1.94461185341893,-0.445522752541793,
10.3513339241093));
#13232=CARTESIAN_POINT('Ctrl Pts',(-1.91836253740937,-0.552371411078604,
10.3579660146973));
#13233=CARTESIAN_POINT('Ctrl Pts',(-1.89506143481118,-0.627672603519763,
10.3625535576307));
#13234=CARTESIAN_POINT('Ctrl Pts',(-1.81072235196523,-0.852211113602893,
10.3764766998439));
#13235=CARTESIAN_POINT('Ctrl Pts',(-1.7360267200154,-0.995581852369622,
10.3857619067119));
#13236=CARTESIAN_POINT('Ctrl Pts',(-1.63819119571098,-1.13819955652697,
10.3964640605663));
#13237=CARTESIAN_POINT('Ctrl Pts',(-1.63138533480839,-1.14793314446265,
10.3972021331043));
#13238=CARTESIAN_POINT('Ctrl Pts',(-1.61697581630869,-1.16815434130887,
10.3987519890598));
#13239=CARTESIAN_POINT('Ctrl Pts',(-1.60935613241041,-1.17862979010106,
10.3995643499355));
#13240=CARTESIAN_POINT('Ctrl Pts',(-1.59791856831349,-1.19403630024654,
10.4007735781002));
#13241=CARTESIAN_POINT('Ctrl Pts',(-1.59417861635016,-1.19902501016681,
10.4011674114112));
#13242=CARTESIAN_POINT('Ctrl Pts',(-1.58749197189173,-1.20785771527005,
10.4018688122353));
#13243=CARTESIAN_POINT('Ctrl Pts',(-1.58455453879079,-1.21170868366848,
10.4021760143881));
#13244=CARTESIAN_POINT('Ctrl Pts',(-1.57835373001984,-1.21977682363448,
10.4028225989371));
#13245=CARTESIAN_POINT('Ctrl Pts',(-1.57508741558319,-1.22399167844573,
10.4031620961127));
#13246=CARTESIAN_POINT('Ctrl Pts',(-1.56645306968251,-1.23504165009495,
10.4040567072672));
#13247=CARTESIAN_POINT('Ctrl Pts',(-1.56105724514487,-1.24185481051626,
10.404612925718));
#13248=CARTESIAN_POINT('Ctrl Pts',(-1.53653796891897,-1.27240231691258,
10.4071279336413));
#13249=CARTESIAN_POINT('Ctrl Pts',(-1.51691743770921,-1.29573064414492,
10.4091066762781));
#13250=CARTESIAN_POINT('Ctrl Pts',(-1.46308583268472,-1.3568360821527,10.4144512115272));
#13251=CARTESIAN_POINT('Ctrl Pts',(-1.42795046770521,-1.39376505465807,
10.417854010747));
#13252=CARTESIAN_POINT('Ctrl Pts',(-1.31940814578906,-1.49943198723187,
10.4281182357644));
#13253=CARTESIAN_POINT('Ctrl Pts',(-1.24218150381892,-1.56400637401052,
10.43511671074));
#13254=CARTESIAN_POINT('Ctrl Pts',(-1.06137171642551,-1.69332459510875,
10.4506264487829));
#13255=CARTESIAN_POINT('Ctrl Pts',(-0.956026066390776,-1.75495857719636,
10.4591154896717));
#13256=CARTESIAN_POINT('Ctrl Pts',(-0.838841174018736,-1.80981503931484,
10.4675632762204));
#13257=CARTESIAN_POINT('Ctrl Pts',(-0.83195936508958,-1.81298886126467,
10.4680558597143));
#13258=CARTESIAN_POINT('Ctrl Pts',(-0.821868305986221,-1.81757319952556,
10.4687728370571));
#13259=CARTESIAN_POINT('Ctrl Pts',(-0.818673263236856,-1.81901455094251,
10.4689990716429));
#13260=CARTESIAN_POINT('Ctrl Pts',(-0.813000440978043,-1.82155570711824,
10.4693993573033));
#13261=CARTESIAN_POINT('Ctrl Pts',(-0.810524201431194,-1.82265889030597,
10.4695736148504));
#13262=CARTESIAN_POINT('Ctrl Pts',(-0.805286634296978,-1.82497948092575,
10.4699411911807));
#13263=CARTESIAN_POINT('Ctrl Pts',(-0.802524798282799,-1.82619566794335,
10.4701344348243));
#13264=CARTESIAN_POINT('Ctrl Pts',(-0.795120863914019,-1.82943598415184,
10.4706509478164));
#13265=CARTESIAN_POINT('Ctrl Pts',(-0.79047376094071,-1.83144872790875,
10.4709735265204));
#13266=CARTESIAN_POINT('Ctrl Pts',(-0.768202191474188,-1.8409943830577,
10.4725120401972));
#13267=CARTESIAN_POINT('Ctrl Pts',(-0.750476698736424,-1.84829102574646,
10.473714194397));
#13268=CARTESIAN_POINT('Ctrl Pts',(-0.700761556226098,-1.86792293660586,
10.4770314407138));
#13269=CARTESIAN_POINT('Ctrl Pts',(-0.668553818667454,-1.87969118054719,
10.47911841663));
#13270=CARTESIAN_POINT('Ctrl Pts',(-0.549978698530407,-1.91958304491796,
10.4866319796354));
#13271=CARTESIAN_POINT('Ctrl Pts',(-0.462017338625488,-1.94263168315626,
10.4918857392383));
#13272=CARTESIAN_POINT('Ctrl Pts',(-0.218444923609957,-1.98896775611201,
10.50626531036));
#13273=CARTESIAN_POINT('Ctrl Pts',(-0.0612006966267063,-1.99998901408843,
10.5154120990274));
#13274=CARTESIAN_POINT('Ctrl Pts',(0.108221283271541,-1.99185162813035,
10.5260044486931));
#13275=CARTESIAN_POINT('Ctrl Pts',(0.120738291768116,-1.99113209207662,
10.5267909904844));
#13276=CARTESIAN_POINT('Ctrl Pts',(0.139386654024394,-1.98988361011119,
10.5279690494609));
#13277=CARTESIAN_POINT('Ctrl Pts',(0.145523854900972,-1.98944420062125,
10.5283577579322));
#13278=CARTESIAN_POINT('Ctrl Pts',(0.156478410912519,-1.98860891893015,
10.5290534194414));
#13279=CARTESIAN_POINT('Ctrl Pts',(0.16129656585185,-1.98822391664034,10.5293600287945));
#13280=CARTESIAN_POINT('Ctrl Pts',(0.171471354898446,-1.98737365556514,
10.5300088782808));
#13281=CARTESIAN_POINT('Ctrl Pts',(0.176827594360679,-1.98690424362226,
10.5303512466373));
#13282=CARTESIAN_POINT('Ctrl Pts',(0.191035310313647,-1.98560119767137,
10.5312615518225));
#13283=CARTESIAN_POINT('Ctrl Pts',(0.199883144178838,-1.98473003968,10.5318306643262));
#13284=CARTESIAN_POINT('Ctrl Pts',(0.241079576602884,-1.98039557265595,
10.5344910971257));
#13285=CARTESIAN_POINT('Ctrl Pts',(0.273344584231785,-1.97620052549477,
10.5366053077691));
#13286=CARTESIAN_POINT('Ctrl Pts',(0.360611388073228,-1.96267628755898,
10.542410723554));
#13287=CARTESIAN_POINT('Ctrl Pts',(0.415344465229656,-1.95182652943739,
10.5461472710146));
#13288=CARTESIAN_POINT('Ctrl Pts',(0.570926474518173,-1.91414502786993,
10.5570357615523));
#13289=CARTESIAN_POINT('Ctrl Pts',(0.670216771690477,-1.8816786353931,10.5643221754441));
#13290=CARTESIAN_POINT('Ctrl Pts',(0.83725513101289,-1.81215458047431,10.5769378764125));
#13291=CARTESIAN_POINT('Ctrl Pts',(0.906255101035868,-1.77865221175082,
10.5822601569202));
#13292=CARTESIAN_POINT('Ctrl Pts',(1.00433413343109,-1.7238375453336,10.5898440444206));
#13293=CARTESIAN_POINT('Ctrl Pts',(1.03503717104551,-1.70557948507905,10.5922204836509));
#13294=CARTESIAN_POINT('Ctrl Pts',(1.07020772134307,-1.68336495761762,10.5949311421024));
#13295=CARTESIAN_POINT('Ctrl Pts',(1.07516601240073,-1.68020242686342,10.5953130107083));
#13296=CARTESIAN_POINT('Ctrl Pts',(1.08307058966223,-1.67511135709487,10.5959212570056));
#13297=CARTESIAN_POINT('Ctrl Pts',(1.08602583433157,-1.67319689471722,10.5961485389156));
#13298=CARTESIAN_POINT('Ctrl Pts',(1.09124913802191,-1.66979347287572,10.5965500177673));
#13299=CARTESIAN_POINT('Ctrl Pts',(1.09351924558171,-1.66830770039268,10.5967244254786));
#13300=CARTESIAN_POINT('Ctrl Pts',(1.09830077468376,-1.6651642638454,10.5970916053569));
#13301=CARTESIAN_POINT('Ctrl Pts',(1.1008114722812,-1.66350555155278,10.597284305124));
#13302=CARTESIAN_POINT('Ctrl Pts',(1.10750528834206,-1.65906143810388,10.5977978255037));
#13303=CARTESIAN_POINT('Ctrl Pts',(1.11168168448165,-1.65626587624701,10.598117969386));
#13304=CARTESIAN_POINT('Ctrl Pts',(1.13138612333396,-1.64296817194723,10.5996274599238));
#13305=CARTESIAN_POINT('Ctrl Pts',(1.14677681283736,-1.63226283953755,10.6008036473113));
#13306=CARTESIAN_POINT('Ctrl Pts',(1.18902416740431,-1.60198417635024,10.6040312050764));
#13307=CARTESIAN_POINT('Ctrl Pts',(1.21554709772955,-1.58195363059456,10.6060562698114));
#13308=CARTESIAN_POINT('Ctrl Pts',(1.30962893178172,-1.507137472088,10.6132844504131));
#13309=CARTESIAN_POINT('Ctrl Pts',(1.37409103710161,-1.4486087153526,10.618326625315));
#13310=CARTESIAN_POINT('Ctrl Pts',(1.53842146773951,-1.27853110688962,10.6320431346923));
#13311=CARTESIAN_POINT('Ctrl Pts',(1.62988055822566,-1.15968298120237,10.6407137791965));
#13312=CARTESIAN_POINT('Ctrl Pts',(1.71482955068276,-1.01911955222699,10.6508737596746));
#13313=CARTESIAN_POINT('Ctrl Pts',(1.72231697876218,-1.00641405805578,10.6517908609697));
#13314=CARTESIAN_POINT('Ctrl Pts',(1.73478709289562,-0.984706624783944,
10.6533562803772));
#13315=CARTESIAN_POINT('Ctrl Pts',(1.73984233691453,-0.975746909253835,
10.6540019894891));
#13316=CARTESIAN_POINT('Ctrl Pts',(1.74785556818487,-0.96128429740752,10.6550438009375));
#13317=CARTESIAN_POINT('Ctrl Pts',(1.75085744720766,-0.955805830591612,
10.6554383311527));
#13318=CARTESIAN_POINT('Ctrl Pts',(1.75614856084709,-0.94604091261946,10.6561413947038));
#13319=CARTESIAN_POINT('Ctrl Pts',(1.75844796989653,-0.941760007962438,
10.6564495628232));
#13320=CARTESIAN_POINT('Ctrl Pts',(1.76321073800917,-0.932814708538876,
10.6570934170523));
#13321=CARTESIAN_POINT('Ctrl Pts',(1.76567128068277,-0.928148864562311,
10.657429199957));
#13322=CARTESIAN_POINT('Ctrl Pts',(1.77201715713776,-0.915998835188689,
10.6583034927319));
#13323=CARTESIAN_POINT('Ctrl Pts',(1.77587355941238,-0.908499735066821,
10.6588430174788));
#13324=CARTESIAN_POINT('Ctrl Pts',(1.7923323104568,-0.875989068056561,10.6611817766987));
#13325=CARTESIAN_POINT('Ctrl Pts',(1.80445415207244,-0.850739113194671,
10.6629976926831));
#13326=CARTESIAN_POINT('Ctrl Pts',(1.83482268135327,-0.783909782881535,
10.667805233995));
#13327=CARTESIAN_POINT('Ctrl Pts',(1.85218751341452,-0.741949931639712,
10.6708253492995));
#13328=CARTESIAN_POINT('Ctrl Pts',(1.93406376010616,-0.523269127556908,
10.6865719840826));
#13329=CARTESIAN_POINT('Ctrl Pts',(1.97476212276504,-0.33869096451433,10.7000043573005));
#13330=CARTESIAN_POINT('Ctrl Pts',(1.99234660748923,-0.107314659255958,
10.7157704787975));
#13331=CARTESIAN_POINT('Ctrl Pts',(1.99422849045971,-0.0633629374779213,
10.7187123599862));
#13332=CARTESIAN_POINT('Ctrl Pts',(1.99472308297479,-0.0124610671240032,
10.7220318806717));
#13333=CARTESIAN_POINT('Ctrl Pts',(1.99475431136252,-0.00554045743301629,
10.7224813256452));
#13334=CARTESIAN_POINT('Ctrl Pts',(1.99474715998255,0.00479442663909356,
10.7231495620163));
#13335=CARTESIAN_POINT('Ctrl Pts',(1.99473603228525,0.00820857572055919,
10.7233698357902));
#13336=CARTESIAN_POINT('Ctrl Pts',(1.99470044057599,0.0143169061739684,
10.7237630545445));
#13337=CARTESIAN_POINT('Ctrl Pts',(1.99467928378891,0.0170110717114556,
10.7239361825155));
#13338=CARTESIAN_POINT('Ctrl Pts',(1.99462195526506,0.0228141224668951,
10.7243084245484));
#13339=CARTESIAN_POINT('Ctrl Pts',(1.99458397396818,0.025922957433382,10.7245074357078));
#13340=CARTESIAN_POINT('Ctrl Pts',(1.99445903355514,0.0345066210568112,
10.725055821331));
#13341=CARTESIAN_POINT('Ctrl Pts',(1.99435679973447,0.0399812516272016,
10.725404349623));
#13342=CARTESIAN_POINT('Ctrl Pts',(1.99367813474335,0.069755786523588,10.7272935142543));
#13343=CARTESIAN_POINT('Ctrl Pts',(1.99268010159679,0.094045294378193,10.728811638043));
#13344=CARTESIAN_POINT('Ctrl Pts',(1.98837141180654,0.166562388805577,10.7332913557142));
#13345=CARTESIAN_POINT('Ctrl Pts',(1.98375149517328,0.21469653039739,10.7361952091585));
#13346=CARTESIAN_POINT('Ctrl Pts',(1.95626295608673,0.421671505889593,10.7485587241063));
#13347=CARTESIAN_POINT('Ctrl Pts',(1.91602708555336,0.577594475442474,10.7576065949878));
#13348=CARTESIAN_POINT('Ctrl Pts',(1.85427768853177,0.735365328215826,10.7677183957267));
#13349=CARTESIAN_POINT('Ctrl Pts',(1.85095449541226,0.743690369059949,10.7682547377486));
#13350=CARTESIAN_POINT('Ctrl Pts',(1.84297473249911,0.763295897262113,10.7695247313493));
#13351=CARTESIAN_POINT('Ctrl Pts',(1.83827056517342,0.774556526290826,10.7702596001816));
#13352=CARTESIAN_POINT('Ctrl Pts',(1.81403816514736,0.831098570915526,10.7739787031621));
#13353=CARTESIAN_POINT('Ctrl Pts',(1.7929402581437,0.875684819317724,10.7770068549754));
#13354=CARTESIAN_POINT('Ctrl Pts',(1.7657661801811,0.928003477347426,10.7806966048273));
#13355=CARTESIAN_POINT('Ctrl Pts',(1.76125686700291,0.936533448543688,10.7813026062099));
#13356=CARTESIAN_POINT('Ctrl Pts',(1.75378596809602,0.950420858841792,10.7822966393666));
#13357=CARTESIAN_POINT('Ctrl Pts',(1.75086125555542,0.955798039990442,10.7826833612187));
#13358=CARTESIAN_POINT('Ctrl Pts',(1.74558455320622,0.965393939784085,10.7833768169972));
#13359=CARTESIAN_POINT('Ctrl Pts',(1.74324189321838,0.969617755829501,10.7836832156246));
#13360=CARTESIAN_POINT('Ctrl Pts',(1.73825002671792,0.97854152433879,10.7843330355319));
#13361=CARTESIAN_POINT('Ctrl Pts',(1.73559705066357,0.983239313201456,10.7846765904934));
#13362=CARTESIAN_POINT('Ctrl Pts',(1.72848099785841,0.995721607690317,10.7855933838986));
#13363=CARTESIAN_POINT('Ctrl Pts',(1.72398443765877,1.00348678831569,10.7861678279731));
#13364=CARTESIAN_POINT('Ctrl Pts',(1.70249255293058,1.04003063407145,10.7888909654517));
#13365=CARTESIAN_POINT('Ctrl Pts',(1.6848289480676,1.06840806960292,10.791063882541));
#13366=CARTESIAN_POINT('Ctrl Pts',(1.6346257325426,1.14471899921039,10.7970731771369));
#13367=CARTESIAN_POINT('Ctrl Pts',(1.60069983857038,1.19169704020361,10.8009588952385));
#13368=CARTESIAN_POINT('Ctrl Pts',(1.46183224266941,1.36734350565572,10.8162137414634));
#13369=CARTESIAN_POINT('Ctrl Pts',(1.34304586006897,1.4841839929986,10.8280230207915));
#13370=CARTESIAN_POINT('Ctrl Pts',(1.20457537589151,1.5899983065899,10.8398882087009));
#13371=CARTESIAN_POINT('Ctrl Pts',(1.19794907056745,1.59499670193988,10.8404517448334));
#13372=CARTESIAN_POINT('Ctrl Pts',(1.15998333046581,1.62326518944805,10.8436555744936));
#13373=CARTESIAN_POINT('Ctrl Pts',(1.12799482236966,1.64565469744037,10.8462587041124));
#13374=CARTESIAN_POINT('Ctrl Pts',(1.0898313312646,1.67073011290138,10.8492353091764));
#13375=CARTESIAN_POINT('Ctrl Pts',(1.08427715325324,1.67434001884288,10.8496653968606));
#13376=CARTESIAN_POINT('Ctrl Pts',(1.07584626368473,1.67976008090876,10.8503134179153));
#13377=CARTESIAN_POINT('Ctrl Pts',(1.07298280759178,1.68159061829356,10.8505326742979));
#13378=CARTESIAN_POINT('Ctrl Pts',(1.06784200519072,1.68485853012347,10.8509247911943));
#13379=CARTESIAN_POINT('Ctrl Pts',(1.06556642355902,1.68629861289665,10.8510978304081));
#13380=CARTESIAN_POINT('Ctrl Pts',(1.06070105572988,1.68936383902179,10.851466664683));
#13381=CARTESIAN_POINT('Ctrl Pts',(1.05811045780334,1.69098763142009,10.8516623700795));
#13382=CARTESIAN_POINT('Ctrl Pts',(1.05100268997079,1.69542006626987,10.8521974839793));
#13383=CARTESIAN_POINT('Ctrl Pts',(1.04647796233831,1.69821663262926,10.8525361032482));
#13384=CARTESIAN_POINT('Ctrl Pts',(1.03635612263194,1.70441675059738,10.8532892076642));
#13385=CARTESIAN_POINT('Ctrl Pts',(1.03075329425527,1.70781091511418,10.8537031047277));
#13386=CARTESIAN_POINT('Ctrl Pts',(1.01348724605751,1.71815467498233,10.8549698085792));
#13387=CARTESIAN_POINT('Ctrl Pts',(1.00176945093445,1.72501300710784,10.8558172214698));
#13388=CARTESIAN_POINT('Ctrl Pts',(0.957266090258331,1.7504540347863,10.8589932170021));
#13389=CARTESIAN_POINT('Ctrl Pts',(0.924024397900348,1.76822707115688,10.8612795273042));
#13390=CARTESIAN_POINT('Ctrl Pts',(0.764848599869605,1.84761635888256,10.8719212785174));
#13391=CARTESIAN_POINT('Ctrl Pts',(0.633147938843941,1.89678897016429,10.8798673279181));
#13392=CARTESIAN_POINT('Ctrl Pts',(0.398270067624479,1.95726360566081,10.8940972575643));
#13393=CARTESIAN_POINT('Ctrl Pts',(0.297365000135306,1.97511254391445,10.9002235989706));
#13394=CARTESIAN_POINT('Ctrl Pts',(0.182801897187334,1.98639748964364,10.9074103018087));
#13395=CARTESIAN_POINT('Ctrl Pts',(0.170047416009286,1.98752997074415,10.9082134201533));
#13396=CARTESIAN_POINT('Ctrl Pts',(0.151096708408553,1.98902887326342,10.909411499708));
#13397=CARTESIAN_POINT('Ctrl Pts',(0.144908076426884,1.98948931184355,10.9098035085367));
#13398=CARTESIAN_POINT('Ctrl Pts',(0.133889393864926,1.99025742459117,10.910502858357));
#13399=CARTESIAN_POINT('Ctrl Pts',(0.129060161153479,1.9905764140209,10.9108098417131));
#13400=CARTESIAN_POINT('Ctrl Pts',(0.118892520502812,1.99121087006749,10.9114571949216));
#13401=CARTESIAN_POINT('Ctrl Pts',(0.113553916667409,1.99152244968456,10.9117976842396));
#13402=CARTESIAN_POINT('Ctrl Pts',(0.0994670428453642,1.99228778240215,
10.9126977184032));
#13403=CARTESIAN_POINT('Ctrl Pts',(0.0907170012092321,1.99270537765926,
10.9132583921254));
#13404=CARTESIAN_POINT('Ctrl Pts',(0.0508163584331215,1.99434628750642,
10.9158226862553));
#13405=CARTESIAN_POINT('Ctrl Pts',(0.0196439302237547,1.99489682687232,
10.9178472310749));
#13406=CARTESIAN_POINT('Ctrl Pts',(-0.0640937880287946,1.994412918141,10.9233461230898));
#13407=CARTESIAN_POINT('Ctrl Pts',(-0.116623582303313,1.99203138321846,
10.9268601614018));
#13408=CARTESIAN_POINT('Ctrl Pts',(-0.347019774684995,1.97244188629581,
10.9425483617762));
#13409=CARTESIAN_POINT('Ctrl Pts',(-0.522178578381608,1.93346017966513,
10.9552937245448));
#13410=CARTESIAN_POINT('Ctrl Pts',(-0.729662010320395,1.8569938569278,10.9703012580068));
#13411=CARTESIAN_POINT('Ctrl Pts',(-0.769053228237434,1.84102976552721,
10.9731409907176));
#13412=CARTESIAN_POINT('Ctrl Pts',(-0.814101039336908,1.82107466773797,
10.9763535481769));
#13413=CARTESIAN_POINT('Ctrl Pts',(-0.820280538466502,1.81829955979445,
10.976793454484));
#13414=CARTESIAN_POINT('Ctrl Pts',(-0.829568244223379,1.8140716248345,10.9774533167758));
#13415=CARTESIAN_POINT('Ctrl Pts',(-0.832686956982909,1.8126422051683,10.9776746677651));
#13416=CARTESIAN_POINT('Ctrl Pts',(-0.838249645143889,1.81007523646692,
10.9780690596784));
#13417=CARTESIAN_POINT('Ctrl Pts',(-0.840695008634041,1.8089407762612,10.9782422881299));
#13418=CARTESIAN_POINT('Ctrl Pts',(-0.845437063942329,1.80672913526672,
10.9785779249696));
#13419=CARTESIAN_POINT('Ctrl Pts',(-0.847733985157901,1.80565253797444,
10.9787403683061));
#13420=CARTESIAN_POINT('Ctrl Pts',(-0.854277159541992,1.80257042850529,
10.9792027628207));
#13421=CARTESIAN_POINT('Ctrl Pts',(-0.858518429323778,1.80055428205638,
10.9795020609028));
#13422=CARTESIAN_POINT('Ctrl Pts',(-0.876824727420797,1.79177274031775,
10.9807922290948));
#13423=CARTESIAN_POINT('Ctrl Pts',(-0.890817678531163,1.78485715268485,
10.9817741298754));
#13424=CARTESIAN_POINT('Ctrl Pts',(-0.927844073483961,1.76601405747701,
10.9843646793023));
#13425=CARTESIAN_POINT('Ctrl Pts',(-0.950729158841067,1.75380001092075,
10.9859578746841));
#13426=CARTESIAN_POINT('Ctrl Pts',(-1.04893575990428,1.69889846082873,10.9927881506313));
#13427=CARTESIAN_POINT('Ctrl Pts',(-1.12167729766783,1.6517762468957,10.9978329164871));
#13428=CARTESIAN_POINT('Ctrl Pts',(-1.32057934302796,1.50370889556682,11.0122272007663));
#13429=CARTESIAN_POINT('Ctrl Pts',(-1.43783833356192,1.39200716739544,11.0215272898759));
#13430=CARTESIAN_POINT('Ctrl Pts',(-1.54715729279438,1.25914509274536,11.0321742106069));
#13431=CARTESIAN_POINT('Ctrl Pts',(-1.55388909503108,1.25082801644079,11.0328388759933));
#13432=CARTESIAN_POINT('Ctrl Pts',(-1.56909255897397,1.23173213310819,11.0343611495779));
#13433=CARTESIAN_POINT('Ctrl Pts',(-1.57752059250481,1.22091943700962,11.0352204021583));
#13434=CARTESIAN_POINT('Ctrl Pts',(-1.58966496891364,1.2050031889213,11.0364817041372));
#13435=CARTESIAN_POINT('Ctrl Pts',(-1.59346972588795,1.19996734534479,11.0368802687716));
#13436=CARTESIAN_POINT('Ctrl Pts',(-1.60016727531381,1.19101467774119,11.037587980364));
#13437=CARTESIAN_POINT('Ctrl Pts',(-1.60306975969126,1.18710514128067,11.0378967452583));
#13438=CARTESIAN_POINT('Ctrl Pts',(-1.60906922151075,1.17896196619303,11.0385393015672));
#13439=CARTESIAN_POINT('Ctrl Pts',(-1.61216386865649,1.17472666483535,11.0388731802423));
#13440=CARTESIAN_POINT('Ctrl Pts',(-1.6201118699108,1.16375855619813,11.0397370338344));
#13441=CARTESIAN_POINT('Ctrl Pts',(-1.62493993481684,1.1570076287283,11.0402679787043));
#13442=CARTESIAN_POINT('Ctrl Pts',(-1.64518548371286,1.12832225184836,11.0425209836365));
#13443=CARTESIAN_POINT('Ctrl Pts',(-1.66020144550007,1.1061091373075,11.0442582464616));
#13444=CARTESIAN_POINT('Ctrl Pts',(-1.69801759708666,1.04766220825605,11.04881276962));
#13445=CARTESIAN_POINT('Ctrl Pts',(-1.72010621887257,1.01098665059158,11.0516549401773));
#13446=CARTESIAN_POINT('Ctrl Pts',(-1.81212349807512,0.846446118276032,
11.0643380862754));
#13447=CARTESIAN_POINT('Ctrl Pts',(-1.86909260842827,0.71186065329645,11.0745801411154));
#13448=CARTESIAN_POINT('Ctrl Pts',(-1.91766546332463,0.549676539188225,
11.0863390863317));
#13449=CARTESIAN_POINT('Ctrl Pts',(-1.92403797224547,0.526937429217819,
11.087973855698));
#13450=CARTESIAN_POINT('Ctrl Pts',(-1.93382961434331,0.48944825423669,11.0906415798658));
#13451=CARTESIAN_POINT('Ctrl Pts',(-1.93748718911132,0.474763078420624,
11.0916797270721));
#13452=CARTESIAN_POINT('Ctrl Pts',(-1.95275747688053,0.410335096913716,
11.0962008682575));
#13453=CARTESIAN_POINT('Ctrl Pts',(-1.96262537482699,0.360193463234318,
11.0996328524568));
#13454=CARTESIAN_POINT('Ctrl Pts',(-1.9716741461021,0.302622368356984,11.103435111308));
#13455=CARTESIAN_POINT('Ctrl Pts',(-1.97275191807297,0.295514990814411,
11.1039021243318));
#13456=CARTESIAN_POINT('Ctrl Pts',(-1.97429258332861,0.284970841996255,
11.104591265172));
#13457=CARTESIAN_POINT('Ctrl Pts',(-1.97478495967614,0.281538538851066,
11.104815012788));
#13458=CARTESIAN_POINT('Ctrl Pts',(-1.97564471696911,0.275432025900574,
11.1052120372398));
#13459=CARTESIAN_POINT('Ctrl Pts',(-1.97601562110247,0.272758343705778,
11.1053855116788));
#13460=CARTESIAN_POINT('Ctrl Pts',(-1.97672398601088,0.267574772269198,
11.1057211331572));
#13461=CARTESIAN_POINT('Ctrl Pts',(-1.97706209223068,0.265065009508012,
11.1058833169833));
#13462=CARTESIAN_POINT('Ctrl Pts',(-1.97779457931958,0.259548379229047,
11.1062391269904));
#13463=CARTESIAN_POINT('Ctrl Pts',(-1.97818688548416,0.256541235552543,
11.1064326364959));
#13464=CARTESIAN_POINT('Ctrl Pts',(-1.97913716594411,0.249125249240378,
11.1069087854463));
#13465=CARTESIAN_POINT('Ctrl Pts',(-1.97968727101385,0.244715388383343,
11.1071909927869));
#13466=CARTESIAN_POINT('Ctrl Pts',(-1.98236366706657,0.222660544509065,
11.1085978967308));
#13467=CARTESIAN_POINT('Ctrl Pts',(-1.98426889430126,0.204988861766575,
11.1097108448385));
#13468=CARTESIAN_POINT('Ctrl Pts',(-1.99176151173023,0.125541988964189,
11.1146595082694));
#13469=CARTESIAN_POINT('Ctrl Pts',(-1.99470237646159,0.063547673007487,
11.118372994414));
#13470=CARTESIAN_POINT('Ctrl Pts',(-1.99474942627503,0.00151290297884356,
11.1220284394135));
#13471=CARTESIAN_POINT('',(-1.99456005621966,0.000760494868686946,11.9209548813952));
#13472=CARTESIAN_POINT('Ctrl Pts',(-1.99474947325114,0.00144964281281663,
11.1209548814577));
#13473=CARTESIAN_POINT('Ctrl Pts',(-1.99480131921667,-0.069891870774131,
11.1255252561228));
#13474=CARTESIAN_POINT('Ctrl Pts',(-1.99102091811838,-0.141380335692712,
11.1300956307879));
#13475=CARTESIAN_POINT('Ctrl Pts',(-1.98339220536142,-0.212562748880289,
11.134666005453));
#13476=CARTESIAN_POINT('Ctrl Pts',(-1.97608236203098,-0.280769837659475,
11.1390453449075));
#13477=CARTESIAN_POINT('Ctrl Pts',(-1.96523955113442,-0.348695383328597,
11.1434246843619));
#13478=CARTESIAN_POINT('Ctrl Pts',(-1.95090270643391,-0.415940130942959,
11.1478040238164));
#13479=CARTESIAN_POINT('Ctrl Pts',(-1.93657592334818,-0.483137686112946,
11.1521802898452));
#13480=CARTESIAN_POINT('Ctrl Pts',(-1.91876007095681,-0.549654897703523,
11.156556555874));
#13481=CARTESIAN_POINT('Ctrl Pts',(-1.89754557233706,-0.615100287273548,
11.1609328219028));
#13482=CARTESIAN_POINT('Ctrl Pts',(-1.87633826744473,-0.68052348464844,
11.1653076039623));
#13483=CARTESIAN_POINT('Ctrl Pts',(-1.85173475778282,-0.744875100833432,
11.1696823860218));
#13484=CARTESIAN_POINT('Ctrl Pts',(-1.82387543994964,-0.807778399097496,
11.1740571680812));
#13485=CARTESIAN_POINT('Ctrl Pts',(-1.79601546514479,-0.87068318073186,
11.1784320533058));
#13486=CARTESIAN_POINT('Ctrl Pts',(-1.76489973735248,-0.93213911629917,
11.1828069385303));
#13487=CARTESIAN_POINT('Ctrl Pts',(-1.73071614738497,-0.991790895139154,
11.1871818237548));
#13488=CARTESIAN_POINT('Ctrl Pts',(-1.69649783545685,-1.05150326523703,
11.1915611527664));
#13489=CARTESIAN_POINT('Ctrl Pts',(-1.65920569757315,-1.10940738467463,
11.1959404817779));
#13490=CARTESIAN_POINT('Ctrl Pts',(-1.61907217740582,-1.16517502841864,
11.2003198107894));
#13491=CARTESIAN_POINT('Ctrl Pts',(-1.57891446872006,-1.22097628338522,
11.2047017792275));
#13492=CARTESIAN_POINT('Ctrl Pts',(-1.53591228988533,-1.2746381099726,11.2090837476656));
#13493=CARTESIAN_POINT('Ctrl Pts',(-1.49033792455086,-1.32586591823813,
11.2134657161038));
#13494=CARTESIAN_POINT('Ctrl Pts',(-1.44468829793984,-1.37717832384728,
11.2178549209024));
#13495=CARTESIAN_POINT('Ctrl Pts',(-1.39645837009637,-1.42604833939218,
11.2222441257011));
#13496=CARTESIAN_POINT('Ctrl Pts',(-1.34595586245941,-1.4722195416483,11.2266333304997));
#13497=CARTESIAN_POINT('Ctrl Pts',(-1.33057399689337,-1.48628219436312,
11.2279701781398));
#13498=CARTESIAN_POINT('Ctrl Pts',(-1.31498152753624,-1.50009478276201,
11.2293070257799));
#13499=CARTESIAN_POINT('Ctrl Pts',(-1.29918768722309,-1.51365085666012,
11.2306438734201));
#13500=CARTESIAN_POINT('Ctrl Pts',(-1.24656660001067,-1.55881627132221,
11.235097912138));
#13501=CARTESIAN_POINT('Ctrl Pts',(-1.19148327420651,-1.6013238553351,11.239551950856));
#13502=CARTESIAN_POINT('Ctrl Pts',(-1.13423719732462,-1.64089412903611,
11.244005989574));
#13503=CARTESIAN_POINT('Ctrl Pts',(-1.07707717019071,-1.68040492246765,
11.2484533331798));
#13504=CARTESIAN_POINT('Ctrl Pts',(-1.01776124374331,-1.71698689262936,
11.2529006767855));
#13505=CARTESIAN_POINT('Ctrl Pts',(-0.956622630222744,-1.75040015592027,
11.2573480203913));
#13506=CARTESIAN_POINT('Ctrl Pts',(-0.895556092843091,-1.78377402840831,
11.2617901210361));
#13507=CARTESIAN_POINT('Ctrl Pts',(-0.832671563617494,-1.81398637971139,
11.2662322216809));
#13508=CARTESIAN_POINT('Ctrl Pts',(-0.768330434763023,-1.84084108643763,
11.2706743223257));
#13509=CARTESIAN_POINT('Ctrl Pts',(-0.704029892577714,-1.86767885309588,
11.2751136208737));
#13510=CARTESIAN_POINT('Ctrl Pts',(-0.63827502424924,-1.89116298870622,
11.2795529194217));
#13511=CARTESIAN_POINT('Ctrl Pts',(-0.571449601274847,-1.91114439949022,
11.2839922179697));
#13512=CARTESIAN_POINT('Ctrl Pts',(-0.504643624635163,-1.93111999564282,
11.2884302246728));
#13513=CARTESIAN_POINT('Ctrl Pts',(-0.436768180595059,-1.94759475026453,
11.2928682313759));
#13514=CARTESIAN_POINT('Ctrl Pts',(-0.36822300174688,-1.96046917432652,
11.2973062380789));
#13515=CARTESIAN_POINT('Ctrl Pts',(-0.299674478550111,-1.97334422653718,
11.3017444613142));
#13516=CARTESIAN_POINT('Ctrl Pts',(-0.230456637258554,-1.98261851141494,
11.3061826845495));
#13517=CARTESIAN_POINT('Ctrl Pts',(-0.160978461993672,-1.98824382239054,
11.3106209077849));
#13518=CARTESIAN_POINT('Ctrl Pts',(-0.0914266822696495,-1.99387509276232,
11.3150638328279));
#13519=CARTESIAN_POINT('Ctrl Pts',(-0.0216145070355556,-1.99584963392224,
11.3195067578709));
#13520=CARTESIAN_POINT('Ctrl Pts',(0.048045874980268,-1.99417129565075,
11.3239496829139));
#13521=CARTESIAN_POINT('Ctrl Pts',(0.117746920628242,-1.99249197766412,
11.3283952014752));
#13522=CARTESIAN_POINT('Ctrl Pts',(0.187295508419194,-1.98715557353959,
11.3328407200364));
#13523=CARTESIAN_POINT('Ctrl Pts',(0.256284174689232,-1.97821788089782,
11.3372862385977));
#13524=CARTESIAN_POINT('Ctrl Pts',(0.325393228107833,-1.96926459173288,
11.3417395147129));
#13525=CARTESIAN_POINT('Ctrl Pts',(0.393939928096308,-1.95669755763645,
11.3461927908282));
#13526=CARTESIAN_POINT('Ctrl Pts',(0.461527390003027,-1.94062361904028,
11.3506460669434));
#13527=CARTESIAN_POINT('Ctrl Pts',(0.497718532255903,-1.93201648715684,
11.3530306682412));
#13528=CARTESIAN_POINT('Ctrl Pts',(0.533634893021944,-1.92240467714963,
11.355415269539));
#13529=CARTESIAN_POINT('Ctrl Pts',(0.569217740337809,-1.91181032704207,
11.3577998708368));
#13530=CARTESIAN_POINT('Ctrl Pts',(0.63568058248553,-1.89202184264661,11.3622539095548));
#13531=CARTESIAN_POINT('Ctrl Pts',(0.701241918662385,-1.86872423163233,
11.3667079482728));
#13532=CARTESIAN_POINT('Ctrl Pts',(0.765504628151487,-1.84201797677945,
11.3711619869908));
#13533=CARTESIAN_POINT('Ctrl Pts',(0.829670740803476,-1.81535186557707,
11.3756093305965));
#13534=CARTESIAN_POINT('Ctrl Pts',(0.892541652685848,-1.78528746619354,
11.3800566742023));
#13535=CARTESIAN_POINT('Ctrl Pts',(0.953735274802135,-1.75197505350336,
11.384504017808));
#13536=CARTESIAN_POINT('Ctrl Pts',(1.01485675592812,-1.71870191272351,11.3889461184528));
#13537=CARTESIAN_POINT('Ctrl Pts',(1.07430444665581,-1.68218859660003,11.3933882190976));
#13538=CARTESIAN_POINT('Ctrl Pts',(1.1317177927405,-1.64263276483046,11.3978303197424));
#13539=CARTESIAN_POINT('Ctrl Pts',(1.18909492223215,-1.6031018850548,11.4022696182904));
#13540=CARTESIAN_POINT('Ctrl Pts',(1.24443985059334,-1.56053257405536,11.4067089168385));
#13541=CARTESIAN_POINT('Ctrl Pts',(1.29741944767327,-1.5151667694677,11.4111482153865));
#13542=CARTESIAN_POINT('Ctrl Pts',(1.35038362758203,-1.46981416642201,11.4155862220895));
#13543=CARTESIAN_POINT('Ctrl Pts',(1.40098347095676,-1.42166700353641,11.4200242287926));
#13544=CARTESIAN_POINT('Ctrl Pts',(1.44891891168712,-1.37100749445632,11.4244622354957));
#13545=CARTESIAN_POINT('Ctrl Pts',(1.49685669120806,-1.3203455136772,11.428900458731));
#13546=CARTESIAN_POINT('Ctrl Pts',(1.54212947525079,-1.26717130058426,11.4333386819663));
#13547=CARTESIAN_POINT('Ctrl Pts',(1.58447530493118,-1.21180261204672,11.4377769052016));
#13548=CARTESIAN_POINT('Ctrl Pts',(1.62686599534494,-1.15637526649402,11.4422198302446));
#13549=CARTESIAN_POINT('Ctrl Pts',(1.6663232443781,-1.09874919494268,11.4466627552876));
#13550=CARTESIAN_POINT('Ctrl Pts',(1.70262712490201,-1.03927303248372,11.4511056803307));
#13551=CARTESIAN_POINT('Ctrl Pts',(1.73895219749533,-0.979762151340572,
11.4555511988919));
#13552=CARTESIAN_POINT('Ctrl Pts',(1.77212000491597,-0.918399460529095,
11.4599967174532));
#13553=CARTESIAN_POINT('Ctrl Pts',(1.80195685377863,-0.855557747682884,
11.4644422360144));
#13554=CARTESIAN_POINT('Ctrl Pts',(1.83184576877543,-0.792606374293586,
11.4688955121297));
#13555=CARTESIAN_POINT('Ctrl Pts',(1.85839193572584,-0.728171279465302,
11.4733487882449));
#13556=CARTESIAN_POINT('Ctrl Pts',(1.88147030347454,-0.662643991630075,
11.4778020643602));
#13557=CARTESIAN_POINT('Ctrl Pts',(1.89382810574432,-0.627556013348388,
11.480186665658));
#13558=CARTESIAN_POINT('Ctrl Pts',(1.90519244737116,-0.592155115030856,
11.4825712669558));
#13559=CARTESIAN_POINT('Ctrl Pts',(1.91555014288408,-0.55650266180565,11.4849558682536));
#13560=CARTESIAN_POINT('Ctrl Pts',(1.93489659584712,-0.489909807393396,
11.4894099069716));
#13561=CARTESIAN_POINT('Ctrl Pts',(1.95080463819388,-0.422175018186061,
11.4938639456896));
#13562=CARTESIAN_POINT('Ctrl Pts',(1.96314374571715,-0.353686578981496,
11.4983179844075));
#13563=CARTESIAN_POINT('Ctrl Pts',(1.97546430564468,-0.285301088542166,
11.5027653280133));
#13564=CARTESIAN_POINT('Ctrl Pts',(1.98422649217828,-0.216164674414784,
11.5072126716191));
#13565=CARTESIAN_POINT('Ctrl Pts',(1.98934978254012,-0.146679941394854,
11.5116600152248));
#13566=CARTESIAN_POINT('Ctrl Pts',(1.99446703306922,-0.0772771237329385,
11.5161021158696));
#13567=CARTESIAN_POINT('Ctrl Pts',(1.99595387185215,-0.00752728862473041,
11.5205442165144));
#13568=CARTESIAN_POINT('Ctrl Pts',(1.99378127442722,0.0621594099342622,
11.5249863171592));
#13569=CARTESIAN_POINT('Ctrl Pts',(1.99161004748637,0.131802149815071,11.5294256157072));
#13570=CARTESIAN_POINT('Ctrl Pts',(1.98578397886954,0.201381343966332,11.5338649142553));
#13571=CARTESIAN_POINT('Ctrl Pts',(1.97632611885387,0.270485922805627,11.5383042128033));
#13572=CARTESIAN_POINT('Ctrl Pts',(1.9668710110948,0.339570392071139,11.5427422195063));
#13573=CARTESIAN_POINT('Ctrl Pts',(1.95378627631826,0.408180035411662,11.5471802262094));
#13574=CARTESIAN_POINT('Ctrl Pts',(1.93714672842288,0.475909776176658,11.5516182329125));
#13575=CARTESIAN_POINT('Ctrl Pts',(1.92050636867686,0.543642821504602,11.5560564561478));
#13576=CARTESIAN_POINT('Ctrl Pts',(1.90031097059076,0.610495404171167,11.5604946793831));
#13577=CARTESIAN_POINT('Ctrl Pts',(1.87668586299971,0.676075242940492,11.5649329026184));
#13578=CARTESIAN_POINT('Ctrl Pts',(1.8530357272144,0.741724556311701,11.5693758276614));
#13579=CARTESIAN_POINT('Ctrl Pts',(1.82594879609034,0.806097973076582,11.5738187527044));
#13580=CARTESIAN_POINT('Ctrl Pts',(1.79559911605028,0.868821832678858,11.5782616777475));
#13581=CARTESIAN_POINT('Ctrl Pts',(1.76523171965278,0.931582306779709,11.5827071963087));
#13582=CARTESIAN_POINT('Ctrl Pts',(1.73159801957856,0.992690878126272,11.58715271487));
#13583=CARTESIAN_POINT('Ctrl Pts',(1.69491740017859,1.05179968105712,11.5915982334312));
#13584=CARTESIAN_POINT('Ctrl Pts',(1.6581727720738,1.11101163049915,11.5960515095465));
#13585=CARTESIAN_POINT('Ctrl Pts',(1.61837089061509,1.16821644373751,11.6005047856617));
#13586=CARTESIAN_POINT('Ctrl Pts',(1.57577323210027,1.22309700494126,11.6049580617769));
#13587=CARTESIAN_POINT('Ctrl Pts',(1.55296341093742,1.2524839672772,11.6073426630747));
#13588=CARTESIAN_POINT('Ctrl Pts',(1.52935262853928,1.28120508871815,11.6097272643725));
#13589=CARTESIAN_POINT('Ctrl Pts',(1.5049853393288,1.30921605967288,11.6121118656703));
#13590=CARTESIAN_POINT('Ctrl Pts',(1.45947129482322,1.36153589581327,11.6165659043883));
#13591=CARTESIAN_POINT('Ctrl Pts',(1.41113556380725,1.41158311938672,11.6210199431063));
#13592=CARTESIAN_POINT('Ctrl Pts',(1.36023393229373,1.45903776919473,11.6254739818242));
#13593=CARTESIAN_POINT('Ctrl Pts',(1.30940881384106,1.50642108729096,11.62992132543));
#13594=CARTESIAN_POINT('Ctrl Pts',(1.25602580513888,1.55121923516703,11.6343686690358));
#13595=CARTESIAN_POINT('Ctrl Pts',(1.20037980321197,1.59314653768597,11.6388160126415));
#13596=CARTESIAN_POINT('Ctrl Pts',(1.14479940220149,1.63502441222494,11.6432581132863));
#13597=CARTESIAN_POINT('Ctrl Pts',(1.08696169573552,1.67403787013299,11.6477002139311));
#13598=CARTESIAN_POINT('Ctrl Pts',(1.02719580968401,1.70994044664357,11.6521423145759));
#13599=CARTESIAN_POINT('Ctrl Pts',(0.967467624218168,1.74582037564985,11.6565816131239));
#13600=CARTESIAN_POINT('Ctrl Pts',(0.905814090722211,1.77859306461083,11.6610209116719));
#13601=CARTESIAN_POINT('Ctrl Pts',(0.842593298733142,1.80805533527876,11.6654602102199));
#13602=CARTESIAN_POINT('Ctrl Pts',(0.779390904123909,1.83750903236565,11.669898216923));
#13603=CARTESIAN_POINT('Ctrl Pts',(0.71462259991777,1.86365401685104,11.6743362236261));
#13604=CARTESIAN_POINT('Ctrl Pts',(0.648669462487063,1.88633387578571,11.6787742303291));
#13605=CARTESIAN_POINT('Ctrl Pts',(0.582713107174641,1.90901484128038,11.6832124535644));
#13606=CARTESIAN_POINT('Ctrl Pts',(0.515572267596593,1.92823018863076,11.6876506767997));
#13607=CARTESIAN_POINT('Ctrl Pts',(0.447644611669163,1.94387290328961,11.692088900035));
#13608=CARTESIAN_POINT('Ctrl Pts',(0.379644993886647,1.95953218967834,11.6965318250781));
#13609=CARTESIAN_POINT('Ctrl Pts',(0.310857374064267,1.97161117899342,11.7009747501211));
#13610=CARTESIAN_POINT('Ctrl Pts',(0.241690140920874,1.98005389782239,11.7054176751641));
#13611=CARTESIAN_POINT('Ctrl Pts',(0.172482532016436,1.98850154501387,11.7098631937254));
#13612=CARTESIAN_POINT('Ctrl Pts',(0.102895357275272,1.99330866309628,11.7143087122866));
#13613=CARTESIAN_POINT('Ctrl Pts',(0.0333398646557803,1.9944713625231,11.7187542308479));
#13614=CARTESIAN_POINT('Ctrl Pts',(-0.0363370042399317,1.99563609089286,
11.7232075069631));
#13615=CARTESIAN_POINT('Ctrl Pts',(-0.105981591456101,1.99314372318742,
11.7276607830783));
#13616=CARTESIAN_POINT('Ctrl Pts',(-0.175185713106997,1.98704240730368,
11.7321140591936));
#13617=CARTESIAN_POINT('Ctrl Pts',(-0.212242530163042,1.98377532810216,
11.7344986604914));
#13618=CARTESIAN_POINT('Ctrl Pts',(-0.249173186378843,1.979474340568,11.7368832617892));
#13619=CARTESIAN_POINT('Ctrl Pts',(-0.285916359980977,1.97415283035413,
11.739267863087));
#13620=CARTESIAN_POINT('Ctrl Pts',(-0.354546498694724,1.96421313412377,
11.743721901805));
#13621=CARTESIAN_POINT('Ctrl Pts',(-0.422793615799594,1.95067066436604,
11.748175940523));
#13622=CARTESIAN_POINT('Ctrl Pts',(-0.490250215933375,1.93356724431225,
11.752629979241));
#13623=CARTESIAN_POINT('Ctrl Pts',(-0.55760541831628,1.9164895333562,11.7570773228467));
#13624=CARTESIAN_POINT('Ctrl Pts',(-0.624171991471304,1.89586161514751,
11.7615246664525));
#13625=CARTESIAN_POINT('Ctrl Pts',(-0.689550091135187,1.87177675867488,
11.7659720100582));
#13626=CARTESIAN_POINT('Ctrl Pts',(-0.754851116739743,1.84772029577237,
11.770414110703));
#13627=CARTESIAN_POINT('Ctrl Pts',(-0.818965994427438,1.82021515722925,
11.7748562113478));
#13628=CARTESIAN_POINT('Ctrl Pts',(-0.881509314446687,1.78940461915234,
11.7792983119926));
#13629=CARTESIAN_POINT('Ctrl Pts',(-0.944013181862676,1.75861351649931,
11.7837376105406));
#13630=CARTESIAN_POINT('Ctrl Pts',(-1.00494702006678,1.7245213664352,11.7881769090886));
#13631=CARTESIAN_POINT('Ctrl Pts',(-1.06394613150128,1.68731923232193,11.7926162076367));
#13632=CARTESIAN_POINT('Ctrl Pts',(-1.12292807407352,1.65012792410587,11.7970542143397));
#13633=CARTESIAN_POINT('Ctrl Pts',(-1.17997599364078,1.60982868941689,11.8014922210428));
#13634=CARTESIAN_POINT('Ctrl Pts',(-1.2347520655769,1.56665723725822,11.8059302277459));
#13635=CARTESIAN_POINT('Ctrl Pts',(-1.28953081006082,1.52348367874609,11.8103684509811));
#13636=CARTESIAN_POINT('Ctrl Pts',(-1.34203710383137,1.47743792945814,11.8148066742164));
#13637=CARTESIAN_POINT('Ctrl Pts',(-1.39196567148208,1.42879639274301,11.8192448974517));
#13638=CARTESIAN_POINT('Ctrl Pts',(-1.44194713294038,1.38010332568753,11.8236878224947));
#13639=CARTESIAN_POINT('Ctrl Pts',(-1.48934506633877,1.32880932473937,11.8281307475378));
#13640=CARTESIAN_POINT('Ctrl Pts',(-1.53389130511928,1.27522744111765,11.8325736725808));
#13641=CARTESIAN_POINT('Ctrl Pts',(-1.57846354737293,1.22161427954498,11.8370191911421));
#13642=CARTESIAN_POINT('Ctrl Pts',(-1.62018048883087,1.1657109695526,11.8414647097033));
#13643=CARTESIAN_POINT('Ctrl Pts',(-1.65881620481107,1.10786116510878,11.8459102282646));
#13644=CARTESIAN_POINT('Ctrl Pts',(-1.69751934119421,1.04991041114129,11.8503635043798));
#13645=CARTESIAN_POINT('Ctrl Pts',(-1.73313026885596,0.990006803099989,
11.854816780495));
#13646=CARTESIAN_POINT('Ctrl Pts',(-1.76546847291161,0.928519592499352,
11.8592700566103));
#13647=CARTESIAN_POINT('Ctrl Pts',(-1.78278465124067,0.89559495939712,11.8616546579081));
#13648=CARTESIAN_POINT('Ctrl Pts',(-1.79916325838748,0.862216626750999,
11.8640392592059));
#13649=CARTESIAN_POINT('Ctrl Pts',(-1.81458234810586,0.828443398454376,
11.8664238605037));
#13650=CARTESIAN_POINT('Ctrl Pts',(-1.84597961350514,0.75967234701184,11.8712795271602));
#13651=CARTESIAN_POINT('Ctrl Pts',(-1.87350349450898,0.689026870672636,
11.8761351938167));
#13652=CARTESIAN_POINT('Ctrl Pts',(-1.89694749304094,0.61694227537565,11.8809908604732));
#13653=CARTESIAN_POINT('Ctrl Pts',(-1.92032753640226,0.545054326678276,
11.8858332808829));
#13654=CARTESIAN_POINT('Ctrl Pts',(-1.93964974790703,0.471735397355194,
11.8906757012927));
#13655=CARTESIAN_POINT('Ctrl Pts',(-1.9547553251231,0.397440789807616,11.8955181217024));
#13656=CARTESIAN_POINT('Ctrl Pts',(-1.96979393975964,0.323475528070162,
11.9003390758049));
#13657=CARTESIAN_POINT('Ctrl Pts',(-1.98065308357961,0.24854353722681,11.9051600299073));
#13658=CARTESIAN_POINT('Ctrl Pts',(-1.98722406893279,0.173112860164138,
11.9099809840098));
#13659=CARTESIAN_POINT('Ctrl Pts',(-1.9922098952135,0.115878787668584,11.9136389498049));
#13660=CARTESIAN_POINT('Ctrl Pts',(-1.99472789398327,0.0583580291533336,
11.9172969156001));
#13661=CARTESIAN_POINT('Ctrl Pts',(-1.99474985500375,0.000760567236024933,
11.9209548813952));
#13662=CARTESIAN_POINT('',(-1.99382857833478,-0.00178311501442863,12.7209548813952));
#13663=CARTESIAN_POINT('Ctrl Pts',(-1.99173490036883,0.00075941768049894,
11.9209548813952));
#13664=CARTESIAN_POINT('Ctrl Pts',(-1.99043489393824,-0.379843555327031,
11.9451632069036));
#13665=CARTESIAN_POINT('Ctrl Pts',(-1.70198160698615,-1.42865295746539,
12.0117568648843));
#13666=CARTESIAN_POINT('Ctrl Pts',(-0.00405728410159747,-2.35857299970061,
12.1207358553372));
#13667=CARTESIAN_POINT('Ctrl Pts',(1.98079133142009,-1.28037055489497,12.2478918527539));
#13668=CARTESIAN_POINT('Ctrl Pts',(2.14890506846846,0.972157427159623,12.3750478501707));
#13669=CARTESIAN_POINT('Ctrl Pts',(0.346093990525894,2.33304565025909,12.5022038475874));
#13670=CARTESIAN_POINT('Ctrl Pts',(-1.57649463483796,1.62673220971673,12.6175061913289));
#13671=CARTESIAN_POINT('Ctrl Pts',(-1.98970252853481,0.476968094023456,
12.6904232025982));
#13672=CARTESIAN_POINT('Ctrl Pts',(-1.99382857833478,-0.00178311501442863,
12.7209548813952));
#13673=CARTESIAN_POINT('',(-1.99474927319053,0.00170282290857631,14.3209548813952));
#13674=CARTESIAN_POINT('Ctrl Pts',(-1.99474916918916,-0.00182058209230188,
12.7204256504633));
#13675=CARTESIAN_POINT('Ctrl Pts',(-1.99460679830126,-0.157811466306289,
12.7312264087668));
#13676=CARTESIAN_POINT('Ctrl Pts',(-1.97616778132757,-0.31325526735429,
12.7423019706705));
#13677=CARTESIAN_POINT('Ctrl Pts',(-1.93667103452653,-0.478030541023614,
12.7535601346536));
#13678=CARTESIAN_POINT('Ctrl Pts',(-1.93340893355319,-0.49105784999197,
12.7544464877575));
#13679=CARTESIAN_POINT('Ctrl Pts',(-1.92837319535795,-0.510339709358736,
12.7557518529825));
#13680=CARTESIAN_POINT('Ctrl Pts',(-1.92670022090365,-0.516619841895187,
12.7561759781784));
#13681=CARTESIAN_POINT('Ctrl Pts',(-1.92359608508044,-0.528047542457987,
12.7569457143287));
#13682=CARTESIAN_POINT('Ctrl Pts',(-1.92217488677198,-0.533197723076139,
12.7572918624728));
#13683=CARTESIAN_POINT('Ctrl Pts',(-1.9199018539286,-0.541307600311889,
12.7578356783885));
#13684=CARTESIAN_POINT('Ctrl Pts',(-1.91906384055371,-0.544271093361395,
12.7580341333404));
#13685=CARTESIAN_POINT('Ctrl Pts',(-1.91747870536807,-0.54982748025022,
12.7584057123258));
#13686=CARTESIAN_POINT('Ctrl Pts',(-1.91673319421761,-0.552420768865559,
12.7585789244244));
#13687=CARTESIAN_POINT('Ctrl Pts',(-1.91502024271313,-0.558334121172091,
12.7589734164481));
#13688=CARTESIAN_POINT('Ctrl Pts',(-1.91404943156409,-0.561653180207082,
12.7591944971162));
#13689=CARTESIAN_POINT('Ctrl Pts',(-1.91104739346366,-0.571818519507528,
12.7598706075471));
#13690=CARTESIAN_POINT('Ctrl Pts',(-1.90898800145358,-0.578656524494429,
12.7603240241146));
#13691=CARTESIAN_POINT('Ctrl Pts',(-1.89228835616597,-0.633046479359327,
12.7639205456607));
#13692=CARTESIAN_POINT('Ctrl Pts',(-1.87590895521207,-0.680051187043739,
12.766967896101));
#13693=CARTESIAN_POINT('Ctrl Pts',(-1.85122230962036,-0.743188074175726,
12.7710398230691));
#13694=CARTESIAN_POINT('Ctrl Pts',(-1.8444300470715,-0.759888402771221,
12.7721147940824));
#13695=CARTESIAN_POINT('Ctrl Pts',(-1.80315008930699,-0.85756877825328,
12.7784023528058));
#13696=CARTESIAN_POINT('Ctrl Pts',(-1.7635581713491,-0.936289686919568,
12.7834734917473));
#13697=CARTESIAN_POINT('Ctrl Pts',(-1.68905244863127,-1.06282096944462,
12.7919988403461));
#13698=CARTESIAN_POINT('Ctrl Pts',(-1.65698452241267,-1.11215487093237,
12.7954259849033));
#13699=CARTESIAN_POINT('Ctrl Pts',(-1.57930105486164,-1.22083051713804,
12.8033327871925));
#13700=CARTESIAN_POINT('Ctrl Pts',(-1.53243537248501,-1.27916337219581,
12.8078405023811));
#13701=CARTESIAN_POINT('Ctrl Pts',(-1.47031737710255,-1.34815465818939,
12.8136028579882));
#13702=CARTESIAN_POINT('Ctrl Pts',(-1.45804320789259,-1.36141989920375,
12.8147319234833));
#13703=CARTESIAN_POINT('Ctrl Pts',(-1.44179249904295,-1.37851091291772,
12.8162153862357));
#13704=CARTESIAN_POINT('Ctrl Pts',(-1.43797768360073,-1.38248982918874,
12.8165628239745));
#13705=CARTESIAN_POINT('Ctrl Pts',(-1.43042839098918,-1.3902988154367,12.8172488422753));
#13706=CARTESIAN_POINT('Ctrl Pts',(-1.42669490061373,-1.39412977789228,
12.817587378461));
#13707=CARTESIAN_POINT('Ctrl Pts',(-1.41955456083233,-1.40139781330903,
12.8182334685947));
#13708=CARTESIAN_POINT('Ctrl Pts',(-1.41615051977085,-1.40483760164717,
12.8185408978828));
#13709=CARTESIAN_POINT('Ctrl Pts',(-1.40835499247842,-1.41265786775097,
12.8192436305046));
#13710=CARTESIAN_POINT('Ctrl Pts',(-1.40395554084635,-1.41703030103379,
12.819639285598));
#13711=CARTESIAN_POINT('Ctrl Pts',(-1.39042276542373,-1.43035508100822,
12.820853529247));
#13712=CARTESIAN_POINT('Ctrl Pts',(-1.38122382111978,-1.43924003129459,
12.8216750514602));
#13713=CARTESIAN_POINT('Ctrl Pts',(-1.29831278994866,-1.51779401831155,
12.8290465316095));
#13714=CARTESIAN_POINT('Ctrl Pts',(-1.21948442709691,-1.58182383899944,
12.8358365595217));
#13715=CARTESIAN_POINT('Ctrl Pts',(-1.01476707034905,-1.7236823899953,12.8529359269563));
#13716=CARTESIAN_POINT('Ctrl Pts',(-0.884437241337347,-1.7940460025461,
12.8634072685098));
#13717=CARTESIAN_POINT('Ctrl Pts',(-0.716745461652485,-1.86182887998794,
12.8757356395092));
#13718=CARTESIAN_POINT('Ctrl Pts',(-0.685642474360487,-1.87350620538434,
12.8779751074788));
#13719=CARTESIAN_POINT('Ctrl Pts',(-0.636620266354247,-1.89052661724212,
12.8814168954455));
#13720=CARTESIAN_POINT('Ctrl Pts',(-0.618894044152356,-1.8964035641936,
12.8826437936863));
#13721=CARTESIAN_POINT('Ctrl Pts',(-0.596262042720049,-1.90355581625355,
12.8841856328525));
#13722=CARTESIAN_POINT('Ctrl Pts',(-0.591431099653924,-1.90506231522886,
12.8845133326984));
#13723=CARTESIAN_POINT('Ctrl Pts',(-0.583710941702521,-1.90743760068412,
12.8850347029975));
#13724=CARTESIAN_POINT('Ctrl Pts',(-0.580825438647956,-1.90831823186895,
12.8852290565953));
#13725=CARTESIAN_POINT('Ctrl Pts',(-0.575343114859659,-1.90997780424531,
12.8855973277552));
#13726=CARTESIAN_POINT('Ctrl Pts',(-0.57274673620158,-1.9107579880196,12.885771314185));
#13727=CARTESIAN_POINT('Ctrl Pts',(-0.566788361835478,-1.91253517929596,
12.8861696329972));
#13728=CARTESIAN_POINT('Ctrl Pts',(-0.56342532544817,-1.91352861547976,
12.8863937549288));
#13729=CARTESIAN_POINT('Ctrl Pts',(-0.554462542651234,-1.9161505316297,
12.8869892454798));
#13730=CARTESIAN_POINT('Ctrl Pts',(-0.548858193039458,-1.91776334750431,
12.8873597183418));
#13731=CARTESIAN_POINT('Ctrl Pts',(-0.509825454254745,-1.9288110415947,
12.8899274032023));
#13732=CARTESIAN_POINT('Ctrl Pts',(-0.476160281378337,-1.93739664735316,
12.892078062006));
#13733=CARTESIAN_POINT('Ctrl Pts',(-0.369545281309147,-1.96163925882593,
12.8987386913856));
#13734=CARTESIAN_POINT('Ctrl Pts',(-0.295928033976509,-1.97408731883704,
12.9031202238321));
#13735=CARTESIAN_POINT('Ctrl Pts',(-0.0926386958131628,-1.99683052226044,
12.9150309613857));
#13736=CARTESIAN_POINT('Ctrl Pts',(0.0375989808105898,-1.99862419921429,
12.922474052959));
#13737=CARTESIAN_POINT('Ctrl Pts',(0.208077979658812,-1.98429420822249,
12.93273237886));
#13738=CARTESIAN_POINT('Ctrl Pts',(0.248953392655578,-1.97958122397856,
12.935229170551));
#13739=CARTESIAN_POINT('Ctrl Pts',(0.306741935923933,-1.97110002409537,
12.9388282845268));
#13740=CARTESIAN_POINT('Ctrl Pts',(0.32379817334263,-1.96837004513549,12.9398991490418));
#13741=CARTESIAN_POINT('Ctrl Pts',(0.353736865043894,-1.96317848165001,
12.9417951230866));
#13742=CARTESIAN_POINT('Ctrl Pts',(0.366634661603345,-1.96081068243473,
12.9426172699228));
#13743=CARTESIAN_POINT('Ctrl Pts',(0.385655416590161,-1.95712459311536,
12.9438379867305));
#13744=CARTESIAN_POINT('Ctrl Pts',(0.391797196955183,-1.95590432494245,
12.944233433526));
#13745=CARTESIAN_POINT('Ctrl Pts',(0.40269990291107,-1.95368472766596,12.9449377343189));
#13746=CARTESIAN_POINT('Ctrl Pts',(0.407463131458751,-1.95269685889412,
12.9452462199318));
#13747=CARTESIAN_POINT('Ctrl Pts',(0.416739118091649,-1.95073764978661,
12.9458485245));
#13748=CARTESIAN_POINT('Ctrl Pts',(0.421252215197863,-1.94976804811328,
12.9461422859941));
#13749=CARTESIAN_POINT('Ctrl Pts',(0.433350350379864,-1.94712489838476,
12.9469317157075));
#13750=CARTESIAN_POINT('Ctrl Pts',(0.440928986778763,-1.94542271033173,
12.9474282997078));
#13751=CARTESIAN_POINT('Ctrl Pts',(0.468599873911747,-1.93903773727626,
12.949249082651));
#13752=CARTESIAN_POINT('Ctrl Pts',(0.488628518270105,-1.93408771940577,
12.9505818339787));
#13753=CARTESIAN_POINT('Ctrl Pts',(0.671050145446621,-1.88598841292785,
12.9628610526209));
#13754=CARTESIAN_POINT('Ctrl Pts',(0.827428707151443,-1.82279982009586,
12.974496735734));
#13755=CARTESIAN_POINT('Ctrl Pts',(1.03859223260738,-1.70464996305835,12.9913766088605));
#13756=CARTESIAN_POINT('Ctrl Pts',(1.10112362756031,-1.66494242939957,12.9965290735613));
#13757=CARTESIAN_POINT('Ctrl Pts',(1.19762375794861,-1.59584463406636,13.0045941421972));
#13758=CARTESIAN_POINT('Ctrl Pts',(1.2330609149702,-1.56862496142643,13.0075819884151));
#13759=CARTESIAN_POINT('Ctrl Pts',(1.27264266974691,-1.536050642658,13.0109227078983));
#13760=CARTESIAN_POINT('Ctrl Pts',(1.27770756447548,-1.53184017583816,13.0113502497672));
#13761=CARTESIAN_POINT('Ctrl Pts',(1.2853141451971,-1.52545282050443,13.0119923153173));
#13762=CARTESIAN_POINT('Ctrl Pts',(1.28787129740379,-1.52329454839005,13.0122081578691));
#13763=CARTESIAN_POINT('Ctrl Pts',(1.2924739137601,-1.51939000190424,13.0125966250882));
#13764=CARTESIAN_POINT('Ctrl Pts',(1.29452127535165,-1.51764602709827,13.0127694140074));
#13765=CARTESIAN_POINT('Ctrl Pts',(1.29896646940969,-1.51384400076335,13.013144544374));
#13766=CARTESIAN_POINT('Ctrl Pts',(1.30136293201885,-1.51178439825401,13.013346768207));
#13767=CARTESIAN_POINT('Ctrl Pts',(1.30795805801339,-1.50608901736665,13.0139032877959));
#13768=CARTESIAN_POINT('Ctrl Pts',(1.31214648636693,-1.50244134988453,13.0142567156789));
#13769=CARTESIAN_POINT('Ctrl Pts',(1.33324989760919,-1.48390700437273,13.0160377588024));
#13770=CARTESIAN_POINT('Ctrl Pts',(1.34992782386582,-1.46875125927684,13.0174462758331));
#13771=CARTESIAN_POINT('Ctrl Pts',(1.51160399704185,-1.31675010068925,13.0311525738477));
#13772=CARTESIAN_POINT('Ctrl Pts',(1.63558659584174,-1.15916296833073,13.0421826743286));
#13773=CARTESIAN_POINT('Ctrl Pts',(1.76057541025715,-0.939288047761927,
13.0571867551679));
#13774=CARTESIAN_POINT('Ctrl Pts',(1.7851229567189,-0.891752862080258,13.060402952193));
#13775=CARTESIAN_POINT('Ctrl Pts',(1.82107415985678,-0.814685723407736,
13.0656184057982));
#13776=CARTESIAN_POINT('Ctrl Pts',(1.83373701955855,-0.785768599972928,
13.0675754043001));
#13777=CARTESIAN_POINT('Ctrl Pts',(1.84904489286473,-0.748423646147957,
13.0701079363825));
#13778=CARTESIAN_POINT('Ctrl Pts',(1.85232789631094,-0.740260988095704,
13.0706617869076));
#13779=CARTESIAN_POINT('Ctrl Pts',(1.85752248557571,-0.727094537834776,
13.0715557500279));
#13780=CARTESIAN_POINT('Ctrl Pts',(1.85946812895349,-0.722104236147295,
13.0718947137212));
#13781=CARTESIAN_POINT('Ctrl Pts',(1.86313283254579,-0.712591759533854,
13.0725411306208));
#13782=CARTESIAN_POINT('Ctrl Pts',(1.86485558867669,-0.708071041753189,
13.072848457088));
#13783=CARTESIAN_POINT('Ctrl Pts',(1.86874507449941,-0.69775190812976,13.0735502712907));
#13784=CARTESIAN_POINT('Ctrl Pts',(1.87090128549016,-0.691949606032181,
13.0739451074359));
#13785=CARTESIAN_POINT('Ctrl Pts',(1.87740737433139,-0.67418916601277,13.0751543876654));
#13786=CARTESIAN_POINT('Ctrl Pts',(1.88166979833925,-0.662199545685784,
13.0759717305749));
#13787=CARTESIAN_POINT('Ctrl Pts',(1.93462754370278,-0.508595727634907,
13.0864573011627));
#13788=CARTESIAN_POINT('Ctrl Pts',(1.96733008104411,-0.362005440389104,
13.0966739134973));
#13789=CARTESIAN_POINT('Ctrl Pts',(1.99243399321145,-0.128438933471832,
13.1130339695099));
#13790=CARTESIAN_POINT('Ctrl Pts',(1.99610201943448,-0.0432103174738727,
13.1190074024435));
#13791=CARTESIAN_POINT('Ctrl Pts',(1.9934006718632,0.0850802574767662,13.1278259638173));
#13792=CARTESIAN_POINT('Ctrl Pts',(1.99109722319045,0.128129848801596,13.1307547908512));
#13793=CARTESIAN_POINT('Ctrl Pts',(1.98547219423881,0.193477003084971,13.1351234634735));
#13794=CARTESIAN_POINT('Ctrl Pts',(1.98316496548815,0.215847192835952,13.1366051061775));
#13795=CARTESIAN_POINT('Ctrl Pts',(1.97984207652003,0.243477810113742,13.1384140784597));
#13796=CARTESIAN_POINT('Ctrl Pts',(1.97918301485427,0.248778389909406,13.1387601430468));
#13797=CARTESIAN_POINT('Ctrl Pts',(1.97811043169272,0.257130638311162,13.1393038574043));
#13798=CARTESIAN_POINT('Ctrl Pts',(1.97771112694384,0.260184057559157,13.1395022938702));
#13799=CARTESIAN_POINT('Ctrl Pts',(1.97694865725338,0.265911358168978,13.1398738571327));
#13800=CARTESIAN_POINT('Ctrl Pts',(1.97658714172015,0.268585396321136,13.1400470719096));
#13801=CARTESIAN_POINT('Ctrl Pts',(1.97574988168768,0.274685145101786,13.1404415947336));
#13802=CARTESIAN_POINT('Ctrl Pts',(1.97527065421958,0.278110350309131,13.140662703405));
#13803=CARTESIAN_POINT('Ctrl Pts',(1.97377430711122,0.288606264528695,13.1413389839619));
#13804=CARTESIAN_POINT('Ctrl Pts',(1.97272809844936,0.295672867620914,13.1417925414698));
#13805=CARTESIAN_POINT('Ctrl Pts',(1.964083492199,0.351973432573512,13.1453931210843));
#13806=CARTESIAN_POINT('Ctrl Pts',(1.95468039609188,0.400917412061402,13.1484441468779));
#13807=CARTESIAN_POINT('Ctrl Pts',(1.93926858598507,0.467557326489517,13.1525523334263));
#13808=CARTESIAN_POINT('Ctrl Pts',(1.93483115752957,0.485593375777294,13.1536595073319));
#13809=CARTESIAN_POINT('Ctrl Pts',(1.89335903109508,0.644554129527794,13.1633962601067));
#13810=CARTESIAN_POINT('Ctrl Pts',(1.84123860629181,0.781090367770322,13.1716437892504));
#13811=CARTESIAN_POINT('Ctrl Pts',(1.74873821181218,0.961341575418219,13.1836318445919));
#13812=CARTESIAN_POINT('Ctrl Pts',(1.72061766441957,1.01081008227968,13.187044264059));
#13813=CARTESIAN_POINT('Ctrl Pts',(1.67290828311319,1.08696545973394,13.192549166655));
#13814=CARTESIAN_POINT('Ctrl Pts',(1.65470286124178,1.11448386144481,13.1945930931445));
#13815=CARTESIAN_POINT('Ctrl Pts',(1.63071184513949,1.14886302404906,13.1972231222505));
#13816=CARTESIAN_POINT('Ctrl Pts',(1.62555037681857,1.15615454769268,13.197785411657));
#13817=CARTESIAN_POINT('Ctrl Pts',(1.61719866423327,1.16778639120521,13.1986897412691));
#13818=CARTESIAN_POINT('Ctrl Pts',(1.61403947472152,1.17214894454351,13.1990305837515));
#13819=CARTESIAN_POINT('Ctrl Pts',(1.608012980178,1.18040042485246,13.1996784713379));
#13820=CARTESIAN_POINT('Ctrl Pts',(1.60514913448571,1.18429184021412,13.1999853806643));
#13821=CARTESIAN_POINT('Ctrl Pts',(1.59861612955871,1.19310170842326,13.2006833264761));
#13822=CARTESIAN_POINT('Ctrl Pts',(1.59493836968672,1.19801369434502,13.2010746972126));
#13823=CARTESIAN_POINT('Ctrl Pts',(1.58372779031625,1.21284333352319,13.2022630990607));
#13824=CARTESIAN_POINT('Ctrl Pts',(1.57612481340966,1.22270733470932,13.203062884784));
#13825=CARTESIAN_POINT('Ctrl Pts',(1.56033147370935,1.24280531712927,13.2047119638263));
#13826=CARTESIAN_POINT('Ctrl Pts',(1.5521316207831,1.25303103802927,13.2055616113609));
#13827=CARTESIAN_POINT('Ctrl Pts',(1.44996213316498,1.37790090780837,13.2160698435598));
#13828=CARTESIAN_POINT('Ctrl Pts',(1.34361496954079,1.48178394063907,13.2262569473503));
#13829=CARTESIAN_POINT('Ctrl Pts',(1.1574594013498,1.62697318623863,13.2427204541973));
#13830=CARTESIAN_POINT('Ctrl Pts',(1.08464744814017,1.67639352202142,13.2488716641467));
#13831=CARTESIAN_POINT('Ctrl Pts',(0.979941461428567,1.73777504832511,13.257146343355));
#13832=CARTESIAN_POINT('Ctrl Pts',(0.950649470120971,1.75397070834892,13.2594030327629));
#13833=CARTESIAN_POINT('Ctrl Pts',(0.904250294865482,1.77812089379548,13.2628727538733));
#13834=CARTESIAN_POINT('Ctrl Pts',(0.887415296080831,1.78658239798831,13.2641106634409));
#13835=CARTESIAN_POINT('Ctrl Pts',(0.865932525493793,1.79700132662705,13.2656615516521));
#13836=CARTESIAN_POINT('Ctrl Pts',(0.861394488730777,1.79918104779167,13.2659875519552));
#13837=CARTESIAN_POINT('Ctrl Pts',(0.854129078571266,1.80263699787101,13.2665068525781));
#13838=CARTESIAN_POINT('Ctrl Pts',(0.851407020973725,1.80392425392159,13.2667008267593));
#13839=CARTESIAN_POINT('Ctrl Pts',(0.846227197220622,1.80635944688689,13.2670688124267));
#13840=CARTESIAN_POINT('Ctrl Pts',(0.84377003472561,1.80750851982913,13.2672428909646));
#13841=CARTESIAN_POINT('Ctrl Pts',(0.838121183428136,1.8101361321636,13.2676419882736));
#13842=CARTESIAN_POINT('Ctrl Pts',(0.834927925133512,1.81161124289155,13.267866793755));
#13843=CARTESIAN_POINT('Ctrl Pts',(0.826396797936264,1.81552480931151,13.2684652928087));
#13844=CARTESIAN_POINT('Ctrl Pts',(0.821051992097934,1.81794819211223,13.2688380762222));
#13845=CARTESIAN_POINT('Ctrl Pts',(0.783334542785741,1.83484935122413,13.2714539631357));
#13846=CARTESIAN_POINT('Ctrl Pts',(0.750589195424921,1.84848624102692,13.2736485184695));
#13847=CARTESIAN_POINT('Ctrl Pts',(0.7072754536045,1.86518335845651,13.2764742729566));
#13848=CARTESIAN_POINT('Ctrl Pts',(0.69702318445152,1.86903884840689,13.2771375635024));
#13849=CARTESIAN_POINT('Ctrl Pts',(0.670810015722815,1.87865093964678,13.2788205837695));
#13850=CARTESIAN_POINT('Ctrl Pts',(0.654806281530004,1.88428877580716,13.2798360097516));
#13851=CARTESIAN_POINT('Ctrl Pts',(0.568108531090599,1.91359290048269,13.2852815374695));
#13852=CARTESIAN_POINT('Ctrl Pts',(0.496198715834034,1.93348726425133,13.289602664025));
#13853=CARTESIAN_POINT('Ctrl Pts',(0.368398015461284,1.96124235590159,13.2971874262387));
#13854=CARTESIAN_POINT('Ctrl Pts',(0.312975950731405,1.97084614455032,13.3004459759949));
#13855=CARTESIAN_POINT('Ctrl Pts',(0.157032436129244,1.99112439144268,13.309665945822));
#13856=CARTESIAN_POINT('Ctrl Pts',(0.0560098044528245,1.99652054836473,
13.3157054147493));
#13857=CARTESIAN_POINT('Ctrl Pts',(-0.0598190941009771,1.99390812031561,
13.3229219794116));
#13858=CARTESIAN_POINT('Ctrl Pts',(-0.0746551103487114,1.9934077635794,
13.3238515869151));
#13859=CARTESIAN_POINT('Ctrl Pts',(-0.0960672529864728,1.99244625372998,
13.3252013740779));
#13860=CARTESIAN_POINT('Ctrl Pts',(-0.102649086167767,1.99211800717658,
13.3256173913731));
#13861=CARTESIAN_POINT('Ctrl Pts',(-0.114117915505229,1.99148904997615,
13.3263442815541));
#13862=CARTESIAN_POINT('Ctrl Pts',(-0.119005682748961,1.9912029483676,13.3266546939597));
#13863=CARTESIAN_POINT('Ctrl Pts',(-0.128441960770964,1.99061573506232,
13.3272552051017));
#13864=CARTESIAN_POINT('Ctrl Pts',(-0.132990594538204,1.99031702076845,
13.3275452266908));
#13865=CARTESIAN_POINT('Ctrl Pts',(-0.144987077762068,1.98948788928263,
13.3283116039575));
#13866=CARTESIAN_POINT('Ctrl Pts',(-0.152432987274602,1.98893124471401,
13.3287887801909));
#13867=CARTESIAN_POINT('Ctrl Pts',(-0.178586625663199,1.98682831389388,
13.3304702536337));
#13868=CARTESIAN_POINT('Ctrl Pts',(-0.197275014016704,1.98505981283332,
13.3316814981852));
#13869=CARTESIAN_POINT('Ctrl Pts',(-0.422204760476087,1.96056684551021,
13.3463816197707));
#13870=CARTESIAN_POINT('Ctrl Pts',(-0.623673038696467,1.90606107047558,
13.3609840152083));
#13871=CARTESIAN_POINT('Ctrl Pts',(-0.864687321768802,1.79848295300659,
13.3792660631763));
#13872=CARTESIAN_POINT('Ctrl Pts',(-0.915324463526708,1.77324764414166,
13.3831441071015));
#13873=CARTESIAN_POINT('Ctrl Pts',(-0.988424635264389,1.73285065072883,
13.3887331243258));
#13874=CARTESIAN_POINT('Ctrl Pts',(-1.0117596025864,1.71933048663833,13.3905156379324));
#13875=CARTESIAN_POINT('Ctrl Pts',(-1.03964711410544,1.70240811575281,13.392637445272));
#13876=CARTESIAN_POINT('Ctrl Pts',(-1.04446719328993,1.69945514753302,13.393003866304));
#13877=CARTESIAN_POINT('Ctrl Pts',(-1.05195193000269,1.69482583433654,13.3935722869875));
#13878=CARTESIAN_POINT('Ctrl Pts',(-1.05462523394687,1.69316363297528,13.3937751951124));
#13879=CARTESIAN_POINT('Ctrl Pts',(-1.05957596719524,1.69006910221778,13.3941507371138));
#13880=CARTESIAN_POINT('Ctrl Pts',(-1.06185441208804,1.68863850726223,13.3943234791955));
#13881=CARTESIAN_POINT('Ctrl Pts',(-1.06697309923974,1.68541011823196,13.3947113567623));
#13882=CARTESIAN_POINT('Ctrl Pts',(-1.0698116870299,1.68360975758649,13.3949263190115));
#13883=CARTESIAN_POINT('Ctrl Pts',(-1.07705361076544,1.67899089185472,13.3954744262642));
#13884=CARTESIAN_POINT('Ctrl Pts',(-1.08145047555473,1.6761622134475,13.3958069071688));
#13885=CARTESIAN_POINT('Ctrl Pts',(-1.106579794563,1.65985547820696,13.397705730972));
#13886=CARTESIAN_POINT('Ctrl Pts',(-1.12707242421554,1.64600939750679,13.3992487275687));
#13887=CARTESIAN_POINT('Ctrl Pts',(-1.3150683005157,1.51383003712872,13.4134053495354));
#13888=CARTESIAN_POINT('Ctrl Pts',(-1.46366043151311,1.37069681692587,13.4247195065143));
#13889=CARTESIAN_POINT('Ctrl Pts',(-1.61694263365183,1.16911808737151,13.4398090495905));
#13890=CARTESIAN_POINT('Ctrl Pts',(-1.64465750403186,1.12979722331419,13.4427126003522));
#13891=CARTESIAN_POINT('Ctrl Pts',(-1.68688281901247,1.06503884003824,13.4474632483764));
#13892=CARTESIAN_POINT('Ctrl Pts',(-1.70230214304197,1.04021567511907,13.449277126273));
#13893=CARTESIAN_POINT('Ctrl Pts',(-1.72152701723658,1.00769320696023,13.4516485291823));
#13894=CARTESIAN_POINT('Ctrl Pts',(-1.72583638906771,1.00029476901316,13.4521876533559));
#13895=CARTESIAN_POINT('Ctrl Pts',(-1.73273778654472,0.988268917991104,
13.4530635315654));
#13896=CARTESIAN_POINT('Ctrl Pts',(-1.73535925271265,0.983658454101459,
13.453399219929));
#13897=CARTESIAN_POINT('Ctrl Pts',(-1.74034313959852,0.974811186966071,
13.4540432150859));
#13898=CARTESIAN_POINT('Ctrl Pts',(-1.74270855633166,0.97057610767373,13.4543514113084));
#13899=CARTESIAN_POINT('Ctrl Pts',(-1.74805622349338,0.960918984256324,
13.4550540300552));
#13900=CARTESIAN_POINT('Ctrl Pts',(-1.75102872749484,0.955491626786637,
13.4554487974626));
#13901=CARTESIAN_POINT('Ctrl Pts',(-1.76019467883963,0.938569519496435,
13.4566793741643));
#13902=CARTESIAN_POINT('Ctrl Pts',(-1.76630045118237,0.927027913828409,
13.457518283898));
#13903=CARTESIAN_POINT('Ctrl Pts',(-1.77788086488448,0.904607918294743,
13.4591474082248));
#13904=CARTESIAN_POINT('Ctrl Pts',(-1.78337007327317,0.893737672019076,
13.4599370634548));
#13905=CARTESIAN_POINT('Ctrl Pts',(-1.85354326899408,0.751553268442137,
13.4702641222799));
#13906=CARTESIAN_POINT('Ctrl Pts',(-1.90366933323944,0.613581557943482,
13.4803164337795));
#13907=CARTESIAN_POINT('Ctrl Pts',(-1.96803454245798,0.34893131267785,13.499307222851));
#13908=CARTESIAN_POINT('Ctrl Pts',(-1.98614827540819,0.223905700191042,
13.5081504270945));
#13909=CARTESIAN_POINT('Ctrl Pts',(-1.99288066089879,0.0870330352683144,
13.5172147805769));
#13910=CARTESIAN_POINT('Ctrl Pts',(-1.99332947349335,0.0760637918280366,
13.5179367987093));
#13911=CARTESIAN_POINT('Ctrl Pts',(-1.99395253407056,0.0569799569801758,
13.5191846199383));
#13912=CARTESIAN_POINT('Ctrl Pts',(-1.99416785586615,0.0488670821884949,
13.5197124786122));
#13913=CARTESIAN_POINT('Ctrl Pts',(-1.99440810164452,0.0371101366683036,
13.5204734340479));
#13914=CARTESIAN_POINT('Ctrl Pts',(-1.99447256002238,0.0334670880705113,
13.5207086697192));
#13915=CARTESIAN_POINT('Ctrl Pts',(-1.99456773343447,0.0271021835891608,
13.5211186621565));
#13916=CARTESIAN_POINT('Ctrl Pts',(-1.99460285953706,0.0243804164211393,
13.5212936647085));
#13917=CARTESIAN_POINT('Ctrl Pts',(-1.99466073433152,0.0190504664484458,
13.5216357345527));
#13918=CARTESIAN_POINT('Ctrl Pts',(-1.99468393878625,0.0164423202752563,
13.5218028275926));
#13919=CARTESIAN_POINT('Ctrl Pts',(-1.99473339151841,0.00931187168358707,
13.5222588583593));
#13920=CARTESIAN_POINT('Ctrl Pts',(-1.99474937675379,0.00478947843869328,
13.5225472241312));
#13921=CARTESIAN_POINT('Ctrl Pts',(-1.9947518565835,-0.0137361267942171,
13.5237250868335));
#13922=CARTESIAN_POINT('Ctrl Pts',(-1.99460627795939,-0.0277393759214068,
13.5246074513443));
#13923=CARTESIAN_POINT('Ctrl Pts',(-1.99241474297638,-0.132448655508878,
13.5311534944693));
#13924=CARTESIAN_POINT('Ctrl Pts',(-1.98432956355882,-0.2229339883265,13.5365216716757));
#13925=CARTESIAN_POINT('Ctrl Pts',(-1.95880170590122,-0.383837398866256,
13.5460309432565));
#13926=CARTESIAN_POINT('Ctrl Pts',(-1.94363461399264,-0.454444639112673,
13.5501909662735));
#13927=CARTESIAN_POINT('Ctrl Pts',(-1.89190391522397,-0.64442650627835,
13.5616588835142));
#13928=CARTESIAN_POINT('Ctrl Pts',(-1.84792265271898,-0.761420471277343,
13.569043723363));
#13929=CARTESIAN_POINT('Ctrl Pts',(-1.78761479390147,-0.885228866413328,
13.5776391827148));
#13930=CARTESIAN_POINT('Ctrl Pts',(-1.7818037667411,-0.89686795090905,13.578454990176));
#13931=CARTESIAN_POINT('Ctrl Pts',(-1.77303495227816,-0.914009644700568,
13.5796683731143));
#13932=CARTESIAN_POINT('Ctrl Pts',(-1.77016441296378,-0.919556698763571,
13.5800628839119));
#13933=CARTESIAN_POINT('Ctrl Pts',(-1.7650210609023,-0.929382423509603,
13.5807650484149));
#13934=CARTESIAN_POINT('Ctrl Pts',(-1.76275861241262,-0.933666486623504,
13.581072333889));
#13935=CARTESIAN_POINT('Ctrl Pts',(-1.75797591366456,-0.942643423616753,
13.5817186431198));
#13936=CARTESIAN_POINT('Ctrl Pts',(-1.75545243093064,-0.947334523251863,
13.5820577799426));
#13937=CARTESIAN_POINT('Ctrl Pts',(-1.74877426631718,-0.959630776713941,
13.5829504212264));
#13938=CARTESIAN_POINT('Ctrl Pts',(-1.74458879691419,-0.967218996866907,
13.5835050213464));
#13939=CARTESIAN_POINT('Ctrl Pts',(-1.72558086116508,-1.0011554253151,13.586002369479));
#13940=CARTESIAN_POINT('Ctrl Pts',(-1.71021068043326,-1.02719071048617,
13.5879647286637));
#13941=CARTESIAN_POINT('Ctrl Pts',(-1.66765998501485,-1.09566265393085,
13.593254408302));
#13942=CARTESIAN_POINT('Ctrl Pts',(-1.63945451104634,-1.13743336707393,
13.5966178070499));
#13943=CARTESIAN_POINT('Ctrl Pts',(-1.55059752970957,-1.25884448808484,
13.6068074846884));
#13944=CARTESIAN_POINT('Ctrl Pts',(-1.48550662201408,-1.33503142406606,
13.6137709875337));
#13945=CARTESIAN_POINT('Ctrl Pts',(-1.32818199005847,-1.49336030230474,
13.6293441809708));
#13946=CARTESIAN_POINT('Ctrl Pts',(-1.23346872288955,-1.57249952554449,
13.6379336920815));
#13947=CARTESIAN_POINT('Ctrl Pts',(-1.12583008634324,-1.64669100060092,
13.6464686967165));
#13948=CARTESIAN_POINT('Ctrl Pts',(-1.11958546388382,-1.65094307238791,
13.6469597321174));
#13949=CARTESIAN_POINT('Ctrl Pts',(-1.11041204924244,-1.65711342331361,
13.6476748841197));
#13950=CARTESIAN_POINT('Ctrl Pts',(-1.10750221803199,-1.65905956925683,
13.6479008283778));
#13951=CARTESIAN_POINT('Ctrl Pts',(-1.10233048015204,-1.66249884824038,
13.6483007840563));
#13952=CARTESIAN_POINT('Ctrl Pts',(-1.10007063819243,-1.6639950418226,13.648475000758));
#13953=CARTESIAN_POINT('Ctrl Pts',(-1.09528607635229,-1.66714879204547,
13.6488426906523));
#13954=CARTESIAN_POINT('Ctrl Pts',(-1.09276064635298,-1.66880521749823,
13.649036087936));
#13955=CARTESIAN_POINT('Ctrl Pts',(-1.08598144410121,-1.67322969790105,
13.6495534465257));
#13956=CARTESIAN_POINT('Ctrl Pts',(-1.0817208182994,-1.67598728858241,13.6498767132344));
#13957=CARTESIAN_POINT('Ctrl Pts',(-1.06121797543951,-1.6891465215322,13.651423535225));
#13958=CARTESIAN_POINT('Ctrl Pts',(-1.0448353165871,-1.69932892365676,13.6526331289959));
#13959=CARTESIAN_POINT('Ctrl Pts',(-0.998669783616965,-1.72710233649159,
13.6559762264157));
#13960=CARTESIAN_POINT('Ctrl Pts',(-0.968572184483595,-1.7441594062842,
13.6580810796015));
#13961=CARTESIAN_POINT('Ctrl Pts',(-0.857073414099578,-1.80357161420617,
13.6656660709162));
#13962=CARTESIAN_POINT('Ctrl Pts',(-0.773216541669191,-1.84108225219575,
13.6709707383685));
#13963=CARTESIAN_POINT('Ctrl Pts',(-0.540926825004352,-1.9263069878786,
13.6853210900567));
#13964=CARTESIAN_POINT('Ctrl Pts',(-0.389033638832481,-1.96262681157849,
13.6943910236463));
#13965=CARTESIAN_POINT('Ctrl Pts',(-0.22198425449101,-1.98239973600362,
13.7048953654109));
#13966=CARTESIAN_POINT('Ctrl Pts',(-0.209481802514728,-1.98375983561964,
13.7056843004836));
#13967=CARTESIAN_POINT('Ctrl Pts',(-0.190837058928924,-1.98560991446025,
13.7068652520011));
#13968=CARTESIAN_POINT('Ctrl Pts',(-0.184703839776413,-1.98618982115298,
13.7072544392017));
#13969=CARTESIAN_POINT('Ctrl Pts',(-0.173753088159362,-1.98717407349497,
13.7079506339012));
#13970=CARTESIAN_POINT('Ctrl Pts',(-0.168936565998396,-1.98758933635946,
13.7082572956933));
#13971=CARTESIAN_POINT('Ctrl Pts',(-0.158764366555967,-1.98842910403805,
13.7089059193552));
#13972=CARTESIAN_POINT('Ctrl Pts',(-0.153408396588484,-1.98884948872417,
13.709248008155));
#13973=CARTESIAN_POINT('Ctrl Pts',(-0.139204099398249,-1.98990665094881,
13.7101567850753));
#13974=CARTESIAN_POINT('Ctrl Pts',(-0.130353189343438,-1.99050604183705,
13.7107246418595));
#13975=CARTESIAN_POINT('Ctrl Pts',(-0.0892311574106101,-1.99301541238939,
13.7133705314204));
#13976=CARTESIAN_POINT('Ctrl Pts',(-0.056922212642224,-1.9941996618506,
13.7154711510732));
#13977=CARTESIAN_POINT('Ctrl Pts',(0.0306819320997055,-1.99528012266538,
13.7212297306897));
#13978=CARTESIAN_POINT('Ctrl Pts',(0.0859639078202527,-1.99366331705495,
13.7249321416479));
#13979=CARTESIAN_POINT('Ctrl Pts',(0.244771904188504,-1.98240144378039,
13.735757126845));
#13980=CARTESIAN_POINT('Ctrl Pts',(0.347700116554994,-1.9669596245787,13.743014511153));
#13981=CARTESIAN_POINT('Ctrl Pts',(0.518426938686605,-1.92752329500175,
13.7552335581274));
#13982=CARTESIAN_POINT('Ctrl Pts',(0.587000182459165,-1.90775903599471,
13.7601893322398));
#13983=CARTESIAN_POINT('Ctrl Pts',(0.662713030689064,-1.88146670996804,
13.7656255059346));
#13984=CARTESIAN_POINT('Ctrl Pts',(0.671035747824405,-1.87851445874288,
13.7662225510292));
#13985=CARTESIAN_POINT('Ctrl Pts',(0.71085800742426,-1.86409019765168,13.769075898882));
#13986=CARTESIAN_POINT('Ctrl Pts',(0.742086858824165,-1.85187979996067,
13.7713034109572));
#13987=CARTESIAN_POINT('Ctrl Pts',(0.77831348089238,-1.83665156452692,13.7738634727205));
#13988=CARTESIAN_POINT('Ctrl Pts',(0.783622080171581,-1.8343928917962,13.7742380080199));
#13989=CARTESIAN_POINT('Ctrl Pts',(0.792124647729441,-1.83073162212737,
13.7748368142688));
#13990=CARTESIAN_POINT('Ctrl Pts',(0.795324816879373,-1.82934364347109,
13.7750619464291));
#13991=CARTESIAN_POINT('Ctrl Pts',(0.801003431197971,-1.82686299487258,
13.7754609809476));
#13992=CARTESIAN_POINT('Ctrl Pts',(0.803483307726371,-1.82577366433469,
13.775635085254));
#13993=CARTESIAN_POINT('Ctrl Pts',(0.808729990388,-1.82345620411572,13.7760031014962));
#13994=CARTESIAN_POINT('Ctrl Pts',(0.811496214154684,-1.82222683011553,
13.7761969353473));
#13995=CARTESIAN_POINT('Ctrl Pts',(0.818920931295585,-1.81890685375166,
13.7767166973144));
#13996=CARTESIAN_POINT('Ctrl Pts',(0.823574253168949,-1.81680463595911,
13.777041919548));
#13997=CARTESIAN_POINT('Ctrl Pts',(0.846081381207996,-1.80653241389346,
13.7786126202225));
#13998=CARTESIAN_POINT('Ctrl Pts',(0.863822733397944,-1.79811663187595,
13.7798436106925));
#13999=CARTESIAN_POINT('Ctrl Pts',(0.913256145319009,-1.77376684802055,
13.7832614458629));
#14000=CARTESIAN_POINT('Ctrl Pts',(0.944652895926133,-1.75724694852104,
13.7854180641716));
#14001=CARTESIAN_POINT('Ctrl Pts',(1.0588760128137,-1.6931998345439,13.7932720581506));
#14002=CARTESIAN_POINT('Ctrl Pts',(1.1387030602224,-1.64057973191981,13.7987816775673));
#14003=CARTESIAN_POINT('Ctrl Pts',(1.21823562510925,-1.57954176858851,13.8045975176185));
#14004=CARTESIAN_POINT('Ctrl Pts',(1.22200275413431,-1.57662915924049,13.8048737913468));
#14005=CARTESIAN_POINT('Ctrl Pts',(1.34054237754247,-1.48429849005539,13.81359359804));
#14006=CARTESIAN_POINT('Ctrl Pts',(1.44518155266242,-1.3826198123348,13.8221163291868));
#14007=CARTESIAN_POINT('Ctrl Pts',(1.54598727698084,-1.26060103973144,13.8319971454823));
#14008=CARTESIAN_POINT('Ctrl Pts',(1.55405021421574,-1.25064765680068,13.8328005582588));
#14009=CARTESIAN_POINT('Ctrl Pts',(1.56587678229632,-1.23575725294827,13.8339989931224));
#14010=CARTESIAN_POINT('Ctrl Pts',(1.56971424079087,-1.23087907058031,13.8343910602453));
#14011=CARTESIAN_POINT('Ctrl Pts',(1.5765034552398,-1.22216522723103,13.8350904754685));
#14012=CARTESIAN_POINT('Ctrl Pts',(1.57946414870929,-1.21833656651237,13.8353974656866));
#14013=CARTESIAN_POINT('Ctrl Pts',(1.58566649092188,-1.21025531799901,13.8360447937092));
#14014=CARTESIAN_POINT('Ctrl Pts',(1.58890502796241,-1.20600040065295,13.8363852508279));
#14015=CARTESIAN_POINT('Ctrl Pts',(1.59740249985309,-1.19474244704764,13.8372851089981));
#14016=CARTESIAN_POINT('Ctrl Pts',(1.60263244524425,-1.18771777064549,13.8378456381307));
#14017=CARTESIAN_POINT('Ctrl Pts',(1.62625411533122,-1.15554989028574,13.8404083171236));
#14018=CARTESIAN_POINT('Ctrl Pts',(1.6441006921545,-1.1300135964279,13.8424313591748));
#14019=CARTESIAN_POINT('Ctrl Pts',(1.69040731019591,-1.06033411940189,13.8479251632032));
#14020=CARTESIAN_POINT('Ctrl Pts',(1.7177325813566,-1.01546998495897,13.8514355260991));
#14021=CARTESIAN_POINT('Ctrl Pts',(1.79271940753026,-0.880648034672342,
13.8619020718953));
#14022=CARTESIAN_POINT('Ctrl Pts',(1.83530232144922,-0.788064673361517,
13.8689946708152));
#14023=CARTESIAN_POINT('Ctrl Pts',(1.9116315202932,-0.581921974203907,13.884330097668));
#14024=CARTESIAN_POINT('Ctrl Pts',(1.94272336619323,-0.467761892707373,
13.8925466142314));
#14025=CARTESIAN_POINT('Ctrl Pts',(1.96488315905716,-0.343977164830148,
13.9007580609771));
#14026=CARTESIAN_POINT('Ctrl Pts',(1.96618828157022,-0.336436865826537,
13.9012555005137));
#14027=CARTESIAN_POINT('Ctrl Pts',(1.96803020612822,-0.3254182746908,13.9019781998201));
#14028=CARTESIAN_POINT('Ctrl Pts',(1.96860122662795,-0.321945890983775,
13.9022053416384));
#14029=CARTESIAN_POINT('Ctrl Pts',(1.96959616892833,-0.315794004044673,
13.9026066606355));
#14030=CARTESIAN_POINT('Ctrl Pts',(1.97002381686889,-0.313115127344135,
13.9027810480091));
#14031=CARTESIAN_POINT('Ctrl Pts',(1.97091447964498,-0.307461766781899,
13.9031482797371));
#14032=CARTESIAN_POINT('Ctrl Pts',(1.97137622556085,-0.3044871125265,13.9033410513282));
#14033=CARTESIAN_POINT('Ctrl Pts',(1.97259164080799,-0.296538511739521,
13.9038549668516));
#14034=CARTESIAN_POINT('Ctrl Pts',(1.97333323695362,-0.291562699246015,
13.904175432223));
#14035=CARTESIAN_POINT('Ctrl Pts',(1.97675713439055,-0.267978117832872,
13.9056887214018));
#14036=CARTESIAN_POINT('Ctrl Pts',(1.9791951938879,-0.249334086534074,13.9068683054678));
#14037=CARTESIAN_POINT('Ctrl Pts',(1.98522763885092,-0.197514836733235,
13.9101075476434));
#14038=CARTESIAN_POINT('Ctrl Pts',(1.98825394017183,-0.164278499112953,
13.9121406680116));
#14039=CARTESIAN_POINT('Ctrl Pts',(1.99619160483572,-0.0436532919129626,
13.9194087086716));
#14040=CARTESIAN_POINT('Ctrl Pts',(1.99618533483194,0.043963104206752,13.9244809522692));
#14041=CARTESIAN_POINT('Ctrl Pts',(1.98063159133876,0.279746294262301,13.9381854976157));
#14042=CARTESIAN_POINT('Ctrl Pts',(1.95426623850361,0.4266096851535,13.9468162839343));
#14043=CARTESIAN_POINT('Ctrl Pts',(1.90756626232315,0.583473421016851,13.9569409452345));
#14044=CARTESIAN_POINT('Ctrl Pts',(1.90314774562963,0.597728130332748,13.9578690641864));
#14045=CARTESIAN_POINT('Ctrl Pts',(1.89544359618929,0.621630907615951,13.9594396531293));
#14046=CARTESIAN_POINT('Ctrl Pts',(1.89224316941717,0.631305942690054,13.9600793464363));
#14047=CARTESIAN_POINT('Ctrl Pts',(1.88697072846152,0.646844416737335,13.9611133090565));
#14048=CARTESIAN_POINT('Ctrl Pts',(1.88494515609302,0.652723514693834,13.9615060443685));
#14049=CARTESIAN_POINT('Ctrl Pts',(1.8812891406975,0.663175922719456,13.9622070512015));
#14050=CARTESIAN_POINT('Ctrl Pts',(1.87966942028213,0.667752952187103,13.9625149649794));
#14051=CARTESIAN_POINT('Ctrl Pts',(1.87625048449666,0.677303220194546,13.9631594514686));
#14052=CARTESIAN_POINT('Ctrl Pts',(1.87444817059189,0.682275301866131,13.963496125358));
#14053=CARTESIAN_POINT('Ctrl Pts',(1.8696995001406,0.695214715739058,13.9643752960744));
#14054=CARTESIAN_POINT('Ctrl Pts',(1.86672200931945,0.703170433128824,13.9649188290253));
#14055=CARTESIAN_POINT('Ctrl Pts',(1.85350437410389,0.737811679144055,13.9672987406728));
#14056=CARTESIAN_POINT('Ctrl Pts',(1.84274258265454,0.764293249764667,13.9691525367127));
#14057=CARTESIAN_POINT('Ctrl Pts',(1.81291974310069,0.833383345159686,13.9740833975887));
#14058=CARTESIAN_POINT('Ctrl Pts',(1.79292668649248,0.87556788092392,13.9771907967008));
#14059=CARTESIAN_POINT('Ctrl Pts',(1.68296810186906,1.08798519929659,13.9933389278402));
#14060=CARTESIAN_POINT('Ctrl Pts',(1.5701948284717,1.24521702220936,14.0071145680869));
#14061=CARTESIAN_POINT('Ctrl Pts',(1.41027053067053,1.41124472081864,14.0227049741085));
#14062=CARTESIAN_POINT('Ctrl Pts',(1.38309971724818,1.43788395560388,14.0252402074162));
#14063=CARTESIAN_POINT('Ctrl Pts',(1.35035870687126,1.46819689488969,14.0281483765619));
#14064=CARTESIAN_POINT('Ctrl Pts',(1.3455137860071,1.47263824953324,14.0285750805002));
#14065=CARTESIAN_POINT('Ctrl Pts',(1.33813866080774,1.47933226872889,14.0292190152375));
#14066=CARTESIAN_POINT('Ctrl Pts',(1.33562458356043,1.48160251385363,14.0294375446393));
#14067=CARTESIAN_POINT('Ctrl Pts',(1.33110208309596,1.48566552574412,14.02982887802));
#14068=CARTESIAN_POINT('Ctrl Pts',(1.3290958120192,1.48746063234251,14.030001857629));
#14069=CARTESIAN_POINT('Ctrl Pts',(1.32475040087298,1.49133286812748,14.0303751681932));
#14070=CARTESIAN_POINT('Ctrl Pts',(1.32241001548226,1.49340855074957,14.0305753906491));
#14071=CARTESIAN_POINT('Ctrl Pts',(1.31589437113479,1.49915993465938,14.0311305195149));
#14072=CARTESIAN_POINT('Ctrl Pts',(1.31170856481017,1.50282372501202,14.0314845450913));
#14073=CARTESIAN_POINT('Ctrl Pts',(1.2881920714096,1.5232343469081,14.0334593624688));
#14074=CARTESIAN_POINT('Ctrl Pts',(1.26855496702423,1.53962662174213,14.0350551617011));
#14075=CARTESIAN_POINT('Ctrl Pts',(1.12039736330129,1.65854288372357,14.0467527892344));
#14076=CARTESIAN_POINT('Ctrl Pts',(0.979942041663491,1.74521719071281,14.0560101728908));
#14077=CARTESIAN_POINT('Ctrl Pts',(0.730475920874315,1.85943988592107,14.072061721505));
#14078=CARTESIAN_POINT('Ctrl Pts',(0.626929162196461,1.89685699182623,14.0786182510588));
#14079=CARTESIAN_POINT('Ctrl Pts',(0.508370114521299,1.92892565464097,14.0862848138036));
#14080=CARTESIAN_POINT('Ctrl Pts',(0.495871109096363,1.93217654088341,14.0870947723244));
#14081=CARTESIAN_POINT('Ctrl Pts',(0.477299835351369,1.93681470720925,14.0883011036752));
#14082=CARTESIAN_POINT('Ctrl Pts',(0.47125104699431,1.93829533151338,14.0886944638391));
#14083=CARTESIAN_POINT('Ctrl Pts',(0.460486545571937,1.94087690316734,14.0893953319801));
#14084=CARTESIAN_POINT('Ctrl Pts',(0.455773549061324,1.94198905331613,14.0897024766012));
#14085=CARTESIAN_POINT('Ctrl Pts',(0.451048087361994,1.94308599538547,14.0900107288729));
#14086=CARTESIAN_POINT('Ctrl Pts',(0.451039591272035,1.94308796756123,14.0900112830925));
#14087=CARTESIAN_POINT('Ctrl Pts',(0.451022618687848,1.94309190724672,14.0900123902554));
#14088=CARTESIAN_POINT('Ctrl Pts',(0.451014142110932,1.94309387477591,14.090012943204));
#14089=CARTESIAN_POINT('Ctrl Pts',(0.450997208663554,1.94309780514339,14.0900140478177));
#14090=CARTESIAN_POINT('Ctrl Pts',(0.45098875162203,1.94309976802165,14.0900145994938));
#14091=CARTESIAN_POINT('Ctrl Pts',(0.450971856898543,1.94310368916857,14.0900157015852));
#14092=CARTESIAN_POINT('Ctrl Pts',(0.450963419250079,1.94310564742973,14.0900162519982));
#14093=CARTESIAN_POINT('Ctrl Pts',(0.450946563230409,1.94310955936236,14.0900173515686));
#14094=CARTESIAN_POINT('Ctrl Pts',(0.450938144895026,1.94311151302578,14.0900179007237));
#14095=CARTESIAN_POINT('Ctrl Pts',(0.450921327437817,1.9431154157785,14.0900189977823));
#14096=CARTESIAN_POINT('Ctrl Pts',(0.450912928337988,1.94311736486297,14.0900195456844));
#14097=CARTESIAN_POINT('Ctrl Pts',(0.450896149287829,1.94312125847344,14.0900206402413));
#14098=CARTESIAN_POINT('Ctrl Pts',(0.450887769335964,1.94312320300007,14.0900211868962));
#14099=CARTESIAN_POINT('Ctrl Pts',(0.450871028619272,1.94312708748694,14.0900222789561));
#14100=CARTESIAN_POINT('Ctrl Pts',(0.450862667788463,1.94312902746275,14.0900228243655));
#14101=CARTESIAN_POINT('Ctrl Pts',(0.450845965149942,1.94313290288682,14.0900239139452));
#14102=CARTESIAN_POINT('Ctrl Pts',(0.450837623352016,1.94313483833306,14.0900244581149));
#14103=CARTESIAN_POINT('Ctrl Pts',(0.445712436350852,1.94432393855725,14.0903587956287));
#14104=CARTESIAN_POINT('Ctrl Pts',(0.44059096277679,1.94549087805976,14.090693237635));
#14105=CARTESIAN_POINT('Ctrl Pts',(0.427247453436127,1.9484758358801,14.0915655262044));
#14106=CARTESIAN_POINT('Ctrl Pts',(0.419018475824329,1.95026202926371,14.0921043884722));
#14107=CARTESIAN_POINT('Ctrl Pts',(0.4009526909984,1.9540637975691,14.093289505301));
#14108=CARTESIAN_POINT('Ctrl Pts',(0.391111523534666,1.9560572986011,14.0939364510269));
#14109=CARTESIAN_POINT('Ctrl Pts',(0.362157647324509,1.96169517831095,14.095844017298));
#14110=CARTESIAN_POINT('Ctrl Pts',(0.34300661950407,1.96513423172292,14.0971110843593));
#14111=CARTESIAN_POINT('Ctrl Pts',(0.275847153198609,1.97618280946162,14.1015741010343));
#14112=CARTESIAN_POINT('Ctrl Pts',(0.227616654485031,1.98231686626571,14.1048146659128));
#14113=CARTESIAN_POINT('Ctrl Pts',(0.0600476630782478,1.99743282104281,
14.1161925064959));
#14114=CARTESIAN_POINT('Ctrl Pts',(-0.05983373020311,1.99743790249784,14.1245580774018));
#14115=CARTESIAN_POINT('Ctrl Pts',(-0.246995628927533,1.98057683442121,
14.1376545033346));
#14116=CARTESIAN_POINT('Ctrl Pts',(-0.31465766922163,1.97095996034574,14.1423914355414));
#14117=CARTESIAN_POINT('Ctrl Pts',(-0.420250004285369,1.95037441021363,
14.1496745242331));
#14118=CARTESIAN_POINT('Ctrl Pts',(-0.458576121107775,1.94172059170124,
14.1522944264559));
#14119=CARTESIAN_POINT('Ctrl Pts',(-0.503052720171037,1.93028743298646,
14.1552879441627));
#14120=CARTESIAN_POINT('Ctrl Pts',(-0.509472628877797,1.92860292871875,
14.1557188841443));
#14121=CARTESIAN_POINT('Ctrl Pts',(-0.519169733065526,1.92600672891297,
14.1563679340139));
#14122=CARTESIAN_POINT('Ctrl Pts',(-0.522453121330005,1.92511866335154,
14.1565873730946));
#14123=CARTESIAN_POINT('Ctrl Pts',(-0.528332219504052,1.92351238145379,
14.1569796874041));
#14124=CARTESIAN_POINT('Ctrl Pts',(-0.530928750029529,1.92279730560957,
14.1571527421038));
#14125=CARTESIAN_POINT('Ctrl Pts',(-0.53652835559629,1.9212429852997,14.1575254849396));
#14126=CARTESIAN_POINT('Ctrl Pts',(-0.5395309027404,1.92040196058962,14.1577250675247));
#14127=CARTESIAN_POINT('Ctrl Pts',(-0.547840098401107,1.91805349810208,
14.1582766315778));
#14128=CARTESIAN_POINT('Ctrl Pts',(-0.553142535064395,1.91653106748637,
14.1586277506138));
#14129=CARTESIAN_POINT('Ctrl Pts',(-0.582338975191743,1.90801695011468,
14.1605567148997));
#14130=CARTESIAN_POINT('Ctrl Pts',(-0.606108063188161,1.90060004179537,
14.1621109123188));
#14131=CARTESIAN_POINT('Ctrl Pts',(-0.677268036377954,1.87692440877626,
14.1667323226522));
#14132=CARTESIAN_POINT('Ctrl Pts',(-0.724193761676973,1.85932282933657,
14.1697373885421));
#14133=CARTESIAN_POINT('Ctrl Pts',(-0.904492790581082,1.78383024896867,
14.1812948314115));
#14134=CARTESIAN_POINT('Ctrl Pts',(-1.03203783113073,1.71320114618023,14.1895273311107));
#14135=CARTESIAN_POINT('Ctrl Pts',(-1.17434099269437,1.6126943095871,14.1998544280922));
#14136=CARTESIAN_POINT('Ctrl Pts',(-1.19753894490107,1.59554381993037,14.2015768445579));
#14137=CARTESIAN_POINT('Ctrl Pts',(-1.26286629641932,1.54501919947881,14.2065540833302));
#14138=CARTESIAN_POINT('Ctrl Pts',(-1.30402707849208,1.51043973353006,14.2098469913305));
#14139=CARTESIAN_POINT('Ctrl Pts',(-1.35107059390338,1.46756063510306,14.2138292785904));
#14140=CARTESIAN_POINT('Ctrl Pts',(-1.35835197126327,1.46082370048428,14.214452149388));
#14141=CARTESIAN_POINT('Ctrl Pts',(-1.3701049018581,1.44978571134198,14.2154683235296));
#14142=CARTESIAN_POINT('Ctrl Pts',(-1.37460723140893,1.44551755743488,14.2158602162599));
#14143=CARTESIAN_POINT('Ctrl Pts',(-1.38258616241949,1.43788264027959,14.2165594358498));
#14144=CARTESIAN_POINT('Ctrl Pts',(-1.38607057537324,1.43452408245359,14.2168664055652));
#14145=CARTESIAN_POINT('Ctrl Pts',(-1.39277871695146,1.42801097739425,14.2174605375819));
#14146=CARTESIAN_POINT('Ctrl Pts',(-1.39600403929216,1.42485810791133,14.2177476254877));
#14147=CARTESIAN_POINT('Ctrl Pts',(-1.40295859262847,1.4180134999054,14.2183697634872));
#14148=CARTESIAN_POINT('Ctrl Pts',(-1.40668399721728,1.41431793796357,14.218704981133));
#14149=CARTESIAN_POINT('Ctrl Pts',(-1.42121147691924,1.39979265190426,14.2200198984145));
#14150=CARTESIAN_POINT('Ctrl Pts',(-1.43190319211175,1.38885375658874,14.2210044416164));
#14151=CARTESIAN_POINT('Ctrl Pts',(-1.48996490074829,1.32806659090648,14.2264456742866));
#14152=CARTESIAN_POINT('Ctrl Pts',(-1.53485355648307,1.27592278644834,14.2310070410109));
#14153=CARTESIAN_POINT('Ctrl Pts',(-1.61307833441772,1.17494042229399,14.2396547067972));
#14154=CARTESIAN_POINT('Ctrl Pts',(-1.64711153839,1.12673397856859,14.2437116930747));
#14155=CARTESIAN_POINT('Ctrl Pts',(-1.76304350119893,0.946020985530517,
14.2586084017862));
#14156=CARTESIAN_POINT('Ctrl Pts',(-1.83149559110271,0.805547899966137,
14.2696511925881));
#14157=CARTESIAN_POINT('Ctrl Pts',(-1.88758510298821,0.645174720774092,
14.2808593455718));
#14158=CARTESIAN_POINT('Ctrl Pts',(-1.8921161350605,0.631763009804888,14.2817861563105));
#14159=CARTESIAN_POINT('Ctrl Pts',(-1.89796473959787,0.613823764000471,
14.2830108333472));
#14160=CARTESIAN_POINT('Ctrl Pts',(-1.89940945525219,0.60933856632469,14.2833157857629));
#14161=CARTESIAN_POINT('Ctrl Pts',(-1.90164065600232,0.602326639120403,
14.2837905472326));
#14162=CARTESIAN_POINT('Ctrl Pts',(-1.90243801746204,0.599803430025924,
14.2839609874213));
#14163=CARTESIAN_POINT('Ctrl Pts',(-1.90395991547368,0.594953896847176,
14.2842877895007));
#14164=CARTESIAN_POINT('Ctrl Pts',(-1.90468520225311,0.592627859197365,
14.2844441923629));
#14165=CARTESIAN_POINT('Ctrl Pts',(-1.90641061662941,0.587058466087206,
14.2848178608698));
#14166=CARTESIAN_POINT('Ctrl Pts',(-1.90740672910799,0.583813884704258,
14.2850348889252));
#14167=CARTESIAN_POINT('Ctrl Pts',(-1.91037970765942,0.574041337216675,
14.2856866241069));
#14168=CARTESIAN_POINT('Ctrl Pts',(-1.91233140354439,0.567505674450074,
14.2861198829101));
#14169=CARTESIAN_POINT('Ctrl Pts',(-1.93061598164805,0.505110414873003,
14.2902324828119));
#14170=CARTESIAN_POINT('Ctrl Pts',(-1.9445321990242,0.448565048757741,14.2937791938054));
#14171=CARTESIAN_POINT('Ctrl Pts',(-1.98164655554369,0.263133038175746,
14.3050692892849));
#14172=CARTESIAN_POINT('Ctrl Pts',(-1.9946405641782,0.132561637484325,14.3125121367147));
#14173=CARTESIAN_POINT('Ctrl Pts',(-1.99474931168446,0.00165711628034759,
14.3201739592359));
#14174=CARTESIAN_POINT('',(-1.994663636046,-0.00099025261153359,15.1209549068572));
#14175=CARTESIAN_POINT('Ctrl Pts',(-1.99474927319053,0.00170282290857632,
14.3209548813952));
#14176=CARTESIAN_POINT('Ctrl Pts',(-1.99480844880348,-0.0676176626926073,
14.3253702812332));
#14177=CARTESIAN_POINT('Ctrl Pts',(-1.99124984682737,-0.137000164295673,
14.3297856810711));
#14178=CARTESIAN_POINT('Ctrl Pts',(-1.98408075767403,-0.206036670346913,
14.3342010809091));
#14179=CARTESIAN_POINT('Ctrl Pts',(-1.97691422051932,-0.275048601300166,
14.3386149089861));
#14180=CARTESIAN_POINT('Ctrl Pts',(-1.96613979730227,-0.34371428884389,
14.3430287370631));
#14181=CARTESIAN_POINT('Ctrl Pts',(-1.95181673263811,-0.411629693649408,
14.3474425651401));
#14182=CARTESIAN_POINT('Ctrl Pts',(-1.93749376889503,-0.479544619919332,
14.3518563621171));
#14183=CARTESIAN_POINT('Ctrl Pts',(-1.91962231764192,-0.546708789784324,
14.356270159094));
#14184=CARTESIAN_POINT('Ctrl Pts',(-1.89831258304288,-0.61272905885152,
14.360683956071));
#14185=CARTESIAN_POINT('Ctrl Pts',(-1.876980577809,-0.678818325178993,14.3651023658722));
#14186=CARTESIAN_POINT('Ctrl Pts',(-1.85220326800389,-0.74376083169,14.3695207756734));
#14187=CARTESIAN_POINT('Ctrl Pts',(-1.82414023188162,-0.807180262971581,
14.3739391854746));
#14188=CARTESIAN_POINT('Ctrl Pts',(-1.79606178800796,-0.870634514107515,
14.378360021163));
#14189=CARTESIAN_POINT('Ctrl Pts',(-1.76469425181013,-0.932563583840136,
14.3827808568514));
#14190=CARTESIAN_POINT('Ctrl Pts',(-1.73024341602082,-0.99261537556931,
14.3872016925398));
#14191=CARTESIAN_POINT('Ctrl Pts',(-1.69572952893114,-1.05277707300822,
14.3916306191622));
#14192=CARTESIAN_POINT('Ctrl Pts',(-1.65812134455463,-1.11105421647625,
14.3960595457846));
#14193=CARTESIAN_POINT('Ctrl Pts',(-1.61766783441448,-1.16712396085453,
14.400488472407));
#14194=CARTESIAN_POINT('Ctrl Pts',(-1.59009756172142,-1.20533716255158,
14.4035069178842));
#14195=CARTESIAN_POINT('Ctrl Pts',(-1.56120656146211,-1.24252572116292,
14.4065253633613));
#14196=CARTESIAN_POINT('Ctrl Pts',(-1.53108363525599,-1.27859706880287,
14.4095438088384));
#14197=CARTESIAN_POINT('Ctrl Pts',(-1.48663404004653,-1.33182419522096,
14.4139978475564));
#14198=CARTESIAN_POINT('Ctrl Pts',(-1.43931749796301,-1.38283607938058,
14.4184518862744));
#14199=CARTESIAN_POINT('Ctrl Pts',(-1.38938328998155,-1.43130766644354,
14.4229059249924));
#14200=CARTESIAN_POINT('Ctrl Pts',(-1.33952414087314,-1.47970639317994,
14.4273532685981));
#14201=CARTESIAN_POINT('Ctrl Pts',(-1.28705548380105,-1.52557206330759,
14.4318006122039));
#14202=CARTESIAN_POINT('Ctrl Pts',(-1.23226639428315,-1.56861311228116,
14.4362479558096));
#14203=CARTESIAN_POINT('Ctrl Pts',(-1.17754189546993,-1.61160342028226,
14.4406900564544));
#14204=CARTESIAN_POINT('Ctrl Pts',(-1.12050278047846,-1.65177541983638,
14.4451321570992));
#14205=CARTESIAN_POINT('Ctrl Pts',(-1.06147313750855,-1.68887605846248,
14.449574257744));
#14206=CARTESIAN_POINT('Ctrl Pts',(-1.0024807306989,-1.72595329384139,14.454013556292));
#14207=CARTESIAN_POINT('Ctrl Pts',(-0.941500700329472,-1.75996275179668,
14.4584528548401));
#14208=CARTESIAN_POINT('Ctrl Pts',(-0.878886965382996,-1.79069407341954,
14.4628921533881));
#14209=CARTESIAN_POINT('Ctrl Pts',(-0.816291451161476,-1.82141645216494,
14.4673301600911));
#14210=CARTESIAN_POINT('Ctrl Pts',(-0.752063615385313,-1.84886237271784,
14.4717681667942));
#14211=CARTESIAN_POINT('Ctrl Pts',(-0.686581302364516,-1.87286776835511,
14.4762061734973));
#14212=CARTESIAN_POINT('Ctrl Pts',(-0.621095794433747,-1.89687433522587,
14.4806443967326));
#14213=CARTESIAN_POINT('Ctrl Pts',(-0.554356148211634,-1.91743987764979,
14.4850826199679));
#14214=CARTESIAN_POINT('Ctrl Pts',(-0.486757792449514,-1.93444938263829,
14.4895208432032));
#14215=CARTESIAN_POINT('Ctrl Pts',(-0.419087823689509,-1.95147690732019,
14.4939637682462));
#14216=CARTESIAN_POINT('Ctrl Pts',(-0.350557805364128,-1.96494075565657,
14.4984066932892));
#14217=CARTESIAN_POINT('Ctrl Pts',(-0.281574914249643,-1.97477672919379,
14.5028496183323));
#14218=CARTESIAN_POINT('Ctrl Pts',(-0.212551754982117,-1.98461844439362,
14.5072951368935));
#14219=CARTESIAN_POINT('Ctrl Pts',(-0.143075684511765,-1.99082802607985,
14.5117406554548));
#14220=CARTESIAN_POINT('Ctrl Pts',(-0.0735577887056503,-1.99339329140557,
14.5161861740161));
#14221=CARTESIAN_POINT('Ctrl Pts',(-0.00391858223084199,-1.99596303319089,
14.5206394501313));
#14222=CARTESIAN_POINT('Ctrl Pts',(0.0657621058233227,-1.9948757716827,
14.5250927262465));
#14223=CARTESIAN_POINT('Ctrl Pts',(0.135075203542659,-1.99017141268985,
14.5295460023618));
#14224=CARTESIAN_POINT('Ctrl Pts',(0.172190374149558,-1.98765236373141,
14.5319306036596));
#14225=CARTESIAN_POINT('Ctrl Pts',(0.209200261547404,-1.98409707230917,
14.5343152049574));
#14226=CARTESIAN_POINT('Ctrl Pts',(0.246043286472205,-1.97951768460955,
14.5366998062552));
#14227=CARTESIAN_POINT('Ctrl Pts',(0.314859930853649,-1.9709641498373,14.5411538449732));
#14228=CARTESIAN_POINT('Ctrl Pts',(0.383366292641739,-1.95880084951107,
14.5456078836912));
#14229=CARTESIAN_POINT('Ctrl Pts',(0.451154115862295,-1.94306137994674,
14.5500619224091));
#14230=CARTESIAN_POINT('Ctrl Pts',(0.518840043452057,-1.92734556925067,
14.5545092660149));
#14231=CARTESIAN_POINT('Ctrl Pts',(0.585809103166717,-1.90806436824703,
14.5589566096206));
#14232=CARTESIAN_POINT('Ctrl Pts',(0.651659651011456,-1.88530296285335,
14.5634039532264));
#14233=CARTESIAN_POINT('Ctrl Pts',(0.717432567829195,-1.86256839081694,
14.5678460538712));
#14234=CARTESIAN_POINT('Ctrl Pts',(0.78208913123683,-1.8363619222356,14.572288154516));
#14235=CARTESIAN_POINT('Ctrl Pts',(0.84524112026654,-1.80681903109043,14.5767302551608));
#14236=CARTESIAN_POINT('Ctrl Pts',(0.908353272741763,-1.77729477573189,
14.5811695537088));
#14237=CARTESIAN_POINT('Ctrl Pts',(0.969962291210684,-1.74443847987309,
14.5856088522568));
#14238=CARTESIAN_POINT('Ctrl Pts',(1.02969969890823,-1.70843381275609,14.5900481508048));
#14239=CARTESIAN_POINT('Ctrl Pts',(1.08941972289794,-1.67243962307086,14.5944861575079));
#14240=CARTESIAN_POINT('Ctrl Pts',(1.14726879824033,-1.63329913347875,14.598924164211));
#14241=CARTESIAN_POINT('Ctrl Pts',(1.20290441521812,-1.59124119175842,14.603362170914));
#14242=CARTESIAN_POINT('Ctrl Pts',(1.25854274668131,-1.54918119801323,14.6078003941493));
#14243=CARTESIAN_POINT('Ctrl Pts',(1.31196701628196,-1.50420376666524,14.6122386173846));
#14244=CARTESIAN_POINT('Ctrl Pts',(1.36286643617424,-1.45657908801744,14.6166768406199));
#14245=CARTESIAN_POINT('Ctrl Pts',(1.41381977838484,-1.40890395627829,14.6211197656629));
#14246=CARTESIAN_POINT('Ctrl Pts',(1.46224257392157,-1.35857631480648,14.625562690706));
#14247=CARTESIAN_POINT('Ctrl Pts',(1.50786039712126,-1.30590374273654,14.630005615749));
#14248=CARTESIAN_POINT('Ctrl Pts',(1.55350484932201,-1.25320042351825,14.6344511343102));
#14249=CARTESIAN_POINT('Ctrl Pts',(1.59634076943718,-1.19814983568675,14.6388966528715));
#14250=CARTESIAN_POINT('Ctrl Pts',(1.63613534788825,-1.14109100683976,14.6433421714327));
#14251=CARTESIAN_POINT('Ctrl Pts',(1.6759993689896,-1.08393260874362,14.647795447548));
#14252=CARTESIAN_POINT('Ctrl Pts',(1.71281119567868,-1.02475938979194,14.6522487236632));
#14253=CARTESIAN_POINT('Ctrl Pts',(1.7463829026841,-0.963936885751685,14.6567019997785));
#14254=CARTESIAN_POINT('Ctrl Pts',(1.76435958637126,-0.931368183897583,
14.6590866010763));
#14255=CARTESIAN_POINT('Ctrl Pts',(1.78140803983468,-0.898326965747828,
14.6614712023741));
#14256=CARTESIAN_POINT('Ctrl Pts',(1.79750513532895,-0.864871580621115,
14.6638558036719));
#14257=CARTESIAN_POINT('Ctrl Pts',(1.82757183312203,-0.802382484093477,
14.6683098423899));
#14258=CARTESIAN_POINT('Ctrl Pts',(1.85443560269746,-0.738199890156618,
14.6727638811079));
#14259=CARTESIAN_POINT('Ctrl Pts',(1.87790365578977,-0.672685232535569,
14.6772179198259));
#14260=CARTESIAN_POINT('Ctrl Pts',(1.90133643275199,-0.607269053624067,
14.6816652634316));
#14261=CARTESIAN_POINT('Ctrl Pts',(1.92138346023068,-0.540525242221817,
14.6861126070374));
#14262=CARTESIAN_POINT('Ctrl Pts',(1.93789890410999,-0.472837604203937,
14.6905599506432));
#14263=CARTESIAN_POINT('Ctrl Pts',(1.95439487797856,-0.40522976295377,14.695002051288));
#14264=CARTESIAN_POINT('Ctrl Pts',(1.96736742174678,-0.336680778312421,
14.6994441519327));
#14265=CARTESIAN_POINT('Ctrl Pts',(1.97672024875239,-0.267590397197427,
14.7038862525775));
#14266=CARTESIAN_POINT('Ctrl Pts',(1.98606717595331,-0.198543598600828,
14.7083255511255));
#14267=CARTESIAN_POINT('Ctrl Pts',(1.99179885047881,-0.128956565028441,
14.7127648496736));
#14268=CARTESIAN_POINT('Ctrl Pts',(1.99387019594011,-0.0592385367960217,
14.7172041482216));
#14269=CARTESIAN_POINT('Ctrl Pts',(1.99594093863565,0.0104592033475351,
14.7216421549247));
#14270=CARTESIAN_POINT('Ctrl Pts',(1.99435345225302,0.0802873733827579,
14.7260801616277));
#14271=CARTESIAN_POINT('Ctrl Pts',(1.9891147034653,0.14983410478972,14.7305181683308));
#14272=CARTESIAN_POINT('Ctrl Pts',(1.98387569907679,0.219384229411427,14.7349563915661));
#14273=CARTESIAN_POINT('Ctrl Pts',(1.97498511775459,0.288652400145195,14.7393946148014));
#14274=CARTESIAN_POINT('Ctrl Pts',(1.96250185980714,0.357231035540775,14.7438328380367));
#14275=CARTESIAN_POINT('Ctrl Pts',(1.95000537722553,0.425882322432253,14.7482757630798));
#14276=CARTESIAN_POINT('Ctrl Pts',(1.93390870918407,0.493842133362405,14.7527186881228));
#14277=CARTESIAN_POINT('Ctrl Pts',(1.91432187784903,0.560713215903262,14.7571616131658));
#14278=CARTESIAN_POINT('Ctrl Pts',(1.89472361287431,0.627623333847515,14.7616071317271));
#14279=CARTESIAN_POINT('Ctrl Pts',(1.8716312916122,0.693442996346155,14.7660526502883));
#14280=CARTESIAN_POINT('Ctrl Pts',(1.84520390820222,0.757792913436942,14.7704981688496));
#14281=CARTESIAN_POINT('Ctrl Pts',(1.81873040827047,0.822255122929385,14.7749514449648));
#14282=CARTESIAN_POINT('Ctrl Pts',(1.7889104383344,0.885242024887659,14.77940472108));
#14283=CARTESIAN_POINT('Ctrl Pts',(1.75594958037184,0.946397714331535,14.7838579971953));
#14284=CARTESIAN_POINT('Ctrl Pts',(1.73829998878123,0.979144827387656,14.7862425984931));
#14285=CARTESIAN_POINT('Ctrl Pts',(1.71975057072094,1.01136734982018,14.7886271997909));
#14286=CARTESIAN_POINT('Ctrl Pts',(1.70033786218429,1.0430142457908,14.7910118010887));
#14287=CARTESIAN_POINT('Ctrl Pts',(1.66407815054065,1.1021253852871,14.7954658398067));
#14288=CARTESIAN_POINT('Ctrl Pts',(1.62466051492961,1.15946051834799,14.7999198785247));
#14289=CARTESIAN_POINT('Ctrl Pts',(1.58228445562378,1.21466187228849,14.8043739172427));
#14290=CARTESIAN_POINT('Ctrl Pts',(1.53997209411923,1.26978025001712,14.8088212608484));
#14291=CARTESIAN_POINT('Ctrl Pts',(1.49471043073078,1.32277082935464,14.8132686044542));
#14292=CARTESIAN_POINT('Ctrl Pts',(1.44674319681738,1.37330320212349,14.8177159480599));
#14293=CARTESIAN_POINT('Ctrl Pts',(1.39883251134216,1.42377600241912,14.8221580487047));
#14294=CARTESIAN_POINT('Ctrl Pts',(1.34822292568409,1.47179599853222,14.8266001493495));
#14295=CARTESIAN_POINT('Ctrl Pts',(1.29519839933177,1.51706580901041,14.8310422499943));
#14296=CARTESIAN_POINT('Ctrl Pts',(1.24220732108556,1.56230706309162,14.8354815485423));
#14297=CARTESIAN_POINT('Ctrl Pts',(1.18680469559286,1.6048012559041,14.8399208470903));
#14298=CARTESIAN_POINT('Ctrl Pts',(1.12931018983699,1.64428892157988,14.8443601456383));
#14299=CARTESIAN_POINT('Ctrl Pts',(1.07183241509984,1.68376509626423,14.8487981523414));
#14300=CARTESIAN_POINT('Ctrl Pts',(1.01226437189007,1.72023620361864,14.8532361590445));
#14301=CARTESIAN_POINT('Ctrl Pts',(0.950956113603648,1.75348511043004,14.8576741657476));
#14302=CARTESIAN_POINT('Ctrl Pts',(0.88964486406114,1.78673563946979,14.8621123889829));
#14303=CARTESIAN_POINT('Ctrl Pts',(0.826593662360921,1.81676342455656,14.8665506122182));
#14304=CARTESIAN_POINT('Ctrl Pts',(0.762177074998283,1.8433973171422,14.8709888354535));
#14305=CARTESIAN_POINT('Ctrl Pts',(0.697692245370325,1.87005942539773,14.8754317604965));
#14306=CARTESIAN_POINT('Ctrl Pts',(0.631839596301452,1.89332027736661,14.8798746855395));
#14307=CARTESIAN_POINT('Ctrl Pts',(0.565012688063195,1.91305729784228,14.8843176105826));
#14308=CARTESIAN_POINT('Ctrl Pts',(0.49814677020792,1.93280583962921,14.8887631291438));
#14309=CARTESIAN_POINT('Ctrl Pts',(0.430305937505898,1.94902634181036,14.8932086477051));
#14310=CARTESIAN_POINT('Ctrl Pts',(0.36189516215694,1.96164712782585,14.8976541662663));
#14311=CARTESIAN_POINT('Ctrl Pts',(0.293365008095398,1.97428993746523,14.9021074423816));
#14312=CARTESIAN_POINT('Ctrl Pts',(0.224263411437848,1.98332042829676,14.9065607184968));
#14313=CARTESIAN_POINT('Ctrl Pts',(0.155000906492105,1.98871875374238,14.911013994612));
#14314=CARTESIAN_POINT('Ctrl Pts',(0.117912826860775,1.99160940178001,14.9133985959098));
#14315=CARTESIAN_POINT('Ctrl Pts',(0.0807786240323059,1.9934594943657,14.9157831972076));
#14316=CARTESIAN_POINT('Ctrl Pts',(0.0436609877912965,1.99427211800323,
14.9181677985054));
#14317=CARTESIAN_POINT('Ctrl Pts',(-0.0256685848673973,1.99578996383686,
14.9226218372234));
#14318=CARTESIAN_POINT('Ctrl Pts',(-0.0952147042007433,1.99369121041427,
14.9270758759414));
#14319=CARTESIAN_POINT('Ctrl Pts',(-0.164568558321337,1.9879498867205,14.9315299146594));
#14320=CARTESIAN_POINT('Ctrl Pts',(-0.23381816282341,1.98221719312829,14.9359772582651));
#14321=CARTESIAN_POINT('Ctrl Pts',(-0.302875591799381,1.97285283653371,
14.9404246018709));
#14322=CARTESIAN_POINT('Ctrl Pts',(-0.371331093043246,1.95988284900892,
14.9448719454766));
#14323=CARTESIAN_POINT('Ctrl Pts',(-0.439705892287796,1.94692815176621,
14.9493140461214));
#14324=CARTESIAN_POINT('Ctrl Pts',(-0.50747969449479,1.93037635664942,14.9537561467662));
#14325=CARTESIAN_POINT('Ctrl Pts',(-0.574248734939866,1.91030519889361,
14.958198247411));
#14326=CARTESIAN_POINT('Ctrl Pts',(-0.640975657178532,1.89024670211301,
14.962637545959));
#14327=CARTESIAN_POINT('Ctrl Pts',(-0.706698607236841,1.86667338732895,
14.967076844507));
#14328=CARTESIAN_POINT('Ctrl Pts',(-0.771026365742641,1.83971353906789,
14.9715161430551));
#14329=CARTESIAN_POINT('Ctrl Pts',(-0.835335404739012,1.81276153617787,
14.9759541497581));
#14330=CARTESIAN_POINT('Ctrl Pts',(-0.898249606883893,1.78242514529255,
14.9803921564612));
#14331=CARTESIAN_POINT('Ctrl Pts',(-0.959396892739438,1.74888111794425,
14.9848301631642));
#14332=CARTESIAN_POINT('Ctrl Pts',(-1.02054716199727,1.71533545396846,14.9892683863995));
#14333=CARTESIAN_POINT('Ctrl Pts',(-1.07992991574231,1.67858208037216,14.9937066096349));
#14334=CARTESIAN_POINT('Ctrl Pts',(-1.13719846480731,1.63884325490265,14.9981448328702));
#14335=CARTESIAN_POINT('Ctrl Pts',(-1.19452768357992,1.59906233053311,15.0025877579132));
#14336=CARTESIAN_POINT('Ctrl Pts',(-1.24973782419091,1.55628992123207,15.0070306829562));
#14337=CARTESIAN_POINT('Ctrl Pts',(-1.30251275241996,1.51079055208966,15.0114736079993));
#14338=CARTESIAN_POINT('Ctrl Pts',(-1.35531848754674,1.46526462309281,15.0159191265605));
#14339=CARTESIAN_POINT('Ctrl Pts',(-1.40568582728078,1.41700890466694,15.0203646451217));
#14340=CARTESIAN_POINT('Ctrl Pts',(-1.45333525226866,1.36632507369703,15.024810163683));
#14341=CARTESIAN_POINT('Ctrl Pts',(-1.50106782683335,1.31555279802716,15.0292634397982));
#14342=CARTESIAN_POINT('Ctrl Pts',(-1.54607270297582,1.26234432549998,15.0337167159134));
#14343=CARTESIAN_POINT('Ctrl Pts',(-1.58811092639866,1.20703407075078,15.0381699920287));
#14344=CARTESIAN_POINT('Ctrl Pts',(-1.61062118615774,1.17741701987729,15.0405545933265));
#14345=CARTESIAN_POINT('Ctrl Pts',(-1.63228156273777,1.14719782153022,15.0429391946243));
#14346=CARTESIAN_POINT('Ctrl Pts',(-1.65306071014801,1.11643085368731,15.0453237959222));
#14347=CARTESIAN_POINT('Ctrl Pts',(-1.69250007913533,1.05803433849728,15.0498498319821));
#14348=CARTESIAN_POINT('Ctrl Pts',(-1.7289149253273,0.997436794586338,15.054375868042));
#14349=CARTESIAN_POINT('Ctrl Pts',(-1.76205646792578,0.934978377472412,
15.0589019041019));
#14350=CARTESIAN_POINT('Ctrl Pts',(-1.79514361190896,0.8726224797688,15.0634205111143));
#14351=CARTESIAN_POINT('Ctrl Pts',(-1.82496790410304,0.808412185118617,
15.0679391181267));
#14352=CARTESIAN_POINT('Ctrl Pts',(-1.85132377080753,0.742716539564723,
15.0724577251391));
#14353=CARTESIAN_POINT('Ctrl Pts',(-1.8776377558735,0.677125289791475,15.0769691517136));
#14354=CARTESIAN_POINT('Ctrl Pts',(-1.90049410200383,0.610053815379963,
15.081480578288));
#14355=CARTESIAN_POINT('Ctrl Pts',(-1.91973394386375,0.541894036945723,
15.0859920048625));
#14356=CARTESIAN_POINT('Ctrl Pts',(-1.93895579597693,0.473797989656515,
15.0904992131371));
#14357=CARTESIAN_POINT('Ctrl Pts',(-1.95456773249438,0.404616108680934,
15.0950064214117));
#14358=CARTESIAN_POINT('Ctrl Pts',(-1.9664600146909,0.334757484041611,15.0995136296864));
#14359=CARTESIAN_POINT('Ctrl Pts',(-1.97834478141561,0.264943007406439,
15.1040179895761));
#14360=CARTESIAN_POINT('Ctrl Pts',(-1.98651448514305,0.19445309810863,15.1085223494659));
#14361=CARTESIAN_POINT('Ctrl Pts',(-1.99091034060607,0.123707631809064,
15.1130267093556));
#14362=CARTESIAN_POINT('Ctrl Pts',(-1.9934894046851,0.0822010144004573,
15.1156694333688));
#14363=CARTESIAN_POINT('Ctrl Pts',(-1.99477039666107,0.0406066125744606,
15.118312157382));
#14364=CARTESIAN_POINT('Ctrl Pts',(-1.99474975438214,-0.000989895140077555,
15.1209548813952));
#14365=CARTESIAN_POINT('',(-1.99474960167085,-0.00126060858409071,15.9209548813952));
#14366=CARTESIAN_POINT('Ctrl Pts',(-1.99194226862274,-0.00100154882577569,
15.1209557114637));
#14367=CARTESIAN_POINT('Ctrl Pts',(-1.99314834912532,-0.270951609428265,
15.1381304054221));
#14368=CARTESIAN_POINT('Ctrl Pts',(-1.81615384618631,-1.20559135040691,
15.1976904318527));
#14369=CARTESIAN_POINT('Ctrl Pts',(-0.39307670270623,-2.32559105654038,
15.2996357907556));
#14370=CARTESIAN_POINT('Ctrl Pts',(1.74244179285117,-1.58958474294282,15.4267917881723));
#14371=CARTESIAN_POINT('Ctrl Pts',(2.27983395951717,0.604351034998105,15.5539477855891));
#14372=CARTESIAN_POINT('Ctrl Pts',(0.726216434408433,2.24399036247175,15.6811037830058));
#14373=CARTESIAN_POINT('Ctrl Pts',(-1.40931799962854,1.84136068164181,15.8034391074587));
#14374=CARTESIAN_POINT('Ctrl Pts',(-1.99268108475784,0.585369840690117,
15.8833890994392));
#14375=CARTESIAN_POINT('Ctrl Pts',(-1.99701534988654,-0.00124451225460149,
15.9209537589475));
#14376=CARTESIAN_POINT('',(-1.9947492845807,0.00168942735318613,16.7209548813952));
#14377=CARTESIAN_POINT('Ctrl Pts',(-1.99474960167085,-0.00126060858409071,
15.9209548813952));
#14378=CARTESIAN_POINT('Ctrl Pts',(-1.99470208524479,-0.0764491906300473,
15.9257751802099));
#14379=CARTESIAN_POINT('Ctrl Pts',(-1.99040364133295,-0.15150312980269,
15.9305954790246));
#14380=CARTESIAN_POINT('Ctrl Pts',(-1.98189826454668,-0.226068200963442,
15.9354157778393));
#14381=CARTESIAN_POINT('Ctrl Pts',(-1.97403915062585,-0.294967604657519,
15.9398698165573));
#14382=CARTESIAN_POINT('Ctrl Pts',(-1.9625673256446,-0.363593144450402,
15.9443238552752));
#14383=CARTESIAN_POINT('Ctrl Pts',(-1.94751226712666,-0.431536246323711,
15.9487778939932));
#14384=CARTESIAN_POINT('Ctrl Pts',(-1.93247983870082,-0.499377219158404,
15.953225237599));
#14385=CARTESIAN_POINT('Ctrl Pts',(-1.9138749719689,-0.566537315980175,
15.9576725812047));
#14386=CARTESIAN_POINT('Ctrl Pts',(-1.89177879811183,-0.632614054155122,
15.9621199248105));
#14387=CARTESIAN_POINT('Ctrl Pts',(-1.86970867337248,-0.698612894647751,
15.9665620254553));
#14388=CARTESIAN_POINT('Ctrl Pts',(-1.8441555706978,-0.763530451062614,
15.9710041261001));
#14389=CARTESIAN_POINT('Ctrl Pts',(-1.8152510421405,-0.826977155977006,
15.9754462267448));
#14390=CARTESIAN_POINT('Ctrl Pts',(-1.78636474668785,-0.890383838428903,
15.9798855252929));
#14391=CARTESIAN_POINT('Ctrl Pts',(-1.75413142171885,-0.952321065487502,
15.9843248238409));
#14392=CARTESIAN_POINT('Ctrl Pts',(-1.71873101120809,-1.01241852690062,
15.9887641223889));
#14393=CARTESIAN_POINT('Ctrl Pts',(-1.68334090228919,-1.07249849982955,
15.993202129092));
#14394=CARTESIAN_POINT('Ctrl Pts',(-1.64478578575177,-1.13073934831471,
15.997640135795));
#14395=CARTESIAN_POINT('Ctrl Pts',(-1.60329104367608,-1.18679627222539,
16.0020781424981));
#14396=CARTESIAN_POINT('Ctrl Pts',(-1.56179427705422,-1.24285593117729,
16.0065163657334));
#14397=CARTESIAN_POINT('Ctrl Pts',(-1.51735789333274,-1.29673106194095,
16.0109545889687));
#14398=CARTESIAN_POINT('Ctrl Pts',(-1.4702489349152,-1.34810816772273,16.015392812204));
#14399=CARTESIAN_POINT('Ctrl Pts',(-1.42309006975507,-1.39953970187818,
16.0198357372471));
#14400=CARTESIAN_POINT('Ctrl Pts',(-1.37325331028224,-1.44846756744527,
16.0242786622901));
#14401=CARTESIAN_POINT('Ctrl Pts',(-1.3210434525273,-1.49461425091385,16.0287215873331));
#14402=CARTESIAN_POINT('Ctrl Pts',(-1.2688031177294,-1.54078787210099,16.0331671058944));
#14403=CARTESIAN_POINT('Ctrl Pts',(-1.21418731085471,-1.58417677519995,
16.0376126244556));
#14404=CARTESIAN_POINT('Ctrl Pts',(-1.15753269447796,-1.62454474352497,
16.0420581430169));
#14405=CARTESIAN_POINT('Ctrl Pts',(-1.10077921421411,-1.66498315508159,
16.0465114191321));
#14406=CARTESIAN_POINT('Ctrl Pts',(-1.0419802354975,-1.70238984602281,16.0509646952473));
#14407=CARTESIAN_POINT('Ctrl Pts',(-0.981499380362869,-1.73657321436423,
16.0554179713626));
#14408=CARTESIAN_POINT('Ctrl Pts',(-0.949113621673195,-1.7548774251073,
16.0578025726604));
#14409=CARTESIAN_POINT('Ctrl Pts',(-0.916246009917864,-1.77225821794876,
16.0601871739582));
#14410=CARTESIAN_POINT('Ctrl Pts',(-0.882954658215231,-1.78869187789178,
16.062571775256));
#14411=CARTESIAN_POINT('Ctrl Pts',(-0.820771948848264,-1.81938722211212,
16.067025813974));
#14412=CARTESIAN_POINT('Ctrl Pts',(-0.756863528050589,-1.84689687916948,
16.071479852692));
#14413=CARTESIAN_POINT('Ctrl Pts',(-0.691588866982415,-1.87102442569999,
16.07593389141));
#14414=CARTESIAN_POINT('Ctrl Pts',(-0.626412323871697,-1.89511570477932,
16.0803812350157));
#14415=CARTESIAN_POINT('Ctrl Pts',(-0.55987407197145,-1.9158347951379,16.0848285786215));
#14416=CARTESIAN_POINT('Ctrl Pts',(-0.49235642696649,-1.93303199956048,
16.0892759222272));
#14417=CARTESIAN_POINT('Ctrl Pts',(-0.424918378324872,-1.95020893024674,
16.093718022872));
#14418=CARTESIAN_POINT('Ctrl Pts',(-0.356503701891035,-1.96387210102227,
16.0981601235168));
#14419=CARTESIAN_POINT('Ctrl Pts',(-0.287511153246104,-1.97392119884738,
16.1026022241616));
#14420=CARTESIAN_POINT('Ctrl Pts',(-0.218562125406478,-1.98396395765708,
16.1070415227096));
#14421=CARTESIAN_POINT('Ctrl Pts',(-0.149036431812932,-1.99039709566335,
16.1114808212577));
#14422=CARTESIAN_POINT('Ctrl Pts',(-0.0793428373953858,-1.99317141175917,
16.1159201198057));
#14423=CARTESIAN_POINT('Ctrl Pts',(-0.00966952395637401,-1.99594492052333,
16.1203581265088));
#14424=CARTESIAN_POINT('Ctrl Pts',(0.060171104389546,-1.99506170156083,
16.1247961332118));
#14425=CARTESIAN_POINT('Ctrl Pts',(0.129767129810311,-1.99052456767577,
16.1292341399149));
#14426=CARTESIAN_POINT('Ctrl Pts',(0.199366550850822,-1.985987212422,16.1336723631502));
#14427=CARTESIAN_POINT('Ctrl Pts',(0.268720856904589,-1.97779562253691,
16.1381105863855));
#14428=CARTESIAN_POINT('Ctrl Pts',(0.337421893263111,-1.96600458505232,
16.1425488096208));
#14429=CARTESIAN_POINT('Ctrl Pts',(0.406195710787947,-1.95420105626475,
16.1469917346639));
#14430=CARTESIAN_POINT('Ctrl Pts',(0.474314393816407,-1.93879055185456,
16.1514346597069));
#14431=CARTESIAN_POINT('Ctrl Pts',(0.541379600595374,-1.91987908227555,
16.1558775847499));
#14432=CARTESIAN_POINT('Ctrl Pts',(0.608483956096018,-1.90095657329332,
16.1603231033112));
#14433=CARTESIAN_POINT('Ctrl Pts',(0.67453314763782,-1.87852918892982,16.1647686218724));
#14434=CARTESIAN_POINT('Ctrl Pts',(0.739146301158942,-1.85275209026547,
16.1692141404337));
#14435=CARTESIAN_POINT('Ctrl Pts',(0.803872206436622,-1.82693000984439,
16.1736674165489));
#14436=CARTESIAN_POINT('Ctrl Pts',(0.86715662689341,-1.79774675175449,16.1781206926642));
#14437=CARTESIAN_POINT('Ctrl Pts',(0.928641602442285,-1.76540429837288,
16.1825739687794));
#14438=CARTESIAN_POINT('Ctrl Pts',(0.961565038738243,-1.74808584465213,
16.1849585700772));
#14439=CARTESIAN_POINT('Ctrl Pts',(0.993972985444529,-1.72986231995028,
16.187343171375));
#14440=CARTESIAN_POINT('Ctrl Pts',(1.02581404086845,-1.71076974372858,16.1897277726728));
#14441=CARTESIAN_POINT('Ctrl Pts',(1.08528783793931,-1.67510798601822,16.1941818113908));
#14442=CARTESIAN_POINT('Ctrl Pts',(1.14301756517406,-1.63627055467081,16.1986358501087));
#14443=CARTESIAN_POINT('Ctrl Pts',(1.19864345620722,-1.59445333183246,16.2030898888267));
#14444=CARTESIAN_POINT('Ctrl Pts',(1.25418573288342,-1.55269896677728,16.2075372324325));
#14445=CARTESIAN_POINT('Ctrl Pts',(1.30763006179368,-1.50797399189125,16.2119845760382));
#14446=CARTESIAN_POINT('Ctrl Pts',(1.35864359363725,-1.46051879411683,16.216431919644));
#14447=CARTESIAN_POINT('Ctrl Pts',(1.40959698577044,-1.41311954114268,16.2208740202888));
#14448=CARTESIAN_POINT('Ctrl Pts',(1.45812491568086,-1.36299678976376,16.2253161209336));
#14449=CARTESIAN_POINT('Ctrl Pts',(1.5039271534303,-1.31043148606672,16.2297582215784));
#14450=CARTESIAN_POINT('Ctrl Pts',(1.54970049892527,-1.25789934079611,16.2341975201264));
#14451=CARTESIAN_POINT('Ctrl Pts',(1.59275124224513,-1.20292806799045,16.2386368186744));
#14452=CARTESIAN_POINT('Ctrl Pts',(1.63281670701351,-1.14583470177751,16.2430761172224));
#14453=CARTESIAN_POINT('Ctrl Pts',(1.67287051264969,-1.08875794985093,16.2475141239255));
#14454=CARTESIAN_POINT('Ctrl Pts',(1.70994048321272,-1.02956073094718,16.2519521306286));
#14455=CARTESIAN_POINT('Ctrl Pts',(1.74380596639477,-0.968590890967903,
16.2563901373316));
#14456=CARTESIAN_POINT('Ctrl Pts',(1.77767310188819,-0.90761807624412,16.2608283605669));
#14457=CARTESIAN_POINT('Ctrl Pts',(1.80833520396687,-0.844872897870323,
16.2652665838022));
#14458=CARTESIAN_POINT('Ctrl Pts',(1.83561735544561,-0.78072817733631,16.2697048070375));
#14459=CARTESIAN_POINT('Ctrl Pts',(1.86292840935303,-0.71651550254979,16.2741477320806));
#14460=CARTESIAN_POINT('Ctrl Pts',(1.88685217379302,-0.650900777687739,
16.2785906571236));
#14461=CARTESIAN_POINT('Ctrl Pts',(1.90726211090804,-0.584276306891349,
16.2830335821666));
#14462=CARTESIAN_POINT('Ctrl Pts',(1.92768396214346,-0.517612944649016,
16.2874791007279));
#14463=CARTESIAN_POINT('Ctrl Pts',(1.94458778476755,-0.449939138391337,
16.2919246192891));
#14464=CARTESIAN_POINT('Ctrl Pts',(1.95789782189687,-0.381659116898178,
16.2963701378504));
#14465=CARTESIAN_POINT('Ctrl Pts',(1.97123108541253,-0.313259944861491,
16.3008234139656));
#14466=CARTESIAN_POINT('Ctrl Pts',(1.98095797655841,-0.244252930624363,
16.3052766900809));
#14467=CARTESIAN_POINT('Ctrl Pts',(1.98705450970589,-0.175048387474627,
16.3097299661961));
#14468=CARTESIAN_POINT('Ctrl Pts',(1.99031902788971,-0.137991344717777,
16.3121145674939));
#14469=CARTESIAN_POINT('Ctrl Pts',(1.9925435086667,-0.100877687560439,16.3144991687917));
#14470=CARTESIAN_POINT('Ctrl Pts',(1.99373040618451,-0.0637701337254548,
16.3168837700896));
#14471=CARTESIAN_POINT('Ctrl Pts',(1.99594733339302,0.00554060667434544,
16.3213378088076));
#14472=CARTESIAN_POINT('Ctrl Pts',(1.99455002903019,0.0751043545663258,
16.3257918475255));
#14473=CARTESIAN_POINT('Ctrl Pts',(1.98950840071178,0.144512580757758,16.3302458862435));
#14474=CARTESIAN_POINT('Ctrl Pts',(1.98447435074406,0.213816475601102,16.3346932298493));
#14475=CARTESIAN_POINT('Ctrl Pts',(1.97580688443937,0.282964828430934,16.339140573455));
#14476=CARTESIAN_POINT('Ctrl Pts',(1.96352790037351,0.351547645355233,16.3435879170608));
#14477=CARTESIAN_POINT('Ctrl Pts',(1.9512633919677,0.420049610187985,16.3480300177056));
#14478=CARTESIAN_POINT('Ctrl Pts',(1.93539590780862,0.487986883710277,16.3524721183504));
#14479=CARTESIAN_POINT('Ctrl Pts',(1.91599910738696,0.55495493780339,16.3569142189952));
#14480=CARTESIAN_POINT('Ctrl Pts',(1.89661454255294,0.621880748151312,16.3613535175432));
#14481=CARTESIAN_POINT('Ctrl Pts',(1.87370521382342,0.687838082780794,16.3657928160912));
#14482=CARTESIAN_POINT('Ctrl Pts',(1.84739545392445,0.752434448519792,16.3702321146392));
#14483=CARTESIAN_POINT('Ctrl Pts',(1.82109335021942,0.817012016584237,16.3746701213423));
#14484=CARTESIAN_POINT('Ctrl Pts',(1.79139296429455,0.880228948804925,16.3791081280453));
#14485=CARTESIAN_POINT('Ctrl Pts',(1.75846728643509,0.941711402202184,16.3835461347484));
#14486=CARTESIAN_POINT('Ctrl Pts',(1.72554000211776,1.00319685535458,16.3879843579837));
#14487=CARTESIAN_POINT('Ctrl Pts',(1.68938734666912,1.06294723122832,16.392422581219));
#14488=CARTESIAN_POINT('Ctrl Pts',(1.65022807032527,1.12061361691287,16.3968608044543));
#14489=CARTESIAN_POINT('Ctrl Pts',(1.61102730904968,1.17834109376909,16.4013037294974));
#14490=CARTESIAN_POINT('Ctrl Pts',(1.5688138449804,1.23397976804312,16.4057466545404));
#14491=CARTESIAN_POINT('Ctrl Pts',(1.52384900168036,1.28721085396984,16.4101895795834));
#14492=CARTESIAN_POINT('Ctrl Pts',(1.47885791055047,1.34047301307249,16.4146350981447));
#14493=CARTESIAN_POINT('Ctrl Pts',(1.43111257864675,1.39132442951403,16.4190806167059));
#14494=CARTESIAN_POINT('Ctrl Pts',(1.38091184868274,1.43948255587472,16.4235261352672));
#14495=CARTESIAN_POINT('Ctrl Pts',(1.33062351704363,1.48772471951021,16.4279794113824));
#14496=CARTESIAN_POINT('Ctrl Pts',(1.27787160477796,1.53326389141308,16.4324326874976));
#14497=CARTESIAN_POINT('Ctrl Pts',(1.22298809976581,1.57585775701084,16.4368859636129));
#14498=CARTESIAN_POINT('Ctrl Pts',(1.19359956110515,1.59866554717565,16.4392705649107));
#14499=CARTESIAN_POINT('Ctrl Pts',(1.16360033488857,1.62062956977358,16.4416551662085));
#14500=CARTESIAN_POINT('Ctrl Pts',(1.133044480218,1.64171793202959,16.4440397675062));
#14501=CARTESIAN_POINT('Ctrl Pts',(1.075971224454,1.68110748619711,16.4484938062242));
#14502=CARTESIAN_POINT('Ctrl Pts',(1.01672846294902,1.71759532923459,16.4529478449422));
#14503=CARTESIAN_POINT('Ctrl Pts',(0.9556433773219,1.75093497819902,16.4574018836602));
#14504=CARTESIAN_POINT('Ctrl Pts',(0.894650112069388,1.78422451249101,16.461849227266));
#14505=CARTESIAN_POINT('Ctrl Pts',(0.831820445286944,1.81437501237467,16.4662965708717));
#14506=CARTESIAN_POINT('Ctrl Pts',(0.767510938572033,1.84118291369225,16.4707439144775));
#14507=CARTESIAN_POINT('Ctrl Pts',(0.703277246155202,1.86795921124974,16.4751860151223));
#14508=CARTESIAN_POINT('Ctrl Pts',(0.637567628450513,1.89140054927231,16.4796281157671));
#14509=CARTESIAN_POINT('Ctrl Pts',(0.570762075637924,1.91134984121523,16.4840702164118));
#14510=CARTESIAN_POINT('Ctrl Pts',(0.503998664063982,1.93128654905642,16.4885095149599));
#14511=CARTESIAN_POINT('Ctrl Pts',(0.436141156807205,1.94773544090862,16.4929488135079));
#14512=CARTESIAN_POINT('Ctrl Pts',(0.367586860665507,1.96058854999362,16.4973881120559));
#14513=CARTESIAN_POINT('Ctrl Pts',(0.299052513964234,1.97343791879757,16.501826118759));
#14514=CARTESIAN_POINT('Ctrl Pts',(0.229822261833278,1.98269349189533,16.506264125462));
#14515=CARTESIAN_POINT('Ctrl Pts',(0.160304074559982,1.9882983091527,16.5107021321651));
#14516=CARTESIAN_POINT('Ctrl Pts',(0.0907824954646867,1.99390339987149,
16.5151403554004));
#14517=CARTESIAN_POINT('Ctrl Pts',(0.0209734415047426,1.99585734415392,
16.5195785786357));
#14518=CARTESIAN_POINT('Ctrl Pts',(-0.0487113021962039,1.9941551523235,
16.524016801871));
#14519=CARTESIAN_POINT('Ctrl Pts',(-0.118469869192843,1.99245115720868,
16.528459726914));
#14520=CARTESIAN_POINT('Ctrl Pts',(-0.188103372686751,1.98708330709254,
16.5329026519571));
#14521=CARTESIAN_POINT('Ctrl Pts',(-0.257202307474941,1.97809871733682,
16.5373455770001));
#14522=CARTESIAN_POINT('Ctrl Pts',(-0.326341578155567,1.96910888290624,
16.5417910955614));
#14523=CARTESIAN_POINT('Ctrl Pts',(-0.394945177390739,1.95649819518938,
16.5462366141226));
#14524=CARTESIAN_POINT('Ctrl Pts',(-0.462613754326337,1.9403649339256,16.5506821326839));
#14525=CARTESIAN_POINT('Ctrl Pts',(-0.530400414817623,1.92420351967056,
16.5551354087991));
#14526=CARTESIAN_POINT('Ctrl Pts',(-0.59724832641095,1.90450739972527,16.5595886849143));
#14527=CARTESIAN_POINT('Ctrl Pts',(-0.662774019135407,1.88142450341732,
16.5640419610296));
#14528=CARTESIAN_POINT('Ctrl Pts',(-0.697861143281239,1.86906427623425,
16.5664265623274));
#14529=CARTESIAN_POINT('Ctrl Pts',(-0.732569496974778,1.85573378313794,
16.5688111636252));
#14530=CARTESIAN_POINT('Ctrl Pts',(-0.766842997887297,1.8414612075988,16.571195764923));
#14531=CARTESIAN_POINT('Ctrl Pts',(-0.830860198668538,1.81480240970457,
16.575649803641));
#14532=CARTESIAN_POINT('Ctrl Pts',(-0.893612360096667,1.78474856275656,
16.580103842359));
#14533=CARTESIAN_POINT('Ctrl Pts',(-0.954715109778675,1.75144129837694,
16.584557881077));
#14534=CARTESIAN_POINT('Ctrl Pts',(-1.01572601253417,1.71818409999074,16.5890052246827));
#14535=CARTESIAN_POINT('Ctrl Pts',(-1.07509199803898,1.68168342278787,16.5934525682885));
#14536=CARTESIAN_POINT('Ctrl Pts',(-1.13244887152319,1.64212883656729,16.5978999118943));
#14537=CARTESIAN_POINT('Ctrl Pts',(-1.18973812714929,1.60262088113805,16.602342012539));
#14538=CARTESIAN_POINT('Ctrl Pts',(-1.24502257389276,1.56006644381997,16.6067841131838));
#14539=CARTESIAN_POINT('Ctrl Pts',(-1.29796440887436,1.51469995569929,16.6112262138286));
#14540=CARTESIAN_POINT('Ctrl Pts',(-1.35087284791194,1.46936208496028,16.6156655123766));
#14541=CARTESIAN_POINT('Ctrl Pts',(-1.40144123578169,1.42121600015034,16.6201048109247));
#14542=CARTESIAN_POINT('Ctrl Pts',(-1.44936369199552,1.370537285456,16.6245441094727));
#14543=CARTESIAN_POINT('Ctrl Pts',(-1.49727220267658,1.31987331837129,16.6289821161758));
#14544=CARTESIAN_POINT('Ctrl Pts',(-1.54253597402509,1.26667853999219,16.6334201228788));
#14545=CARTESIAN_POINT('Ctrl Pts',(-1.58488623643313,1.21126511551552,16.6378581295819));
#14546=CARTESIAN_POINT('Ctrl Pts',(-1.62723856512853,1.15584898739425,16.6422963528172));
#14547=CARTESIAN_POINT('Ctrl Pts',(-1.66667680728718,1.09821438868407,16.6467345760525));
#14548=CARTESIAN_POINT('Ctrl Pts',(-1.70297382245688,1.03870482935558,16.6511727992878));
#14549=CARTESIAN_POINT('Ctrl Pts',(-1.73930929030848,0.979132226216345,
16.6556157243308));
#14550=CARTESIAN_POINT('Ctrl Pts',(-1.77249663364252,0.917681116656479,
16.6600586493739));
#14551=CARTESIAN_POINT('Ctrl Pts',(-1.80235375408574,0.854721304071116,
16.6645015744169));
#14552=CARTESIAN_POINT('Ctrl Pts',(-1.83222830335912,0.791724739251659,
16.6689470929782));
#14553=CARTESIAN_POINT('Ctrl Pts',(-1.85876857412591,0.727218171366367,
16.6733926115394));
#14554=CARTESIAN_POINT('Ctrl Pts',(-1.88184098253303,0.661590567465335,
16.6778381301007));
#14555=CARTESIAN_POINT('Ctrl Pts',(-1.90495365293689,0.595848441563515,
16.6822914062159));
#14556=CARTESIAN_POINT('Ctrl Pts',(-1.9245862431658,0.528981844325455,16.6867446823311));
#14557=CARTESIAN_POINT('Ctrl Pts',(-1.94065551072978,0.461393271704447,
16.6911979584464));
#14558=CARTESIAN_POINT('Ctrl Pts',(-1.94926014140979,0.4252015346961,16.6935825597442));
#14559=CARTESIAN_POINT('Ctrl Pts',(-1.95684394291397,0.388802938335382,
16.695967161042));
#14560=CARTESIAN_POINT('Ctrl Pts',(-1.96340024706993,0.352259893126834,
16.6983517623397));
#14561=CARTESIAN_POINT('Ctrl Pts',(-1.98210878387135,0.247983628655827,
16.7051562668403));
#14562=CARTESIAN_POINT('Ctrl Pts',(-1.99251386625485,0.142175269986685,
16.7119607713409));
#14563=CARTESIAN_POINT('Ctrl Pts',(-1.99442689448622,0.0359016023326883,
16.7187652758415));
#14564=CARTESIAN_POINT('Ctrl Pts',(-1.99463209077638,0.0245024175287777,
16.7194951443594));
#14565=CARTESIAN_POINT('Ctrl Pts',(-1.99473962231119,0.0130979115153709,
16.7202250128773));
#14566=CARTESIAN_POINT('Ctrl Pts',(-1.9947492845807,0.00168942735318613,
16.7209548813952));
#14567=CARTESIAN_POINT('',(-1.99474912755533,-0.00183980182347288,18.3208813761083));
#14568=CARTESIAN_POINT('Ctrl Pts',(-1.99474925275694,0.00172659365242297,
16.7215926364432));
#14569=CARTESIAN_POINT('Ctrl Pts',(-1.9948994043772,-0.171744930408297,
16.7317021781126));
#14570=CARTESIAN_POINT('Ctrl Pts',(-1.97242273040134,-0.344485109801641,
16.7415934927886));
#14571=CARTESIAN_POINT('Ctrl Pts',(-1.92332842871311,-0.529292035933361,
16.7533687939037));
#14572=CARTESIAN_POINT('Ctrl Pts',(-1.91854507022307,-0.546376323251258,
16.7544681225366));
#14573=CARTESIAN_POINT('Ctrl Pts',(-1.90971083131583,-0.576381289381483,
16.7564191862247));
#14574=CARTESIAN_POINT('Ctrl Pts',(-1.90575503525689,-0.589328924470519,
16.7572678390983));
#14575=CARTESIAN_POINT('Ctrl Pts',(-1.89975133155701,-0.608286722314829,
16.758520745853));
#14576=CARTESIAN_POINT('Ctrl Pts',(-1.89780597949355,-0.614329163383226,
16.7589216349931));
#14577=CARTESIAN_POINT('Ctrl Pts',(-1.89432082183775,-0.624979833699323,
16.7596310405278));
#14578=CARTESIAN_POINT('Ctrl Pts',(-1.89279295214639,-0.629591937845154,
16.7599391615746));
#14579=CARTESIAN_POINT('Ctrl Pts',(-1.88977632663741,-0.638587841829782,
16.7605419778444));
#14580=CARTESIAN_POINT('Ctrl Pts',(-1.88828912784532,-0.642972134324393,
16.7608366199334));
#14581=CARTESIAN_POINT('Ctrl Pts',(-1.88424328583784,-0.654764251324876,
16.7616314115169));
#14582=CARTESIAN_POINT('Ctrl Pts',(-1.88165624629358,-0.662162180222608,
16.7621324994249));
#14583=CARTESIAN_POINT('Ctrl Pts',(-1.87194113812885,-0.689426888809651,
16.76398848772));
#14584=CARTESIAN_POINT('Ctrl Pts',(-1.86454168532692,-0.709194829619769,
16.7653523793483));
#14585=CARTESIAN_POINT('Ctrl Pts',(-1.79906712736228,-0.876000939067973,
16.7770210675995));
#14586=CARTESIAN_POINT('Ctrl Pts',(-1.72402591656126,-1.01574373637432,
16.7879273345357));
#14587=CARTESIAN_POINT('Ctrl Pts',(-1.60084333265233,-1.19143849657189,
16.8028983703572));
#14588=CARTESIAN_POINT('Ctrl Pts',(-1.56642649265493,-1.23633871549537,
16.8068448240526));
#14589=CARTESIAN_POINT('Ctrl Pts',(-1.48724104459771,-1.33102015279967,
16.8153594114098));
#14590=CARTESIAN_POINT('Ctrl Pts',(-1.44177620401722,-1.38013910794963,
16.8199044840105));
#14591=CARTESIAN_POINT('Ctrl Pts',(-1.38713736152488,-1.43351579268262,
16.8249086803122));
#14592=CARTESIAN_POINT('Ctrl Pts',(-1.38030290565556,-1.44009773448856,
16.8255269360352));
#14593=CARTESIAN_POINT('Ctrl Pts',(-1.37121476338787,-1.44872595574021,
16.8263386600464));
#14594=CARTESIAN_POINT('Ctrl Pts',(-1.36900313404944,-1.45081606050871,
16.8265353910736));
#14595=CARTESIAN_POINT('Ctrl Pts',(-1.3649408153359,-1.45463760293236,16.826895260109));
#14596=CARTESIAN_POINT('Ctrl Pts',(-1.36309159758088,-1.45637058539894,
16.8270585156862));
#14597=CARTESIAN_POINT('Ctrl Pts',(-1.35926721863651,-1.45994091243707,
16.8273949793856));
#14598=CARTESIAN_POINT('Ctrl Pts',(-1.35729165717887,-1.46177775223665,
16.8275681458309));
#14599=CARTESIAN_POINT('Ctrl Pts',(-1.35278065399623,-1.4659549686477,16.8279621055132));
#14600=CARTESIAN_POINT('Ctrl Pts',(-1.35024286756976,-1.46829277289816,
16.8281827015492));
#14601=CARTESIAN_POINT('Ctrl Pts',(-1.34363014384941,-1.47435275911044,
16.8287548618229));
#14602=CARTESIAN_POINT('Ctrl Pts',(-1.33954576808004,-1.47806466661737,
16.8291056590812));
#14603=CARTESIAN_POINT('Ctrl Pts',(-1.31385095224521,-1.50122229483311,
16.8312966892293));
#14604=CARTESIAN_POINT('Ctrl Pts',(-1.29183164696232,-1.52021179910685,
16.8331044695181));
#14605=CARTESIAN_POINT('Ctrl Pts',(-1.25845104809376,-1.5477500207383,16.8357567859099));
#14606=CARTESIAN_POINT('Ctrl Pts',(-1.2474019478171,-1.55666874050016,16.83662083217));
#14607=CARTESIAN_POINT('Ctrl Pts',(-1.20548670207555,-1.5897694100824,16.8398508627155));
#14608=CARTESIAN_POINT('Ctrl Pts',(-1.17400376007209,-1.61315852831366,
16.8421810471608));
#14609=CARTESIAN_POINT('Ctrl Pts',(-1.01786649088892,-1.72216122292385,
16.8533871055019));
#14610=CARTESIAN_POINT('Ctrl Pts',(-0.88444612827677,-1.79433771774679,
16.8619525983611));
#14611=CARTESIAN_POINT('Ctrl Pts',(-0.702313560237534,-1.86756966347505,
16.8736804603366));
#14612=CARTESIAN_POINT('Ctrl Pts',(-0.659921588079329,-1.88296676857671,
16.8764088542704));
#14613=CARTESIAN_POINT('Ctrl Pts',(-0.591111789626785,-1.90534988709954,
16.8808604994485));
#14614=CARTESIAN_POINT('Ctrl Pts',(-0.565007894413109,-1.91325306901849,
16.8825543678677));
#14615=CARTESIAN_POINT('Ctrl Pts',(-0.530358470074206,-1.92297255179209,
16.8848127223741));
#14616=CARTESIAN_POINT('Ctrl Pts',(-0.521950570935666,-1.92527170532885,
16.8853614881375));
#14617=CARTESIAN_POINT('Ctrl Pts',(-0.508369856064159,-1.92888987416888,
16.8862492058251));
#14618=CARTESIAN_POINT('Ctrl Pts',(-0.503206279167951,-1.93024337764132,
16.8865870378666));
#14619=CARTESIAN_POINT('Ctrl Pts',(-0.493348682451939,-1.93278505927322,
16.8872325965002));
#14620=CARTESIAN_POINT('Ctrl Pts',(-0.488655640713422,-1.9339769057428,
16.8875402018763));
#14621=CARTESIAN_POINT('Ctrl Pts',(-0.477920263904788,-1.93666169540857,
16.8882444797975));
#14622=CARTESIAN_POINT('Ctrl Pts',(-0.471875210960821,-1.93814346345745,
16.8886415097306));
#14623=CARTESIAN_POINT('Ctrl Pts',(-0.4532823114638,-1.94260882801189,16.8898641116329));
#14624=CARTESIAN_POINT('Ctrl Pts',(-0.440712579907381,-1.94549899035605,
16.8906926763946));
#14625=CARTESIAN_POINT('Ctrl Pts',(-0.322053805326525,-1.97157329820106,
16.8985346764807));
#14626=CARTESIAN_POINT('Ctrl Pts',(-0.214284177716429,-1.98617599770517,
16.9058249880465));
#14627=CARTESIAN_POINT('Ctrl Pts',(0.0105743818970425,-1.99812789040067,
16.9213305372507));
#14628=CARTESIAN_POINT('Ctrl Pts',(0.127338589318617,-1.99409380935541,
16.9295457174404));
#14629=CARTESIAN_POINT('Ctrl Pts',(0.308036457627854,-1.97190877770144,
16.9421124625644));
#14630=CARTESIAN_POINT('Ctrl Pts',(0.372569782670456,-1.96074074657256,
16.9465662921488));
#14631=CARTESIAN_POINT('Ctrl Pts',(0.444197396236631,-1.94467976401054,
16.9513911718664));
#14632=CARTESIAN_POINT('Ctrl Pts',(0.451941174288067,-1.94289471955762,
16.9519112068623));
#14633=CARTESIAN_POINT('Ctrl Pts',(0.465673474099328,-1.93964269581101,
16.9528303252453));
#14634=CARTESIAN_POINT('Ctrl Pts',(0.471666198362962,-1.93819415220633,
16.9532303807111));
#14635=CARTESIAN_POINT('Ctrl Pts',(0.480829461178627,-1.93593421911843,
16.9538403896719));
#14636=CARTESIAN_POINT('Ctrl Pts',(0.484004811672894,-1.93514278908439,
16.9540514628638));
#14637=CARTESIAN_POINT('Ctrl Pts',(0.489534727765527,-1.93375004024472,
16.954418485626));
#14638=CARTESIAN_POINT('Ctrl Pts',(0.491890145365829,-1.93315223222354,
16.9545746362311));
#14639=CARTESIAN_POINT('Ctrl Pts',(0.497215144611382,-1.93179037795604,
16.9549272442797));
#14640=CARTESIAN_POINT('Ctrl Pts',(0.500184053111433,-1.93102379004457,
16.9551235523412));
#14641=CARTESIAN_POINT('Ctrl Pts',(0.508262478038432,-1.92891801695474,
16.9556569597983));
#14642=CARTESIAN_POINT('Ctrl Pts',(0.513368507351877,-1.92756536592288,
16.9559932877992));
#14643=CARTESIAN_POINT('Ctrl Pts',(0.536775865871086,-1.92126485636246,
16.9575316078273));
#14644=CARTESIAN_POINT('Ctrl Pts',(0.555012190995416,-1.91607633193075,
16.958720271562));
#14645=CARTESIAN_POINT('Ctrl Pts',(0.772893989837999,-1.85071361081576,
16.9728345776938));
#14646=CARTESIAN_POINT('Ctrl Pts',(0.962014661774332,-1.75984760028207,
16.9843177136664));
#14647=CARTESIAN_POINT('Ctrl Pts',(1.17498156820318,-1.61275233921025,16.9997125136978));
#14648=CARTESIAN_POINT('Ctrl Pts',(1.21522493314839,-1.58264954477472,17.0027409572631));
#14649=CARTESIAN_POINT('Ctrl Pts',(1.27767310424683,-1.53214997706384,17.0076721875744));
#14650=CARTESIAN_POINT('Ctrl Pts',(1.30062742208306,-1.51271288465045,17.0095381713437));
#14651=CARTESIAN_POINT('Ctrl Pts',(1.32964809270891,-1.48699001827664,17.0119718292607));
#14652=CARTESIAN_POINT('Ctrl Pts',(1.33612557928478,-1.48117244013243,17.0125199621396));
#14653=CARTESIAN_POINT('Ctrl Pts',(1.34651102714585,-1.47172147055319,17.0134069025389));
#14654=CARTESIAN_POINT('Ctrl Pts',(1.35044290581014,-1.46811443367237,17.0137445937677));
#14655=CARTESIAN_POINT('Ctrl Pts',(1.35791552585645,-1.46120376324465,17.0143900471389));
#14656=CARTESIAN_POINT('Ctrl Pts',(1.36145880687509,-1.45790292186587,17.014697688757));
#14657=CARTESIAN_POINT('Ctrl Pts',(1.36953178293895,-1.45032722186913,17.0154022806826));
#14658=CARTESIAN_POINT('Ctrl Pts',(1.37405352866221,-1.44604400136752,17.0157995895204));
#14659=CARTESIAN_POINT('Ctrl Pts',(1.38789307432268,-1.43281097737236,17.0170238909704));
#14660=CARTESIAN_POINT('Ctrl Pts',(1.39714389626438,-1.42379190990298,17.0178538884728));
#14661=CARTESIAN_POINT('Ctrl Pts',(1.48450426569155,-1.33694887347381,17.0258052492516));
#14662=CARTESIAN_POINT('Ctrl Pts',(1.55610872897948,-1.25287804302608,17.0332124779335));
#14663=CARTESIAN_POINT('Ctrl Pts',(1.72069295185624,-1.02363122956328,17.0526580529795));
#14664=CARTESIAN_POINT('Ctrl Pts',(1.80250219960301,-0.871545664910423,
17.0649278097243));
#14665=CARTESIAN_POINT('Ctrl Pts',(1.87045707916498,-0.693374228043355,
17.0775748386209));
#14666=CARTESIAN_POINT('Ctrl Pts',(1.87687755349391,-0.67580190648771,17.0788038610264));
#14667=CARTESIAN_POINT('Ctrl Pts',(1.88470707528509,-0.653400354238045,
17.0803452457166));
#14668=CARTESIAN_POINT('Ctrl Pts',(1.88634611592212,-0.648653308651839,
17.0806704399948));
#14669=CARTESIAN_POINT('Ctrl Pts',(1.88893830440373,-0.641052801666418,
17.0811887589727));
#14670=CARTESIAN_POINT('Ctrl Pts',(1.88990294140914,-0.638203325528641,
17.0813825531489));
#14671=CARTESIAN_POINT('Ctrl Pts',(1.8917253641804,-0.632779638716112,17.0817504047403));
#14672=CARTESIAN_POINT('Ctrl Pts',(1.89258433324488,-0.630205891986746,
17.0819245283432));
#14673=CARTESIAN_POINT('Ctrl Pts',(1.89454643989515,-0.624286599877598,
17.0823240011495));
#14674=CARTESIAN_POINT('Ctrl Pts',(1.89564596778135,-0.620939881958067,
17.0825491356964));
#14675=CARTESIAN_POINT('Ctrl Pts',(1.89911191100711,-0.61029531361799,17.0832629519958));
#14676=CARTESIAN_POINT('Ctrl Pts',(1.90144512903528,-0.602986605325512,
17.0837497182536));
#14677=CARTESIAN_POINT('Ctrl Pts',(1.93860849380738,-0.484212959314738,
17.0916086666477));
#14678=CARTESIAN_POINT('Ctrl Pts',(1.96363218844635,-0.369895265604416,
17.0984454910807));
#14679=CARTESIAN_POINT('Ctrl Pts',(1.9915189556957,-0.15269870485207,17.1111697144121));
#14680=CARTESIAN_POINT('Ctrl Pts',(1.99672509665209,-0.0505228940066942,
17.1170514265565));
#14681=CARTESIAN_POINT('Ctrl Pts',(1.99270943470483,0.104661765903216,17.1262635987637));
#14682=CARTESIAN_POINT('Ctrl Pts',(1.98921912902339,0.157643813186542,17.1294565384666));
#14683=CARTESIAN_POINT('Ctrl Pts',(1.98030894344449,0.24163944795052,17.1346375721887));
#14684=CARTESIAN_POINT('Ctrl Pts',(1.97626092486122,0.272774118786872,17.1365841223805));
#14685=CARTESIAN_POINT('Ctrl Pts',(1.97014267021654,0.312478056773421,17.1391049179435));
#14686=CARTESIAN_POINT('Ctrl Pts',(1.96874797688675,0.321148060098795,17.1396577293189));
#14687=CARTESIAN_POINT('Ctrl Pts',(1.96641112796066,0.335087283356144,17.1405504160252));
#14688=CARTESIAN_POINT('Ctrl Pts',(1.96550492070334,0.340362479445814,17.1408891484088));
#14689=CARTESIAN_POINT('Ctrl Pts',(1.96373909107313,0.350399425856803,17.1415353881304));
#14690=CARTESIAN_POINT('Ctrl Pts',(1.96288335132864,0.355161827690542,17.1418427698532));
#14691=CARTESIAN_POINT('Ctrl Pts',(1.96089217282094,0.366016188404977,17.1425450791558));
#14692=CARTESIAN_POINT('Ctrl Pts',(1.95974566113158,0.37210604113401,17.1429403569519));
#14693=CARTESIAN_POINT('Ctrl Pts',(1.95669444715618,0.387907654978254,17.1439692887114));
#14694=CARTESIAN_POINT('Ctrl Pts',(1.95474583018036,0.397610666165398,17.1446043378246));
#14695=CARTESIAN_POINT('Ctrl Pts',(1.94964671769277,0.422057507515832,17.146212678081));
#14696=CARTESIAN_POINT('Ctrl Pts',(1.94640116564796,0.436780660137741,17.1471889775793));
#14697=CARTESIAN_POINT('Ctrl Pts',(1.9066627737484,0.607804360083217,17.1586211796375));
#14698=CARTESIAN_POINT('Ctrl Pts',(1.85160712706223,0.759157293208993,17.1697041949126));
#14699=CARTESIAN_POINT('Ctrl Pts',(1.74322663116028,0.972860235438245,17.1864225992283));
#14700=CARTESIAN_POINT('Ctrl Pts',(1.70324107813413,1.0412815395203,17.1919458046493));
#14701=CARTESIAN_POINT('Ctrl Pts',(1.64187964560899,1.13324447116701,17.1994676687122));
#14702=CARTESIAN_POINT('Ctrl Pts',(1.62385259757086,1.15892828729962,17.201579440419));
#14703=CARTESIAN_POINT('Ctrl Pts',(1.5945464757368,1.19865455301218,17.2048507223536));
#14704=CARTESIAN_POINT('Ctrl Pts',(1.58367097175322,1.2129870196339,17.2060319681563));
#14705=CARTESIAN_POINT('Ctrl Pts',(1.56955484254393,1.23107664328562,17.207522138583));
#14706=CARTESIAN_POINT('Ctrl Pts',(1.56649251216811,1.23497097779534,17.2078428982823));
#14707=CARTESIAN_POINT('Ctrl Pts',(1.5615567591525,1.24119982649268,17.2083558156659));
#14708=CARTESIAN_POINT('Ctrl Pts',(1.55969255993737,1.24354157152334,17.2085486189048));
#14709=CARTESIAN_POINT('Ctrl Pts',(1.55612570656695,1.24800149574357,17.2089157488679));
#14710=CARTESIAN_POINT('Ctrl Pts',(1.55442401550327,1.25012036545342,17.2090901369908));
#14711=CARTESIAN_POINT('Ctrl Pts',(1.55048800687116,1.25500084515398,17.209491751099));
#14712=CARTESIAN_POINT('Ctrl Pts',(1.54825063974357,1.25775996827669,17.2097187546575));
#14713=CARTESIAN_POINT('Ctrl Pts',(1.54105754683689,1.26658221993967,17.2104445066029));
#14714=CARTESIAN_POINT('Ctrl Pts',(1.53607340755764,1.27262224323984,17.2109412477218));
#14715=CARTESIAN_POINT('Ctrl Pts',(1.47564383043641,1.344981503694,17.2168927474639));
#14716=CARTESIAN_POINT('Ctrl Pts',(1.41597160064059,1.40766775509536,17.2220559096054));
#14717=CARTESIAN_POINT('Ctrl Pts',(1.22623957411825,1.58266429463629,17.2371968185742));
#14718=CARTESIAN_POINT('Ctrl Pts',(1.08558352783285,1.68225970412614,17.2469054006261));
#14719=CARTESIAN_POINT('Ctrl Pts',(0.89557424447002,1.78293490792719,17.2599707501284));
#14720=CARTESIAN_POINT('Ctrl Pts',(0.856584877135238,1.80199112775066,17.2626447013052));
#14721=CARTESIAN_POINT('Ctrl Pts',(0.80809841153772,1.82375982176157,17.2659752072149));
#14722=CARTESIAN_POINT('Ctrl Pts',(0.799160343714983,1.82769408539495,17.2665893522579));
#14723=CARTESIAN_POINT('Ctrl Pts',(0.785078933710558,1.83376925011825,17.2675573561786));
#14724=CARTESIAN_POINT('Ctrl Pts',(0.779954815427775,1.83595454183938,17.2679096989869));
#14725=CARTESIAN_POINT('Ctrl Pts',(0.770836431191546,1.83979821254026,17.2685368881432));
#14726=CARTESIAN_POINT('Ctrl Pts',(0.766845783110801,1.84146512618626,17.2688114422993));
#14727=CARTESIAN_POINT('Ctrl Pts',(0.757619946758024,1.84528361376427,17.2694463416233));
#14728=CARTESIAN_POINT('Ctrl Pts',(0.752380978013727,1.84742590156835,17.2698069986207));
#14729=CARTESIAN_POINT('Ctrl Pts',(0.737953680735875,1.85325387821658,17.2708005710434));
#14730=CARTESIAN_POINT('Ctrl Pts',(0.72874701791864,1.85689346760762,17.2714350337709));
#14731=CARTESIAN_POINT('Ctrl Pts',(0.703863442471546,1.86651691227008,17.2731511598997));
#14732=CARTESIAN_POINT('Ctrl Pts',(0.688137769142466,1.87237162750896,17.2742371022593));
#14733=CARTESIAN_POINT('Ctrl Pts',(0.521498476140861,1.93202909694234,17.2857616622243));
#14734=CARTESIAN_POINT('Ctrl Pts',(0.364729055316256,1.96765077856525,17.2968236595056));
#14735=CARTESIAN_POINT('Ctrl Pts',(0.126474170586867,1.99231828461863,17.3135360253376));
#14736=CARTESIAN_POINT('Ctrl Pts',(0.0471001584396288,1.99577321602486,
17.3190736188889));
#14737=CARTESIAN_POINT('Ctrl Pts',(-0.0636875971098499,1.99398060404727,
17.3266126631736));
#14738=CARTESIAN_POINT('Ctrl Pts',(-0.0950886864389171,1.99273007043515,
17.3287276943776));
#14739=CARTESIAN_POINT('Ctrl Pts',(-0.144422003463991,1.98959648773868,
17.3320034596387));
#14740=CARTESIAN_POINT('Ctrl Pts',(-0.162379633226104,1.98821146003813,
17.3331859978699));
#14741=CARTESIAN_POINT('Ctrl Pts',(-0.185252458312706,1.986135355567,17.3346775565301));
#14742=CARTESIAN_POINT('Ctrl Pts',(-0.190186496529454,1.98566896076926,
17.3349984384976));
#14743=CARTESIAN_POINT('Ctrl Pts',(-0.198098004156083,1.98489135838566,
17.3355115048271));
#14744=CARTESIAN_POINT('Ctrl Pts',(-0.201076560368469,1.98459183234377,
17.3357043353986));
#14745=CARTESIAN_POINT('Ctrl Pts',(-0.206757705118685,1.98400761054813,
17.3360714848802));
#14746=CARTESIAN_POINT('Ctrl Pts',(-0.20946035300823,1.98372410075963,17.3362458653217));
#14747=CARTESIAN_POINT('Ctrl Pts',(-0.215693700460661,1.98305733715093,
17.3366474186275));
#14748=CARTESIAN_POINT('Ctrl Pts',(-0.219223960627447,1.98267017691049,
17.3368743692849));
#14749=CARTESIAN_POINT('Ctrl Pts',(-0.230530440077363,1.98139963862068,
17.3375997817186));
#14750=CARTESIAN_POINT('Ctrl Pts',(-0.238302622397368,1.98047991071433,
17.338096238868));
#14751=CARTESIAN_POINT('Ctrl Pts',(-0.331048132189682,1.96895090834338,
17.3439963553587));
#14752=CARTESIAN_POINT('Ctrl Pts',(-0.415270758554667,1.9529246701269,17.3491139004739));
#14753=CARTESIAN_POINT('Ctrl Pts',(-0.593622913615264,1.90692113303631,
17.3599225081251));
#14754=CARTESIAN_POINT('Ctrl Pts',(-0.687079757781419,1.87527557139098,
17.3655728624317));
#14755=CARTESIAN_POINT('Ctrl Pts',(-0.871734246862315,1.79708349037046,
17.3772962555882));
#14756=CARTESIAN_POINT('Ctrl Pts',(-0.962451576591365,1.75017503768663,
17.3833618547817));
#14757=CARTESIAN_POINT('Ctrl Pts',(-1.0660925151378,1.68608119888674,17.3909134006739));
#14758=CARTESIAN_POINT('Ctrl Pts',(-1.08284870152087,1.67536912495483,17.3921545956018));
#14759=CARTESIAN_POINT('Ctrl Pts',(-1.10562337586787,1.66032508996702,17.3938709641429));
#14760=CARTESIAN_POINT('Ctrl Pts',(-1.1117824178352,1.65620720522415,17.3943381246782));
#14761=CARTESIAN_POINT('Ctrl Pts',(-1.12210303833124,1.64922341256424,17.3951260641116));
#14762=CARTESIAN_POINT('Ctrl Pts',(-1.12627696042839,1.64637580789518,17.3954461494356));
#14763=CARTESIAN_POINT('Ctrl Pts',(-1.13449141994371,1.64072574189826,17.3960789279609));
#14764=CARTESIAN_POINT('Ctrl Pts',(-1.13853250469233,1.63792413655212,17.3963915870803));
#14765=CARTESIAN_POINT('Ctrl Pts',(-1.14739454843415,1.63173161169286,17.3970802748918));
#14766=CARTESIAN_POINT('Ctrl Pts',(-1.1522109069493,1.6283342184722,17.3974565497375));
#14767=CARTESIAN_POINT('Ctrl Pts',(-1.16891808618526,1.61643796432891,17.3987687715272));
#14768=CARTESIAN_POINT('Ctrl Pts',(-1.18073027044309,1.60782996435622,17.3997089146109));
#14769=CARTESIAN_POINT('Ctrl Pts',(-1.19992253414018,1.59351825975766,17.4012572071185));
#14770=CARTESIAN_POINT('Ctrl Pts',(-1.20735923560672,1.58789111824626,17.4018623476765));
#14771=CARTESIAN_POINT('Ctrl Pts',(-1.34300538959531,1.48374769037878,17.4129967260343));
#14772=CARTESIAN_POINT('Ctrl Pts',(-1.45878229483117,1.37007450571178,17.4241665843122));
#14773=CARTESIAN_POINT('Ctrl Pts',(-1.60840435151322,1.18245579487212,17.4409099962785));
#14774=CARTESIAN_POINT('Ctrl Pts',(-1.65360603875303,1.11837141116755,17.4463739566062));
#14775=CARTESIAN_POINT('Ctrl Pts',(-1.71136239424292,1.02529918178006,17.4538250631175));
#14776=CARTESIAN_POINT('Ctrl Pts',(-1.72717976129861,0.998423736011658,
17.4559233984122));
#14777=CARTESIAN_POINT('Ctrl Pts',(-1.75108121923019,0.95554324262941,17.4591761890734));
#14778=CARTESIAN_POINT('Ctrl Pts',(-1.75959030918713,0.939782061866815,
17.4603520982517));
#14779=CARTESIAN_POINT('Ctrl Pts',(-1.77017730692112,0.919523969635986,
17.4618365347741));
#14780=CARTESIAN_POINT('Ctrl Pts',(-1.77245201322734,0.915131624824078,
17.4621567882204));
#14781=CARTESIAN_POINT('Ctrl Pts',(-1.77607615253173,0.90806938687654,17.4626690888841));
#14782=CARTESIAN_POINT('Ctrl Pts',(-1.77743594036857,0.905404875815389,
17.4628617789466));
#14783=CARTESIAN_POINT('Ctrl Pts',(-1.78001985731118,0.90031342232702,17.46322882833));
#14784=CARTESIAN_POINT('Ctrl Pts',(-1.78124500473685,0.897887066407594,
17.4634032484988));
#14785=CARTESIAN_POINT('Ctrl Pts',(-1.78406138964187,0.89228087701745,17.4638051154565));
#14786=CARTESIAN_POINT('Ctrl Pts',(-1.78564908670546,0.889099288678411,
17.4640323389037));
#14787=CARTESIAN_POINT('Ctrl Pts',(-1.79071443365552,0.878880534899564,
17.4647595031237));
#14788=CARTESIAN_POINT('Ctrl Pts',(-1.79415911046175,0.871826971808802,
17.4652574256228));
#14789=CARTESIAN_POINT('Ctrl Pts',(-1.83693772413718,0.782903076458022,
17.471486767677));
#14790=CARTESIAN_POINT('Ctrl Pts',(-1.87068274842977,0.698446964221641,
17.4768960059342));
#14791=CARTESIAN_POINT('Ctrl Pts',(-1.93624957873512,0.495035771416332,
17.4894088522375));
#14792=CARTESIAN_POINT('Ctrl Pts',(-1.96305815659874,0.374867614614655,
17.496423188457));
#14793=CARTESIAN_POINT('Ctrl Pts',(-1.98936136456924,0.169154535858712,
17.5086988579682));
#14794=CARTESIAN_POINT('Ctrl Pts',(-1.99474073223447,0.0847263743773186,
17.513807208732));
#14795=CARTESIAN_POINT('Ctrl Pts',(-1.99475112954771,-0.0102038292329521,
17.5197422069454));
#14796=CARTESIAN_POINT('Ctrl Pts',(-1.99467058830128,-0.0206258223393189,
17.5203962915775));
#14797=CARTESIAN_POINT('Ctrl Pts',(-1.99441052937542,-0.0373326610394684,
17.521449022418));
#14798=CARTESIAN_POINT('Ctrl Pts',(-1.99428296315399,-0.0436182148692334,
17.5218460427155));
#14799=CARTESIAN_POINT('Ctrl Pts',(-1.99400396827773,-0.0547668596103046,
17.5225519711169));
#14800=CARTESIAN_POINT('Ctrl Pts',(-1.99386445644917,-0.0596302191894833,
17.5228605036146));
#14801=CARTESIAN_POINT('Ctrl Pts',(-1.99353720496559,-0.0697467245359906,
17.523503537274));
#14802=CARTESIAN_POINT('Ctrl Pts',(-1.99334649089587,-0.0749997301784337,
17.5238381292959));
#14803=CARTESIAN_POINT('Ctrl Pts',(-1.99279910222661,-0.088594670650877,
17.5247058961218));
#14804=CARTESIAN_POINT('Ctrl Pts',(-1.99241081308839,-0.096935163261249,
17.5252400576319));
#14805=CARTESIAN_POINT('Ctrl Pts',(-1.99053186766449,-0.132488514316083,
17.5275248470496));
#14806=CARTESIAN_POINT('Ctrl Pts',(-1.98853601645113,-0.159670634361929,
17.5292912172278));
#14807=CARTESIAN_POINT('Ctrl Pts',(-1.98188607586114,-0.230369328634577,
17.5339389009797));
#14808=CARTESIAN_POINT('Ctrl Pts',(-1.97635593077795,-0.273786778155299,
17.5368464111109));
#14809=CARTESIAN_POINT('Ctrl Pts',(-1.94137661118417,-0.491110768626978,
17.5516684061906));
#14810=CARTESIAN_POINT('Ctrl Pts',(-1.89037955059374,-0.660744432216657,
17.5642028836821));
#14811=CARTESIAN_POINT('Ctrl Pts',(-1.79409452485747,-0.873818014964737,
17.580231626911));
#14812=CARTESIAN_POINT('Ctrl Pts',(-1.76816224768061,-0.92516850869737,
17.5841092770111));
#14813=CARTESIAN_POINT('Ctrl Pts',(-1.73679189510264,-0.981134921331046,
17.5882967221517));
#14814=CARTESIAN_POINT('Ctrl Pts',(-1.7335100010753,-0.986921932040363,
17.5887292261407));
#14815=CARTESIAN_POINT('Ctrl Pts',(-1.72850362256902,-0.995647727566108,
17.5893805068171));
#14816=CARTESIAN_POINT('Ctrl Pts',(-1.72680050019734,-0.998598619857602,
17.5896006076347));
#14817=CARTESIAN_POINT('Ctrl Pts',(-1.7238256822776,-1.00372253067246,17.5899825094721));
#14818=CARTESIAN_POINT('Ctrl Pts',(-1.72255742440441,-1.00589752025858,
17.5901445305578));
#14819=CARTESIAN_POINT('Ctrl Pts',(-1.71987736205356,-1.01047374085955,
17.5904852309469));
#14820=CARTESIAN_POINT('Ctrl Pts',(-1.71846464118588,-1.01287442391382,
17.59066384791));
#14821=CARTESIAN_POINT('Ctrl Pts',(-1.71501104082833,-1.0187152161917,17.5910981585293));
#14822=CARTESIAN_POINT('Ctrl Pts',(-1.71296481972022,-1.02215218482433,
17.5913535055847));
#14823=CARTESIAN_POINT('Ctrl Pts',(-1.70565533308627,-1.03434608903644,
17.5922587464883));
#14824=CARTESIAN_POINT('Ctrl Pts',(-1.70033503249705,-1.04306890234821,
17.5929050231705));
#14825=CARTESIAN_POINT('Ctrl Pts',(-1.66843616127588,-1.09447549839847,
17.5967085247111));
#14826=CARTESIAN_POINT('Ctrl Pts',(-1.64031599907426,-1.13618669424728,
17.5997733019453));
#14827=CARTESIAN_POINT('Ctrl Pts',(-1.55172863609338,-1.25743386831411,
17.6087578006898));
#14828=CARTESIAN_POINT('Ctrl Pts',(-1.48683394121714,-1.33354003546741,
17.6145054875879));
#14829=CARTESIAN_POINT('Ctrl Pts',(-1.31605458674032,-1.50578331778779,
17.6285860865113));
#14830=CARTESIAN_POINT('Ctrl Pts',(-1.20503863752363,-1.59601271191814,
17.6369558075612));
#14831=CARTESIAN_POINT('Ctrl Pts',(-1.07456229653539,-1.68062756600788,
17.6466635514261));
#14832=CARTESIAN_POINT('Ctrl Pts',(-1.06369866054543,-1.68752430855239,
17.6474705974339));
#14833=CARTESIAN_POINT('Ctrl Pts',(-1.04748760312937,-1.69759711053858,
17.648673415891));
#14834=CARTESIAN_POINT('Ctrl Pts',(-1.04219068212773,-1.70085414103689,
17.6490662014147));
#14835=CARTESIAN_POINT('Ctrl Pts',(-1.03274280632244,-1.70660285267582,
17.6497664233492));
#14836=CARTESIAN_POINT('Ctrl Pts',(-1.02859782792752,-1.70910430005826,
17.6500734988373));
#14837=CARTESIAN_POINT('Ctrl Pts',(-1.01986088364867,-1.71433365130621,
17.6507205199001));
#14838=CARTESIAN_POINT('Ctrl Pts',(-1.0152669918736,-1.71705824720494,17.6510605829325));
#14839=CARTESIAN_POINT('Ctrl Pts',(-1.00313538206474,-1.72418768917835,
17.6519582871014));
#14840=CARTESIAN_POINT('Ctrl Pts',(-0.995579657592115,-1.72856151861411,
17.6525170466032));
#14841=CARTESIAN_POINT('Ctrl Pts',(-0.961174407214186,-1.7481774907725,
17.6550600433646));
#14842=CARTESIAN_POINT('Ctrl Pts',(-0.934003178637936,-1.76284391394069,
17.6570647823076));
#14843=CARTESIAN_POINT('Ctrl Pts',(-0.860300077091477,-1.80044487332619,
17.6624967453241));
#14844=CARTESIAN_POINT('Ctrl Pts',(-0.813198285158574,-1.82220353790668,
17.6659624833597));
#14845=CARTESIAN_POINT('Ctrl Pts',(-0.671797713720952,-1.88094876611135,
17.6763452783997));
#14846=CARTESIAN_POINT('Ctrl Pts',(-0.575475070755421,-1.91261746519453,
17.6833990402685));
#14847=CARTESIAN_POINT('Ctrl Pts',(-0.415910801236494,-1.9519289927508,
17.6948642796277));
#14848=CARTESIAN_POINT('Ctrl Pts',(-0.353963276914826,-1.96410773646576,
17.6992610176573));
#14849=CARTESIAN_POINT('Ctrl Pts',(-0.235304746832726,-1.98163839802535,
17.7074804977728));
#14850=CARTESIAN_POINT('Ctrl Pts',(-0.178733139937995,-1.98753991260297,
17.7113130376734));
#14851=CARTESIAN_POINT('Ctrl Pts',(-0.114628371203731,-1.99146733977011,
17.7155046723049));
#14852=CARTESIAN_POINT('Ctrl Pts',(-0.107273008347744,-1.99187708823847,
17.715983369167));
#14853=CARTESIAN_POINT('Ctrl Pts',(-0.0964549146075904,-1.99241963879861,
17.7166839521736));
#14854=CARTESIAN_POINT('Ctrl Pts',(-0.0929939444592117,-1.99258417497532,
17.7169075632708));
#14855=CARTESIAN_POINT('Ctrl Pts',(-0.0868296987374572,-1.99286113062781,
17.7173048800954));
#14856=CARTESIAN_POINT('Ctrl Pts',(-0.0841266077297025,-1.9929770688,17.7174787815254));
#14857=CARTESIAN_POINT('Ctrl Pts',(-0.0783853087056505,-1.99321161704227,
17.7178474446986));
#14858=CARTESIAN_POINT('Ctrl Pts',(-0.0753470721161254,-1.99332878019652,
17.7180421241848));
#14859=CARTESIAN_POINT('Ctrl Pts',(-0.0671458204932518,-1.99362626642608,
17.7185665446482));
#14860=CARTESIAN_POINT('Ctrl Pts',(-0.0619823089349076,-1.99379348133345,
17.7188955576537));
#14861=CARTESIAN_POINT('Ctrl Pts',(-0.0365014481755044,-1.99451956866293,
17.720513690727));
#14862=CARTESIAN_POINT('Ctrl Pts',(-0.0161761367286923,-1.99478797769539,
17.7217872461601));
#14863=CARTESIAN_POINT('Ctrl Pts',(0.0414048321838454,-1.99466816312559,
17.7253554920779));
#14864=CARTESIAN_POINT('Ctrl Pts',(0.0786519580405387,-1.99354700656881,
17.7276166428052));
#14865=CARTESIAN_POINT('Ctrl Pts',(0.214982634216695,-1.98561601142922,
17.7357905447983));
#14866=CARTESIAN_POINT('Ctrl Pts',(0.313554358590365,-1.97245396449799,
17.7415075736065));
#14867=CARTESIAN_POINT('Ctrl Pts',(0.551441419672148,-1.92239774847684,
17.7556177643597));
#14868=CARTESIAN_POINT('Ctrl Pts',(0.68850604270232,-1.87767188310536,17.7640476713814));
#14869=CARTESIAN_POINT('Ctrl Pts',(0.831279855749553,-1.81333021871249,
17.7738237125587));
#14870=CARTESIAN_POINT('Ctrl Pts',(0.84294350953833,-1.80793775005939,17.7746296383553));
#14871=CARTESIAN_POINT('Ctrl Pts',(0.860169522359573,-1.7997707012786,17.7758311054142));
#14872=CARTESIAN_POINT('Ctrl Pts',(0.865772483585711,-1.79708213213058,
17.7762236696229));
#14873=CARTESIAN_POINT('Ctrl Pts',(0.875717318770753,-1.79225282092793,
17.7769236428986));
#14874=CARTESIAN_POINT('Ctrl Pts',(0.880064155110382,-1.79012236417851,
17.7772306919798));
#14875=CARTESIAN_POINT('Ctrl Pts',(0.889192297766664,-1.78560722656828,
17.7778778069346));
#14876=CARTESIAN_POINT('Ctrl Pts',(0.893971857424668,-1.78321911923274,
17.7782179908361));
#14877=CARTESIAN_POINT('Ctrl Pts',(0.906543280636337,-1.77687456208028,
17.7791163556581));
#14878=CARTESIAN_POINT('Ctrl Pts',(0.914318771834836,-1.77288609574165,
17.7796756579206));
#14879=CARTESIAN_POINT('Ctrl Pts',(0.9495207173819,-1.75453596017913,17.7822246746493));
#14880=CARTESIAN_POINT('Ctrl Pts',(0.976635479038798,-1.73958874169027,
17.7842350098196));
#14881=CARTESIAN_POINT('Ctrl Pts',(1.04838971400838,-1.69782727066911,17.7896858557162));
#14882=CARTESIAN_POINT('Ctrl Pts',(1.09234295313662,-1.66988757639833,17.7931652104746));
#14883=CARTESIAN_POINT('Ctrl Pts',(1.21854033942849,-1.58255219291744,17.8035735862334));
#14884=CARTESIAN_POINT('Ctrl Pts',(1.29740169037872,-1.51857089226017,17.8106392277323));
#14885=CARTESIAN_POINT('Ctrl Pts',(1.45758196066959,-1.36699489872244,17.8260246992894));
#14886=CARTESIAN_POINT('Ctrl Pts',(1.53661544819668,-1.27751332608872,17.8343191784467));
#14887=CARTESIAN_POINT('Ctrl Pts',(1.611717276486,-1.17535239138241,17.8425984509952));
#14888=CARTESIAN_POINT('Ctrl Pts',(1.61620302575589,-1.16917646544714,17.843094622018));
#14889=CARTESIAN_POINT('Ctrl Pts',(1.62270281643937,-1.16011873950325,17.8438158271586));
#14890=CARTESIAN_POINT('Ctrl Pts',(1.62474479742218,-1.15725721598166,17.8440427324922));
#14891=CARTESIAN_POINT('Ctrl Pts',(1.62834884940332,-1.15217834710361,17.8444437818181));
#14892=CARTESIAN_POINT('Ctrl Pts',(1.62991397407453,-1.14996319782766,17.8446181350349));
#14893=CARTESIAN_POINT('Ctrl Pts',(1.63320775995145,-1.14528120938414,17.8449854551085));
#14894=CARTESIAN_POINT('Ctrl Pts',(1.63493534860058,-1.14281365144335,17.8451783485868));
#14895=CARTESIAN_POINT('Ctrl Pts',(1.6395381995543,-1.13620748526903,17.8456929347163));
#14896=CARTESIAN_POINT('Ctrl Pts',(1.64240340316338,-1.13206184459615,17.8460139456953));
#14897=CARTESIAN_POINT('Ctrl Pts',(1.65593668933284,-1.11232111135646,17.8475337048314));
#14898=CARTESIAN_POINT('Ctrl Pts',(1.66639898381683,-1.09658518305492,17.8487190755787));
#14899=CARTESIAN_POINT('Ctrl Pts',(1.69484032405585,-1.05246036571681,17.8519782565764));
#14900=CARTESIAN_POINT('Ctrl Pts',(1.71232872503927,-1.02376127829014,17.854025130412));
#14901=CARTESIAN_POINT('Ctrl Pts',(1.77317573400123,-0.917983873852684,
17.8613598709024));
#14902=CARTESIAN_POINT('Ctrl Pts',(1.81212444557359,-0.838482987201785,
17.8664821872471));
#14903=CARTESIAN_POINT('Ctrl Pts',(1.90162104155844,-0.620178429027883,
17.8801656359342));
#14904=CARTESIAN_POINT('Ctrl Pts',(1.94225469961493,-0.477936660902421,
17.8887286315749));
#14905=CARTESIAN_POINT('Ctrl Pts',(1.96915135884961,-0.318846230820188,
17.8987097158277));
#14906=CARTESIAN_POINT('Ctrl Pts',(1.97132101712113,-0.305144925284576,
17.8995720979636));
#14907=CARTESIAN_POINT('Ctrl Pts',(1.97492179246937,-0.280762509787471,
17.9011122847096));
#14908=CARTESIAN_POINT('Ctrl Pts',(1.97640960494237,-0.270090243249286,
17.9017883000064));
#14909=CARTESIAN_POINT('Ctrl Pts',(1.97864189725565,-0.253070430387111,
17.9028695768465));
#14910=CARTESIAN_POINT('Ctrl Pts',(1.9794424798818,-0.24673035404821,17.9032730676696));
#14911=CARTESIAN_POINT('Ctrl Pts',(1.98080088518131,-0.235540332380596,
17.9039864979108));
#14912=CARTESIAN_POINT('Ctrl Pts',(1.98137139752668,-0.230691957558923,
17.9042960345878));
#14913=CARTESIAN_POINT('Ctrl Pts',(1.98251421188178,-0.220662930169388,
17.9049372190628));
#14914=CARTESIAN_POINT('Ctrl Pts',(1.98308401747772,-0.21548203600036,17.905268943024));
#14915=CARTESIAN_POINT('Ctrl Pts',(1.98449261329214,-0.202195535615407,
17.9061209517925));
#14916=CARTESIAN_POINT('Ctrl Pts',(1.98530204484354,-0.194086976139843,
17.906642156468));
#14917=CARTESIAN_POINT('Ctrl Pts',(1.98844004289059,-0.160575489641808,
17.9088014811636));
#14918=CARTESIAN_POINT('Ctrl Pts',(1.99033081098259,-0.13513494905966,17.9104532723644));
#14919=CARTESIAN_POINT('Ctrl Pts',(2.00178117421162,0.0728242028844208,
17.9240642447832));
#14920=CARTESIAN_POINT('Ctrl Pts',(1.98669830232853,0.255798641183532,17.9368416232503));
#14921=CARTESIAN_POINT('Ctrl Pts',(1.92596965389718,0.528160805176158,17.956257947305));
#14922=CARTESIAN_POINT('Ctrl Pts',(1.89820864899906,0.62058175034428,17.9628942795221));
#14923=CARTESIAN_POINT('Ctrl Pts',(1.86107220839135,0.717982935641215,17.9697034669122));
#14924=CARTESIAN_POINT('Ctrl Pts',(1.85823049033752,0.725305942665645,17.9702142075742));
#14925=CARTESIAN_POINT('Ctrl Pts',(1.85403927112303,0.73592023589072,17.9709525509397));
#14926=CARTESIAN_POINT('Ctrl Pts',(1.85272415162696,0.739224885213897,17.9711821510295));
#14927=CARTESIAN_POINT('Ctrl Pts',(1.85038834141296,0.745048949678202,17.9715862858542));
#14928=CARTESIAN_POINT('Ctrl Pts',(1.84937133110063,0.747569817153153,17.9717610408681));
#14929=CARTESIAN_POINT('Ctrl Pts',(1.84722447603255,0.752860042249826,17.9721274134368));
#14930=CARTESIAN_POINT('Ctrl Pts',(1.84609355743296,0.755628933778719,17.972318964466));
#14931=CARTESIAN_POINT('Ctrl Pts',(1.8430766590256,0.76296817505723,17.972826166518));
#14932=CARTESIAN_POINT('Ctrl Pts',(1.84117989257265,0.767534111061243,17.9731411698098));
#14933=CARTESIAN_POINT('Ctrl Pts',(1.83234257732728,0.788586205315364,17.9745912615566));
#14934=CARTESIAN_POINT('Ctrl Pts',(1.82519718194176,0.804986226480913,17.9757144150661));
#14935=CARTESIAN_POINT('Ctrl Pts',(1.8050171960147,0.84965240281804,17.9787613756287));
#14936=CARTESIAN_POINT('Ctrl Pts',(1.79153971137327,0.877714058296531,17.9806623213574));
#14937=CARTESIAN_POINT('Ctrl Pts',(1.74195088544175,0.975057538678526,17.9872486740085));
#14938=CARTESIAN_POINT('Ctrl Pts',(1.70243057531053,1.04252670875458,17.9918012209703));
#14939=CARTESIAN_POINT('Ctrl Pts',(1.56910509468137,1.24224892322164,18.0057420815429));
#14940=CARTESIAN_POINT('Ctrl Pts',(1.46309232466983,1.36551339394418,18.0150752526007));
#14941=CARTESIAN_POINT('Ctrl Pts',(1.33791686616869,1.47954722867949,18.0255538278731));
#14942=CARTESIAN_POINT('Ctrl Pts',(1.33245834169282,1.48446499053168,18.0260096848435));
#14943=CARTESIAN_POINT('Ctrl Pts',(1.31529664735945,1.4997555970717,18.0274396952075));
#14944=CARTESIAN_POINT('Ctrl Pts',(1.30349880461244,1.51002084948233,18.0284181356453));
#14945=CARTESIAN_POINT('Ctrl Pts',(1.28683674490259,1.52417765464905,18.0297941819199));
#14946=CARTESIAN_POINT('Ctrl Pts',(1.28207293965561,1.52818693455425,18.0301869514299));
#14947=CARTESIAN_POINT('Ctrl Pts',(1.27379388902218,1.53508873155506,18.0308684641422));
#14948=CARTESIAN_POINT('Ctrl Pts',(1.27028734913369,1.53799165652066,18.0311567810533));
#14949=CARTESIAN_POINT('Ctrl Pts',(1.26298564499185,1.54399444149703,18.0317564733145));
#14950=CARTESIAN_POINT('Ctrl Pts',(1.25918893733225,1.54709236770938,18.0320679241215));
#14951=CARTESIAN_POINT('Ctrl Pts',(1.25024065340345,1.55433896599792,18.032801113714));
#14952=CARTESIAN_POINT('Ctrl Pts',(1.24507980499479,1.55847604732731,18.0332233143362));
#14953=CARTESIAN_POINT('Ctrl Pts',(1.22842982330269,1.57168765297546,18.0345833789358));
#14954=CARTESIAN_POINT('Ctrl Pts',(1.21686154192868,1.58066121546026,18.0355252424823));
#14955=CARTESIAN_POINT('Ctrl Pts',(1.1894555371009,1.60144100016847,18.037749812225));
#14956=CARTESIAN_POINT('Ctrl Pts',(1.17353937596763,1.61314073730684,18.0390365497288));
#14957=CARTESIAN_POINT('Ctrl Pts',(1.11701216261136,1.65341372340212,18.0435894678087));
#14958=CARTESIAN_POINT('Ctrl Pts',(1.07551319030384,1.68070336478576,18.0469022662731));
#14959=CARTESIAN_POINT('Ctrl Pts',(0.890261898015245,1.79285218579264,18.0615596729402));
#14960=CARTESIAN_POINT('Ctrl Pts',(0.737220681768395,1.86101584780977,18.0734089144645));
#14961=CARTESIAN_POINT('Ctrl Pts',(0.522176223435725,1.92605801477154,18.0888128446357));
#14962=CARTESIAN_POINT('Ctrl Pts',(0.466151833800666,1.94037918660384,18.092711294495));
#14963=CARTESIAN_POINT('Ctrl Pts',(0.403060921556072,1.95361557407042,18.0969187568469));
#14964=CARTESIAN_POINT('Ctrl Pts',(0.396535932593443,1.95495042774208,18.0973517391718));
#14965=CARTESIAN_POINT('Ctrl Pts',(0.386661123960933,1.95691909862524,18.0980036164436));
#14966=CARTESIAN_POINT('Ctrl Pts',(0.383316244449521,1.95757703309735,18.0982238388772));
#14967=CARTESIAN_POINT('Ctrl Pts',(0.377497576830527,1.95870607373735,18.0986058925785));
#14968=CARTESIAN_POINT('Ctrl Pts',(0.375024566086652,1.95918107351359,18.0987679443388));
#14969=CARTESIAN_POINT('Ctrl Pts',(0.369814652292523,1.96017153373276,18.0991086441019));
#14970=CARTESIAN_POINT('Ctrl Pts',(0.367077560252191,1.96068594721808,18.0992872299656));
#14971=CARTESIAN_POINT('Ctrl Pts',(0.360409201347693,1.96192475633389,18.099721351188));
#14972=CARTESIAN_POINT('Ctrl Pts',(0.356476789919736,1.96264307525741,18.0999765406657));
#14973=CARTESIAN_POINT('Ctrl Pts',(0.34299298172454,1.96506424952078,18.1008488415164));
#14974=CARTESIAN_POINT('Ctrl Pts',(0.333431145975211,1.96670927446056,18.1014627547518));
#14975=CARTESIAN_POINT('Ctrl Pts',(0.209129848934509,1.98716155256814,18.10938743277));
#14976=CARTESIAN_POINT('Ctrl Pts',(0.0929525732555075,1.99597458098033,
18.116182060956));
#14977=CARTESIAN_POINT('Ctrl Pts',(-0.138400077857139,1.99326674061518,
18.1296202051874));
#14978=CARTESIAN_POINT('Ctrl Pts',(-0.253115249334878,1.98196814987794,
18.136244703859));
#14979=CARTESIAN_POINT('Ctrl Pts',(-0.384207628065902,1.95748489703089,
18.1442271810741));
#14980=CARTESIAN_POINT('Ctrl Pts',(-0.402153684666894,1.9538769178248,18.1453286872309));
#14981=CARTESIAN_POINT('Ctrl Pts',(-0.466371061604144,1.9400440887738,18.1493057247579));
#14982=CARTESIAN_POINT('Ctrl Pts',(-0.512321428374567,1.92841884129845,
18.1522183436847));
#14983=CARTESIAN_POINT('Ctrl Pts',(-0.566958277114803,1.91250532861324,
18.1557805492576));
#14984=CARTESIAN_POINT('Ctrl Pts',(-0.576085549471598,1.90977583883887,
18.1563789722728));
#14985=CARTESIAN_POINT('Ctrl Pts',(-0.591008859065501,1.90519634237726,
18.1573630471616));
#14986=CARTESIAN_POINT('Ctrl Pts',(-0.596816674890876,1.90338499251752,
18.1577474332588));
#14987=CARTESIAN_POINT('Ctrl Pts',(-0.607216636834413,1.90008915827409,
18.1584383104895));
#14988=CARTESIAN_POINT('Ctrl Pts',(-0.611811872166747,1.89861451744267,
18.1587444761764));
#14989=CARTESIAN_POINT('Ctrl Pts',(-0.621554167508126,1.89544911041258,
18.1593955086079));
#14990=CARTESIAN_POINT('Ctrl Pts',(-0.626699772984551,1.89375402491891,
18.1597405156441));
#14991=CARTESIAN_POINT('Ctrl Pts',(-0.639904040936078,1.88934451355837,
18.1606288385329));
#14992=CARTESIAN_POINT('Ctrl Pts',(-0.647952302676579,1.88659950234825,
18.1611731614578));
#14993=CARTESIAN_POINT('Ctrl Pts',(-0.685028985473981,1.87368856672921,
18.1636942353336));
#14994=CARTESIAN_POINT('Ctrl Pts',(-0.713836044586039,1.86290404524583,
18.1656914112461));
#14995=CARTESIAN_POINT('Ctrl Pts',(-0.790477493450411,1.83217305166076,
18.1711122870743));
#14996=CARTESIAN_POINT('Ctrl Pts',(-0.837800420342886,1.8110224837659,18.1745745543083));
#14997=CARTESIAN_POINT('Ctrl Pts',(-0.980441267375064,1.74048261193429,
18.1853645608122));
#14998=CARTESIAN_POINT('Ctrl Pts',(-1.07263587421954,1.68522795846736,18.1928532071582));
#14999=CARTESIAN_POINT('Ctrl Pts',(-1.1742396242555,1.61260603314266,18.2015635994442));
#15000=CARTESIAN_POINT('Ctrl Pts',(-1.18841287730972,1.60218967471311,18.2027894499162));
#15001=CARTESIAN_POINT('Ctrl Pts',(-1.27876441131116,1.53392894978689,18.2106674030049));
#15002=CARTESIAN_POINT('Ctrl Pts',(-1.3508467609082,1.47084813557862,18.2172524367816));
#15003=CARTESIAN_POINT('Ctrl Pts',(-1.42365569877746,1.39724504897519,18.2240152465508));
#15004=CARTESIAN_POINT('Ctrl Pts',(-1.4291474241504,1.39162743597586,18.2245260491834));
#15005=CARTESIAN_POINT('Ctrl Pts',(-1.43707727433885,1.38341935842972,18.2252644653367));
#15006=CARTESIAN_POINT('Ctrl Pts',(-1.43954179741868,1.38085467289842,18.2254940767887));
#15007=CARTESIAN_POINT('Ctrl Pts',(-1.44387768747441,1.37631834079527,18.2258982246797));
#15008=CARTESIAN_POINT('Ctrl Pts',(-1.44575189999769,1.37434944450483,18.2260729814441));
#15009=CARTESIAN_POINT('Ctrl Pts',(-1.44967978616557,1.37020619803607,18.226439350284));
#15010=CARTESIAN_POINT('Ctrl Pts',(-1.4517325915474,1.3680310634198,18.2266308958619));
#15011=CARTESIAN_POINT('Ctrl Pts',(-1.45590621420345,1.36358875606364,18.2270205021071));
#15012=CARTESIAN_POINT('Ctrl Pts',(-1.4580266473514,1.36132123179924,18.2272185333485));
#15013=CARTESIAN_POINT('Ctrl Pts',(-1.46705017737417,1.35162648512567,18.2280616889004));
#15014=CARTESIAN_POINT('Ctrl Pts',(-1.4739020388927,1.34415146777639,18.2287030051971));
#15015=CARTESIAN_POINT('Ctrl Pts',(-1.55687066987215,1.2522397910728,18.2364867635286));
#15016=CARTESIAN_POINT('Ctrl Pts',(-1.62570380758713,1.16148429945965,18.2431385889086));
#15017=CARTESIAN_POINT('Ctrl Pts',(-1.71020089168383,1.02772587400507,18.2523307904085));
#15018=CARTESIAN_POINT('Ctrl Pts',(-1.73270026685849,0.989321661939559,
18.2549055760555));
#15019=CARTESIAN_POINT('Ctrl Pts',(-1.77380303863056,0.913453192944326,
18.2599207781885));
#15020=CARTESIAN_POINT('Ctrl Pts',(-1.79254955189127,0.876093548689596,
18.2623585408199));
#15021=CARTESIAN_POINT('Ctrl Pts',(-1.84921892711085,0.753711122927371,
18.2703029728698));
#15022=CARTESIAN_POINT('Ctrl Pts',(-1.88236494324017,0.66662571498682,18.2759001242718));
#15023=CARTESIAN_POINT('Ctrl Pts',(-1.91296499328664,0.565466124660871,
18.2824994027861));
#15024=CARTESIAN_POINT('Ctrl Pts',(-1.91650605563652,0.553345760534934,
18.2832914942293));
#15025=CARTESIAN_POINT('Ctrl Pts',(-1.92160590407678,0.53525357473922,18.2844762595219));
#15026=CARTESIAN_POINT('Ctrl Pts',(-1.92325248021467,0.529306655740876,
18.2848660769413));
#15027=CARTESIAN_POINT('Ctrl Pts',(-1.92614010744719,0.518686062869001,
18.2855629745102));
#15028=CARTESIAN_POINT('Ctrl Pts',(-1.92739181273776,0.514015315771662,
18.2858697062904));
#15029=CARTESIAN_POINT('Ctrl Pts',(-1.92999688028532,0.50415117514907,18.2865180372963));
#15030=CARTESIAN_POINT('Ctrl Pts',(-1.93134628943714,0.498956786369663,
18.2868597617611));
#15031=CARTESIAN_POINT('Ctrl Pts',(-1.93404534686989,0.488392076524176,
18.2875554548888));
#15032=CARTESIAN_POINT('Ctrl Pts',(-1.93539362779187,0.483021457741381,
18.2879094644375));
#15033=CARTESIAN_POINT('Ctrl Pts',(-1.93868125589117,0.469691036640193,
18.2887890514043));
#15034=CARTESIAN_POINT('Ctrl Pts',(-1.94059394643289,0.461724824523402,
18.2893154828785));
#15035=CARTESIAN_POINT('Ctrl Pts',(-1.9495551985194,0.423362377373257,18.2918545668947));
#15036=CARTESIAN_POINT('Ctrl Pts',(-1.95593864292376,0.392816772766463,
18.2938883596265));
#15037=CARTESIAN_POINT('Ctrl Pts',(-1.98377043023989,0.24205848726371,18.3039906943939));
#15038=CARTESIAN_POINT('Ctrl Pts',(-1.99486174487414,0.120222297344481,
18.3123781448069));
#15039=CARTESIAN_POINT('Ctrl Pts',(-1.99474915136337,-0.00184000954739135,
18.3208813519367));
#15040=CARTESIAN_POINT('',(-1.99474949800079,0.00141517687806603,19.9197876209294));
#15041=CARTESIAN_POINT('Ctrl Pts',(-1.99474915155247,-0.00183980452437414,
18.3208813376543));
#15042=CARTESIAN_POINT('Ctrl Pts',(-1.99462759758103,-0.133630806333513,
18.3300622732238));
#15043=CARTESIAN_POINT('Ctrl Pts',(-1.98144557580629,-0.265099424167756,
18.3393350990873));
#15044=CARTESIAN_POINT('Ctrl Pts',(-1.95303027127133,-0.406008020399977,
18.3488600952125));
#15045=CARTESIAN_POINT('Ctrl Pts',(-1.95056824805384,-0.417676045126906,
18.3496454702622));
#15046=CARTESIAN_POINT('Ctrl Pts',(-1.94671783721713,-0.435146879524617,
18.3508156982726));
#15047=CARTESIAN_POINT('Ctrl Pts',(-1.94540785890408,-0.440966449010872,
18.3512045451171));
#15048=CARTESIAN_POINT('Ctrl Pts',(-1.94325116638932,-0.450350852338331,
18.3518299391367));
#15049=CARTESIAN_POINT('Ctrl Pts',(-1.94242071351959,-0.453919329925472,
18.3520673643239));
#15050=CARTESIAN_POINT('Ctrl Pts',(-1.9408036719361,-0.460782096193919,
18.3525232041302));
#15051=CARTESIAN_POINT('Ctrl Pts',(-1.94001851664671,-0.464076705576403,
18.3527416981309));
#15052=CARTESIAN_POINT('Ctrl Pts',(-1.93865430829428,-0.469737126002959,
18.3531164837775));
#15053=CARTESIAN_POINT('Ctrl Pts',(-1.93807931141267,-0.472103884254078,
18.3532730076802));
#15054=CARTESIAN_POINT('Ctrl Pts',(-1.93686976583747,-0.47704307193831,
18.3535992715911));
#15055=CARTESIAN_POINT('Ctrl Pts',(-1.93623442909215,-0.479615281344062,
18.3537689648504));
#15056=CARTESIAN_POINT('Ctrl Pts',(-1.93445094247747,-0.486774560627539,
18.3542406900202));
#15057=CARTESIAN_POINT('Ctrl Pts',(-1.93329159467776,-0.491358863541545,
18.3545420801177));
#15058=CARTESIAN_POINT('Ctrl Pts',(-1.92856563578903,-0.509770602602811,
18.3557500056353));
#15059=CARTESIAN_POINT('Ctrl Pts',(-1.92486678470205,-0.52356410110425,
18.3566491905607));
#15060=CARTESIAN_POINT('Ctrl Pts',(-1.88703482460906,-0.658821185222753,
18.3654205065383));
#15061=CARTESIAN_POINT('Ctrl Pts',(-1.84159328818003,-0.776845797463386,
18.3727194278233));
#15062=CARTESIAN_POINT('Ctrl Pts',(-1.75721826554491,-0.946136273270623,
18.3836897187713));
#15063=CARTESIAN_POINT('Ctrl Pts',(-1.7264890648432,-1.00111192242871,18.3873370462227));
#15064=CARTESIAN_POINT('Ctrl Pts',(-1.64525246181721,-1.13154859111573,
18.3963680846301));
#15065=CARTESIAN_POINT('Ctrl Pts',(-1.59210033830179,-1.20518517772239,
18.4018008303851));
#15066=CARTESIAN_POINT('Ctrl Pts',(-1.52279642022826,-1.28857785250226,
18.4085335397413));
#15067=CARTESIAN_POINT('Ctrl Pts',(-1.51128508331362,-1.30205959328525,
18.409641298453));
#15068=CARTESIAN_POINT('Ctrl Pts',(-1.49598190657535,-1.31950586718404,
18.4111011997342));
#15069=CARTESIAN_POINT('Ctrl Pts',(-1.49235100202034,-1.32361100181805,
18.4114466649023));
#15070=CARTESIAN_POINT('Ctrl Pts',(-1.48515745364468,-1.33167686767978,
18.4121293305835));
#15071=CARTESIAN_POINT('Ctrl Pts',(-1.48159576788444,-1.33563839482039,
18.4124664894086));
#15072=CARTESIAN_POINT('Ctrl Pts',(-1.47476481091289,-1.34317526255086,
18.4131115479566));
#15073=CARTESIAN_POINT('Ctrl Pts',(-1.4714982951989,-1.34675305827823,18.4134193297798));
#15074=CARTESIAN_POINT('Ctrl Pts',(-1.4639913983891,-1.35491540207385,18.4141251243271));
#15075=CARTESIAN_POINT('Ctrl Pts',(-1.45974247347117,-1.35949199005081,
18.4145234999533));
#15076=CARTESIAN_POINT('Ctrl Pts',(-1.44657950290927,-1.37353719239036,
18.4157543144724));
#15077=CARTESIAN_POINT('Ctrl Pts',(-1.43759444168374,-1.38293849647789,
18.4165898048474));
#15078=CARTESIAN_POINT('Ctrl Pts',(-1.34398372145361,-1.4789877113255,18.4252481752068));
#15079=CARTESIAN_POINT('Ctrl Pts',(-1.25174145564546,-1.55782877832362,
18.4334193699797));
#15080=CARTESIAN_POINT('Ctrl Pts',(-1.06112453288347,-1.69283801173296,
18.449576828833));
#15081=CARTESIAN_POINT('Ctrl Pts',(-0.963977295391744,-1.74998090385539,
18.4575021479227));
#15082=CARTESIAN_POINT('Ctrl Pts',(-0.823116780739672,-1.81753050532631,
18.4682428726371));
#15083=CARTESIAN_POINT('Ctrl Pts',(-0.78308818477667,-1.835132640282,18.4712149245023));
#15084=CARTESIAN_POINT('Ctrl Pts',(-0.728556700565041,-1.85700262098791,
18.4751292543194));
#15085=CARTESIAN_POINT('Ctrl Pts',(-0.714539233750911,-1.86244122441266,
18.4761237397397));
#15086=CARTESIAN_POINT('Ctrl Pts',(-0.690829082602297,-1.87133336609236,
18.4777846921561));
#15087=CARTESIAN_POINT('Ctrl Pts',(-0.681168963118902,-1.87487126039451,
18.4784555409911));
#15088=CARTESIAN_POINT('Ctrl Pts',(-0.668558285060478,-1.87937942424264,
18.479323280405));
#15089=CARTESIAN_POINT('Ctrl Pts',(-0.665632450961819,-1.88041767736137,
18.4795240478167));
#15090=CARTESIAN_POINT('Ctrl Pts',(-0.659883170213068,-1.88244275068446,
18.4799174437997));
#15091=CARTESIAN_POINT('Ctrl Pts',(-0.657059905421901,-1.88343005946907,
18.4801101006658));
#15092=CARTESIAN_POINT('Ctrl Pts',(-0.651666465467604,-1.88530256708706,
18.4804771264877));
#15093=CARTESIAN_POINT('Ctrl Pts',(-0.649096732927811,-1.88618885137734,
18.4806515561297));
#15094=CARTESIAN_POINT('Ctrl Pts',(-0.643160428001201,-1.88822267665594,
18.4810534975855));
#15095=CARTESIAN_POINT('Ctrl Pts',(-0.6397925933529,-1.88936646809299,18.4812807857879));
#15096=CARTESIAN_POINT('Ctrl Pts',(-0.628977134240288,-1.89300740337191,
18.4820083662368));
#15097=CARTESIAN_POINT('Ctrl Pts',(-0.621517696367855,-1.89546960477566,
18.4825066369598));
#15098=CARTESIAN_POINT('Ctrl Pts',(-0.525387535355053,-1.92657161611299,
18.4888847514072));
#15099=CARTESIAN_POINT('Ctrl Pts',(-0.434816930272576,-1.94901243781041,
18.4944253753076));
#15100=CARTESIAN_POINT('Ctrl Pts',(-0.21027536994351,-1.98820614528123,
18.5077581318166));
#15101=CARTESIAN_POINT('Ctrl Pts',(-0.0755524049126808,-1.99786659074581,
18.5154384625263));
#15102=CARTESIAN_POINT('Ctrl Pts',(0.126662429618491,-1.99187116151396,
18.5275039937355));
#15103=CARTESIAN_POINT('Ctrl Pts',(0.194056969051639,-1.98643764084671,
18.531610241012));
#15104=CARTESIAN_POINT('Ctrl Pts',(0.27405178554565,-1.9758783894734,18.5366447093487));
#15105=CARTESIAN_POINT('Ctrl Pts',(0.287044998068462,-1.97403266111248,
18.5374674574447));
#15106=CARTESIAN_POINT('Ctrl Pts',(0.306314494665547,-1.97110109986061,
18.5386954565545));
#15107=CARTESIAN_POINT('Ctrl Pts',(0.312605496657503,-1.97011317376604,
18.5390976094803));
#15108=CARTESIAN_POINT('Ctrl Pts',(0.323690580442947,-1.96831796335097,
18.5398084599857));
#15109=CARTESIAN_POINT('Ctrl Pts',(0.32848666697723,-1.96752324145114,18.5401167568242));
#15110=CARTESIAN_POINT('Ctrl Pts',(0.337837774769023,-1.9659385983518,18.5407193173927));
#15111=CARTESIAN_POINT('Ctrl Pts',(0.342393052775504,-1.96515035846332,
18.5410135258707));
#15112=CARTESIAN_POINT('Ctrl Pts',(0.354629517970881,-1.962989137315,18.541805679774));
#15113=CARTESIAN_POINT('Ctrl Pts',(0.362305396317866,-1.96158692011463,
18.5423045524556));
#15114=CARTESIAN_POINT('Ctrl Pts',(0.390477979158265,-1.9562693970089,18.5441428810597));
#15115=CARTESIAN_POINT('Ctrl Pts',(0.410920524660765,-1.95207768115321,
18.5454911058565));
#15116=CARTESIAN_POINT('Ctrl Pts',(0.591873008594086,-1.9120053452765,18.557556942262));
#15117=CARTESIAN_POINT('Ctrl Pts',(0.74740747747759,-1.85672787215594,18.5689313871662));
#15118=CARTESIAN_POINT('Ctrl Pts',(0.992589544051896,-1.73374452907766,
18.5880687800573));
#15119=CARTESIAN_POINT('Ctrl Pts',(1.08658917675904,-1.67643465144908,18.5957244228537));
#15120=CARTESIAN_POINT('Ctrl Pts',(1.18371060915936,-1.6056035139274,18.6036647499401));
#15121=CARTESIAN_POINT('Ctrl Pts',(1.19197776249049,-1.59947568730832,18.6043408114044));
#15122=CARTESIAN_POINT('Ctrl Pts',(1.20629689338689,-1.58868929738754,18.6055115501763));
#15123=CARTESIAN_POINT('Ctrl Pts',(1.21237014618414,-1.58405950388187,18.6060080275575));
#15124=CARTESIAN_POINT('Ctrl Pts',(1.2212638923656,-1.57719846496799,18.6067347807355));
#15125=CARTESIAN_POINT('Ctrl Pts',(1.2241050889327,-1.57499435695499,18.6069669047436));
#15126=CARTESIAN_POINT('Ctrl Pts',(1.22908104566906,-1.5711125730376,18.6073733357633));
#15127=CARTESIAN_POINT('Ctrl Pts',(1.23121835793159,-1.56943820822291,18.6075478755051));
#15128=CARTESIAN_POINT('Ctrl Pts',(1.23541540319,-1.56613640364816,18.6078905462941));
#15129=CARTESIAN_POINT('Ctrl Pts',(1.23747533378436,-1.56450926866605,18.60805869767));
#15130=CARTESIAN_POINT('Ctrl Pts',(1.24314126960825,-1.56001556612682,18.608521133273));
#15131=CARTESIAN_POINT('Ctrl Pts',(1.24674059525025,-1.5571405434131,18.6088148174071));
#15132=CARTESIAN_POINT('Ctrl Pts',(1.26075063719846,-1.5458700650061,18.6099577813468));
#15133=CARTESIAN_POINT('Ctrl Pts',(1.27108706906765,-1.53738222737988,18.6108006682163));
#15134=CARTESIAN_POINT('Ctrl Pts',(1.2834878210131,-1.52698868578518,18.6118125219571));
#15135=CARTESIAN_POINT('Ctrl Pts',(1.28563416903998,-1.52518202743319,18.6119876788632));
#15136=CARTESIAN_POINT('Ctrl Pts',(1.44891520787254,-1.38715291824462,18.6253149467192));
#15137=CARTESIAN_POINT('Ctrl Pts',(1.58744669100734,-1.22621130523688,18.6369208906312));
#15138=CARTESIAN_POINT('Ctrl Pts',(1.72509991501907,-1.00284082721485,18.6525133566531));
#15139=CARTESIAN_POINT('Ctrl Pts',(1.75031802548324,-0.95814698539679,18.65560332213));
#15140=CARTESIAN_POINT('Ctrl Pts',(1.78779610785187,-0.885297004582001,
18.6606316618557));
#15141=CARTESIAN_POINT('Ctrl Pts',(1.80117815393882,-0.857742856546517,
18.6625315733318));
#15142=CARTESIAN_POINT('Ctrl Pts',(1.81754202782522,-0.821975872103614,
18.6649999306644));
#15143=CARTESIAN_POINT('Ctrl Pts',(1.82111215065194,-0.81403555702936,18.6655480360842));
#15144=CARTESIAN_POINT('Ctrl Pts',(1.82678626980328,-0.80119158540571,18.6664349427594));
#15145=CARTESIAN_POINT('Ctrl Pts',(1.82892279605632,-0.79630235289724,18.6667726278791));
#15146=CARTESIAN_POINT('Ctrl Pts',(1.83296093642385,-0.786959477264073,
18.6674180766912));
#15147=CARTESIAN_POINT('Ctrl Pts',(1.83486600175896,-0.782507359851042,
18.6677257198896));
#15148=CARTESIAN_POINT('Ctrl Pts',(1.83918425599522,-0.772313168227375,
18.6684303254765));
#15149=CARTESIAN_POINT('Ctrl Pts',(1.84158679087301,-0.76656666216677,18.6688276464452));
#15150=CARTESIAN_POINT('Ctrl Pts',(1.84889038619227,-0.748865039447626,
18.6700520218467));
#15151=CARTESIAN_POINT('Ctrl Pts',(1.85370215796984,-0.736873668913815,
18.6708820816968));
#15152=CARTESIAN_POINT('Ctrl Pts',(1.89849001249891,-0.622042807307998,
18.6788383052211));
#15153=CARTESIAN_POINT('Ctrl Pts',(1.9299783331343,-0.51611797389255,18.6862507378249));
#15154=CARTESIAN_POINT('Ctrl Pts',(1.98774285460882,-0.239778097251125,
18.7057040007797));
#15155=CARTESIAN_POINT('Ctrl Pts',(2.00101247593706,-0.0675661981849562,
18.7179758740718));
#15156=CARTESIAN_POINT('Ctrl Pts',(1.99105329750384,0.122804526027687,18.7306176191976));
#15157=CARTESIAN_POINT('Ctrl Pts',(1.98982035192278,0.14138321626499,18.7318407105203));
#15158=CARTESIAN_POINT('Ctrl Pts',(1.98792540381359,0.164940256753106,18.7333757488135));
#15159=CARTESIAN_POINT('Ctrl Pts',(1.98750455287962,0.169936320523003,18.7337004019351));
#15160=CARTESIAN_POINT('Ctrl Pts',(1.98680121171316,0.177925676545154,18.7342180618197));
#15161=CARTESIAN_POINT('Ctrl Pts',(1.98653078677484,0.180919967745124,18.7344117351217));
#15162=CARTESIAN_POINT('Ctrl Pts',(1.98600337900854,0.186615931642054,18.734779497184));
#15163=CARTESIAN_POINT('Ctrl Pts',(1.98574765564003,0.18931765785895,18.7349536515509));
#15164=CARTESIAN_POINT('Ctrl Pts',(1.98514697628989,0.195528716707812,18.7353533787729));
#15165=CARTESIAN_POINT('Ctrl Pts',(1.98479822826952,0.199037659892524,18.735578736046));
#15166=CARTESIAN_POINT('Ctrl Pts',(1.98365926390856,0.210196656186417,18.7362939683203));
#15167=CARTESIAN_POINT('Ctrl Pts',(1.98283409777959,0.217843188690037,18.7367819170554));
#15168=CARTESIAN_POINT('Ctrl Pts',(1.96891227422089,0.340213078106433,18.7445589595946));
#15169=CARTESIAN_POINT('Ctrl Pts',(1.9459204166028,0.453610810322624,18.7513247974727));
#15170=CARTESIAN_POINT('Ctrl Pts',(1.88420965684906,0.662803283733112,18.7640012259607));
#15171=CARTESIAN_POINT('Ctrl Pts',(1.84763235638712,0.758820121710295,18.7699058932705));
#15172=CARTESIAN_POINT('Ctrl Pts',(1.78093284945403,0.900101642474769,18.7791732225278));
#15173=CARTESIAN_POINT('Ctrl Pts',(1.75608743554031,0.947660815068347,18.7823985816048));
#15174=CARTESIAN_POINT('Ctrl Pts',(1.7135919535303,1.02158249716475,18.7876275879875));
#15175=CARTESIAN_POINT('Ctrl Pts',(1.69717732333449,1.04862631083313,18.7895886939736));
#15176=CARTESIAN_POINT('Ctrl Pts',(1.67538117404773,1.08268324384145,18.7921258388849));
#15177=CARTESIAN_POINT('Ctrl Pts',(1.67058603883131,1.09006759776965,18.7926800964343));
#15178=CARTESIAN_POINT('Ctrl Pts',(1.66279470007617,1.10189384803548,18.7935745595206));
#15179=CARTESIAN_POINT('Ctrl Pts',(1.6598291765474,1.10635589694647,18.7939136138198));
#15180=CARTESIAN_POINT('Ctrl Pts',(1.65415187629761,1.11482399261759,18.794560100361));
#15181=CARTESIAN_POINT('Ctrl Pts',(1.65144342823373,1.11883223364406,18.7948674054245));
#15182=CARTESIAN_POINT('Ctrl Pts',(1.64523763387576,1.12794457922984,18.7955690268544));
#15183=CARTESIAN_POINT('Ctrl Pts',(1.64173107923765,1.13304232391135,18.7959636909271));
#15184=CARTESIAN_POINT('Ctrl Pts',(1.6309484016413,1.14856277504649,18.7971719297165));
#15185=CARTESIAN_POINT('Ctrl Pts',(1.62359643371152,1.15893215722208,18.7979883959766));
#15186=CARTESIAN_POINT('Ctrl Pts',(1.60895909472359,1.17916433516313,18.7995999503035));
#15187=CARTESIAN_POINT('Ctrl Pts',(1.60168088446205,1.18903163582935,18.8003947378128));
#15188=CARTESIAN_POINT('Ctrl Pts',(1.49754442605915,1.3275215751273,18.811676579866));
#15189=CARTESIAN_POINT('Ctrl Pts',(1.38556985143681,1.44399741018749,18.8227969336188));
#15190=CARTESIAN_POINT('Ctrl Pts',(1.19977304147385,1.59555153108657,18.839526078278));
#15191=CARTESIAN_POINT('Ctrl Pts',(1.13579364657578,1.64171072887518,18.8450237703146));
#15192=CARTESIAN_POINT('Ctrl Pts',(1.04283352101743,1.70073655021552,18.8525151666493));
#15193=CARTESIAN_POINT('Ctrl Pts',(1.01602681260715,1.7168856432162,18.8546211553225));
#15194=CARTESIAN_POINT('Ctrl Pts',(0.973255789743627,1.74129926494946,18.8578844805762));
#15195=CARTESIAN_POINT('Ctrl Pts',(0.957541666725978,1.74998970693847,18.8590634312595));
#15196=CARTESIAN_POINT('Ctrl Pts',(0.93734735555561,1.76080436376682,18.8605511360423));
#15197=CARTESIAN_POINT('Ctrl Pts',(0.932974290446479,1.76312536340153,18.8608716782923));
#15198=CARTESIAN_POINT('Ctrl Pts',(0.925944194897727,1.76682309947044,18.8613843307796));
#15199=CARTESIAN_POINT('Ctrl Pts',(0.923292664123198,1.76821016102545,18.8615770854072));
#15200=CARTESIAN_POINT('Ctrl Pts',(0.918226926846699,1.77084563416485,18.8619441807123));
#15201=CARTESIAN_POINT('Ctrl Pts',(0.915813319758448,1.77209506309847,18.8621185825521));
#15202=CARTESIAN_POINT('Ctrl Pts',(0.910237862333229,1.77496682373411,18.8625203050492));
#15203=CARTESIAN_POINT('Ctrl Pts',(0.90707422588605,1.77658564122103,18.8627474028874));
#15204=CARTESIAN_POINT('Ctrl Pts',(0.89691846924848,1.78174809341721,18.8634737601523));
#15205=CARTESIAN_POINT('Ctrl Pts',(0.889909672188349,1.78525902577176,18.8639710075975));
#15206=CARTESIAN_POINT('Ctrl Pts',(0.80465094407919,1.82734100733099,18.8699732100781));
#15207=CARTESIAN_POINT('Ctrl Pts',(0.723961451506604,1.86078540840954,18.8751811442561));
#15208=CARTESIAN_POINT('Ctrl Pts',(0.474923381145423,1.9453429548555,18.8906032763594));
#15209=CARTESIAN_POINT('Ctrl Pts',(0.301791225474709,1.97960416794822,18.900540973221));
#15210=CARTESIAN_POINT('Ctrl Pts',(0.0874065022654165,1.993217241716,18.9136362010896));
#15211=CARTESIAN_POINT('Ctrl Pts',(0.0483421880211279,1.99454696076952,
18.9160498261827));
#15212=CARTESIAN_POINT('Ctrl Pts',(-0.000184182018821294,1.99477237698326,
18.9190919929695));
#15213=CARTESIAN_POINT('Ctrl Pts',(-0.00963439826761239,1.99474911789121,
18.9196864903936));
#15214=CARTESIAN_POINT('Ctrl Pts',(-0.024584807190945,1.99460607935654,
18.9206303805908));
#15215=CARTESIAN_POINT('Ctrl Pts',(-0.0300853641101711,1.9945306952837,
18.9209783816573));
#15216=CARTESIAN_POINT('Ctrl Pts',(-0.0403996229948302,1.99434666399179,
18.9216323167224));
#15217=CARTESIAN_POINT('Ctrl Pts',(-0.0452133898834948,1.99424333881827,
18.9219380817066));
#15218=CARTESIAN_POINT('Ctrl Pts',(-0.0559827783491645,1.99397316637189,
18.9226234308082));
#15219=CARTESIAN_POINT('Ctrl Pts',(-0.0619381021696555,1.99379706337182,
18.9230033022824));
#15220=CARTESIAN_POINT('Ctrl Pts',(-0.0770067850007071,1.9932838945299,
18.9239667622487));
#15221=CARTESIAN_POINT('Ctrl Pts',(-0.0861187111557444,1.99291100958607,
18.9245514675075));
#15222=CARTESIAN_POINT('Ctrl Pts',(-0.111788007053477,1.9916841808652,18.9262047313863));
#15223=CARTESIAN_POINT('Ctrl Pts',(-0.128337435444675,1.99068629117969,
18.9272777638642));
#15224=CARTESIAN_POINT('Ctrl Pts',(-0.304701315740075,1.97784365080766,
18.9387915399578));
#15225=CARTESIAN_POINT('Ctrl Pts',(-0.462514645459761,1.94698956524212,
18.9498561227056));
#15226=CARTESIAN_POINT('Ctrl Pts',(-0.690388617649494,1.87314908885194,
18.9665692310685));
#15227=CARTESIAN_POINT('Ctrl Pts',(-0.764351364330066,1.84420504166587,
18.9721050536836));
#15228=CARTESIAN_POINT('Ctrl Pts',(-0.864915374895666,1.79775854592652,
18.9796419834379));
#15229=CARTESIAN_POINT('Ctrl Pts',(-0.893121025354515,1.78391408473116,
18.981756613516));
#15230=CARTESIAN_POINT('Ctrl Pts',(-0.93696221813571,1.76109443668826,18.9850318270928));
#15231=CARTESIAN_POINT('Ctrl Pts',(-0.952822370918598,1.75256423523097,
18.9862142063184));
#15232=CARTESIAN_POINT('Ctrl Pts',(-0.972897816596316,1.74141378199585,
18.9877055941949));
#15233=CARTESIAN_POINT('Ctrl Pts',(-0.977221205534696,1.73899132786698,
18.9880264611269));
#15234=CARTESIAN_POINT('Ctrl Pts',(-0.984141603076149,1.73507977586952,
18.9885395091405));
#15235=CARTESIAN_POINT('Ctrl Pts',(-0.986744330563269,1.73360092002989,
18.9887323363509));
#15236=CARTESIAN_POINT('Ctrl Pts',(-0.991703465782193,1.73076837947129,
18.9890994834311));
#15237=CARTESIAN_POINT('Ctrl Pts',(-0.994060407424666,1.7294157550719,18.989273864816));
#15238=CARTESIAN_POINT('Ctrl Pts',(-0.999491283842019,1.72628426080426,
18.9896754255931));
#15239=CARTESIAN_POINT('Ctrl Pts',(-1.00256323622078,1.72450199577505,18.9899023827516));
#15240=CARTESIAN_POINT('Ctrl Pts',(-1.0123897958372,1.71876575533445,18.9906278369023));
#15241=CARTESIAN_POINT('Ctrl Pts',(-1.01912600303422,1.71478016527551,18.9911243289434));
#15242=CARTESIAN_POINT('Ctrl Pts',(-1.11527861181748,1.65712312439682,18.9982021436406));
#15243=CARTESIAN_POINT('Ctrl Pts',(-1.20038931483934,1.59655114342592,19.0043577097433));
#15244=CARTESIAN_POINT('Ctrl Pts',(-1.29377169615538,1.51838310720742,19.0114543864536));
#15245=CARTESIAN_POINT('Ctrl Pts',(-1.30701356560473,1.50699967121291,19.0124693331214));
#15246=CARTESIAN_POINT('Ctrl Pts',(-1.38993866161861,1.43379746776894,19.018891373008));
#15247=CARTESIAN_POINT('Ctrl Pts',(-1.45536769441989,1.367336348808,19.0242651121018));
#15248=CARTESIAN_POINT('Ctrl Pts',(-1.55204766831419,1.25429922722888,19.0330748031148));
#15249=CARTESIAN_POINT('Ctrl Pts',(-1.58639959137859,1.2105594195541,19.0364131852246));
#15250=CARTESIAN_POINT('Ctrl Pts',(-1.63784172652565,1.13910295306852,19.0418090721298));
#15251=CARTESIAN_POINT('Ctrl Pts',(-1.65615861181991,1.11230370069679,19.0438204543072));
#15252=CARTESIAN_POINT('Ctrl Pts',(-1.67864507651206,1.07761643745878,19.0464140125854));
#15253=CARTESIAN_POINT('Ctrl Pts',(-1.68342746359027,1.0701301088647,19.0469731851214));
#15254=CARTESIAN_POINT('Ctrl Pts',(-1.69102301814097,1.05806313962287,19.0478736857798));
#15255=CARTESIAN_POINT('Ctrl Pts',(-1.69386799071595,1.05350257921687,19.0482138343073));
#15256=CARTESIAN_POINT('Ctrl Pts',(-1.69923633291403,1.04481903386631,19.0488611722867));
#15257=CARTESIAN_POINT('Ctrl Pts',(-1.7017632206451,1.040698260212,19.0491682292814));
#15258=CARTESIAN_POINT('Ctrl Pts',(-1.70747390642219,1.03130902959119,19.0498675729913));
#15259=CARTESIAN_POINT('Ctrl Pts',(-1.71064833331723,1.02603495746683,19.0502601990836));
#15260=CARTESIAN_POINT('Ctrl Pts',(-1.72022119555614,1.0099624482373,19.051456141146));
#15261=CARTESIAN_POINT('Ctrl Pts',(-1.72654207019005,0.999118399581432,
19.0522622633811));
#15262=CARTESIAN_POINT('Ctrl Pts',(-1.81034008412279,0.85218502913537,19.0631762960184));
#15263=CARTESIAN_POINT('Ctrl Pts',(-1.87161514653113,0.707521813089579,
19.0738885840095));
#15264=CARTESIAN_POINT('Ctrl Pts',(-1.95127628739698,0.433700962961726,
19.0937666322128));
#15265=CARTESIAN_POINT('Ctrl Pts',(-1.9751813042528,0.306985718346887,19.1028022149009));
#15266=CARTESIAN_POINT('Ctrl Pts',(-1.98771019595702,0.167805072338022,
19.112047353306));
#15267=CARTESIAN_POINT('Ctrl Pts',(-1.98861177279394,0.15675967393898,19.1127763069781));
#15268=CARTESIAN_POINT('Ctrl Pts',(-1.99001848749443,0.137552997706097,
19.1140349845805));
#15269=CARTESIAN_POINT('Ctrl Pts',(-1.99056557319754,0.12939517818003,19.1145668112959));
#15270=CARTESIAN_POINT('Ctrl Pts',(-1.99128461251944,0.117586184358204,
19.1153324192907));
#15271=CARTESIAN_POINT('Ctrl Pts',(-1.99149670501233,0.113937672679454,
19.1155683756559));
#15272=CARTESIAN_POINT('Ctrl Pts',(-1.99184935975692,0.107569088295612,
19.1159791973249));
#15273=CARTESIAN_POINT('Ctrl Pts',(-1.99199437964554,0.104849284916977,
19.116154311442));
#15274=CARTESIAN_POINT('Ctrl Pts',(-1.99228610422705,0.0991588976492834,
19.1165199796931));
#15275=CARTESIAN_POINT('Ctrl Pts',(-1.9924317358545,0.0961882857901529,
19.1167104728276));
#15276=CARTESIAN_POINT('Ctrl Pts',(-1.99279826689133,0.088353487577497,
19.1172118564511));
#15277=CARTESIAN_POINT('Ctrl Pts',(-1.9930080028155,0.0834887609890627,
19.117522125465));
#15278=CARTESIAN_POINT('Ctrl Pts',(-1.99380599890046,0.0632585406961544,
19.1188082258013));
#15279=CARTESIAN_POINT('Ctrl Pts',(-1.99423441356957,0.047886768939276,
19.1197754603846));
#15280=CARTESIAN_POINT('Ctrl Pts',(-1.9946576362865,0.0219229165871689,
19.1213946140827));
#15281=CARTESIAN_POINT('Ctrl Pts',(-1.99474591490793,0.0113333676914158,
19.1220509090515));
#15282=CARTESIAN_POINT('Ctrl Pts',(-1.99476839303552,-0.048983006416836,
19.1257683116931));
#15283=CARTESIAN_POINT('Ctrl Pts',(-1.99292749707664,-0.0986965709033473,
19.1287521200525));
#15284=CARTESIAN_POINT('Ctrl Pts',(-1.97716859296675,-0.310089713484085,
19.1412897896345));
#15285=CARTESIAN_POINT('Ctrl Pts',(-1.94541352259528,-0.469809221487074,
19.1504385273581));
#15286=CARTESIAN_POINT('Ctrl Pts',(-1.8742613111753,-0.685876414871118,
19.1640443629668));
#15287=CARTESIAN_POINT('Ctrl Pts',(-1.8508355279696,-0.74678537698661,19.1680190355975));
#15288=CARTESIAN_POINT('Ctrl Pts',(-1.82023017919837,-0.816026759479792,
19.172751580658));
#15289=CARTESIAN_POINT('Ctrl Pts',(-1.81591425457809,-0.825586452630829,
19.1734097952444));
#15290=CARTESIAN_POINT('Ctrl Pts',(-1.80888297058829,-0.840838707910833,
19.174467906899));
#15291=CARTESIAN_POINT('Ctrl Pts',(-1.80621561883299,-0.846553288816695,
19.1748661512205));
#15292=CARTESIAN_POINT('Ctrl Pts',(-1.80144121860599,-0.856656757236279,
19.175573492567));
#15293=CARTESIAN_POINT('Ctrl Pts',(-1.79934510765298,-0.861050780551459,
19.1758822088685));
#15294=CARTESIAN_POINT('Ctrl Pts',(-1.79495618389666,-0.870165156154452,
19.1765248622556));
#15295=CARTESIAN_POINT('Ctrl Pts',(-1.79266078974096,-0.874884216997918,
19.1768588873432));
#15296=CARTESIAN_POINT('Ctrl Pts',(-1.78668250115603,-0.887052567836725,
19.1777235444016));
#15297=CARTESIAN_POINT('Ctrl Pts',(-1.78297165922339,-0.894487941217826,
19.1782551497565));
#15298=CARTESIAN_POINT('Ctrl Pts',(-1.76705150854837,-0.925894270987347,
19.1805146460061));
#15299=CARTESIAN_POINT('Ctrl Pts',(-1.75440489313891,-0.949639188376966,
19.1822578490267));
#15300=CARTESIAN_POINT('Ctrl Pts',(-1.72030560483097,-1.01065579717979,
19.1868313393125));
#15301=CARTESIAN_POINT('Ctrl Pts',(-1.69812193986251,-1.04750080433859,
19.1896867957139));
#15302=CARTESIAN_POINT('Ctrl Pts',(-1.58360803362604,-1.22448897400096,
19.2038714932848));
#15303=CARTESIAN_POINT('Ctrl Pts',(-1.47503888079859,-1.35330497143333,
19.2157573295699));
#15304=CARTESIAN_POINT('Ctrl Pts',(-1.33863676598694,-1.4789836508341,19.2285350574922));
#15305=CARTESIAN_POINT('Ctrl Pts',(-1.3254566144096,-1.49080710433722,19.2297497642909));
#15306=CARTESIAN_POINT('Ctrl Pts',(-1.27455659047977,-1.53525903134374,
19.2343604340685));
#15307=CARTESIAN_POINT('Ctrl Pts',(-1.23577175977686,-1.56664735245848,
19.2377088687697));
#15308=CARTESIAN_POINT('Ctrl Pts',(-1.19012837665718,-1.60083511549484,
19.2414292448915));
#15309=CARTESIAN_POINT('Ctrl Pts',(-1.18438624525612,-1.60508811151589,
19.2418934381641));
#15310=CARTESIAN_POINT('Ctrl Pts',(-1.1758307125715,-1.61135398408785,19.242579228929));
#15311=CARTESIAN_POINT('Ctrl Pts',(-1.17303480856813,-1.61339048744984,
19.2428024237873));
#15312=CARTESIAN_POINT('Ctrl Pts',(-1.16804833011863,-1.61700276511912,
19.2431988384401));
#15313=CARTESIAN_POINT('Ctrl Pts',(-1.16585984748929,-1.61858137275435,
19.2433722535158));
#15314=CARTESIAN_POINT('Ctrl Pts',(-1.16116722341014,-1.62195182507142,
19.2437428846018));
#15315=CARTESIAN_POINT('Ctrl Pts',(-1.15866214290623,-1.62374230790631,
19.2439400065799));
#15316=CARTESIAN_POINT('Ctrl Pts',(-1.15180119584587,-1.62862214311728,
19.2444779149781));
#15317=CARTESIAN_POINT('Ctrl Pts',(-1.14743701401561,-1.63169984379864,
19.2448179078511));
#15318=CARTESIAN_POINT('Ctrl Pts',(-1.12464457279186,-1.64763682419787,
19.2465826130695));
#15319=CARTESIAN_POINT('Ctrl Pts',(-1.10601145432191,-1.66020218236204,
19.2479881723778));
#15320=CARTESIAN_POINT('Ctrl Pts',(-1.05107035289388,-1.69591639934581,
19.2520380519196));
#15321=CARTESIAN_POINT('Ctrl Pts',(-1.01421880307146,-1.71820896810674,
19.2546369334057));
#15322=CARTESIAN_POINT('Ctrl Pts',(-0.904327494207502,-1.7799166836451,
19.2621356140406));
#15323=CARTESIAN_POINT('Ctrl Pts',(-0.829515123935788,-1.81598943981576,
19.2669303912729));
#15324=CARTESIAN_POINT('Ctrl Pts',(-0.611798877444507,-1.90469654178063,
19.2805670291109));
#15325=CARTESIAN_POINT('Ctrl Pts',(-0.464847824657405,-1.94578370274167,
19.2894465545446));
#15326=CARTESIAN_POINT('Ctrl Pts',(-0.302142015231538,-1.97177549886785,
19.2997343912466));
#15327=CARTESIAN_POINT('Ctrl Pts',(-0.289599475004221,-1.97365664378116,
19.3005299457173));
#15328=CARTESIAN_POINT('Ctrl Pts',(-0.270918257092855,-1.97627656825619,
19.3017188939477));
#15329=CARTESIAN_POINT('Ctrl Pts',(-0.264792537492503,-1.97710664531663,
19.3021094013073));
#15330=CARTESIAN_POINT('Ctrl Pts',(-0.253867072191385,-1.97853543500308,
19.3028070695785));
#15331=CARTESIAN_POINT('Ctrl Pts',(-0.249068800022455,-1.97914519176484,
19.3031138792046));
#15332=CARTESIAN_POINT('Ctrl Pts',(-0.238948011232242,-1.98039393753044,
19.3037618957626));
#15333=CARTESIAN_POINT('Ctrl Pts',(-0.233625049232619,-1.98102893349015,
19.3041032260982));
#15334=CARTESIAN_POINT('Ctrl Pts',(-0.219539099495734,-1.98265173742433,
19.3050078570906));
#15335=CARTESIAN_POINT('Ctrl Pts',(-0.21077208682156,-1.9836028965983,19.3055723074751));
#15336=CARTESIAN_POINT('Ctrl Pts',(-0.170386904903891,-1.98771365003396,
19.3081791674521));
#15337=CARTESIAN_POINT('Ctrl Pts',(-0.138703890513937,-1.99017544176523,
19.3102433602147));
#15338=CARTESIAN_POINT('Ctrl Pts',(-0.0530774929440565,-1.9947741436719,
19.3158770728432));
#15339=CARTESIAN_POINT('Ctrl Pts',(0.00091289138800443,-1.99547974140178,
19.3194887166107));
#15340=CARTESIAN_POINT('Ctrl Pts',(0.157733712683046,-1.99116506483945,
19.3301446071597));
#15341=CARTESIAN_POINT('Ctrl Pts',(0.260224995331925,-1.9803782276437,19.337324491093));
#15342=CARTESIAN_POINT('Ctrl Pts',(0.474155444052555,-1.94096509563844,
19.3524974236475));
#15343=CARTESIAN_POINT('Ctrl Pts',(0.58490847222163,-1.91051240722891,19.3604622101961));
#15344=CARTESIAN_POINT('Ctrl Pts',(0.699578072011126,-1.86806744222649,
19.3684472071921));
#15345=CARTESIAN_POINT('Ctrl Pts',(0.706698156315862,-1.8653855279601,19.3689418496829));
#15346=CARTESIAN_POINT('Ctrl Pts',(0.71713160345363,-1.86138726051182,19.3696647822078));
#15347=CARTESIAN_POINT('Ctrl Pts',(0.720456953983365,-1.86010269829635,
19.3698949116593));
#15348=CARTESIAN_POINT('Ctrl Pts',(0.726313033624408,-1.85782247142042,
19.3702996557139));
#15349=CARTESIAN_POINT('Ctrl Pts',(0.728845192026877,-1.85683053738073,
19.3704744927677));
#15350=CARTESIAN_POINT('Ctrl Pts',(0.734154262788085,-1.85473825717146,
19.3708406938882));
#15351=CARTESIAN_POINT('Ctrl Pts',(0.736930728580738,-1.85363685379489,
19.371031992736));
#15352=CARTESIAN_POINT('Ctrl Pts',(0.744279783292718,-1.85070241663658,
19.3715378078947));
#15353=CARTESIAN_POINT('Ctrl Pts',(0.748848110106667,-1.84885865874066,
19.3718516827719));
#15354=CARTESIAN_POINT('Ctrl Pts',(0.769802485695587,-1.84031115173197,
19.3732890645036));
#15355=CARTESIAN_POINT('Ctrl Pts',(0.786106290284432,-1.83340610745724,
19.3744008901022));
#15356=CARTESIAN_POINT('Ctrl Pts',(0.830407735590246,-1.81394375877727,
19.37740971865));
#15357=CARTESIAN_POINT('Ctrl Pts',(0.85821194795794,-1.80095570001954,19.3792845533385));
#15358=CARTESIAN_POINT('Ctrl Pts',(0.954030039250381,-1.75347329833501,
19.3857353190476));
#15359=CARTESIAN_POINT('Ctrl Pts',(1.02036054452499,-1.71572372907188,19.3901841556255));
#15360=CARTESIAN_POINT('Ctrl Pts',(1.22261733967541,-1.5847282583496,19.4041786494978));
#15361=CARTESIAN_POINT('Ctrl Pts',(1.3492244997805,-1.47842582543381,19.4136540525626));
#15362=CARTESIAN_POINT('Ctrl Pts',(1.47549225304111,-1.34252875701256,19.4251349004271));
#15363=CARTESIAN_POINT('Ctrl Pts',(1.48942093545346,-1.32705918406338,19.4264327682386));
#15364=CARTESIAN_POINT('Ctrl Pts',(1.50822903482301,-1.30550124512892,19.4282306553767));
#15365=CARTESIAN_POINT('Ctrl Pts',(1.51331895316874,-1.29959765531884,19.4287219147869));
#15366=CARTESIAN_POINT('Ctrl Pts',(1.52137123390345,-1.29014669270614,19.429506714626));
#15367=CARTESIAN_POINT('Ctrl Pts',(1.52435613193959,-1.28661855360503,19.429799325983));
#15368=CARTESIAN_POINT('Ctrl Pts',(1.53045622720997,-1.27935723708179,19.4304008308354));
#15369=CARTESIAN_POINT('Ctrl Pts',(1.5335700871459,-1.27562298137129,19.4307097760893));
#15370=CARTESIAN_POINT('Ctrl Pts',(1.54073370236568,-1.26696796927881,19.4314249555176));
#15371=CARTESIAN_POINT('Ctrl Pts',(1.54477357385966,-1.26203913597407,19.4318315865641));
#15372=CARTESIAN_POINT('Ctrl Pts',(1.55740458190825,-1.24647719635869,19.4331134877558));
#15373=CARTESIAN_POINT('Ctrl Pts',(1.56590992835681,-1.23577526824021,19.4339921875742));
#15374=CARTESIAN_POINT('Ctrl Pts',(1.65083171511155,-1.12663717349122,19.4429260621571));
#15375=CARTESIAN_POINT('Ctrl Pts',(1.71796008638762,-1.02135170846673,19.4513504643823));
#15376=CARTESIAN_POINT('Ctrl Pts',(1.83574210664646,-0.791764391708617,
19.4692242591229));
#15377=CARTESIAN_POINT('Ctrl Pts',(1.88459073080402,-0.667202286636079,
19.4786593256417));
#15378=CARTESIAN_POINT('Ctrl Pts',(1.93109057120555,-0.501413899195394,
19.4903108470931));
#15379=CARTESIAN_POINT('Ctrl Pts',(1.94045999604452,-0.463834221967416,
19.4928924240836));
#15380=CARTESIAN_POINT('Ctrl Pts',(1.95014130214841,-0.419547523949938,
19.4958473087531));
#15381=CARTESIAN_POINT('Ctrl Pts',(1.95152038051191,-0.413085258302716,
19.4962763188432));
#15382=CARTESIAN_POINT('Ctrl Pts',(1.95355938964025,-0.403292449171764,
19.4969230388686));
#15383=CARTESIAN_POINT('Ctrl Pts',(1.95424295373218,-0.399966956908765,
19.4971420640202));
#15384=CARTESIAN_POINT('Ctrl Pts',(1.95545345057473,-0.394000781382996,
19.4975339313515));
#15385=CARTESIAN_POINT('Ctrl Pts',(1.95598352714996,-0.391360773335032,
19.497706951255));
#15386=CARTESIAN_POINT('Ctrl Pts',(1.95711678186754,-0.385656862491291,
19.498079949533));
#15387=CARTESIAN_POINT('Ctrl Pts',(1.95771810965317,-0.382592625278867,
19.4982798210231));
#15388=CARTESIAN_POINT('Ctrl Pts',(1.95936579969838,-0.374090748190541,
19.4988329938481));
#15389=CARTESIAN_POINT('Ctrl Pts',(1.96039672930861,-0.368650092072454,
19.4991854244682));
#15390=CARTESIAN_POINT('Ctrl Pts',(1.9659934612328,-0.338426240792695,19.5011349195552));
#15391=CARTESIAN_POINT('Ctrl Pts',(1.97011221114455,-0.313561205596149,
19.5027077389574));
#15392=CARTESIAN_POINT('Ctrl Pts',(1.99728902559753,-0.127711838216945,
19.5142779357084));
#15393=CARTESIAN_POINT('Ctrl Pts',(2.00105681247822,0.0354939515073905,
19.5234447187878));
#15394=CARTESIAN_POINT('Ctrl Pts',(1.98296508720919,0.217449997489708,19.5341341875849));
#15395=CARTESIAN_POINT('Ctrl Pts',(1.98066309160486,0.237505229415738,19.5353181439386));
#15396=CARTESIAN_POINT('Ctrl Pts',(1.96612913265591,0.349142386546518,19.5419518897035));
#15397=CARTESIAN_POINT('Ctrl Pts',(1.94785169654975,0.439811924896973,19.5475097644353));
#15398=CARTESIAN_POINT('Ctrl Pts',(1.92001813227682,0.541033055582209,19.5540650021422));
#15399=CARTESIAN_POINT('Ctrl Pts',(1.91656161764104,0.553152736294349,19.5548555968101));
#15400=CARTESIAN_POINT('Ctrl Pts',(1.91124336186034,0.571151812234453,19.5560385537288));
#15401=CARTESIAN_POINT('Ctrl Pts',(1.90946878039123,0.577056805001016,19.5564280724569));
#15402=CARTESIAN_POINT('Ctrl Pts',(1.90625385994332,0.58757736630923,19.5571246367674));
#15403=CARTESIAN_POINT('Ctrl Pts',(1.90482405738415,0.592196124340333,19.5574313352424));
#15404=CARTESIAN_POINT('Ctrl Pts',(1.90177098821307,0.601933137743208,19.558079804301));
#15405=CARTESIAN_POINT('Ctrl Pts',(1.90014382185789,0.607050120869674,19.5584217009231));
#15406=CARTESIAN_POINT('Ctrl Pts',(1.895777681335,0.620590853041795,19.5593294273112));
#15407=CARTESIAN_POINT('Ctrl Pts',(1.89300324776476,0.629002959993402,19.5598964209307));
#15408=CARTESIAN_POINT('Ctrl Pts',(1.87988804530172,0.667895567992703,19.5625323625652));
#15409=CARTESIAN_POINT('Ctrl Pts',(1.86886702568252,0.69813995137732,19.564623691124));
#15410=CARTESIAN_POINT('Ctrl Pts',(1.83706195017677,0.779262849624398,19.5703503303172));
#15411=CARTESIAN_POINT('Ctrl Pts',(1.81490048429291,0.829567665639743,19.5740294898851));
#15412=CARTESIAN_POINT('Ctrl Pts',(1.74501600509554,0.97195364741234,19.5848111966556));
#15413=CARTESIAN_POINT('Ctrl Pts',(1.69215724610676,1.06130832576484,19.5920487764715));
#15414=CARTESIAN_POINT('Ctrl Pts',(1.59697525989306,1.19688839243667,19.6036014060277));
#15415=CARTESIAN_POINT('Ctrl Pts',(1.55900191879886,1.24594764334008,19.6079132913364));
#15416=CARTESIAN_POINT('Ctrl Pts',(1.48563751044459,1.33211338625452,19.6156409856782));
#15417=CARTESIAN_POINT('Ctrl Pts',(1.45098180929269,1.36978017117031,19.6190785459187));
#15418=CARTESIAN_POINT('Ctrl Pts',(1.40984365532526,1.4111768650237,19.6228862631286));
#15419=CARTESIAN_POINT('Ctrl Pts',(1.40474697358939,1.41625040895099,19.6233534613281));
#15420=CARTESIAN_POINT('Ctrl Pts',(1.39715188823104,1.42372967604132,19.6240428221016));
#15421=CARTESIAN_POINT('Ctrl Pts',(1.39467453985458,1.42615655436457,19.6242666059536));
#15422=CARTESIAN_POINT('Ctrl Pts',(1.39025767596323,1.43046091988443,19.6246636704338));
#15423=CARTESIAN_POINT('Ctrl Pts',(1.38832067092181,1.43234093843091,19.6248371488174));
#15424=CARTESIAN_POINT('Ctrl Pts',(1.38417004653905,1.43635312184936,19.6252074801518));
#15425=CARTESIAN_POINT('Ctrl Pts',(1.38195532142411,1.43848409733394,19.625404240789));
#15426=CARTESIAN_POINT('Ctrl Pts',(1.37589763094082,1.4442858145237,19.6259401501067));
#15427=CARTESIAN_POINT('Ctrl Pts',(1.37204487285791,1.44794636409177,19.6262785151126));
#15428=CARTESIAN_POINT('Ctrl Pts',(1.35206714848454,1.46677609141313,19.6280205743258));
#15429=CARTESIAN_POINT('Ctrl Pts',(1.33570432662753,1.4816921838507,19.6294056958277));
#15430=CARTESIAN_POINT('Ctrl Pts',(1.28749237698159,1.52419352282174,19.6333794615361));
#15431=CARTESIAN_POINT('Ctrl Pts',(1.25501206974719,1.55104729485839,19.6359246791852));
#15432=CARTESIAN_POINT('Ctrl Pts',(1.11929795674476,1.65619489474771,19.6461486394356));
#15433=CARTESIAN_POINT('Ctrl Pts',(1.00940302885524,1.72537490426838,19.6535166351076));
#15434=CARTESIAN_POINT('Ctrl Pts',(0.798341270827465,1.83112644503387,19.6673447423129));
#15435=CARTESIAN_POINT('Ctrl Pts',(0.699456781502086,1.87113021093521,19.6737083273922));
#15436=CARTESIAN_POINT('Ctrl Pts',(0.585583691370159,1.90690453422303,19.6811593534654));
#15437=CARTESIAN_POINT('Ctrl Pts',(0.573269927538925,1.9106424940467,19.6819664416302));
#15438=CARTESIAN_POINT('Ctrl Pts',(0.554953670335571,1.91600956517889,19.6831693109417));
#15439=CARTESIAN_POINT('Ctrl Pts',(0.548978168530095,1.91773022063343,19.6835621047909));
#15440=CARTESIAN_POINT('Ctrl Pts',(0.538336269393341,1.92074075866265,19.684262336082));
#15441=CARTESIAN_POINT('Ctrl Pts',(0.533673017053685,1.92204165176616,19.6845694125659));
#15442=CARTESIAN_POINT('Ctrl Pts',(0.528996770175458,1.92332783989592,19.6848775917535));
#15443=CARTESIAN_POINT('Ctrl Pts',(0.528988431769083,1.92333013329206,19.6848781412812));
#15444=CARTESIAN_POINT('Ctrl Pts',(0.528971774508747,1.92333471459013,19.6848792390495));
#15445=CARTESIAN_POINT('Ctrl Pts',(0.528963455439792,1.92333700255146,19.6848797873043));
#15446=CARTESIAN_POINT('Ctrl Pts',(0.528946836530065,1.92334157306988,19.6848808825483));
#15447=CARTESIAN_POINT('Ctrl Pts',(0.528938536674659,1.92334385563127,19.6848814295385));
#15448=CARTESIAN_POINT('Ctrl Pts',(0.528921956022896,1.92334841539713,19.6848825222643));
#15449=CARTESIAN_POINT('Ctrl Pts',(0.528913675266873,1.92335069259078,19.6848830679972));
#15450=CARTESIAN_POINT('Ctrl Pts',(0.528897132834853,1.92335524161619,19.6848841582073));
#15451=CARTESIAN_POINT('Ctrl Pts',(0.52888887113718,1.92335751345418,19.6848847026858));
#15452=CARTESIAN_POINT('Ctrl Pts',(0.528872366698314,1.92336205180304,19.6848857903951));
#15453=CARTESIAN_POINT('Ctrl Pts',(0.528864123974618,1.92336431830936,19.6848863336246));
#15454=CARTESIAN_POINT('Ctrl Pts',(0.52884765740287,1.9233688460179,19.6848874188414));
#15455=CARTESIAN_POINT('Ctrl Pts',(0.528839433581744,1.92337110721298,19.6848879608267));
#15456=CARTESIAN_POINT('Ctrl Pts',(0.523767009059326,1.9247657695497,19.6852222559986));
#15457=CARTESIAN_POINT('Ctrl Pts',(0.518697369340324,1.926138153295,19.6855566576926));
#15458=CARTESIAN_POINT('Ctrl Pts',(0.505457569011053,1.9296661904875,19.6864307625936));
#15459=CARTESIAN_POINT('Ctrl Pts',(0.497279093834176,1.9317899626959,19.6869714932033));
#15460=CARTESIAN_POINT('Ctrl Pts',(0.479334087869849,1.93632838327724,19.688159749012));
#15461=CARTESIAN_POINT('Ctrl Pts',(0.469562331226193,1.93872122457047,19.6888079628767));
#15462=CARTESIAN_POINT('Ctrl Pts',(0.440789333833013,1.94553666803724,19.690720216513));
#15463=CARTESIAN_POINT('Ctrl Pts',(0.421741266328446,1.94975445197798,19.6919907404962));
#15464=CARTESIAN_POINT('Ctrl Pts',(0.354849177478144,1.9635401929018,19.6964695151028));
#15465=CARTESIAN_POINT('Ctrl Pts',(0.306721796246643,1.97163107906789,19.6997227287004));
#15466=CARTESIAN_POINT('Ctrl Pts',(0.140754504018667,1.99330885840251,19.7110433475078));
#15467=CARTESIAN_POINT('Ctrl Pts',(0.0220338853879719,1.99814947685828,
19.7193332512861));
#15468=CARTESIAN_POINT('Ctrl Pts',(-0.16861596155308,1.98892525505808,19.7326368020005));
#15469=CARTESIAN_POINT('Ctrl Pts',(-0.240594339664068,1.98150720372225,
19.7376519979553));
#15470=CARTESIAN_POINT('Ctrl Pts',(-0.347870086339265,1.96451820581839,
19.7449868298044));
#15471=CARTESIAN_POINT('Ctrl Pts',(-0.383566160362162,1.95786178977921,
19.7474034302511));
#15472=CARTESIAN_POINT('Ctrl Pts',(-0.424841420474535,1.94899262659045,
19.7501545771088));
#15473=CARTESIAN_POINT('Ctrl Pts',(-0.430614109898085,1.94772533524217,
19.7505383566897));
#15474=CARTESIAN_POINT('Ctrl Pts',(-0.439825355828883,1.94566021636343,
19.7511490604085));
#15475=CARTESIAN_POINT('Ctrl Pts',(-0.44326751951239,1.94487889797425,19.7513769001245));
#15476=CARTESIAN_POINT('Ctrl Pts',(-0.449352983855655,1.94348059568533,
19.7517790162262));
#15477=CARTESIAN_POINT('Ctrl Pts',(-0.451997119432893,1.9428673486079,19.7519535056696));
#15478=CARTESIAN_POINT('Ctrl Pts',(-0.457565585880516,1.94156388638086,
19.7523204826375));
#15479=CARTESIAN_POINT('Ctrl Pts',(-0.460489604128814,1.94087246233817,
19.752512899199));
#15480=CARTESIAN_POINT('Ctrl Pts',(-0.468280637801568,1.93901156828188,
19.7530248616521));
#15481=CARTESIAN_POINT('Ctrl Pts',(-0.473144872205223,1.93783037154559,
19.7533437380114));
#15482=CARTESIAN_POINT('Ctrl Pts',(-0.495995359310248,1.93219035009836,
19.7548383495802));
#15483=CARTESIAN_POINT('Ctrl Pts',(-0.513924080764138,1.92749916844414,
19.756001238207));
#15484=CARTESIAN_POINT('Ctrl Pts',(-0.697586910028123,1.87669746826354,
19.7678374729394));
#15485=CARTESIAN_POINT('Ctrl Pts',(-0.856784177585974,1.80957464040822,
19.777502249278));
#15486=CARTESIAN_POINT('Ctrl Pts',(-1.10075860959072,1.66719702552204,19.7940254301368));
#15487=CARTESIAN_POINT('Ctrl Pts',(-1.19131115462912,1.60374186942225,19.8006085318692));
#15488=CARTESIAN_POINT('Ctrl Pts',(-1.28607029787913,1.52486640889814,19.8083045050831));
#15489=CARTESIAN_POINT('Ctrl Pts',(-1.29591634681992,1.51650756200604,19.8091145155165));
#15490=CARTESIAN_POINT('Ctrl Pts',(-1.31038844955407,1.50397754511282,19.810320909472));
#15491=CARTESIAN_POINT('Ctrl Pts',(-1.31507739272414,1.49987926002241,19.8107142798681));
#15492=CARTESIAN_POINT('Ctrl Pts',(-1.32337814762155,1.4925552889251,19.8114151595231));
#15493=CARTESIAN_POINT('Ctrl Pts',(-1.32699756514698,1.4893382669887,19.8117223053826));
#15494=CARTESIAN_POINT('Ctrl Pts',(-1.33396467964407,1.48310017522629,19.8123165374281));
#15495=CARTESIAN_POINT('Ctrl Pts',(-1.33731392036838,1.48008086743015,19.8126035483229));
#15496=CARTESIAN_POINT('Ctrl Pts',(-1.34613465986495,1.47207467417824,19.8133630345146));
#15497=CARTESIAN_POINT('Ctrl Pts',(-1.35158864412761,1.4670686771462,19.8138363187944));
#15498=CARTESIAN_POINT('Ctrl Pts',(-1.37260447468016,1.4475624154564,19.8156744776291));
#15499=CARTESIAN_POINT('Ctrl Pts',(-1.38796140542261,1.43284439815516,19.8170486632067));
#15500=CARTESIAN_POINT('Ctrl Pts',(-1.4256472744616,1.39555201765806,19.8205005852092));
#15501=CARTESIAN_POINT('Ctrl Pts',(-1.44767746247111,1.3726854558754,19.8225908999529));
#15502=CARTESIAN_POINT('Ctrl Pts',(-1.51759829961032,1.29655412155817,19.8294685569744));
#15503=CARTESIAN_POINT('Ctrl Pts',(-1.56316421686485,1.24123850464797,19.8343430623945));
#15504=CARTESIAN_POINT('Ctrl Pts',(-1.6631517477396,1.10559666915233,19.8459759612245));
#15505=CARTESIAN_POINT('Ctrl Pts',(-1.71488871361407,1.02351037431295,19.8527803439846));
#15506=CARTESIAN_POINT('Ctrl Pts',(-1.79990058259537,0.863957685751478,
19.8653189250707));
#15507=CARTESIAN_POINT('Ctrl Pts',(-1.83464359959019,0.787496943212655,
19.8710596827132));
#15508=CARTESIAN_POINT('Ctrl Pts',(-1.86725083618624,0.701757103145022,
19.8770513451247));
#15509=CARTESIAN_POINT('Ctrl Pts',(-1.86998768077486,0.694431275005862,
19.8775598086447));
#15510=CARTESIAN_POINT('Ctrl Pts',(-1.87390431186957,0.683756387065318,
19.8782954767469));
#15511=CARTESIAN_POINT('Ctrl Pts',(-1.87511830866236,0.680420087809079,
19.8785246587431));
#15512=CARTESIAN_POINT('Ctrl Pts',(-1.87724574141984,0.674524552974935,
19.8789283130932));
#15513=CARTESIAN_POINT('Ctrl Pts',(-1.87816286291818,0.671966671019204,
19.8791030040108));
#15514=CARTESIAN_POINT('Ctrl Pts',(-1.8800795470413,0.666586396500776,19.8794695152996));
#15515=CARTESIAN_POINT('Ctrl Pts',(-1.88107798050172,0.66376363169755,19.8796612681041));
#15516=CARTESIAN_POINT('Ctrl Pts',(-1.88371299409546,0.656260241596638,
19.8801695798418));
#15517=CARTESIAN_POINT('Ctrl Pts',(-1.88533849720944,0.651575706297139,
19.8804854859878));
#15518=CARTESIAN_POINT('Ctrl Pts',(-1.8927953063312,0.629824393445433,19.8819458308175));
#15519=CARTESIAN_POINT('Ctrl Pts',(-1.89841267591128,0.612684425602411,
19.8830781277802));
#15520=CARTESIAN_POINT('Ctrl Pts',(-1.94958707766242,0.449073010482196,
19.893733024));
#15521=CARTESIAN_POINT('Ctrl Pts',(-1.97834515292007,0.297860772534878,
19.9024453692807));
#15522=CARTESIAN_POINT('Ctrl Pts',(-1.99295987685804,0.0971005213254474,
19.9141562793086));
#15523=CARTESIAN_POINT('Ctrl Pts',(-1.99471555074445,0.0492652185206632,
19.9169542660838));
#15524=CARTESIAN_POINT('Ctrl Pts',(-1.99474949800079,0.00141517687806603,
19.9197876209294));
#15525=CARTESIAN_POINT('',(-1.9947498118588,-0.000866365563652432,21.5209548813952));
#15526=CARTESIAN_POINT('Ctrl Pts',(-1.9947494997464,0.00141271422995681,
19.9197877667508));
#15527=CARTESIAN_POINT('Ctrl Pts',(-1.99479242181115,-0.0591931502589759,
19.9233764363657));
#15528=CARTESIAN_POINT('Ctrl Pts',(-1.99207330674086,-0.119766089450529,
19.92701909106));
#15529=CARTESIAN_POINT('Ctrl Pts',(-1.98427649614867,-0.205760107810383,
19.9323275983535));
#15530=CARTESIAN_POINT('Ctrl Pts',(-1.98145557484169,-0.23135285878207,
19.9339246943544));
#15531=CARTESIAN_POINT('Ctrl Pts',(-1.97720826146773,-0.264059509659338,
19.9359905909697));
#15532=CARTESIAN_POINT('Ctrl Pts',(-1.97623727196789,-0.271230854685799,
19.9364450986454));
#15533=CARTESIAN_POINT('Ctrl Pts',(-1.9745091744404,-0.283491724204659,
19.9372248656381));
#15534=CARTESIAN_POINT('Ctrl Pts',(-1.97377135266513,-0.288583929276865,
19.9375495162768));
#15535=CARTESIAN_POINT('Ctrl Pts',(-1.97235065208835,-0.298128763649968,
19.9381595609322));
#15536=CARTESIAN_POINT('Ctrl Pts',(-1.97167237512711,-0.302582053542001,
19.9384448078909));
#15537=CARTESIAN_POINT('Ctrl Pts',(-1.97022956283687,-0.311844096913889,
19.939039380726));
#15538=CARTESIAN_POINT('Ctrl Pts',(-1.96946249399423,-0.316652420037105,
19.9393487850847));
#15539=CARTESIAN_POINT('Ctrl Pts',(-1.96766076359161,-0.327686609082672,
19.9400605227809));
#15540=CARTESIAN_POINT('Ctrl Pts',(-1.96661414820451,-0.33391044445781,
19.9404632330166));
#15541=CARTESIAN_POINT('Ctrl Pts',(-1.96374678398932,-0.350480366210433,
19.9415387778681));
#15542=CARTESIAN_POINT('Ctrl Pts',(-1.96187383131615,-0.360817102841638,
19.9422132651641));
#15543=CARTESIAN_POINT('Ctrl Pts',(-1.94771184974379,-0.43560414074995,
19.9471194231022));
#15544=CARTESIAN_POINT('Ctrl Pts',(-1.93233255721125,-0.49942131411221,
19.9514492071957));
#15545=CARTESIAN_POINT('Ctrl Pts',(-1.91156642651027,-0.570093272099501,
19.9564107267023));
#15546=CARTESIAN_POINT('Ctrl Pts',(-1.90924704253492,-0.577813351980916,
19.9569549558359));
#15547=CARTESIAN_POINT('Ctrl Pts',(-1.89464786547637,-0.625359014479997,
19.9603204373245));
#15548=CARTESIAN_POINT('Ctrl Pts',(-1.8811698387206,-0.664803844915511,
19.963172451783));
#15549=CARTESIAN_POINT('Ctrl Pts',(-1.80943664049553,-0.855040321389873,
19.9771980535711));
#15550=CARTESIAN_POINT('Ctrl Pts',(-1.73423640267897,-0.998789196798814,
19.9886997930666));
#15551=CARTESIAN_POINT('Ctrl Pts',(-1.62836430537238,-1.15242317448586,
20.0011597777289));
#15552=CARTESIAN_POINT('Ctrl Pts',(-1.61382876731584,-1.17269191890948,
20.0028059757612));
#15553=CARTESIAN_POINT('Ctrl Pts',(-1.59561595972442,-1.19710807213246,
20.0047867453344));
#15554=CARTESIAN_POINT('Ctrl Pts',(-1.59229739590086,-1.20151863575145,
20.0051444606489));
#15555=CARTESIAN_POINT('Ctrl Pts',(-1.58707511269118,-1.20839971682064,
20.0057023245488));
#15556=CARTESIAN_POINT('Ctrl Pts',(-1.58518386567472,-1.21087959817152,
20.0059033286226));
#15557=CARTESIAN_POINT('Ctrl Pts',(-1.58164862772257,-1.21549267127319,
20.0062771357978));
#15558=CARTESIAN_POINT('Ctrl Pts',(-1.58000614996346,-1.21762694685455,
20.006450038568));
#15559=CARTESIAN_POINT('Ctrl Pts',(-1.57628001318787,-1.22244854511872,
20.0068405593417));
#15560=CARTESIAN_POINT('Ctrl Pts',(-1.57419380750376,-1.22513386300254,
20.0070579935741));
#15561=CARTESIAN_POINT('Ctrl Pts',(-1.56801802592562,-1.23304137328696,
20.0076981413747));
#15562=CARTESIAN_POINT('Ctrl Pts',(-1.56390920793133,-1.23824858174801,
20.0081195131413));
#15563=CARTESIAN_POINT('Ctrl Pts',(-1.53533827365717,-1.27408817308612,
20.011019232702));
#15564=CARTESIAN_POINT('Ctrl Pts',(-1.51000183529451,-1.30401658030183,
20.0134384331073));
#15565=CARTESIAN_POINT('Ctrl Pts',(-1.36971462689488,-1.46015279329921,
20.026167868741));
#15566=CARTESIAN_POINT('Ctrl Pts',(-1.23979731203901,-1.57196657313992,
20.0357332527269));
#15567=CARTESIAN_POINT('Ctrl Pts',(-1.0469137785901,-1.69900765564511,20.0493668248969));
#15568=CARTESIAN_POINT('Ctrl Pts',(-0.995140993583359,-1.72984073468567,
20.0529719496541));
#15569=CARTESIAN_POINT('Ctrl Pts',(-0.922120102045771,-1.76896398912641,
20.0580409048379));
#15570=CARTESIAN_POINT('Ctrl Pts',(-0.90200492531467,-1.77930495690598,
20.0594355188257));
#15571=CARTESIAN_POINT('Ctrl Pts',(-0.871674559966865,-1.79425093291625,
20.0615381590494));
#15572=CARTESIAN_POINT('Ctrl Pts',(-0.861588918620203,-1.79911574837504,
20.0622373030771));
#15573=CARTESIAN_POINT('Ctrl Pts',(-0.843107877248631,-1.80783905012206,
20.0635186459925));
#15574=CARTESIAN_POINT('Ctrl Pts',(-0.834725559921038,-1.81172463658849,
20.0640998984985));
#15575=CARTESIAN_POINT('Ctrl Pts',(-0.821378830990571,-1.81779916694763,
20.0650256544875));
#15576=CARTESIAN_POINT('Ctrl Pts',(-0.816431890768744,-1.82002636303509,
20.0653688398655));
#15577=CARTESIAN_POINT('Ctrl Pts',(-0.811452372601198,-1.82224383938231,
20.0657143557928));
#15578=CARTESIAN_POINT('Ctrl Pts',(-0.811428779107624,-1.82225434547509,
20.0657159928861));
#15579=CARTESIAN_POINT('Ctrl Pts',(-0.811381288711448,-1.82227549166231,
20.0657192881286));
#15580=CARTESIAN_POINT('Ctrl Pts',(-0.811357391962236,-1.82228613167428,
20.0657209462673));
#15581=CARTESIAN_POINT('Ctrl Pts',(-0.811309290455628,-1.82230754770491,
20.0657242839199));
#15582=CARTESIAN_POINT('Ctrl Pts',(-0.811285085828311,-1.82231832365107,
20.0657259634248));
#15583=CARTESIAN_POINT('Ctrl Pts',(-0.811236363870772,-1.82234001359621,
20.0657293441357));
#15584=CARTESIAN_POINT('Ctrl Pts',(-0.81121184665814,-1.82235092752785,
20.0657310453336));
#15585=CARTESIAN_POINT('Ctrl Pts',(-0.811162494767885,-1.82237289551859,
20.0657344697611));
#15586=CARTESIAN_POINT('Ctrl Pts',(-0.811137660191363,-1.82238394951727,
20.0657361929838));
#15587=CARTESIAN_POINT('Ctrl Pts',(-0.811087668688827,-1.82240619976971,
20.0657396617998));
#15588=CARTESIAN_POINT('Ctrl Pts',(-0.811062511872667,-1.82241739595872,
20.0657414073856));
#15589=CARTESIAN_POINT('Ctrl Pts',(-0.811011871336272,-1.82243993257105,
20.0657449212442));
#15590=CARTESIAN_POINT('Ctrl Pts',(-0.810986387715586,-1.82245127293383,
20.06574668951));
#15591=CARTESIAN_POINT('Ctrl Pts',(-0.806558507015552,-1.82442159490524,
20.0660539330803));
#15592=CARTESIAN_POINT('Ctrl Pts',(-0.80214905969472,-1.82636460394891,
20.0663599532106));
#15593=CARTESIAN_POINT('Ctrl Pts',(-0.792229842600683,-1.83069262432347,
20.0670485029469));
#15594=CARTESIAN_POINT('Ctrl Pts',(-0.786716276654396,-1.83306876766923,
20.0674313319715));
#15595=CARTESIAN_POINT('Ctrl Pts',(-0.77266487932607,-1.83904932854881,
20.0684072753684));
#15596=CARTESIAN_POINT('Ctrl Pts',(-0.76411257462137,-1.84261917309844,
20.0690015574059));
#15597=CARTESIAN_POINT('Ctrl Pts',(-0.715195050354891,-1.86263886677943,
20.0724026295087));
#15598=CARTESIAN_POINT('Ctrl Pts',(-0.674326864209431,-1.87782062308033,
20.0752517724722));
#15599=CARTESIAN_POINT('Ctrl Pts',(-0.442531567006431,-1.95538550791613,
20.091468764879));
#15600=CARTESIAN_POINT('Ctrl Pts',(-0.243544485317435,-1.98998074044987,
20.1057669371418));
#15601=CARTESIAN_POINT('Ctrl Pts',(0.0149965974241431,-1.99553169137539,
20.1234889706565));
#15602=CARTESIAN_POINT('Ctrl Pts',(0.0728444019736701,-1.99425845241336,
20.127386943109));
#15603=CARTESIAN_POINT('Ctrl Pts',(0.137358847003102,-1.99002676398459,
20.1316021771146));
#15604=CARTESIAN_POINT('Ctrl Pts',(0.14415464525435,-1.98954603257756,20.1320445499404));
#15605=CARTESIAN_POINT('Ctrl Pts',(0.154330615376551,-1.98877377594213,
20.1327043492917));
#15606=CARTESIAN_POINT('Ctrl Pts',(0.157712635383516,-1.98850843492736,
20.1329232044504));
#15607=CARTESIAN_POINT('Ctrl Pts',(0.163522320692667,-1.98803771307875,
20.1332983965466));
#15608=CARTESIAN_POINT('Ctrl Pts',(0.165950295365517,-1.98783651181328,
20.1334549672031));
#15609=CARTESIAN_POINT('Ctrl Pts',(0.171015416410893,-1.98740743081919,
20.1337811155609));
#15610=CARTESIAN_POINT('Ctrl Pts',(0.173652468767516,-1.98717875114867,
20.1339506472422));
#15611=CARTESIAN_POINT('Ctrl Pts',(0.18098642003887,-1.98652805592749,20.1344214006493));
#15612=CARTESIAN_POINT('Ctrl Pts',(0.185682328377892,-1.98609462897701,
20.1347219849775));
#15613=CARTESIAN_POINT('Ctrl Pts',(0.204495594539168,-1.98429087825898,
20.1359230190562));
#15614=CARTESIAN_POINT('Ctrl Pts',(0.218600118751808,-1.98278661314207,
20.1368162231703));
#15615=CARTESIAN_POINT('Ctrl Pts',(0.386972575220258,-1.96301093468113,
20.14740523603));
#15616=CARTESIAN_POINT('Ctrl Pts',(0.538637684361655,-1.92692624618761,
20.1562329312064));
#15617=CARTESIAN_POINT('Ctrl Pts',(0.802024509770539,-1.83068703996755,
20.1725392943375));
#15618=CARTESIAN_POINT('Ctrl Pts',(0.915143355373243,-1.77684123458739,
20.1799071661889));
#15619=CARTESIAN_POINT('Ctrl Pts',(1.03276503576493,-1.70662463783894,20.1884146737901));
#15620=CARTESIAN_POINT('Ctrl Pts',(1.04300257482063,-1.7003872772655,20.1891624092736));
#15621=CARTESIAN_POINT('Ctrl Pts',(1.05922868764331,-1.69029962586952,20.1903594957024));
#15622=CARTESIAN_POINT('Ctrl Pts',(1.06525404988323,-1.68650883337295,20.1908066778012));
#15623=CARTESIAN_POINT('Ctrl Pts',(1.07666168239751,-1.67924632042429,20.191658453532));
#15624=CARTESIAN_POINT('Ctrl Pts',(1.08204778591495,-1.67578076443359,20.1920628162118));
#15625=CARTESIAN_POINT('Ctrl Pts',(1.09144223189616,-1.66967196471206,20.1927720062544));
#15626=CARTESIAN_POINT('Ctrl Pts',(1.09545791589045,-1.66704006225553,20.1930764083502));
#15627=CARTESIAN_POINT('Ctrl Pts',(1.10326116963773,-1.66188539435368,20.1936703931438));
#15628=CARTESIAN_POINT('Ctrl Pts',(1.10704968818211,-1.65936411306473,20.1939599187794));
#15629=CARTESIAN_POINT('Ctrl Pts',(1.11599653188098,-1.6533656589976,20.1946463830493));
#15630=CARTESIAN_POINT('Ctrl Pts',(1.12114726076934,-1.64987729232838,20.195043743059));
#15631=CARTESIAN_POINT('Ctrl Pts',(1.13916154660351,-1.6375536833124,20.1964411451163));
#15632=CARTESIAN_POINT('Ctrl Pts',(1.15193739497465,-1.62859181811261,20.1974459903224));
#15633=CARTESIAN_POINT('Ctrl Pts',(1.17061080672154,-1.61516333459023,20.1989355249391));
#15634=CARTESIAN_POINT('Ctrl Pts',(1.17659100265964,-1.610812176584,20.1994157518666));
#15635=CARTESIAN_POINT('Ctrl Pts',(1.31301858295191,-1.51038314581824,20.2104452930694));
#15636=CARTESIAN_POINT('Ctrl Pts',(1.43127827499866,-1.39881974470935,20.2216387844796));
#15637=CARTESIAN_POINT('Ctrl Pts',(1.58463474830905,-1.21411048565386,20.2383891589667));
#15638=CARTESIAN_POINT('Ctrl Pts',(1.63097000502012,-1.15111670860131,20.2438371815435));
#15639=CARTESIAN_POINT('Ctrl Pts',(1.69043175016869,-1.05945122359411,20.2512692480526));
#15640=CARTESIAN_POINT('Ctrl Pts',(1.70675840794183,-1.03294354199485,20.2533639637883));
#15641=CARTESIAN_POINT('Ctrl Pts',(1.73148089291526,-0.990616711170692,
20.2566117704436));
#15642=CARTESIAN_POINT('Ctrl Pts',(1.74029512342846,-0.975048967630145,
20.2577862395534));
#15643=CARTESIAN_POINT('Ctrl Pts',(1.75127700569248,-0.955029244193715,
20.2592691283358));
#15644=CARTESIAN_POINT('Ctrl Pts',(1.75363881324052,-0.950685501046682,
20.2595892447869));
#15645=CARTESIAN_POINT('Ctrl Pts',(1.7574034095743,-0.943700039306297,20.26010137856));
#15646=CARTESIAN_POINT('Ctrl Pts',(1.75881643072066,-0.941063904039953,
20.260294037995));
#15647=CARTESIAN_POINT('Ctrl Pts',(1.76150234204841,-0.936025881358682,
20.2606610656389));
#15648=CARTESIAN_POINT('Ctrl Pts',(1.76277623615511,-0.933624599579384,
20.2608354945467));
#15649=CARTESIAN_POINT('Ctrl Pts',(1.76570560807453,-0.928075383702448,
20.2612374302321));
#15650=CARTESIAN_POINT('Ctrl Pts',(1.76735757764585,-0.924925621570219,
20.2614647134193));
#15651=CARTESIAN_POINT('Ctrl Pts',(1.77263074876813,-0.914805709640665,
20.2621922616264));
#15652=CARTESIAN_POINT('Ctrl Pts',(1.77621926551058,-0.907818475030365,
20.2626905053746));
#15653=CARTESIAN_POINT('Ctrl Pts',(1.82172275233032,-0.817915417753545,
20.2690513521827));
#15654=CARTESIAN_POINT('Ctrl Pts',(1.85784268602966,-0.732178205888365,
20.2745767373536));
#15655=CARTESIAN_POINT('Ctrl Pts',(1.94344577454608,-0.4813238441476,20.2900825155914));
#15656=CARTESIAN_POINT('Ctrl Pts',(1.97771413277032,-0.311927668813766,
20.2998443312433));
#15657=CARTESIAN_POINT('Ctrl Pts',(1.99243410422429,-0.103065153755157,
20.3126263748458));
#15658=CARTESIAN_POINT('Ctrl Pts',(1.99401157475412,-0.0658304146854652,
20.3149298343639));
#15659=CARTESIAN_POINT('Ctrl Pts',(1.9946786197535,-0.0192706417985699,
20.3178495623386));
#15660=CARTESIAN_POINT('Ctrl Pts',(1.99474681062649,-0.0099654660445462,
20.3184350355625));
#15661=CARTESIAN_POINT('Ctrl Pts',(1.99475170100866,0.00480872997366494,
20.3193678440524));
#15662=CARTESIAN_POINT('Ctrl Pts',(1.99473101969195,0.0102776781660031,
20.3197138431944));
#15663=CARTESIAN_POINT('Ctrl Pts',(1.99464981067008,0.020564877771902,20.3203660238381));
#15664=CARTESIAN_POINT('Ctrl Pts',(1.99459431389083,0.0253831386789562,
20.3206720454563));
#15665=CARTESIAN_POINT('Ctrl Pts',(1.99443045653339,0.0362044934741236,
20.3213606129202));
#15666=CARTESIAN_POINT('Ctrl Pts',(1.99431244983192,0.0422073742234864,
20.321743458251));
#15667=CARTESIAN_POINT('Ctrl Pts',(1.99394334663295,0.0574751610892135,
20.3227194705791));
#15668=CARTESIAN_POINT('Ctrl Pts',(1.99365477777623,0.0667389388400438,
20.3233138055254));
#15669=CARTESIAN_POINT('Ctrl Pts',(1.99266731392193,0.0926377164936513,
20.3249815143098));
#15670=CARTESIAN_POINT('Ctrl Pts',(1.99182470320534,0.109266162367065,20.3260593511536));
#15671=CARTESIAN_POINT('Ctrl Pts',(1.98133160514239,0.275210751262127,20.3368886728175));
#15672=CARTESIAN_POINT('Ctrl Pts',(1.95511937340708,0.42297449776889,20.3471770189872));
#15673=CARTESIAN_POINT('Ctrl Pts',(1.8879712910272,0.649727796131091,20.3636706248955));
#15674=CARTESIAN_POINT('Ctrl Pts',(1.8578711453071,0.731367165901559,20.3697508510924));
#15675=CARTESIAN_POINT('Ctrl Pts',(1.80903980370499,0.84113364971112,20.3779395117561));
#15676=CARTESIAN_POINT('Ctrl Pts',(1.79478231045014,0.871141524241555,20.3801789723188));
#15677=CARTESIAN_POINT('Ctrl Pts',(1.77131853760501,0.917501715654971,20.3836251952925));
#15678=CARTESIAN_POINT('Ctrl Pts',(1.76262029176508,0.934103061649808,20.3848564521717));
#15679=CARTESIAN_POINT('Ctrl Pts',(1.75129434072319,0.95499787745647,20.3864002269747));
#15680=CARTESIAN_POINT('Ctrl Pts',(1.74888297380177,0.959406670330965,20.3867256244546));
#15681=CARTESIAN_POINT('Ctrl Pts',(1.74500108018825,0.966440813857832,20.3872441909134));
#15682=CARTESIAN_POINT('Ctrl Pts',(1.74354124880967,0.969071994509439,20.3874380304731));
#15683=CARTESIAN_POINT('Ctrl Pts',(1.74075380771411,0.974069353061834,20.387805915784));
#15684=CARTESIAN_POINT('Ctrl Pts',(1.73942734069538,0.976436096305653,20.3879800279408));
#15685=CARTESIAN_POINT('Ctrl Pts',(1.7363681396033,0.981868446485246,20.3883794056964));
#15686=CARTESIAN_POINT('Ctrl Pts',(1.73463211517322,0.984932174267653,20.3886044569844));
#15687=CARTESIAN_POINT('Ctrl Pts',(1.72909159917604,0.994649965661014,20.3893177444066));
#15688=CARTESIAN_POINT('Ctrl Pts',(1.72525680647491,1.00128680647013,20.3898040690614));
#15689=CARTESIAN_POINT('Ctrl Pts',(1.66205887503232,1.10922185105847,20.397702513933));
#15690=CARTESIAN_POINT('Ctrl Pts',(1.59389398038868,1.20512394107381,20.4045734217356));
#15691=CARTESIAN_POINT('Ctrl Pts',(1.45151610834776,1.37205044870794,20.4173206131978));
#15692=CARTESIAN_POINT('Ctrl Pts',(1.37950954412721,1.44442856191274,20.4231912272128));
#15693=CARTESIAN_POINT('Ctrl Pts',(1.26228600791003,1.54546122065721,20.4323767514708));
#15694=CARTESIAN_POINT('Ctrl Pts',(1.22093359471928,1.57833356897252,20.4355540437508));
#15695=CARTESIAN_POINT('Ctrl Pts',(1.15309023831855,1.62800147221333,20.4407119061672));
#15696=CARTESIAN_POINT('Ctrl Pts',(1.12742252343561,1.64588097243942,20.4426514091995));
#15697=CARTESIAN_POINT('Ctrl Pts',(1.09403386983818,1.66799111822129,20.4451642864853));
#15698=CARTESIAN_POINT('Ctrl Pts',(1.08668984643283,1.67278499889293,20.4457163938856));
#15699=CARTESIAN_POINT('Ctrl Pts',(1.07481535912721,1.68042498449573,20.446608215898));
#15700=CARTESIAN_POINT('Ctrl Pts',(1.0703045850078,1.68330160076405,20.44694679159));
#15701=CARTESIAN_POINT('Ctrl Pts',(1.06169170776679,1.68874559913378,20.4475929117929));
#15702=CARTESIAN_POINT('Ctrl Pts',(1.05759172133641,1.69131627178864,20.4479003314515));
#15703=CARTESIAN_POINT('Ctrl Pts',(1.04821632604041,1.69714718139791,20.4486029785833));
#15704=CARTESIAN_POINT('Ctrl Pts',(1.04293500640171,1.70039777478409,20.4489985575047));
#15705=CARTESIAN_POINT('Ctrl Pts',(1.02672118213745,1.71027324866801,20.4502123390152));
#15706=CARTESIAN_POINT('Ctrl Pts',(1.01574025088417,1.71681760855535,20.4510334720099));
#15707=CARTESIAN_POINT('Ctrl Pts',(0.917374144094689,1.77416728787789,20.4583822378194));
#15708=CARTESIAN_POINT('Ctrl Pts',(0.826321905547917,1.81835947875799,20.4651482406193));
#15709=CARTESIAN_POINT('Ctrl Pts',(0.605075010338799,1.90568285797185,20.4814756537266));
#15710=CARTESIAN_POINT('Ctrl Pts',(0.473003692761791,1.94268050614358,20.4911502714083));
#15711=CARTESIAN_POINT('Ctrl Pts',(0.297829671004234,1.97281581792902,20.5033462977443));
#15712=CARTESIAN_POINT('Ctrl Pts',(0.257261759115728,1.97851500154823,20.5061249824409));
#15713=CARTESIAN_POINT('Ctrl Pts',(0.194962608905754,1.98531823103365,20.5102956576953));
#15714=CARTESIAN_POINT('Ctrl Pts',(0.173342507588657,1.98732266338522,20.5117253456603));
#15715=CARTESIAN_POINT('Ctrl Pts',(0.146427683155607,1.98937537435739,20.5134796909425));
#15716=CARTESIAN_POINT('Ctrl Pts',(0.141160797328923,1.98975603462713,20.5138217830972));
#15717=CARTESIAN_POINT('Ctrl Pts',(0.132833602318584,1.99032464598095,20.5143606679976));
#15718=CARTESIAN_POINT('Ctrl Pts',(0.129774312197578,1.99052646064033,20.5145582245351));
#15719=CARTESIAN_POINT('Ctrl Pts',(0.124019357671447,1.99089277834887,20.5149290472526));
#15720=CARTESIAN_POINT('Ctrl Pts',(0.121323856507004,1.99105885847344,20.5151023973534));
#15721=CARTESIAN_POINT('Ctrl Pts',(0.11515408525755,1.9914264259324,20.5154984224195));
#15722=CARTESIAN_POINT('Ctrl Pts',(0.111679625980287,1.99162429560499,20.5157208922369));
#15723=CARTESIAN_POINT('Ctrl Pts',(0.10096244672493,1.99220650308178,20.5164054709382));
#15724=CARTESIAN_POINT('Ctrl Pts',(0.0937180333631,1.99256043840029,20.516865907245));
#15725=CARTESIAN_POINT('Ctrl Pts',(0.0335271412239369,1.99517214770625,
20.5206734701203));
#15726=CARTESIAN_POINT('Ctrl Pts',(-0.0194934466101668,1.99535889247161,
20.5239118451415));
#15727=CARTESIAN_POINT('Ctrl Pts',(-0.0844524814965636,1.99299755764539,
20.5278057348098));
#15728=CARTESIAN_POINT('Ctrl Pts',(-0.0964374010264595,1.99245359365059,
20.5285210672771));
#15729=CARTESIAN_POINT('Ctrl Pts',(-0.125170213864799,1.99088962186312,
20.5302300962095));
#15730=CARTESIAN_POINT('Ctrl Pts',(-0.141911683615441,1.98976635867055,
20.5312210529331));
#15731=CARTESIAN_POINT('Ctrl Pts',(-0.290806118425057,1.97788754877191,
20.540006184642));
#15732=CARTESIAN_POINT('Ctrl Pts',(-0.421593539049683,1.95419227140571,
20.5475487826682));
#15733=CARTESIAN_POINT('Ctrl Pts',(-0.603448879475862,1.90212436001939,
20.558744292095));
#15734=CARTESIAN_POINT('Ctrl Pts',(-0.657142043551478,1.88424817580111,
20.5621387694196));
#15735=CARTESIAN_POINT('Ctrl Pts',(-0.740710876634706,1.85241867079597,
20.5676172748485));
#15736=CARTESIAN_POINT('Ctrl Pts',(-0.771126394859202,1.83996506003104,
20.5696533426045));
#15737=CARTESIAN_POINT('Ctrl Pts',(-0.809389311769057,1.82318295781121,
20.5722745680411));
#15738=CARTESIAN_POINT('Ctrl Pts',(-0.8175352652182,1.81954478967146,20.5728361093579));
#15739=CARTESIAN_POINT('Ctrl Pts',(-0.8305572653057,1.81362376896694,20.5737395199621));
#15740=CARTESIAN_POINT('Ctrl Pts',(-0.835449015815305,1.8113755787689,20.5740801958878));
#15741=CARTESIAN_POINT('Ctrl Pts',(-0.844714031626783,1.80707197343552,
20.5747279508996));
#15742=CARTESIAN_POINT('Ctrl Pts',(-0.849089053415256,1.8050204129313,20.5750348950033));
#15743=CARTESIAN_POINT('Ctrl Pts',(-0.859006997116744,1.80032559613853,
20.5757331731187));
#15744=CARTESIAN_POINT('Ctrl Pts',(-0.864545233652749,1.79767260945412,
20.5761248426012));
#15745=CARTESIAN_POINT('Ctrl Pts',(-0.878811565815129,1.79075742074562,
20.5771383374503));
#15746=CARTESIAN_POINT('Ctrl Pts',(-0.887520857897589,1.78645700463712,
20.5777614897655));
#15747=CARTESIAN_POINT('Ctrl Pts',(-0.941189212997062,1.75946768302033,
20.5816293786211));
#15748=CARTESIAN_POINT('Ctrl Pts',(-0.985303481227544,1.73514839473152,
20.5849311254791));
#15749=CARTESIAN_POINT('Ctrl Pts',(-1.03949924452423,1.7025378852015,20.5891483143672));
#15750=CARTESIAN_POINT('Ctrl Pts',(-1.05048614523531,1.69578087522475,20.5900117981823));
#15751=CARTESIAN_POINT('Ctrl Pts',(-1.21378610460489,1.5931544266316,20.602973923477));
#15752=CARTESIAN_POINT('Ctrl Pts',(-1.35249743114452,1.47721084274037,20.6157695875899));
#15753=CARTESIAN_POINT('Ctrl Pts',(-1.50040907552634,1.31505319330308,20.6308128725818));
#15754=CARTESIAN_POINT('Ctrl Pts',(-1.52619330470094,1.28503957650769,20.6334938675085));
#15755=CARTESIAN_POINT('Ctrl Pts',(-1.56439614818339,1.23779701381252,20.6375348915239));
#15756=CARTESIAN_POINT('Ctrl Pts',(-1.57745999806839,1.22110474568321,20.6389300467152));
#15757=CARTESIAN_POINT('Ctrl Pts',(-1.59341856218805,1.20003012189358,20.6406479728508));
#15758=CARTESIAN_POINT('Ctrl Pts',(-1.59656475554194,1.19584112266082,20.6409873390003));
#15759=CARTESIAN_POINT('Ctrl Pts',(-1.60152045472826,1.18918843698579,20.6415229084615));
#15760=CARTESIAN_POINT('Ctrl Pts',(-1.60334083569106,1.18673293983441,20.6417198600094));
#15761=CARTESIAN_POINT('Ctrl Pts',(-1.60675994161487,1.18209870785874,20.6420901828289));
#15762=CARTESIAN_POINT('Ctrl Pts',(-1.60835986416405,1.17992093487049,20.6422636352126));
#15763=CARTESIAN_POINT('Ctrl Pts',(-1.61201912293962,1.17491877481369,20.6426607357722));
#15764=CARTESIAN_POINT('Ctrl Pts',(-1.61407546096146,1.17209222628186,20.6428841746914));
#15765=CARTESIAN_POINT('Ctrl Pts',(-1.6204217721527,1.16332050233936,20.6435746964268));
#15766=CARTESIAN_POINT('Ctrl Pts',(-1.62468646825637,1.15735698671764,20.6440400643391));
#15767=CARTESIAN_POINT('Ctrl Pts',(-1.66100985819509,1.10596791605636,20.6480165773126));
#15768=CARTESIAN_POINT('Ctrl Pts',(-1.69119265516384,1.05923910265295,20.6514079180133));
#15769=CARTESIAN_POINT('Ctrl Pts',(-1.79926703275165,0.875494821153208,
20.6641514014759));
#15770=CARTESIAN_POINT('Ctrl Pts',(-1.86277918839679,0.73069352628767,20.6730280035329));
#15771=CARTESIAN_POINT('Ctrl Pts',(-1.92526130054272,0.525056429637518,
20.6857407611268));
#15772=CARTESIAN_POINT('Ctrl Pts',(-1.93955662679941,0.469504650158746,
20.6891795882415));
#15773=CARTESIAN_POINT('Ctrl Pts',(-1.95831579792431,0.380956437260862,
20.6947233178837));
#15774=CARTESIAN_POINT('Ctrl Pts',(-1.96438138607436,0.34833050436023,20.6967787786271));
#15775=CARTESIAN_POINT('Ctrl Pts',(-1.97104627442373,0.30673158863422,20.6994217252029));
#15776=CARTESIAN_POINT('Ctrl Pts',(-1.97240280381546,0.297883968488223,
20.6999851073734));
#15777=CARTESIAN_POINT('Ctrl Pts',(-1.97448073489066,0.283694280298412,
20.7008907794232));
#15778=CARTESIAN_POINT('Ctrl Pts',(-1.97524012111888,0.278357827481949,
20.701231865197));
#15779=CARTESIAN_POINT('Ctrl Pts',(-1.97663906246905,0.268232952779412,
20.7018799471772));
#15780=CARTESIAN_POINT('Ctrl Pts',(-1.97728287118298,0.263445149674797,
20.7021868064467));
#15781=CARTESIAN_POINT('Ctrl Pts',(-1.9787040825883,0.252577289975345,20.7028842704407));
#15782=CARTESIAN_POINT('Ctrl Pts',(-1.97947086257799,0.246495916155972,
20.7032752076468));
#15783=CARTESIAN_POINT('Ctrl Pts',(-1.98137576863466,0.230805657671517,
20.7042855777556));
#15784=CARTESIAN_POINT('Ctrl Pts',(-1.98247201949211,0.221191940618317,
20.7049063239957));
#15785=CARTESIAN_POINT('Ctrl Pts',(-1.98877561538315,0.162095063971895,
20.7087327770602));
#15786=CARTESIAN_POINT('Ctrl Pts',(-1.99219954589707,0.112443290831706,
20.7119940994087));
#15787=CARTESIAN_POINT('Ctrl Pts',(-1.99417609501043,0.0496110026008232,
20.7161836792089));
#15788=CARTESIAN_POINT('Ctrl Pts',(-1.99445915379104,0.0364996015807987,
20.7170613192942));
#15789=CARTESIAN_POINT('Ctrl Pts',(-1.99470984809288,0.0151182046908656,
20.7184979916602));
#15790=CARTESIAN_POINT('Ctrl Pts',(-1.99475537897366,0.00684938086552253,
20.719054926578));
#15791=CARTESIAN_POINT('Ctrl Pts',(-1.9946100620358,-0.197369456595239,
20.7328422358179));
#15792=CARTESIAN_POINT('Ctrl Pts',(-1.96560205531286,-0.392193577328893,
20.7468804505239));
#15793=CARTESIAN_POINT('Ctrl Pts',(-1.89853482066006,-0.613033905744123,
20.7624479192687));
#15794=CARTESIAN_POINT('Ctrl Pts',(-1.88752054710186,-0.646151364402517,
20.7647685248146));
#15795=CARTESIAN_POINT('Ctrl Pts',(-1.8736545560808,-0.684456185077023,
20.7674228128994));
#15796=CARTESIAN_POINT('Ctrl Pts',(-1.87164272227315,-0.68993853859147,
20.7678019826271));
#15797=CARTESIAN_POINT('Ctrl Pts',(-1.86838349125195,-0.698700941296271,
20.7684067565021));
#15798=CARTESIAN_POINT('Ctrl Pts',(-1.86715148340375,-0.701986619699435,
20.7686332489318));
#15799=CARTESIAN_POINT('Ctrl Pts',(-1.86495215540258,-0.707805320815279,
20.7690338279411));
#15800=CARTESIAN_POINT('Ctrl Pts',(-1.8639883341604,-0.710339640300019,
20.7692081220512));
#15801=CARTESIAN_POINT('Ctrl Pts',(-1.86194164043274,-0.715688468442729,
20.769575598871));
#15802=CARTESIAN_POINT('Ctrl Pts',(-1.86085755515423,-0.718502481527094,
20.7697687071209));
#15803=CARTESIAN_POINT('Ctrl Pts',(-1.85793932084751,-0.726026577473509,
20.7702844750227));
#15804=CARTESIAN_POINT('Ctrl Pts',(-1.85609362848988,-0.730732204555316,
20.7706064475051));
#15805=CARTESIAN_POINT('Ctrl Pts',(-1.84720254326062,-0.75314915631005,
20.7721376799633));
#15806=CARTESIAN_POINT('Ctrl Pts',(-1.83992112339173,-0.770766639069918,
20.7733333165269));
#15807=CARTESIAN_POINT('Ctrl Pts',(-1.81894529539213,-0.819525914191428,
20.7766279722166));
#15808=CARTESIAN_POINT('Ctrl Pts',(-1.80470467243861,-0.85042697394291,
20.7786993374704));
#15809=CARTESIAN_POINT('Ctrl Pts',(-1.74995624745865,-0.961650197362051,
20.7861468898134));
#15810=CARTESIAN_POINT('Ctrl Pts',(-1.70481705014267,-1.03957635876646,
20.7913528236881));
#15811=CARTESIAN_POINT('Ctrl Pts',(-1.57339024153744,-1.23474414577757,
20.8049988208855));
#15812=CARTESIAN_POINT('Ctrl Pts',(-1.47929207904489,-1.34604527304376,
20.8134457532166));
#15813=CARTESIAN_POINT('Ctrl Pts',(-1.36524178585288,-1.45440248027703,
20.8231773110015));
#15814=CARTESIAN_POINT('Ctrl Pts',(-1.35646341169134,-1.46259314627146,
20.823923189817));
#15815=CARTESIAN_POINT('Ctrl Pts',(-1.33790159393532,-1.47960141263342,
20.8254942409664));
#15816=CARTESIAN_POINT('Ctrl Pts',(-1.32810372194146,-1.48840233332446,
20.8263200478444));
#15817=CARTESIAN_POINT('Ctrl Pts',(-1.31355905234826,-1.50120909247444,
20.8275412303598));
#15818=CARTESIAN_POINT('Ctrl Pts',(-1.308879409405,-1.50529093983634,20.8279334318287));
#15819=CARTESIAN_POINT('Ctrl Pts',(-1.30050801611161,-1.51252438774131,
20.8286338283504));
#15820=CARTESIAN_POINT('Ctrl Pts',(-1.29682366189243,-1.51568450304025,
20.8289416678805));
#15821=CARTESIAN_POINT('Ctrl Pts',(-1.28909777334214,-1.5222622992407,20.8295863492634));
#15822=CARTESIAN_POINT('Ctrl Pts',(-1.28505410194472,-1.52567740073389,
20.829923293616));
#15823=CARTESIAN_POINT('Ctrl Pts',(-1.27447089750961,-1.53454357170409,
20.8308039444234));
#15824=CARTESIAN_POINT('Ctrl Pts',(-1.26791002823204,-1.53996889534798,
20.8313486934817));
#15825=CARTESIAN_POINT('Ctrl Pts',(-1.23903432563877,-1.56353721434392,
20.8337412327279));
#15826=CARTESIAN_POINT('Ctrl Pts',(-1.21636429349494,-1.58123762998937,
20.8356066694672));
#15827=CARTESIAN_POINT('Ctrl Pts',(-1.15560645527117,-1.62659655852417,
20.8405756204348));
#15828=CARTESIAN_POINT('Ctrl Pts',(-1.11691054209888,-1.65340645121867,
20.8437100519143));
#15829=CARTESIAN_POINT('Ctrl Pts',(-0.91038837707266,-1.78593242263189,
20.8602822007481));
#15830=CARTESIAN_POINT('Ctrl Pts',(-0.728463023318176,-1.86753483391751,
20.874504795066));
#15831=CARTESIAN_POINT('Ctrl Pts',(-0.50650362552567,-1.92964204842676,
20.8900137602047));
#15832=CARTESIAN_POINT('Ctrl Pts',(-0.475287560147974,-1.93756713064289,
20.8921513836738));
#15833=CARTESIAN_POINT('Ctrl Pts',(-0.438336246375368,-1.94600137787034,
20.8946201474641));
#15834=CARTESIAN_POINT('Ctrl Pts',(-0.432775812642055,-1.94724552264663,
20.8949900164422));
#15835=CARTESIAN_POINT('Ctrl Pts',(-0.4238234159628,-1.94920837654142,20.895582807777));
#15836=CARTESIAN_POINT('Ctrl Pts',(-0.420434827394113,-1.9499420861806,
20.8958065644607));
#15837=CARTESIAN_POINT('Ctrl Pts',(-0.414398269748004,-1.95123267656597,
20.8962040452472));
#15838=CARTESIAN_POINT('Ctrl Pts',(-0.411751065246293,-1.95179300764166,
20.8963779656506));
#15839=CARTESIAN_POINT('Ctrl Pts',(-0.406128125515926,-1.9529712605796,
20.8967465648302));
#15840=CARTESIAN_POINT('Ctrl Pts',(-0.40315212482149,-1.95358776704287,
20.8969411617546));
#15841=CARTESIAN_POINT('Ctrl Pts',(-0.395119347344425,-1.95523269514151,
20.8974651271883));
#15842=CARTESIAN_POINT('Ctrl Pts',(-0.390059926392017,-1.95624830889371,
20.897793769896));
#15843=CARTESIAN_POINT('Ctrl Pts',(-0.365121032815253,-1.96115387337369,
20.8994072014873));
#15844=CARTESIAN_POINT('Ctrl Pts',(-0.345186175856508,-1.96476066347969,
20.9006765342936));
#15845=CARTESIAN_POINT('Ctrl Pts',(-0.288619592715493,-1.97410761441455,
20.9042297547318));
#15846=CARTESIAN_POINT('Ctrl Pts',(-0.251876475528161,-1.97913130842792,
20.9064804421477));
#15847=CARTESIAN_POINT('Ctrl Pts',(-0.116588878985594,-1.9937993041374,
20.9146271748516));
#15848=CARTESIAN_POINT('Ctrl Pts',(-0.0175012433060566,-1.99712914866581,
20.9203279107129));
#15849=CARTESIAN_POINT('Ctrl Pts',(0.225683976457441,-1.98719362009591,
20.93445414833));
#15850=CARTESIAN_POINT('Ctrl Pts',(0.368849238669334,-1.96565853077005,
20.942916317776));
#15851=CARTESIAN_POINT('Ctrl Pts',(0.520833112324559,-1.9255973166994,20.9527283576347));
#15852=CARTESIAN_POINT('Ctrl Pts',(0.533206745406368,-1.92220777008531,
20.9535330174232));
#15853=CARTESIAN_POINT('Ctrl Pts',(0.55152045498289,-1.91700060571973,20.954732957018));
#15854=CARTESIAN_POINT('Ctrl Pts',(0.557486293815827,-1.91527417499024,
20.9551252709088));
#15855=CARTESIAN_POINT('Ctrl Pts',(0.568087184320572,-1.91215269859454,
20.9558249630875));
#15856=CARTESIAN_POINT('Ctrl Pts',(0.572725424275385,-1.91076858343534,
20.9561319824491));
#15857=CARTESIAN_POINT('Ctrl Pts',(0.58247486618747,-1.90782052692217,20.9567792043199));
#15858=CARTESIAN_POINT('Ctrl Pts',(0.587584904571797,-1.90625289814548,
20.9571195255037));
#15859=CARTESIAN_POINT('Ctrl Pts',(0.601041792041376,-1.90206541951755,
20.9580186406849));
#15860=CARTESIAN_POINT('Ctrl Pts',(0.609377741369181,-1.89941118775901,
20.9585785594084));
#15861=CARTESIAN_POINT('Ctrl Pts',(0.647225144674249,-1.8870854871126,20.9611344314811));
#15862=CARTESIAN_POINT('Ctrl Pts',(0.676524347806539,-1.87678092742672,
20.963151141521));
#15863=CARTESIAN_POINT('Ctrl Pts',(0.754480109971616,-1.84730117953563,
20.9686235246129));
#15864=CARTESIAN_POINT('Ctrl Pts',(0.802640332179603,-1.82689068730709,
20.9721184201241));
#15865=CARTESIAN_POINT('Ctrl Pts',(0.941846148511684,-1.76132729666965,
20.9825559635148));
#15866=CARTESIAN_POINT('Ctrl Pts',(1.03030424240772,-1.71108675512941,20.9896351315254));
#15867=CARTESIAN_POINT('Ctrl Pts',(1.21290803591734,-1.58806450054347,21.0049958740511));
#15868=CARTESIAN_POINT('Ctrl Pts',(1.30517895326536,-1.51314563847197,21.0132515933771));
#15869=CARTESIAN_POINT('Ctrl Pts',(1.39573191626292,-1.42513800682212,21.0214969120381));
#15870=CARTESIAN_POINT('Ctrl Pts',(1.4011796000356,-1.41978225569463,21.0219935012636));
#15871=CARTESIAN_POINT('Ctrl Pts',(1.4090899295764,-1.41191554244734,21.0227151990423));
#15872=CARTESIAN_POINT('Ctrl Pts',(1.41157683404156,-1.40942923579045,21.0229421823796));
#15873=CARTESIAN_POINT('Ctrl Pts',(1.41597030656416,-1.40501352688308,21.0233433206312));
#15874=CARTESIAN_POINT('Ctrl Pts',(1.41787952821951,-1.40308679831506,21.0235176850901));
#15875=CARTESIAN_POINT('Ctrl Pts',(1.42190022054802,-1.39901264994102,21.023884975909));
#15876=CARTESIAN_POINT('Ctrl Pts',(1.42401075449825,-1.39686434676299,21.0240778290937));
#15877=CARTESIAN_POINT('Ctrl Pts',(1.42963789061094,-1.39111050255342,21.0245921935277));
#15878=CARTESIAN_POINT('Ctrl Pts',(1.43314574539413,-1.38749637922964,21.0249130241341));
#15879=CARTESIAN_POINT('Ctrl Pts',(1.44972671799818,-1.37028312579255,21.0264306411278));
#15880=CARTESIAN_POINT('Ctrl Pts',(1.46262072175605,-1.35651173559781,21.0276140957702));
#15881=CARTESIAN_POINT('Ctrl Pts',(1.49788040817889,-1.31776539128471,21.0308666699606));
#15882=CARTESIAN_POINT('Ctrl Pts',(1.51981562555559,-1.29240553945169,21.0329089855605));
#15883=CARTESIAN_POINT('Ctrl Pts',(1.59705604680829,-1.19841810458524,21.0402218338353));
#15884=CARTESIAN_POINT('Ctrl Pts',(1.6484401232475,-1.12669484232694,21.045327754139));
#15885=CARTESIAN_POINT('Ctrl Pts',(1.77290117628542,-0.926133810089712,
21.0590172826626));
#15886=CARTESIAN_POINT('Ctrl Pts',(1.83665920948988,-0.792198367766934,
21.0676016713935));
#15887=CARTESIAN_POINT('Ctrl Pts',(1.88920826161322,-0.640377274174271,
21.0775399959862));
#15888=CARTESIAN_POINT('Ctrl Pts',(1.89327240423629,-0.628259898985119,
21.0783342255829));
#15889=CARTESIAN_POINT('Ctrl Pts',(1.90113095664229,-0.604060432197417,
21.0799229024063));
#15890=CARTESIAN_POINT('Ctrl Pts',(1.90492731057444,-0.591979602429236,
21.0807172436709));
#15891=CARTESIAN_POINT('Ctrl Pts',(1.91040418666343,-0.573952586946305,
21.0819047266506));
#15892=CARTESIAN_POINT('Ctrl Pts',(1.91217257300423,-0.568033254430364,
21.0822949924822));
#15893=CARTESIAN_POINT('Ctrl Pts',(1.91527628550666,-0.557465428217436,
21.0829923908085));
#15894=CARTESIAN_POINT('Ctrl Pts',(1.916622262665,-0.552820092854428,21.0832991730387));
#15895=CARTESIAN_POINT('Ctrl Pts',(1.91942506882256,-0.543013561396558,
21.0839472989757));
#15896=CARTESIAN_POINT('Ctrl Pts',(1.92087800236137,-0.537851300828639,
21.0842887667269));
#15897=CARTESIAN_POINT('Ctrl Pts',(1.92466755075472,-0.524175844298953,
21.0851941488291));
#15898=CARTESIAN_POINT('Ctrl Pts',(1.92696847776183,-0.515652962980549,
21.0857592163292));
#15899=CARTESIAN_POINT('Ctrl Pts',(1.93731611958467,-0.476287544190206,
21.0883731017618));
#15900=CARTESIAN_POINT('Ctrl Pts',(1.94467902536546,-0.445271675272963,
21.0904438463828));
#15901=CARTESIAN_POINT('Ctrl Pts',(1.96254928289318,-0.361063408537297,
21.0960999470022));
#15902=CARTESIAN_POINT('Ctrl Pts',(1.97163577217638,-0.307600343180028,
21.0997278388892));
#15903=CARTESIAN_POINT('Ctrl Pts',(1.99165227990602,-0.151581874465548,
21.1104140314671));
#15904=CARTESIAN_POINT('Ctrl Pts',(1.99682328000519,-0.0484705651595451,
21.1176078296984));
#15905=CARTESIAN_POINT('Ctrl Pts',(1.99379232062132,0.0622841673958293,
21.125335662298));
#15906=CARTESIAN_POINT('Ctrl Pts',(1.99353639737591,0.0699983432818144,
21.1258738519295));
#15907=CARTESIAN_POINT('Ctrl Pts',(1.98909753291257,0.183852493546946,21.1338148660226));
#15908=CARTESIAN_POINT('Ctrl Pts',(1.9764871354067,0.289508541748631,21.1411657672692));
#15909=CARTESIAN_POINT('Ctrl Pts',(1.95397852476055,0.401318295830868,21.148615230746));
#15910=CARTESIAN_POINT('Ctrl Pts',(1.95239367482064,0.408958913811939,21.1491225711915));
#15911=CARTESIAN_POINT('Ctrl Pts',(1.95002321099888,0.420059068435008,21.1498569194152));
#15912=CARTESIAN_POINT('Ctrl Pts',(1.9492731648176,0.423526001336987,21.1500858947915));
#15913=CARTESIAN_POINT('Ctrl Pts',(1.94793230925023,0.429644809430461,21.1504893119248));
#15914=CARTESIAN_POINT('Ctrl Pts',(1.94734532519913,0.432297499965828,21.1506639713979));
#15915=CARTESIAN_POINT('Ctrl Pts',(1.94609970927008,0.437872650808429,21.1510305523355));
#15916=CARTESIAN_POINT('Ctrl Pts',(1.9454399146961,0.440794822275182,21.1512224057161));
#15917=CARTESIAN_POINT('Ctrl Pts',(1.9436689804174,0.448556701140902,21.1517312705918));
#15918=CARTESIAN_POINT('Ctrl Pts',(1.94254633909445,0.453393803799022,21.1520476267737));
#15919=CARTESIAN_POINT('Ctrl Pts',(1.93724556342371,0.47585202186095,21.1535131104189));
#15920=CARTESIAN_POINT('Ctrl Pts',(1.93284548940349,0.493420601163006,21.1546499918112));
#15921=CARTESIAN_POINT('Ctrl Pts',(1.88853711373006,0.660637459966116,21.1654007722305));
#15922=CARTESIAN_POINT('Ctrl Pts',(1.83156112754935,0.80524075626327,21.1741895899601));
#15923=CARTESIAN_POINT('Ctrl Pts',(1.69804571279293,1.05452216612797,21.1906474539205));
#15924=CARTESIAN_POINT('Ctrl Pts',(1.62698926676855,1.16115251718609,21.1982054511876));
#15925=CARTESIAN_POINT('Ctrl Pts',(1.53800063199992,1.27033504213925,21.2069966860118));
#15926=CARTESIAN_POINT('Ctrl Pts',(1.52967688789764,1.28034591777179,21.207813127801));
#15927=CARTESIAN_POINT('Ctrl Pts',(1.51725793794711,1.29498807506561,21.2090230532045));
#15928=CARTESIAN_POINT('Ctrl Pts',(1.5132381278138,1.29968308904885,21.2094134471023));
#15929=CARTESIAN_POINT('Ctrl Pts',(1.50602527257307,1.30802865501071,21.210111782075));
#15930=CARTESIAN_POINT('Ctrl Pts',(1.50284059824372,1.31168640289811,21.2104193751378));
#15931=CARTESIAN_POINT('Ctrl Pts',(1.4961430018652,1.3193224959066,21.2110647405154));
#15932=CARTESIAN_POINT('Ctrl Pts',(1.49262748267046,1.32329850272519,21.2114026198667));
#15933=CARTESIAN_POINT('Ctrl Pts',(1.48338819313383,1.33366435904992,21.2122883855493));
#15934=CARTESIAN_POINT('Ctrl Pts',(1.47763904447411,1.34003134461906,21.212837336993));
#15935=CARTESIAN_POINT('Ctrl Pts',(1.45201974401431,1.36803850222311,21.2152740314479));
#15936=CARTESIAN_POINT('Ctrl Pts',(1.43171486662948,1.38927429546161,21.2171802351394));
#15937=CARTESIAN_POINT('Ctrl Pts',(1.37669986162268,1.44432426930366,21.2222833051189));
#15938=CARTESIAN_POINT('Ctrl Pts',(1.3412157213491,1.47733369619487,21.225513191772));
#15939=CARTESIAN_POINT('Ctrl Pts',(1.14722572461027,1.64504095987245,21.2428521327635));
#15940=CARTESIAN_POINT('Ctrl Pts',(0.969608390870513,1.75559930403204,21.2578261174242));
#15941=CARTESIAN_POINT('Ctrl Pts',(0.758076266883175,1.84521612858551,21.2731232882376));
#15942=CARTESIAN_POINT('Ctrl Pts',(0.737877424147387,1.85338587215017,21.2745587947379));
#15943=CARTESIAN_POINT('Ctrl Pts',(0.712426568041568,1.8631978082461,21.2763326532876));
#15944=CARTESIAN_POINT('Ctrl Pts',(0.707297145329823,1.86515104949738,21.2766884023554));
#15945=CARTESIAN_POINT('Ctrl Pts',(0.699216112055657,1.86819010836508,21.2772460241247));
#15946=CARTESIAN_POINT('Ctrl Pts',(0.696269932511647,1.86929014167604,21.2774487308661));
#15947=CARTESIAN_POINT('Ctrl Pts',(0.690860328089097,1.87129539550569,21.2778198302121));
#15948=CARTESIAN_POINT('Ctrl Pts',(0.688397740493991,1.87220271370261,21.2779883454065));
#15949=CARTESIAN_POINT('Ctrl Pts',(0.682866618728271,1.87422821699942,21.2783659072095));
#15950=CARTESIAN_POINT('Ctrl Pts',(0.679797134702418,1.87534372433257,21.2785747925397));
#15951=CARTESIAN_POINT('Ctrl Pts',(0.673378296120105,1.87765861892346,21.2790102967682));
#15952=CARTESIAN_POINT('Ctrl Pts',(0.670028440402363,1.87885659602409,21.2792368325837));
#15953=CARTESIAN_POINT('Ctrl Pts',(0.661295213569867,1.88195345024514,21.2798255284858));
#15954=CARTESIAN_POINT('Ctrl Pts',(0.655906819036435,1.88383820828055,21.2801868837038));
#15955=CARTESIAN_POINT('Ctrl Pts',(0.639905861027281,1.88935806265989,21.2812546084325));
#15956=CARTESIAN_POINT('Ctrl Pts',(0.629270445442786,1.89292686584507,21.2819573690833));
#15957=CARTESIAN_POINT('Ctrl Pts',(0.492998142387599,1.9373787206482,21.2908804117389));
#15958=CARTESIAN_POINT('Ctrl Pts',(0.363612019889337,1.96577718373651,21.2984846259256));
#15959=CARTESIAN_POINT('Ctrl Pts',(0.0807314232905281,1.99895350571148,
21.3150051523248));
#15960=CARTESIAN_POINT('Ctrl Pts',(-0.0724047272334247,1.99927015113472,
21.323913934323));
#15961=CARTESIAN_POINT('Ctrl Pts',(-0.236652603846043,1.98070277337642,
21.3342347931947));
#15962=CARTESIAN_POINT('Ctrl Pts',(-0.249222069166602,1.97916049875238,
21.3350291622058));
#15963=CARTESIAN_POINT('Ctrl Pts',(-0.267900292353994,1.97668792755281,
21.3362166786983));
#15964=CARTESIAN_POINT('Ctrl Pts',(-0.274020957726963,1.97584873988561,
21.336606950056));
#15965=CARTESIAN_POINT('Ctrl Pts',(-0.284926072165954,1.97430192396778,
21.3373043545567));
#15966=CARTESIAN_POINT('Ctrl Pts',(-0.289712052823314,1.97360529978933,
21.3376111374119));
#15967=CARTESIAN_POINT('Ctrl Pts',(-0.299799455714704,1.9720995432572,21.338259260838));
#15968=CARTESIAN_POINT('Ctrl Pts',(-0.30510023537524,1.97128642454866,21.3386007254386));
#15969=CARTESIAN_POINT('Ctrl Pts',(-0.319117912143108,1.96907827446178,
21.3395060903192));
#15970=CARTESIAN_POINT('Ctrl Pts',(-0.327828861419671,1.96764674834489,
21.3400711436698));
#15971=CARTESIAN_POINT('Ctrl Pts',(-0.367945671243436,1.96078030631115,
21.3426848677974));
#15972=CARTESIAN_POINT('Ctrl Pts',(-0.399226427436191,1.95465124531873,
21.3447554619619));
#15973=CARTESIAN_POINT('Ctrl Pts',(-0.483275315968002,1.93608131477752,
21.350411048117));
#15974=CARTESIAN_POINT('Ctrl Pts',(-0.535702070232386,1.92223523459837,
21.3540385665032));
#15975=CARTESIAN_POINT('Ctrl Pts',(-0.681220041163365,1.87738789108652,
21.3643833192158));
#15976=CARTESIAN_POINT('Ctrl Pts',(-0.772679098247907,1.84163247082297,
21.3712174510201));
#15977=CARTESIAN_POINT('Ctrl Pts',(-0.893370244615706,1.78387069910344,
21.3805522947377));
#15978=CARTESIAN_POINT('Ctrl Pts',(-0.925190250563382,1.76757691118878,
21.3830441283775));
#15979=CARTESIAN_POINT('Ctrl Pts',(-1.02954274245299,1.71055173330923,21.3912898174433));
#15980=CARTESIAN_POINT('Ctrl Pts',(-1.09997358277768,1.66613538522129,21.3969795042038));
#15981=CARTESIAN_POINT('Ctrl Pts',(-1.17377049805303,1.6128705706331,21.4029241522094));
#15982=CARTESIAN_POINT('Ctrl Pts',(-1.18008167613837,1.60825865527067,21.403432374985));
#15983=CARTESIAN_POINT('Ctrl Pts',(-1.1892192744445,1.60149857301408,21.4041677601809));
#15984=CARTESIAN_POINT('Ctrl Pts',(-1.19206722919607,1.5993798434493,21.404396897909));
#15985=CARTESIAN_POINT('Ctrl Pts',(-1.19704267703937,1.59565769785177,21.4047970745962));
#15986=CARTESIAN_POINT('Ctrl Pts',(-1.19917263184068,1.59405760835466,21.4049683441796));
#15987=CARTESIAN_POINT('Ctrl Pts',(-1.20362893308726,1.5906959070808,21.4053265767195));
#15988=CARTESIAN_POINT('Ctrl Pts',(-1.20595461654526,1.58893346005113,21.4055134790407));
#15989=CARTESIAN_POINT('Ctrl Pts',(-1.2119853985493,1.58434235094546,21.4059980224421));
#15990=CARTESIAN_POINT('Ctrl Pts',(-1.21568449108141,1.58150577314775,21.40629511083));
#15991=CARTESIAN_POINT('Ctrl Pts',(-1.22380616509327,1.57523249137289,21.4069472233459));
#15992=CARTESIAN_POINT('Ctrl Pts',(-1.22822430173893,1.57179006167214,21.4073018561508));
#15993=CARTESIAN_POINT('Ctrl Pts',(-1.24121725117295,1.56157825514952,21.4083446316888));
#15994=CARTESIAN_POINT('Ctrl Pts',(-1.24975117467722,1.55475687007307,21.4090293630749));
#15995=CARTESIAN_POINT('Ctrl Pts',(-1.27968530665324,1.53042401491538,21.4114322802541));
#15996=CARTESIAN_POINT('Ctrl Pts',(-1.30077794136407,1.51253729155804,21.4131274972556));
#15997=CARTESIAN_POINT('Ctrl Pts',(-1.40638286874237,1.41913976159621,21.4216657757238));
#15998=CARTESIAN_POINT('Ctrl Pts',(-1.48472803919417,1.33695835454334,21.4281796005928));
#15999=CARTESIAN_POINT('Ctrl Pts',(-1.64581356421066,1.1362500414249,21.4431171330949));
#16000=CARTESIAN_POINT('Ctrl Pts',(-1.72351187809355,1.01452686542029,21.4515594516503));
#16001=CARTESIAN_POINT('Ctrl Pts',(-1.79312880497959,0.874003190847164,
21.4613493612533));
#16002=CARTESIAN_POINT('Ctrl Pts',(-1.79871842421699,0.862441016507123,
21.4621548235912));
#16003=CARTESIAN_POINT('Ctrl Pts',(-1.80684603313699,0.845206234413241,
21.4633557314999));
#16004=CARTESIAN_POINT('Ctrl Pts',(-1.80946986351918,0.839574283640657,
21.4637482040969));
#16005=CARTESIAN_POINT('Ctrl Pts',(-1.81409102551261,0.829532848004732,
21.4644480744782));
#16006=CARTESIAN_POINT('Ctrl Pts',(-1.81609870769831,0.825128158520763,
21.4647551126643));
#16007=CARTESIAN_POINT('Ctrl Pts',(-1.82028894971991,0.815845731621414,
21.4654022666595));
#16008=CARTESIAN_POINT('Ctrl Pts',(-1.82246797844415,0.810966451159789,
21.4657425007329));
#16009=CARTESIAN_POINT('Ctrl Pts',(-1.82816011398378,0.798081817633999,
21.4666411397859));
#16010=CARTESIAN_POINT('Ctrl Pts',(-1.83164021465107,0.790062092519377,
21.4672006673437));
#16011=CARTESIAN_POINT('Ctrl Pts',(-1.84721845289589,0.753506604056222,
21.4697521872498));
#16012=CARTESIAN_POINT('Ctrl Pts',(-1.85870265210972,0.724715451980229,
21.4717648499011));
#16013=CARTESIAN_POINT('Ctrl Pts',(-1.88769758749171,0.64679579237316,21.477223555745));
#16014=CARTESIAN_POINT('Ctrl Pts',(-1.90395925273267,0.597231404802596,
21.4807085808336));
#16015=CARTESIAN_POINT('Ctrl Pts',(-1.9690839704532,0.368885002774501,21.4968136172544));
#16016=CARTESIAN_POINT('Ctrl Pts',(-1.99482013392882,0.184503243835848,
21.5100601477585));
#16017=CARTESIAN_POINT('Ctrl Pts',(-1.99474985647505,-0.000756698609384009,
21.5225779118923));
#16018=CARTESIAN_POINT('',(-1.99474917376081,0.00181556617883987,22.3209548813952));
#16019=CARTESIAN_POINT('Ctrl Pts',(-1.9947498118588,-0.000866365563652432,
21.5209548813952));
#16020=CARTESIAN_POINT('Ctrl Pts',(-1.99472877578325,-0.0493005479633061,
21.524063142322));
#16021=CARTESIAN_POINT('Ctrl Pts',(-1.99294386346395,-0.0976946259360165,
21.5271714032488));
#16022=CARTESIAN_POINT('Ctrl Pts',(-1.989402859888,-0.145958293938546,21.5302796641756));
#16023=CARTESIAN_POINT('Ctrl Pts',(-1.98432871476336,-0.215118590007016,
21.5347337028936));
#16024=CARTESIAN_POINT('Ctrl Pts',(-1.97563375315188,-0.284150938386916,
21.5391877416116));
#16025=CARTESIAN_POINT('Ctrl Pts',(-1.96333095162286,-0.352645908667128,
21.5436417803296));
#16026=CARTESIAN_POINT('Ctrl Pts',(-1.95104664311606,-0.421037920364781,
21.5480891239353));
#16027=CARTESIAN_POINT('Ctrl Pts',(-1.93516534412893,-0.488893679248685,
21.5525364675411));
#16028=CARTESIAN_POINT('Ctrl Pts',(-1.91575188852089,-0.555807758247975,
21.5569838111469));
#16029=CARTESIAN_POINT('Ctrl Pts',(-1.89636131938151,-0.622642952426204,
21.5614259117917));
#16030=CARTESIAN_POINT('Ctrl Pts',(-1.87344699969841,-0.688538203701612,
21.5658680124364));
#16031=CARTESIAN_POINT('Ctrl Pts',(-1.84712466402983,-0.753098956334872,
21.5703101130812));
#16032=CARTESIAN_POINT('Ctrl Pts',(-1.8208189326072,-0.817618983759374,
21.5747494116293));
#16033=CARTESIAN_POINT('Ctrl Pts',(-1.79110963429111,-0.880805730216488,
21.5791887101773));
#16034=CARTESIAN_POINT('Ctrl Pts',(-1.75816163279785,-0.942281929922031,
21.5836280087253));
#16035=CARTESIAN_POINT('Ctrl Pts',(-1.72522321924043,-1.00374023992769,
21.5880660154284));
#16036=CARTESIAN_POINT('Ctrl Pts',(-1.68904820459707,-1.06348856006338,
21.5925040221314));
#16037=CARTESIAN_POINT('Ctrl Pts',(-1.64984788249783,-1.1211732814857,21.5969420288345));
#16038=CARTESIAN_POINT('Ctrl Pts',(-1.61064564779819,-1.17886081737014,
21.6013802520698));
#16039=CARTESIAN_POINT('Ctrl Pts',(-1.56841808973195,-1.2344841510782,21.6058184753051));
#16040=CARTESIAN_POINT('Ctrl Pts',(-1.52341939076268,-1.28771927156048,
21.6102566985404));
#16041=CARTESIAN_POINT('Ctrl Pts',(-1.47837302063779,-1.34101078877803,
21.6146996235834));
#16042=CARTESIAN_POINT('Ctrl Pts',(-1.43054996672539,-1.39190866828392,
21.6191425486265));
#16043=CARTESIAN_POINT('Ctrl Pts',(-1.38024358553733,-1.44012333051133,
21.6235854736695));
#16044=CARTESIAN_POINT('Ctrl Pts',(-1.32990783844394,-1.48836613762162,
21.6280309922308));
#16045=CARTESIAN_POINT('Ctrl Pts',(-1.27708624961189,-1.5339222900707,21.632476510792));
#16046=CARTESIAN_POINT('Ctrl Pts',(-1.22210568159205,-1.57654218640683,
21.6369220293533));
#16047=CARTESIAN_POINT('Ctrl Pts',(-1.16702917094622,-1.61923645565182,
21.6413753054685));
#16048=CARTESIAN_POINT('Ctrl Pts',(-1.10978656263195,-1.65898396146875,
21.6458285815837));
#16049=CARTESIAN_POINT('Ctrl Pts',(-1.05073345595025,-1.69557859359183,
21.650281857699));
#16050=CARTESIAN_POINT('Ctrl Pts',(-1.01911221549959,-1.71517396674983,
21.6526664589968));
#16051=CARTESIAN_POINT('Ctrl Pts',(-0.986972274373024,-1.73386610538307,
21.6550510602946));
#16052=CARTESIAN_POINT('Ctrl Pts',(-0.954370742035125,-1.75162897020097,
21.6574356615924));
#16053=CARTESIAN_POINT('Ctrl Pts',(-0.893476500539938,-1.78480704811022,
21.6618897003104));
#16054=CARTESIAN_POINT('Ctrl Pts',(-0.830729479086657,-1.81487162492435,
21.6663437390284));
#16055=CARTESIAN_POINT('Ctrl Pts',(-0.766480935041935,-1.84161194031675,
21.6707977777464));
#16056=CARTESIAN_POINT('Ctrl Pts',(-0.702328966541362,-1.86831206086041,
21.6752451213521));
#16057=CARTESIAN_POINT('Ctrl Pts',(-0.636680403370564,-1.89169765097144,
21.6796924649579));
#16058=CARTESIAN_POINT('Ctrl Pts',(-0.569911213208941,-1.91160371718584,
21.6841398085636));
#16059=CARTESIAN_POINT('Ctrl Pts',(-0.503220737059332,-1.93148631619431,
21.6885819092084));
#16060=CARTESIAN_POINT('Ctrl Pts',(-0.435412724688168,-1.94789739920132,
21.6930240098532));
#16061=CARTESIAN_POINT('Ctrl Pts',(-0.366881561862411,-1.96072065375601,
21.697466110498));
#16062=CARTESIAN_POINT('Ctrl Pts',(-0.298393628797768,-1.97353581934492,
21.701905409046));
#16063=CARTESIAN_POINT('Ctrl Pts',(-0.229183930300444,-1.98276755635265,
21.706344707594));
#16064=CARTESIAN_POINT('Ctrl Pts',(-0.159658914585722,-1.98835021902413,
21.7107840061421));
#16065=CARTESIAN_POINT('Ctrl Pts',(-0.0901541307927484,-1.99393125712935,
21.7152220128451));
#16066=CARTESIAN_POINT('Ctrl Pts',(-0.0203346996770724,-1.99586528974961,
21.7196600195482));
#16067=CARTESIAN_POINT('Ctrl Pts',(0.04938768259161,-1.99413851557715,21.7240980262513));
#16068=CARTESIAN_POINT('Ctrl Pts',(0.119113466645032,-1.99241165715464,
21.7285362494866));
#16069=CARTESIAN_POINT('Ctrl Pts',(0.188741703099653,-1.9870236518403,21.7329744727219));
#16070=CARTESIAN_POINT('Ctrl Pts',(0.257862359831198,-1.97801278203208,
21.7374126959572));
#16071=CARTESIAN_POINT('Ctrl Pts',(0.327056242270525,-1.96899236620172,
21.7418556210002));
#16072=CARTESIAN_POINT('Ctrl Pts',(0.395740985292811,-1.95634148877475,
21.7462985460433));
#16073=CARTESIAN_POINT('Ctrl Pts',(0.463514296007958,-1.94015000963746,
21.7507414710863));
#16074=CARTESIAN_POINT('Ctrl Pts',(0.531327168794214,-1.92394907886734,
21.7551869896475));
#16075=CARTESIAN_POINT('Ctrl Pts',(0.598227080627999,-1.90420357129347,
21.7596325082088));
#16076=CARTESIAN_POINT('Ctrl Pts',(0.663827209953822,-1.88105316188164,
21.7640780267701));
#16077=CARTESIAN_POINT('Ctrl Pts',(0.729541813336523,-1.85786235435916,
21.7685313028853));
#16078=CARTESIAN_POINT('Ctrl Pts',(0.793951654136786,-1.83125497129768,
21.7729845790005));
#16079=CARTESIAN_POINT('Ctrl Pts',(0.856690917923904,-1.80141839494513,
21.7774378551158));
#16080=CARTESIAN_POINT('Ctrl Pts',(0.890285989502041,-1.78544176631252,
21.7798224564136));
#16081=CARTESIAN_POINT('Ctrl Pts',(0.923402490549147,-1.76854001431263,
21.7822070577113));
#16082=CARTESIAN_POINT('Ctrl Pts',(0.955987608595106,-1.75074705617705,
21.7845916590091));
#16083=CARTESIAN_POINT('Ctrl Pts',(1.016851190923,-1.71751276895384,21.7890456977271));
#16084=CARTESIAN_POINT('Ctrl Pts',(1.07610019080042,-1.68103505666552,21.7934997364451));
#16085=CARTESIAN_POINT('Ctrl Pts',(1.13336723499775,-1.64149513344802,21.7979537751631));
#16086=CARTESIAN_POINT('Ctrl Pts',(1.19054819792991,-1.60201464487856,21.8024011187688));
#16087=CARTESIAN_POINT('Ctrl Pts',(1.24575271854935,-1.55948135703953,21.8068484623746));
#16088=CARTESIAN_POINT('Ctrl Pts',(1.29863852400445,-1.51412203816982,21.8112958059804));
#16089=CARTESIAN_POINT('Ctrl Pts',(1.35146198253106,-1.46881619327457,21.8157379066251));
#16090=CARTESIAN_POINT('Ctrl Pts',(1.40197178521234,-1.42069125150546,21.8201800072699));
#16091=CARTESIAN_POINT('Ctrl Pts',(1.44985661635391,-1.37001582272425,21.8246221079147));
#16092=CARTESIAN_POINT('Ctrl Pts',(1.49771124153186,-1.31937236022801,21.8290614064627));
#16093=CARTESIAN_POINT('Ctrl Pts',(1.54294384452758,-1.26618195732962,21.8335007050108));
#16094=CARTESIAN_POINT('Ctrl Pts',(1.58527917729993,-1.21075079703433,21.8379400035588));
#16095=CARTESIAN_POINT('Ctrl Pts',(1.62760219040385,-1.15533576732006,21.8423780102618));
#16096=CARTESIAN_POINT('Ctrl Pts',(1.66702930999776,-1.09768166352848,21.8468160169649));
#16097=CARTESIAN_POINT('Ctrl Pts',(1.70332603534491,-1.03812715011996,21.851254023668));
#16098=CARTESIAN_POINT('Ctrl Pts',(1.73962453162478,-0.978569731021327,
21.8556922469033));
#16099=CARTESIAN_POINT('Ctrl Pts',(1.77279207768687,-0.917112137501394,
21.8601304701386));
#16100=CARTESIAN_POINT('Ctrl Pts',(1.80263886349575,-0.854119833697089,
21.8645686933739));
#16101=CARTESIAN_POINT('Ctrl Pts',(1.83251726868036,-0.791060796498634,
21.8690116184169));
#16102=CARTESIAN_POINT('Ctrl Pts',(1.85906768185369,-0.726464247178823,
21.87345454346));
#16103=CARTESIAN_POINT('Ctrl Pts',(1.88214784725472,-0.660717067718424,
21.877897468503));
#16104=CARTESIAN_POINT('Ctrl Pts',(1.9052414854983,-0.594931508923145,21.8823429870642));
#16105=CARTESIAN_POINT('Ctrl Pts',(1.92486070625319,-0.527994453044673,
21.8867885056255));
#16106=CARTESIAN_POINT('Ctrl Pts',(1.94091351252505,-0.460306744896983,
21.8912340241867));
#16107=CARTESIAN_POINT('Ctrl Pts',(1.95699433139197,-0.392500919809078,
21.895687300302));
#16108=CARTESIAN_POINT('Ctrl Pts',(1.96949622475257,-0.323942309207001,
21.9001405764172));
#16109=CARTESIAN_POINT('Ctrl Pts',(1.97837867937509,-0.255039925294245,
21.9045938525325));
#16110=CARTESIAN_POINT('Ctrl Pts',(1.98313497839465,-0.218144680119672,
21.9069784538303));
#16111=CARTESIAN_POINT('Ctrl Pts',(1.98685436922854,-0.181150923968879,
21.9093630551281));
#16112=CARTESIAN_POINT('Ctrl Pts',(1.98953677474743,-0.144121422514414,
21.9117476564259));
#16113=CARTESIAN_POINT('Ctrl Pts',(1.99454706223212,-0.0749564709830513,
21.9162016951439));
#16114=CARTESIAN_POINT('Ctrl Pts',(1.99595626162719,-0.00539296304012958,
21.9206557338619));
#16115=CARTESIAN_POINT('Ctrl Pts',(1.99371782986213,0.0641621180278543,
21.9251097725799));
#16116=CARTESIAN_POINT('Ctrl Pts',(1.99148276280781,0.133612647002035,21.9295571161856));
#16117=CARTESIAN_POINT('Ctrl Pts',(1.98561096251939,0.203054288922361,21.9340044597914));
#16118=CARTESIAN_POINT('Ctrl Pts',(1.97610777552311,0.272076500302983,21.9384518033971));
#16119=CARTESIAN_POINT('Ctrl Pts',(1.96661579180746,0.34101734159118,21.9428939040419));
#16120=CARTESIAN_POINT('Ctrl Pts',(1.9535009905037,0.409539251765541,21.9473360046867));
#16121=CARTESIAN_POINT('Ctrl Pts',(1.93682065736895,0.477235061252748,21.9517781053315));
#16122=CARTESIAN_POINT('Ctrl Pts',(1.92015084626223,0.544888167923446,21.9562174038795));
#16123=CARTESIAN_POINT('Ctrl Pts',(1.89992008198059,0.611715733424842,21.9606567024275));
#16124=CARTESIAN_POINT('Ctrl Pts',(1.87623676763892,0.677320569789411,21.9650960009756));
#16125=CARTESIAN_POINT('Ctrl Pts',(1.85256034519017,0.742906315012403,21.9695340076786));
#16126=CARTESIAN_POINT('Ctrl Pts',(1.82543353331394,0.807269577211512,21.9739720143817));
#16127=CARTESIAN_POINT('Ctrl Pts',(1.79501410522617,0.870029841177362,21.9784100210848));
#16128=CARTESIAN_POINT('Ctrl Pts',(1.76459319296152,0.932793167243267,21.9828482443201));
#16129=CARTESIAN_POINT('Ctrl Pts',(1.73087956121856,0.993952900301384,21.9872864675554));
#16130=CARTESIAN_POINT('Ctrl Pts',(1.69407771131804,1.05315158952329,21.9917246907907));
#16131=CARTESIAN_POINT('Ctrl Pts',(1.65723687391894,1.11241299322336,21.9961676158337));
#16132=CARTESIAN_POINT('Ctrl Pts',(1.61730154733726,1.16970878987996,22.0006105408767));
#16133=CARTESIAN_POINT('Ctrl Pts',(1.57451998655462,1.22470991440424,22.0050534659197));
#16134=CARTESIAN_POINT('Ctrl Pts',(1.531713452414,1.27974314534883,22.009498984481));
#16135=CARTESIAN_POINT('Ctrl Pts',(1.48605769765005,1.33247866781368,22.0139445030422));
#16136=CARTESIAN_POINT('Ctrl Pts',(1.4378399272931,1.38262211250283,22.0183900216035));
#16137=CARTESIAN_POINT('Ctrl Pts',(1.38953801558089,1.43285305890269,22.0228432977187));
#16138=CARTESIAN_POINT('Ctrl Pts',(1.33866552111773,1.48048256375399,22.027296573834));
#16139=CARTESIAN_POINT('Ctrl Pts',(1.28554438964709,1.52525512120002,22.0317498499492));
#16140=CARTESIAN_POINT('Ctrl Pts',(1.25709955133765,1.54922953819746,22.034134451247));
#16141=CARTESIAN_POINT('Ctrl Pts',(1.22801049480845,1.57238550184667,22.0365190525448));
#16142=CARTESIAN_POINT('Ctrl Pts',(1.19832994901216,1.5946889652219,22.0389036538426));
#16143=CARTESIAN_POINT('Ctrl Pts',(1.14289162468103,1.63634812623567,22.0433576925606));
#16144=CARTESIAN_POINT('Ctrl Pts',(1.08516853929668,1.67519542850972,22.0478117312785));
#16145=CARTESIAN_POINT('Ctrl Pts',(1.02547766814925,1.71097139503476,22.0522657699965));
#16146=CARTESIAN_POINT('Ctrl Pts',(0.965876521655493,1.7466935847235,22.0567131136023));
#16147=CARTESIAN_POINT('Ctrl Pts',(0.904313876563793,1.7793533520302,22.061160457208));
#16148=CARTESIAN_POINT('Ctrl Pts',(0.84113779507104,1.80873291898031,22.0656078008138));
#16149=CARTESIAN_POINT('Ctrl Pts',(0.778036191684482,1.83807785044091,22.0700499014586));
#16150=CARTESIAN_POINT('Ctrl Pts',(0.713325371423766,1.8641500564919,22.0744920021034));
#16151=CARTESIAN_POINT('Ctrl Pts',(0.64737868035834,1.88677725413402,22.0789341027481));
#16152=CARTESIAN_POINT('Ctrl Pts',(0.581473588757775,1.90939017843962,22.0833734012962));
#16153=CARTESIAN_POINT('Ctrl Pts',(0.514334634872293,1.92856224680548,22.0878126998442));
#16154=CARTESIAN_POINT('Ctrl Pts',(0.446354448204243,1.94416955769508,22.0922519983922));
#16155=CARTESIAN_POINT('Ctrl Pts',(0.378394043909549,1.95977232682529,22.0966900050953));
#16156=CARTESIAN_POINT('Ctrl Pts',(0.309593369703032,1.97181228829576,22.1011280117983));
#16157=CARTESIAN_POINT('Ctrl Pts',(0.240357766897769,1.98021607568263,22.1055660185014));
#16158=CARTESIAN_POINT('Ctrl Pts',(0.171118786057906,1.98862027309387,22.1100042417367));
#16159=CARTESIAN_POINT('Ctrl Pts',(0.101445320770596,1.9933878875812,22.114442464972));
#16160=CARTESIAN_POINT('Ctrl Pts',(0.0317486199466149,1.99449732705549,
22.1188806882073));
#16161=CARTESIAN_POINT('Ctrl Pts',(-0.0380219168402537,1.99560794185846,
22.1233236132503));
#16162=CARTESIAN_POINT('Ctrl Pts',(-0.107815247820187,1.99305263866246,
22.1277665382934));
#16163=CARTESIAN_POINT('Ctrl Pts',(-0.177220300856193,1.98686197997356,
22.1322094633364));
#16164=CARTESIAN_POINT('Ctrl Pts',(-0.246665868478446,1.98066770754236,
22.1366549818977));
#16165=CARTESIAN_POINT('Ctrl Pts',(-0.315722222209281,1.97083392484672,
22.1411005004589));
#16166=CARTESIAN_POINT('Ctrl Pts',(-0.383986372642777,1.95744272665247,
22.1455460190202));
#16167=CARTESIAN_POINT('Ctrl Pts',(-0.452369645924388,1.94402816044355,
22.1499992951354));
#16168=CARTESIAN_POINT('Ctrl Pts',(-0.519957481606996,1.92704390617596,
22.1544525712506));
#16169=CARTESIAN_POINT('Ctrl Pts',(-0.58636075597997,1.90662230825788,22.1589058473659));
#16170=CARTESIAN_POINT('Ctrl Pts',(-0.62191779986246,1.89568712983211,22.1612904486637));
#16171=CARTESIAN_POINT('Ctrl Pts',(-0.65713551031104,1.88376719975309,22.1636750499615));
#16172=CARTESIAN_POINT('Ctrl Pts',(-0.691956714037148,1.8708884168755,22.1660596512594));
#16173=CARTESIAN_POINT('Ctrl Pts',(-0.756996932602777,1.84683299191644,
22.1705136899774));
#16174=CARTESIAN_POINT('Ctrl Pts',(-0.820910056479831,1.81933426328133,
22.1749677286953));
#16175=CARTESIAN_POINT('Ctrl Pts',(-0.88330631424359,1.78851824640326,22.1794217674133));
#16176=CARTESIAN_POINT('Ctrl Pts',(-0.945608780737224,1.75774855078654,
22.1838691110191));
#16177=CARTESIAN_POINT('Ctrl Pts',(-1.00639847115222,1.72367167871072,22.1883164546248));
#16178=CARTESIAN_POINT('Ctrl Pts',(-1.0653038420214,1.68646235851099,22.1927637982306));
#16179=CARTESIAN_POINT('Ctrl Pts',(-1.12413976951322,1.64929690427501,22.1972058988754));
#16180=CARTESIAN_POINT('Ctrl Pts',(-1.1810953775753,1.60900659653896,22.2016479995202));
#16181=CARTESIAN_POINT('Ctrl Pts',(-1.23582368399509,1.56581205276266,22.206090100165));
#16182=CARTESIAN_POINT('Ctrl Pts',(-1.29051746755672,1.52264475629594,22.210529398713));
#16183=CARTESIAN_POINT('Ctrl Pts',(-1.34298635325931,1.47657716066309,22.214968697261));
#16184=CARTESIAN_POINT('Ctrl Pts',(-1.39291359569009,1.4278722903123,22.219407995809));
#16185=CARTESIAN_POINT('Ctrl Pts',(-1.44282630919121,1.3791815931784,22.2238460025121));
#16186=CARTESIAN_POINT('Ctrl Pts',(-1.4901984974338,1.32785548652114,22.2282840092151));
#16187=CARTESIAN_POINT('Ctrl Pts',(-1.53474902045629,1.27419504264789,22.2327220159182));
#16188=CARTESIAN_POINT('Ctrl Pts',(-1.57930171711783,1.22053198065866,22.2371602391535));
#16189=CARTESIAN_POINT('Ctrl Pts',(-1.62103216435493,1.16453473352599,22.2415984623888));
#16190=CARTESIAN_POINT('Ctrl Pts',(-1.65969955342409,1.10653737165261,22.2460366856241));
#16191=CARTESIAN_POINT('Ctrl Pts',(-1.69840790632471,1.0484785679748,22.2504796106671));
#16192=CARTESIAN_POINT('Ctrl Pts',(-1.73404645213506,0.988415828474916,
22.2549225357102));
#16193=CARTESIAN_POINT('Ctrl Pts',(-1.76641832718732,0.926711312047483,
22.2593654607532));
#16194=CARTESIAN_POINT('Ctrl Pts',(-1.7988090990355,0.864970776153984,22.2638109793144));
#16195=CARTESIAN_POINT('Ctrl Pts',(-1.82792920023711,0.8015870007953,22.2682564978757));
#16196=CARTESIAN_POINT('Ctrl Pts',(-1.85362946934576,0.736943249424911,
22.2727020164369));
#16197=CARTESIAN_POINT('Ctrl Pts',(-1.87937458614142,0.672186692903873,
22.2771552925522));
#16198=CARTESIAN_POINT('Ctrl Pts',(-1.90168780150769,0.606166235125184,
22.2816085686674));
#16199=CARTESIAN_POINT('Ctrl Pts',(-1.9204697088147,0.539280687606346,22.2860618447827));
#16200=CARTESIAN_POINT('Ctrl Pts',(-1.93052688007029,0.503465400323477,
22.2884464460804));
#16201=CARTESIAN_POINT('Ctrl Pts',(-1.93957239482412,0.467402253967104,
22.2908310473782));
#16202=CARTESIAN_POINT('Ctrl Pts',(-1.94759707343737,0.431153339356435,
22.293215648676));
#16203=CARTESIAN_POINT('Ctrl Pts',(-1.96820349956193,0.338070411426196,
22.2993390229378));
#16204=CARTESIAN_POINT('Ctrl Pts',(-1.98214332905318,0.243462071757729,
22.3054623971996));
#16205=CARTESIAN_POINT('Ctrl Pts',(-1.98924225493863,0.148131069214597,
22.3115857714614));
#16206=CARTESIAN_POINT('Ctrl Pts',(-1.99286284135548,0.0995104555497706,
22.314708808106));
#16207=CARTESIAN_POINT('Ctrl Pts',(-1.99470467848154,0.0507022014321492,
22.3178318447506));
#16208=CARTESIAN_POINT('Ctrl Pts',(-1.99474917376081,0.00181556617883987,
22.3209548813952));
#16209=CARTESIAN_POINT('',(-1.99474923905662,-0.00174234986216392,23.9213503181716));
#16210=CARTESIAN_POINT('Ctrl Pts',(-1.99474916465735,0.00182554069043293,
22.3211268459801));
#16211=CARTESIAN_POINT('Ctrl Pts',(-1.99487395450769,-0.134531019874973,
22.3290365499321));
#16212=CARTESIAN_POINT('Ctrl Pts',(-1.98101782205593,-0.270531511972645,
22.3369252531668));
#16213=CARTESIAN_POINT('Ctrl Pts',(-1.94710944369394,-0.434461115772628,
22.3471604031875));
#16214=CARTESIAN_POINT('Ctrl Pts',(-1.94011124694327,-0.464714787064044,
22.3490789461331));
#16215=CARTESIAN_POINT('Ctrl Pts',(-1.93038366978814,-0.502705870542994,
22.3515307718075));
#16216=CARTESIAN_POINT('Ctrl Pts',(-1.92830864928981,-0.510607534976442,
22.3520430636427));
#16217=CARTESIAN_POINT('Ctrl Pts',(-1.92474835120962,-0.523833850233449,
22.3529046033478));
#16218=CARTESIAN_POINT('Ctrl Pts',(-1.92328936086948,-0.529165523732292,
22.3532530023818));
#16219=CARTESIAN_POINT('Ctrl Pts',(-1.92037199803809,-0.539655151635728,
22.3539406561053));
#16220=CARTESIAN_POINT('Ctrl Pts',(-1.91891495862294,-0.544813430629328,
22.3542798651057));
#16221=CARTESIAN_POINT('Ctrl Pts',(-1.91610356291509,-0.554615267846382,
22.3549264708628));
#16222=CARTESIAN_POINT('Ctrl Pts',(-1.91475307036602,-0.559259902005289,
22.3552337396913));
#16223=CARTESIAN_POINT('Ctrl Pts',(-1.91163787845738,-0.569830160003168,
22.3559350334784));
#16224=CARTESIAN_POINT('Ctrl Pts',(-1.90986250206253,-0.575752560910539,
22.3563294049467));
#16225=CARTESIAN_POINT('Ctrl Pts',(-1.90435976351267,-0.593803372294288,
22.3575358739453));
#16226=CARTESIAN_POINT('Ctrl Pts',(-1.90054424744259,-0.60590436950045,
22.3583508506658));
#16227=CARTESIAN_POINT('Ctrl Pts',(-1.84952423541691,-0.762490572959903,
22.368978717291));
#16228=CARTESIAN_POINT('Ctrl Pts',(-1.7860807614038,-0.901126382508468,
22.3793579959026));
#16229=CARTESIAN_POINT('Ctrl Pts',(-1.67596060795108,-1.08347321158767,
22.3941981638717));
#16230=CARTESIAN_POINT('Ctrl Pts',(-1.64200104140563,-1.13427988143001,
22.3984709038721));
#16231=CARTESIAN_POINT('Ctrl Pts',(-1.5583125971607,-1.24783265163207,22.4082529300103));
#16232=CARTESIAN_POINT('Ctrl Pts',(-1.50702614251558,-1.3093126967328,22.413728134514));
#16233=CARTESIAN_POINT('Ctrl Pts',(-1.44522760339684,-1.37493548274255,
22.4196396335748));
#16234=CARTESIAN_POINT('Ctrl Pts',(-1.43821863180487,-1.38226538151872,
22.4203009061064));
#16235=CARTESIAN_POINT('Ctrl Pts',(-1.42899124246175,-1.3917691007664,22.4211591902352));
#16236=CARTESIAN_POINT('Ctrl Pts',(-1.42682338304109,-1.39399147587231,
22.4213599586059));
#16237=CARTESIAN_POINT('Ctrl Pts',(-1.42255686900396,-1.39834490110462,
22.4217533562102));
#16238=CARTESIAN_POINT('Ctrl Pts',(-1.42045859312581,-1.40047630951062,
22.4219460137397));
#16239=CARTESIAN_POINT('Ctrl Pts',(-1.41644414808854,-1.40453584041459,
22.4223130400321));
#16240=CARTESIAN_POINT('Ctrl Pts',(-1.41452885499875,-1.40646474186768,
22.4224874694846));
#16241=CARTESIAN_POINT('Ctrl Pts',(-1.41009838865867,-1.41090848283683,
22.42288940945));
#16242=CARTESIAN_POINT('Ctrl Pts',(-1.4075804287362,-1.41342051412752,22.4231166963572));
#16243=CARTESIAN_POINT('Ctrl Pts',(-1.39948008423508,-1.42145867217602,
22.423844268479));
#16244=CARTESIAN_POINT('Ctrl Pts',(-1.39387168546872,-1.42695865119918,
22.4243425322353));
#16245=CARTESIAN_POINT('Ctrl Pts',(-1.31909535599593,-1.49942790603792,
22.4309160123608));
#16246=CARTESIAN_POINT('Ctrl Pts',(-1.24518908697355,-1.56134754712361,
22.436628900454));
#16247=CARTESIAN_POINT('Ctrl Pts',(-1.09135981255622,-1.67232807643898,
22.4477112811479));
#16248=CARTESIAN_POINT('Ctrl Pts',(-1.01188806633998,-1.72157781333676,
22.4530741377689));
#16249=CARTESIAN_POINT('Ctrl Pts',(-0.864721201832706,-1.79905649938952,
22.4628163271807));
#16250=CARTESIAN_POINT('Ctrl Pts',(-0.798374361419991,-1.82946549577,22.4671451795131));
#16251=CARTESIAN_POINT('Ctrl Pts',(-0.706530623005226,-1.86561154098105,
22.473161268282));
#16252=CARTESIAN_POINT('Ctrl Pts',(-0.682365869914973,-1.87458493319584,
22.4747459691639));
#16253=CARTESIAN_POINT('Ctrl Pts',(-0.640980396582672,-1.88904686650893,
22.4774672084792));
#16254=CARTESIAN_POINT('Ctrl Pts',(-0.623846252970294,-1.89477432734875,
22.4785958978355));
#16255=CARTESIAN_POINT('Ctrl Pts',(-0.601395855381872,-1.9019413392695,
22.4800783362717));
#16256=CARTESIAN_POINT('Ctrl Pts',(-0.596147741509026,-1.90359284044834,
22.4804251284474));
#16257=CARTESIAN_POINT('Ctrl Pts',(-0.585790564057796,-1.90680505443428,
22.4811100490443));
#16258=CARTESIAN_POINT('Ctrl Pts',(-0.580681928207997,-1.90836699769781,
22.48144813397));
#16259=CARTESIAN_POINT('Ctrl Pts',(-0.570931946440271,-1.91130523754168,
22.4820938825083));
#16260=CARTESIAN_POINT('Ctrl Pts',(-0.566291737200668,-1.91268519788796,
22.4824014236653));
#16261=CARTESIAN_POINT('Ctrl Pts',(-0.555681758800476,-1.91579852491365,
22.4831051418711));
#16262=CARTESIAN_POINT('Ctrl Pts',(-0.549708841161825,-1.91752089783329,
22.4835016742704));
#16263=CARTESIAN_POINT('Ctrl Pts',(-0.531356591316559,-1.92272022723358,
22.4847212477045));
#16264=CARTESIAN_POINT('Ctrl Pts',(-0.518951804649607,-1.92610537378607,
22.4855472600358));
#16265=CARTESIAN_POINT('Ctrl Pts',(-0.404201076652255,-1.95623075228686,
22.4932049159982));
#16266=CARTESIAN_POINT('Ctrl Pts',(-0.299929795218202,-1.97490576431392,
22.500298653188));
#16267=CARTESIAN_POINT('Ctrl Pts',(-0.0623218021041458,-1.99820717833908,
22.5167200655941));
#16268=CARTESIAN_POINT('Ctrl Pts',(0.0709996732814402,-1.99791713716561,
22.5261210426059));
#16269=CARTESIAN_POINT('Ctrl Pts',(0.243327821427617,-1.98026221060951,
22.5380005699284));
#16270=CARTESIAN_POINT('Ctrl Pts',(0.283228240406341,-1.9749503930941,22.5407293573752));
#16271=CARTESIAN_POINT('Ctrl Pts',(0.344040504107337,-1.96497347873874,
22.5448293420469));
#16272=CARTESIAN_POINT('Ctrl Pts',(0.365081916101651,-1.96117309968721,
22.5462370083217));
#16273=CARTESIAN_POINT('Ctrl Pts',(0.391207605213068,-1.9560193531349,22.5479677705432));
#16274=CARTESIAN_POINT('Ctrl Pts',(0.396352069611487,-1.95498341134752,
22.5483077513314));
#16275=CARTESIAN_POINT('Ctrl Pts',(0.404511858954576,-1.95330673991214,
22.5488456259945));
#16276=CARTESIAN_POINT('Ctrl Pts',(0.40752984465648,-1.95267931065289,22.5490442647244));
#16277=CARTESIAN_POINT('Ctrl Pts',(0.41318653923977,-1.95148961693505,22.5494160003781));
#16278=CARTESIAN_POINT('Ctrl Pts',(0.415825531454692,-1.95092900145483,
22.5495891862112));
#16279=CARTESIAN_POINT('Ctrl Pts',(0.421840281774882,-1.94963849655661,
22.5499833736897));
#16280=CARTESIAN_POINT('Ctrl Pts',(0.425215279774653,-1.94890519442826,
22.5502041772537));
#16281=CARTESIAN_POINT('Ctrl Pts',(0.435541167469643,-1.94663353888735,
22.5508786055035));
#16282=CARTESIAN_POINT('Ctrl Pts',(0.44248583561854,-1.9450667166557,22.5513306286604));
#16283=CARTESIAN_POINT('Ctrl Pts',(0.497300725493365,-1.93239087664798,
22.5548871962136));
#16284=CARTESIAN_POINT('Ctrl Pts',(0.544758553400688,-1.9195524363302,22.5578983500583));
#16285=CARTESIAN_POINT('Ctrl Pts',(0.762528660113038,-1.85191150700659,
22.5716023927544));
#16286=CARTESIAN_POINT('Ctrl Pts',(0.925453263414701,-1.77611166426968,
22.581599861375));
#16287=CARTESIAN_POINT('Ctrl Pts',(1.11632211931106,-1.65382427314641,22.5951108083804));
#16288=CARTESIAN_POINT('Ctrl Pts',(1.1556059033512,-1.62661743942888,22.5979956596301));
#16289=CARTESIAN_POINT('Ctrl Pts',(1.21709308396422,-1.58068089018479,22.6027126656628));
#16290=CARTESIAN_POINT('Ctrl Pts',(1.23993104127373,-1.5628302943425,22.6045119884421));
#16291=CARTESIAN_POINT('Ctrl Pts',(1.2687859998665,-1.53924601365169,22.6068510977748));
#16292=CARTESIAN_POINT('Ctrl Pts',(1.27516809100609,-1.53396301791901,22.6073727035432));
#16293=CARTESIAN_POINT('Ctrl Pts',(1.28564224884653,-1.52518213608453,22.6082358857634));
#16294=CARTESIAN_POINT('Ctrl Pts',(1.28975343932334,-1.52170713512081,22.6085765265738));
#16295=CARTESIAN_POINT('Ctrl Pts',(1.29752835917773,-1.5150812092403,22.6092242536879));
#16296=CARTESIAN_POINT('Ctrl Pts',(1.30119480910814,-1.5119335241797,22.6095312051768));
#16297=CARTESIAN_POINT('Ctrl Pts',(1.30949530691094,-1.50475490576425,22.6102295536084));
#16298=CARTESIAN_POINT('Ctrl Pts',(1.31412223074216,-1.50071584469483,22.6106212862797));
#16299=CARTESIAN_POINT('Ctrl Pts',(1.3260205553458,-1.49023201457492,22.6116350508912));
#16300=CARTESIAN_POINT('Ctrl Pts',(1.33326358602594,-1.48375542967492,22.612258410958));
#16301=CARTESIAN_POINT('Ctrl Pts',(1.35187761188666,-1.46686476298206,22.6138767940778));
#16302=CARTESIAN_POINT('Ctrl Pts',(1.36317551915813,-1.45637144718114,22.6148751541644));
#16303=CARTESIAN_POINT('Ctrl Pts',(1.49057246350765,-1.33526598134491,22.6263200324392));
#16304=CARTESIAN_POINT('Ctrl Pts',(1.59302573901624,-1.21119372229919,22.6373921507008));
#16305=CARTESIAN_POINT('Ctrl Pts',(1.72228372922423,-1.00948098766119,22.6541076937224));
#16306=CARTESIAN_POINT('Ctrl Pts',(1.76104324387832,-0.940234594272093,
22.6596386027489));
#16307=CARTESIAN_POINT('Ctrl Pts',(1.80925582585188,-0.840599037396781,
22.6671696654947));
#16308=CARTESIAN_POINT('Ctrl Pts',(1.8222635334276,-0.812015536752611,22.6692831825295));
#16309=CARTESIAN_POINT('Ctrl Pts',(1.84165860881691,-0.766580160989994,
22.6725568652198));
#16310=CARTESIAN_POINT('Ctrl Pts',(1.84850140832012,-0.749929446026353,
22.6737388031703));
#16311=CARTESIAN_POINT('Ctrl Pts',(1.8569394428166,-0.72857945417306,22.6752297170721));
#16312=CARTESIAN_POINT('Ctrl Pts',(1.85874357280237,-0.723964396346133,
22.6755505422672));
#16313=CARTESIAN_POINT('Ctrl Pts',(1.86160996844704,-0.716550659800417,
22.6760635394373));
#16314=CARTESIAN_POINT('Ctrl Pts',(1.8626831493131,-0.713756266688654,22.6762563573176));
#16315=CARTESIAN_POINT('Ctrl Pts',(1.86471862599565,-0.708420350863957,
22.6766234977335));
#16316=CARTESIAN_POINT('Ctrl Pts',(1.86568200652061,-0.705879308576643,
22.6767978817389));
#16317=CARTESIAN_POINT('Ctrl Pts',(1.86789254083851,-0.700012595232482,
22.677199463264));
#16318=CARTESIAN_POINT('Ctrl Pts',(1.86913600683422,-0.696685557505772,
22.677426438475));
#16319=CARTESIAN_POINT('Ctrl Pts',(1.87245111052919,-0.687742850226298,
22.678034520194));
#16320=CARTESIAN_POINT('Ctrl Pts',(1.87450638966861,-0.682121093825888,
22.6784146699298));
#16321=CARTESIAN_POINT('Ctrl Pts',(1.88937661409514,-0.640872127323986,
22.6811890930592));
#16322=CARTESIAN_POINT('Ctrl Pts',(1.90120120440005,-0.604892969929968,
22.6835279541159));
#16323=CARTESIAN_POINT('Ctrl Pts',(1.9361116318199,-0.487501113056454,22.690965121051));
#16324=CARTESIAN_POINT('Ctrl Pts',(1.95504633017762,-0.404946698496029,
22.6959007483728));
#16325=CARTESIAN_POINT('Ctrl Pts',(1.98491678741861,-0.221999158367863,
22.7066647979654));
#16326=CARTESIAN_POINT('Ctrl Pts',(1.99359468472123,-0.121480026991771,
22.7124727196927));
#16327=CARTESIAN_POINT('Ctrl Pts',(1.99517545653653,0.0305468418019273,
22.7215078341762));
#16328=CARTESIAN_POINT('Ctrl Pts',(1.99373045347125,0.0818320573321208,
22.7245971045408));
#16329=CARTESIAN_POINT('Ctrl Pts',(1.98826916154383,0.163557734931406,22.7296244118648));
#16330=CARTESIAN_POINT('Ctrl Pts',(1.98552399057693,0.194061111342069,22.7315240064004));
#16331=CARTESIAN_POINT('Ctrl Pts',(1.98109816598418,0.233138167037473,22.7339920070998));
#16332=CARTESIAN_POINT('Ctrl Pts',(1.98006185089138,0.241781742423838,22.7345400801569));
#16333=CARTESIAN_POINT('Ctrl Pts',(1.97829918228246,0.255711509741991,22.7354269470858));
#16334=CARTESIAN_POINT('Ctrl Pts',(1.97760813189825,0.261002119879242,22.7357646250052));
#16335=CARTESIAN_POINT('Ctrl Pts',(1.97624940024058,0.271089139639613,22.7364100684452));
#16336=CARTESIAN_POINT('Ctrl Pts',(1.97558546153878,0.275886021861949,22.7367177135068));
#16337=CARTESIAN_POINT('Ctrl Pts',(1.97402761923951,0.286847204205327,22.7374223351988));
#16338=CARTESIAN_POINT('Ctrl Pts',(1.97312230030656,0.293009806421168,22.7378196704677));
#16339=CARTESIAN_POINT('Ctrl Pts',(1.97025015172648,0.311943707031555,22.7390441330497));
#16340=CARTESIAN_POINT('Ctrl Pts',(1.96818810705046,0.324700013760337,22.7398742664013));
#16341=CARTESIAN_POINT('Ctrl Pts',(1.9473228653218,0.446267415820006,22.7478362360987));
#16342=CARTESIAN_POINT('Ctrl Pts',(1.91964232292156,0.553341513907452,22.7552548186305));
#16343=CARTESIAN_POINT('Ctrl Pts',(1.82651577628048,0.820055639187041,22.7747219809042));
#16344=CARTESIAN_POINT('Ctrl Pts',(1.74898915740276,0.974519898479016,22.7870015472129));
#16345=CARTESIAN_POINT('Ctrl Pts',(1.64226378352394,1.13240353731302,22.7996368929803));
#16346=CARTESIAN_POINT('Ctrl Pts',(1.63171701388448,1.14754858402196,22.8008490518177));
#16347=CARTESIAN_POINT('Ctrl Pts',(1.61804810445454,1.16660742205184,22.8023723836902));
#16348=CARTESIAN_POINT('Ctrl Pts',(1.61511978651685,1.17065820034293,22.8026960324628));
#16349=CARTESIAN_POINT('Ctrl Pts',(1.61040777531065,1.17712504765559,22.8032124690612));
#16350=CARTESIAN_POINT('Ctrl Pts',(1.60863382234227,1.1795481365798,22.8034059179874));
#16351=CARTESIAN_POINT('Ctrl Pts',(1.60524577815102,1.18415409649484,22.8037735149481));
#16352=CARTESIAN_POINT('Ctrl Pts',(1.60363272266733,1.18633765150904,22.8039477275079));
#16353=CARTESIAN_POINT('Ctrl Pts',(1.59991026973095,1.19135518293681,22.8043479318962));
#16354=CARTESIAN_POINT('Ctrl Pts',(1.59779779913364,1.19418685165022,22.8045737064086));
#16355=CARTESIAN_POINT('Ctrl Pts',(1.59212493318368,1.20174906429766,22.8051764789548));
#16356=CARTESIAN_POINT('Ctrl Pts',(1.58855094706958,1.2064694389381,22.8055525461816));
#16357=CARTESIAN_POINT('Ctrl Pts',(1.56278310013225,1.2401895365013,22.8082382091873));
#16358=CARTESIAN_POINT('Ctrl Pts',(1.53981593869398,1.26859307402303,22.8104962928574));
#16359=CARTESIAN_POINT('Ctrl Pts',(1.4667283614622,1.35406879227771,22.8173348484934));
#16360=CARTESIAN_POINT('Ctrl Pts',(1.41411676423863,1.40892513374242,22.8217871962587));
#16361=CARTESIAN_POINT('Ctrl Pts',(1.28219245229713,1.53162336391116,22.8322689832983));
#16362=CARTESIAN_POINT('Ctrl Pts',(1.20044215311522,1.59650415665228,22.8382584351856));
#16363=CARTESIAN_POINT('Ctrl Pts',(1.06777988036323,1.68581673644667,22.8477295656777));
#16364=CARTESIAN_POINT('Ctrl Pts',(1.02028094304673,1.71498046362059,22.8510749061639));
#16365=CARTESIAN_POINT('Ctrl Pts',(0.943235443344064,1.75795086202701,22.8564810489308));
#16366=CARTESIAN_POINT('Ctrl Pts',(0.914463069262987,1.7730881084232,22.8584955028114));
#16367=CARTESIAN_POINT('Ctrl Pts',(0.877370059248215,1.7914598356594,22.8610925049177));
#16368=CARTESIAN_POINT('Ctrl Pts',(0.869379031980131,1.79535140245078,22.8616519737826));
#16369=CARTESIAN_POINT('Ctrl Pts',(0.856513180651841,1.80151093198391,22.8625528384647));
#16370=CARTESIAN_POINT('Ctrl Pts',(0.85165466865916,1.80381284814027,22.8628930529684));
#16371=CARTESIAN_POINT('Ctrl Pts',(0.842410455150029,1.80814699391779,22.8635404428854));
#16372=CARTESIAN_POINT('Ctrl Pts',(0.838026549818965,1.81018298182334,22.8638474855249));
#16373=CARTESIAN_POINT('Ctrl Pts',(0.828044612911843,1.81477479364279,22.8645466948078));
#16374=CARTESIAN_POINT('Ctrl Pts',(0.822442087992473,1.81732067701587,22.8649392003359));
#16375=CARTESIAN_POINT('Ctrl Pts',(0.805385364236191,1.82497651701979,22.8661344171093));
#16376=CARTESIAN_POINT('Ctrl Pts',(0.793894843269383,1.83000432744978,22.8669399296299));
#16377=CARTESIAN_POINT('Ctrl Pts',(0.637986272532171,1.89647920221075,22.8778757303823));
#16378=CARTESIAN_POINT('Ctrl Pts',(0.48688591149088,1.94076831641874,22.8886133361283));
#16379=CARTESIAN_POINT('Ctrl Pts',(0.242528399290034,1.98203857291557,22.9058881910641));
#16380=CARTESIAN_POINT('Ctrl Pts',(0.151928392206219,1.9910338931163,22.9122583810231));
#16381=CARTESIAN_POINT('Ctrl Pts',(0.0267241362351118,1.99486621983656,
22.9208052199254));
#16382=CARTESIAN_POINT('Ctrl Pts',(-0.00760323781957737,1.99503080134012,
22.9231213435121));
#16383=CARTESIAN_POINT('Ctrl Pts',(-0.0610970543308081,1.99390637768921,
22.9266719372443));
#16384=CARTESIAN_POINT('Ctrl Pts',(-0.0802684116077697,1.99322666607084,
22.9279326279261));
#16385=CARTESIAN_POINT('Ctrl Pts',(-0.104487052154384,1.99201799135356,
22.9295078450429));
#16386=CARTESIAN_POINT('Ctrl Pts',(-0.109545358246763,1.99174622826215,
22.9298358853588));
#16387=CARTESIAN_POINT('Ctrl Pts',(-0.117615683156636,1.99128180377935,
22.9303576702476));
#16388=CARTESIAN_POINT('Ctrl Pts',(-0.120628352459527,1.99110157246374,
22.9305520998308));
#16389=CARTESIAN_POINT('Ctrl Pts',(-0.126346212928537,1.99074647944261,
22.9309204286286));
#16390=CARTESIAN_POINT('Ctrl Pts',(-0.129051423148523,1.99057294294943,
22.9310943970733));
#16391=CARTESIAN_POINT('Ctrl Pts',(-0.135253185204583,1.99016241047088,
22.9314925620557));
#16392=CARTESIAN_POINT('Ctrl Pts',(-0.138749468457328,1.98992171444525,
22.9317165487041));
#16393=CARTESIAN_POINT('Ctrl Pts',(-0.149801137813084,1.98913161119218,
22.9324230942243));
#16394=CARTESIAN_POINT('Ctrl Pts',(-0.15735415065229,1.98854837085257,22.9329037924214));
#16395=CARTESIAN_POINT('Ctrl Pts',(-0.28648262272367,1.97783679620507,22.9410875448193));
#16396=CARTESIAN_POINT('Ctrl Pts',(-0.406901180141803,1.95661746999596,
22.9482056002925));
#16397=CARTESIAN_POINT('Ctrl Pts',(-0.621530690257861,1.89810757757316,
22.9611217636335));
#16398=CARTESIAN_POINT('Ctrl Pts',(-0.716285028780494,1.86441609797625,
22.9669126470896));
#16399=CARTESIAN_POINT('Ctrl Pts',(-0.854614684721749,1.80312235940427,
22.9759071334529));
#16400=CARTESIAN_POINT('Ctrl Pts',(-0.900325374427479,1.78073864722669,
22.9789727220304));
#16401=CARTESIAN_POINT('Ctrl Pts',(-0.97194032319833,1.74220738601696,22.9839648429509));
#16402=CARTESIAN_POINT('Ctrl Pts',(-0.998417588995791,1.7271701505935,22.9858536225567));
#16403=CARTESIAN_POINT('Ctrl Pts',(-1.03199352782441,1.70707129254735,22.9883094515749));
#16404=CARTESIAN_POINT('Ctrl Pts',(-1.03941844569094,1.70256052174982,22.9888564171801));
#16405=CARTESIAN_POINT('Ctrl Pts',(-1.0513520291994,1.69520349792219,22.9897419240131));
#16406=CARTESIAN_POINT('Ctrl Pts',(-1.05587921942695,1.69238738524937,22.9900793555606));
#16407=CARTESIAN_POINT('Ctrl Pts',(-1.06449755453409,1.68697835768705,22.9907246157254));
#16408=CARTESIAN_POINT('Ctrl Pts',(-1.06859065758722,1.68438862165204,22.9910323250967));
#16409=CARTESIAN_POINT('Ctrl Pts',(-1.07793219279699,1.6784304104782,22.99173750054));
#16410=CARTESIAN_POINT('Ctrl Pts',(-1.08317432106507,1.67505219136933,22.9921353272643));
#16411=CARTESIAN_POINT('Ctrl Pts',(-1.09926195288677,1.66457763535729,22.993362788102));
#16412=CARTESIAN_POINT('Ctrl Pts',(-1.11005403220569,1.65740024665056,22.9941954496608));
#16413=CARTESIAN_POINT('Ctrl Pts',(-1.21483124195331,1.58623462481342,23.0023717791739));
#16414=CARTESIAN_POINT('Ctrl Pts',(-1.30323624114396,1.51443798564161,23.0100203358722));
#16415=CARTESIAN_POINT('Ctrl Pts',(-1.50116996399817,1.32346489153158,23.0289967490486));
#16416=CARTESIAN_POINT('Ctrl Pts',(-1.60327700833823,1.19773717721527,23.0404789963379));
#16417=CARTESIAN_POINT('Ctrl Pts',(-1.70234724473211,1.04002864368377,23.05291554291));
#16418=CARTESIAN_POINT('Ctrl Pts',(-1.71517869549642,1.01872857297808,23.0545566636392));
#16419=CARTESIAN_POINT('Ctrl Pts',(-1.73036589387726,0.992417171983663,
23.056532158617));
#16420=CARTESIAN_POINT('Ctrl Pts',(-1.73310276251856,0.987629883228585,
23.0568895340401));
#16421=CARTESIAN_POINT('Ctrl Pts',(-1.7373558430498,0.980118337971587,23.0574469854864));
#16422=CARTESIAN_POINT('Ctrl Pts',(-1.73888555378862,0.977401817555047,
23.0576479149568));
#16423=CARTESIAN_POINT('Ctrl Pts',(-1.7417248953565,0.972331838970681,23.0580216553195));
#16424=CARTESIAN_POINT('Ctrl Pts',(-1.74303611474329,0.969979339477833,
23.0581945655442));
#16425=CARTESIAN_POINT('Ctrl Pts',(-1.7459928653227,0.96464918521885,23.0585851951958));
#16426=CARTESIAN_POINT('Ctrl Pts',(-1.74763554162708,0.961669979963943,
23.0588027304219));
#16427=CARTESIAN_POINT('Ctrl Pts',(-1.75246197112126,0.95286341941922,23.0594434493249));
#16428=CARTESIAN_POINT('Ctrl Pts',(-1.755624296569,0.947024280885827,23.0598652876223));
#16429=CARTESIAN_POINT('Ctrl Pts',(-1.77737433577252,0.906380114963131,
23.0627816430493));
#16430=CARTESIAN_POINT('Ctrl Pts',(-1.79495642220029,0.8710432771751,23.0652162207104));
#16431=CARTESIAN_POINT('Ctrl Pts',(-1.8399621045117,0.773430284616103,23.0717332378804));
#16432=CARTESIAN_POINT('Ctrl Pts',(-1.86526779382775,0.710234016399131,
23.0757294286686));
#16433=CARTESIAN_POINT('Ctrl Pts',(-1.91109823134709,0.576311706650971,
23.083974474948));
#16434=CARTESIAN_POINT('Ctrl Pts',(-1.9310371488245,0.505496973663527,23.0882121008464));
#16435=CARTESIAN_POINT('Ctrl Pts',(-1.97224762056614,0.320508096779724,
23.0992750624989));
#16436=CARTESIAN_POINT('Ctrl Pts',(-1.98754377539282,0.205304950558999,
23.1061703190404));
#16437=CARTESIAN_POINT('Ctrl Pts',(-1.9933461117447,0.0760207468025642,
23.1142438290231));
#16438=CARTESIAN_POINT('Ctrl Pts',(-1.99381268178783,0.0626007273850999,
23.1150856383549));
#16439=CARTESIAN_POINT('Ctrl Pts',(-1.99429969261233,0.0428523872649563,
23.1163303205717));
#16440=CARTESIAN_POINT('Ctrl Pts',(-1.99442557610496,0.0365268521593845,
23.1167298923532));
#16441=CARTESIAN_POINT('Ctrl Pts',(-1.99459487876957,0.025345795898488,
23.1174377951233));
#16442=CARTESIAN_POINT('Ctrl Pts',(-1.9946506658732,0.0204904912615598,
23.1177457363784));
#16443=CARTESIAN_POINT('Ctrl Pts',(-1.99473016566779,0.0103480754011308,
23.1183901519715));
#16444=CARTESIAN_POINT('Ctrl Pts',(-1.99475058642723,0.00506098315732062,
23.1187267270038));
#16445=CARTESIAN_POINT('Ctrl Pts',(-1.99474902517757,-0.0087138660979068,
23.1196053566625));
#16446=CARTESIAN_POINT('Ctrl Pts',(-1.9946938891948,-0.0172014425346067,
23.1201484450481));
#16447=CARTESIAN_POINT('Ctrl Pts',(-1.99421732812472,-0.0542043318696857,
23.1225237571064));
#16448=CARTESIAN_POINT('Ctrl Pts',(-1.99323860203648,-0.0827078989382515,
23.1243733150328));
#16449=CARTESIAN_POINT('Ctrl Pts',(-1.98905590780223,-0.157635912292106,
23.1292903308347));
#16450=CARTESIAN_POINT('Ctrl Pts',(-1.98483814030236,-0.203983992940521,
23.1323879126468));
#16451=CARTESIAN_POINT('Ctrl Pts',(-1.95455248711019,-0.443592193144321,
23.1486909148887));
#16452=CARTESIAN_POINT('Ctrl Pts',(-1.90187522353625,-0.632379154602995,
23.1626549211699));
#16453=CARTESIAN_POINT('Ctrl Pts',(-1.80804089939705,-0.843392388790838,
23.1782463106551));
#16454=CARTESIAN_POINT('Ctrl Pts',(-1.79253034456599,-0.875875549766268,
23.1806414509516));
#16455=CARTESIAN_POINT('Ctrl Pts',(-1.77346524620833,-0.913172124085858,
23.1833709687034));
#16456=CARTESIAN_POINT('Ctrl Pts',(-1.77075903035547,-0.918408823045166,
23.1837537300751));
#16457=CARTESIAN_POINT('Ctrl Pts',(-1.76639735237753,-0.926757995672966,
23.1843631245572));
#16458=CARTESIAN_POINT('Ctrl Pts',(-1.76475680942004,-0.929878160354736,
23.1845906671854));
#16459=CARTESIAN_POINT('Ctrl Pts',(-1.76183874938753,-0.935392509872981,
23.1849924437385));
#16460=CARTESIAN_POINT('Ctrl Pts',(-1.76056460846337,-0.937788454904466,
23.1851668895022));
#16461=CARTESIAN_POINT('Ctrl Pts',(-1.75786827307977,-0.942833887326651,
23.1855339738396));
#16462=CARTESIAN_POINT('Ctrl Pts',(-1.75644497947497,-0.945482754450112,
23.1857265406866));
#16463=CARTESIAN_POINT('Ctrl Pts',(-1.75263144473794,-0.952541727892574,
23.1862393298405));
#16464=CARTESIAN_POINT('Ctrl Pts',(-1.75023052963959,-0.956946089857879,
23.1865588787993));
#16465=CARTESIAN_POINT('Ctrl Pts',(-1.73882750533259,-0.977677906821048,
23.1880613664042));
#16466=CARTESIAN_POINT('Ctrl Pts',(-1.72961302219979,-0.993888342299916,
23.1892312934512));
#16467=CARTESIAN_POINT('Ctrl Pts',(-1.63309970154953,-1.15826934146475,
23.2010695161742));
#16468=CARTESIAN_POINT('Ctrl Pts',(-1.52720194505438,-1.29471050508555,
23.2107312579881));
#16469=CARTESIAN_POINT('Ctrl Pts',(-1.32679705967998,-1.49358808513795,
23.2272465626159));
#16470=CARTESIAN_POINT('Ctrl Pts',(-1.24219966557471,-1.56465031829176,
23.2338246066446));
#16471=CARTESIAN_POINT('Ctrl Pts',(-1.14162357909098,-1.63581481464676,
23.2415152945552));
#16472=CARTESIAN_POINT('Ctrl Pts',(-1.13100420169006,-1.64317497163366,
23.2423256127113));
#16473=CARTESIAN_POINT('Ctrl Pts',(-1.11516086298745,-1.65392944428732,
23.2435323777622));
#16474=CARTESIAN_POINT('Ctrl Pts',(-1.10999115150386,-1.65740339060022,
23.243925808805));
#16475=CARTESIAN_POINT('Ctrl Pts',(-1.10077329374681,-1.66353514211645,
23.2446267567087));
#16476=CARTESIAN_POINT('Ctrl Pts',(-1.09673156150811,-1.66620253708753,
23.2449339099134));
#16477=CARTESIAN_POINT('Ctrl Pts',(-1.08821621177744,-1.67177794836034,
23.2455806604972));
#16478=CARTESIAN_POINT('Ctrl Pts',(-1.08374056529833,-1.67468278142873,
23.2459203736799));
#16479=CARTESIAN_POINT('Ctrl Pts',(-1.07193161152075,-1.68227999406973,
23.2468161655731));
#16480=CARTESIAN_POINT('Ctrl Pts',(-1.06457920834362,-1.68694234145723,
23.2473733540514));
#16481=CARTESIAN_POINT('Ctrl Pts',(-1.03122238256557,-1.70778984284034,
23.2498990087871));
#16482=CARTESIAN_POINT('Ctrl Pts',(-1.00487897809935,-1.7234221234075,23.251887635923));
#16483=CARTESIAN_POINT('Ctrl Pts',(-0.933475600799488,-1.76359942893007,
23.257265357599));
#16484=CARTESIAN_POINT('Ctrl Pts',(-0.887813513219818,-1.78702155907183,
23.2606920268837));
#16485=CARTESIAN_POINT('Ctrl Pts',(-0.74989968001803,-1.85117264763509,
23.2710012891206));
#16486=CARTESIAN_POINT('Ctrl Pts',(-0.655412613570665,-1.88669570874792,
23.2780208097599));
#16487=CARTESIAN_POINT('Ctrl Pts',(-0.476956152970249,-1.93875815817386,
23.2909906949848));
#16488=CARTESIAN_POINT('Ctrl Pts',(-0.393810231563768,-1.95734149815231,
23.2969216868984));
#16489=CARTESIAN_POINT('Ctrl Pts',(-0.272841538709948,-1.97635502766549,
23.3051984700274));
#16490=CARTESIAN_POINT('Ctrl Pts',(-0.23579768814716,-1.9811162493413,23.3076857610451));
#16491=CARTESIAN_POINT('Ctrl Pts',(-0.192708361052063,-1.98542856268389,
23.3105080609151));
#16492=CARTESIAN_POINT('Ctrl Pts',(-0.186774775760275,-1.98599553757468,
23.3108951482672));
#16493=CARTESIAN_POINT('Ctrl Pts',(-0.177308789349377,-1.98685724672708,
23.3115101031235));
#16494=CARTESIAN_POINT('Ctrl Pts',(-0.173778047380773,-1.98716917155475,
23.311738906018));
#16495=CARTESIAN_POINT('Ctrl Pts',(-0.167539926545156,-1.98770352783902,
23.3121421252462));
#16496=CARTESIAN_POINT('Ctrl Pts',(-0.164832902839687,-1.98792984183838,
23.3123167585887));
#16497=CARTESIAN_POINT('Ctrl Pts',(-0.159138252878659,-1.98839421675648,
23.3126833982275));
#16498=CARTESIAN_POINT('Ctrl Pts',(-0.156150557010321,-1.98863107402954,
23.3128753360066));
#16499=CARTESIAN_POINT('Ctrl Pts',(-0.148205419613642,-1.98924292951431,
23.3133846650563));
#16500=CARTESIAN_POINT('Ctrl Pts',(-0.143247050664874,-1.98960613257581,
23.3137013988908));
#16501=CARTESIAN_POINT('Ctrl Pts',(-0.120158958304453,-1.99121058944073,
23.3151712093473));
#16502=CARTESIAN_POINT('Ctrl Pts',(-0.102013460011142,-1.9922226525018,
23.3163119516667));
#16503=CARTESIAN_POINT('Ctrl Pts',(0.0721482535332635,-1.99955059285529,
23.3271443796006));
#16504=CARTESIAN_POINT('Ctrl Pts',(0.228407247983973,-1.98777586765281,
23.3359982637772));
#16505=CARTESIAN_POINT('Ctrl Pts',(0.505905225920262,-1.93367475198033,
23.3524575742911));
#16506=CARTESIAN_POINT('Ctrl Pts',(0.627495153678901,-1.89770416836332,
23.3599421174552));
#16507=CARTESIAN_POINT('Ctrl Pts',(0.756922254093729,-1.84560710890173,
23.3686500867499));
#16508=CARTESIAN_POINT('Ctrl Pts',(0.768945875507025,-1.84063008965246,
23.3694661371741));
#16509=CARTESIAN_POINT('Ctrl Pts',(0.786667708233827,-1.83309042301939,
23.3706798129451));
#16510=CARTESIAN_POINT('Ctrl Pts',(0.792404126349157,-1.83061800527753,
23.3710743714424));
#16511=CARTESIAN_POINT('Ctrl Pts',(0.802568961300915,-1.82618019315275,
23.3717765897554));
#16512=CARTESIAN_POINT('Ctrl Pts',(0.80700202865933,-1.82422552349433,23.3720838811373));
#16513=CARTESIAN_POINT('Ctrl Pts',(0.816293693860386,-1.82008805784805,
23.3727301711858));
#16514=CARTESIAN_POINT('Ctrl Pts',(0.821150751457561,-1.81790191578938,
23.3730692827983));
#16515=CARTESIAN_POINT('Ctrl Pts',(0.833885484590942,-1.81210861439441,
23.3739617862645));
#16516=CARTESIAN_POINT('Ctrl Pts',(0.84174844855115,-1.8084695676751,23.3745162731614));
#16517=CARTESIAN_POINT('Ctrl Pts',(0.8769238999694,-1.79191096902896,23.3770123905391));
#16518=CARTESIAN_POINT('Ctrl Pts',(0.903963212586597,-1.77842368151106,
23.3789736084757));
#16519=CARTESIAN_POINT('Ctrl Pts',(0.975216696786217,-1.74083740676136,
23.3842594739241));
#16520=CARTESIAN_POINT('Ctrl Pts',(1.01883999213167,-1.71567095796115,23.3876201356824));
#16521=CARTESIAN_POINT('Ctrl Pts',(1.14616281086576,-1.63564866321966,23.397804624408));
#16522=CARTESIAN_POINT('Ctrl Pts',(1.22673212697761,-1.57612204790798,23.4047656862329));
#16523=CARTESIAN_POINT('Ctrl Pts',(1.39582846739347,-1.43034182055913,23.4203430100627));
#16524=CARTESIAN_POINT('Ctrl Pts',(1.48152101030504,-1.34138651921141,23.428939245322));
#16525=CARTESIAN_POINT('Ctrl Pts',(1.56317762342597,-1.23917729437307,23.4374802745958));
#16526=CARTESIAN_POINT('Ctrl Pts',(1.56786016952027,-1.23324739713201,23.4379713729433));
#16527=CARTESIAN_POINT('Ctrl Pts',(1.57466290298419,-1.22453115928623,23.4386865991766));
#16528=CARTESIAN_POINT('Ctrl Pts',(1.57680955813855,-1.22176570418388,23.43891255525));
#16529=CARTESIAN_POINT('Ctrl Pts',(1.58060518530478,-1.21684927422991,23.4393125243509));
#16530=CARTESIAN_POINT('Ctrl Pts',(1.58225706528265,-1.21470057533529,23.4394867427081));
#16531=CARTESIAN_POINT('Ctrl Pts',(1.58574039398235,-1.21015043947522,23.4398544279491));
#16532=CARTESIAN_POINT('Ctrl Pts',(1.58757076486305,-1.20774821470317,23.4400478189554));
#16533=CARTESIAN_POINT('Ctrl Pts',(1.59246206786622,-1.20129841286687,23.4405651429938));
#16534=CARTESIAN_POINT('Ctrl Pts',(1.59551304754545,-1.19724326301008,23.4408883815903));
#16535=CARTESIAN_POINT('Ctrl Pts',(1.61008246577444,-1.17772400221129,23.4424348631599));
#16536=CARTESIAN_POINT('Ctrl Pts',(1.62139222879797,-1.16210441840951,23.4436441520524));
#16537=CARTESIAN_POINT('Ctrl Pts',(1.65234309306941,-1.11802739496867,23.4469861887131));
#16538=CARTESIAN_POINT('Ctrl Pts',(1.6714742034511,-1.08921863447767,23.4490903080501));
#16539=CARTESIAN_POINT('Ctrl Pts',(1.73855742906047,-0.982267292718258,
23.4566699342053));
#16540=CARTESIAN_POINT('Ctrl Pts',(1.78185919567237,-0.901338475025759,
23.4619702574825));
#16541=CARTESIAN_POINT('Ctrl Pts',(1.88329833705338,-0.675632609041538,
23.4763218962617));
#16542=CARTESIAN_POINT('Ctrl Pts',(1.9302826131601,-0.526585044463319,23.4853972505017));
#16543=CARTESIAN_POINT('Ctrl Pts',(1.96180649197478,-0.361249142563708,
23.4959077948642));
#16544=CARTESIAN_POINT('Ctrl Pts',(1.96404452639658,-0.348876398957765,
23.4966965630493));
#16545=CARTESIAN_POINT('Ctrl Pts',(1.96720450914525,-0.330411755365373,
23.4978773128872));
#16546=CARTESIAN_POINT('Ctrl Pts',(1.96821547587624,-0.324335240180608,
23.4982664667296));
#16547=CARTESIAN_POINT('Ctrl Pts',(1.9699695713428,-0.313481772045245,23.4989626242555));
#16548=CARTESIAN_POINT('Ctrl Pts',(1.97072351440209,-0.308706596187221,
23.4992692823731));
#16549=CARTESIAN_POINT('Ctrl Pts',(1.97227870373655,-0.298618726618705,
23.4999179216718));
#16550=CARTESIAN_POINT('Ctrl Pts',(1.97307585794811,-0.293305449916991,
23.5002600298725));
#16551=CARTESIAN_POINT('Ctrl Pts',(1.97513249206851,-0.279209461670281,
23.5011689128497));
#16552=CARTESIAN_POINT('Ctrl Pts',(1.97635484519537,-0.270421534579042,
23.5017368567759));
#16553=CARTESIAN_POINT('Ctrl Pts',(1.9817603742648,-0.229563441443843,23.5043837528508));
#16554=CARTESIAN_POINT('Ctrl Pts',(1.98522162512093,-0.197404279792403,
23.5064853128086));
#16555=CARTESIAN_POINT('Ctrl Pts',(1.99248029282498,-0.110046304635909,
23.5122471284698));
#16556=CARTESIAN_POINT('Ctrl Pts',(1.99476539572911,-0.0547538784678133,
23.515951896427));
#16557=CARTESIAN_POINT('Ctrl Pts',(1.99472083995126,0.10451325394847,23.526781267626));
#16558=CARTESIAN_POINT('Ctrl Pts',(1.9865654187481,0.208299913540758,23.5340406579857));
#16559=CARTESIAN_POINT('Ctrl Pts',(1.95915198494756,0.381997034783298,23.5463031836596));
#16560=CARTESIAN_POINT('Ctrl Pts',(1.94410889756941,0.452371616561821,23.5513002630426));
#16561=CARTESIAN_POINT('Ctrl Pts',(1.92459300799034,0.52438207763953,23.5563582050747));
#16562=CARTESIAN_POINT('Ctrl Pts',(1.92388355714886,0.526979001876972,23.5565405317299));
#16563=CARTESIAN_POINT('Ctrl Pts',(1.91293780788876,0.566728884556873,23.5593300370431));
#16564=CARTESIAN_POINT('Ctrl Pts',(1.90163135373923,0.603582109440011,23.5618992216618));
#16565=CARTESIAN_POINT('Ctrl Pts',(1.88714598905568,0.646336688542688,23.5648416176739));
#16566=CARTESIAN_POINT('Ctrl Pts',(1.88499768322268,0.652575540593402,23.5652700112501));
#16567=CARTESIAN_POINT('Ctrl Pts',(1.88169783714548,0.662006287213307,23.5659159868007));
#16568=CARTESIAN_POINT('Ctrl Pts',(1.88056907120851,0.665206015803639,23.5661348795406));
#16569=CARTESIAN_POINT('Ctrl Pts',(1.8785299182394,0.670939757755498,23.5665266041083));
#16570=CARTESIAN_POINT('Ctrl Pts',(1.87762256378575,0.673474810599133,23.566699613101));
#16571=CARTESIAN_POINT('Ctrl Pts',(1.87565131502325,0.678947322787018,23.5670726941056));
#16572=CARTESIAN_POINT('Ctrl Pts',(1.87458565584975,0.681884111765686,23.5672726588038));
#16573=CARTESIAN_POINT('Ctrl Pts',(1.87160975254923,0.690025531034069,23.5678263509243));
#16574=CARTESIAN_POINT('Ctrl Pts',(1.86968468490016,0.695224769503947,23.5681792049505));
#16575=CARTESIAN_POINT('Ctrl Pts',(1.8588546071197,0.724104388849254,23.5701353838328));
#16576=CARTESIAN_POINT('Ctrl Pts',(1.84952091343033,0.747623001823085,23.5717142674897));
#16577=CARTESIAN_POINT('Ctrl Pts',(1.77672407169122,0.921338327501038,23.5833155069715));
#16578=CARTESIAN_POINT('Ctrl Pts',(1.69549862677927,1.06344329104048,23.5925040380343));
#16579=CARTESIAN_POINT('Ctrl Pts',(1.53109117556448,1.28344508501932,23.6085625433659));
#16580=CARTESIAN_POINT('Ctrl Pts',(1.4569463657648,1.36703089007972,23.6152105917116));
#16581=CARTESIAN_POINT('Ctrl Pts',(1.36684771682189,1.45290131481923,23.6229796625555));
#16582=CARTESIAN_POINT('Ctrl Pts',(1.35739682748506,1.46173484317861,23.6237909587903));
#16583=CARTESIAN_POINT('Ctrl Pts',(1.34326708730211,1.47468638280055,23.6249989032714));
#16584=CARTESIAN_POINT('Ctrl Pts',(1.33865365091826,1.47887551771544,23.6253925269934));
#16585=CARTESIAN_POINT('Ctrl Pts',(1.33042007070808,1.48628175407773,23.6260936917885));
#16586=CARTESIAN_POINT('Ctrl Pts',(1.32680768147181,1.48950743293105,23.6264008683893));
#16587=CARTESIAN_POINT('Ctrl Pts',(1.31919197301362,1.49625818407874,23.6270475392056));
#16588=CARTESIAN_POINT('Ctrl Pts',(1.31518619492876,1.49978041287506,23.6273871487336));
#16589=CARTESIAN_POINT('Ctrl Pts',(1.30461071510917,1.50900434553152,23.6282823740344));
#16590=CARTESIAN_POINT('Ctrl Pts',(1.29801781657593,1.5146791662547,23.6288390970325));
#16591=CARTESIAN_POINT('Ctrl Pts',(1.26852141581792,1.539734112662,23.6313239912969));
#16592=CARTESIAN_POINT('Ctrl Pts',(1.24522053660386,1.55863830704041,23.6332714379365));
#16593=CARTESIAN_POINT('Ctrl Pts',(1.18191530166107,1.60767261629807,23.6385249713219));
#16594=CARTESIAN_POINT('Ctrl Pts',(1.14118987123898,1.63683230458749,23.6418667609568));
#16595=CARTESIAN_POINT('Ctrl Pts',(0.940859549598415,1.7691576096526,23.6581228254526));
#16596=CARTESIAN_POINT('Ctrl Pts',(0.768181820920613,1.85068050346722,23.6717211793796));
#16597=CARTESIAN_POINT('Ctrl Pts',(0.552643863484696,1.91699617388569,23.6869401403451));
#16598=CARTESIAN_POINT('Ctrl Pts',(0.518414199006579,1.92653488787829,23.6893038023525));
#16599=CARTESIAN_POINT('Ctrl Pts',(0.478249402392898,1.93657934166554,23.6920015694262));
#16600=CARTESIAN_POINT('Ctrl Pts',(0.472546934248044,1.93797869814918,23.6923828249911));
#16601=CARTESIAN_POINT('Ctrl Pts',(0.463417611951749,1.94017629571473,23.692990282724));
#16602=CARTESIAN_POINT('Ctrl Pts',(0.45999473453063,1.9409906713302,23.6932173854796));
#16603=CARTESIAN_POINT('Ctrl Pts',(0.453929010551228,1.94241689000338,23.6936186599172));
#16604=CARTESIAN_POINT('Ctrl Pts',(0.451287051159835,1.94303240297234,23.6937930416336));
#16605=CARTESIAN_POINT('Ctrl Pts',(0.445710364076144,1.94431964897152,23.6941602878834));
#16606=CARTESIAN_POINT('Ctrl Pts',(0.442775376528311,1.94499012651898,23.6943530795521));
#16607=CARTESIAN_POINT('Ctrl Pts',(0.435029191163544,1.94674124639669,23.6948606453425));
#16608=CARTESIAN_POINT('Ctrl Pts',(0.430215446881831,1.9478107064346,23.6951747824341));
#16609=CARTESIAN_POINT('Ctrl Pts',(0.408050723907701,1.95264882282056,23.6966155324378));
#16610=CARTESIAN_POINT('Ctrl Pts',(0.390653213139125,1.95620370573333,23.6977304015264));
#16611=CARTESIAN_POINT('Ctrl Pts',(0.204940835335811,1.99157434516518,23.7094837883902));
#16612=CARTESIAN_POINT('Ctrl Pts',(0.0332189798035813,2.00182024001185,
23.7191134295983));
#16613=CARTESIAN_POINT('Ctrl Pts',(-0.249371251815618,1.98226314295159,
23.735673871603));
#16614=CARTESIAN_POINT('Ctrl Pts',(-0.360157589699307,1.96515504596192,
23.7423425028749));
#16615=CARTESIAN_POINT('Ctrl Pts',(-0.481494251299651,1.9358094723581,23.7501346318597));
#16616=CARTESIAN_POINT('Ctrl Pts',(-0.494042288972022,1.93264513851989,
23.7509462056751));
#16617=CARTESIAN_POINT('Ctrl Pts',(-0.512586591501544,1.92777628177231,
23.7521544848603));
#16618=CARTESIAN_POINT('Ctrl Pts',(-0.518607257418771,1.92616534011788,
23.7525481632421));
#16619=CARTESIAN_POINT('Ctrl Pts',(-0.529292821961587,1.92325248647641,
23.7532493895822));
#16620=CARTESIAN_POINT('Ctrl Pts',(-0.533960735595123,1.92196174527034,
23.7535565728365));
#16621=CARTESIAN_POINT('Ctrl Pts',(-0.543759390674064,1.91921383261398,
23.7542032211045));
#16622=CARTESIAN_POINT('Ctrl Pts',(-0.548889073906283,1.91775305862833,
23.7545428012916));
#16623=CARTESIAN_POINT('Ctrl Pts',(-0.562367470627117,1.91385632305801,
23.7554378662082));
#16624=CARTESIAN_POINT('Ctrl Pts',(-0.570706147551424,1.91138632581234,
23.7559944574439));
#16625=CARTESIAN_POINT('Ctrl Pts',(-0.604992364418687,1.90098605029883,
23.7582949190547));
#16626=CARTESIAN_POINT('Ctrl Pts',(-0.630791909139028,1.89258161542398,
23.7600542336474));
#16627=CARTESIAN_POINT('Ctrl Pts',(-0.698689076826157,1.8689209807639,23.7647621105274));
#16628=CARTESIAN_POINT('Ctrl Pts',(-0.740456204801879,1.85276986005703,
23.7677390252861));
#16629=CARTESIAN_POINT('Ctrl Pts',(-0.909454284734698,1.78079188784509,
23.7801191361801));
#16630=CARTESIAN_POINT('Ctrl Pts',(-1.03121915171044,1.71315659905379,23.789871457052));
#16631=CARTESIAN_POINT('Ctrl Pts',(-1.22072439977651,1.58032328031969,23.8059602169694));
#16632=CARTESIAN_POINT('Ctrl Pts',(-1.29271876487694,1.52199618006782,23.8123206104895));
#16633=CARTESIAN_POINT('Ctrl Pts',(-1.36615420523471,1.45351709097308,23.8188795583615));
#16634=CARTESIAN_POINT('Ctrl Pts',(-1.3718666376865,1.44812678298547,23.8193902384723));
#16635=CARTESIAN_POINT('Ctrl Pts',(-1.38011944227563,1.4402466928626,23.820128510716));
#16636=CARTESIAN_POINT('Ctrl Pts',(-1.38268513775431,1.43778371863211,23.820358099703));
#16637=CARTESIAN_POINT('Ctrl Pts',(-1.38720015276246,1.43342620580564,23.8207622217604));
#16638=CARTESIAN_POINT('Ctrl Pts',(-1.38915220347169,1.43153452884168,23.8209369750641));
#16639=CARTESIAN_POINT('Ctrl Pts',(-1.39324406521857,1.42755297040368,23.8213033512786));
#16640=CARTESIAN_POINT('Ctrl Pts',(-1.39538303964321,1.42546226942006,23.8214949076363));
#16641=CARTESIAN_POINT('Ctrl Pts',(-1.39973270937868,1.42119159301034,23.8218845401698));
#16642=CARTESIAN_POINT('Ctrl Pts',(-1.40194303478421,1.41901125058355,23.8220825868988));
#16643=CARTESIAN_POINT('Ctrl Pts',(-1.41135220183156,1.40968627479287,23.8229259225855));
#16644=CARTESIAN_POINT('Ctrl Pts',(-1.41850175010443,1.40249179187023,23.8235674014619));
#16645=CARTESIAN_POINT('Ctrl Pts',(-1.47692329544274,1.34279929116321,23.8288179677158));
#16646=CARTESIAN_POINT('Ctrl Pts',(-1.5253237470081,1.28755676184601,23.8332251170261));
#16647=CARTESIAN_POINT('Ctrl Pts',(-1.60653713303421,1.18383649492422,23.8409893840692));
#16648=CARTESIAN_POINT('Ctrl Pts',(-1.6404691108211,1.13635025668703,23.8443725172661));
#16649=CARTESIAN_POINT('Ctrl Pts',(-1.75326816242585,0.962887809147457,
23.8563728741762));
#16650=CARTESIAN_POINT('Ctrl Pts',(-1.82008480420641,0.82969052032929,23.864993293892));
#16651=CARTESIAN_POINT('Ctrl Pts',(-1.87616565224984,0.677652026728188,
23.8750178796965));
#16652=CARTESIAN_POINT('Ctrl Pts',(-1.88070891294721,0.664938940771866,
23.8758570534069));
#16653=CARTESIAN_POINT('Ctrl Pts',(-1.88906313910096,0.640791131455061,
23.8774533668785));
#16654=CARTESIAN_POINT('Ctrl Pts',(-1.89290020856103,0.629366036516225,
23.8782096185501));
#16655=CARTESIAN_POINT('Ctrl Pts',(-1.89853473711962,0.612071145671082,
23.8793561668438));
#16656=CARTESIAN_POINT('Ctrl Pts',(-1.90040906792504,0.606226532405844,
23.8797439313981));
#16657=CARTESIAN_POINT('Ctrl Pts',(-1.90371064622489,0.595765628862508,
23.8804385434803));
#16658=CARTESIAN_POINT('Ctrl Pts',(-1.90514815752673,0.591152608285838,
23.8807450513088));
#16659=CARTESIAN_POINT('Ctrl Pts',(-1.90815241219042,0.581387080402761,
23.8813943551046));
#16660=CARTESIAN_POINT('Ctrl Pts',(-1.90971507567197,0.576233367847167,
23.8817372818706));
#16661=CARTESIAN_POINT('Ctrl Pts',(-1.91381323816139,0.5625177217628,23.8826506400654));
#16662=CARTESIAN_POINT('Ctrl Pts',(-1.91631212581144,0.553945060475702,
23.8832222612265));
#16663=CARTESIAN_POINT('Ctrl Pts',(-1.92164618138673,0.535177986340756,
23.8844753789138));
#16664=CARTESIAN_POINT('Ctrl Pts',(-1.92445794802636,0.524977259124959,
23.885157618341));
#16665=CARTESIAN_POINT('Ctrl Pts',(-1.93258636608511,0.49454530847942,23.8871964645244));
#16666=CARTESIAN_POINT('Ctrl Pts',(-1.93766594980546,0.474252819067026,
23.8885606169804));
#16667=CARTESIAN_POINT('Ctrl Pts',(-1.97733335685798,0.30449394592668,23.9000136371151));
#16668=CARTESIAN_POINT('Ctrl Pts',(-1.9948831837466,0.151605765928437,23.9106520774232));
#16669=CARTESIAN_POINT('Ctrl Pts',(-1.99474923905662,-0.00174234986216392,
23.9213503181716));
#16670=CARTESIAN_POINT('',(-1.99474926718243,0.0010867435194402,25.5194715405958));
#16671=CARTESIAN_POINT('Ctrl Pts',(-1.99474923809175,-0.00174345415664474,
23.921350395212));
#16672=CARTESIAN_POINT('Ctrl Pts',(-1.99465279067116,-0.112092451863815,
23.9290488277685));
#16673=CARTESIAN_POINT('Ctrl Pts',(-1.98539976672746,-0.222258981767481,
23.9367300039541));
#16674=CARTESIAN_POINT('Ctrl Pts',(-1.9655027770055,-0.340465031149384,
23.9446282277757));
#16675=CARTESIAN_POINT('Ctrl Pts',(-1.96386091420468,-0.349811265962468,
23.9452502755261));
#16676=CARTESIAN_POINT('Ctrl Pts',(-1.96129918682364,-0.363806979434425,
23.9461777490928));
#16677=CARTESIAN_POINT('Ctrl Pts',(-1.96042937329275,-0.368465319865975,
23.94648577956));
#16678=CARTESIAN_POINT('Ctrl Pts',(-1.95895292373932,-0.376219291464799,
23.9469973399604));
#16679=CARTESIAN_POINT('Ctrl Pts',(-1.95835553605177,-0.379316632175001,
23.9472013731833));
#16680=CARTESIAN_POINT('Ctrl Pts',(-1.95717076530788,-0.385382033945181,
23.9476002971232));
#16681=CARTESIAN_POINT('Ctrl Pts',(-1.95658397186845,-0.388350200194083,
23.9477952203578));
#16682=CARTESIAN_POINT('Ctrl Pts',(-1.95545899848093,-0.393973357184122,
23.9481639272714));
#16683=CARTESIAN_POINT('Ctrl Pts',(-1.95492217013066,-0.396628553850687,
23.9483377825302));
#16684=CARTESIAN_POINT('Ctrl Pts',(-1.95368117794911,-0.402702872206078,
23.9487349645909));
#16685=CARTESIAN_POINT('Ctrl Pts',(-1.95297344754239,-0.406121240522431,
23.9489580850993));
#16686=CARTESIAN_POINT('Ctrl Pts',(-1.95107046975322,-0.415192690172853,
23.9495491769418));
#16687=CARTESIAN_POINT('Ctrl Pts',(-1.94985961674241,-0.420842517918806,
23.9499162733754));
#16688=CARTESIAN_POINT('Ctrl Pts',(-1.94142015396722,-0.459402516522879,
23.9524150602883));
#16689=CARTESIAN_POINT('Ctrl Pts',(-1.93338273436137,-0.492132517417653,
23.954502973977));
#16690=CARTESIAN_POINT('Ctrl Pts',(-1.90440374169407,-0.598434083893761,
23.9612223348132));
#16691=CARTESIAN_POINT('Ctrl Pts',(-1.88005922411456,-0.671011385436395,
23.9657133471563));
#16692=CARTESIAN_POINT('Ctrl Pts',(-1.83716998721847,-0.778035824832143,
23.9724255051228));
#16693=CARTESIAN_POINT('Ctrl Pts',(-1.8216874782631,-0.813626497658147,
23.9746729601069));
#16694=CARTESIAN_POINT('Ctrl Pts',(-1.79086914167354,-0.879173470817844,
23.9788748868046));
#16695=CARTESIAN_POINT('Ctrl Pts',(-1.77579462330578,-0.909236868255141,
23.9808277094315));
#16696=CARTESIAN_POINT('Ctrl Pts',(-1.71652760379852,-1.02033233302828,
23.9881802475092));
#16697=CARTESIAN_POINT('Ctrl Pts',(-1.66749369487277,-1.09863874415188,
23.9936466243389));
#16698=CARTESIAN_POINT('Ctrl Pts',(-1.5952864039728,-1.19792255513778,24.001181778613));
#16699=CARTESIAN_POINT('Ctrl Pts',(-1.57679117181271,-1.22216471970837,
24.0030729722191));
#16700=CARTESIAN_POINT('Ctrl Pts',(-1.55227739557933,-1.25281250263351,
24.0055356771755));
#16701=CARTESIAN_POINT('Ctrl Pts',(-1.54676148439092,-1.25961628524112,
24.0060870758325));
#16702=CARTESIAN_POINT('Ctrl Pts',(-1.5378061436593,-1.27051502241697,24.0069780273091));
#16703=CARTESIAN_POINT('Ctrl Pts',(-1.53439470184874,-1.27463291017202,
24.0073164452571));
#16704=CARTESIAN_POINT('Ctrl Pts',(-1.52786418681096,-1.28245156367787,
24.0079624455536));
#16705=CARTESIAN_POINT('Ctrl Pts',(-1.5247481174861,-1.28615479786205,24.0082699038189));
#16706=CARTESIAN_POINT('Ctrl Pts',(-1.51760552899487,-1.29458083506208,
24.0089728930618));
#16707=CARTESIAN_POINT('Ctrl Pts',(-1.51357039935403,-1.29929624216576,
24.0093687767347));
#16708=CARTESIAN_POINT('Ctrl Pts',(-1.50114117973247,-1.31368441565182,
24.0105844077761));
#16709=CARTESIAN_POINT('Ctrl Pts',(-1.49267601609012,-1.32329508564254,
24.0114070985766));
#16710=CARTESIAN_POINT('Ctrl Pts',(-1.38615133566813,-1.44191193243975,
24.0216969295528));
#16711=CARTESIAN_POINT('Ctrl Pts',(-1.27647576917412,-1.53984363938957,
24.0316879210935));
#16712=CARTESIAN_POINT('Ctrl Pts',(-1.0702558457911,-1.68669602331309,24.0493104153485));
#16713=CARTESIAN_POINT('Ctrl Pts',(-0.978603550161111,-1.74147288182424,
24.0568001916866));
#16714=CARTESIAN_POINT('Ctrl Pts',(-0.855730961011988,-1.80213140402328,
24.0661142930362));
#16715=CARTESIAN_POINT('Ctrl Pts',(-0.828145634363181,-1.8149733047239,
24.0681603329142));
#16716=CARTESIAN_POINT('Ctrl Pts',(-0.784218998465963,-1.83421247526352,
24.0713365951796));
#16717=CARTESIAN_POINT('Ctrl Pts',(-0.768069486342853,-1.84103344833148,
24.0724872693959));
#16718=CARTESIAN_POINT('Ctrl Pts',(-0.747291076407721,-1.84948848021564,
24.0739441232411));
#16719=CARTESIAN_POINT('Ctrl Pts',(-0.742743809329414,-1.8513193204498,
24.0742615129731));
#16720=CARTESIAN_POINT('Ctrl Pts',(-0.735399127518461,-1.85424505102597,
24.0747717891419));
#16721=CARTESIAN_POINT('Ctrl Pts',(-0.732605943601032,-1.85535040294364,
24.0749652969065));
#16722=CARTESIAN_POINT('Ctrl Pts',(-0.727283928081611,-1.8574426018349,
24.0753329370241));
#16723=CARTESIAN_POINT('Ctrl Pts',(-0.724755610275348,-1.85843058428661,
24.0755071341862));
#16724=CARTESIAN_POINT('Ctrl Pts',(-0.718933757633465,-1.86069188286548,
24.0759072128252));
#16725=CARTESIAN_POINT('Ctrl Pts',(-0.715638855198403,-1.86196161620634,
24.0761328774428));
#16726=CARTESIAN_POINT('Ctrl Pts',(-0.706815859720396,-1.86533479211552,
24.0767351648404));
#16727=CARTESIAN_POINT('Ctrl Pts',(-0.701281701269774,-1.86742242778882,
24.0771108591689));
#16728=CARTESIAN_POINT('Ctrl Pts',(-0.66162711299586,-1.8821800789354,24.0797885291145));
#16729=CARTESIAN_POINT('Ctrl Pts',(-0.627172277782475,-1.89393970981801,
24.0820393367));
#16730=CARTESIAN_POINT('Ctrl Pts',(-0.551681195802812,-1.91741882002782,
24.0868472279642));
#16731=CARTESIAN_POINT('Ctrl Pts',(-0.510551773686136,-1.92877794768979,
24.0893892755834));
#16732=CARTESIAN_POINT('Ctrl Pts',(-0.323099646129521,-1.97413126349641,
24.100755001292));
#16733=CARTESIAN_POINT('Ctrl Pts',(-0.173591687040931,-1.99285105981596,
24.1092601102918));
#16734=CARTESIAN_POINT('Ctrl Pts',(0.0240842515977598,-1.99516971525552,
24.1210459103544));
#16735=CARTESIAN_POINT('Ctrl Pts',(0.0715662878921597,-1.99403109702275,
24.1239139078616));
#16736=CARTESIAN_POINT('Ctrl Pts',(0.147359413969956,-1.98950299507709,
24.128580815825));
#16737=CARTESIAN_POINT('Ctrl Pts',(0.175718014996744,-1.98719903766466,
24.1303468470648));
#16738=CARTESIAN_POINT('Ctrl Pts',(0.212757002036039,-1.98339083978368,
24.1326832479322));
#16739=CARTESIAN_POINT('Ctrl Pts',(0.221491287196444,-1.9824344556556,24.1332363726432));
#16740=CARTESIAN_POINT('Ctrl Pts',(0.235536690430103,-1.9808025371232,24.1341294442246));
#16741=CARTESIAN_POINT('Ctrl Pts',(0.240851971477427,-1.9801632636064,24.1344682463535));
#16742=CARTESIAN_POINT('Ctrl Pts',(0.250966031543559,-1.97890551165015,
24.1351145394054));
#16743=CARTESIAN_POINT('Ctrl Pts',(0.255765266877857,-1.97829095448804,
24.1354219043741));
#16744=CARTESIAN_POINT('Ctrl Pts',(0.26670389895806,-1.97684975863752,24.1361240639416));
#16745=CARTESIAN_POINT('Ctrl Pts',(0.272841752749752,-1.97601197224867,
24.1365192082104));
#16746=CARTESIAN_POINT('Ctrl Pts',(0.288768295710323,-1.97376245909409,
24.1375475675274));
#16747=CARTESIAN_POINT('Ctrl Pts',(0.298550471832266,-1.97230651356485,
24.1381821751678));
#16748=CARTESIAN_POINT('Ctrl Pts',(0.360902967211727,-1.96255168495387,
24.1422466868669));
#16749=CARTESIAN_POINT('Ctrl Pts',(0.41312975383929,-1.95222513536441,24.1457404505359));
#16750=CARTESIAN_POINT('Ctrl Pts',(0.493921979091102,-1.93286333653532,
24.1512909246542));
#16751=CARTESIAN_POINT('Ctrl Pts',(0.522805370618792,-1.92525167296347,
24.1533047261749));
#16752=CARTESIAN_POINT('Ctrl Pts',(0.700896802238948,-1.87401602107133,
24.1659001550139));
#16753=CARTESIAN_POINT('Ctrl Pts',(0.844732785471984,-1.8137285152229,24.1769147240754));
#16754=CARTESIAN_POINT('Ctrl Pts',(1.01717125465571,-1.71645026982445,24.1905156988104));
#16755=CARTESIAN_POINT('Ctrl Pts',(1.05356330410089,-1.69435644420534,24.193406871667));
#16756=CARTESIAN_POINT('Ctrl Pts',(1.10785586492808,-1.65896884516567,24.1977225723866));
#16757=CARTESIAN_POINT('Ctrl Pts',(1.12628537179292,-1.64651256017508,24.199187926505));
#16758=CARTESIAN_POINT('Ctrl Pts',(1.14884918654194,-1.63070575536196,24.2009787457159));
#16759=CARTESIAN_POINT('Ctrl Pts',(1.15318266446678,-1.6276441435174,24.201322528226));
#16760=CARTESIAN_POINT('Ctrl Pts',(1.1600250501193,-1.62276893866617,24.2018650386116));
#16761=CARTESIAN_POINT('Ctrl Pts',(1.16254200175584,-1.62096676081837,24.2020645330235));
#16762=CARTESIAN_POINT('Ctrl Pts',(1.16724314087684,-1.61758408776861,24.202437006543));
#16763=CARTESIAN_POINT('Ctrl Pts',(1.16942829507573,-1.61600504136666,24.202610078474));
#16764=CARTESIAN_POINT('Ctrl Pts',(1.17438936357263,-1.61240471845241,24.2030028866066));
#16765=CARTESIAN_POINT('Ctrl Pts',(1.17716325780369,-1.6103807060039,24.2032224300741));
#16766=CARTESIAN_POINT('Ctrl Pts',(1.18540549262256,-1.604333963078,24.2038745545989));
#16767=CARTESIAN_POINT('Ctrl Pts',(1.19085860858676,-1.60029041882337,24.2043057178331));
#16768=CARTESIAN_POINT('Ctrl Pts',(1.23057322461868,-1.57052618273185,24.2074446060734));
#16769=CARTESIAN_POINT('Ctrl Pts',(1.26402178832222,-1.54373330140024,24.2100815212263));
#16770=CARTESIAN_POINT('Ctrl Pts',(1.31132018422234,-1.50327740400627,24.2138430072335));
#16771=CARTESIAN_POINT('Ctrl Pts',(1.32587203846001,-1.49045863996984,24.2150049986557));
#16772=CARTESIAN_POINT('Ctrl Pts',(1.4197816107232,-1.40526952655246,24.2225525144359));
#16773=CARTESIAN_POINT('Ctrl Pts',(1.49337437433657,-1.32679978512355,24.2287070769935));
#16774=CARTESIAN_POINT('Ctrl Pts',(1.63924810156653,-1.14365761095221,24.2423338040877));
#16775=CARTESIAN_POINT('Ctrl Pts',(1.70856460972787,-1.03724984490412,24.2498235495663));
#16776=CARTESIAN_POINT('Ctrl Pts',(1.77368214543783,-0.912834937453798,
24.2585810730765));
#16777=CARTESIAN_POINT('Ctrl Pts',(1.77992145239572,-0.900608452332835,
24.2594413874956));
#16778=CARTESIAN_POINT('Ctrl Pts',(1.78887675680459,-0.882603116836053,
24.260708296405));
#16779=CARTESIAN_POINT('Ctrl Pts',(1.79169207574805,-0.876873888907671,
24.2611114163569));
#16780=CARTESIAN_POINT('Ctrl Pts',(1.79660387799518,-0.866755861908511,
24.2618233746603));
#16781=CARTESIAN_POINT('Ctrl Pts',(1.79871191132452,-0.862372702462842,
24.2621318081385));
#16782=CARTESIAN_POINT('Ctrl Pts',(1.80279016010193,-0.853812934315414,
24.2627341815745));
#16783=CARTESIAN_POINT('Ctrl Pts',(1.80476194522063,-0.849637104096287,
24.2630280646748));
#16784=CARTESIAN_POINT('Ctrl Pts',(1.81001545410144,-0.838410461586305,
24.263818236068));
#16785=CARTESIAN_POINT('Ctrl Pts',(1.81327044726143,-0.831347297122637,
24.2643154432615));
#16786=CARTESIAN_POINT('Ctrl Pts',(1.825031216009,-0.805429371343678,24.2661403235196));
#16787=CARTESIAN_POINT('Ctrl Pts',(1.83328464078335,-0.786462194827535,
24.267476597395));
#16788=CARTESIAN_POINT('Ctrl Pts',(1.90551667062883,-0.613147517489005,
24.2796984130807));
#16789=CARTESIAN_POINT('Ctrl Pts',(1.95014818225195,-0.451489706270898,
24.2912644850565));
#16790=CARTESIAN_POINT('Ctrl Pts',(1.98391298754606,-0.218595361575162,
24.3076817646254));
#16791=CARTESIAN_POINT('Ctrl Pts',(1.99023569928573,-0.150523786525468,
24.3124396476893));
#16792=CARTESIAN_POINT('Ctrl Pts',(1.99447905525916,-0.0477118212640706,
24.319462270324));
#16793=CARTESIAN_POINT('Ctrl Pts',(1.99500651553182,-0.0131309361932714,
24.3217962472275));
#16794=CARTESIAN_POINT('Ctrl Pts',(1.99442734688521,0.040730414786778,24.3253710777205));
#16795=CARTESIAN_POINT('Ctrl Pts',(1.99394040476064,0.0600094924994351,
24.3266385612098));
#16796=CARTESIAN_POINT('Ctrl Pts',(1.99297224901735,0.084350043741496,24.3282210238128));
#16797=CARTESIAN_POINT('Ctrl Pts',(1.99275120751043,0.0894200289155129,
24.3285496652554));
#16798=CARTESIAN_POINT('Ctrl Pts',(1.99236775925638,0.0975058729650793,
24.3290721821101));
#16799=CARTESIAN_POINT('Ctrl Pts',(1.99221784929738,0.100522259355966,24.3292667458315));
#16800=CARTESIAN_POINT('Ctrl Pts',(1.99192040963798,0.106244951995511,24.3296351767487));
#16801=CARTESIAN_POINT('Ctrl Pts',(1.9917742166748,0.108951264478881,24.3298091138144));
#16802=CARTESIAN_POINT('Ctrl Pts',(1.99142654850298,0.115152593399556,24.3302070089047));
#16803=CARTESIAN_POINT('Ctrl Pts',(1.99122138840926,0.118647379439393,24.3304307580262));
#16804=CARTESIAN_POINT('Ctrl Pts',(1.99054439881678,0.129682854629902,24.3311358046469));
#16805=CARTESIAN_POINT('Ctrl Pts',(1.99003892020851,0.137221524846043,24.331615252671));
#16806=CARTESIAN_POINT('Ctrl Pts',(1.98052531225459,0.267973035464976,24.3398956453475));
#16807=CARTESIAN_POINT('Ctrl Pts',(1.96013097686202,0.390111179758361,24.347096542537));
#16808=CARTESIAN_POINT('Ctrl Pts',(1.90303792717769,0.606180446493574,24.360069550165));
#16809=CARTESIAN_POINT('Ctrl Pts',(1.87029669565566,0.700711897142247,24.3658330992057));
#16810=CARTESIAN_POINT('Ctrl Pts',(1.80056189805657,0.861816562679126,24.376274683477));
#16811=CARTESIAN_POINT('Ctrl Pts',(1.76658773575693,0.929471168230145,24.3808661325634));
#16812=CARTESIAN_POINT('Ctrl Pts',(1.72321374659392,1.00483328680699,24.3863041298895));
#16813=CARTESIAN_POINT('Ctrl Pts',(1.71748724564385,1.01459011593004,24.3870145854276));
#16814=CARTESIAN_POINT('Ctrl Pts',(1.70864694147781,1.02936292832067,24.3881003338285));
#16815=CARTESIAN_POINT('Ctrl Pts',(1.70559328749342,1.03441478395331,24.3884734335319));
#16816=CARTESIAN_POINT('Ctrl Pts',(1.7002510890917,1.04316475666656,24.3891228329462));
#16817=CARTESIAN_POINT('Ctrl Pts',(1.69797277958277,1.04686910108838,24.3893987555987));
#16818=CARTESIAN_POINT('Ctrl Pts',(1.69320296228229,1.05456789930382,24.3899743035228));
#16819=CARTESIAN_POINT('Ctrl Pts',(1.69070939342061,1.05856103843683,24.3902740036549));
#16820=CARTESIAN_POINT('Ctrl Pts',(1.68381607659257,1.06951333341939,24.3910992895908));
#16821=CARTESIAN_POINT('Ctrl Pts',(1.67938738019203,1.07645407428068,24.3916259462001));
#16822=CARTESIAN_POINT('Ctrl Pts',(1.66381088131199,1.10053577774974,24.393466153971));
#16823=CARTESIAN_POINT('Ctrl Pts',(1.65244290318465,1.11753212339374,24.3947879021905));
#16824=CARTESIAN_POINT('Ctrl Pts',(1.553307943506,1.26092895789727,24.4061409948184));
#16825=CARTESIAN_POINT('Ctrl Pts',(1.45146380432375,1.37693216016352,24.4167397099128));
#16826=CARTESIAN_POINT('Ctrl Pts',(1.24286395492987,1.56541568042858,24.4363525405638));
#16827=CARTESIAN_POINT('Ctrl Pts',(1.14043242965982,1.64154139354727,24.4452620599943));
#16828=CARTESIAN_POINT('Ctrl Pts',(1.02307466799342,1.71243719233642,24.4542467322188));
#16829=CARTESIAN_POINT('Ctrl Pts',(1.01467939891546,1.71742500296605,24.4548830692597));
#16830=CARTESIAN_POINT('Ctrl Pts',(1.00285613105903,1.72433250019094,24.4557699538541));
#16831=CARTESIAN_POINT('Ctrl Pts',(0.999458745204333,1.72630391533398,24.4560237311901));
#16832=CARTESIAN_POINT('Ctrl Pts',(0.993654395430378,1.72964915095251,24.4564554579586));
#16833=CARTESIAN_POINT('Ctrl Pts',(0.991250361729803,1.731028007763,24.4566337318285));
#16834=CARTESIAN_POINT('Ctrl Pts',(0.986644425630587,1.73365704537647,24.4569742512903));
#16835=CARTESIAN_POINT('Ctrl Pts',(0.984443014531997,1.73490804509254,24.4571365510909));
#16836=CARTESIAN_POINT('Ctrl Pts',(0.979224826230272,1.73786026398153,24.4575202097655));
#16837=CARTESIAN_POINT('Ctrl Pts',(0.976205976155617,1.73955783174615,24.4577413337628));
#16838=CARTESIAN_POINT('Ctrl Pts',(0.967182128225263,1.74460125745333,24.4583998774732));
#16839=CARTESIAN_POINT('Ctrl Pts',(0.961164163686093,1.74792398873556,24.4588358510935));
#16840=CARTESIAN_POINT('Ctrl Pts',(0.850580883783602,1.80823712305644,24.4667907576366));
#16841=CARTESIAN_POINT('Ctrl Pts',(0.741118302338165,1.85579153776437,24.4737522235301));
#16842=CARTESIAN_POINT('Ctrl Pts',(0.531813067990394,1.92522292595316,24.4865610883943));
#16843=CARTESIAN_POINT('Ctrl Pts',(0.433282923212879,1.9497623728666,24.4924027281299));
#16844=CARTESIAN_POINT('Ctrl Pts',(0.28194835801721,1.97541069586179,24.5015184778251));
#16845=CARTESIAN_POINT('Ctrl Pts',(0.230259840528209,1.98210041858869,24.5046548890355));
#16846=CARTESIAN_POINT('Ctrl Pts',(0.147520336951575,1.98952878325001,24.5097521605438));
#16847=CARTESIAN_POINT('Ctrl Pts',(0.116610259064667,1.99157950179583,24.5116731847748));
#16848=CARTESIAN_POINT('Ctrl Pts',(0.0769338970957597,1.99328501037302,
24.5141652903314));
#16849=CARTESIAN_POINT('Ctrl Pts',(0.0681993019638421,1.99360297160564,
24.5147155398574));
#16850=CARTESIAN_POINT('Ctrl Pts',(0.0541220424738574,1.99402279784403,
24.5156050799119));
#16851=CARTESIAN_POINT('Ctrl Pts',(0.0487804996123187,1.99416061934702,
24.5159432421207));
#16852=CARTESIAN_POINT('Ctrl Pts',(0.038598871393781,1.9943823913274,24.516589048915));
#16853=CARTESIAN_POINT('Ctrl Pts',(0.0337589009995935,1.99447018820393,
24.5168965706667));
#16854=CARTESIAN_POINT('Ctrl Pts',(0.0227053724201449,1.99463045250019,
24.5176001188872));
#16855=CARTESIAN_POINT('Ctrl Pts',(0.0164917229766111,1.99469150437021,
24.5179965000875));
#16856=CARTESIAN_POINT('Ctrl Pts',(-0.00256827801079911,1.99478971230896,
24.519215154022));
#16857=CARTESIAN_POINT('Ctrl Pts',(-0.0154145857663771,1.99473180405164,
24.5200403915418));
#16858=CARTESIAN_POINT('Ctrl Pts',(-0.172184840180993,1.99251065078239,
24.5301601197068));
#16859=CARTESIAN_POINT('Ctrl Pts',(-0.315436724216096,1.9749000268383,24.5399580096762));
#16860=CARTESIAN_POINT('Ctrl Pts',(-0.552149893694806,1.91937728125612,
24.5568744293126));
#16861=CARTESIAN_POINT('Ctrl Pts',(-0.646955330323089,1.88953126734442,
24.5638452416923));
#16862=CARTESIAN_POINT('Ctrl Pts',(-0.773692497982777,1.83897003895562,
24.5731792577456));
#16863=CARTESIAN_POINT('Ctrl Pts',(-0.807848050673968,1.82422388238281,
24.5756952989373));
#16864=CARTESIAN_POINT('Ctrl Pts',(-0.859979598503877,1.79996522289418,
24.5795158526611));
#16865=CARTESIAN_POINT('Ctrl Pts',(-0.878254925247854,1.79111922520407,
24.5808513263986));
#16866=CARTESIAN_POINT('Ctrl Pts',(-0.901006199927359,1.77967470578203,
24.5825060938361));
#16867=CARTESIAN_POINT('Ctrl Pts',(-0.90561056873868,1.77733613307732,24.5828405780685));
#16868=CARTESIAN_POINT('Ctrl Pts',(-0.912910953474712,1.77359251104837,
24.5833702075762));
#16869=CARTESIAN_POINT('Ctrl Pts',(-0.915612888767559,1.77219915428476,
24.5835660735578));
#16870=CARTESIAN_POINT('Ctrl Pts',(-0.920713568435187,1.76955401390615,
24.583935519528));
#16871=CARTESIAN_POINT('Ctrl Pts',(-0.923112921844298,1.76830354205627,
24.58410917555));
#16872=CARTESIAN_POINT('Ctrl Pts',(-0.928579767823083,1.76544022489674,
24.5845045565699));
#16873=CARTESIAN_POINT('Ctrl Pts',(-0.931645601753395,1.76382426734391,
24.5847260818944));
#16874=CARTESIAN_POINT('Ctrl Pts',(-0.939736413563216,1.75953273459614,
24.5853101883261));
#16875=CARTESIAN_POINT('Ctrl Pts',(-0.944754220846486,1.75684360008956,
24.5856719271693));
#16876=CARTESIAN_POINT('Ctrl Pts',(-0.977996552490043,1.73884481977141,
24.5880654306901));
#16877=CARTESIAN_POINT('Ctrl Pts',(-1.00586130043403,1.72287605264944,24.5900574896322));
#16878=CARTESIAN_POINT('Ctrl Pts',(-1.0423339995788,1.70078752285367,24.5926622664386));
#16879=CARTESIAN_POINT('Ctrl Pts',(-1.05129465642398,1.69526337715488,24.593301990847));
#16880=CARTESIAN_POINT('Ctrl Pts',(-1.21488619405234,1.5926150738254,24.6049850767716));
#16881=CARTESIAN_POINT('Ctrl Pts',(-1.35551269500975,1.47477784745069,24.6151685484025));
#16882=CARTESIAN_POINT('Ctrl Pts',(-1.51202133911129,1.30206118178868,24.6290295725916));
#16883=CARTESIAN_POINT('Ctrl Pts',(-1.54445941879055,1.26341456983849,24.6320695834745));
#16884=CARTESIAN_POINT('Ctrl Pts',(-1.59395474535689,1.1996879522464,24.6370236714478));
#16885=CARTESIAN_POINT('Ctrl Pts',(-1.6119662035686,1.17537556457359,24.6389007328936));
#16886=CARTESIAN_POINT('Ctrl Pts',(-1.63441740665788,1.14358316017397,24.6413433685512));
#16887=CARTESIAN_POINT('Ctrl Pts',(-1.63937145886673,1.13646993776835,24.6418891272794));
#16888=CARTESIAN_POINT('Ctrl Pts',(-1.64729497814889,1.12493341924129,24.6427731519681));
#16889=CARTESIAN_POINT('Ctrl Pts',(-1.65029340039267,1.1205300685312,24.6431103150676));
#16890=CARTESIAN_POINT('Ctrl Pts',(-1.6559848401882,1.11209947501826,24.6437553767652));
#16891=CARTESIAN_POINT('Ctrl Pts',(-1.65868089947099,1.10807432346332,24.6440631574425));
#16892=CARTESIAN_POINT('Ctrl Pts',(-1.66481855852499,1.09883835337637,24.6447689422366));
#16893=CARTESIAN_POINT('Ctrl Pts',(-1.66825039208598,1.09362113526534,24.6451673092199));
#16894=CARTESIAN_POINT('Ctrl Pts',(-1.67875280985181,1.07749044666894,24.6463980708924));
#16895=CARTESIAN_POINT('Ctrl Pts',(-1.68574110689991,1.06652405806988,24.6472335166841));
#16896=CARTESIAN_POINT('Ctrl Pts',(-1.75653363288302,0.952998665625529,
24.6558704774647));
#16897=CARTESIAN_POINT('Ctrl Pts',(-1.81099275340321,0.844933407534047,
24.6640182995758));
#16898=CARTESIAN_POINT('Ctrl Pts',(-1.89669653932677,0.627892676070149,
24.6801576601004));
#16899=CARTESIAN_POINT('Ctrl Pts',(-1.92910970265941,0.519848325567508,
24.6880896858351));
#16900=CARTESIAN_POINT('Ctrl Pts',(-1.96124544112281,0.366700833071344,
24.6988497710607));
#16901=CARTESIAN_POINT('Ctrl Pts',(-1.96883819819459,0.323465416687952,
24.7018336885393));
#16902=CARTESIAN_POINT('Ctrl Pts',(-1.97819467383585,0.25747168457394,24.7062746383364));
#16903=CARTESIAN_POINT('Ctrl Pts',(-1.98100445365406,0.234877203149722,
24.7077750160446));
#16904=CARTESIAN_POINT('Ctrl Pts',(-1.98399751677331,0.206906196102912,
24.7096036396167));
#16905=CARTESIAN_POINT('Ctrl Pts',(-1.98454659819748,0.201571629320054,
24.709951100188));
#16906=CARTESIAN_POINT('Ctrl Pts',(-1.98537756954806,0.193165681766397,
24.7104965111316));
#16907=CARTESIAN_POINT('Ctrl Pts',(-1.98567385577742,0.190095799732308,
24.7106952563148));
#16908=CARTESIAN_POINT('Ctrl Pts',(-1.98621595263948,0.184339440572999,
24.7110670830157));
#16909=CARTESIAN_POINT('Ctrl Pts',(-1.9864634306143,0.18165318278547,24.7112402539311));
#16910=CARTESIAN_POINT('Ctrl Pts',(-1.98701509888672,0.175529114314983,
24.7116342663681));
#16911=CARTESIAN_POINT('Ctrl Pts',(-1.98731581663326,0.172091018284429,
24.7118549104847));
#16912=CARTESIAN_POINT('Ctrl Pts',(-1.98820843694681,0.161571264060495,
24.7125283718489));
#16913=CARTESIAN_POINT('Ctrl Pts',(-1.98877142928303,0.154487112236704,
24.7129795942538));
#16914=CARTESIAN_POINT('Ctrl Pts',(-1.99290202203708,0.0987410107736622,
24.7165133331227));
#16915=CARTESIAN_POINT('Ctrl Pts',(-1.99472128911868,0.0499613971369182,
24.7195037966203));
#16916=CARTESIAN_POINT('Ctrl Pts',(-1.99480080932865,-0.0868098885426201,
24.7277257662376));
#16917=CARTESIAN_POINT('Ctrl Pts',(-1.98903262344727,-0.174692803194069,
24.7328230142401));
#16918=CARTESIAN_POINT('Ctrl Pts',(-1.95803198486501,-0.408752169165059,
24.74651622615));
#16919=CARTESIAN_POINT('Ctrl Pts',(-1.92229262429381,-0.552948044952065,
24.7551123909539));
#16920=CARTESIAN_POINT('Ctrl Pts',(-1.86641816742885,-0.704045295008075,
24.7650778956838));
#16921=CARTESIAN_POINT('Ctrl Pts',(-1.86179041892914,-0.71619339342671,
24.7658857943512));
#16922=CARTESIAN_POINT('Ctrl Pts',(-1.85247219293728,-0.739953483439173,
24.767479631554));
#16923=CARTESIAN_POINT('Ctrl Pts',(-1.84779044288463,-0.751568261066158,
24.7682652530824));
#16924=CARTESIAN_POINT('Ctrl Pts',(-1.84064690531058,-0.76882010561023,
24.7694421996398));
#16925=CARTESIAN_POINT('Ctrl Pts',(-1.83826784203443,-0.774491268114423,
24.7698307238299));
#16926=CARTESIAN_POINT('Ctrl Pts',(-1.8339723382099,-0.784599506098843,
24.770526180263));
#16927=CARTESIAN_POINT('Ctrl Pts',(-1.83206591720916,-0.789040807953773,
24.7708327695994));
#16928=CARTESIAN_POINT('Ctrl Pts',(-1.82800393169236,-0.798409742002944,
24.771481706832));
#16929=CARTESIAN_POINT('Ctrl Pts',(-1.8258445440323,-0.803335664900426,
24.7718241834518));
#16930=CARTESIAN_POINT('Ctrl Pts',(-1.82005982986606,-0.816387748305625,
24.7727350805117));
#16931=CARTESIAN_POINT('Ctrl Pts',(-1.81640003862968,-0.824498414361877,
24.7733046793466));
#16932=CARTESIAN_POINT('Ctrl Pts',(-1.79907367186601,-0.862221042952241,
24.7759707674385));
#16933=CARTESIAN_POINT('Ctrl Pts',(-1.78473713218674,-0.891518010709639,
24.7780902656372));
#16934=CARTESIAN_POINT('Ctrl Pts',(-1.74386291663732,-0.97010430071404,
24.7839139396217));
#16935=CARTESIAN_POINT('Ctrl Pts',(-1.71596003467865,-1.01864636614899,
24.7876638079324));
#16936=CARTESIAN_POINT('Ctrl Pts',(-1.63023492685055,-1.15424147042592,
24.7985770710958));
#16937=CARTESIAN_POINT('Ctrl Pts',(-1.56756881966963,-1.23800810630327,
24.8058748004737));
#16938=CARTESIAN_POINT('Ctrl Pts',(-1.44754524723948,-1.37463955385313,
24.8185549930584));
#16939=CARTESIAN_POINT('Ctrl Pts',(-1.39310497077041,-1.42978368481388,
24.823930585147));
#16940=CARTESIAN_POINT('Ctrl Pts',(-1.30989680635394,-1.50479061653673,
24.831484744924));
#16941=CARTESIAN_POINT('Ctrl Pts',(-1.28359995612032,-1.5272838483881,24.8337851872403));
#16942=CARTESIAN_POINT('Ctrl Pts',(-1.25220610460746,-1.55275283303931,
24.8364190931154));
#16943=CARTESIAN_POINT('Ctrl Pts',(-1.24766668556361,-1.55640268976449,
24.8367972744302));
#16944=CARTESIAN_POINT('Ctrl Pts',(-1.24037045001631,-1.56221669154071,
24.8374007760712));
#16945=CARTESIAN_POINT('Ctrl Pts',(-1.23762384665511,-1.56439351163755,
24.837626978875));
#16946=CARTESIAN_POINT('Ctrl Pts',(-1.23274260626034,-1.56824123702767,
24.8380272283957));
#16947=CARTESIAN_POINT('Ctrl Pts',(-1.23061028531054,-1.56991504128184,
24.8382014814548));
#16948=CARTESIAN_POINT('Ctrl Pts',(-1.2260967647778,-1.57344316522101,24.8385690701382));
#16949=CARTESIAN_POINT('Ctrl Pts',(-1.22371477355211,-1.57529642419013,
24.838762330539));
#16950=CARTESIAN_POINT('Ctrl Pts',(-1.21732365050612,-1.58024566137745,
24.8392789357539));
#16951=CARTESIAN_POINT('Ctrl Pts',(-1.21330688337693,-1.58333181250433,
24.8396015894927));
#16952=CARTESIAN_POINT('Ctrl Pts',(-1.1940248446609,-1.59803006813968,24.8411410069655));
#16953=CARTESIAN_POINT('Ctrl Pts',(-1.17860374706491,-1.60943738668073,
24.8423439703263));
#16954=CARTESIAN_POINT('Ctrl Pts',(-1.13514035863695,-1.64062838231273,
24.8456640249635));
#16955=CARTESIAN_POINT('Ctrl Pts',(-1.10674751427758,-1.65991425981153,
24.8477529422688));
#16956=CARTESIAN_POINT('Ctrl Pts',(-1.00136579363134,-1.72758808519944,
24.85527428219));
#16957=CARTESIAN_POINT('Ctrl Pts',(-0.921587320028886,-1.77143250008126,
24.8605335887246));
#16958=CARTESIAN_POINT('Ctrl Pts',(-0.696700288990083,-1.87570529516955,
24.8749099665122));
#16959=CARTESIAN_POINT('Ctrl Pts',(-0.547038822559078,-1.92468201091436,
24.8840483904333));
#16960=CARTESIAN_POINT('Ctrl Pts',(-0.38089898564765,-1.9580860104944,24.8946311564645));
#16961=CARTESIAN_POINT('Ctrl Pts',(-0.368580340605556,-1.9604421396274,
24.8954179634974));
#16962=CARTESIAN_POINT('Ctrl Pts',(-0.35018566129031,-1.9637809027981,24.8965963430807));
#16963=CARTESIAN_POINT('Ctrl Pts',(-0.344125808957736,-1.96485186662963,
24.8969851046454));
#16964=CARTESIAN_POINT('Ctrl Pts',(-0.333297445260089,-1.96671394448956,
24.897680825257));
#16965=CARTESIAN_POINT('Ctrl Pts',(-0.328530810786781,-1.96751580226344,
24.8979874403947));
#16966=CARTESIAN_POINT('Ctrl Pts',(-0.318456321448877,-1.96917293261258,
24.8986362646849));
#16967=CARTESIAN_POINT('Ctrl Pts',(-0.313147837028925,-1.97002408575012,
24.898978601917));
#16968=CARTESIAN_POINT('Ctrl Pts',(-0.299054022946336,-1.97222545842726,
24.8998887369477));
#16969=CARTESIAN_POINT('Ctrl Pts',(-0.290263076973265,-1.97353842359669,
24.90045770964));
#16970=CARTESIAN_POINT('Ctrl Pts',(-0.249278590371073,-1.97937987150333,
24.9031165190084));
#16971=CARTESIAN_POINT('Ctrl Pts',(-0.216987773772212,-1.98317941448709,
24.9052292120486));
#16972=CARTESIAN_POINT('Ctrl Pts',(-0.129135933739827,-1.99134541417093,
24.9110293912699));
#16973=CARTESIAN_POINT('Ctrl Pts',(-0.073464799946427,-1.99417517199349,
24.914762119613));
#16974=CARTESIAN_POINT('Ctrl Pts',(0.086511349446103,-1.99559893616663,
24.9256435069905));
#16975=CARTESIAN_POINT('Ctrl Pts',(0.190680115523286,-1.98835037163982,
24.932926675516));
#16976=CARTESIAN_POINT('Ctrl Pts',(0.369272373697638,-1.96175649805191,
24.9455168792244));
#16977=CARTESIAN_POINT('Ctrl Pts',(0.44404751974304,-1.94619475763947,24.9508169181002));
#16978=CARTESIAN_POINT('Ctrl Pts',(0.55263844868642,-1.91700895452849,24.9584093896121));
#16979=CARTESIAN_POINT('Ctrl Pts',(0.587267110705992,-1.90668569281275,
24.960813952761));
#16980=CARTESIAN_POINT('Ctrl Pts',(0.627206283165518,-1.89358777632888,
24.9635529691945));
#16981=CARTESIAN_POINT('Ctrl Pts',(0.632805678472392,-1.89172391318637,
24.963936178456));
#16982=CARTESIAN_POINT('Ctrl Pts',(0.641738426139534,-1.88870638151676,
24.9645461488819));
#16983=CARTESIAN_POINT('Ctrl Pts',(0.645077079576406,-1.88756869147619,
24.9647738222278));
#16984=CARTESIAN_POINT('Ctrl Pts',(0.650979276237851,-1.88553995179913,
24.9651757481395));
#16985=CARTESIAN_POINT('Ctrl Pts',(0.653544038195908,-1.88465251927691,
24.9653502130806));
#16986=CARTESIAN_POINT('Ctrl Pts',(0.658945727421706,-1.88277112963622,
24.9657172499799));
#16987=CARTESIAN_POINT('Ctrl Pts',(0.661782214298192,-1.88177599607677,
24.9659097505482));
#16988=CARTESIAN_POINT('Ctrl Pts',(0.669341590003951,-1.87910471055398,
24.9664221751043));
#16989=CARTESIAN_POINT('Ctrl Pts',(0.67406046870462,-1.87741715214741,24.9667414274281));
#16990=CARTESIAN_POINT('Ctrl Pts',(0.69625759808999,-1.86938456844525,24.9682404361089));
#16991=CARTESIAN_POINT('Ctrl Pts',(0.713653637166449,-1.86281288756075,
24.9694072538952));
#16992=CARTESIAN_POINT('Ctrl Pts',(0.890985755314345,-1.79297341069414,
24.9812443533709));
#16993=CARTESIAN_POINT('Ctrl Pts',(1.04221640274193,-1.70950660411171,24.9909072358625));
#16994=CARTESIAN_POINT('Ctrl Pts',(1.26981173988946,-1.54233023613869,25.0074257501017));
#16995=CARTESIAN_POINT('Ctrl Pts',(1.35316004384931,-1.46974729997954,25.014005993112));
#16996=CARTESIAN_POINT('Ctrl Pts',(1.43908206178811,-1.38138963969378,25.0216991421134));
#16997=CARTESIAN_POINT('Ctrl Pts',(1.44799969571827,-1.37203913424563,25.0225094916385));
#16998=CARTESIAN_POINT('Ctrl Pts',(1.46108043357888,-1.35805387406573,25.0237162945179));
#16999=CARTESIAN_POINT('Ctrl Pts',(1.46531380302344,-1.35348506289926,25.0241097317422));
#17000=CARTESIAN_POINT('Ctrl Pts',(1.47280035437641,-1.34532900420376,25.0248106866029));
#17001=CARTESIAN_POINT('Ctrl Pts',(1.47606201653617,-1.34174958023644,25.0251178405568));
#17002=CARTESIAN_POINT('Ctrl Pts',(1.48288995625797,-1.33420141256047,25.0257645885746));
#17003=CARTESIAN_POINT('Ctrl Pts',(1.48645340394456,-1.33023017130069,25.0261042984264));
#17004=CARTESIAN_POINT('Ctrl Pts',(1.4957890802489,-1.31974178595706,25.0270000721123));
#17005=CARTESIAN_POINT('Ctrl Pts',(1.50153460164272,-1.31320112331544,25.0275572456325));
#17006=CARTESIAN_POINT('Ctrl Pts',(1.52729902619214,-1.28348092787749,25.030082735839));
#17007=CARTESIAN_POINT('Ctrl Pts',(1.54682436238642,-1.25988087772748,25.0320712101852));
#17008=CARTESIAN_POINT('Ctrl Pts',(1.59757961749283,-1.19557453135403,25.03744841836));
#17009=CARTESIAN_POINT('Ctrl Pts',(1.62779379377285,-1.15409952051872,25.0408747181047));
#17010=CARTESIAN_POINT('Ctrl Pts',(1.7125433396656,-1.02780550294126,25.0511832837765));
#17011=CARTESIAN_POINT('Ctrl Pts',(1.76228246845434,-0.939971293937737,
25.0582024793581));
#17012=CARTESIAN_POINT('Ctrl Pts',(1.84140073235156,-0.771700978370523,
25.0711756313807));
#17013=CARTESIAN_POINT('Ctrl Pts',(1.87266489551997,-0.692392317305198,
25.0771102018213));
#17014=CARTESIAN_POINT('Ctrl Pts',(1.91019762187873,-0.575816023739283,
25.0853877873001));
#17015=CARTESIAN_POINT('Ctrl Pts',(1.92063229033387,-0.539991754106582,
25.0878726528258));
#17016=CARTESIAN_POINT('Ctrl Pts',(1.93156203286626,-0.49812767712736,25.0906925137743));
#17017=CARTESIAN_POINT('Ctrl Pts',(1.93304145916679,-0.492355348155817,
25.0910794888549));
#17018=CARTESIAN_POINT('Ctrl Pts',(1.93535949081565,-0.483139486498522,
25.0916942994721));
#17019=CARTESIAN_POINT('Ctrl Pts',(1.93621480950124,-0.479700254376378,
25.0919230697235));
#17020=CARTESIAN_POINT('Ctrl Pts',(1.93770951607528,-0.473620916431468,
25.0923262515093));
#17021=CARTESIAN_POINT('Ctrl Pts',(1.93835268222469,-0.470981762748864,
25.0925008799186));
#17022=CARTESIAN_POINT('Ctrl Pts',(1.93969419203956,-0.465427746969418,
25.0928675307246));
#17023=CARTESIAN_POINT('Ctrl Pts',(1.94039135598954,-0.462512629203602,
25.0930594845218));
#17024=CARTESIAN_POINT('Ctrl Pts',(1.94222767790006,-0.454757009309252,
25.0935689016688));
#17025=CARTESIAN_POINT('Ctrl Pts',(1.94335531988057,-0.44991376094942,25.0938857071792));
#17026=CARTESIAN_POINT('Ctrl Pts',(1.94852203638172,-0.427340721807538,
25.0953563403367));
#17027=CARTESIAN_POINT('Ctrl Pts',(1.95233682679962,-0.409559751454695,
25.0964978168665));
#17028=CARTESIAN_POINT('Ctrl Pts',(1.98661881322881,-0.238389054834851,
25.1073458660057));
#17029=CARTESIAN_POINT('Ctrl Pts',(1.99919564234486,-0.0819470161938231,
25.1162121936474));
#17030=CARTESIAN_POINT('Ctrl Pts',(1.98865459414495,0.200564536396305,25.1326716628265));
#17031=CARTESIAN_POINT('Ctrl Pts',(1.97197607481659,0.326001148856512,25.1401419867168));
#17032=CARTESIAN_POINT('Ctrl Pts',(1.94062866068086,0.461689626740882,25.1488339543987));
#17033=CARTESIAN_POINT('Ctrl Pts',(1.93757545531006,0.474339806781253,25.1496500308768));
#17034=CARTESIAN_POINT('Ctrl Pts',(1.93287381458685,0.493016632630669,25.1508637380492));
#17035=CARTESIAN_POINT('Ctrl Pts',(1.93132044786469,0.499067038967568,25.1512583016611));
#17036=CARTESIAN_POINT('Ctrl Pts',(1.92851187615533,0.509796997967594,25.1519605257441));
#17037=CARTESIAN_POINT('Ctrl Pts',(1.92726798780158,0.514479482706144,25.1522678177598));
#17038=CARTESIAN_POINT('Ctrl Pts',(1.92462081592243,0.524300150133571,25.152914105753));
#17039=CARTESIAN_POINT('Ctrl Pts',(1.92321398841665,0.529437329967593,25.1532532146637));
#17040=CARTESIAN_POINT('Ctrl Pts',(1.91946474980384,0.54291592606885,25.1541457033592));
#17041=CARTESIAN_POINT('Ctrl Pts',(1.91708855835524,0.551247751935289,25.1547001781214));
#17042=CARTESIAN_POINT('Ctrl Pts',(1.90618314158928,0.58856279687398,25.1571961636292));
#17043=CARTESIAN_POINT('Ctrl Pts',(1.89705077685446,0.617364170174376,25.1591572592904));
#17044=CARTESIAN_POINT('Ctrl Pts',(1.87096583212223,0.693576895376227,25.1644427161337));
#17045=CARTESIAN_POINT('Ctrl Pts',(1.85286732378634,0.740570063176308,25.1678030847046));
#17046=CARTESIAN_POINT('Ctrl Pts',(1.79355256349569,0.878751531526024,25.1779870175077));
#17047=CARTESIAN_POINT('Ctrl Pts',(1.74723694013402,0.967571604557962,25.1849478177556));
#17048=CARTESIAN_POINT('Ctrl Pts',(1.62942935987013,1.15722823864101,25.2005255827653));
#17049=CARTESIAN_POINT('Ctrl Pts',(1.55482702089374,1.25568213924491,25.2091225372248));
#17050=CARTESIAN_POINT('Ctrl Pts',(1.46650390259364,1.35220226100939,25.2176642117622));
#17051=CARTESIAN_POINT('Ctrl Pts',(1.46137142972671,1.35774747276934,25.2181553176304));
#17052=CARTESIAN_POINT('Ctrl Pts',(1.45381492270092,1.36581916401153,25.2188705527326));
#17053=CARTESIAN_POINT('Ctrl Pts',(1.45141562518083,1.36836855477227,25.2190965102177));
#17054=CARTESIAN_POINT('Ctrl Pts',(1.44714695153783,1.37288040581725,25.2194964809223));
#17055=CARTESIAN_POINT('Ctrl Pts',(1.44528027469255,1.37484538620069,25.2196706994773));
#17056=CARTESIAN_POINT('Ctrl Pts',(1.44132508237051,1.37899191082734,25.2200383841626));
#17057=CARTESIAN_POINT('Ctrl Pts',(1.43923562158321,1.38117251241863,25.220231774419));
#17058=CARTESIAN_POINT('Ctrl Pts',(1.4336220092909,1.38700441538083,25.2207490943302));
#17059=CARTESIAN_POINT('Ctrl Pts',(1.43008883407581,1.39064705868255,25.2210723295686));
#17060=CARTESIAN_POINT('Ctrl Pts',(1.4130643138257,1.4080655503945,25.22261877048));
#17061=CARTESIAN_POINT('Ctrl Pts',(1.39938704075417,1.4216593566299,25.2238280229595));
#17062=CARTESIAN_POINT('Ctrl Pts',(1.36064190698567,1.45906697956981,25.2271699329368));
#17063=CARTESIAN_POINT('Ctrl Pts',(1.33514796046321,1.48243147124427,25.229273964634));
#17064=CARTESIAN_POINT('Ctrl Pts',(1.23989624063009,1.56527522918585,25.2368529452548));
#17065=CARTESIAN_POINT('Ctrl Pts',(1.16666583658701,1.62059320225945,25.242152745272));
#17066=CARTESIAN_POINT('Ctrl Pts',(0.959419053620506,1.75579277432634,25.2565040421057));
#17067=CARTESIAN_POINT('Ctrl Pts',(0.819453601606901,1.82531633140499,25.2655795428492));
#17068=CARTESIAN_POINT('Ctrl Pts',(0.660994947086356,1.88209230981788,25.2760905708652));
#17069=CARTESIAN_POINT('Ctrl Pts',(0.649113895048487,1.8862229249087,25.2768796545449));
#17070=CARTESIAN_POINT('Ctrl Pts',(0.631356503317253,1.89220889096321,25.2780607856478));
#17071=CARTESIAN_POINT('Ctrl Pts',(0.625509189245483,1.89414988163734,25.2784500025495));
#17072=CARTESIAN_POINT('Ctrl Pts',(0.615057740853982,1.89756552191504,25.2791462303498));
#17073=CARTESIAN_POINT('Ctrl Pts',(0.61045704111994,1.89905058774584,25.2794528954159));
#17074=CARTESIAN_POINT('Ctrl Pts',(0.601167635079508,1.90201188222467,25.280072489065));
#17075=CARTESIAN_POINT('Ctrl Pts',(0.596478781267086,1.90348753302351,25.2803854341549));
#17076=CARTESIAN_POINT('Ctrl Pts',(0.583983428860944,1.90736930040159,25.281219969518));
#17077=CARTESIAN_POINT('Ctrl Pts',(0.576167587145081,1.90974480010562,25.2817425584719));
#17078=CARTESIAN_POINT('Ctrl Pts',(0.559092958117396,1.91482000149295,25.2828855785421));
#17079=CARTESIAN_POINT('Ctrl Pts',(0.549828778280709,1.91750068658948,25.283506616645));
#17080=CARTESIAN_POINT('Ctrl Pts',(0.522834370146129,1.92510008418684,25.2853189058666));
#17081=CARTESIAN_POINT('Ctrl Pts',(0.505055456178126,1.92984068288694,25.2865158620665));
#17082=CARTESIAN_POINT('Ctrl Pts',(0.443639074286026,1.94531004451985,25.2906630637096));
#17083=CARTESIAN_POINT('Ctrl Pts',(0.399708790363694,1.95480923933301,25.2936512515341));
#17084=CARTESIAN_POINT('Ctrl Pts',(0.173303818173071,1.99581485446975,25.3091609518814));
#17085=CARTESIAN_POINT('Ctrl Pts',(-0.0125627512863938,2.00328165767449,
25.3223660965633));
#17086=CARTESIAN_POINT('Ctrl Pts',(-0.205872429791445,1.9841188672704,25.3355976124627));
#17087=CARTESIAN_POINT('Ctrl Pts',(-0.214963567943442,1.98315450890887,
25.3362184251348));
#17088=CARTESIAN_POINT('Ctrl Pts',(-0.262654926561549,1.9777637622472,25.3394665218398));
#17089=CARTESIAN_POINT('Ctrl Pts',(-0.30112949358743,1.97227245371955,25.3420572794784));
#17090=CARTESIAN_POINT('Ctrl Pts',(-0.345940196942792,1.96453472753261,
25.3450214157219));
#17091=CARTESIAN_POINT('Ctrl Pts',(-0.352452816560508,1.96337676736608,
25.3454508835194));
#17092=CARTESIAN_POINT('Ctrl Pts',(-0.362300709367983,1.96157520748857,
25.3460981561912));
#17093=CARTESIAN_POINT('Ctrl Pts',(-0.365640216612522,1.96095546381316,
25.3463172795906));
#17094=CARTESIAN_POINT('Ctrl Pts',(-0.371624495345527,1.95982908647198,
25.3467092529198));
#17095=CARTESIAN_POINT('Ctrl Pts',(-0.374269827063037,1.95932562647602,
25.3468822809883));
#17096=CARTESIAN_POINT('Ctrl Pts',(-0.379979511768562,1.95822697287139,
25.3472552182032));
#17097=CARTESIAN_POINT('Ctrl Pts',(-0.383043478596804,1.95762994472311,
25.3474550207829));
#17098=CARTESIAN_POINT('Ctrl Pts',(-0.391533831439984,1.9559548636944,25.348007809767));
#17099=CARTESIAN_POINT('Ctrl Pts',(-0.396957205147604,1.95486141427164,
25.3483599274359));
#17100=CARTESIAN_POINT('Ctrl Pts',(-0.426986673208195,1.94867681194214,
25.3503045000139));
#17101=CARTESIAN_POINT('Ctrl Pts',(-0.451500743017651,1.94314337053519,
25.3518728537722));
#17102=CARTESIAN_POINT('Ctrl Pts',(-0.633543265873735,1.89842042511688,
25.3634212358615));
#17103=CARTESIAN_POINT('Ctrl Pts',(-0.78588523078916,1.8405911992282,25.37257287806));
#17104=CARTESIAN_POINT('Ctrl Pts',(-1.02905128753731,1.71252104917088,25.3886372441771));
#17105=CARTESIAN_POINT('Ctrl Pts',(-1.12393032684882,1.65180208095046,25.3953364334316));
#17106=CARTESIAN_POINT('Ctrl Pts',(-1.22345443788887,1.57554888302259,25.4031624465996));
#17107=CARTESIAN_POINT('Ctrl Pts',(-1.23365026270109,1.56757840669953,25.4039740613711));
#17108=CARTESIAN_POINT('Ctrl Pts',(-1.24864032139483,1.55562326922265,25.4051823899399));
#17109=CARTESIAN_POINT('Ctrl Pts',(-1.25349473546096,1.55171432767096,25.4055760763858));
#17110=CARTESIAN_POINT('Ctrl Pts',(-1.26208861649509,1.54472759488179,25.4062773118063));
#17111=CARTESIAN_POINT('Ctrl Pts',(-1.26583536050546,1.54165880067281,25.4065844960429));
#17112=CARTESIAN_POINT('Ctrl Pts',(-1.26961518176168,1.53853984545137,25.4068958847872));
#17113=CARTESIAN_POINT('Ctrl Pts',(-1.26965949729428,1.53850327485241,25.4068995357919));
#17114=CARTESIAN_POINT('Ctrl Pts',(-1.26974649857748,1.53843147228389,25.406906703938));
#17115=CARTESIAN_POINT('Ctrl Pts',(-1.26978918487027,1.5383962400987,25.4069102211091));
#17116=CARTESIAN_POINT('Ctrl Pts',(-1.26987300193491,1.53832705375073,25.4069171276624));
#17117=CARTESIAN_POINT('Ctrl Pts',(-1.26991413294785,1.53829309960223,25.4069205170507));
#17118=CARTESIAN_POINT('Ctrl Pts',(-1.26999490917778,1.53822641240021,25.4069271737433));
#17119=CARTESIAN_POINT('Ctrl Pts',(-1.27003455464942,1.53819367933285,25.4069304410558));
#17120=CARTESIAN_POINT('Ctrl Pts',(-1.27011242570285,1.5381293804595,25.4069368589908));
#17121=CARTESIAN_POINT('Ctrl Pts',(-1.27015065153884,1.53809781462458,25.4069400096225));
#17122=CARTESIAN_POINT('Ctrl Pts',(-1.27022574561321,1.53803579931277,25.4069461992954));
#17123=CARTESIAN_POINT('Ctrl Pts',(-1.27026261412418,1.53800534977765,25.4069492383482));
#17124=CARTESIAN_POINT('Ctrl Pts',(-1.27033505244023,1.53794551892126,25.4069552096858));
#17125=CARTESIAN_POINT('Ctrl Pts',(-1.27037062255348,1.53791613749949,25.406958141986));
#17126=CARTESIAN_POINT('Ctrl Pts',(-1.27044051988546,1.53785839722504,25.4069639043897));
#17127=CARTESIAN_POINT('Ctrl Pts',(-1.27047484740529,1.53783003826589,25.4069667345089));
#17128=CARTESIAN_POINT('Ctrl Pts',(-1.27054231236415,1.53777429970718,25.4069722968775));
#17129=CARTESIAN_POINT('Ctrl Pts',(-1.2705754501318,1.5377469199676,25.4069750291455));
#17130=CARTESIAN_POINT('Ctrl Pts',(-1.27064058564112,1.53769309888039,25.4069803999137));
#17131=CARTESIAN_POINT('Ctrl Pts',(-1.27067258373281,1.53766665736514,25.4069830384348));
#17132=CARTESIAN_POINT('Ctrl Pts',(-1.27073548737102,1.53761467385142,25.4069882256012));
#17133=CARTESIAN_POINT('Ctrl Pts',(-1.27076639328057,1.53758913166551,25.4069907742691));
#17134=CARTESIAN_POINT('Ctrl Pts',(-1.27082715756168,1.53753890994798,25.4069957854189));
#17135=CARTESIAN_POINT('Ctrl Pts',(-1.27085701633089,1.53751423019196,25.4069982479268));
#17136=CARTESIAN_POINT('Ctrl Pts',(-1.27091572911641,1.53746569827937,25.4070030902652));
#17137=CARTESIAN_POINT('Ctrl Pts',(-1.27094458352759,1.53744184589302,25.4070054701221));
#17138=CARTESIAN_POINT('Ctrl Pts',(-1.27100132818265,1.53739493545644,25.4070101504871));
#17139=CARTESIAN_POINT('Ctrl Pts',(-1.2710292188541,1.53737187714237,25.4070124510248));
#17140=CARTESIAN_POINT('Ctrl Pts',(-1.27108407463135,1.53732652320266,25.4070169759185));
#17141=CARTESIAN_POINT('Ctrl Pts',(-1.27111104017678,1.53730422729675,25.4070192003053));
#17142=CARTESIAN_POINT('Ctrl Pts',(-1.27116408238187,1.53726036809214,25.407023575907));
#17143=CARTESIAN_POINT('Ctrl Pts',(-1.27119015950882,1.53723880448432,25.4070257271554));
#17144=CARTESIAN_POINT('Ctrl Pts',(-1.27124145980536,1.53719638122225,25.4070299593467));
#17145=CARTESIAN_POINT('Ctrl Pts',(-1.27126668345654,1.53717552124154,25.4070320403248));
#17146=CARTESIAN_POINT('Ctrl Pts',(-1.27131630996516,1.53713447802036,25.4070361346978));
#17147=CARTESIAN_POINT('Ctrl Pts',(-1.27134071336545,1.53711429439768,25.4070381481332));
#17148=CARTESIAN_POINT('Ctrl Pts',(-1.27138873104009,1.53707457789883,25.4070421100208));
#17149=CARTESIAN_POINT('Ctrl Pts',(-1.27141234585355,1.53705504463884,25.4070440585135));
#17150=CARTESIAN_POINT('Ctrl Pts',(-1.27145881654325,1.53701660407873,25.4070478929946));
#17151=CARTESIAN_POINT('Ctrl Pts',(-1.27148167295819,1.5369976963908,25.4070497790238));
#17152=CARTESIAN_POINT('Ctrl Pts',(-1.27574962478244,1.53346692543189,25.4074019654472));
#17153=CARTESIAN_POINT('Ctrl Pts',(-1.27998011785712,1.52993751944739,25.4077529796671));
#17154=CARTESIAN_POINT('Ctrl Pts',(-1.29153622893392,1.52021503434459,25.4087171319949));
#17155=CARTESIAN_POINT('Ctrl Pts',(-1.29883180586143,1.51398663007387,25.4093317165086));
#17156=CARTESIAN_POINT('Ctrl Pts',(-1.31495396252914,1.50002047177767,25.4107031879422));
#17157=CARTESIAN_POINT('Ctrl Pts',(-1.32375768372676,1.49225699003033,25.4114611310597));
#17158=CARTESIAN_POINT('Ctrl Pts',(-1.35045093437283,1.46829568855202,25.4137873300332));
#17159=CARTESIAN_POINT('Ctrl Pts',(-1.36811493896041,1.45185102016609,25.4153658545363));
#17160=CARTESIAN_POINT('Ctrl Pts',(-1.43309189406048,1.38912049028472,25.4213231071439));
#17161=CARTESIAN_POINT('Ctrl Pts',(-1.47838608368565,1.34081361978432,25.4257857602523));
#17162=CARTESIAN_POINT('Ctrl Pts',(-1.6464999015215,1.14262431408354,25.4435933239477));
#17163=CARTESIAN_POINT('Ctrl Pts',(-1.74961403818921,0.977445694349946,
25.4575012252794));
#17164=CARTESIAN_POINT('Ctrl Pts',(-1.83205831167327,0.789132852286655,
25.4710191590031));
#17165=CARTESIAN_POINT('Ctrl Pts',(-1.83671947784287,0.77822226403292,25.4717942380369));
#17166=CARTESIAN_POINT('Ctrl Pts',(-1.84297012791455,0.763222055011605,
25.4728481053546));
#17167=CARTESIAN_POINT('Ctrl Pts',(-1.8446437626905,0.759168088964304,25.4731317577943));
#17168=CARTESIAN_POINT('Ctrl Pts',(-1.84728113973141,0.752719480200086,
25.4735810729072));
#17169=CARTESIAN_POINT('Ctrl Pts',(-1.84825361549842,0.750328460118517,
25.4737472591281));
#17170=CARTESIAN_POINT('Ctrl Pts',(-1.85024719710819,0.745399460660219,
25.474088989483));
#17171=CARTESIAN_POINT('Ctrl Pts',(-1.85126772157716,0.742861272030986,
25.4742644952618));
#17172=CARTESIAN_POINT('Ctrl Pts',(-1.85366729200975,0.736857547005966,
25.4746785387774));
#17173=CARTESIAN_POINT('Ctrl Pts',(-1.85504185417118,0.733390205736809,
25.4749168057301));
#17174=CARTESIAN_POINT('Ctrl Pts',(-1.85955157316575,0.721920614458185,
25.4757022055144));
#17175=CARTESIAN_POINT('Ctrl Pts',(-1.86264479308468,0.713901819598324,
25.4762468735828));
#17176=CARTESIAN_POINT('Ctrl Pts',(-1.90319204420191,0.606730267578278,
25.4834706295395));
#17177=CARTESIAN_POINT('Ctrl Pts',(-1.93274312340243,0.504749843138312,
25.4897143119683));
#17178=CARTESIAN_POINT('Ctrl Pts',(-1.98104299422856,0.269322839103342,
25.5037084226064));
#17179=CARTESIAN_POINT('Ctrl Pts',(-1.99467637956076,0.135379192454375,
25.5113976063033));
#17180=CARTESIAN_POINT('Ctrl Pts',(-1.99474970266067,0.00108914423437002,
25.5194706385773));
#17181=CARTESIAN_POINT('',(-1.99774652581851,-0.000397439823534614,27.121064794965));
#17182=CARTESIAN_POINT('Ctrl Pts',(-1.99474970399463,0.00108669836046226,
25.5194707856144));
#17183=CARTESIAN_POINT('Ctrl Pts',(-1.99477864875537,-0.0520444694238004,
25.5226648409668));
#17184=CARTESIAN_POINT('Ctrl Pts',(-1.99268484369696,-0.105152553496392,
25.525910525209));
#17185=CARTESIAN_POINT('Ctrl Pts',(-1.98770903672266,-0.167730301252841,
25.5298244945845));
#17186=CARTESIAN_POINT('Ctrl Pts',(-1.98687443595081,-0.177343280728575,
25.5304282250247));
#17187=CARTESIAN_POINT('Ctrl Pts',(-1.98539402199652,-0.193069746082949,
25.5314201301886));
#17188=CARTESIAN_POINT('Ctrl Pts',(-1.98478962838246,-0.199187045601989,
25.5318070107077));
#17189=CARTESIAN_POINT('Ctrl Pts',(-1.98366966429628,-0.210011056358707,
25.5324934584308));
#17190=CARTESIAN_POINT('Ctrl Pts',(-1.98316559096884,-0.214718930257409,
25.5327926632004));
#17191=CARTESIAN_POINT('Ctrl Pts',(-1.98213581040468,-0.224023657046903,
25.5333852948594));
#17192=CARTESIAN_POINT('Ctrl Pts',(-1.98161086148757,-0.228620565236366,
25.5336786961248));
#17193=CARTESIAN_POINT('Ctrl Pts',(-1.98053342780961,-0.237772919096294,
25.5342640997872));
#17194=CARTESIAN_POINT('Ctrl Pts',(-1.97998120732606,-0.242328367680629,
25.5345560921402));
#17195=CARTESIAN_POINT('Ctrl Pts',(-1.9784694140785,-0.254449403544559,
25.5353346810353));
#17196=CARTESIAN_POINT('Ctrl Pts',(-1.97748217253519,-0.262011404404,25.5358221481648));
#17197=CARTESIAN_POINT('Ctrl Pts',(-1.97378249076125,-0.289137236450202,
25.5375770682697));
#17198=CARTESIAN_POINT('Ctrl Pts',(-1.97082295538693,-0.308665667319003,
25.5388522942848));
#17199=CARTESIAN_POINT('Ctrl Pts',(-1.96679912246105,-0.332792672738863,
25.5404430042626));
#17200=CARTESIAN_POINT('Ctrl Pts',(-1.96600777458543,-0.337436187717719,
25.5407498529842));
#17201=CARTESIAN_POINT('Ctrl Pts',(-1.96432787954298,-0.347087030740639,
25.5413890535205));
#17202=CARTESIAN_POINT('Ctrl Pts',(-1.96343661677771,-0.352093845963292,
25.5417214878768));
#17203=CARTESIAN_POINT('Ctrl Pts',(-1.96024240326387,-0.369648529909305,
25.5428899482147));
#17204=CARTESIAN_POINT('Ctrl Pts',(-1.95783827062313,-0.3821774574721,25.5437290834988));
#17205=CARTESIAN_POINT('Ctrl Pts',(-1.94949663589628,-0.423503150266057,
25.5465142362819));
#17206=CARTESIAN_POINT('Ctrl Pts',(-1.94304284970025,-0.452190660058426,
25.5484756149738));
#17207=CARTESIAN_POINT('Ctrl Pts',(-1.89123154692902,-0.660843664870152,
25.5629451046473));
#17208=CARTESIAN_POINT('Ctrl Pts',(-1.82159886484378,-0.833805591687323,
25.5761740976607));
#17209=CARTESIAN_POINT('Ctrl Pts',(-1.71211966430217,-1.02412448254609,
25.5911507781912));
#17210=CARTESIAN_POINT('Ctrl Pts',(-1.69440540703044,-1.05317391897498,
25.5934458506026));
#17211=CARTESIAN_POINT('Ctrl Pts',(-1.66561893046525,-1.09777250078535,
25.5969678330164));
#17212=CARTESIAN_POINT('Ctrl Pts',(-1.65505260113188,-1.11363900725513,
25.5982204844435));
#17213=CARTESIAN_POINT('Ctrl Pts',(-1.64139828641327,-1.13351875876011,
25.5997871213441));
#17214=CARTESIAN_POINT('Ctrl Pts',(-1.63852071950873,-1.13767436650348,
25.600114446007));
#17215=CARTESIAN_POINT('Ctrl Pts',(-1.63390119445739,-1.14429172110258,
25.6006353594349));
#17216=CARTESIAN_POINT('Ctrl Pts',(-1.6321694199426,-1.14676049859343,25.6008296292908));
#17217=CARTESIAN_POINT('Ctrl Pts',(-1.62886992297318,-1.15144156965472,
25.6011978371068));
#17218=CARTESIAN_POINT('Ctrl Pts',(-1.62730330778364,-1.15365456652143,
25.6013718435343));
#17219=CARTESIAN_POINT('Ctrl Pts',(-1.62369884132374,-1.1587242762833,25.601770332676));
#17220=CARTESIAN_POINT('Ctrl Pts',(-1.62165796287589,-1.16157880820284,
25.6019946043177));
#17221=CARTESIAN_POINT('Ctrl Pts',(-1.61620062536082,-1.16916945028297,
25.6025907533652));
#17222=CARTESIAN_POINT('Ctrl Pts',(-1.6127708513584,-1.17389601240402,25.602961731871));
#17223=CARTESIAN_POINT('Ctrl Pts',(-1.58870393238541,-1.20675799676233,
25.6055398962061));
#17224=CARTESIAN_POINT('Ctrl Pts',(-1.56735093539493,-1.23436479702641,
25.6077000987887));
#17225=CARTESIAN_POINT('Ctrl Pts',(-1.54073273981344,-1.26697354625184,
25.6102639542189));
#17226=CARTESIAN_POINT('Ctrl Pts',(-1.53615220418561,-1.27252337916334,
25.6107007487528));
#17227=CARTESIAN_POINT('Ctrl Pts',(-1.42433724646804,-1.40651617035846,
25.621260595513));
#17228=CARTESIAN_POINT('Ctrl Pts',(-1.30138765723827,-1.52099482943121,
25.6306497529312));
#17229=CARTESIAN_POINT('Ctrl Pts',(-1.11622624933578,-1.65431692984031,
25.6441128832599));
#17230=CARTESIAN_POINT('Ctrl Pts',(-1.06528135306669,-1.68757229534346,
25.6477512160482));
#17231=CARTESIAN_POINT('Ctrl Pts',(-0.993286704744341,-1.73000792544056,
25.6528638217586));
#17232=CARTESIAN_POINT('Ctrl Pts',(-0.973477406028795,-1.74123162623372,
25.6542675030687));
#17233=CARTESIAN_POINT('Ctrl Pts',(-0.943597971386984,-1.75749168672217,
25.6563826589878));
#17234=CARTESIAN_POINT('Ctrl Pts',(-0.933669843593652,-1.76278608331482,
25.6570851238751));
#17235=CARTESIAN_POINT('Ctrl Pts',(-0.915465337038046,-1.77229711055161,
25.6583728577642));
#17236=CARTESIAN_POINT('Ctrl Pts',(-0.907203235712548,-1.77654049090059,
25.6589571731339));
#17237=CARTESIAN_POINT('Ctrl Pts',(-0.894064416504118,-1.78317297751809,
25.6598863182768));
#17238=CARTESIAN_POINT('Ctrl Pts',(-0.889206989527557,-1.78560017289269,
25.6602298098434));
#17239=CARTESIAN_POINT('Ctrl Pts',(-0.884316295315165,-1.78801908631444,
25.6605756548241));
#17240=CARTESIAN_POINT('Ctrl Pts',(-0.884292839033272,-1.7880306871022,
25.6605773135329));
#17241=CARTESIAN_POINT('Ctrl Pts',(-0.884245628714148,-1.78805403478252,
25.6605806520062));
#17242=CARTESIAN_POINT('Ctrl Pts',(-0.884221874858119,-1.78806578157084,
25.660582331758));
#17243=CARTESIAN_POINT('Ctrl Pts',(-0.884174065173737,-1.78808942329354,
25.6605857126155));
#17244=CARTESIAN_POINT('Ctrl Pts',(-0.884150009408023,-1.78810131818191,
25.6605874137168));
#17245=CARTESIAN_POINT('Ctrl Pts',(-0.884101591323205,-1.78812525832456,
25.6605908375974));
#17246=CARTESIAN_POINT('Ctrl Pts',(-0.884077229137599,-1.78813730349739,
25.6605925603672));
#17247=CARTESIAN_POINT('Ctrl Pts',(-0.884028193735618,-1.78816154637605,
25.6605960279014));
#17248=CARTESIAN_POINT('Ctrl Pts',(-0.884003520605003,-1.78817374402361,
25.6605977726597));
#17249=CARTESIAN_POINT('Ctrl Pts',(-0.88395385868617,-1.78819829409122,
25.6606012844981));
#17250=CARTESIAN_POINT('Ctrl Pts',(-0.883928869990882,-1.78821064644901,
25.6606030515717));
#17251=CARTESIAN_POINT('Ctrl Pts',(-0.883878572263243,-1.78823550820099,
25.6606066083714));
#17252=CARTESIAN_POINT('Ctrl Pts',(-0.883853263324179,-1.78824801753229,
25.660608398091));
#17253=CARTESIAN_POINT('Ctrl Pts',(-0.883802320262145,-1.78827319557633,
25.6606120005256));
#17254=CARTESIAN_POINT('Ctrl Pts',(-0.883776686272227,-1.78828586420606,
25.6606138132312));
#17255=CARTESIAN_POINT('Ctrl Pts',(-0.883725088377709,-1.78831136313296,
25.6606174619724));
#17256=CARTESIAN_POINT('Ctrl Pts',(-0.883699124529804,-1.78832419338439,
25.660619298004));
#17257=CARTESIAN_POINT('Ctrl Pts',(-0.883646861939137,-1.78835001796223,
25.6606229937493));
#17258=CARTESIAN_POINT('Ctrl Pts',(-0.883620563290989,-1.78836301222368,
25.6606248534563));
#17259=CARTESIAN_POINT('Ctrl Pts',(-0.883567626114362,-1.78838916722994,
25.6606285969051));
#17260=CARTESIAN_POINT('Ctrl Pts',(-0.883540987661871,-1.78840232791848,
25.6606304806415));
#17261=CARTESIAN_POINT('Ctrl Pts',(-0.883487365828111,-1.78842881821666,
25.6606342725059));
#17262=CARTESIAN_POINT('Ctrl Pts',(-0.88346038249933,-1.7884421477811,25.6606361806303));
#17263=CARTESIAN_POINT('Ctrl Pts',(-0.883406064966736,-1.78846897871039,
25.6606400216913));
#17264=CARTESIAN_POINT('Ctrl Pts',(-0.883378730823474,-1.7884824800254,
25.6606419546236));
#17265=CARTESIAN_POINT('Ctrl Pts',(-0.883325223270455,-1.78850890780177,
25.6606457384071));
#17266=CARTESIAN_POINT('Ctrl Pts',(-0.88329904764392,-1.78852183542261,
25.6606475894151));
#17267=CARTESIAN_POINT('Ctrl Pts',(-0.883245212885875,-1.78854842186774,
25.6606513963371));
#17268=CARTESIAN_POINT('Ctrl Pts',(-0.883217554049297,-1.78856208046313,
25.6606533522303));
#17269=CARTESIAN_POINT('Ctrl Pts',(-0.883160667422736,-1.78859017079928,
25.6606573749653));
#17270=CARTESIAN_POINT('Ctrl Pts',(-0.883131439891513,-1.78860460231923,
25.6606594417887));
#17271=CARTESIAN_POINT('Ctrl Pts',(-0.883071325402392,-1.78863428289252,
25.6606636927822));
#17272=CARTESIAN_POINT('Ctrl Pts',(-0.883040438667561,-1.78864953173175,
25.6606658769363));
#17273=CARTESIAN_POINT('Ctrl Pts',(-0.882976910296061,-1.78868089376194,
25.6606703693426));
#17274=CARTESIAN_POINT('Ctrl Pts',(-0.882944268887404,-1.7886970067242,
25.6606726775786));
#17275=CARTESIAN_POINT('Ctrl Pts',(-0.878574451415106,-1.79085395554171,
25.6609816890757));
#17276=CARTESIAN_POINT('Ctrl Pts',(-0.874229536845616,-1.79297899401761,
25.661288941372));
#17277=CARTESIAN_POINT('Ctrl Pts',(-0.864314891262726,-1.79778350549814,
25.6619900851228));
#17278=CARTESIAN_POINT('Ctrl Pts',(-0.858740370195685,-1.80045292609238,
25.662384322539));
#17279=CARTESIAN_POINT('Ctrl Pts',(-0.84169392356628,-1.80851862755688,
25.6635899812172));
#17280=CARTESIAN_POINT('Ctrl Pts',(-0.83018305748607,-1.81383140504161,
25.6644042760221));
#17281=CARTESIAN_POINT('Ctrl Pts',(-0.732337026640794,-1.8578651983485,
25.6713284603613));
#17282=CARTESIAN_POINT('Ctrl Pts',(-0.64341138965896,-1.89050194453488,
25.677646094022));
#17283=CARTESIAN_POINT('Ctrl Pts',(-0.434635845709935,-1.95068449279221,
25.6925172173992));
#17284=CARTESIAN_POINT('Ctrl Pts',(-0.313874224238932,-1.97371678918793,
25.7011550429326));
#17285=CARTESIAN_POINT('Ctrl Pts',(-0.136089932802466,-1.99088844185003,
25.7135235544777));
#17286=CARTESIAN_POINT('Ctrl Pts',(-0.0801992898656494,-1.99392233875122,
25.7173588056173));
#17287=CARTESIAN_POINT('Ctrl Pts',(0.00252348216109496,-1.9949281144154,
25.722893859219));
#17288=CARTESIAN_POINT('Ctrl Pts',(0.029303629749624,-1.99471452137963,
25.724663729083));
#17289=CARTESIAN_POINT('Ctrl Pts',(0.0617114573816073,-1.99380316899235,
25.726772499811));
#17290=CARTESIAN_POINT('Ctrl Pts',(0.0673493722532456,-1.99362068723922,
25.7271381459563));
#17291=CARTESIAN_POINT('Ctrl Pts',(0.0761297242379217,-1.99329920497823,
25.727705627592));
#17292=CARTESIAN_POINT('Ctrl Pts',(0.0792726789278182,-1.99317668514128,
25.7279083667849));
#17293=CARTESIAN_POINT('Ctrl Pts',(0.08510363008286,-1.99293556689998,25.7282837526516));
#17294=CARTESIAN_POINT('Ctrl Pts',(0.0877916507410601,-1.99281896515401,
25.7284565067773));
#17295=CARTESIAN_POINT('Ctrl Pts',(0.0938407044030223,-1.99254430460726,
25.7288446087131));
#17296=CARTESIAN_POINT('Ctrl Pts',(0.0972015680904663,-1.99238318081486,
25.7290597823846));
#17297=CARTESIAN_POINT('Ctrl Pts',(0.105794302577378,-1.99194944072073,
25.7296087874463));
#17298=CARTESIAN_POINT('Ctrl Pts',(0.1110255767775,-1.99166471365752,25.7299419510193));
#17299=CARTESIAN_POINT('Ctrl Pts',(0.141092151570577,-1.98990942432509,
25.7318509463703));
#17300=CARTESIAN_POINT('Ctrl Pts',(0.165900660110943,-1.9879948745994,25.7334031411506));
#17301=CARTESIAN_POINT('Ctrl Pts',(0.39466952605564,-1.96602741558078,25.7475577469129));
#17302=CARTESIAN_POINT('Ctrl Pts',(0.594457564142217,-1.91511710448562,
25.7588649070505));
#17303=CARTESIAN_POINT('Ctrl Pts',(0.827221246453771,-1.81577633732689,
25.7739450648069));
#17304=CARTESIAN_POINT('Ctrl Pts',(0.870737583357324,-1.79531452617533,
25.7768474743026));
#17305=CARTESIAN_POINT('Ctrl Pts',(0.930632560316081,-1.764461194807,25.7809877021675));
#17306=CARTESIAN_POINT('Ctrl Pts',(0.947665253100583,-1.75537198304105,
25.7821820494005));
#17307=CARTESIAN_POINT('Ctrl Pts',(0.973302588009724,-1.74120915659556,
25.7840071263342));
#17308=CARTESIAN_POINT('Ctrl Pts',(0.982005774331486,-1.73631561310041,
25.784631551375));
#17309=CARTESIAN_POINT('Ctrl Pts',(0.997990221366245,-1.72716941172006,
25.7857875905996));
#17310=CARTESIAN_POINT('Ctrl Pts',(1.00528199285063,-1.72293550954634,25.7863185268859));
#17311=CARTESIAN_POINT('Ctrl Pts',(1.01705416968354,-1.71599992682536,25.787181606723));
#17312=CARTESIAN_POINT('Ctrl Pts',(1.02155122629428,-1.71332659587749,25.7875127190309));
#17313=CARTESIAN_POINT('Ctrl Pts',(1.03018977175762,-1.70814520422992,25.7881515089942));
#17314=CARTESIAN_POINT('Ctrl Pts',(1.03433275265107,-1.70563969251474,25.7884590918867));
#17315=CARTESIAN_POINT('Ctrl Pts',(1.04377832705844,-1.69988031094873,25.7891631743345));
#17316=CARTESIAN_POINT('Ctrl Pts',(1.0490748815663,-1.69661668004448,25.7895600305664));
#17317=CARTESIAN_POINT('Ctrl Pts',(1.0652931086993,-1.68651835176321,25.7907815746728));
#17318=CARTESIAN_POINT('Ctrl Pts',(1.07616373038996,-1.67960268239853,25.7916092478226));
#17319=CARTESIAN_POINT('Ctrl Pts',(1.17691520531392,-1.61412700138943,25.7993651544078));
#17320=CARTESIAN_POINT('Ctrl Pts',(1.26198662125724,-1.54852131668962,25.8065632728672));
#17321=CARTESIAN_POINT('Ctrl Pts',(1.43220889047856,-1.39386904468949,25.822391630411));
#17322=CARTESIAN_POINT('Ctrl Pts',(1.51523941591109,-1.30312734898599,25.8310487804382));
#17323=CARTESIAN_POINT('Ctrl Pts',(1.61745508094546,-1.16834154709674,25.84270063217));
#17324=CARTESIAN_POINT('Ctrl Pts',(1.64421010318575,-1.13037899443386,25.8458633273837));
#17325=CARTESIAN_POINT('Ctrl Pts',(1.68256145873976,-1.07171547255883,25.8505375077663));
#17326=CARTESIAN_POINT('Ctrl Pts',(1.69515278252784,-1.05168639965404,25.8520975212853));
#17327=CARTESIAN_POINT('Ctrl Pts',(1.71019257122284,-1.02679034037971,25.8539885365143));
#17328=CARTESIAN_POINT('Ctrl Pts',(1.71298070295101,-1.02213215718674,25.8543403180291));
#17329=CARTESIAN_POINT('Ctrl Pts',(1.71733039127652,-1.01479726636076,25.85489097836));
#17330=CARTESIAN_POINT('Ctrl Pts',(1.71890476065637,-1.012128247175,25.8550906773256));
#17331=CARTESIAN_POINT('Ctrl Pts',(1.72183703087128,-1.0071306110716,25.8554633292266));
#17332=CARTESIAN_POINT('Ctrl Pts',(1.72319641603441,-1.00480293616457,25.8556363759171));
#17333=CARTESIAN_POINT('Ctrl Pts',(1.72627443342344,-0.999507829862,25.8560288634599));
#17334=CARTESIAN_POINT('Ctrl Pts',(1.72799013065602,-0.996538724903854,
25.8562481128267));
#17335=CARTESIAN_POINT('Ctrl Pts',(1.73306863173539,-0.987697559558204,
25.8568985610925));
#17336=CARTESIAN_POINT('Ctrl Pts',(1.73640926436061,-0.981812722097654,
25.8573283529338));
#17337=CARTESIAN_POINT('Ctrl Pts',(1.76042407689899,-0.93900241183533,25.8604329558507));
#17338=CARTESIAN_POINT('Ctrl Pts',(1.77995024042742,-0.901441188220266,
25.8630386940851));
#17339=CARTESIAN_POINT('Ctrl Pts',(1.83288686438338,-0.791171291581292,
25.8704346156787));
#17340=CARTESIAN_POINT('Ctrl Pts',(1.86313925828265,-0.717035772964954,
25.8750999933681));
#17341=CARTESIAN_POINT('Ctrl Pts',(1.92122907527788,-0.545934711010538,
25.8855921925858));
#17342=CARTESIAN_POINT('Ctrl Pts',(1.94633272388889,-0.44827856855005,25.8913968898663));
#17343=CARTESIAN_POINT('Ctrl Pts',(1.97291971163532,-0.298727448959983,
25.9004243087824));
#17344=CARTESIAN_POINT('Ctrl Pts',(1.97993798019173,-0.247982396716648,
25.9035090895083));
#17345=CARTESIAN_POINT('Ctrl Pts',(1.98801726507701,-0.166585385870296,
25.9085297281418));
#17346=CARTESIAN_POINT('Ctrl Pts',(1.9903379835977,-0.136080451487063,25.9104272749125));
#17347=CARTESIAN_POINT('Ctrl Pts',(1.99241668309104,-0.0968454992855836,
25.9128929712981));
#17348=CARTESIAN_POINT('Ctrl Pts',(1.99282020784631,-0.0881527374766316,
25.9134408351324));
#17349=CARTESIAN_POINT('Ctrl Pts',(1.99337933952493,-0.0741271314738322,
25.9143274451045));
#17350=CARTESIAN_POINT('Ctrl Pts',(1.99357045687673,-0.068795751551865,
25.914665076476));
#17351=CARTESIAN_POINT('Ctrl Pts',(1.99389425951927,-0.0586233501982341,
25.915310485207));
#17352=CARTESIAN_POINT('Ctrl Pts',(1.9940307067648,-0.0537824797845978,
25.9156181423365));
#17353=CARTESIAN_POINT('Ctrl Pts',(1.99430238156014,-0.0427128653186683,
25.9163228682519));
#17354=CARTESIAN_POINT('Ctrl Pts',(1.99442605794871,-0.0364839126123607,
25.9167202960553));
#17355=CARTESIAN_POINT('Ctrl Pts',(1.99471664821841,-0.017326845509537,
25.9179453228491));
#17356=CARTESIAN_POINT('Ctrl Pts',(1.99478704939554,-0.00439780997735998,
25.9187759319005));
#17357=CARTESIAN_POINT('Ctrl Pts',(1.99426185797431,0.118406896693262,25.9267031633904));
#17358=CARTESIAN_POINT('Ctrl Pts',(1.98471466589682,0.228037020273399,25.9340835522411));
#17359=CARTESIAN_POINT('Ctrl Pts',(1.96453818861248,0.345996943436812,25.9423284372156));
#17360=CARTESIAN_POINT('Ctrl Pts',(1.96280940949652,0.355673161983693,25.9430068938583));
#17361=CARTESIAN_POINT('Ctrl Pts',(1.9401839880797,0.477119293833564,25.9515478353791));
#17362=CARTESIAN_POINT('Ctrl Pts',(1.9098397745849,0.58691415201389,25.9595589842457));
#17363=CARTESIAN_POINT('Ctrl Pts',(1.85503359399821,0.734716242874107,25.9703987642592));
#17364=CARTESIAN_POINT('Ctrl Pts',(1.83840174070168,0.775394853529512,25.9733862077173));
#17365=CARTESIAN_POINT('Ctrl Pts',(1.81112455695698,0.836286126899067,25.9778317768523));
#17366=CARTESIAN_POINT('Ctrl Pts',(1.80145418941835,0.856918642892758,25.9793333478071));
#17367=CARTESIAN_POINT('Ctrl Pts',(1.78907260376595,0.882199270848949,25.9811632221525));
#17368=CARTESIAN_POINT('Ctrl Pts',(1.78669381593469,0.887007071420386,25.9815107709976));
#17369=CARTESIAN_POINT('Ctrl Pts',(1.78291666128578,0.89456428222356,25.9820562892128));
#17370=CARTESIAN_POINT('Ctrl Pts',(1.78153128347637,0.897320100316879,25.9822550539083));
#17371=CARTESIAN_POINT('Ctrl Pts',(1.778922287721,0.9024801016507,25.9826268973211));
#17372=CARTESIAN_POINT('Ctrl Pts',(1.77770019892014,0.904884988547796,25.9828000655256));
#17373=CARTESIAN_POINT('Ctrl Pts',(1.77490369323756,0.910360560287811,25.9831940459864));
#17374=CARTESIAN_POINT('Ctrl Pts',(1.77332618787937,0.913429637036049,25.9834146609613));
#17375=CARTESIAN_POINT('Ctrl Pts',(1.76847676335533,0.922804403181734,25.9840879456939));
#17376=CARTESIAN_POINT('Ctrl Pts',(1.76517907215287,0.929096806555903,25.9845390218287));
#17377=CARTESIAN_POINT('Ctrl Pts',(1.73899800009601,0.978410966779382,25.9880686154783));
#17378=CARTESIAN_POINT('Ctrl Pts',(1.71457658295664,1.02060281694847,25.9910553215393));
#17379=CARTESIAN_POINT('Ctrl Pts',(1.68054852643241,1.07471614644264,25.9948982501646));
#17380=CARTESIAN_POINT('Ctrl Pts',(1.67231846800554,1.08747832402456,25.9958054947261));
#17381=CARTESIAN_POINT('Ctrl Pts',(1.63288112388631,1.14712634662467,26.0000561249536));
#17382=CARTESIAN_POINT('Ctrl Pts',(1.59984178874383,1.19277256806037,26.0033399375662));
#17383=CARTESIAN_POINT('Ctrl Pts',(1.50212077393058,1.31640214040468,26.0124927508386));
#17384=CARTESIAN_POINT('Ctrl Pts',(1.43337099195527,1.39094498415361,26.0183274019524));
#17385=CARTESIAN_POINT('Ctrl Pts',(1.32125231619151,1.49533174266239,26.0274264166253));
#17386=CARTESIAN_POINT('Ctrl Pts',(1.28187717936533,1.52922038162306,26.0305530306983));
#17387=CARTESIAN_POINT('Ctrl Pts',(1.21703578395128,1.58076134278926,26.035635770227));
#17388=CARTESIAN_POINT('Ctrl Pts',(1.19240225858182,1.59942465043815,26.0375523515315));
#17389=CARTESIAN_POINT('Ctrl Pts',(1.16026458267995,1.62261823278915,26.0400394609623));
#17390=CARTESIAN_POINT('Ctrl Pts',(1.15314959502155,1.62768235193344,26.0405892611953));
#17391=CARTESIAN_POINT('Ctrl Pts',(1.14162946884152,1.63576839819618,26.041478249417));
#17392=CARTESIAN_POINT('Ctrl Pts',(1.13724499083379,1.63881967482166,26.0418163116435));
#17393=CARTESIAN_POINT('Ctrl Pts',(1.12886364557716,1.64460264776726,26.0424620430906));
#17394=CARTESIAN_POINT('Ctrl Pts',(1.12486898045824,1.64733748074666,26.0427695899667));
#17395=CARTESIAN_POINT('Ctrl Pts',(1.11572171645459,1.65355110750593,26.0434733581944));
#17396=CARTESIAN_POINT('Ctrl Pts',(1.11056275012345,1.65702039525595,26.0438699350786));
#17397=CARTESIAN_POINT('Ctrl Pts',(1.09468126240914,1.66759285302972,26.0450897791169));
#17398=CARTESIAN_POINT('Ctrl Pts',(1.08390635783943,1.67461636929122,26.0459160194851));
#17399=CARTESIAN_POINT('Ctrl Pts',(0.952689205382368,1.75835204048236,26.0559631584849));
#17400=CARTESIAN_POINT('Ctrl Pts',(0.82443882223363,1.82200541545647,26.0656788882564));
#17401=CARTESIAN_POINT('Ctrl Pts',(0.596849724799946,1.90598189114176,26.0825533825283));
#17402=CARTESIAN_POINT('Ctrl Pts',(0.500713760629589,1.93346404181297,26.0895671071567));
#17403=CARTESIAN_POINT('Ctrl Pts',(0.366140608924806,1.96121877204345,26.0989693445146));
#17404=CARTESIAN_POINT('Ctrl Pts',(0.329149317566016,1.96776500465066,26.1015106883999));
#17405=CARTESIAN_POINT('Ctrl Pts',(0.271772924509367,1.97625525746801,26.1053651905389));
#17406=CARTESIAN_POINT('Ctrl Pts',(0.251507089699256,1.97893648955981,26.1067099342092));
#17407=CARTESIAN_POINT('Ctrl Pts',(0.226061599615823,1.98190577631284,26.1083745302139));
#17408=CARTESIAN_POINT('Ctrl Pts',(0.220918144399159,1.98248569425699,26.108709787391));
#17409=CARTESIAN_POINT('Ctrl Pts',(0.21274761949423,1.98337471765808,26.1092403575557));
#17410=CARTESIAN_POINT('Ctrl Pts',(0.209722044188232,1.98369692360802,26.1094363955803));
#17411=CARTESIAN_POINT('Ctrl Pts',(0.204005154906916,1.9842925129566,26.1098059787241));
#17412=CARTESIAN_POINT('Ctrl Pts',(0.201314055002673,1.98456734114928,26.109979600685));
#17413=CARTESIAN_POINT('Ctrl Pts',(0.195178431731702,1.98518133218912,26.1103746633527));
#17414=CARTESIAN_POINT('Ctrl Pts',(0.191733584684177,1.98551700441769,26.110595905561));
#17415=CARTESIAN_POINT('Ctrl Pts',(0.182635416155084,1.98637964762467,26.1111787749106));
#17416=CARTESIAN_POINT('Ctrl Pts',(0.176980637970635,1.98689145536221,26.1115395655058));
#17417=CARTESIAN_POINT('Ctrl Pts',(0.139604520138677,1.99011349467939,26.113914948589));
#17418=CARTESIAN_POINT('Ctrl Pts',(0.107822258080884,1.99208829679993,26.1158905150858));
#17419=CARTESIAN_POINT('Ctrl Pts',(-0.122430932623135,2.00086780924987,
26.1299705230797));
#17420=CARTESIAN_POINT('Ctrl Pts',(-0.320901624951784,1.97876321495778,
26.1409631319081));
#17421=CARTESIAN_POINT('Ctrl Pts',(-0.558400312333835,1.91557767715059,
26.1556192864236));
#17422=CARTESIAN_POINT('Ctrl Pts',(-0.603498923023268,1.90185102235544,
26.1584666489346));
#17423=CARTESIAN_POINT('Ctrl Pts',(-0.666069549896328,1.88035668408686,
26.1625336791399));
#17424=CARTESIAN_POINT('Ctrl Pts',(-0.683982295194189,1.87391517593918,
26.1637116263799));
#17425=CARTESIAN_POINT('Ctrl Pts',(-0.715204798918712,1.86218010435634,
26.1657904182511));
#17426=CARTESIAN_POINT('Ctrl Pts',(-0.728555009176556,1.85699763787855,
26.1666875815025));
#17427=CARTESIAN_POINT('Ctrl Pts',(-0.747876741195922,1.84925664043125,
26.167998631637));
#17428=CARTESIAN_POINT('Ctrl Pts',(-0.753893601325338,1.84681189579846,
26.1684086857675));
#17429=CARTESIAN_POINT('Ctrl Pts',(-0.764410984831291,1.84247855604525,
26.169128638015));
#17430=CARTESIAN_POINT('Ctrl Pts',(-0.768916739464059,1.8406027355994,26.1694381014841));
#17431=CARTESIAN_POINT('Ctrl Pts',(-0.777641267934519,1.83693294301787,
26.1700393354339));
#17432=CARTESIAN_POINT('Ctrl Pts',(-0.781860834535907,1.83514092471938,
26.1703310379046));
#17433=CARTESIAN_POINT('Ctrl Pts',(-0.793061823184645,1.83033830509514,
26.1711078404132));
#17434=CARTESIAN_POINT('Ctrl Pts',(-0.800032221187363,1.82730233100656,
26.1715938036627));
#17435=CARTESIAN_POINT('Ctrl Pts',(-0.824909929847585,1.81629715331854,
26.173337519136));
#17436=CARTESIAN_POINT('Ctrl Pts',(-0.842716443699149,1.80810417051011,
26.1746029143048));
#17437=CARTESIAN_POINT('Ctrl Pts',(-0.95314596916628,1.75530867440647,26.1825618115649));
#17438=CARTESIAN_POINT('Ctrl Pts',(-1.04231188331705,1.70387083882086,26.1894943428646));
#17439=CARTESIAN_POINT('Ctrl Pts',(-1.26080109961505,1.55424111626821,26.2077592632226));
#17440=CARTESIAN_POINT('Ctrl Pts',(-1.38283847185585,1.44673541264575,26.2192909718127));
#17441=CARTESIAN_POINT('Ctrl Pts',(-1.50717392643413,1.30693600594174,26.2317864893768));
#17442=CARTESIAN_POINT('Ctrl Pts',(-1.52346710663281,1.28790647476713,26.2334400607132));
#17443=CARTESIAN_POINT('Ctrl Pts',(-1.54291335661809,1.26430869817792,26.2354284872711));
#17444=CARTESIAN_POINT('Ctrl Pts',(-1.54641060120708,1.26002871576761,26.2357866940909));
#17445=CARTESIAN_POINT('Ctrl Pts',(-1.5518543993518,1.25330970731822,26.2363451543882));
#17446=CARTESIAN_POINT('Ctrl Pts',(-1.55381306204281,1.25088059693913,26.2365462663092));
#17447=CARTESIAN_POINT('Ctrl Pts',(-1.55745146445279,1.24634656111072,26.2369201702297));
#17448=CARTESIAN_POINT('Ctrl Pts',(-1.55913262412154,1.24424285212039,26.2370930623844));
#17449=CARTESIAN_POINT('Ctrl Pts',(-1.56292557622647,1.23947680614966,26.2374834264998));
#17450=CARTESIAN_POINT('Ctrl Pts',(-1.56503482321811,1.23681248066952,26.2377007153082));
#17451=CARTESIAN_POINT('Ctrl Pts',(-1.571234413546,1.22894012633011,26.2383400411756));
#17452=CARTESIAN_POINT('Ctrl Pts',(-1.57530569270704,1.22371703997052,26.2387607415737));
#17453=CARTESIAN_POINT('Ctrl Pts',(-1.60317302015194,1.18759620235874,26.2416470540721));
#17454=CARTESIAN_POINT('Ctrl Pts',(-1.62608639224044,1.15602422432862,26.2440541342699));
#17455=CARTESIAN_POINT('Ctrl Pts',(-1.74443309118259,0.982467638912514,
26.2567960451355));
#17456=CARTESIAN_POINT('Ctrl Pts',(-1.822233538656,0.829316865170294,26.2663805023754));
#17457=CARTESIAN_POINT('Ctrl Pts',(-1.89967946163673,0.6114421817386,26.2800308128428));
#17458=CARTESIAN_POINT('Ctrl Pts',(-1.91724614571517,0.553904242374328,
26.2836302757754));
#17459=CARTESIAN_POINT('Ctrl Pts',(-1.94071476147354,0.46241941585726,26.2894095603495));
#17460=CARTESIAN_POINT('Ctrl Pts',(-1.94838317109513,0.428961884230149,
26.2915343620131));
#17461=CARTESIAN_POINT('Ctrl Pts',(-1.95697879364363,0.386449925805058,
26.2942548760653));
#17462=CARTESIAN_POINT('Ctrl Pts',(-1.95871273972537,0.377563164004095,
26.29482469995));
#17463=CARTESIAN_POINT('Ctrl Pts',(-1.96138656100846,0.363345047903939,
26.2957382855517));
#17464=CARTESIAN_POINT('Ctrl Pts',(-1.9623653533818,0.358021067041667,26.2960808052573));
#17465=CARTESIAN_POINT('Ctrl Pts',(-1.9641758859554,0.3479424515438,26.2967300502989));
#17466=CARTESIAN_POINT('Ctrl Pts',(-1.96501206449619,0.343188645305611,
26.2970366319125));
#17467=CARTESIAN_POINT('Ctrl Pts',(-1.96686437449493,0.332429232462508,
26.297731339858));
#17468=CARTESIAN_POINT('Ctrl Pts',(-1.96787026552719,0.326421933924422,
26.2981197885187));
#17469=CARTESIAN_POINT('Ctrl Pts',(-1.97038262530088,0.310984047049956,
26.2991195593547));
#17470=CARTESIAN_POINT('Ctrl Pts',(-1.97184889681389,0.301547161270824,
26.2997321491823));
#17471=CARTESIAN_POINT('Ctrl Pts',(-1.98023994509146,0.24486246526018,26.3034208341351));
#17472=CARTESIAN_POINT('Ctrl Pts',(-1.98553353090647,0.197392540164988,
26.3065480367885));
#17473=CARTESIAN_POINT('Ctrl Pts',(-1.99012763534971,0.136382250053488,
26.3106197701565));
#17474=CARTESIAN_POINT('Ctrl Pts',(-1.99100117429133,0.122973304434868,
26.3115178568455));
#17475=CARTESIAN_POINT('Ctrl Pts',(-1.99377655691672,0.0725169374495927,
26.314909136307));
#17476=CARTESIAN_POINT('Ctrl Pts',(-1.99478023382093,0.0354292575438041,
26.3174261235079));
#17477=CARTESIAN_POINT('Ctrl Pts',(-1.99460412678541,-0.17578471832943,
26.3318843840123));
#17478=CARTESIAN_POINT('Ctrl Pts',(-1.97166284332363,-0.349123068784183,
26.3443142834677));
#17479=CARTESIAN_POINT('Ctrl Pts',(-1.918691056218,-0.546408367989368,26.3580335800415));
#17480=CARTESIAN_POINT('Ctrl Pts',(-1.91020842683993,-0.575362045656703,
26.3600333459574));
#17481=CARTESIAN_POINT('Ctrl Pts',(-1.89938054039609,-0.60943605859832,
26.3623615716245));
#17482=CARTESIAN_POINT('Ctrl Pts',(-1.89766696246977,-0.614751045636675,
26.3627240019386));
#17483=CARTESIAN_POINT('Ctrl Pts',(-1.89485235788306,-0.623357158307403,
26.3633095824338));
#17484=CARTESIAN_POINT('Ctrl Pts',(-1.89376503799945,-0.626652683938401,
26.3635335144055));
#17485=CARTESIAN_POINT('Ctrl Pts',(-1.89181658524206,-0.632506804685954,
26.3639307425749));
#17486=CARTESIAN_POINT('Ctrl Pts',(-1.89095885507573,-0.635066499592859,
26.36410423715));
#17487=CARTESIAN_POINT('Ctrl Pts',(-1.88911394872385,-0.640535313916996,
26.3644744943596));
#17488=CARTESIAN_POINT('Ctrl Pts',(-1.88812525126198,-0.643443886828484,
26.3646711651092));
#17489=CARTESIAN_POINT('Ctrl Pts',(-1.8854099220658,-0.651371754444841,
26.3652065773537));
#17490=CARTESIAN_POINT('Ctrl Pts',(-1.88366995363748,-0.65638650506382,
26.3655445376205));
#17491=CARTESIAN_POINT('Ctrl Pts',(-1.87459671124977,-0.682203214941757,
26.3672810178602));
#17492=CARTESIAN_POINT('Ctrl Pts',(-1.86693845244365,-0.70289043921845,
26.3686611066377));
#17493=CARTESIAN_POINT('Ctrl Pts',(-1.84374070659885,-0.76249833401675,
26.3726162181632));
#17494=CARTESIAN_POINT('Ctrl Pts',(-1.82731534158822,-0.801063436021313,
26.3751482999223));
#17495=CARTESIAN_POINT('Ctrl Pts',(-1.75471198944255,-0.957649823863518,
26.3854292521458));
#17496=CARTESIAN_POINT('Ctrl Pts',(-1.68821691862545,-1.07053009148921,
26.3928596036727));
#17497=CARTESIAN_POINT('Ctrl Pts',(-1.54882912941497,-1.26147932492719,
26.4067117767347));
#17498=CARTESIAN_POINT('Ctrl Pts',(-1.47982477256909,-1.34175843473198,
26.4130296890303));
#17499=CARTESIAN_POINT('Ctrl Pts',(-1.39566419424561,-1.42524184998158,
26.4204298009215));
#17500=CARTESIAN_POINT('Ctrl Pts',(-1.38644886770617,-1.43420793434731,
26.4212361936577));
#17501=CARTESIAN_POINT('Ctrl Pts',(-1.37265067476396,-1.44737566920481,
26.4224382240405));
#17502=CARTESIAN_POINT('Ctrl Pts',(-1.36813367926805,-1.45164611285514,
26.4228308805203));
#17503=CARTESIAN_POINT('Ctrl Pts',(-1.36006353019259,-1.45920464367752,
26.4235309574526));
#17504=CARTESIAN_POINT('Ctrl Pts',(-1.35651821282052,-1.46250105500789,
26.4238380175285));
#17505=CARTESIAN_POINT('Ctrl Pts',(-1.34903539215994,-1.46940791216685,
26.4244850932653));
#17506=CARTESIAN_POINT('Ctrl Pts',(-1.34509531973702,-1.47301550621327,
26.4248252267161));
#17507=CARTESIAN_POINT('Ctrl Pts',(-1.33467456585134,-1.48248024304729,
26.4257233157824));
#17508=CARTESIAN_POINT('Ctrl Pts',(-1.32816987583134,-1.48831066806087,
26.4262823914972));
#17509=CARTESIAN_POINT('Ctrl Pts',(-1.29846490397567,-1.51458665235052,
26.4288288937035));
#17510=CARTESIAN_POINT('Ctrl Pts',(-1.27483047793644,-1.53453279805448,
26.4308368911397));
#17511=CARTESIAN_POINT('Ctrl Pts',(-1.21024745778367,-1.58651535148252,
26.4362798463231));
#17512=CARTESIAN_POINT('Ctrl Pts',(-1.16849646028572,-1.6175120113899,26.4397535099787));
#17513=CARTESIAN_POINT('Ctrl Pts',(-1.04191462758986,-1.70402837929633,
26.4501511971157));
#17514=CARTESIAN_POINT('Ctrl Pts',(-0.954013597706767,-1.75475170945212,
26.4572118767671));
#17515=CARTESIAN_POINT('Ctrl Pts',(-0.855502264728771,-1.80200062440219,
26.46483432746));
#17516=CARTESIAN_POINT('Ctrl Pts',(-0.848335881024695,-1.8053854459854,
26.4653871833649));
#17517=CARTESIAN_POINT('Ctrl Pts',(-0.774193153054797,-1.83986555427451,
26.471089046765));
#17518=CARTESIAN_POINT('Ctrl Pts',(-0.705554993997839,-1.8672637295543,
26.4762195795999));
#17519=CARTESIAN_POINT('Ctrl Pts',(-0.598624248243548,-1.90320631581014,
26.4838547097468));
#17520=CARTESIAN_POINT('Ctrl Pts',(-0.561337915077519,-1.91453532581896,
26.4864526390203));
#17521=CARTESIAN_POINT('Ctrl Pts',(-0.517352955306116,-1.92650390802183,
26.4894240026949));
#17522=CARTESIAN_POINT('Ctrl Pts',(-0.510956410642753,-1.92821029387603,
26.489853829232));
#17523=CARTESIAN_POINT('Ctrl Pts',(-0.5012641960562,-1.93074423795946,26.4905015350181));
#17524=CARTESIAN_POINT('Ctrl Pts',(-0.49797479084882,-1.93159525127854,
26.4907207353879));
#17525=CARTESIAN_POINT('Ctrl Pts',(-0.492074417172123,-1.93310568313844,
26.4911127918006));
#17526=CARTESIAN_POINT('Ctrl Pts',(-0.489464284526345,-1.93376822000055,
26.4912858263069));
#17527=CARTESIAN_POINT('Ctrl Pts',(-0.483826434209728,-1.93518714415077,
26.4916587158718));
#17528=CARTESIAN_POINT('Ctrl Pts',(-0.480798291678137,-1.93594170996259,
26.4918584646121));
#17529=CARTESIAN_POINT('Ctrl Pts',(-0.472400757895147,-1.93801332581395,
26.4924109537523));
#17530=CARTESIAN_POINT('Ctrl Pts',(-0.467027591755882,-1.93931517742277,
26.4927628269616));
#17531=CARTESIAN_POINT('Ctrl Pts',(-0.437259334388041,-1.94639676250448,
26.4947035647494));
#17532=CARTESIAN_POINT('Ctrl Pts',(-0.412761062312387,-1.95173884780165,
26.496268439976));
#17533=CARTESIAN_POINT('Ctrl Pts',(-0.229162515185292,-1.98816238159269,
26.5078004067795));
#17534=CARTESIAN_POINT('Ctrl Pts',(-0.0668850640269317,-2.00021145098082,
26.516940738108));
#17535=CARTESIAN_POINT('Ctrl Pts',(0.207682379064669,-1.98710948842253,
26.5330064919151));
#17536=CARTESIAN_POINT('Ctrl Pts',(0.319611763620731,-1.97220155669412,
26.5397209213675));
#17537=CARTESIAN_POINT('Ctrl Pts',(0.442320410307593,-1.94513442475644,
26.5475643696767));
#17538=CARTESIAN_POINT('Ctrl Pts',(0.454939108758556,-1.94222183863556,
26.5483765391001));
#17539=CARTESIAN_POINT('Ctrl Pts',(0.473589023105039,-1.93772543641813,
26.5495855364325));
#17540=CARTESIAN_POINT('Ctrl Pts',(0.479642786246814,-1.93623583943572,
26.5499793320645));
#17541=CARTESIAN_POINT('Ctrl Pts',(0.490386988582767,-1.93353862693419,
26.5506806904484));
#17542=CARTESIAN_POINT('Ctrl Pts',(0.495080220679038,-1.93234225613173,
26.5509878879997));
#17543=CARTESIAN_POINT('Ctrl Pts',(0.504931603781281,-1.92979275451388,
26.5516344880191));
#17544=CARTESIAN_POINT('Ctrl Pts',(0.510088771878332,-1.92843600976659,
26.5519740053624));
#17545=CARTESIAN_POINT('Ctrl Pts',(0.523637879894014,-1.92481336552385,
26.5528687267591));
#17546=CARTESIAN_POINT('Ctrl Pts',(0.532020484927929,-1.92251328240117,
26.5534250357786));
#17547=CARTESIAN_POINT('Ctrl Pts',(0.569741253302596,-1.91189757626506,
26.5559410358045));
#17548=CARTESIAN_POINT('Ctrl Pts',(0.598900094825213,-1.90296503988263,
26.5579206992819));
#17549=CARTESIAN_POINT('Ctrl Pts',(0.676240318042172,-1.87731899727726,
26.5632683232878));
#17550=CARTESIAN_POINT('Ctrl Pts',(0.724002204467846,-1.85942132128623,
26.5666733430939));
#17551=CARTESIAN_POINT('Ctrl Pts',(0.863764592783322,-1.80084703445125,
26.5769417616456));
#17552=CARTESIAN_POINT('Ctrl Pts',(0.953427038871567,-1.75502503740542,
26.583942198752));
#17553=CARTESIAN_POINT('Ctrl Pts',(1.05674765737386,-1.69196111948414,26.5923876798864));
#17554=CARTESIAN_POINT('Ctrl Pts',(1.07408476183507,-1.68100861780158,26.5938180630293));
#17555=CARTESIAN_POINT('Ctrl Pts',(1.17559554214738,-1.61466878461484,26.602262744138));
#17556=CARTESIAN_POINT('Ctrl Pts',(1.25565493814225,-1.55322765029401,26.6092172160306));
#17557=CARTESIAN_POINT('Ctrl Pts',(1.33658106659261,-1.48075662463046,26.6163132050611));
#17558=CARTESIAN_POINT('Ctrl Pts',(1.34239545496186,-1.47548757243513,26.6168233947685));
#17559=CARTESIAN_POINT('Ctrl Pts',(1.35079894185163,-1.46778146197996,26.6175610909664));
#17560=CARTESIAN_POINT('Ctrl Pts',(1.35341276377315,-1.46537165687626,26.6177905900025));
#17561=CARTESIAN_POINT('Ctrl Pts',(1.35801356460308,-1.46110715162975,26.6181946086389));
#17562=CARTESIAN_POINT('Ctrl Pts',(1.36000321195562,-1.45925536285512,26.6183693481036));
#17563=CARTESIAN_POINT('Ctrl Pts',(1.36417487842115,-1.45535679946785,26.6187357539314));
#17564=CARTESIAN_POINT('Ctrl Pts',(1.36635607490487,-1.45330918580058,26.6189273535179));
#17565=CARTESIAN_POINT('Ctrl Pts',(1.37213224134577,-1.44786227021083,26.619434822615));
#17566=CARTESIAN_POINT('Ctrl Pts',(1.37571921384765,-1.4444544600488,26.6197500431793));
#17567=CARTESIAN_POINT('Ctrl Pts',(1.39224129355025,-1.42864025403441,26.6212025955013));
#17568=CARTESIAN_POINT('Ctrl Pts',(1.40502200223316,-1.41607274613837,26.622327942864));
#17569=CARTESIAN_POINT('Ctrl Pts',(1.439588913497,-1.38115364771536,26.6253823062752));
#17570=CARTESIAN_POINT('Ctrl Pts',(1.46102340915189,-1.3584595908769,26.6272883250738));
#17571=CARTESIAN_POINT('Ctrl Pts',(1.53445356755619,-1.27696491137922,26.6339011045656));
#17572=CARTESIAN_POINT('Ctrl Pts',(1.58350646538346,-1.21560525531993,26.6384738714332));
#17573=CARTESIAN_POINT('Ctrl Pts',(1.72203520137679,-1.01965555229839,26.6524043996169));
#17574=CARTESIAN_POINT('Ctrl Pts',(1.79888496597703,-0.876988223770606,
26.6617097844222));
#17575=CARTESIAN_POINT('Ctrl Pts',(1.86143030003341,-0.717084212650901,
26.6723348320138));
#17576=CARTESIAN_POINT('Ctrl Pts',(1.86508874791876,-0.707514301115196,
26.6729711537058));
#17577=CARTESIAN_POINT('Ctrl Pts',(1.87357378104815,-0.684795611325849,
26.6744831068838));
#17578=CARTESIAN_POINT('Ctrl Pts',(1.87833586643428,-0.671623480303962,
26.6753607865642));
#17579=CARTESIAN_POINT('Ctrl Pts',(1.88506019929044,-0.652392629358714,
26.6766441375281));
#17580=CARTESIAN_POINT('Ctrl Pts',(1.8871328469539,-0.646372736285141,26.6770461469071));
#17581=CARTESIAN_POINT('Ctrl Pts',(1.89074251763782,-0.635723280272227,
26.6777578526926));
#17582=CARTESIAN_POINT('Ctrl Pts',(1.89229145233172,-0.631097786261059,
26.6780671525897));
#17583=CARTESIAN_POINT('Ctrl Pts',(1.89546336637253,-0.62150901625406,26.6787087263598));
#17584=CARTESIAN_POINT('Ctrl Pts',(1.89708385196261,-0.616544960496398,
26.6790410796741));
#17585=CARTESIAN_POINT('Ctrl Pts',(1.90119672856272,-0.603776189745432,
26.6798965524599));
#17586=CARTESIAN_POINT('Ctrl Pts',(1.90366054134505,-0.59596243841925,26.6804206063504));
#17587=CARTESIAN_POINT('Ctrl Pts',(1.91370779322722,-0.56340041594603,26.6826069442676));
#17588=CARTESIAN_POINT('Ctrl Pts',(1.92085701684684,-0.538521830995022,
26.6842833321697));
#17589=CARTESIAN_POINT('Ctrl Pts',(1.97447475946923,-0.337262192228768,
26.6978991188951));
#17590=CARTESIAN_POINT('Ctrl Pts',(1.99702493684115,-0.155434445352629,
26.7106518453713));
#17591=CARTESIAN_POINT('Ctrl Pts',(1.99370248397765,0.0911933319285907,
26.7278134125995));
#17592=CARTESIAN_POINT('Ctrl Pts',(1.98972480144048,0.15544192155548,26.7322585120981));
#17593=CARTESIAN_POINT('Ctrl Pts',(1.97889508195542,0.25331119533604,26.7388956553218));
#17594=CARTESIAN_POINT('Ctrl Pts',(1.97427130654853,0.287133174424992,26.7411642950898));
#17595=CARTESIAN_POINT('Ctrl Pts',(1.96784858906812,0.326547301282571,26.7437660239765));
#17596=CARTESIAN_POINT('Ctrl Pts',(1.96689067741463,0.332268377355896,26.7441426296243));
#17597=CARTESIAN_POINT('Ctrl Pts',(1.96531520264734,0.341432202951507,26.7447441025668));
#17598=CARTESIAN_POINT('Ctrl Pts',(1.96471352616173,0.344877595016709,26.7449698431203));
#17599=CARTESIAN_POINT('Ctrl Pts',(1.96362960052148,0.350989597476334,26.7453695674785));
#17600=CARTESIAN_POINT('Ctrl Pts',(1.96315097625513,0.353656825692593,26.7455437557285));
#17601=CARTESIAN_POINT('Ctrl Pts',(1.96212710995711,0.359296393844331,26.7459115262723));
#17602=CARTESIAN_POINT('Ctrl Pts',(1.96158055004727,0.362268464308082,26.7461050321147));
#17603=CARTESIAN_POINT('Ctrl Pts',(1.96009657599152,0.370236154242418,26.7466229882504));
#17604=CARTESIAN_POINT('Ctrl Pts',(1.95914681059267,0.375229493822779,26.7469467411475));
#17605=CARTESIAN_POINT('Ctrl Pts',(1.95448527410917,0.399237007486242,26.7484994632784));
#17606=CARTESIAN_POINT('Ctrl Pts',(1.95051556888445,0.418200858702199,26.7497143418867));
#17607=CARTESIAN_POINT('Ctrl Pts',(1.93864354439568,0.471062712964736,26.7530758453256));
#17608=CARTESIAN_POINT('Ctrl Pts',(1.93012914789979,0.504817435055281,26.7551934359065));
#17609=CARTESIAN_POINT('Ctrl Pts',(1.89564977476314,0.627837238823449,26.7628617639749));
#17610=CARTESIAN_POINT('Ctrl Pts',(1.8643371691419,0.715483693555913,26.7682327513939));
#17611=CARTESIAN_POINT('Ctrl Pts',(1.76518250623002,0.941752498827515,26.7825611851712));
#17612=CARTESIAN_POINT('Ctrl Pts',(1.68721054741629,1.07521087950721,26.7915459232161));
#17613=CARTESIAN_POINT('Ctrl Pts',(1.58708477675972,1.2084488925758,26.801952976811));
#17614=CARTESIAN_POINT('Ctrl Pts',(1.57940809276774,1.21846496848483,26.8027446031987));
#17615=CARTESIAN_POINT('Ctrl Pts',(1.56783790872435,1.23326798121766,26.8039288066492));
#17616=CARTESIAN_POINT('Ctrl Pts',(1.56401629744102,1.23811091646886,26.8043185312953));
#17617=CARTESIAN_POINT('Ctrl Pts',(1.55715935714487,1.24671796333868,26.8050153253286));
#17618=CARTESIAN_POINT('Ctrl Pts',(1.55413267812496,1.25048892908516,26.8053220467383));
#17619=CARTESIAN_POINT('Ctrl Pts',(1.54771729480738,1.25842264344559,26.8059704204983));
#17620=CARTESIAN_POINT('Ctrl Pts',(1.54432544439457,1.26258278740416,26.8063121983354));
#17621=CARTESIAN_POINT('Ctrl Pts',(1.53529710376685,1.27356534220925,26.8072192754075));
#17622=CARTESIAN_POINT('Ctrl Pts',(1.52963198258032,1.28036396051745,26.8077857355272));
#17623=CARTESIAN_POINT('Ctrl Pts',(1.50320909495184,1.31164796964203,26.8104155483966));
#17624=CARTESIAN_POINT('Ctrl Pts',(1.48190844501357,1.3356665528501,26.8125011550772));
#17625=CARTESIAN_POINT('Ctrl Pts',(1.42273690421611,1.39922989617158,26.8182081552235));
#17626=CARTESIAN_POINT('Ctrl Pts',(1.38380462716622,1.43774422154937,26.8218730297614));
#17627=CARTESIAN_POINT('Ctrl Pts',(1.26682262299384,1.54431280508697,26.8326281361314));
#17628=CARTESIAN_POINT('Ctrl Pts',(1.18500034915161,1.60795289803314,26.8398535337512));
#17629=CARTESIAN_POINT('Ctrl Pts',(1.00442903832286,1.7271028278075,26.8549414240114));
#17630=CARTESIAN_POINT('Ctrl Pts',(0.905123122068543,1.7811570744217,26.8627753378795));
#17631=CARTESIAN_POINT('Ctrl Pts',(0.795389644129964,1.82932539034632,26.8706017864889));
#17632=CARTESIAN_POINT('Ctrl Pts',(0.788997555393894,1.83209140896231,26.8710547836139));
#17633=CARTESIAN_POINT('Ctrl Pts',(0.779384327556876,1.83619165280441,26.8717315708446));
#17634=CARTESIAN_POINT('Ctrl Pts',(0.776174047680886,1.8375509690965,26.8719568324296));
#17635=CARTESIAN_POINT('Ctrl Pts',(0.770620563290229,1.83988530917972,26.8723452029793));
#17636=CARTESIAN_POINT('Ctrl Pts',(0.768279044638956,1.84086428430984,26.8725085502532));
#17637=CARTESIAN_POINT('Ctrl Pts',(0.763436227959547,1.84287818799214,26.8728455522712));
#17638=CARTESIAN_POINT('Ctrl Pts',(0.760934688422781,1.84391249521189,26.8730191668976));
#17639=CARTESIAN_POINT('Ctrl Pts',(0.754933708331309,1.84637941844366,26.8734345627591));
#17640=CARTESIAN_POINT('Ctrl Pts',(0.75143226087567,1.84780719197532,26.8736760505919));
#17641=CARTESIAN_POINT('Ctrl Pts',(0.743956420899055,1.85083082651158,26.8741897982653));
#17642=CARTESIAN_POINT('Ctrl Pts',(0.739980897419763,1.85242386532358,26.8744618913414));
#17643=CARTESIAN_POINT('Ctrl Pts',(0.729040933464063,1.85676679853037,26.8752076822775));
#17644=CARTESIAN_POINT('Ctrl Pts',(0.722066009535537,1.85949033574795,26.8756798806225));
#17645=CARTESIAN_POINT('Ctrl Pts',(0.660729874755481,1.88304343617787,26.8798048770609));
#17646=CARTESIAN_POINT('Ctrl Pts',(0.605490722030305,1.90152541885122,26.8833316051077));
#17647=CARTESIAN_POINT('Ctrl Pts',(0.439327508296859,1.94914281083134,26.8936068513424));
#17648=CARTESIAN_POINT('Ctrl Pts',(0.326616864578987,1.97116472661776,26.9001575546848));
#17649=CARTESIAN_POINT('Ctrl Pts',(0.0946988516750447,1.99602812463555,
26.9137649673544));
#17650=CARTESIAN_POINT('Ctrl Pts',(-0.0241112902371501,1.99812630916227,
26.9208089214977));
#17651=CARTESIAN_POINT('Ctrl Pts',(-0.155358036647482,1.98873335596743,
26.9290217024561));
#17652=CARTESIAN_POINT('Ctrl Pts',(-0.168312104225953,1.98767892365156,
26.9298367542556));
#17653=CARTESIAN_POINT('Ctrl Pts',(-0.187472306828389,1.98593068285675,
26.9310492263832));
#17654=CARTESIAN_POINT('Ctrl Pts',(-0.1936871543292,1.98533418540749,26.9314435887757));
#17655=CARTESIAN_POINT('Ctrl Pts',(-0.204719147762053,1.98422304747911,
26.9321455858987));
#17656=CARTESIAN_POINT('Ctrl Pts',(-0.209537433549834,1.98372001423352,
26.9324528530268));
#17657=CARTESIAN_POINT('Ctrl Pts',(-0.219650951059132,1.98262689625758,
26.9330992221074));
#17658=CARTESIAN_POINT('Ctrl Pts',(-0.224945739569568,1.98203313882651,
26.9334384374999));
#17659=CARTESIAN_POINT('Ctrl Pts',(-0.238851556323302,1.98041730221149,
26.934331508299));
#17660=CARTESIAN_POINT('Ctrl Pts',(-0.24745833586246,1.97936028174012,26.9348864612837));
#17661=CARTESIAN_POINT('Ctrl Pts',(-0.286092619304876,1.97435958660014,
26.9373876491137));
#17662=CARTESIAN_POINT('Ctrl Pts',(-0.316033502074888,1.96978867440507,
26.9393535692194));
#17663=CARTESIAN_POINT('Ctrl Pts',(-0.395603831471121,1.95578029875629,
26.9446551557187));
#17664=CARTESIAN_POINT('Ctrl Pts',(-0.444995765098567,1.94513675971318,
26.9480271007642));
#17665=CARTESIAN_POINT('Ctrl Pts',(-0.597703835169315,1.90610878474122,
26.9587030040645));
#17666=CARTESIAN_POINT('Ctrl Pts',(-0.699167089008799,1.87127284054934,
26.966171819159));
#17667=CARTESIAN_POINT('Ctrl Pts',(-0.903395741189436,1.78221546839838,
26.9817134233405));
#17668=CARTESIAN_POINT('Ctrl Pts',(-1.00524668134954,1.72681838756154,26.9897567143344));
#17669=CARTESIAN_POINT('Ctrl Pts',(-1.10814050981651,1.65864743691404,26.9978169065957));
#17670=CARTESIAN_POINT('Ctrl Pts',(-1.11452726749546,1.65436262172344,26.9983168735835));
#17671=CARTESIAN_POINT('Ctrl Pts',(-1.12380604525255,1.64805945559564,26.9990425487904));
#17672=CARTESIAN_POINT('Ctrl Pts',(-1.12671765027172,1.64607026993382,26.9992701607283));
#17673=CARTESIAN_POINT('Ctrl Pts',(-1.13179884374909,1.64257904002938,26.9996671829498));
#17674=CARTESIAN_POINT('Ctrl Pts',(-1.1339707440804,1.64108039941883,26.9998368225525));
#17675=CARTESIAN_POINT('Ctrl Pts',(-1.13614693334299,1.63957241634298,27.0000067302211));
#17676=CARTESIAN_POINT('Ctrl Pts',(-1.13615416727734,1.63956740354172,27.0000072950154));
#17677=CARTESIAN_POINT('Ctrl Pts',(-1.13616860543781,1.63955739838358,27.0000084222831));
#17678=CARTESIAN_POINT('Ctrl Pts',(-1.13617579222358,1.63955241811355,27.0000089833948));
#17679=CARTESIAN_POINT('Ctrl Pts',(-1.13619011434815,1.63954249308558,27.0000101016001));
#17680=CARTESIAN_POINT('Ctrl Pts',(-1.13619724899851,1.63953754880576,27.00001065864));
#17681=CARTESIAN_POINT('Ctrl Pts',(-1.13621146735668,1.63952769541166,27.0000117687408));
#17682=CARTESIAN_POINT('Ctrl Pts',(-1.13621855040836,1.6395227867531,27.0000123217507));
#17683=CARTESIAN_POINT('Ctrl Pts',(-1.13623266624489,1.63951300413619,27.0000134238444));
#17684=CARTESIAN_POINT('Ctrl Pts',(-1.13623969828764,1.63950813069313,27.0000139728704));
#17685=CARTESIAN_POINT('Ctrl Pts',(-1.13625371274421,1.63949841806804,27.0000150670461));
#17686=CARTESIAN_POINT('Ctrl Pts',(-1.13626069439538,1.63949357941554,27.0000156121364));
#17687=CARTESIAN_POINT('Ctrl Pts',(-1.13627460833467,1.63948393619013,27.0000166984616));
#17688=CARTESIAN_POINT('Ctrl Pts',(-1.13628154001269,1.63947913204103,27.0000172396489));
#17689=CARTESIAN_POINT('Ctrl Pts',(-1.13629535488644,1.6394695572148,27.000018318237));
#17690=CARTESIAN_POINT('Ctrl Pts',(-1.13630223722509,1.63946478713265,27.0000188555709));
#17691=CARTESIAN_POINT('Ctrl Pts',(-1.1363159539005,1.63945528011008,27.0000199264895));
#17692=CARTESIAN_POINT('Ctrl Pts',(-1.13632278740328,1.63945054374864,27.0000204600093));
#17693=CARTESIAN_POINT('Ctrl Pts',(-1.13633640710348,1.63944110368742,27.0000215233541));
#17694=CARTESIAN_POINT('Ctrl Pts',(-1.1363431923928,1.63943640061798,27.0000220531083));
#17695=CARTESIAN_POINT('Ctrl Pts',(-1.1363567158736,1.63942702699959,27.0000231089384));
#17696=CARTESIAN_POINT('Ctrl Pts',(-1.13636345336495,1.63942235693681,27.0000236349596));
#17697=CARTESIAN_POINT('Ctrl Pts',(-1.13637688186724,1.63941304890638,27.0000246833719));
#17698=CARTESIAN_POINT('Ctrl Pts',(-1.13638357207035,1.63940841149955,27.0000252056999));
#17699=CARTESIAN_POINT('Ctrl Pts',(-1.13639690669461,1.63939916829942,27.0000262467803));
#17700=CARTESIAN_POINT('Ctrl Pts',(-1.13640355018902,1.63939456314938,27.0000267654603));
#17701=CARTESIAN_POINT('Ctrl Pts',(-1.13641679171046,1.63938538424726,27.0000277992694));
#17702=CARTESIAN_POINT('Ctrl Pts',(-1.13642338891197,1.63938081106828,27.000028314334));
#17703=CARTESIAN_POINT('Ctrl Pts',(-1.13643653856968,1.63937169561022,27.0000293409686));
#17704=CARTESIAN_POINT('Ctrl Pts',(-1.13644309005181,1.6393671540072,27.0000298524626));
#17705=CARTESIAN_POINT('Ctrl Pts',(-1.13645614861715,1.63935810146337,27.000030871983));
#17706=CARTESIAN_POINT('Ctrl Pts',(-1.13646265482215,1.63935359113216,27.0000313799408));
#17707=CARTESIAN_POINT('Ctrl Pts',(-1.13647562332389,1.63934460079418,27.0000323924274));
#17708=CARTESIAN_POINT('Ctrl Pts',(-1.13648208470954,1.63934012141982,27.0000328968849));
#17709=CARTESIAN_POINT('Ctrl Pts',(-1.1364949641901,1.63933119256976,27.000033902419));
#17710=CARTESIAN_POINT('Ctrl Pts',(-1.13650138127918,1.63932674379216,27.0000344034171));
#17711=CARTESIAN_POINT('Ctrl Pts',(-1.13651417252758,1.63931787588764,27.0000354020604));
#17712=CARTESIAN_POINT('Ctrl Pts',(-1.13652054573941,1.63931345741839,27.0000358996317));
#17713=CARTESIAN_POINT('Ctrl Pts',(-1.13653324979937,1.6393046497404,27.0000368914658));
#17714=CARTESIAN_POINT('Ctrl Pts',(-1.13653957962073,1.63930026124429,27.0000373856485));
#17715=CARTESIAN_POINT('Ctrl Pts',(-1.13655219733819,1.63929151321081,27.0000383707394));
#17716=CARTESIAN_POINT('Ctrl Pts',(-1.13655848421218,1.63928715438284,27.000038861568));
#17717=CARTESIAN_POINT('Ctrl Pts',(-1.13657101653701,1.6392784653397,27.00003983999));
#17718=CARTESIAN_POINT('Ctrl Pts',(-1.13657726094238,1.63927413585014,27.0000403275018));
#17719=CARTESIAN_POINT('Ctrl Pts',(-1.13658970860037,1.63926550529847,27.0000412993116));
#17720=CARTESIAN_POINT('Ctrl Pts',(-1.13659591088148,1.63926120491069,27.0000417835337));
#17721=CARTESIAN_POINT('Ctrl Pts',(-1.13660827507727,1.6392526320195,27.0000427488253));
#17722=CARTESIAN_POINT('Ctrl Pts',(-1.13661443580719,1.63924836033828,27.0000432298024));
#17723=CARTESIAN_POINT('Ctrl Pts',(-1.1366267170069,1.63923984478854,27.0000441886123));
#17724=CARTESIAN_POINT('Ctrl Pts',(-1.13663283649539,1.63923560160117,27.0000446663686));
#17725=CARTESIAN_POINT('Ctrl Pts',(-1.13664503586386,1.63922714258933,27.0000456187878));
#17726=CARTESIAN_POINT('Ctrl Pts',(-1.13665111461065,1.63922292755133,27.0000460933622));
#17727=CARTESIAN_POINT('Ctrl Pts',(-1.13666323275968,1.63921452465721,27.0000470394385));
#17728=CARTESIAN_POINT('Ctrl Pts',(-1.13666927110875,1.63921033753206,27.0000475108581));
#17729=CARTESIAN_POINT('Ctrl Pts',(-1.13668130906122,1.63920199005035,27.0000484506714));
#17730=CARTESIAN_POINT('Ctrl Pts',(-1.13668730747326,1.63919783052058,27.000048918972));
#17731=CARTESIAN_POINT('Ctrl Pts',(-1.13669926598296,1.63918953793247,27.0000498525811));
#17732=CARTESIAN_POINT('Ctrl Pts',(-1.13670522489986,1.63918540569359,27.0000503177974));
#17733=CARTESIAN_POINT('Ctrl Pts',(-1.13671710459646,1.63917716756629,27.0000512452516));
#17734=CARTESIAN_POINT('Ctrl Pts',(-1.13672302431496,1.63917306241443,27.0000517074067));
#17735=CARTESIAN_POINT('Ctrl Pts',(-1.13673484376495,1.63916486587626,27.0000526301554));
#17736=CARTESIAN_POINT('Ctrl Pts',(-1.13674074236875,1.63916077527178,27.0000530906612));
#17737=CARTESIAN_POINT('Ctrl Pts',(-1.13675243253278,1.63915266820433,27.0000540033147));
#17738=CARTESIAN_POINT('Ctrl Pts',(-1.13675827556691,1.63914861604453,27.0000544594811));
#17739=CARTESIAN_POINT('Ctrl Pts',(-1.13676992373392,1.63914053791732,27.000055368854));
#17740=CARTESIAN_POINT('Ctrl Pts',(-1.13677572883104,1.6391365119753,27.0000558220578));
#17741=CARTESIAN_POINT('Ctrl Pts',(-1.13925346042638,1.63741813988066,27.0002492582776));
#17742=CARTESIAN_POINT('Ctrl Pts',(-1.14172152583069,1.63569819026981,27.0004418561164));
#17743=CARTESIAN_POINT('Ctrl Pts',(-1.14680250842919,1.63214024351572,27.0008382036692));
#17744=CARTESIAN_POINT('Ctrl Pts',(-1.14941492217656,1.63030153801773,27.0010419046971));
#17745=CARTESIAN_POINT('Ctrl Pts',(-1.15597054390786,1.62566387878496,27.0015528960393));
#17746=CARTESIAN_POINT('Ctrl Pts',(-1.15990803898893,1.62285682899108,27.0018596492554));
#17747=CARTESIAN_POINT('Ctrl Pts',(-1.1710594687979,1.61484562897684,27.0027280663771));
#17748=CARTESIAN_POINT('Ctrl Pts',(-1.17824896006961,1.60960743030116,27.0032875384669));
#17749=CARTESIAN_POINT('Ctrl Pts',(-1.25118828974313,1.55571390605083,27.0089620474535));
#17750=CARTESIAN_POINT('Ctrl Pts',(-1.31392972634342,1.50310007948615,27.0138322171744));
#17751=CARTESIAN_POINT('Ctrl Pts',(-1.45250522768332,1.37156519692618,27.0250263347644));
#17752=CARTESIAN_POINT('Ctrl Pts',(-1.52542867529026,1.28997301021428,27.0312780848205));
#17753=CARTESIAN_POINT('Ctrl Pts',(-1.65036240995438,1.12468827804653,27.0434563626732));
#17754=CARTESIAN_POINT('Ctrl Pts',(-1.7035774775518,1.0423241588984,27.0493321343861));
#17755=CARTESIAN_POINT('Ctrl Pts',(-1.75662703441401,0.945225351725706,
27.0562402803651));
#17756=CARTESIAN_POINT('Ctrl Pts',(-1.76262126908009,0.93399986799092,27.0570384941142));
#17757=CARTESIAN_POINT('Ctrl Pts',(-1.77137099424231,0.917229895786987,
27.0582306534771));
#17758=CARTESIAN_POINT('Ctrl Pts',(-1.77420882270258,0.911728541293544,
27.0586216895752));
#17759=CARTESIAN_POINT('Ctrl Pts',(-1.77921882373372,0.901904288128219,
27.0593199493309));
#17760=CARTESIAN_POINT('Ctrl Pts',(-1.78140097253769,0.897586509501173,
27.0596268194676));
#17761=CARTESIAN_POINT('Ctrl Pts',(-1.78596587102549,0.888471810392974,
27.0602745991854));
#17762=CARTESIAN_POINT('Ctrl Pts',(-1.78834504743077,0.883673152663318,
27.0606156307748));
#17763=CARTESIAN_POINT('Ctrl Pts',(-1.79458102689322,0.870967221096795,
27.0615186288622));
#17764=CARTESIAN_POINT('Ctrl Pts',(-1.79840486034249,0.863043982942444,
27.0620817376635));
#17765=CARTESIAN_POINT('Ctrl Pts',(-1.81570537622565,0.826581897798144,
27.0646733929321));
#17766=CARTESIAN_POINT('Ctrl Pts',(-1.82855533660106,0.797752366493689,
27.0667234136914));
#17767=CARTESIAN_POINT('Ctrl Pts',(-1.86131944681613,0.719289011886853,
27.0723088058111));
#17768=CARTESIAN_POINT('Ctrl Pts',(-1.8799294563882,0.669142103562591,27.075885419658));
#17769=CARTESIAN_POINT('Ctrl Pts',(-1.96163191599517,0.418542261647544,
27.0937817462154));
#17770=CARTESIAN_POINT('Ctrl Pts',(-1.99477977691127,0.209778699509114,
27.1089346316281));
#17771=CARTESIAN_POINT('Ctrl Pts',(-1.99474997993175,-0.000282952760035267,
27.122784593986));
#17772=CARTESIAN_POINT('',(-1.99423734260986,0.00182902437498021,27.9209545793481));
#17773=CARTESIAN_POINT('Ctrl Pts',(-1.99793803718199,-0.000404756772601905,
27.1209548813952));
#17774=CARTESIAN_POINT('Ctrl Pts',(-1.997998332643,-0.0221817108798109,
27.1223511044342));
#17775=CARTESIAN_POINT('Ctrl Pts',(-1.98780192015059,-0.704986784517505,
27.1661326599454));
#17776=CARTESIAN_POINT('Ctrl Pts',(-1.21104617766535,-2.02391951718273,
27.2522995479288));
#17777=CARTESIAN_POINT('Ctrl Pts',(1.04595081287402,-2.11397018747171,27.3794555453455));
#17778=CARTESIAN_POINT('Ctrl Pts',(2.34362649946087,-0.265137487911111,
27.5066115427623));
#17779=CARTESIAN_POINT('Ctrl Pts',(1.49178348806736,1.82687303368368,27.633767540179));
#17780=CARTESIAN_POINT('Ctrl Pts',(-0.728287993893816,2.24331889271703,
27.7609235375957));
#17781=CARTESIAN_POINT('Ctrl Pts',(-1.89678409583614,1.00784192457324,27.8566525506522));
#17782=CARTESIAN_POINT('Ctrl Pts',(-1.9957770503294,0.173571652796369,27.9099962312363));
#17783=CARTESIAN_POINT('Ctrl Pts',(-1.99423734260986,0.00182902437498021,
27.9209545793481));
#17784=CARTESIAN_POINT('',(-1.99474936733483,-0.00158871561299351,29.5209548813952));
#17785=CARTESIAN_POINT('Ctrl Pts',(-1.99474918095302,0.00180764687956112,
27.9206602738335));
#17786=CARTESIAN_POINT('Ctrl Pts',(-1.9948488587779,-0.108187431123657,
27.9270492254735));
#17787=CARTESIAN_POINT('Ctrl Pts',(-1.98585070424739,-0.217993836220585,
27.9334945456375));
#17788=CARTESIAN_POINT('Ctrl Pts',(-1.96280274044711,-0.356908002681124,
27.9421072468327));
#17789=CARTESIAN_POINT('Ctrl Pts',(-1.9570528110152,-0.387197695487376,
27.9440126623984));
#17790=CARTESIAN_POINT('Ctrl Pts',(-1.94891803625653,-0.425218712387804,
27.9464440727496));
#17791=CARTESIAN_POINT('Ctrl Pts',(-1.94718482462179,-0.433086274475436,
27.9469493474341));
#17792=CARTESIAN_POINT('Ctrl Pts',(-1.94419251863576,-0.446288079912747,
27.9478009135796));
#17793=CARTESIAN_POINT('Ctrl Pts',(-1.94295900246288,-0.451628069954507,
27.9481463870098));
#17794=CARTESIAN_POINT('Ctrl Pts',(-1.94048310403884,-0.462148532350955,
27.9488290667236));
#17795=CARTESIAN_POINT('Ctrl Pts',(-1.93924194380808,-0.467329247417154,
27.9491662313082));
#17796=CARTESIAN_POINT('Ctrl Pts',(-1.93683248032129,-0.477211668323058,
27.9498112941003));
#17797=CARTESIAN_POINT('Ctrl Pts',(-1.93566777079769,-0.481914218119599,
27.9501190743796));
#17798=CARTESIAN_POINT('Ctrl Pts',(-1.93296257107925,-0.492668507097055,
27.9508248557851));
#17799=CARTESIAN_POINT('Ctrl Pts',(-1.93141077643851,-0.498717325014549,
27.9512232197657));
#17800=CARTESIAN_POINT('Ctrl Pts',(-1.92654017102483,-0.517338982165583,
27.9524539630782));
#17801=CARTESIAN_POINT('Ctrl Pts',(-1.92312685526473,-0.529886533407515,
27.9532893933809));
#17802=CARTESIAN_POINT('Ctrl Pts',(-1.88442469594449,-0.666856263853798,
27.962477870555));
#17803=CARTESIAN_POINT('Ctrl Pts',(-1.83724525305854,-0.787573412683344,
27.9712312103594));
#17804=CARTESIAN_POINT('Ctrl Pts',(-1.74804307272968,-0.963311674636439,
27.9848971552858));
#17805=CARTESIAN_POINT('Ctrl Pts',(-1.71429530269545,-1.02216208096058,
27.9896414887885));
#17806=CARTESIAN_POINT('Ctrl Pts',(-1.63197275561775,-1.15013510460071,
28.0002342633297));
#17807=CARTESIAN_POINT('Ctrl Pts',(-1.58186718386549,-1.21813173898929,
28.0060598161889));
#17808=CARTESIAN_POINT('Ctrl Pts',(-1.51535754053711,-1.29733633466164,
28.012922383088));
#17809=CARTESIAN_POINT('Ctrl Pts',(-1.50290561404906,-1.31174114134049,
28.0141736481886));
#17810=CARTESIAN_POINT('Ctrl Pts',(-1.48686705141871,-1.32976682757914,
28.0157410995416));
#17811=CARTESIAN_POINT('Ctrl Pts',(-1.48347072918528,-1.33355466380578,
28.0160705710444));
#17812=CARTESIAN_POINT('Ctrl Pts',(-1.47803327046113,-1.33957245116844,
28.0165940985729));
#17813=CARTESIAN_POINT('Ctrl Pts',(-1.47600152080552,-1.34181079567804,
28.016788847474));
#17814=CARTESIAN_POINT('Ctrl Pts',(-1.47213897557386,-1.34604670832224,
28.0171574201381));
#17815=CARTESIAN_POINT('Ctrl Pts',(-1.47030922084485,-1.34804514003558,
28.0173313146525));
#17816=CARTESIAN_POINT('Ctrl Pts',(-1.46610954310895,-1.35261324460278,
28.0177288406101));
#17817=CARTESIAN_POINT('Ctrl Pts',(-1.46373693623552,-1.35518041744453,
28.0179522645005));
#17818=CARTESIAN_POINT('Ctrl Pts',(-1.45623345015291,-1.36325653303465,
28.0186552618542));
#17819=CARTESIAN_POINT('Ctrl Pts',(-1.45107805077573,-1.36874275563258,
28.0191330010981));
#17820=CARTESIAN_POINT('Ctrl Pts',(-1.36038545806823,-1.46416677106235,
28.0274485389371));
#17821=CARTESIAN_POINT('Ctrl Pts',(-1.26665378726315,-1.54597262294863,
28.0346804661315));
#17822=CARTESIAN_POINT('Ctrl Pts',(-1.0827549897518,-1.67844336836413,28.0478359617263));
#17823=CARTESIAN_POINT('Ctrl Pts',(-0.995108985266902,-1.73184504700242,
28.0537487871243));
#17824=CARTESIAN_POINT('Ctrl Pts',(-0.860785713910868,-1.80011069958239,
28.0627261743796));
#17825=CARTESIAN_POINT('Ctrl Pts',(-0.817043979552869,-1.8203816075785,
28.0656357674478));
#17826=CARTESIAN_POINT('Ctrl Pts',(-0.745720868464329,-1.85034558920585,
28.0703894867717));
#17827=CARTESIAN_POINT('Ctrl Pts',(-0.718584957935787,-1.86105183518369,
28.0722001092982));
#17828=CARTESIAN_POINT('Ctrl Pts',(-0.68325472321027,-1.87410318339886,
28.0745640509535));
#17829=CARTESIAN_POINT('Ctrl Pts',(-0.675265701005148,-1.87699653389703,
28.0750990168539));
#17830=CARTESIAN_POINT('Ctrl Pts',(-0.662223200767148,-1.88162603722634,
28.0759731616288));
#17831=CARTESIAN_POINT('Ctrl Pts',(-0.657180745557097,-1.88339310245237,
28.0763113109999));
#17832=CARTESIAN_POINT('Ctrl Pts',(-0.647556457609245,-1.88672245716853,
28.0769571081101));
#17833=CARTESIAN_POINT('Ctrl Pts',(-0.642975911679219,-1.88828837111734,
28.0772646330781));
#17834=CARTESIAN_POINT('Ctrl Pts',(-0.632502220472329,-1.89182639846025,
28.0779682095009));
#17835=CARTESIAN_POINT('Ctrl Pts',(-0.62660549108438,-1.89378766970104,
28.0783646157899));
#17836=CARTESIAN_POINT('Ctrl Pts',(-0.608489224189546,-1.89971932330413,
28.0795834222711));
#17837=CARTESIAN_POINT('Ctrl Pts',(-0.59624060283813,-1.90359916315779,
28.0804087883287));
#17838=CARTESIAN_POINT('Ctrl Pts',(-0.48345272111354,-1.93813019163594,
28.0880222251436));
#17839=CARTESIAN_POINT('Ctrl Pts',(-0.380692221166983,-1.96090339362935,
28.0950689128245));
#17840=CARTESIAN_POINT('Ctrl Pts',(-0.100033376169267,-2.00020475838216,
28.114555936729));
#17841=CARTESIAN_POINT('Ctrl Pts',(0.0790748157565712,-2.0011427882299,
28.1273016039473));
#17842=CARTESIAN_POINT('Ctrl Pts',(0.272842792996786,-1.97607579201594,
28.1402460280279));
#17843=CARTESIAN_POINT('Ctrl Pts',(0.289737189206642,-1.97366945921006,
28.1413667161402));
#17844=CARTESIAN_POINT('Ctrl Pts',(0.311873338906946,-1.97022614729791,
28.1428228900185));
#17845=CARTESIAN_POINT('Ctrl Pts',(0.31714413784571,-1.96938458621994,28.1431687038633));
#17846=CARTESIAN_POINT('Ctrl Pts',(0.325449628297174,-1.96802428321856,
28.1437121134531));
#17847=CARTESIAN_POINT('Ctrl Pts',(0.328486557322551,-1.9675196623847,28.1439104944396));
#17848=CARTESIAN_POINT('Ctrl Pts',(0.334183327919764,-1.96655952055514,
28.1442820105553));
#17849=CARTESIAN_POINT('Ctrl Pts',(0.336843382502719,-1.96610563813862,
28.1444552334097));
#17850=CARTESIAN_POINT('Ctrl Pts',(0.342911938531253,-1.96505748912088,
28.1448498488545));
#17851=CARTESIAN_POINT('Ctrl Pts',(0.346319813258752,-1.9644597528389,28.145071041712));
#17852=CARTESIAN_POINT('Ctrl Pts',(0.356765585649676,-1.96259955278517,
28.1457478338592));
#17853=CARTESIAN_POINT('Ctrl Pts',(0.36379836145671,-1.96130809502991,28.1462018152134));
#17854=CARTESIAN_POINT('Ctrl Pts',(0.419956561957444,-1.95068307309188,
28.1498146181818));
#17855=CARTESIAN_POINT('Ctrl Pts',(0.468726922964491,-1.93954221601898,
28.1528767133679));
#17856=CARTESIAN_POINT('Ctrl Pts',(0.536098762612736,-1.92146179429727,
28.1570657349328));
#17857=CARTESIAN_POINT('Ctrl Pts',(0.555089568336457,-1.91606182574416,
28.1582418990978));
#17858=CARTESIAN_POINT('Ctrl Pts',(0.728676409687609,-1.86390550983009,
28.1689753750146));
#17859=CARTESIAN_POINT('Ctrl Pts',(0.877138124724071,-1.79881777428652,
28.178080382989));
#17860=CARTESIAN_POINT('Ctrl Pts',(1.05538048424197,-1.69330442618159,28.190449385624));
#17861=CARTESIAN_POINT('Ctrl Pts',(1.09381852538397,-1.66873258359326,28.1932080947884));
#17862=CARTESIAN_POINT('Ctrl Pts',(1.15444640877626,-1.62698049305864,28.1977360210615));
#17863=CARTESIAN_POINT('Ctrl Pts',(1.1771759258225,-1.61061129777603,28.199475686612));
#17864=CARTESIAN_POINT('Ctrl Pts',(1.20617196199933,-1.5887873996286,28.2017539001802));
#17865=CARTESIAN_POINT('Ctrl Pts',(1.21276031457067,-1.58376406677148,28.2022755826487));
#17866=CARTESIAN_POINT('Ctrl Pts',(1.22353879826998,-1.57543924864277,28.2031358104581));
#17867=CARTESIAN_POINT('Ctrl Pts',(1.22774736325156,-1.57216170547532,28.2034734077741));
#17868=CARTESIAN_POINT('Ctrl Pts',(1.23575166575061,-1.5658763799264,28.2041187911353));
#17869=CARTESIAN_POINT('Ctrl Pts',(1.23954970052589,-1.5628715736948,28.2044264571183));
#17870=CARTESIAN_POINT('Ctrl Pts',(1.24820944106847,-1.5559690171367,28.2051312594031));
#17871=CARTESIAN_POINT('Ctrl Pts',(1.25306388184865,-1.55206227246578,28.2055287550005));
#17872=CARTESIAN_POINT('Ctrl Pts',(1.26793844878344,-1.53997628400777,28.2067541952492));
#17873=CARTESIAN_POINT('Ctrl Pts',(1.27789723030394,-1.53172240333836,28.2075851529109));
#17874=CARTESIAN_POINT('Ctrl Pts',(1.37287002259834,-1.4514376536507,28.2156127728789));
#17875=CARTESIAN_POINT('Ctrl Pts',(1.45177324786449,-1.37251234376398,28.2231016668819));
#17876=CARTESIAN_POINT('Ctrl Pts',(1.62898361928755,-1.16278435095738,28.2420294174698));
#17877=CARTESIAN_POINT('Ctrl Pts',(1.71860637284411,-1.02569372192877,28.2536460575304));
#17878=CARTESIAN_POINT('Ctrl Pts',(1.80169253844813,-0.85648865762175,28.2662394804382));
#17879=CARTESIAN_POINT('Ctrl Pts',(1.81242093894593,-0.833546227255345,
28.2679115426011));
#17880=CARTESIAN_POINT('Ctrl Pts',(1.82496317330089,-0.805337030873813,
28.2699191567834));
#17881=CARTESIAN_POINT('Ctrl Pts',(1.82719510511738,-0.800260186951465,
28.2702785854422));
#17882=CARTESIAN_POINT('Ctrl Pts',(1.8306513900512,-0.792308533959701,28.2708385281359));
#17883=CARTESIAN_POINT('Ctrl Pts',(1.83189018888251,-0.78944009341247,28.2710399079798));
#17884=CARTESIAN_POINT('Ctrl Pts',(1.83418396613771,-0.784094376031744,
28.2714140530573));
#17885=CARTESIAN_POINT('Ctrl Pts',(1.8352406577118,-0.781617899346844,28.2715869196527));
#17886=CARTESIAN_POINT('Ctrl Pts',(1.83761743222252,-0.77601626537026,28.2719768983158));
#17887=CARTESIAN_POINT('Ctrl Pts',(1.83893455534687,-0.772889884068806,
28.2721938287564));
#17888=CARTESIAN_POINT('Ctrl Pts',(1.84278904494335,-0.763675065119153,
28.2728311312038));
#17889=CARTESIAN_POINT('Ctrl Pts',(1.84530422713305,-0.7575773105841,28.2732501791638));
#17890=CARTESIAN_POINT('Ctrl Pts',(1.86229067836662,-0.715809173467616,
28.2761030371072));
#17891=CARTESIAN_POINT('Ctrl Pts',(1.87575816200899,-0.679736076481537,
28.2784798387642));
#17892=CARTESIAN_POINT('Ctrl Pts',(1.89084255242143,-0.635460831147216,
28.2813184266714));
#17893=CARTESIAN_POINT('Ctrl Pts',(1.89346222303099,-0.627612013538339,
28.2818186713254));
#17894=CARTESIAN_POINT('Ctrl Pts',(1.91942574578575,-0.548180092639143,
28.2868535298067));
#17895=CARTESIAN_POINT('Ctrl Pts',(1.93874935254281,-0.475341032032919,
28.2912452195888));
#17896=CARTESIAN_POINT('Ctrl Pts',(1.97421614778847,-0.302775202752894,
28.3014757249079));
#17897=CARTESIAN_POINT('Ctrl Pts',(1.98699887005701,-0.202574944284822,
28.307289862144));
#17898=CARTESIAN_POINT('Ctrl Pts',(1.99477475220788,-0.0504702691893337,
28.3163398191186));
#17899=CARTESIAN_POINT('Ctrl Pts',(1.99541273629413,0.000980898739392213,
28.319437753608));
#17900=CARTESIAN_POINT('Ctrl Pts',(1.99325562074871,0.0830746017359388,
28.3244779275436));
#17901=CARTESIAN_POINT('Ctrl Pts',(1.99174169969109,0.1137286266368,28.3263814704997));
#17902=CARTESIAN_POINT('Ctrl Pts',(1.98889097181835,0.153023406443363,28.3288539138327));
#17903=CARTESIAN_POINT('Ctrl Pts',(1.988203691165,0.161708191687293,28.329402389689));
#17904=CARTESIAN_POINT('Ctrl Pts',(1.98700367172813,0.175705591025923,28.3302897513201));
#17905=CARTESIAN_POINT('Ctrl Pts',(1.98652645835821,0.18102120184792,28.3306275188579));
#17906=CARTESIAN_POINT('Ctrl Pts',(1.98557559174698,0.191155904136875,28.3312730292296));
#17907=CARTESIAN_POINT('Ctrl Pts',(1.98510571109182,0.195975318188174,28.3315806511644));
#17908=CARTESIAN_POINT('Ctrl Pts',(1.98399157535436,0.206987329738948,28.3322850727164));
#17909=CARTESIAN_POINT('Ctrl Pts',(1.98333586890655,0.213178693600943,28.3326822302442));
#17910=CARTESIAN_POINT('Ctrl Pts',(1.98123169889738,0.232196314470544,28.3339056094976));
#17911=CARTESIAN_POINT('Ctrl Pts',(1.97968773895219,0.245011461753481,28.3347348295458));
#17912=CARTESIAN_POINT('Ctrl Pts',(1.96007379363193,0.395497073248164,28.3445307409932));
#17913=CARTESIAN_POINT('Ctrl Pts',(1.92780509994746,0.530905244818358,28.3539633486042));
#17914=CARTESIAN_POINT('Ctrl Pts',(1.85006895750508,0.751924979456092,28.3702475278558));
#17915=CARTESIAN_POINT('Ctrl Pts',(1.81195759263666,0.839616850551108,28.3769543942392));
#17916=CARTESIAN_POINT('Ctrl Pts',(1.7476381706149,0.962634550685788,28.3864960103221));
#17917=CARTESIAN_POINT('Ctrl Pts',(1.72631807205538,1.00036538123331,28.3894407175468));
#17918=CARTESIAN_POINT('Ctrl Pts',(1.69204864893731,1.05664951501344,28.3938302446829));
#17919=CARTESIAN_POINT('Ctrl Pts',(1.67998579527088,1.07572518001221,28.395317305614));
#17920=CARTESIAN_POINT('Ctrl Pts',(1.66466682059457,1.09906348074963,28.3971319636515));
#17921=CARTESIAN_POINT('Ctrl Pts',(1.6617144412548,1.10352221347523,28.397478433907));
#17922=CARTESIAN_POINT('Ctrl Pts',(1.6570329396053,1.11053090486523,28.3980226413182));
#17923=CARTESIAN_POINT('Ctrl Pts',(1.65531580609073,1.11308878173306,28.3982211675244));
#17924=CARTESIAN_POINT('Ctrl Pts',(1.65208367773634,1.11787940512931,28.3985928071755));
#17925=CARTESIAN_POINT('Ctrl Pts',(1.65057009619025,1.1201130301579,28.3987660090131));
#17926=CARTESIAN_POINT('Ctrl Pts',(1.64710722883944,1.12520099795319,28.3991603826025));
#17927=CARTESIAN_POINT('Ctrl Pts',(1.64515505739347,1.12805334389094,28.3993813555543));
#17928=CARTESIAN_POINT('Ctrl Pts',(1.63915172603117,1.1367761676498,28.4000568118091));
#17929=CARTESIAN_POINT('Ctrl Pts',(1.63507643004821,1.14263008357578,28.4005096864588));
#17930=CARTESIAN_POINT('Ctrl Pts',(1.60246143774226,1.18894773292987,28.404090633603));
#17931=CARTESIAN_POINT('Ctrl Pts',(1.57245273435331,1.22836180101792,28.4071238766074));
#17932=CARTESIAN_POINT('Ctrl Pts',(1.52751188910998,1.28303802050906,28.4113758953845));
#17933=CARTESIAN_POINT('Ctrl Pts',(1.51375665571716,1.2992382263748,28.4126415931688));
#17934=CARTESIAN_POINT('Ctrl Pts',(1.46585609938205,1.35385937919311,28.4169411445562));
#17935=CARTESIAN_POINT('Ctrl Pts',(1.43048526794351,1.39117992386851,28.4199348891131));
#17936=CARTESIAN_POINT('Ctrl Pts',(1.32175213313475,1.49736959089023,28.4287596645015));
#17937=CARTESIAN_POINT('Ctrl Pts',(1.24458219000189,1.56210064787829,28.4345587782487));
#17938=CARTESIAN_POINT('Ctrl Pts',(1.12136227061537,1.65050999415747,28.4435728786602));
#17939=CARTESIAN_POINT('Ctrl Pts',(1.07873527500381,1.67867989518207,28.4466498935754));
#17940=CARTESIAN_POINT('Ctrl Pts',(1.00897644832623,1.72102478567767,28.4516589950286));
#17941=CARTESIAN_POINT('Ctrl Pts',(0.982517221822658,1.73626597533137,28.4535529969281));
#17942=CARTESIAN_POINT('Ctrl Pts',(0.948086501498887,1.75505987768894,28.4560147039504));
#17943=CARTESIAN_POINT('Ctrl Pts',(0.940426228301183,1.75917642488258,28.4565622050836));
#17944=CARTESIAN_POINT('Ctrl Pts',(0.928024848082484,1.76573664242315,28.4574483696088));
#17945=CARTESIAN_POINT('Ctrl Pts',(0.923300371903209,1.76821164779454,28.4577859202893));
#17946=CARTESIAN_POINT('Ctrl Pts',(0.914266994254903,1.77289787680985,28.4584312689427));
#17947=CARTESIAN_POINT('Ctrl Pts',(0.90995984838636,1.77511241672905,28.4587389470827));
#17948=CARTESIAN_POINT('Ctrl Pts',(0.900091411353814,1.78014096639524,28.4594438541086));
#17949=CARTESIAN_POINT('Ctrl Pts',(0.894524932225519,1.78294462987522,28.4598414426709));
#17950=CARTESIAN_POINT('Ctrl Pts',(0.877359703756071,1.79148960536398,28.4610674500144));
#17951=CARTESIAN_POINT('Ctrl Pts',(0.86571833009461,1.79714407205301,28.4618988858538));
#17952=CARTESIAN_POINT('Ctrl Pts',(0.752116882131041,1.85096282619706,28.4700133791482));
#17953=CARTESIAN_POINT('Ctrl Pts',(0.646319007684455,1.8905044296857,28.4775960849527));
#17954=CARTESIAN_POINT('Ctrl Pts',(0.381651232324477,1.96459952588244,28.4965521000674));
#17955=CARTESIAN_POINT('Ctrl Pts',(0.220796412546314,1.98911000588865,28.5080893573319));
#17956=CARTESIAN_POINT('Ctrl Pts',(0.0336924542626241,1.99462296304493,
28.5205913915823));
#17957=CARTESIAN_POINT('Ctrl Pts',(0.00862257998748717,1.99488890472777,
28.5222462745928));
#17958=CARTESIAN_POINT('Ctrl Pts',(-0.0219751936630706,1.99463661249876,
28.5242360629406));
#17959=CARTESIAN_POINT('Ctrl Pts',(-0.0275032138512781,1.99456804848868,
28.5245943569389));
#17960=CARTESIAN_POINT('Ctrl Pts',(-0.0361511979486837,1.99442482735281,
28.5251529230146));
#17961=CARTESIAN_POINT('Ctrl Pts',(-0.0392713397609173,1.99436582985066,
28.5253540540604));
#17962=CARTESIAN_POINT('Ctrl Pts',(-0.0450836736811598,1.99424228134761,
28.5257279751567));
#17963=CARTESIAN_POINT('Ctrl Pts',(-0.0477758455136173,1.99417960150707,
28.5259008654485));
#17964=CARTESIAN_POINT('Ctrl Pts',(-0.0538645722213104,1.99402550507804,
28.526291201874));
#17965=CARTESIAN_POINT('Ctrl Pts',(-0.0572610162880835,1.99393086226059,
28.5265084649647));
#17966=CARTESIAN_POINT('Ctrl Pts',(-0.0672745137298622,1.99362622656238,
28.5271476455265));
#17967=CARTESIAN_POINT('Ctrl Pts',(-0.0738908635736979,1.99339196714712,
28.5275682272445));
#17968=CARTESIAN_POINT('Ctrl Pts',(-0.119437105290997,1.99155226927821,
28.5304521519316));
#17969=CARTESIAN_POINT('Ctrl Pts',(-0.158316924483955,1.9888393357482,28.5328570723449));
#17970=CARTESIAN_POINT('Ctrl Pts',(-0.205613072318936,1.98414316379529,
28.5357401070166));
#17971=CARTESIAN_POINT('Ctrl Pts',(-0.214125411102993,1.9832425828003,28.5362573075835));
#17972=CARTESIAN_POINT('Ctrl Pts',(-0.296658556264859,1.97397323843552,
28.54125779541));
#17973=CARTESIAN_POINT('Ctrl Pts',(-0.37016661640658,1.96151849363895,28.545602647005));
#17974=CARTESIAN_POINT('Ctrl Pts',(-0.54116471114962,1.92258768611686,28.5557867603395));
#17975=CARTESIAN_POINT('Ctrl Pts',(-0.637677343617685,1.8927675919447,28.5616010101356));
#17976=CARTESIAN_POINT('Ctrl Pts',(-0.779374357505934,1.83691302177656,
28.5706512359994));
#17977=CARTESIAN_POINT('Ctrl Pts',(-0.82648162855732,1.81620520495156,28.5737493275081));
#17978=CARTESIAN_POINT('Ctrl Pts',(-0.900330158003393,1.78027386590774,
28.578789734592));
#17979=CARTESIAN_POINT('Ctrl Pts',(-0.927612022138495,1.76621210705733,
28.5806933490642));
#17980=CARTESIAN_POINT('Ctrl Pts',(-0.962207341533233,1.74735814721426,
28.5831658728592));
#17981=CARTESIAN_POINT('Ctrl Pts',(-0.969829645405149,1.74313909879577,
28.5837143560037));
#17982=CARTESIAN_POINT('Ctrl Pts',(-0.982076390068085,1.7362551686107,28.5846017265861));
#17983=CARTESIAN_POINT('Ctrl Pts',(-0.986718258210205,1.73362139017375,
28.5849394957454));
#17984=CARTESIAN_POINT('Ctrl Pts',(-0.995551411923868,1.72856252313407,
28.5855850073296));
#17985=CARTESIAN_POINT('Ctrl Pts',(-0.999744552194042,1.7261407358168,28.5858926288472));
#17986=CARTESIAN_POINT('Ctrl Pts',(-1.00930878390367,1.72057028448836,28.5865970467841));
#17987=CARTESIAN_POINT('Ctrl Pts',(-1.01467401450222,1.71741170601885,28.5869942011008));
#17988=CARTESIAN_POINT('Ctrl Pts',(-1.03111665556537,1.70762777244415,28.5882175607874));
#17989=CARTESIAN_POINT('Ctrl Pts',(-1.04214444286321,1.70092007860325,28.5890467643408));
#17990=CARTESIAN_POINT('Ctrl Pts',(-1.17103221474944,1.6207996448405,28.5988428251249));
#17991=CARTESIAN_POINT('Ctrl Pts',(-1.28095765868645,1.53539606730419,28.6082756176316));
#17992=CARTESIAN_POINT('Ctrl Pts',(-1.4504619328874,1.37274409901416,28.6246034630679));
#17993=CARTESIAN_POINT('Ctrl Pts',(-1.51491446163045,1.30126893012597,28.6313547668556));
#17994=CARTESIAN_POINT('Ctrl Pts',(-1.61243254779729,1.17601450054307,28.6422622615272));
#17995=CARTESIAN_POINT('Ctrl Pts',(-1.64855816363113,1.12481402539167,28.6464949243507));
#17996=CARTESIAN_POINT('Ctrl Pts',(-1.68593207919727,1.06616525152659,28.6510299329688));
#17997=CARTESIAN_POINT('Ctrl Pts',(-1.68961565521088,1.06031799961346,28.6514787299775));
#17998=CARTESIAN_POINT('Ctrl Pts',(-1.69507253972901,1.05155517700529,28.6521461938519));
#17999=CARTESIAN_POINT('Ctrl Pts',(-1.69686882686442,1.04865408504055,28.6523663381321));
#18000=CARTESIAN_POINT('Ctrl Pts',(-1.69993623789927,1.04367154675,28.6527429858973));
#18001=CARTESIAN_POINT('Ctrl Pts',(-1.70121099411477,1.04159236948486,28.6528997283202));
#18002=CARTESIAN_POINT('Ctrl Pts',(-1.70385668843163,1.03725932482433,28.6532254843586));
#18003=CARTESIAN_POINT('Ctrl Pts',(-1.70522696424618,1.03500508320219,28.6533944545134));
#18004=CARTESIAN_POINT('Ctrl Pts',(-1.70901131811047,1.02875152449604,28.6538618280001));
#18005=CARTESIAN_POINT('Ctrl Pts',(-1.71141584531744,1.02474640279759,28.6541596091982));
#18006=CARTESIAN_POINT('Ctrl Pts',(-1.7208899483535,1.00883942184153,28.6553363152862));
#18007=CARTESIAN_POINT('Ctrl Pts',(-1.72784982559635,0.996872208043418,
28.656208360038));
#18008=CARTESIAN_POINT('Ctrl Pts',(-1.80206153953116,0.866155714711338,
28.6656017863877));
#18009=CARTESIAN_POINT('Ctrl Pts',(-1.85709241189678,0.740858143128636,
28.6734488105635));
#18010=CARTESIAN_POINT('Ctrl Pts',(-1.94471316947856,0.468503516428646,
28.6900445652401));
#18011=CARTESIAN_POINT('Ctrl Pts',(-1.97435651117497,0.321422753812011,
28.6987770975993));
#18012=CARTESIAN_POINT('Ctrl Pts',(-1.98849629030544,0.158450929540045,
28.7089755260542));
#18013=CARTESIAN_POINT('Ctrl Pts',(-1.98956099339607,0.14446878984764,28.7098542040393));
#18014=CARTESIAN_POINT('Ctrl Pts',(-1.99089936413085,0.124051394489923,
28.7111431302214));
#18015=CARTESIAN_POINT('Ctrl Pts',(-1.99128943734173,0.117623984478175,
28.7115497275067));
#18016=CARTESIAN_POINT('Ctrl Pts',(-1.99191996600305,0.106330374348276,
28.7122656839352));
#18017=CARTESIAN_POINT('Ctrl Pts',(-1.99217372820879,0.101464946733168,
28.7125746233066));
#18018=CARTESIAN_POINT('Ctrl Pts',(-1.99263245246311,0.092003464455076,
28.7131763823591));
#18019=CARTESIAN_POINT('Ctrl Pts',(-1.99283934402496,0.0874075305839507,
28.7134691395138));
#18020=CARTESIAN_POINT('Ctrl Pts',(-1.99334947385015,0.0751301183457592,
28.7142524272093));
#18021=CARTESIAN_POINT('Ctrl Pts',(-1.99362420707482,0.0674475930284423,
28.7147438478344));
#18022=CARTESIAN_POINT('Ctrl Pts',(-1.9944580660606,0.039628166695913,28.7165281078017));
#18023=CARTESIAN_POINT('Ctrl Pts',(-1.99475653782484,0.0194852291280238,
28.7178290653352));
#18024=CARTESIAN_POINT('Ctrl Pts',(-1.99471414962915,-0.108981530156663,
28.726186735529));
#18025=CARTESIAN_POINT('Ctrl Pts',(-1.98585510854521,-0.217104110198715,
28.7335099860569));
#18026=CARTESIAN_POINT('Ctrl Pts',(-1.95017202380689,-0.433903165838728,
28.7486975897034));
#18027=CARTESIAN_POINT('Ctrl Pts',(-1.92289666575832,-0.54213527506093,
28.7565445088277));
#18028=CARTESIAN_POINT('Ctrl Pts',(-1.88156110723056,-0.662577316698417,
28.7653130744021));
#18029=CARTESIAN_POINT('Ctrl Pts',(-1.87621425332714,-0.677569920442628,
28.7664049622123));
#18030=CARTESIAN_POINT('Ctrl Pts',(-1.85310804433251,-0.739988247359653,
28.7709483466015));
#18031=CARTESIAN_POINT('Ctrl Pts',(-1.83372374141393,-0.786797486294951,
28.7743499537053));
#18032=CARTESIAN_POINT('Ctrl Pts',(-1.80958200636124,-0.839340202702134,
28.7781224611971));
#18033=CARTESIAN_POINT('Ctrl Pts',(-1.80655206119685,-0.845841987371237,
28.7785884576203));
#18034=CARTESIAN_POINT('Ctrl Pts',(-1.80200678919792,-0.855459581685445,
28.7792763908909));
#18035=CARTESIAN_POINT('Ctrl Pts',(-1.80051835286999,-0.858587925396768,
28.7794999394336));
#18036=CARTESIAN_POINT('Ctrl Pts',(-1.79785583679301,-0.864146536755718,
28.7798967440929));
#18037=CARTESIAN_POINT('Ctrl Pts',(-1.79668497023471,-0.866578308597457,
28.7800701969766));
#18038=CARTESIAN_POINT('Ctrl Pts',(-1.79416923394782,-0.871776222614569,
28.7804406471021));
#18039=CARTESIAN_POINT('Ctrl Pts',(-1.79282290566948,-0.874541623698549,
28.7806375513462));
#18040=CARTESIAN_POINT('Ctrl Pts',(-1.78912837884946,-0.882085913014618,
28.7811742549826));
#18041=CARTESIAN_POINT('Ctrl Pts',(-1.78676741226213,-0.88685857383781,
28.7815132667839));
#18042=CARTESIAN_POINT('Ctrl Pts',(-1.77443295389376,-0.911543312931353,
28.7832642839135));
#18043=CARTESIAN_POINT('Ctrl Pts',(-1.76414514815424,-0.931297759400841,
28.7846574881144));
#18044=CARTESIAN_POINT('Ctrl Pts',(-1.73327129156678,-0.988232768113368,
28.788661286012));
#18045=CARTESIAN_POINT('Ctrl Pts',(-1.71182445327314,-1.02493459135154,
28.7912276651434));
#18046=CARTESIAN_POINT('Ctrl Pts',(-1.6667314124389,-1.09673233812433,28.7962749160996));
#18047=CARTESIAN_POINT('Ctrl Pts',(-1.64310909123347,-1.13181632821076,
28.7987548732284));
#18048=CARTESIAN_POINT('Ctrl Pts',(-1.51105934730419,-1.31507967487548,
28.8119230576086));
#18049=CARTESIAN_POINT('Ctrl Pts',(-1.38369502282115,-1.44848791593372,
28.8223800174364));
#18050=CARTESIAN_POINT('Ctrl Pts',(-1.22473389858077,-1.57462014987328,
28.8349569923934));
#18051=CARTESIAN_POINT('Ctrl Pts',(-1.20940731850038,-1.58642227525399,
28.8361642133571));
#18052=CARTESIAN_POINT('Ctrl Pts',(-1.18785383824973,-1.60252550942171,
28.8378556223933));
#18053=CARTESIAN_POINT('Ctrl Pts',(-1.18177011838386,-1.60701715427708,
28.8383323573164));
#18054=CARTESIAN_POINT('Ctrl Pts',(-1.17196385512846,-1.61417137558665,
28.8390997728462));
#18055=CARTESIAN_POINT('Ctrl Pts',(-1.16825739186188,-1.61685595316363,
28.8393895986907));
#18056=CARTESIAN_POINT('Ctrl Pts',(-1.16057559543045,-1.62237964532267,
28.8399898110114));
#18057=CARTESIAN_POINT('Ctrl Pts',(-1.15659900935151,-1.62521695694302,
28.8403002642142));
#18058=CARTESIAN_POINT('Ctrl Pts',(-1.14728884903925,-1.63180832183931,
28.8410265402503));
#18059=CARTESIAN_POINT('Ctrl Pts',(-1.14194722931651,-1.63555086320754,
28.8414427999714));
#18060=CARTESIAN_POINT('Ctrl Pts',(-1.1246950284426,-1.64751269306515,28.8427858967837));
#18061=CARTESIAN_POINT('Ctrl Pts',(-1.11271354660261,-1.65562843828706,
28.8437166466276));
#18062=CARTESIAN_POINT('Ctrl Pts',(-1.08455977215657,-1.6742549545944,28.8458994631623));
#18063=CARTESIAN_POINT('Ctrl Pts',(-1.06832145412354,-1.68466280891969,
28.847155256294));
#18064=CARTESIAN_POINT('Ctrl Pts',(-1.01114414279012,-1.72015115414572,
28.8515670047184));
#18065=CARTESIAN_POINT('Ctrl Pts',(-0.969455373519259,-1.74398627378409,
28.8547664537349));
#18066=CARTESIAN_POINT('Ctrl Pts',(-0.745721542894918,-1.86140173857443,
28.8718446249199));
#18067=CARTESIAN_POINT('Ctrl Pts',(-0.550969067616661,-1.92803863518309,
28.8865600281095));
#18068=CARTESIAN_POINT('Ctrl Pts',(-0.324646806815428,-1.96831644570493,
28.9019239899371));
#18069=CARTESIAN_POINT('Ctrl Pts',(-0.299703112936946,-1.97226858489174,
28.9035921542577));
#18070=CARTESIAN_POINT('Ctrl Pts',(-0.269474391401096,-1.97647131023088,
28.9055781287364));
#18071=CARTESIAN_POINT('Ctrl Pts',(-0.264256152169708,-1.97717575732305,
28.9059196788122));
#18072=CARTESIAN_POINT('Ctrl Pts',(-0.255690802489784,-1.97829753886518,
28.9064781426427));
#18073=CARTESIAN_POINT('Ctrl Pts',(-0.2523453553774,-1.97872705565714,28.9066957257752));
#18074=CARTESIAN_POINT('Ctrl Pts',(-0.246328760360316,-1.97948401011462,
28.9070860442729));
#18075=CARTESIAN_POINT('Ctrl Pts',(-0.243658038688621,-1.97981452791526,
28.9072589512672));
#18076=CARTESIAN_POINT('Ctrl Pts',(-0.237870546319849,-1.98051887628678,
28.9076328776779));
#18077=CARTESIAN_POINT('Ctrl Pts',(-0.2347535708981,-1.98089075352932,28.9078337854563));
#18078=CARTESIAN_POINT('Ctrl Pts',(-0.226061533751702,-1.98190697096103,
28.9083927393424));
#18079=CARTESIAN_POINT('Ctrl Pts',(-0.220484556727129,-1.98253514991819,
28.9087498846769));
#18080=CARTESIAN_POINT('Ctrl Pts',(-0.188728861274787,-1.98597638753548,
28.910775397344));
#18081=CARTESIAN_POINT('Ctrl Pts',(-0.162497652783014,-1.98829461373648,
28.9124172394034));
#18082=CARTESIAN_POINT('Ctrl Pts',(-0.0818331088866023,-1.99381629885062,
28.9173912975349));
#18083=CARTESIAN_POINT('Ctrl Pts',(-0.0273052753965819,-1.99530835900851,
28.9206496380073));
#18084=CARTESIAN_POINT('Ctrl Pts',(0.20736304840412,-1.99210592287502,28.9344791456531));
#18085=CARTESIAN_POINT('Ctrl Pts',(0.38633516320598,-1.96525631504857,28.9446191812516));
#18086=CARTESIAN_POINT('Ctrl Pts',(0.600730879483488,-1.90263375907195,
28.9581839365838));
#18087=CARTESIAN_POINT('Ctrl Pts',(0.641780317589034,-1.8891824699964,28.960844073649));
#18088=CARTESIAN_POINT('Ctrl Pts',(0.691040121572739,-1.87124997485393,
28.9641268921308));
#18089=CARTESIAN_POINT('Ctrl Pts',(0.699699385512237,-1.86802935826141,
28.9647074111543));
#18090=CARTESIAN_POINT('Ctrl Pts',(0.713940085196567,-1.86261994419518,
28.9656679321634));
#18091=CARTESIAN_POINT('Ctrl Pts',(0.719534645891043,-1.86046590773675,
28.9660467700006));
#18092=CARTESIAN_POINT('Ctrl Pts',(0.729607597320129,-1.85653535595333,
28.9667315926145));
#18093=CARTESIAN_POINT('Ctrl Pts',(0.734089440017328,-1.85476776642234,
28.9670372753345));
#18094=CARTESIAN_POINT('Ctrl Pts',(0.743650898288416,-1.85095674773058,
28.96769152649));
#18095=CARTESIAN_POINT('Ctrl Pts',(0.748728582957581,-1.84890861011862,
28.9680402518389));
#18096=CARTESIAN_POINT('Ctrl Pts',(0.762439089720262,-1.84331259148635,
28.9689853660675));
#18097=CARTESIAN_POINT('Ctrl Pts',(0.771055464585957,-1.83972501779039,
28.9695830949572));
#18098=CARTESIAN_POINT('Ctrl Pts',(0.814261921305348,-1.8213784299329,28.9725996871596));
#18099=CARTESIAN_POINT('Ctrl Pts',(0.848452900643053,-1.80570463168776,
28.9750495551128));
#18100=CARTESIAN_POINT('Ctrl Pts',(1.03735806830711,-1.71255698347804,28.9889518884468));
#18101=CARTESIAN_POINT('Ctrl Pts',(1.18190057624895,-1.61618457713856,29.0010869333275));
#18102=CARTESIAN_POINT('Ctrl Pts',(1.38119475596547,-1.44212606645502,29.0194783669569));
#18103=CARTESIAN_POINT('Ctrl Pts',(1.4459937290459,-1.37714670146729,29.025775024701));
#18104=CARTESIAN_POINT('Ctrl Pts',(1.51124880282904,-1.30200471192509,29.032275921467));
#18105=CARTESIAN_POINT('Ctrl Pts',(1.5163622153359,-1.29604585211747,29.0327864665345));
#18106=CARTESIAN_POINT('Ctrl Pts',(1.52374025164694,-1.28734449703983,29.033524580157));
#18107=CARTESIAN_POINT('Ctrl Pts',(1.5260328571933,-1.28462598751368,29.0337541443793));
#18108=CARTESIAN_POINT('Ctrl Pts',(1.53006500723379,-1.27981874679317,29.0341582379606));
#18109=CARTESIAN_POINT('Ctrl Pts',(1.53180756694164,-1.27773257343879,29.0343329874514));
#18110=CARTESIAN_POINT('Ctrl Pts',(1.53545875071363,-1.27334321161228,29.0346993718054));
#18111=CARTESIAN_POINT('Ctrl Pts',(1.53736645588965,-1.27103929533922,29.0348909400539));
#18112=CARTESIAN_POINT('Ctrl Pts',(1.54241442116777,-1.2649149270363,29.0353982368048));
#18113=CARTESIAN_POINT('Ctrl Pts',(1.54554569365455,-1.2610870427348,29.0357133171453));
#18114=CARTESIAN_POINT('Ctrl Pts',(1.55994474606134,-1.24335045875706,29.0371642809629));
#18115=CARTESIAN_POINT('Ctrl Pts',(1.57103966019165,-1.22930159609517,29.0382882119811));
#18116=CARTESIAN_POINT('Ctrl Pts',(1.60092235390202,-1.19039732681759,29.0413377954715));
#18117=CARTESIAN_POINT('Ctrl Pts',(1.61931996037841,-1.1652472988396,29.0432405385104));
#18118=CARTESIAN_POINT('Ctrl Pts',(1.68182768286329,-1.0754561395538,29.0498362511993));
#18119=CARTESIAN_POINT('Ctrl Pts',(1.7227193695473,-1.00865750056799,29.0543959596488));
#18120=CARTESIAN_POINT('Ctrl Pts',(1.83580657082673,-0.796885439706245,
29.0683330555924));
#18121=CARTESIAN_POINT('Ctrl Pts',(1.89436954801904,-0.645421549219721,
29.0776562873066));
#18122=CARTESIAN_POINT('Ctrl Pts',(1.93609728797778,-0.480237901491215,
29.0881992892549));
#18123=CARTESIAN_POINT('Ctrl Pts',(1.93814460186183,-0.471907458398522,
29.0887317670717));
#18124=CARTESIAN_POINT('Ctrl Pts',(1.94358041390635,-0.449157153770234,
29.0901882930147));
#18125=CARTESIAN_POINT('Ctrl Pts',(1.94686207603639,-0.434712562798446,
29.0911156242695));
#18126=CARTESIAN_POINT('Ctrl Pts',(1.951264204639,-0.414285627306019,29.0924311177005));
#18127=CARTESIAN_POINT('Ctrl Pts',(1.95251868579219,-0.4083324106673,29.0928149929511));
#18128=CARTESIAN_POINT('Ctrl Pts',(1.9546568830613,-0.397950282866235,29.0934853411271));
#18129=CARTESIAN_POINT('Ctrl Pts',(1.95555283410524,-0.393523913640471,
29.0937714212993));
#18130=CARTESIAN_POINT('Ctrl Pts',(1.9573948691668,-0.384261847740866,29.0943706401701));
#18131=CARTESIAN_POINT('Ctrl Pts',(1.95833808154993,-0.379425617353974,
29.0946838683166));
#18132=CARTESIAN_POINT('Ctrl Pts',(1.96053461222629,-0.367936714056487,
29.0954288079074));
#18133=CARTESIAN_POINT('Ctrl Pts',(1.96177199554775,-0.361281091261387,
29.0958610237646));
#18134=CARTESIAN_POINT('Ctrl Pts',(1.96579554065173,-0.339008984680679,
29.0973096749342));
#18135=CARTESIAN_POINT('Ctrl Pts',(1.9684292379113,-0.323365908056735,29.0983309345434));
#18136=CARTESIAN_POINT('Ctrl Pts',(1.98132649765105,-0.2407547901593,29.1037453602466));
#18137=CARTESIAN_POINT('Ctrl Pts',(1.98835883985264,-0.17333461019308,29.1082394640348));
#18138=CARTESIAN_POINT('Ctrl Pts',(2.00186604230606,0.0812282774462531,
29.1254932894691));
#18139=CARTESIAN_POINT('Ctrl Pts',(1.98542547337194,0.268584748349885,29.1388737696367));
#18140=CARTESIAN_POINT('Ctrl Pts',(1.9343622492687,0.488643386563524,29.1541608676364));
#18141=CARTESIAN_POINT('Ctrl Pts',(1.92450248806679,0.526137182303195,29.1567450723227));
#18142=CARTESIAN_POINT('Ctrl Pts',(1.91168903488861,0.569663307121081,29.1597026049817));
#18143=CARTESIAN_POINT('Ctrl Pts',(1.90979092533172,0.575994682353422,29.1601317459518));
#18144=CARTESIAN_POINT('Ctrl Pts',(1.90687014339245,0.585564127636601,29.1607786240099));
#18145=CARTESIAN_POINT('Ctrl Pts',(1.90587063928647,0.588809135512055,29.1609976772601));
#18146=CARTESIAN_POINT('Ctrl Pts',(1.90406363099731,0.594622991808482,29.1613895749004));
#18147=CARTESIAN_POINT('Ctrl Pts',(1.90325921006232,0.597192760236961,29.161562597133));
#18148=CARTESIAN_POINT('Ctrl Pts',(1.90151077950734,0.602738804891277,29.1619355779196));
#18149=CARTESIAN_POINT('Ctrl Pts',(1.90056498814935,0.605714485259134,29.1621354296799));
#18150=CARTESIAN_POINT('Ctrl Pts',(1.89792294039877,0.613959869602264,29.1626884926003));
#18151=CARTESIAN_POINT('Ctrl Pts',(1.89621171163819,0.619224802134308,29.1630408336124));
#18152=CARTESIAN_POINT('Ctrl Pts',(1.88659587582984,0.648396142182027,29.1649889176962));
#18153=CARTESIAN_POINT('Ctrl Pts',(1.87826066461932,0.672159635344352,29.1665604570017));
#18154=CARTESIAN_POINT('Ctrl Pts',(1.81278531401672,0.848089029542241,29.1781243127945));
#18155=CARTESIAN_POINT('Ctrl Pts',(1.73768097503996,0.992937477844196,29.1872866822992));
#18156=CARTESIAN_POINT('Ctrl Pts',(1.58243076691096,1.21964194985828,29.2033488437942));
#18157=CARTESIAN_POINT('Ctrl Pts',(1.51135606335686,1.30667941536661,29.2100326477412));
#18158=CARTESIAN_POINT('Ctrl Pts',(1.42434822255959,1.3965769767511,29.2178417766725));
#18159=CARTESIAN_POINT('Ctrl Pts',(1.41525595760601,1.40579005295335,29.2186535514238));
#18160=CARTESIAN_POINT('Ctrl Pts',(1.40165357133843,1.41930746499783,29.2198620728897));
#18161=CARTESIAN_POINT('Ctrl Pts',(1.39721177599965,1.42368032430728,29.2202557908326));
#18162=CARTESIAN_POINT('Ctrl Pts',(1.38928238885809,1.43141379862778,29.2209570617215));
#18163=CARTESIAN_POINT('Ctrl Pts',(1.38580290018288,1.43478268042937,29.221264249796));
#18164=CARTESIAN_POINT('Ctrl Pts',(1.37846608552437,1.44183468462931,29.2219108817663));
#18165=CARTESIAN_POINT('Ctrl Pts',(1.37460619328911,1.4455150705549,29.2222504407349));
#18166=CARTESIAN_POINT('Ctrl Pts',(1.36441447012293,1.45515508637172,29.2231453896666));
#18167=CARTESIAN_POINT('Ctrl Pts',(1.35805840411952,1.4610888195806,29.2237018856157));
#18168=CARTESIAN_POINT('Ctrl Pts',(1.32921678955223,1.48766324307162,29.2262199345689));
#18169=CARTESIAN_POINT('Ctrl Pts',(1.30629910538465,1.50782680502601,29.2282014999488));
#18170=CARTESIAN_POINT('Ctrl Pts',(1.24383269620646,1.56029310964375,29.2335555053475));
#18171=CARTESIAN_POINT('Ctrl Pts',(1.20349329841,1.59161474576416,29.2369651135961));
#18172=CARTESIAN_POINT('Ctrl Pts',(1.08022265222433,1.6799610180319,29.2472421948056));
#18173=CARTESIAN_POINT('Ctrl Pts',(0.994135253928337,1.73229379294682,29.2542466834574));
#18174=CARTESIAN_POINT('Ctrl Pts',(0.796145412018442,1.83301745511139,29.2697453494907));
#18175=CARTESIAN_POINT('Ctrl Pts',(0.682989870473569,1.87811944952291,29.2782169818174));
#18176=CARTESIAN_POINT('Ctrl Pts',(0.559148921622868,1.91479438893901,29.2866497187329));
#18177=CARTESIAN_POINT('Ctrl Pts',(0.551865436926842,1.91690626074134,29.2871426342446));
#18178=CARTESIAN_POINT('Ctrl Pts',(0.541197102529507,1.91993373607495,29.2878600029908));
#18179=CARTESIAN_POINT('Ctrl Pts',(0.53782171038397,1.9208820013229,29.2880862997733));
#18180=CARTESIAN_POINT('Ctrl Pts',(0.531831944999803,1.92254770920063,29.2884866561701));
#18181=CARTESIAN_POINT('Ctrl Pts',(0.529218591041382,1.92326872670535,29.2886609225122));
#18182=CARTESIAN_POINT('Ctrl Pts',(0.526598875463822,1.92398575537491,29.2888351988449));
#18183=CARTESIAN_POINT('Ctrl Pts',(0.526594021266306,1.92398708397222,29.2888355217685));
#18184=CARTESIAN_POINT('Ctrl Pts',(0.526585806943274,1.92398933220484,29.2888360682208));
#18185=CARTESIAN_POINT('Ctrl Pts',(0.526582446839744,1.92399025184443,29.2888362917487));
#18186=CARTESIAN_POINT('Ctrl Pts',(0.526575727171443,1.92399209095724,29.2888367387674));
#18187=CARTESIAN_POINT('Ctrl Pts',(0.526572367517595,1.92399301045483,29.288836962264));
#18188=CARTESIAN_POINT('Ctrl Pts',(0.526565648734988,1.9239948492874,29.288837409221));
#18189=CARTESIAN_POINT('Ctrl Pts',(0.526562289576874,1.9239957686304,29.2888376326834));
#18190=CARTESIAN_POINT('Ctrl Pts',(0.526555571464562,1.92399760724169,29.2888380795931));
#18191=CARTESIAN_POINT('Ctrl Pts',(0.52655221268682,1.92399852646169,29.2888383030288));
#18192=CARTESIAN_POINT('Ctrl Pts',(0.526545495467737,1.9240003647907,29.2888387498763));
#18193=CARTESIAN_POINT('Ctrl Pts',(0.526542137070716,1.9240012838876,29.2888389732853));
#18194=CARTESIAN_POINT('Ctrl Pts',(0.526535420810581,1.92400312191637,29.2888394200664));
#18195=CARTESIAN_POINT('Ctrl Pts',(0.526532062868687,1.92400404086981,29.2888396434437));
#18196=CARTESIAN_POINT('Ctrl Pts',(0.526525347386487,1.92400587864789,29.2888400901704));
#18197=CARTESIAN_POINT('Ctrl Pts',(0.526521989875334,1.92400679746456,29.2888403135177));
#18198=CARTESIAN_POINT('Ctrl Pts',(0.526515275131037,1.92400863500292,29.2888407601925));
#18199=CARTESIAN_POINT('Ctrl Pts',(0.526511917969968,1.92400955370489,29.2888409835152));
#18200=CARTESIAN_POINT('Ctrl Pts',(0.526505204189689,1.92401139094167,29.2888414301232));
#18201=CARTESIAN_POINT('Ctrl Pts',(0.526501847451382,1.92401230950906,29.2888416534164));
#18202=CARTESIAN_POINT('Ctrl Pts',(0.526495134525531,1.92401414647425,29.2888420999648));
#18203=CARTESIAN_POINT('Ctrl Pts',(0.526491778253567,1.92401506489515,29.2888423232257));
#18204=CARTESIAN_POINT('Ctrl Pts',(0.526485066010145,1.92401690163585,29.288842769726));
#18205=CARTESIAN_POINT('Ctrl Pts',(0.526481710127783,1.92401781993126,29.2888429929596));
#18206=CARTESIAN_POINT('Ctrl Pts',(0.526474998730395,1.92401965640269,29.2888434394009));
#18207=CARTESIAN_POINT('Ctrl Pts',(0.526471643256011,1.9240205745676,29.288843662606));
#18208=CARTESIAN_POINT('Ctrl Pts',(0.526464932562657,1.92402241080864,29.2888441089978));
#18209=CARTESIAN_POINT('Ctrl Pts',(0.526461577398764,1.92402332886972,29.2888443321809));
#18210=CARTESIAN_POINT('Ctrl Pts',(0.526454867820843,1.92402516476782,29.2888447784958));
#18211=CARTESIAN_POINT('Ctrl Pts',(0.526451513191697,1.92402608266371,29.2888450016419));
#18212=CARTESIAN_POINT('Ctrl Pts',(0.526444804048318,1.92402791840519,29.2888454479252));
#18213=CARTESIAN_POINT('Ctrl Pts',(0.526441449729462,1.92402883619733,29.2888456710493));
#18214=CARTESIAN_POINT('Ctrl Pts',(0.526434741628938,1.92403067161575,29.2888461172605));
#18215=CARTESIAN_POINT('Ctrl Pts',(0.526431387788079,1.92403158925825,29.2888463403515));
#18216=CARTESIAN_POINT('Ctrl Pts',(0.526424680200753,1.92403342449855,29.2888467865259));
#18217=CARTESIAN_POINT('Ctrl Pts',(0.526421326651363,1.92403434204245,29.2888470095962));
#18218=CARTESIAN_POINT('Ctrl Pts',(0.526414620032519,1.92403617698008,29.2888474557034));
#18219=CARTESIAN_POINT('Ctrl Pts',(0.526411266864753,1.92403709440071,29.2888476787469));
#18220=CARTESIAN_POINT('Ctrl Pts',(0.526404561024508,1.92403892908763,29.2888481247997));
#18221=CARTESIAN_POINT('Ctrl Pts',(0.52640120823694,1.9240398463854,29.2888483478165));
#18222=CARTESIAN_POINT('Ctrl Pts',(0.526394503275733,1.92404168079415,29.2888487938081));
#18223=CARTESIAN_POINT('Ctrl Pts',(0.526391150973658,1.92404259794026,29.2888490167914));
#18224=CARTESIAN_POINT('Ctrl Pts',(0.52638444638585,1.92404443220918,29.2888494627554));
#18225=CARTESIAN_POINT('Ctrl Pts',(0.52638109428231,1.92404534928214,29.2888496857241));
#18226=CARTESIAN_POINT('Ctrl Pts',(0.526374391079874,1.92404718313439,29.2888501315932));
#18227=CARTESIAN_POINT('Ctrl Pts',(0.526371039620971,1.92404810001216,29.2888503545177));
#18228=CARTESIAN_POINT('Ctrl Pts',(0.526364336506501,1.92404993380269,29.2888508003783));
#18229=CARTESIAN_POINT('Ctrl Pts',(0.526360985294928,1.92405085059398,29.288851023285));
#18230=CARTESIAN_POINT('Ctrl Pts',(0.526354283170577,1.924052684076,29.288851469077));
#18231=CARTESIAN_POINT('Ctrl Pts',(0.526350932321706,1.92405360074925,29.2888516919582));
#18232=CARTESIAN_POINT('Ctrl Pts',(0.526344230833431,1.92405543401962,29.2888521377053));
#18233=CARTESIAN_POINT('Ctrl Pts',(0.526340880232287,1.92405635060628,29.2888523605686));
#18234=CARTESIAN_POINT('Ctrl Pts',(0.526334179846777,1.92405818353736,29.2888528062396));
#18235=CARTESIAN_POINT('Ctrl Pts',(0.526330829737993,1.92405909997052,29.2888530290689));
#18236=CARTESIAN_POINT('Ctrl Pts',(0.523444962036975,1.92484853037316,29.2890449791875));
#18237=CARTESIAN_POINT('Ctrl Pts',(0.520560652967708,1.92563057205457,29.2892363261919));
#18238=CARTESIAN_POINT('Ctrl Pts',(0.512941638471936,1.92767799601785,29.2897404855866));
#18239=CARTESIAN_POINT('Ctrl Pts',(0.508203971277021,1.92893242639931,29.2900526682332));
#18240=CARTESIAN_POINT('Ctrl Pts',(0.497653502177141,1.93168439043918,29.2907450552458));
#18241=CARTESIAN_POINT('Ctrl Pts',(0.491838440440571,1.93317317981301,29.2911247740662));
#18242=CARTESIAN_POINT('Ctrl Pts',(0.474350811353059,1.93756639916924,29.2922612418029));
#18243=CARTESIAN_POINT('Ctrl Pts',(0.462658371402987,1.94039158179283,29.2930138074731));
#18244=CARTESIAN_POINT('Ctrl Pts',(0.299897405222967,1.97816377265397,29.3033977192652));
#18245=CARTESIAN_POINT('Ctrl Pts',(0.145259127038876,1.99549110389519,29.3121958439943));
#18246=CARTESIAN_POINT('Ctrl Pts',(-0.137514151733409,1.99409569077006,
29.3286539196592));
#18247=CARTESIAN_POINT('Ctrl Pts',(-0.264809590281865,1.98121090914016,
29.3362014417442));
#18248=CARTESIAN_POINT('Ctrl Pts',(-0.402758096348126,1.95371004751011,
29.3449807793766));
#18249=CARTESIAN_POINT('Ctrl Pts',(-0.415499521244889,1.95104002239023,
29.3457971510764));
#18250=CARTESIAN_POINT('Ctrl Pts',(-0.434315590364653,1.94690435376797,
29.3470112140561));
#18251=CARTESIAN_POINT('Ctrl Pts',(-0.440411125990315,1.94553453668032,
29.347405835616));
#18252=CARTESIAN_POINT('Ctrl Pts',(-0.451222159309834,1.94305162044443,
29.3481081250778));
#18253=CARTESIAN_POINT('Ctrl Pts',(-0.45594024713903,1.9419499290981,29.3484154242786));
#18254=CARTESIAN_POINT('Ctrl Pts',(-0.465836157238374,1.93960114510146,
29.3490616890073));
#18255=CARTESIAN_POINT('Ctrl Pts',(-0.471013085414775,1.93835048428567,
29.3494007673224));
#18256=CARTESIAN_POINT('Ctrl Pts',(-0.484596411258688,1.93501134618326,
29.3502930887589));
#18257=CARTESIAN_POINT('Ctrl Pts',(-0.492994250691818,1.93288883708351,
29.3508474261109));
#18258=CARTESIAN_POINT('Ctrl Pts',(-0.530599777236812,1.92312322612536,
29.3533419188591));
#18259=CARTESIAN_POINT('Ctrl Pts',(-0.559644193068901,1.91487265305356,
29.3553016304287));
#18260=CARTESIAN_POINT('Ctrl Pts',(-0.636546004130525,1.89112834085122,
29.3605824628041));
#18261=CARTESIAN_POINT('Ctrl Pts',(-0.684020968464962,1.87447907879639,
29.3639395134397));
#18262=CARTESIAN_POINT('Ctrl Pts',(-0.877009309647185,1.79849082090125,
29.3779855539883));
#18263=CARTESIAN_POINT('Ctrl Pts',(-1.01588641501043,1.72385612758125,29.3891084312968));
#18264=CARTESIAN_POINT('Ctrl Pts',(-1.15816819419156,1.62417691584422,29.4010730848067));
#18265=CARTESIAN_POINT('Ctrl Pts',(-1.17167120532949,1.61446301603628,29.4022141337267));
#18266=CARTESIAN_POINT('Ctrl Pts',(-1.2254971517718,1.57471026591049,29.4067807582112));
#18267=CARTESIAN_POINT('Ctrl Pts',(-1.26480316879583,1.54331773453885,29.4101574429467));
#18268=CARTESIAN_POINT('Ctrl Pts',(-1.30830599146299,1.50579356562667,29.4139055239344));
#18269=CARTESIAN_POINT('Ctrl Pts',(-1.31370266596423,1.50108765193655,29.4143706782977));
#18270=CARTESIAN_POINT('Ctrl Pts',(-1.32167084967598,1.4940634898813,29.4150576111325));
#18271=CARTESIAN_POINT('Ctrl Pts',(-1.32426177684032,1.49176750652514,29.4152809946002));
#18272=CARTESIAN_POINT('Ctrl Pts',(-1.32886183630325,1.48766967620366,29.4156776171537));
#18273=CARTESIAN_POINT('Ctrl Pts',(-1.33087329673132,1.48587049026725,29.4158510523132));
#18274=CARTESIAN_POINT('Ctrl Pts',(-1.33476567303237,1.48237464117745,29.4161866716514));
#18275=CARTESIAN_POINT('Ctrl Pts',(-1.33664699623711,1.48067848851036,29.4163488923398));
#18276=CARTESIAN_POINT('Ctrl Pts',(-1.34196330440937,1.47586705228716,29.4168073298297));
#18277=CARTESIAN_POINT('Ctrl Pts',(-1.3453906930421,1.47274334170204,29.4171029154284));
#18278=CARTESIAN_POINT('Ctrl Pts',(-1.35975657592307,1.45955832188375,29.4183421626729));
#18279=CARTESIAN_POINT('Ctrl Pts',(-1.37059369238887,1.44938656079903,29.4192777465109));
#18280=CARTESIAN_POINT('Ctrl Pts',(-1.39889776274354,1.42221886229217,29.4217265184902));
#18281=CARTESIAN_POINT('Ctrl Pts',(-1.41616916638921,1.40502186804519,29.423226181648));
#18282=CARTESIAN_POINT('Ctrl Pts',(-1.48724150274162,1.33161325546986,29.4294430938483));
#18283=CARTESIAN_POINT('Ctrl Pts',(-1.53804898580005,1.27259124628305,29.434002331739));
#18284=CARTESIAN_POINT('Ctrl Pts',(-1.69063016584929,1.07281037687863,29.4486235896082));
#18285=CARTESIAN_POINT('Ctrl Pts',(-1.77751339314154,0.921733095427336,
29.4585617250565));
#18286=CARTESIAN_POINT('Ctrl Pts',(-1.85148388442406,0.742593858594666,
29.4705631289605));
#18287=CARTESIAN_POINT('Ctrl Pts',(-1.85893201674481,0.723747140169397,
29.4718270808956));
#18288=CARTESIAN_POINT('Ctrl Pts',(-1.86881432579185,0.697581511353945,
29.4735850218788));
#18289=CARTESIAN_POINT('Ctrl Pts',(-1.87149529970507,0.69035663953955,29.4740707513966));
#18290=CARTESIAN_POINT('Ctrl Pts',(-1.87571106679072,0.678790656576213,
29.4748489253556));
#18291=CARTESIAN_POINT('Ctrl Pts',(-1.87727282945137,0.674459401861553,
29.4751404692842));
#18292=CARTESIAN_POINT('Ctrl Pts',(-1.88045569981373,0.665535606017815,
29.4757414333433));
#18293=CARTESIAN_POINT('Ctrl Pts',(-1.88207501034069,0.660942460883671,
29.4760509108131));
#18294=CARTESIAN_POINT('Ctrl Pts',(-1.88579229141064,0.650274024335524,
29.4767701154539));
#18295=CARTESIAN_POINT('Ctrl Pts',(-1.88787774294877,0.6441944575584,29.4771802540189));
#18296=CARTESIAN_POINT('Ctrl Pts',(-1.89439904545617,0.624879720646166,
29.4784842406023));
#18297=CARTESIAN_POINT('Ctrl Pts',(-1.89872529447193,0.611608247459151,
29.4793816888355));
#18298=CARTESIAN_POINT('Ctrl Pts',(-1.94370667663957,0.468541821870589,
29.4890736027176));
#18299=CARTESIAN_POINT('Ctrl Pts',(-1.9711160912107,0.334985082796009,29.4983125905171));
#18300=CARTESIAN_POINT('Ctrl Pts',(-1.99145641015902,0.132836524806506,
29.5124297477425));
#18301=CARTESIAN_POINT('Ctrl Pts',(-1.99480094638918,0.0656729622107595,
29.5171344356621));
#18302=CARTESIAN_POINT('Ctrl Pts',(-1.9947494135177,-0.00152963093166499,
29.5218050102941));
#18303=CARTESIAN_POINT('',(-1.99474949650966,0.00141727712894259,30.3209548813952));
#18304=CARTESIAN_POINT('Ctrl Pts',(-1.99474936733483,-0.00158871561299351,
29.5209548813952));
#18305=CARTESIAN_POINT('Ctrl Pts',(-1.99466579522125,-0.106519654372253,
29.5276724214068));
#18306=CARTESIAN_POINT('Ctrl Pts',(-1.98630072391948,-0.211129095682814,
29.5343899614184));
#18307=CARTESIAN_POINT('Ctrl Pts',(-1.96981585838482,-0.314409043374509,
29.54110750143));
#18308=CARTESIAN_POINT('Ctrl Pts',(-1.95888563255435,-0.382888410079444,
29.545561540148));
#18309=CARTESIAN_POINT('Ctrl Pts',(-1.94435854313491,-0.450932742343483,
29.550015578866));
#18310=CARTESIAN_POINT('Ctrl Pts',(-1.92628229647851,-0.518135191599125,
29.554469617584));
#18311=CARTESIAN_POINT('Ctrl Pts',(-1.90823322122938,-0.585236625132148,
29.5589169611897));
#18312=CARTESIAN_POINT('Ctrl Pts',(-1.88664570339129,-0.651498218418248,
29.5633643047955));
#18313=CARTESIAN_POINT('Ctrl Pts',(-1.86161877916089,-0.716521516477704,
29.5678116484013));
#18314=CARTESIAN_POINT('Ctrl Pts',(-1.83662135910167,-0.781468158752438,
29.572253749046));
#18315=CARTESIAN_POINT('Ctrl Pts',(-1.80819276081117,-0.84517895051031,
29.5766958496908));
#18316=CARTESIAN_POINT('Ctrl Pts',(-1.77648181383497,-0.907270592278627,
29.5811379503356));
#18317=CARTESIAN_POINT('Ctrl Pts',(-1.74479087026461,-0.969323066364258,
29.5855772488836));
#18318=CARTESIAN_POINT('Ctrl Pts',(-1.70982190759389,-1.02975798163676,
29.5900165474316));
#18319=CARTESIAN_POINT('Ctrl Pts',(-1.67177123838613,-1.08821343908487,
29.5944558459797));
#18320=CARTESIAN_POINT('Ctrl Pts',(-1.63373164200094,-1.14665188587529,
29.5988938526827));
#18321=CARTESIAN_POINT('Ctrl Pts',(-1.59261238627219,-1.20311160826029,
29.6033318593858));
#18322=CARTESIAN_POINT('Ctrl Pts',(-1.54865403648486,-1.25725822239472,
29.6077698660888));
#18323=CARTESIAN_POINT('Ctrl Pts',(-1.50469354195092,-1.31140747836554,
29.6122080893241));
#18324=CARTESIAN_POINT('Ctrl Pts',(-1.45789398876281,-1.36324302345215,
29.6166463125594));
#18325=CARTESIAN_POINT('Ctrl Pts',(-1.40853616203275,-1.41246360758289,
29.6210845357947));
#18326=CARTESIAN_POINT('Ctrl Pts',(-1.35912604613227,-1.46173633549065,
29.6255274608378));
#18327=CARTESIAN_POINT('Ctrl Pts',(-1.30715259458788,-1.50838822675202,
29.6299703858808));
#18328=CARTESIAN_POINT('Ctrl Pts',(-1.25293270040905,-1.55215566575833,
29.6344133109238));
#18329=CARTESIAN_POINT('Ctrl Pts',(-1.19868115584625,-1.59594865362029,
29.6388588294851));
#18330=CARTESIAN_POINT('Ctrl Pts',(-1.14218095524136,-1.63685355069029,
29.6433043480463));
#18331=CARTESIAN_POINT('Ctrl Pts',(-1.08377898084886,-1.67464942097449,
29.6477498666076));
#18332=CARTESIAN_POINT('Ctrl Pts',(-1.02527509338074,-1.71251124610742,
29.6522031427228));
#18333=CARTESIAN_POINT('Ctrl Pts',(-0.964863231852163,-1.74725297047359,
29.656656418838));
#18334=CARTESIAN_POINT('Ctrl Pts',(-0.902915217312026,-1.7786994329696,
29.6611096949532));
#18335=CARTESIAN_POINT('Ctrl Pts',(-0.869743836950932,-1.79553810933735,
29.6634942962511));
#18336=CARTESIAN_POINT('Ctrl Pts',(-0.83613235041454,-1.81143275734089,
29.6658788975489));
#18337=CARTESIAN_POINT('Ctrl Pts',(-0.802139872537429,-1.82636228262238,
29.6682634988468));
#18338=CARTESIAN_POINT('Ctrl Pts',(-0.738647576059334,-1.85424815339875,
29.6727175375648));
#18339=CARTESIAN_POINT('Ctrl Pts',(-0.673573653503056,-1.8788744012535,
29.6771715762827));
#18340=CARTESIAN_POINT('Ctrl Pts',(-0.607285994646577,-1.90006086302679,
29.6816256150007));
#18341=CARTESIAN_POINT('Ctrl Pts',(-0.541097976440631,-1.92121547825625,
29.6860729586065));
#18342=CARTESIAN_POINT('Ctrl Pts',(-0.473700305504764,-1.93894042180044,
29.6905203022122));
#18343=CARTESIAN_POINT('Ctrl Pts',(-0.405481605230866,-1.95310323084045,
29.694967645818));
#18344=CARTESIAN_POINT('Ctrl Pts',(-0.337343327792411,-1.96724934338439,
29.6994097464628));
#18345=CARTESIAN_POINT('Ctrl Pts',(-0.268386420431636,-1.97784156290728,
29.7038518471076));
#18346=CARTESIAN_POINT('Ctrl Pts',(-0.199013723142859,-1.98479749609395,
29.7082939477524));
#18347=CARTESIAN_POINT('Ctrl Pts',(-0.129684786458864,-1.99174904144715,
29.7127332463004));
#18348=CARTESIAN_POINT('Ctrl Pts',(-0.0599410661421116,-1.99506880207736,
29.7171725448484));
#18349=CARTESIAN_POINT('Ctrl Pts',(0.00980688254372123,-1.9947258928371,
29.7216118433964));
#18350=CARTESIAN_POINT('Ctrl Pts',(0.0795345344338355,-1.99438308338414,
29.7260498500995));
#18351=CARTESIAN_POINT('Ctrl Pts',(0.149265922945748,-1.99037972233577,
29.7304878568026));
#18352=CARTESIAN_POINT('Ctrl Pts',(0.218589667450933,-1.98273702739009,
29.7349258635056));
#18353=CARTESIAN_POINT('Ctrl Pts',(0.28791679429119,-1.97509395955407,29.7393640867409));
#18354=CARTESIAN_POINT('Ctrl Pts',(0.356835751287597,-1.96381126131426,
29.7438023099762));
#18355=CARTESIAN_POINT('Ctrl Pts',(0.424941239790018,-1.94896190450858,
29.7482405332115));
#18356=CARTESIAN_POINT('Ctrl Pts',(0.493118878541495,-1.93409681644812,
29.7526834582546));
#18357=CARTESIAN_POINT('Ctrl Pts',(0.560480849449957,-1.91565763265303,
29.7571263832976));
#18358=CARTESIAN_POINT('Ctrl Pts',(0.626633946079841,-1.89376805869156,
29.7615693083406));
#18359=CARTESIAN_POINT('Ctrl Pts',(0.692825658995164,-1.87186570688478,
29.7660148269019));
#18360=CARTESIAN_POINT('Ctrl Pts',(0.757806636869767,-1.84650913402551,
29.7704603454631));
#18361=CARTESIAN_POINT('Ctrl Pts',(0.821203319942807,-1.81787036661444,
29.7749058640244));
#18362=CARTESIAN_POINT('Ctrl Pts',(0.884710631997507,-1.7891816237548,29.7793591401396));
#18363=CARTESIAN_POINT('Ctrl Pts',(0.946627695619021,-1.75719947783284,
29.7838124162549));
#18364=CARTESIAN_POINT('Ctrl Pts',(1.00660593447129,-1.72214170589623,29.7882656923701));
#18365=CARTESIAN_POINT('Ctrl Pts',(1.03872255659511,-1.70336927717314,29.7906502936679));
#18366=CARTESIAN_POINT('Ctrl Pts',(1.0702837584668,-1.6837157177325,29.7930348949657));
#18367=CARTESIAN_POINT('Ctrl Pts',(1.10123979937458,-1.663219308081,29.7954194962635));
#18368=CARTESIAN_POINT('Ctrl Pts',(1.15906053648768,-1.62493542295007,29.7998735349814));
#18369=CARTESIAN_POINT('Ctrl Pts',(1.21499703220259,-1.58355697533055,29.8043275736994));
#18370=CARTESIAN_POINT('Ctrl Pts',(1.26869863310333,-1.53929572885191,29.8087816124174));
#18371=CARTESIAN_POINT('Ctrl Pts',(1.32231951215414,-1.49510101390373,29.8132289560232));
#18372=CARTESIAN_POINT('Ctrl Pts',(1.37371178925215,-1.44803240944277,29.8176762996289));
#18373=CARTESIAN_POINT('Ctrl Pts',(1.42255368997764,-1.39834493657001,29.8221236432347));
#18374=CARTESIAN_POINT('Ctrl Pts',(1.47133801112264,-1.3487160401204,29.8265657438795));
#18375=CARTESIAN_POINT('Ctrl Pts',(1.51757758591197,-1.2964747546224,29.8310078445243));
#18376=CARTESIAN_POINT('Ctrl Pts',(1.56098503920093,-1.2419151621149,29.8354499451691));
#18377=CARTESIAN_POINT('Ctrl Pts',(1.60436511087606,-1.18738998604005,29.8398892437171));
#18378=CARTESIAN_POINT('Ctrl Pts',(1.64491630099581,-1.13054978623273,29.8443285422651));
#18379=CARTESIAN_POINT('Ctrl Pts',(1.68239036315675,-1.07172301853478,29.8487678408131));
#18380=CARTESIAN_POINT('Ctrl Pts',(1.71985352028893,-1.01291336954658,29.8532058475162));
#18381=CARTESIAN_POINT('Ctrl Pts',(1.75424106418017,-0.952118712967176,
29.8576438542193));
#18382=CARTESIAN_POINT('Ctrl Pts',(1.78534810742408,-0.889696407667943,
29.8620818609223));
#18383=CARTESIAN_POINT('Ctrl Pts',(1.81645666839392,-0.827271056757785,
29.8665200841576));
#18384=CARTESIAN_POINT('Ctrl Pts',(1.84428419473193,-0.763218338697194,
29.8709583073929));
#18385=CARTESIAN_POINT('Ctrl Pts',(1.86867260456926,-0.697918519192841,
29.8753965306283));
#18386=CARTESIAN_POINT('Ctrl Pts',(1.89308685123536,-0.63254952173609,29.8798394556713));
#18387=CARTESIAN_POINT('Ctrl Pts',(1.91405453779159,-0.565931245383549,
29.8842823807143));
#18388=CARTESIAN_POINT('Ctrl Pts',(1.93146678400278,-0.498461257064151,
29.8887253057573));
#18389=CARTESIAN_POINT('Ctrl Pts',(1.94888919445878,-0.430951883735447,
29.8931708243186));
#18390=CARTESIAN_POINT('Ctrl Pts',(1.96275193628476,-0.362590288802527,
29.8976163428798));
#18391=CARTESIAN_POINT('Ctrl Pts',(1.97299739237546,-0.293783682629998,
29.9020618614411));
#18392=CARTESIAN_POINT('Ctrl Pts',(1.98326072707303,-0.224857007008966,
29.9065151375563));
#18393=CARTESIAN_POINT('Ctrl Pts',(1.98989412902908,-0.155484257288521,
29.9109684136716));
#18394=CARTESIAN_POINT('Ctrl Pts',(1.99289197257705,-0.0860764087190482,
29.9154216897868));
#18395=CARTESIAN_POINT('Ctrl Pts',(1.99449723158865,-0.0489105017563579,
29.9178062910846));
#18396=CARTESIAN_POINT('Ctrl Pts',(1.99506096221642,-0.0117345139403332,
29.9201908923825));
#18397=CARTESIAN_POINT('Ctrl Pts',(1.99458841887372,0.025389009331597,29.9225754936803));
#18398=CARTESIAN_POINT('Ctrl Pts',(1.99370578648303,0.0947295779843875,
29.9270295323983));
#18399=CARTESIAN_POINT('Ctrl Pts',(1.98920122678504,0.164161389297369,29.9314835711163));
#18400=CARTESIAN_POINT('Ctrl Pts',(1.9810629337309,0.233274977435445,29.9359376098343));
#18401=CARTESIAN_POINT('Ctrl Pts',(1.97293687379569,0.302284677112187,29.94038495344));
#18402=CARTESIAN_POINT('Ctrl Pts',(1.96118797813399,0.370976620758892,29.9448322970458));
#18403=CARTESIAN_POINT('Ctrl Pts',(1.94585644517227,0.438942202666316,29.9492796406515));
#18404=CARTESIAN_POINT('Ctrl Pts',(1.93054298651197,0.506827660138852,29.9537217412963));
#18405=CARTESIAN_POINT('Ctrl Pts',(1.911655386283,0.573987981347018,29.9581638419411));
#18406=CARTESIAN_POINT('Ctrl Pts',(1.88928530786421,0.640022333976274,29.9626059425859));
#18407=CARTESIAN_POINT('Ctrl Pts',(1.86692934058998,0.706015031843367,29.9670452411339));
#18408=CARTESIAN_POINT('Ctrl Pts',(1.84109540971041,0.770882707534618,29.971484539682));
#18409=CARTESIAN_POINT('Ctrl Pts',(1.81192526340182,0.834238816134948,29.97592383823));
#18410=CARTESIAN_POINT('Ctrl Pts',(1.78276360566548,0.89757648797808,29.9803618449331));
#18411=CARTESIAN_POINT('Ctrl Pts',(1.75026786441981,0.959403021476149,29.9847998516361));
#18412=CARTESIAN_POINT('Ctrl Pts',(1.71462756335534,1.01935267767447,29.9892378583392));
#18413=CARTESIAN_POINT('Ctrl Pts',(1.6789855233854,1.07930525884206,29.9936760815745));
#18414=CARTESIAN_POINT('Ctrl Pts',(1.64019887122271,1.13738036131342,29.9981143048098));
#18415=CARTESIAN_POINT('Ctrl Pts',(1.59850173072441,1.19323919620966,30.0025525280451));
#18416=CARTESIAN_POINT('Ctrl Pts',(1.55676041670735,1.24915720737701,30.0069954530881));
#18417=CARTESIAN_POINT('Ctrl Pts',(1.5121027535873,1.30285387159713,30.0114383781312));
#18418=CARTESIAN_POINT('Ctrl Pts',(1.46480404970151,1.35402239954813,30.0158813031742));
#18419=CARTESIAN_POINT('Ctrl Pts',(1.4174777356154,1.40522079667502,30.0203268217355));
#18420=CARTESIAN_POINT('Ctrl Pts',(1.36750766303851,1.45388777849408,30.0247723402967));
#18421=CARTESIAN_POINT('Ctrl Pts',(1.315205002565,1.49975443447519,30.029217858858));
#18422=CARTESIAN_POINT('Ctrl Pts',(1.26281107248893,1.54570112905136,30.0336711349732));
#18423=CARTESIAN_POINT('Ctrl Pts',(1.20807681366987,1.58883744016883,30.0381244110884));
#18424=CARTESIAN_POINT('Ctrl Pts',(1.15134471083882,1.62893613113697,30.0425776872037));
#18425=CARTESIAN_POINT('Ctrl Pts',(1.12096630120605,1.6504078270407,30.0449622885015));
#18426=CARTESIAN_POINT('Ctrl Pts',(1.0900155202146,1.67100930801374,30.0473468897992));
#18427=CARTESIAN_POINT('Ctrl Pts',(1.05854779817953,1.69071112892454,30.049731491097));
#18428=CARTESIAN_POINT('Ctrl Pts',(0.999771325801679,1.72751085441041,30.054185529815));
#18429=CARTESIAN_POINT('Ctrl Pts',(0.938957186119689,1.76131481712195,30.058639568533));
#18430=CARTESIAN_POINT('Ctrl Pts',(0.876443248680132,1.79189140138096,30.063093607251));
#18431=CARTESIAN_POINT('Ctrl Pts',(0.814023279401504,1.82242202428306,30.0675409508567));
#18432=CARTESIAN_POINT('Ctrl Pts',(0.749909019715537,1.84973468391449,30.0719882944625));
#18433=CARTESIAN_POINT('Ctrl Pts',(0.684465771850529,1.87364195343322,30.0764356380682));
#18434=CARTESIAN_POINT('Ctrl Pts',(0.619099674847843,1.89752103873862,30.080877738713));
#18435=CARTESIAN_POINT('Ctrl Pts',(0.552408159028457,1.91800254026798,30.0853198393578));
#18436=CARTESIAN_POINT('Ctrl Pts',(0.484777854815494,1.93494650933314,30.0897619400026));
#18437=CARTESIAN_POINT('Ctrl Pts',(0.417190212098042,1.95187979006755,30.0942012385506));
#18438=CARTESIAN_POINT('Ctrl Pts',(0.348665429541026,1.96527984640244,30.0986405370986));
#18439=CARTESIAN_POINT('Ctrl Pts',(0.279605241831666,1.97505657418725,30.1030798356467));
#18440=CARTESIAN_POINT('Ctrl Pts',(0.210565150778193,1.98483045692426,30.1075178423497));
#18441=CARTESIAN_POINT('Ctrl Pts',(0.140990448347648,1.9909830356668,30.1119558490528));
#18442=CARTESIAN_POINT('Ctrl Pts',(0.071291242688871,1.99347563848066,30.1163938557558));
#18443=CARTESIAN_POINT('Ctrl Pts',(0.00158863637605586,1.99596836290968,
30.1208320789912));
#18444=CARTESIAN_POINT('Ctrl Pts',(-0.0682379958922396,1.99480074177305,
30.1252703022265));
#18445=CARTESIAN_POINT('Ctrl Pts',(-0.137777057387593,1.9899861921525,30.1297085254618));
#18446=CARTESIAN_POINT('Ctrl Pts',(-0.207389787844344,1.98516654204796,
30.1341514505048));
#18447=CARTESIAN_POINT('Ctrl Pts',(-0.276713850096724,1.97669228594301,
30.1385943755478));
#18448=CARTESIAN_POINT('Ctrl Pts',(-0.345342253519151,1.96462879202009,
30.1430373005909));
#18449=CARTESIAN_POINT('Ctrl Pts',(-0.414010718165479,1.95255825613922,
30.1474828191521));
#18450=CARTESIAN_POINT('Ctrl Pts',(-0.481982238513912,1.93689442218222,
30.1519283377134));
#18451=CARTESIAN_POINT('Ctrl Pts',(-0.548862254567311,1.91775331782044,
30.1563738562746));
#18452=CARTESIAN_POINT('Ctrl Pts',(-0.615858978115655,1.89857881169722,
30.1608271323898));
#18453=CARTESIAN_POINT('Ctrl Pts',(-0.681759932334584,1.87591508167937,
30.1652804085051));
#18454=CARTESIAN_POINT('Ctrl Pts',(-0.746188640976332,1.84992704574475,
30.1697336846203));
#18455=CARTESIAN_POINT('Ctrl Pts',(-0.780688361691636,1.83601119983405,
30.1721182859181));
#18456=CARTESIAN_POINT('Ctrl Pts',(-0.814766331291456,1.82114298372511,
30.174502887216));
#18457=CARTESIAN_POINT('Ctrl Pts',(-0.848367782930703,1.80535305892926,
30.1768874885138));
#18458=CARTESIAN_POINT('Ctrl Pts',(-0.911129707416232,1.77586010492511,
30.1813415272318));
#18459=CARTESIAN_POINT('Ctrl Pts',(-0.972476139029651,1.7430320253504,30.1857955659497));
#18460=CARTESIAN_POINT('Ctrl Pts',(-1.03202941857197,1.70702748709621,30.1902496046677));
#18461=CARTESIAN_POINT('Ctrl Pts',(-1.09149318028213,1.67107706925717,30.1946969482735));
#18462=CARTESIAN_POINT('Ctrl Pts',(-1.14916872406153,1.63195992057579,30.1991442918792));
#18463=CARTESIAN_POINT('Ctrl Pts',(-1.20470069042879,1.58988169653607,30.203591635485));
#18464=CARTESIAN_POINT('Ctrl Pts',(-1.26016719031588,1.54785307839722,30.2080337361298));
#18465=CARTESIAN_POINT('Ctrl Pts',(-1.31349474353205,1.50287061231141,30.2124758367746));
#18466=CARTESIAN_POINT('Ctrl Pts',(-1.3643563608736,1.45518359083785,30.2169179374193));
#18467=CARTESIAN_POINT('Ctrl Pts',(-1.41518589448164,1.40752665054867,30.2213572359674));
#18468=CARTESIAN_POINT('Ctrl Pts',(-1.46355222170617,1.35716887334317,30.2257965345154));
#18469=CARTESIAN_POINT('Ctrl Pts',(-1.50916208288596,1.30439923722735,30.2302358330634));
#18470=CARTESIAN_POINT('Ctrl Pts',(-1.55475867150285,1.25164495718359,30.2346738397665));
#18471=CARTESIAN_POINT('Ctrl Pts',(-1.59760006647602,1.19648058172043,30.2391118464695));
#18472=CARTESIAN_POINT('Ctrl Pts',(-1.63743171667576,1.13922997490598,30.2435498531726));
#18473=CARTESIAN_POINT('Ctrl Pts',(-1.67726531027866,1.08197657481006,30.2479880764079));
#18474=CARTESIAN_POINT('Ctrl Pts',(-1.71408858993195,1.02263714450766,30.2524262996432));
#18475=CARTESIAN_POINT('Ctrl Pts',(-1.74768999280331,0.961565001211662,
30.2568645228785));
#18476=CARTESIAN_POINT('Ctrl Pts',(-1.78132699265284,0.900428158719596,
30.2613074479216));
#18477=CARTESIAN_POINT('Ctrl Pts',(-1.8117350666283,0.837555369209269,30.2657503729646));
#18478=CARTESIAN_POINT('Ctrl Pts',(-1.83874882397477,0.773324204219296,
30.2701932980076));
#18479=CARTESIAN_POINT('Ctrl Pts',(-1.86577835036331,0.70905554485449,30.2746388165689));
#18480=CARTESIAN_POINT('Ctrl Pts',(-1.88940945046268,0.643427392505011,
30.2790843351301));
#18481=CARTESIAN_POINT('Ctrl Pts',(-1.90952605595385,0.576834295212516,
30.2835298536914));
#18482=CARTESIAN_POINT('Ctrl Pts',(-1.92967776548315,0.510124991106323,
30.2879831298066));
#18483=CARTESIAN_POINT('Ctrl Pts',(-1.94630262127761,0.44244785615585,30.2924364059218));
#18484=CARTESIAN_POINT('Ctrl Pts',(-1.95933545066732,0.374208704145551,
30.2968896820371));
#18485=CARTESIAN_POINT('Ctrl Pts',(-1.96631415602319,0.337668600582921,
30.2992742833349));
#18486=CARTESIAN_POINT('Ctrl Pts',(-1.97226380792002,0.300967462935943,
30.3016588846326));
#18487=CARTESIAN_POINT('Ctrl Pts',(-1.97718053383544,0.264167937347107,
30.3040434859304));
#18488=CARTESIAN_POINT('Ctrl Pts',(-1.98880353854548,0.177174871920036,
30.309680617752));
#18489=CARTESIAN_POINT('Ctrl Pts',(-1.99468698571734,0.0893982153310911,
30.3153177495736));
#18490=CARTESIAN_POINT('Ctrl Pts',(-1.99474949650966,0.00141727712894259,
30.3209548813952));
#18491=CARTESIAN_POINT('',(-1.99474901027189,-0.00181008235116998,31.9203783954114));
#18492=CARTESIAN_POINT('Ctrl Pts',(-1.994749448555,0.00148323617099721,
30.3220724695856));
#18493=CARTESIAN_POINT('Ctrl Pts',(-1.99486339498652,-0.151759103715625,
30.3311167672701));
#18494=CARTESIAN_POINT('Ctrl Pts',(-1.97731920438673,-0.304509772329282,
30.3397836599352));
#18495=CARTESIAN_POINT('Ctrl Pts',(-1.93170678897217,-0.499769147293737,
30.3517403697977));
#18496=CARTESIAN_POINT('Ctrl Pts',(-1.91932723631203,-0.545383159862958,
30.3545948799917));
#18497=CARTESIAN_POINT('Ctrl Pts',(-1.89969508734825,-0.608728035408092,
30.3586714187028));
#18498=CARTESIAN_POINT('Ctrl Pts',(-1.89378881198397,-0.62686134308302,
30.359851501595));
#18499=CARTESIAN_POINT('Ctrl Pts',(-1.88298687396782,-0.658478308137421,
30.3619337530981));
#18500=CARTESIAN_POINT('Ctrl Pts',(-1.87820400918912,-0.671999205833263,
30.3628322232345));
#18501=CARTESIAN_POINT('Ctrl Pts',(-1.87104275201591,-0.691569817744031,
30.364144836028));
#18502=CARTESIAN_POINT('Ctrl Pts',(-1.86877985749518,-0.697661547803978,
30.3645551329124));
#18503=CARTESIAN_POINT('Ctrl Pts',(-1.86476516292163,-0.708309449584588,
30.3652753665149));
#18504=CARTESIAN_POINT('Ctrl Pts',(-1.86302632129088,-0.712870475402617,
30.3655848675377));
#18505=CARTESIAN_POINT('Ctrl Pts',(-1.85962237571779,-0.721701592300385,
30.3661860676579));
#18506=CARTESIAN_POINT('Ctrl Pts',(-1.85795926001988,-0.725972421051901,
30.3664776983657));
#18507=CARTESIAN_POINT('Ctrl Pts',(-1.85350030155023,-0.737307202484019,
30.3672540581546));
#18508=CARTESIAN_POINT('Ctrl Pts',(-1.85067881829888,-0.744360925583806,
30.3677396486224));
#18509=CARTESIAN_POINT('Ctrl Pts',(-1.84044782789998,-0.769520684348089,
30.3694806031659));
#18510=CARTESIAN_POINT('Ctrl Pts',(-1.83281253926961,-0.78753313669766,
30.3707435783314));
#18511=CARTESIAN_POINT('Ctrl Pts',(-1.75159838836013,-0.971545216472034,
30.3838216678952));
#18512=CARTESIAN_POINT('Ctrl Pts',(-1.65595850478544,-1.12684049535055,
30.396458586788));
#18513=CARTESIAN_POINT('Ctrl Pts',(-1.49613467506367,-1.32118362177827,
30.4139916377149));
#18514=CARTESIAN_POINT('Ctrl Pts',(-1.44876431476313,-1.37296337027864,
30.4188527721933));
#18515=CARTESIAN_POINT('Ctrl Pts',(-1.38108385926314,-1.4395311006474,30.4252648687568));
#18516=CARTESIAN_POINT('Ctrl Pts',(-1.36308196423649,-1.45658851365651,
30.4269235183857));
#18517=CARTESIAN_POINT('Ctrl Pts',(-1.33363276270172,-1.48346837601047,
30.4295563417819));
#18518=CARTESIAN_POINT('Ctrl Pts',(-1.32238446779618,-1.49350397425057,
30.4305437666554));
#18519=CARTESIAN_POINT('Ctrl Pts',(-1.30751815263498,-1.50646787860957,
30.4318239776783));
#18520=CARTESIAN_POINT('Ctrl Pts',(-1.30400249660119,-1.50951206642114,
30.4321249405963));
#18521=CARTESIAN_POINT('Ctrl Pts',(-1.29855487980258,-1.51419589449613,
30.4325884948834));
#18522=CARTESIAN_POINT('Ctrl Pts',(-1.29663041669918,-1.5158441692452,30.4327517174545));
#18523=CARTESIAN_POINT('Ctrl Pts',(-1.29265032105877,-1.51923993799457,
30.4330881734918));
#18524=CARTESIAN_POINT('Ctrl Pts',(-1.29059430903508,-1.52098690702118,
30.4332613650642));
#18525=CARTESIAN_POINT('Ctrl Pts',(-1.28589753409171,-1.52496132051165,
30.4336556194801));
#18526=CARTESIAN_POINT('Ctrl Pts',(-1.28325453054251,-1.5271860749503,30.4338764839836));
#18527=CARTESIAN_POINT('Ctrl Pts',(-1.27636353039978,-1.53295607062898,
30.4344497974799));
#18528=CARTESIAN_POINT('Ctrl Pts',(-1.27210650360312,-1.53649055364581,
30.434801474389));
#18529=CARTESIAN_POINT('Ctrl Pts',(-1.24521294785643,-1.55863108785729,
30.4370079128167));
#18530=CARTESIAN_POINT('Ctrl Pts',(-1.22218205700449,-1.57675533706004,
30.4388296970858));
#18531=CARTESIAN_POINT('Ctrl Pts',(-1.1128894596893,-1.65892931781301,30.4472084576566));
#18532=CARTESIAN_POINT('Ctrl Pts',(-1.02193505155617,-1.71645656980635,
30.4534330831218));
#18533=CARTESIAN_POINT('Ctrl Pts',(-0.849168405902545,-1.80710335158789,
30.4647488712847));
#18534=CARTESIAN_POINT('Ctrl Pts',(-0.768958918600692,-1.84266400643804,
30.4698246504608));
#18535=CARTESIAN_POINT('Ctrl Pts',(-0.638721543276217,-1.89041555838437,
30.4780696528934));
#18536=CARTESIAN_POINT('Ctrl Pts',(-0.590113963383805,-1.90614823789107,
30.4811464465909));
#18537=CARTESIAN_POINT('Ctrl Pts',(-0.511572290956982,-1.92827733384457,
30.4861552193534));
#18538=CARTESIAN_POINT('Ctrl Pts',(-0.482000855644467,-1.93588085954542,
30.488049120221));
#18539=CARTESIAN_POINT('Ctrl Pts',(-0.443798081162261,-1.94477413826615,
30.490510713536));
#18540=CARTESIAN_POINT('Ctrl Pts',(-0.435315694382959,-1.94669037807191,
30.4910582043222));
#18541=CARTESIAN_POINT('Ctrl Pts',(-0.421611186598649,-1.94969228751494,
30.49194435614));
#18542=CARTESIAN_POINT('Ctrl Pts',(-0.416396703231105,-1.95081259820036,
30.4922819045187));
#18543=CARTESIAN_POINT('Ctrl Pts',(-0.406438702614553,-1.95291028966642,
30.49292725146));
#18544=CARTESIAN_POINT('Ctrl Pts',(-0.401695989322101,-1.95389133524634,
30.493234930201));
#18545=CARTESIAN_POINT('Ctrl Pts',(-0.390841669741732,-1.95609539621993,
30.4939398424017));
#18546=CARTESIAN_POINT('Ctrl Pts',(-0.384727833572551,-1.95730705371852,
30.4943374355564));
#18547=CARTESIAN_POINT('Ctrl Pts',(-0.365901448791162,-1.96094650490501,
30.4955634709181));
#18548=CARTESIAN_POINT('Ctrl Pts',(-0.353171071807441,-1.96327920740757,
30.4963949303834));
#18549=CARTESIAN_POINT('Ctrl Pts',(-0.230003854588047,-1.98461155955905,
30.5044639779534));
#18550=CARTESIAN_POINT('Ctrl Pts',(-0.118193260868712,-1.99439398798779,
30.5119972909011));
#18551=CARTESIAN_POINT('Ctrl Pts',(0.165010467986752,-1.9952698910346,30.5315249135389));
#18552=CARTESIAN_POINT('Ctrl Pts',(0.335543026691079,-1.97376359847848,
30.5437336824178));
#18553=CARTESIAN_POINT('Ctrl Pts',(0.512698639338938,-1.92777278888097,
30.5558598579801));
#18554=CARTESIAN_POINT('Ctrl Pts',(0.524135297764521,-1.92469478762665,
30.556639783861));
#18555=CARTESIAN_POINT('Ctrl Pts',(0.541261978256587,-1.91992142189045,
30.5578026825184));
#18556=CARTESIAN_POINT('Ctrl Pts',(0.546972725007384,-1.9183022795032,30.5581895924199));
#18557=CARTESIAN_POINT('Ctrl Pts',(0.557253096091754,-1.91533789152785,
30.5588844621814));
#18558=CARTESIAN_POINT('Ctrl Pts',(0.561825263686943,-1.91400173094101,
30.5591929178396));
#18559=CARTESIAN_POINT('Ctrl Pts',(0.569270786304491,-1.91179688889727,
30.5596942150529));
#18560=CARTESIAN_POINT('Ctrl Pts',(0.57214701044523,-1.91093808671764,30.5598876221662));
#18561=CARTESIAN_POINT('Ctrl Pts',(0.577607769266245,-1.90929414272724,
30.5602543413023));
#18562=CARTESIAN_POINT('Ctrl Pts',(0.580192616621806,-1.90851025312674,
30.5604277205826));
#18563=CARTESIAN_POINT('Ctrl Pts',(0.586108382582246,-1.90670308860113,
30.5608240571881));
#18564=CARTESIAN_POINT('Ctrl Pts',(0.589438211649311,-1.90567633645207,
30.5610468081733));
#18565=CARTESIAN_POINT('Ctrl Pts',(0.599712284950682,-1.90247882297546,
30.56173310812));
#18566=CARTESIAN_POINT('Ctrl Pts',(0.606647453901798,-1.90027876038925,
30.562194972301));
#18567=CARTESIAN_POINT('Ctrl Pts',(0.664692071413225,-1.88151495452746,
30.5660500557109));
#18568=CARTESIAN_POINT('Ctrl Pts',(0.715130415396461,-1.86292880750781,
30.5693314713035));
#18569=CARTESIAN_POINT('Ctrl Pts',(0.787160307041539,-1.83302874296689,
30.5740006035073));
#18570=CARTESIAN_POINT('Ctrl Pts',(0.809388358443597,-1.8233228656232,30.5754390245067));
#18571=CARTESIAN_POINT('Ctrl Pts',(0.954956575308382,-1.75657374073807,
30.5848763214426));
#18572=CARTESIAN_POINT('Ctrl Pts',(1.07236769065602,-1.68746039417972,30.5925967011685));
#18573=CARTESIAN_POINT('Ctrl Pts',(1.25048146368272,-1.5564649688693,30.6056792896637));
#18574=CARTESIAN_POINT('Ctrl Pts',(1.31580685651395,-1.501644632093,30.6108269963243));
#18575=CARTESIAN_POINT('Ctrl Pts',(1.38581103446804,-1.43481351558923,30.6168777072078));
#18576=CARTESIAN_POINT('Ctrl Pts',(1.39412895587978,-1.42673280367127,30.6176057939713));
#18577=CARTESIAN_POINT('Ctrl Pts',(1.40661575435763,-1.414388641094,30.6187129932036));
#18578=CARTESIAN_POINT('Ctrl Pts',(1.41083685144731,-1.41017817519839,30.6190897762606));
#18579=CARTESIAN_POINT('Ctrl Pts',(1.41840172413926,-1.40256439223164,30.6197695873615));
#18580=CARTESIAN_POINT('Ctrl Pts',(1.42175229845131,-1.39916786934136,30.6200723120978));
#18581=CARTESIAN_POINT('Ctrl Pts',(1.428926957879,-1.39184243770791,30.6207240751154));
#18582=CARTESIAN_POINT('Ctrl Pts',(1.43274708700504,-1.3879097254672,30.6210732828345));
#18583=CARTESIAN_POINT('Ctrl Pts',(1.44304985958778,-1.37721545463019,30.6220210452301));
#18584=CARTESIAN_POINT('Ctrl Pts',(1.44950110448985,-1.37042396682332,30.6226209527871));
#18585=CARTESIAN_POINT('Ctrl Pts',(1.47868708987422,-1.33926204888278,30.6253648656451));
#18586=CARTESIAN_POINT('Ctrl Pts',(1.50085554452308,-1.31437085962979,30.6275327697879));
#18587=CARTESIAN_POINT('Ctrl Pts',(1.52668795766337,-1.28385969045721,30.6301639994736));
#18588=CARTESIAN_POINT('Ctrl Pts',(1.53096141755554,-1.27876071298762,30.6306028708265));
#18589=CARTESIAN_POINT('Ctrl Pts',(1.66677555185849,-1.11505430237392,30.6446660489814));
#18590=CARTESIAN_POINT('Ctrl Pts',(1.77296153164015,-0.937048985632428,
30.6593369465018));
#18591=CARTESIAN_POINT('Ctrl Pts',(1.86475313632124,-0.709422684456393,
30.676157820554));
#18592=CARTESIAN_POINT('Ctrl Pts',(1.87842333115145,-0.672392008025104,
30.6788321917695));
#18593=CARTESIAN_POINT('Ctrl Pts',(1.89544833846604,-0.621690924862446,
30.6823893307402));
#18594=CARTESIAN_POINT('Ctrl Pts',(1.89976994599906,-0.608356957110443,
30.6833151849895));
#18595=CARTESIAN_POINT('Ctrl Pts',(1.90688191613028,-0.585598404351281,
30.6848778075225));
#18596=CARTESIAN_POINT('Ctrl Pts',(1.9097437678265,-0.576196914324994,30.6855182432239));
#18597=CARTESIAN_POINT('Ctrl Pts',(1.91365499477745,-0.562998784093583,
30.6864098371225));
#18598=CARTESIAN_POINT('Ctrl Pts',(1.91476272450163,-0.5592197952835,30.6866642704505));
#18599=CARTESIAN_POINT('Ctrl Pts',(1.91663149296347,-0.552773890383566,
30.6870967782753));
#18600=CARTESIAN_POINT('Ctrl Pts',(1.91739817054981,-0.550108634379652,
30.6872751800331));
#18601=CARTESIAN_POINT('Ctrl Pts',(1.91885361008304,-0.545008977960254,
30.6876156947161));
#18602=CARTESIAN_POINT('Ctrl Pts',(1.91954330002405,-0.542574863493146,
30.6877778627617));
#18603=CARTESIAN_POINT('Ctrl Pts',(1.92116396173383,-0.536813313000923,
30.6881608711194));
#18604=CARTESIAN_POINT('Ctrl Pts',(1.9220909265001,-0.533484743532981,30.6883814784617));
#18605=CARTESIAN_POINT('Ctrl Pts',(1.92482762873337,-0.523557993642024,
30.6890374598215));
#18606=CARTESIAN_POINT('Ctrl Pts',(1.92661209615481,-0.516952809482917,
30.689471403394));
#18607=CARTESIAN_POINT('Ctrl Pts',(1.95931465938991,-0.393383053584198,
30.6975444595539));
#18608=CARTESIAN_POINT('Ctrl Pts',(1.97956782976853,-0.273833846997455,
30.7046079769933));
#18609=CARTESIAN_POINT('Ctrl Pts',(1.9965979475928,-0.0527030153000745,
30.7174866778348));
#18610=CARTESIAN_POINT('Ctrl Pts',(1.99671136958516,0.0482033673076015,
30.7232952989587));
#18611=CARTESIAN_POINT('Ctrl Pts',(1.98537695738878,0.199845621745218,30.7323320830419));
#18612=CARTESIAN_POINT('Ctrl Pts',(1.9795804643585,0.250839619821902,30.7354223276943));
#18613=CARTESIAN_POINT('Ctrl Pts',(1.96719461776964,0.331830036590219,30.7404510820538));
#18614=CARTESIAN_POINT('Ctrl Pts',(1.9618673992654,0.361997217729801,30.7423511208136));
#18615=CARTESIAN_POINT('Ctrl Pts',(1.95413690544867,0.400564995504602,30.7448196213694));
#18616=CARTESIAN_POINT('Ctrl Pts',(1.95237002333362,0.409090025516215,30.7453677397847));
#18617=CARTESIAN_POINT('Ctrl Pts',(1.94943037014696,0.422820605588681,30.7462546624203));
#18618=CARTESIAN_POINT('Ctrl Pts',(1.94829240739916,0.428033558181985,30.7465923504312));
#18619=CARTESIAN_POINT('Ctrl Pts',(1.94608178426778,0.437968836955508,30.747237801401));
#18620=CARTESIAN_POINT('Ctrl Pts',(1.94501281433492,0.442691952260742,30.7475454438513));
#18621=CARTESIAN_POINT('Ctrl Pts',(1.94252965595338,0.453480861724678,30.7482500429725));
#18622=CARTESIAN_POINT('Ctrl Pts',(1.94110424019645,0.459543995114412,30.7486473581997));
#18623=CARTESIAN_POINT('Ctrl Pts',(1.93663470927983,0.478163673360718,30.7498716986004));
#18624=CARTESIAN_POINT('Ctrl Pts',(1.93349702365987,0.490697200061785,30.7507017289416));
#18625=CARTESIAN_POINT('Ctrl Pts',(1.90241319493669,0.6099326689843,30.7586556496614));
#18626=CARTESIAN_POINT('Ctrl Pts',(1.86578885299894,0.714155680104044,30.7660656178356));
#18627=CARTESIAN_POINT('Ctrl Pts',(1.7504920215807,0.971796052374219,30.7855151316985));
#18628=CARTESIAN_POINT('Ctrl Pts',(1.66022992120136,1.11903860830284,30.7977858858425));
#18629=CARTESIAN_POINT('Ctrl Pts',(1.54047938103484,1.26739854869901,30.8104301363296));
#18630=CARTESIAN_POINT('Ctrl Pts',(1.52855476108158,1.28175512836226,30.8116561243319));
#18631=CARTESIAN_POINT('Ctrl Pts',(1.51317000171402,1.29975739504236,30.8131942625387));
#18632=CARTESIAN_POINT('Ctrl Pts',(1.50989567813382,1.30355965821875,30.8135191802807));
#18633=CARTESIAN_POINT('Ctrl Pts',(1.50463599353901,1.309620988541,30.8140371624583));
#18634=CARTESIAN_POINT('Ctrl Pts',(1.50265983767933,1.31188795985032,30.8142308948687));
#18635=CARTESIAN_POINT('Ctrl Pts',(1.49889082445507,1.31619193980454,30.8145987006605));
#18636=CARTESIAN_POINT('Ctrl Pts',(1.49709895952063,1.31822973397114,30.8147728399328));
#18637=CARTESIAN_POINT('Ctrl Pts',(1.4929701742655,1.32290590864273,30.8151724425145));
#18638=CARTESIAN_POINT('Ctrl Pts',(1.49063041757929,1.32554175453735,30.8153976906953));
#18639=CARTESIAN_POINT('Ctrl Pts',(1.48436040477098,1.3325676230156,30.8159981408393));
#18640=CARTESIAN_POINT('Ctrl Pts',(1.48041762566146,1.33694649739031,30.8163724232446));
#18641=CARTESIAN_POINT('Ctrl Pts',(1.45228777589943,1.36791065535068,30.8190199880785));
#18642=CARTESIAN_POINT('Ctrl Pts',(1.42740368168694,1.3938574047772,30.8212433878503));
#18643=CARTESIAN_POINT('Ctrl Pts',(1.34747252838203,1.47281475136465,30.8280792903375));
#18644=CARTESIAN_POINT('Ctrl Pts',(1.29007000064105,1.52334724299725,30.8325595986038));
#18645=CARTESIAN_POINT('Ctrl Pts',(1.14781640890008,1.63475275359846,30.8430721567568));
#18646=CARTESIAN_POINT('Ctrl Pts',(1.06081618589832,1.69250328575342,30.8490645059462));
#18647=CARTESIAN_POINT('Ctrl Pts',(0.920949457372957,1.77030843599053,30.8585425940331));
#18648=CARTESIAN_POINT('Ctrl Pts',(0.871084148335126,1.79536946538252,30.8618920317424));
#18649=CARTESIAN_POINT('Ctrl Pts',(0.790577342626261,1.83168603485874,30.867304212372));
#18650=CARTESIAN_POINT('Ctrl Pts',(0.760596238883982,1.84433712651924,30.869320473659));
#18651=CARTESIAN_POINT('Ctrl Pts',(0.722046714252709,1.85950400799374,30.8719195019825));
#18652=CARTESIAN_POINT('Ctrl Pts',(0.713751432085641,1.86270381499112,30.8724791449987));
#18653=CARTESIAN_POINT('Ctrl Pts',(0.700405716205775,1.8677495298035,30.8733802236168));
#18654=CARTESIAN_POINT('Ctrl Pts',(0.695368663239752,1.86963068402178,30.8737204768945));
#18655=CARTESIAN_POINT('Ctrl Pts',(0.685789262623026,1.87316417129478,30.8743678973662));
#18656=CARTESIAN_POINT('Ctrl Pts',(0.681248387502507,1.874820407186,30.8746749316005));
#18657=CARTESIAN_POINT('Ctrl Pts',(0.670913660495918,1.87854738542141,30.8753740620321));
#18658=CARTESIAN_POINT('Ctrl Pts',(0.665116178913216,1.88060785020684,30.8757664968253));
#18659=CARTESIAN_POINT('Ctrl Pts',(0.647477083563837,1.8867851389567,30.8769612881837));
#18660=CARTESIAN_POINT('Ctrl Pts',(0.63560628641287,1.89081711729916,30.8777664430997));
#18661=CARTESIAN_POINT('Ctrl Pts',(0.474428311750013,1.94387274851212,30.8887148909155));
#18662=CARTESIAN_POINT('Ctrl Pts',(0.319907205858484,1.97518669768371,30.8994672139777));
#18663=CARTESIAN_POINT('Ctrl Pts',(0.0728499961683398,1.99548641557686,
30.9167474341474));
#18664=CARTESIAN_POINT('Ctrl Pts',(-0.0180556620561916,1.99673443990206,
30.9231081777207));
#18665=CARTESIAN_POINT('Ctrl Pts',(-0.142959146209348,1.98991587033445,
30.9316428457092));
#18666=CARTESIAN_POINT('Ctrl Pts',(-0.177133731669345,1.98716542383185,
30.9339560064639));
#18667=CARTESIAN_POINT('Ctrl Pts',(-0.230279295259759,1.98150606611897,
30.9375025755029));
#18668=CARTESIAN_POINT('Ctrl Pts',(-0.249306786369179,1.97920212135878,
30.938762136657));
#18669=CARTESIAN_POINT('Ctrl Pts',(-0.273316927669692,1.97594308203664,
30.9403361485827));
#18670=CARTESIAN_POINT('Ctrl Pts',(-0.278332348221803,1.97524284879026,
30.9406640886255));
#18671=CARTESIAN_POINT('Ctrl Pts',(-0.286332199636548,1.97409486610209,
30.9411857514131));
#18672=CARTESIAN_POINT('Ctrl Pts',(-0.289318333071517,1.97365943652027,
30.9413801586184));
#18673=CARTESIAN_POINT('Ctrl Pts',(-0.294985113746101,1.97281998521662,
30.9417484704258));
#18674=CARTESIAN_POINT('Ctrl Pts',(-0.297665892261701,1.97241728041262,
30.9419224441514));
#18675=CARTESIAN_POINT('Ctrl Pts',(-0.303811077270586,1.97148134099633,
30.9423206543658));
#18676=CARTESIAN_POINT('Ctrl Pts',(-0.307274901448389,1.97094443959432,
30.9425446808002));
#18677=CARTESIAN_POINT('Ctrl Pts',(-0.318223433167899,1.96921782560283,
30.9432514775746));
#18678=CARTESIAN_POINT('Ctrl Pts',(-0.32570289680005,1.96799456948557,30.9437323853592));
#18679=CARTESIAN_POINT('Ctrl Pts',(-0.453220661742656,1.94639231382624,
30.9519010928209));
#18680=CARTESIAN_POINT('Ctrl Pts',(-0.571172914234161,1.91510398424772,
30.9590062235002));
#18681=CARTESIAN_POINT('Ctrl Pts',(-0.779934036278527,1.83870388260991,
30.971913531284));
#18682=CARTESIAN_POINT('Ctrl Pts',(-0.871570577203989,1.79707892404917,
30.977708657515));
#18683=CARTESIAN_POINT('Ctrl Pts',(-1.00437105303593,1.72419999591981,30.9867132523392));
#18684=CARTESIAN_POINT('Ctrl Pts',(-1.04810647246567,1.69796910002529,30.9897847281217));
#18685=CARTESIAN_POINT('Ctrl Pts',(-1.1163151962039,1.65341998241997,30.994785598706));
#18686=CARTESIAN_POINT('Ctrl Pts',(-1.14145669976805,1.63616432573231,30.9966770699671));
#18687=CARTESIAN_POINT('Ctrl Pts',(-1.17324378991871,1.61325823280222,30.9991359287365));
#18688=CARTESIAN_POINT('Ctrl Pts',(-1.18026236019065,1.60813055239652,30.9996831705399));
#18689=CARTESIAN_POINT('Ctrl Pts',(-1.19153232237129,1.59978333655726,31.0005690165759));
#18690=CARTESIAN_POINT('Ctrl Pts',(-1.19580476153005,1.59659229942491,31.0009065095651));
#18691=CARTESIAN_POINT('Ctrl Pts',(-1.20393313718495,1.59047037751699,31.0015518153356));
#18692=CARTESIAN_POINT('Ctrl Pts',(-1.20779130059531,1.58754250150899,31.0018595085681));
#18693=CARTESIAN_POINT('Ctrl Pts',(-1.21659132000148,1.58081371179655,31.0025645454249));
#18694=CARTESIAN_POINT('Ctrl Pts',(-1.22152607713847,1.5770036375097,31.0029622491975));
#18695=CARTESIAN_POINT('Ctrl Pts',(-1.23665677050138,1.56520775759385,31.004188959543));
#18696=CARTESIAN_POINT('Ctrl Pts',(-1.2467926984259,1.55714586550453,31.0050209881958));
#18697=CARTESIAN_POINT('Ctrl Pts',(-1.3444485473297,1.47790778560608,31.0131390546253));
#18698=CARTESIAN_POINT('Ctrl Pts',(-1.42584497091852,1.39953974556395,31.0207249829138));
#18699=CARTESIAN_POINT('Ctrl Pts',(-1.60699223410081,1.19284118011406,31.0396813484366));
#18700=CARTESIAN_POINT('Ctrl Pts',(-1.69855696436631,1.05839457902608,31.051215189611));
#18701=CARTESIAN_POINT('Ctrl Pts',(-1.78433231401984,0.892083818100652,
31.0637132140072));
#18702=CARTESIAN_POINT('Ctrl Pts',(-1.79539737586752,0.86959976587737,31.0653672913686));
#18703=CARTESIAN_POINT('Ctrl Pts',(-1.80838329073121,0.841907352272181,
31.067356243298));
#18704=CARTESIAN_POINT('Ctrl Pts',(-1.81070933565115,0.836892955853869,
31.0677144837592));
#18705=CARTESIAN_POINT('Ctrl Pts',(-1.81431587511598,0.829032692511845,
31.0682729848755));
#18706=CARTESIAN_POINT('Ctrl Pts',(-1.81561056394719,0.82619342793486,31.0684741041768));
#18707=CARTESIAN_POINT('Ctrl Pts',(-1.81801013308818,0.820898270458103,
31.0688480147248));
#18708=CARTESIAN_POINT('Ctrl Pts',(-1.81911669132216,0.818443203857005,
31.0690209061598));
#18709=CARTESIAN_POINT('Ctrl Pts',(-1.8216082945035,0.812885188778279,31.0694112595866));
#18710=CARTESIAN_POINT('Ctrl Pts',(-1.82299038087419,0.809780945934544,
31.0696285384681));
#18711=CARTESIAN_POINT('Ctrl Pts',(-1.82704226331502,0.800617246149869,
31.0702678082462));
#18712=CARTESIAN_POINT('Ctrl Pts',(-1.8296898609783,0.794547935859148,31.0706884628325));
#18713=CARTESIAN_POINT('Ctrl Pts',(-1.84771682335492,0.752655252470618,
31.0735738540965));
#18714=CARTESIAN_POINT('Ctrl Pts',(-1.86207456068305,0.716398079434474,
31.0759801010687));
#18715=CARTESIAN_POINT('Ctrl Pts',(-1.93366207878036,0.518892619388813,
31.0887229589495));
#18716=CARTESIAN_POINT('Ctrl Pts',(-1.97103251085257,0.351200079802946,
31.0983088032602));
#18717=CARTESIAN_POINT('Ctrl Pts',(-1.99199024364157,0.12090298573795,31.1119603016667));
#18718=CARTESIAN_POINT('Ctrl Pts',(-1.99472892756107,0.0608133453232126,
31.1155593179837));
#18719=CARTESIAN_POINT('Ctrl Pts',(-1.99476161122894,-0.0329699496448909,
31.1212980005034));
#18720=CARTESIAN_POINT('Ctrl Pts',(-1.99392110288183,-0.0666282922424112,
31.1233817344041));
#18721=CARTESIAN_POINT('Ctrl Pts',(-1.99176245094213,-0.109527298676257,
31.1260746683796));
#18722=CARTESIAN_POINT('Ctrl Pts',(-1.99123068893374,-0.118803320202428,
31.1266591688895));
#18723=CARTESIAN_POINT('Ctrl Pts',(-1.99027977406249,-0.133583107009423,
31.1275941251489));
#18724=CARTESIAN_POINT('Ctrl Pts',(-1.98990254352114,-0.139089510067221,
31.1279432641407));
#18725=CARTESIAN_POINT('Ctrl Pts',(-1.9891535798515,-0.149394658826164,
31.1285982157194));
#18726=CARTESIAN_POINT('Ctrl Pts',(-1.98878732101095,-0.154193772381355,
31.1289038541489));
#18727=CARTESIAN_POINT('Ctrl Pts',(-1.98793081947946,-0.164905483622833,
31.1295874664061));
#18728=CARTESIAN_POINT('Ctrl Pts',(-1.98743156155206,-0.17081729554009,
31.129965720991));
#18729=CARTESIAN_POINT('Ctrl Pts',(-1.98589097507003,-0.188137823472534,
31.1310768227705));
#18730=CARTESIAN_POINT('Ctrl Pts',(-1.98477774199113,-0.199539748630938,
31.1318119227424));
#18731=CARTESIAN_POINT('Ctrl Pts',(-1.9750825026045,-0.290712347049115,
31.1377201748076));
#18732=CARTESIAN_POINT('Ctrl Pts',(-1.96179428833453,-0.369898289376839,
31.1430415488625));
#18733=CARTESIAN_POINT('Ctrl Pts',(-1.92076118483009,-0.547908037891753,
31.1554441052938));
#18734=CARTESIAN_POINT('Ctrl Pts',(-1.8900879170194,-0.64582593183677,31.162590044847));
#18735=CARTESIAN_POINT('Ctrl Pts',(-1.8089546633255,-0.848622853619035,
31.1778265384721));
#18736=CARTESIAN_POINT('Ctrl Pts',(-1.75656185825405,-0.95235233947074,
31.1858893772912));
#18737=CARTESIAN_POINT('Ctrl Pts',(-1.69139589264723,-1.0574812221192,31.1939664512548));
#18738=CARTESIAN_POINT('Ctrl Pts',(-1.68730992401064,-1.0639886398782,31.1944659542551));
#18739=CARTESIAN_POINT('Ctrl Pts',(-1.68129477289349,-1.07344672613286,
31.195191083263));
#18740=CARTESIAN_POINT('Ctrl Pts',(-1.67939527139257,-1.07641604879225,
31.1954186090028));
#18741=CARTESIAN_POINT('Ctrl Pts',(-1.67601952907078,-1.08166236152653,
31.1958203662638));
#18742=CARTESIAN_POINT('Ctrl Pts',(-1.67454650166678,-1.0839413915343,31.1959948095547));
#18743=CARTESIAN_POINT('Ctrl Pts',(-1.67143129868892,-1.08873964710231,
31.1963619000435));
#18744=CARTESIAN_POINT('Ctrl Pts',(-1.66978807998935,-1.09125816085304,
31.1965544754713));
#18745=CARTESIAN_POINT('Ctrl Pts',(-1.66538832977033,-1.09796832451124,
31.1970673118286));
#18746=CARTESIAN_POINT('Ctrl Pts',(-1.66262164745684,-1.10215334200357,
31.197386899192));
#18747=CARTESIAN_POINT('Ctrl Pts',(-1.64949489575883,-1.12184758998798,
31.1988898378255));
#18748=CARTESIAN_POINT('Ctrl Pts',(-1.63893301141333,-1.13722208525549,
31.2000601680128));
#18749=CARTESIAN_POINT('Ctrl Pts',(-1.52880180633214,-1.29281351054718,
31.2118985563979));
#18750=CARTESIAN_POINT('Ctrl Pts',(-1.41169782662066,-1.41976390645456,
31.2215601666435));
#18751=CARTESIAN_POINT('Ctrl Pts',(-1.19512902499347,-1.60089388611909,
31.2380750574649));
#18752=CARTESIAN_POINT('Ctrl Pts',(-1.10480553221594,-1.66451019209258,
31.2446527987425));
#18753=CARTESIAN_POINT('Ctrl Pts',(-0.998552940405137,-1.72687189089505,
31.2523431478212));
#18754=CARTESIAN_POINT('Ctrl Pts',(-0.987346834026734,-1.73330341232639,
31.2531534616558));
#18755=CARTESIAN_POINT('Ctrl Pts',(-0.970647347051169,-1.74267325810439,
31.2543602214951));
#18756=CARTESIAN_POINT('Ctrl Pts',(-0.965201255853096,-1.74569553219334,
31.2547536516862));
#18757=CARTESIAN_POINT('Ctrl Pts',(-0.955495897536749,-1.75102215949897,
31.2554545986315));
#18758=CARTESIAN_POINT('Ctrl Pts',(-0.951242206671017,-1.75333661252938,
31.255761751733));
#18759=CARTESIAN_POINT('Ctrl Pts',(-0.94228405452954,-1.75816859056641,
31.2564085026703));
#18760=CARTESIAN_POINT('Ctrl Pts',(-0.937577841947787,-1.76068277144161,
31.2567482163119));
#18761=CARTESIAN_POINT('Ctrl Pts',(-0.925166228396138,-1.76724950378136,
31.2576440107137));
#18762=CARTESIAN_POINT('Ctrl Pts',(-0.917444351300789,-1.77127050928435,
31.2582012012529));
#18763=CARTESIAN_POINT('Ctrl Pts',(-0.882436988769638,-1.78920952658631,
31.2607268786577));
#18764=CARTESIAN_POINT('Ctrl Pts',(-0.854860700788525,-1.80254785730686,
31.2627155268454));
#18765=CARTESIAN_POINT('Ctrl Pts',(-0.78030175782316,-1.83651541931024,
31.2680933192741));
#18766=CARTESIAN_POINT('Ctrl Pts',(-0.732814525939007,-1.85597463156181,
31.2715200394762));
#18767=CARTESIAN_POINT('Ctrl Pts',(-0.589948822745992,-1.90817981500322,
31.2818293976884));
#18768=CARTESIAN_POINT('Ctrl Pts',(-0.492785294275005,-1.93554880165563,
31.2888489631142));
#18769=CARTESIAN_POINT('Ctrl Pts',(-0.31055985986979,-1.97226301299191,
31.3018182539593));
#18770=CARTESIAN_POINT('Ctrl Pts',(-0.226145057893152,-1.98371598325275,
31.3077486088162));
#18771=CARTESIAN_POINT('Ctrl Pts',(-0.104000930112791,-1.9923870143389,
31.3160252832614));
#18772=CARTESIAN_POINT('Ctrl Pts',(-0.0666797487889978,-1.99398507070906,
31.318513038267));
#18773=CARTESIAN_POINT('Ctrl Pts',(-0.0233727295804408,-1.99462197154133,
31.3213358046737));
#18774=CARTESIAN_POINT('Ctrl Pts',(-0.0174121017075229,-1.99468291082677,
31.3217229134923));
#18775=CARTESIAN_POINT('Ctrl Pts',(-0.00790670810490513,-1.99473747904275,
31.3223378959271));
#18776=CARTESIAN_POINT('Ctrl Pts',(-0.0043621354115291,-1.99474837976677,
31.3225667050627));
#18777=CARTESIAN_POINT('Ctrl Pts',(0.00189893929976689,-1.99475094577658,
31.3229699314499));
#18778=CARTESIAN_POINT('Ctrl Pts',(0.00461541722253504,-1.99474651019386,
31.3231445657359));
#18779=CARTESIAN_POINT('Ctrl Pts',(0.0103288967384952,-1.99472550952791,
31.3235112032417));
#18780=CARTESIAN_POINT('Ctrl Pts',(0.0133258654602947,-1.99470773951213,
31.3237031379598));
#18781=CARTESIAN_POINT('Ctrl Pts',(0.0212939952866249,-1.99464253505055,
31.3242124501749));
#18782=CARTESIAN_POINT('Ctrl Pts',(0.0262650786026712,-1.99458327070993,
31.3245291703128));
#18783=CARTESIAN_POINT('Ctrl Pts',(0.0494035287369734,-1.994220899404,31.3259988236147));
#18784=CARTESIAN_POINT('Ctrl Pts',(0.0675671473895573,-1.99368815045075,
31.3271394256868));
#18785=CARTESIAN_POINT('Ctrl Pts',(0.241673483147874,-1.98619924508064,
31.3379688731667));
#18786=CARTESIAN_POINT('Ctrl Pts',(0.396322512233222,-1.96120799433469,
31.3468203829917));
#18787=CARTESIAN_POINT('Ctrl Pts',(0.668230310714495,-1.88375123072126,
31.3632796418581));
#18788=CARTESIAN_POINT('Ctrl Pts',(0.786372787210431,-1.83756943174109,
31.3707668742538));
#18789=CARTESIAN_POINT('Ctrl Pts',(0.910950628707126,-1.77464527598959,
31.3794778856057));
#18790=CARTESIAN_POINT('Ctrl Pts',(0.922508205036043,-1.768664892623,31.380293946435));
#18791=CARTESIAN_POINT('Ctrl Pts',(0.9395257587789,-1.75964710414976,31.3815076347467));
#18792=CARTESIAN_POINT('Ctrl Pts',(0.945031470324931,-1.75669635999092,
31.3819021952866));
#18793=CARTESIAN_POINT('Ctrl Pts',(0.954782659815761,-1.75141117618418,
31.3826044159038));
#18794=CARTESIAN_POINT('Ctrl Pts',(0.959033682556298,-1.74908702773522,
31.3829117075387));
#18795=CARTESIAN_POINT('Ctrl Pts',(0.967940325547837,-1.74417529479058,
31.3835579967661));
#18796=CARTESIAN_POINT('Ctrl Pts',(0.972594126987176,-1.74158450728703,
31.3838971072994));
#18797=CARTESIAN_POINT('Ctrl Pts',(0.984790681146831,-1.73473051071344,
31.384789604866));
#18798=CARTESIAN_POINT('Ctrl Pts',(0.992316067389571,-1.73043677981765,
31.3853440869163));
#18799=CARTESIAN_POINT('Ctrl Pts',(1.02595722414324,-1.71095066460426,31.3878401516244));
#18800=CARTESIAN_POINT('Ctrl Pts',(1.05175260086252,-1.69521582769805,31.3898013207235));
#18801=CARTESIAN_POINT('Ctrl Pts',(1.11955404455345,-1.65171457975108,31.3950870229719));
#18802=CARTESIAN_POINT('Ctrl Pts',(1.16088075581609,-1.62293483096847,31.3984475676285));
#18803=CARTESIAN_POINT('Ctrl Pts',(1.28094432433038,-1.53238934424328,31.4086318343161));
#18804=CARTESIAN_POINT('Ctrl Pts',(1.35616562476787,-1.46623563772346,31.4155927916674));
#18805=CARTESIAN_POINT('Ctrl Pts',(1.51227113446591,-1.30661846339647,31.4311702917142));
#18806=CARTESIAN_POINT('Ctrl Pts',(1.59010096463137,-1.21070317562561,31.4397668142298));
#18807=CARTESIAN_POINT('Ctrl Pts',(1.66278311415867,-1.10192421029253,31.4483081012237));
#18808=CARTESIAN_POINT('Ctrl Pts',(1.66694508326684,-1.09561797345798,31.4487992025702));
#18809=CARTESIAN_POINT('Ctrl Pts',(1.67298291261794,-1.08635537106709,31.4495144323402));
#18810=CARTESIAN_POINT('Ctrl Pts',(1.67488691938656,-1.0834175676466,31.4497403889765));
#18811=CARTESIAN_POINT('Ctrl Pts',(1.67825123764825,-1.0781964994122,31.4501403587169));
#18812=CARTESIAN_POINT('Ctrl Pts',(1.67971463995098,-1.07591525535121,31.450314577153));
#18813=CARTESIAN_POINT('Ctrl Pts',(1.68279889382045,-1.07108569507647,31.4506822621726));
#18814=CARTESIAN_POINT('Ctrl Pts',(1.68441860454787,-1.068536685468,31.45087565288));
#18815=CARTESIAN_POINT('Ctrl Pts',(1.68874437659218,-1.06169475117012,31.451392975273));
#18816=CARTESIAN_POINT('Ctrl Pts',(1.69143987832476,-1.05739512648215,31.4517162125306));
#18817=CARTESIAN_POINT('Ctrl Pts',(1.70429856072879,-1.03670911002054,31.4532626778878));
#18818=CARTESIAN_POINT('Ctrl Pts',(1.71424061994018,-1.02018553545962,31.4544719522605));
#18819=CARTESIAN_POINT('Ctrl Pts',(1.74133536787651,-0.973639588628749,
31.4578139384052));
#18820=CARTESIAN_POINT('Ctrl Pts',(1.7579500889906,-0.94331049498492,31.4599180227951));
#18821=CARTESIAN_POINT('Ctrl Pts',(1.81570467359106,-0.83105163146685,31.4674973916642));
#18822=CARTESIAN_POINT('Ctrl Pts',(1.85197477854992,-0.746740896551033,
31.4727975064046));
#18823=CARTESIAN_POINT('Ctrl Pts',(1.93387665227392,-0.513238090566147,
31.4871489607838));
#18824=CARTESIAN_POINT('Ctrl Pts',(1.96803228989639,-0.360737962115578,
31.4962243243801));
#18825=CARTESIAN_POINT('Ctrl Pts',(1.9854000917869,-0.193318893556025,31.5067350360599));
#18826=CARTESIAN_POINT('Ctrl Pts',(1.98657939846431,-0.180798233188507,
31.5075239625511));
#18827=CARTESIAN_POINT('Ctrl Pts',(1.9881598890501,-0.162128870647861,31.5087049036983));
#18828=CARTESIAN_POINT('Ctrl Pts',(1.9886511197695,-0.155987940499084,31.5090940891839));
#18829=CARTESIAN_POINT('Ctrl Pts',(1.98947704994391,-0.145024141891785,
31.5097902819723));
#18830=CARTESIAN_POINT('Ctrl Pts',(1.98982267984085,-0.140202125881214,
31.5100969435755));
#18831=CARTESIAN_POINT('Ctrl Pts',(1.990515392184,-0.130018842934366,31.5107455680417));
#18832=CARTESIAN_POINT('Ctrl Pts',(1.9908583505561,-0.124657342861111,31.511087657839));
#18833=CARTESIAN_POINT('Ctrl Pts',(1.99171018268322,-0.110439169708111,
31.511996440212));
#18834=CARTESIAN_POINT('Ctrl Pts',(1.99218163557418,-0.101580454187658,
31.5125643014764));
#18835=CARTESIAN_POINT('Ctrl Pts',(1.99409664275567,-0.0604256581406491,
31.515210242771));
#18836=CARTESIAN_POINT('Ctrl Pts',(1.99481396147143,-0.0281022429469557,
31.5173109107531));
#18837=CARTESIAN_POINT('Ctrl Pts',(1.99462848699205,0.0595108459868649,
31.5230696566777));
#18838=CARTESIAN_POINT('Ctrl Pts',(1.99221291629348,0.114765431808765,31.5267721887616));
#18839=CARTESIAN_POINT('Ctrl Pts',(1.9786568764814,0.273397176545756,31.5375973993595));
#18840=CARTESIAN_POINT('Ctrl Pts',(1.9617288349155,0.376092801969814,31.5448548867649));
#18841=CARTESIAN_POINT('Ctrl Pts',(1.91982099236979,0.546264088238355,31.5570762498082));
#18842=CARTESIAN_POINT('Ctrl Pts',(1.89905670194791,0.614574610478577,31.5620342278734));
#18843=CARTESIAN_POINT('Ctrl Pts',(1.87180484754695,0.689525026096684,31.5674433288023));
#18844=CARTESIAN_POINT('Ctrl Pts',(1.86888403523982,0.697402764452382,31.5680114404149));
#18845=CARTESIAN_POINT('Ctrl Pts',(1.85393417509735,0.736955652157489,31.5708609669836));
#18846=CARTESIAN_POINT('Ctrl Pts',(1.84114838143125,0.768341417690629,31.5731128651521));
#18847=CARTESIAN_POINT('Ctrl Pts',(1.825248821063,0.804691122415102,31.5756976405419));
#18848=CARTESIAN_POINT('Ctrl Pts',(1.82290627416089,0.809983813984174,31.5760734080373));
#18849=CARTESIAN_POINT('Ctrl Pts',(1.81911278480998,0.818454913064945,31.5766738015535));
#18850=CARTESIAN_POINT('Ctrl Pts',(1.81767649248571,0.821639785855652,31.5768992959467));
#18851=CARTESIAN_POINT('Ctrl Pts',(1.81511154039312,0.827287736378873,31.5772987410034));
#18852=CARTESIAN_POINT('Ctrl Pts',(1.81398622271243,0.829752304600239,31.5774728951019));
#18853=CARTESIAN_POINT('Ctrl Pts',(1.81159425920694,0.834962841633406,31.5778407641809));
#18854=CARTESIAN_POINT('Ctrl Pts',(1.8103263931149,0.837708217454025,31.5780344020515));
#18855=CARTESIAN_POINT('Ctrl Pts',(1.80690679726172,0.845068824695993,31.5785530849939));
#18856=CARTESIAN_POINT('Ctrl Pts',(1.80474361190948,0.849678756419764,31.5788774292591));
#18857=CARTESIAN_POINT('Ctrl Pts',(1.79422115995368,0.871881513028842,31.5804373605036));
#18858=CARTESIAN_POINT('Ctrl Pts',(1.7856218200629,0.889360291550394,31.5816586982367));
#18859=CARTESIAN_POINT('Ctrl Pts',(1.76082648907991,0.937948576875685,31.5850427452575));
#18860=CARTESIAN_POINT('Ctrl Pts',(1.74406351044277,0.968762217277947,31.5871759463878));
#18861=CARTESIAN_POINT('Ctrl Pts',(1.6793539848186,1.0805813788873,31.5949278823048));
#18862=CARTESIAN_POINT('Ctrl Pts',(1.62650269323416,1.15861006759258,31.6003629717028));
#18863=CARTESIAN_POINT('Ctrl Pts',(1.4741393642354,1.35247112854636,31.6146650352651));
#18864=CARTESIAN_POINT('Ctrl Pts',(1.36653146868423,1.46111179526675,31.6235619180456));
#18865=CARTESIAN_POINT('Ctrl Pts',(1.23772666560627,1.56435954324196,31.6338692246638));
#18866=CARTESIAN_POINT('Ctrl Pts',(1.22776598683763,1.57218915816348,31.6346639562076));
#18867=CARTESIAN_POINT('Ctrl Pts',(1.21283747479742,1.58369536325086,31.6358519105663));
#18868=CARTESIAN_POINT('Ctrl Pts',(1.20792591540474,1.58744471568395,31.6362422541167));
#18869=CARTESIAN_POINT('Ctrl Pts',(1.19913902701572,1.59408799907364,31.6369397392887));
#18870=CARTESIAN_POINT('Ctrl Pts',(1.19527042730956,1.59699078263677,31.6372465303173));
#18871=CARTESIAN_POINT('Ctrl Pts',(1.18709063689994,1.60308207373148,31.6378946209762));
#18872=CARTESIAN_POINT('Ctrl Pts',(1.18277707606709,1.60626731982539,31.6382360444444));
#18873=CARTESIAN_POINT('Ctrl Pts',(1.17150506883954,1.61452084020461,31.6391273782408));
#18874=CARTESIAN_POINT('Ctrl Pts',(1.16452662147575,1.61956148811715,31.6396783519874));
#18875=CARTESIAN_POINT('Ctrl Pts',(1.14915533829825,1.63051370881752,31.6408902213807));
#18876=CARTESIAN_POINT('Ctrl Pts',(1.14074909498099,1.63640595266676,31.6415518392329));
#18877=CARTESIAN_POINT('Ctrl Pts',(1.11578178752173,1.65362058048429,31.6435137726419));
#18878=CARTESIAN_POINT('Ctrl Pts',(1.09909537341397,1.66475804039522,31.6448209789791));
#18879=CARTESIAN_POINT('Ctrl Pts',(1.03961029349712,1.70317758601556,31.6494680590969));
#18880=CARTESIAN_POINT('Ctrl Pts',(0.995944244245937,1.72907425543426,31.6528566974803));
#18881=CARTESIAN_POINT('Ctrl Pts',(0.819969521404237,1.82455950937282,31.666420412365));
#18882=CARTESIAN_POINT('Ctrl Pts',(0.68100801141268,1.88084745961469,31.676977320569));
#18883=CARTESIAN_POINT('Ctrl Pts',(0.46675892014263,1.94074642214977,31.6923454881173));
#18884=CARTESIAN_POINT('Ctrl Pts',(0.395392680491269,1.95653463536107,31.6973140243895));
#18885=CARTESIAN_POINT('Ctrl Pts',(0.315812509173411,1.96960600202633,31.702580553906));
#18886=CARTESIAN_POINT('Ctrl Pts',(0.308304467064475,1.97079519592032,31.7030747501903));
#18887=CARTESIAN_POINT('Ctrl Pts',(0.297266964541532,1.9724787989843,31.7037971522802));
#18888=CARTESIAN_POINT('Ctrl Pts',(0.293742796407353,1.97300669808625,31.7040271937461));
#18889=CARTESIAN_POINT('Ctrl Pts',(0.287526848072439,1.97392078580919,31.7044318364722));
#18890=CARTESIAN_POINT('Ctrl Pts',(0.284835669729489,1.97431091741512,31.7046066598221));
#18891=CARTESIAN_POINT('Ctrl Pts',(0.279186113964529,1.97511812353048,31.7049728891172));
#18892=CARTESIAN_POINT('Ctrl Pts',(0.276227601326714,1.97553405454891,31.7051642296273));
#18893=CARTESIAN_POINT('Ctrl Pts',(0.26838537885304,1.97661861477747,31.7056702739139));
#18894=CARTESIAN_POINT('Ctrl Pts',(0.263500067111318,1.97727579658209,31.705984335218));
#18895=CARTESIAN_POINT('Ctrl Pts',(0.241394414231006,1.98016610999669,31.7074003129144));
#18896=CARTESIAN_POINT('Ctrl Pts',(0.224147152122042,1.98219252093038,31.7084910317905));
#18897=CARTESIAN_POINT('Ctrl Pts',(0.177025709124408,1.98710596697326,31.7114380964622));
#18898=CARTESIAN_POINT('Ctrl Pts',(0.147108356580656,1.98954456057873,31.7132732349823));
#18899=CARTESIAN_POINT('Ctrl Pts',(0.0438243656781907,1.9956206098865,31.7195197359325));
#18900=CARTESIAN_POINT('Ctrl Pts',(-0.0296846664218811,1.99588139112504,
31.7238125094491));
#18901=CARTESIAN_POINT('Ctrl Pts',(-0.231575504118225,1.98543814595198,
31.7355605813361));
#18902=CARTESIAN_POINT('Ctrl Pts',(-0.35915154540047,1.96636708545194,31.7429565556513));
#18903=CARTESIAN_POINT('Ctrl Pts',(-0.489162829433394,1.93384994966077,
31.7510296138392));
#18904=CARTESIAN_POINT('Ctrl Pts',(-0.494321966244416,1.93253763080756,
31.7513508270761));
#18905=CARTESIAN_POINT('Ctrl Pts',(-0.547525015231715,1.91877749789665,
31.754672430475));
#18906=CARTESIAN_POINT('Ctrl Pts',(-0.595090240832385,1.90456233695754,
31.757719614464));
#18907=CARTESIAN_POINT('Ctrl Pts',(-0.651226834633883,1.88547729968685,
31.7614303712885));
#18908=CARTESIAN_POINT('Ctrl Pts',(-0.6603576727969,1.88229880106584,31.7620375981266));
#18909=CARTESIAN_POINT('Ctrl Pts',(-0.675236709955617,1.87699773314875,
31.7630332409085));
#18910=CARTESIAN_POINT('Ctrl Pts',(-0.680998944901184,1.87491480883781,
31.7634203397282));
#18911=CARTESIAN_POINT('Ctrl Pts',(-0.691286782467627,1.87114229338679,
31.7641142131815));
#18912=CARTESIAN_POINT('Ctrl Pts',(-0.695816035630299,1.86946274143192,
31.7644206509254));
#18913=CARTESIAN_POINT('Ctrl Pts',(-0.705387508850471,1.8658738152518,31.7650702824904));
#18914=CARTESIAN_POINT('Ctrl Pts',(-0.710428169980008,1.86396041976275,
31.7654136089461));
#18915=CARTESIAN_POINT('Ctrl Pts',(-0.72338247670079,1.85898288574999,31.7662990923728));
#18916=CARTESIAN_POINT('Ctrl Pts',(-0.731284374631854,1.85588866498951,
31.7668422561172));
#18917=CARTESIAN_POINT('Ctrl Pts',(-0.767167960746504,1.84157263896357,
31.769322880701));
#18918=CARTESIAN_POINT('Ctrl Pts',(-0.794911509966742,1.82976828871729,
31.7712799077328));
#18919=CARTESIAN_POINT('Ctrl Pts',(-0.868300506866143,1.79655858791936,
31.776565498473));
#18920=CARTESIAN_POINT('Ctrl Pts',(-0.913417500753582,1.7740451741792,31.7799303033142));
#18921=CARTESIAN_POINT('Ctrl Pts',(-1.03578884163965,1.7070756619626,31.7893781633339));
#18922=CARTESIAN_POINT('Ctrl Pts',(-1.11098733074868,1.65911739166735,31.7955588969136));
#18923=CARTESIAN_POINT('Ctrl Pts',(-1.28322350500532,1.53229934263323,31.8104770178804));
#18924=CARTESIAN_POINT('Ctrl Pts',(-1.37656752317831,1.44902442193596,31.8192216794944));
#18925=CARTESIAN_POINT('Ctrl Pts',(-1.47114721374974,1.34720207922994,31.8283894168494));
#18926=CARTESIAN_POINT('Ctrl Pts',(-1.48066187909967,1.33673781807645,31.8293153497696));
#18927=CARTESIAN_POINT('Ctrl Pts',(-1.49319632535118,1.32265433253208,31.8305390479337));
#18928=CARTESIAN_POINT('Ctrl Pts',(-1.49631544689657,1.31912464683561,31.8308438853024));
#18929=CARTESIAN_POINT('Ctrl Pts',(-1.5011670570152,1.31359507833088,31.8313185091842));
#18930=CARTESIAN_POINT('Ctrl Pts',(-1.50290809294974,1.31160277036519,31.8314889262303));
#18931=CARTESIAN_POINT('Ctrl Pts',(-1.50624487384275,1.30776904673698,31.831815711239));
#18932=CARTESIAN_POINT('Ctrl Pts',(-1.50784119014367,1.30592819288101,31.8319721200723));
#18933=CARTESIAN_POINT('Ctrl Pts',(-1.51165352281501,1.30151554504969,31.8323458435939));
#18934=CARTESIAN_POINT('Ctrl Pts',(-1.51386634857698,1.29894101717877,31.8325629204929));
#18935=CARTESIAN_POINT('Ctrl Pts',(-1.52050776387904,1.29117399150973,31.8332149466197));
#18936=CARTESIAN_POINT('Ctrl Pts',(-1.52491634669059,1.28596433668023,31.8336484456093));
#18937=CARTESIAN_POINT('Ctrl Pts',(-1.55774094453056,1.24676909900251,31.8368821570024));
#18938=CARTESIAN_POINT('Ctrl Pts',(-1.58504700276328,1.21186498156154,31.8396064832872));
#18939=CARTESIAN_POINT('Ctrl Pts',(-1.65353665537894,1.11803740971378,31.8466186035995));
#18940=CARTESIAN_POINT('Ctrl Pts',(-1.6927389853383,1.05774631889586,31.8508209615641));
#18941=CARTESIAN_POINT('Ctrl Pts',(-1.76233776563529,0.936889773050073,
31.8589277130956));
#18942=CARTESIAN_POINT('Ctrl Pts',(-1.79307194369008,0.876635478967391,
31.8628298354817));
#18943=CARTESIAN_POINT('Ctrl Pts',(-1.86718057560378,0.711066249269365,
31.8734281650186));
#18944=CARTESIAN_POINT('Ctrl Pts',(-1.90469293873118,0.603421726761332,
31.8802027303199));
#18945=CARTESIAN_POINT('Ctrl Pts',(-1.93602775299199,0.480616393460285,
31.8881135814245));
#18946=CARTESIAN_POINT('Ctrl Pts',(-1.93910990009059,0.468026025727867,
31.8889264749027));
#18947=CARTESIAN_POINT('Ctrl Pts',(-1.94349290799761,0.449334813640755,
31.8901363451999));
#18948=CARTESIAN_POINT('Ctrl Pts',(-1.94488825245045,0.443256294069004,
31.8905302833063));
#18949=CARTESIAN_POINT('Ctrl Pts',(-1.94731658961138,0.432445514538081,
31.8912318021872));
#18950=CARTESIAN_POINT('Ctrl Pts',(-1.94836089941323,0.427715826430847,
31.8915390171575));
#18951=CARTESIAN_POINT('Ctrl Pts',(-1.9505184963178,0.417772166165348,31.8921855587713));
#18952=CARTESIAN_POINT('Ctrl Pts',(-1.95162812518011,0.412557447389252,
31.8925249999285));
#18953=CARTESIAN_POINT('Ctrl Pts',(-1.95383721984987,0.401967391309332,
31.8932151275237));
#18954=CARTESIAN_POINT('Ctrl Pts',(-1.95493543980102,0.396591843789078,
31.8935658506495));
#18955=CARTESIAN_POINT('Ctrl Pts',(-1.95759427977766,0.383297969662468,
31.89443424546));
#18956=CARTESIAN_POINT('Ctrl Pts',(-1.95912903714579,0.375374626731649,
31.8949527378347));
#18957=CARTESIAN_POINT('Ctrl Pts',(-1.96623799565932,0.337442314827941,
31.8974395116789));
#18958=CARTESIAN_POINT('Ctrl Pts',(-1.97117076890211,0.307318727113851,
31.8994280055389));
#18959=CARTESIAN_POINT('Ctrl Pts',(-1.98837368233782,0.184679224694825,
31.9075830637462));
#18960=CARTESIAN_POINT('Ctrl Pts',(-1.99483390543644,0.0914821201817975,
31.9139244644951));
#18961=CARTESIAN_POINT('Ctrl Pts',(-1.99474917736343,-0.00181160368489115,
31.9203782084164));
#18962=CARTESIAN_POINT('',(-1.99474925803387,0.00172048636055072,33.5209548813952));
#18963=CARTESIAN_POINT('Ctrl Pts',(-1.99474917872611,-0.00181010262051109,
31.9203781045778));
#18964=CARTESIAN_POINT('Ctrl Pts',(-1.99460252920774,-0.16341917550937,
31.9315576712192));
#18965=CARTESIAN_POINT('Ctrl Pts',(-1.97481767395285,-0.324419874890402,
31.9430492725144));
#18966=CARTESIAN_POINT('Ctrl Pts',(-1.93294150007795,-0.492856000596897,
31.9545502494962));
#18967=CARTESIAN_POINT('Ctrl Pts',(-1.92995931024995,-0.504407530381109,
31.9553359810977));
#18968=CARTESIAN_POINT('Ctrl Pts',(-1.92533025441611,-0.521695868119121,
31.9565066885494));
#18969=CARTESIAN_POINT('Ctrl Pts',(-1.92376104628966,-0.527452942263791,
31.9568956620103));
#18970=CARTESIAN_POINT('Ctrl Pts',(-1.92083256957472,-0.538009932115742,
31.9576072193171));
#18971=CARTESIAN_POINT('Ctrl Pts',(-1.91948108940886,-0.542811934376364,
31.957930226192));
#18972=CARTESIAN_POINT('Ctrl Pts',(-1.91728779153198,-0.550494406747934,
31.9584458809308));
#18973=CARTESIAN_POINT('Ctrl Pts',(-1.91645747436394,-0.553378095578015,
31.9586391864287));
#18974=CARTESIAN_POINT('Ctrl Pts',(-1.91486342593632,-0.558867601387181,
31.9590066786028));
#18975=CARTESIAN_POINT('Ctrl Pts',(-1.91410089066589,-0.561473700453169,
31.9591809291117));
#18976=CARTESIAN_POINT('Ctrl Pts',(-1.91233281169241,-0.567470960080185,
31.9595814419069));
#18977=CARTESIAN_POINT('Ctrl Pts',(-1.91132356872471,-0.570861007004688,
31.9598074857575));
#18978=CARTESIAN_POINT('Ctrl Pts',(-1.90859668714099,-0.579932301769424,
31.9604114478899));
#18979=CARTESIAN_POINT('Ctrl Pts',(-1.90686268444612,-0.585608652263019,
31.9607884295772));
#18980=CARTESIAN_POINT('Ctrl Pts',(-1.89419062109161,-0.626438211830169,
31.9634937694718));
#18981=CARTESIAN_POINT('Ctrl Pts',(-1.88230572916969,-0.661293052708772,
31.9657697635236));
#18982=CARTESIAN_POINT('Ctrl Pts',(-1.86528990525225,-0.707010738500025,
31.9687351437457));
#18983=CARTESIAN_POINT('Ctrl Pts',(-1.86101709121346,-0.718182436511426,
31.9694581646588));
#18984=CARTESIAN_POINT('Ctrl Pts',(-1.84774248610002,-0.7519760751726,31.9716422706262));
#18985=CARTESIAN_POINT('Ctrl Pts',(-1.83842659305895,-0.77447275424995,
31.9730921712081));
#18986=CARTESIAN_POINT('Ctrl Pts',(-1.79448605613852,-0.875319534647171,
31.9795966136992));
#18987=CARTESIAN_POINT('Ctrl Pts',(-1.75524759582562,-0.95156265087637,
31.9845311265067));
#18988=CARTESIAN_POINT('Ctrl Pts',(-1.68091434912792,-1.0756553270946,31.9929320771693));
#18989=CARTESIAN_POINT('Ctrl Pts',(-1.64837183615551,-1.12488989467681,
31.9963721626078));
#18990=CARTESIAN_POINT('Ctrl Pts',(-1.56949208003522,-1.2334410527669,32.004323521974));
#18991=CARTESIAN_POINT('Ctrl Pts',(-1.52188760685677,-1.29171916462684,
32.0088642042278));
#18992=CARTESIAN_POINT('Ctrl Pts',(-1.46022191589947,-1.35905831162468,
32.0145429407434));
#18993=CARTESIAN_POINT('Ctrl Pts',(-1.44918911949883,-1.37081669449004,
32.0155515798706));
#18994=CARTESIAN_POINT('Ctrl Pts',(-1.43432210778034,-1.3862813750418,32.0169017064251));
#18995=CARTESIAN_POINT('Ctrl Pts',(-1.43061362308862,-1.39010813255543,
32.0172377533172));
#18996=CARTESIAN_POINT('Ctrl Pts',(-1.4237314943523,-1.39715304198638,32.0178600586814));
#18997=CARTESIAN_POINT('Ctrl Pts',(-1.42056215296713,-1.40037536387611,
32.0181461281878));
#18998=CARTESIAN_POINT('Ctrl Pts',(-1.41398778118754,-1.40701435135392,
32.0187385012264));
#18999=CARTESIAN_POINT('Ctrl Pts',(-1.41058125726587,-1.41042948999318,
32.0190448696595));
#19000=CARTESIAN_POINT('Ctrl Pts',(-1.40286752908041,-1.41810682835442,
32.0197373480939));
#19001=CARTESIAN_POINT('Ctrl Pts',(-1.39855323826709,-1.42236181021825,
32.0201237721689));
#19002=CARTESIAN_POINT('Ctrl Pts',(-1.38746265193813,-1.43320068990382,
32.0211149418448));
#19003=CARTESIAN_POINT('Ctrl Pts',(-1.38065890500309,-1.43975616372936,
32.0217209185731));
#19004=CARTESIAN_POINT('Ctrl Pts',(-1.34032893501446,-1.4780657068254,32.0253011037511));
#19005=CARTESIAN_POINT('Ctrl Pts',(-1.30575726045412,-1.5086938974447,32.0283230096475));
#19006=CARTESIAN_POINT('Ctrl Pts',(-1.26283843678116,-1.54413623642788,
32.0320230364921));
#19007=CARTESIAN_POINT('Ctrl Pts',(-1.25547757605955,-1.55012699004072,
32.0326558418));
#19008=CARTESIAN_POINT('Ctrl Pts',(-1.22678999376674,-1.57313646426422,
32.0351152222687));
#19009=CARTESIAN_POINT('Ctrl Pts',(-1.20515842159974,-1.58976888156951,
32.0369551975045));
#19010=CARTESIAN_POINT('Ctrl Pts',(-1.1075329151385,-1.66169497587215,32.0451928170896));
#19011=CARTESIAN_POINT('Ctrl Pts',(-1.02803340041024,-1.71201754397389,
32.0517340861286));
#19012=CARTESIAN_POINT('Ctrl Pts',(-0.876292452786206,-1.79367738510105,
32.063757075621));
#19013=CARTESIAN_POINT('Ctrl Pts',(-0.805163029398242,-1.82671310937933,
32.0692220707789));
#19014=CARTESIAN_POINT('Ctrl Pts',(-0.702995319109108,-1.86703393796488,
32.0766957938108));
#19015=CARTESIAN_POINT('Ctrl Pts',(-0.673448107138935,-1.8778940398252,
32.0788145500876));
#19016=CARTESIAN_POINT('Ctrl Pts',(-0.626652773150874,-1.89384701632228,
32.0820908752231));
#19017=CARTESIAN_POINT('Ctrl Pts',(-0.609572685989556,-1.89941343982065,
32.0832704101091));
#19018=CARTESIAN_POINT('Ctrl Pts',(-0.587650401972819,-1.9062317558416,
32.0847615362654));
#19019=CARTESIAN_POINT('Ctrl Pts',(-0.582876170339136,-1.90769700772375,
32.0850848999818));
#19020=CARTESIAN_POINT('Ctrl Pts',(-0.575223217954676,-1.91001435184936,
32.0856009893714));
#19021=CARTESIAN_POINT('Ctrl Pts',(-0.572348028118944,-1.91087788980509,
32.0857943746047));
#19022=CARTESIAN_POINT('Ctrl Pts',(-0.566868817688548,-1.91251004638703,
32.0861619249559));
#19023=CARTESIAN_POINT('Ctrl Pts',(-0.564265209478509,-1.91327982988665,
32.0863361542917));
#19024=CARTESIAN_POINT('Ctrl Pts',(-0.558268326463397,-1.91503956410968,
32.0867364952955));
#19025=CARTESIAN_POINT('Ctrl Pts',(-0.554873988370586,-1.91602581244035,
32.0869623891513));
#19026=CARTESIAN_POINT('Ctrl Pts',(-0.545780951681496,-1.91864166678052,
32.0875656887129));
#19027=CARTESIAN_POINT('Ctrl Pts',(-0.540077527244917,-1.9202549204255,
32.0879421610499));
#19028=CARTESIAN_POINT('Ctrl Pts',(-0.4990570264107,-1.93166063937621,32.0906365277402));
#19029=CARTESIAN_POINT('Ctrl Pts',(-0.463480527727685,-1.94050430400641,
32.0929025339778));
#19030=CARTESIAN_POINT('Ctrl Pts',(-0.357583642502776,-1.96374933176799,
32.0994942583546));
#19031=CARTESIAN_POINT('Ctrl Pts',(-0.286704381305827,-1.97534293697457,
32.103709992737));
#19032=CARTESIAN_POINT('Ctrl Pts',(-0.0893910275549665,-1.99676975127825,
32.1152687563291));
#19033=CARTESIAN_POINT('Ctrl Pts',(0.0375775172028492,-1.99841604695161,
32.1225262440107));
#19034=CARTESIAN_POINT('Ctrl Pts',(0.207362483962403,-1.98442313844537,
32.1327173192462));
#19035=CARTESIAN_POINT('Ctrl Pts',(0.250750174591868,-1.97940858510854,
32.1353624102951));
#19036=CARTESIAN_POINT('Ctrl Pts',(0.311766711138105,-1.97031826397244,
32.1391598462591));
#19037=CARTESIAN_POINT('Ctrl Pts',(0.329559857134827,-1.96742034443492,
32.1402765781414));
#19038=CARTESIAN_POINT('Ctrl Pts',(0.360680684387621,-1.96191777278961,
32.142247536168));
#19039=CARTESIAN_POINT('Ctrl Pts',(0.374025763436493,-1.95941741777467,
32.1430984687277));
#19040=CARTESIAN_POINT('Ctrl Pts',(0.393572809090104,-1.95554808800512,
32.1443537219922));
#19041=CARTESIAN_POINT('Ctrl Pts',(0.399795615123871,-1.95428537966441,
32.1447546545595));
#19042=CARTESIAN_POINT('Ctrl Pts',(0.410788308822708,-1.95200008315828,
32.1454652923288));
#19043=CARTESIAN_POINT('Ctrl Pts',(0.415560695784435,-1.95098966341245,
32.1457746061943));
#19044=CARTESIAN_POINT('Ctrl Pts',(0.424815088748768,-1.94899480764177,
32.1463759797159));
#19045=CARTESIAN_POINT('Ctrl Pts',(0.429297502412028,-1.94801239053715,
32.1466679728914));
#19046=CARTESIAN_POINT('Ctrl Pts',(0.4412202199058,-1.94535612163037,32.1474465668618));
#19047=CARTESIAN_POINT('Ctrl Pts',(0.448654325315004,-1.9436550661366,32.1479340382652));
#19048=CARTESIAN_POINT('Ctrl Pts',(0.475306592498861,-1.93739549973819,
32.1496889902946));
#19049=CARTESIAN_POINT('Ctrl Pts',(0.494466041284157,-1.93259436163314,
32.1509642443329));
#19050=CARTESIAN_POINT('Ctrl Pts',(0.518108159569669,-1.9262953419642,32.1525553853301));
#19051=CARTESIAN_POINT('Ctrl Pts',(0.522661483916753,-1.92506487736978,
32.1528626380069));
#19052=CARTESIAN_POINT('Ctrl Pts',(0.532138335301516,-1.92246780551564,
32.1535038191477));
#19053=CARTESIAN_POINT('Ctrl Pts',(0.537061056009767,-1.92109840780178,
32.1538378344566));
#19054=CARTESIAN_POINT('Ctrl Pts',(0.746345972827151,-1.86201245102816,
32.1680790841398));
#19055=CARTESIAN_POINT('Ctrl Pts',(0.940164518691378,-1.77205298992048,
32.1831462798589));
#19056=CARTESIAN_POINT('Ctrl Pts',(1.15327514841124,-1.62818825993466,32.2008387844464));
#19057=CARTESIAN_POINT('Ctrl Pts',(1.18960681367958,-1.60183544162223,32.2038918576719));
#19058=CARTESIAN_POINT('Ctrl Pts',(1.24322178855893,-1.56011505909323,32.208419867963));
#19059=CARTESIAN_POINT('Ctrl Pts',(1.2611764906913,-1.54563688704249,32.2099402012554));
#19060=CARTESIAN_POINT('Ctrl Pts',(1.28303408548211,-1.52737698035299,32.2117918319514));
#19061=CARTESIAN_POINT('Ctrl Pts',(1.28717707561612,-1.5238871619295,32.2121428349445));
#19062=CARTESIAN_POINT('Ctrl Pts',(1.29366567520833,-1.51837619485871,32.2126925497014));
#19063=CARTESIAN_POINT('Ctrl Pts',(1.29602084382523,-1.51636642043307,32.2128920770251));
#19064=CARTESIAN_POINT('Ctrl Pts',(1.3004180102707,-1.51259638671973,32.2132645791995));
#19065=CARTESIAN_POINT('Ctrl Pts',(1.30246109610733,-1.5108374908643,32.2134376470236));
#19066=CARTESIAN_POINT('Ctrl Pts',(1.30709781585268,-1.50682933605535,32.2138304033565));
#19067=CARTESIAN_POINT('Ctrl Pts',(1.30968920694528,-1.50457752536953,32.2140498993328));
#19068=CARTESIAN_POINT('Ctrl Pts',(1.31638830382908,-1.49872586809576,32.2146173411055));
#19069=CARTESIAN_POINT('Ctrl Pts',(1.32048709491006,-1.49511579083626,32.2149645406434));
#19070=CARTESIAN_POINT('Ctrl Pts',(1.34561735429383,-1.47279794790838,32.2170937382671));
#19071=CARTESIAN_POINT('Ctrl Pts',(1.36626698134848,-1.45366247508109,32.2188453447964));
#19072=CARTESIAN_POINT('Ctrl Pts',(1.52841085904421,-1.2968992086817,32.232683053994));
#19073=CARTESIAN_POINT('Ctrl Pts',(1.64918308215051,-1.13938762449178,32.2436132713659));
#19074=CARTESIAN_POINT('Ctrl Pts',(1.76937314968082,-0.922444594052505,
32.2583606975573));
#19075=CARTESIAN_POINT('Ctrl Pts',(1.7921895088438,-0.877292170717651,32.261408478619));
#19076=CARTESIAN_POINT('Ctrl Pts',(1.82589763842589,-0.803768787432854,
32.2663741237908));
#19077=CARTESIAN_POINT('Ctrl Pts',(1.83790050341204,-0.775930431535747,
32.2682547491953));
#19078=CARTESIAN_POINT('Ctrl Pts',(1.85251591244637,-0.739788888702187,
32.2707013980596));
#19079=CARTESIAN_POINT('Ctrl Pts',(1.85571536527151,-0.731726236361655,
32.2712475246266));
#19080=CARTESIAN_POINT('Ctrl Pts',(1.86079517436667,-0.718677449071006,
32.2721320010526));
#19081=CARTESIAN_POINT('Ctrl Pts',(1.86270833973315,-0.713704138238731,
32.272469245974));
#19082=CARTESIAN_POINT('Ctrl Pts',(1.86632270486252,-0.704194995302186,
32.2731143680412));
#19083=CARTESIAN_POINT('Ctrl Pts',(1.86802735586801,-0.699660508491388,
32.2734221268617));
#19084=CARTESIAN_POINT('Ctrl Pts',(1.87189071192426,-0.689268953521005,
32.2741277253156));
#19085=CARTESIAN_POINT('Ctrl Pts',(1.874038466982,-0.683407894660107,32.2745259271383));
#19086=CARTESIAN_POINT('Ctrl Pts',(1.88057104249785,-0.665318624547086,
32.275755679142));
#19087=CARTESIAN_POINT('Ctrl Pts',(1.8848638787623,-0.653057779460557,32.2765902731791));
#19088=CARTESIAN_POINT('Ctrl Pts',(1.93001052458401,-0.519959299641784,
32.2856633390346));
#19089=CARTESIAN_POINT('Ctrl Pts',(1.95929563314645,-0.395534648478494,
32.2942905487739));
#19090=CARTESIAN_POINT('Ctrl Pts',(1.99745154162072,-0.11537668503847,32.3138866368626));
#19091=CARTESIAN_POINT('Ctrl Pts',(2.0003749271544,0.0403581757162858,32.3249010773372));
#19092=CARTESIAN_POINT('Ctrl Pts',(1.98343881142725,0.212900461363933,32.3363915194624));
#19093=CARTESIAN_POINT('Ctrl Pts',(1.98142222563669,0.230915884995325,32.337581849748));
#19094=CARTESIAN_POINT('Ctrl Pts',(1.97854045645687,0.253830450614741,32.3390817747177));
#19095=CARTESIAN_POINT('Ctrl Pts',(1.97790224287163,0.258756554367711,32.3394033910826));
#19096=CARTESIAN_POINT('Ctrl Pts',(1.97684958585329,0.266650058701996,32.3399173520342));
#19097=CARTESIAN_POINT('Ctrl Pts',(1.9764468513592,0.269618958787515,32.3401103467698));
#19098=CARTESIAN_POINT('Ctrl Pts',(1.9756661743089,0.275278242874885,32.3404776139538));
#19099=CARTESIAN_POINT('Ctrl Pts',(1.97528942918531,0.27796872906143,32.3406519487306));
#19100=CARTESIAN_POINT('Ctrl Pts',(1.97440821043105,0.284169593650608,32.3410531389782));
#19101=CARTESIAN_POINT('Ctrl Pts',(1.97389987136427,0.287679400854737,32.3412797735571));
#19102=CARTESIAN_POINT('Ctrl Pts',(1.97251110822302,0.297091058185662,32.3418863475102));
#19103=CARTESIAN_POINT('Ctrl Pts',(1.97161354931177,0.302990401265001,32.3422653375212));
#19104=CARTESIAN_POINT('Ctrl Pts',(1.96488639775802,0.345909598558773,32.3450142944206));
#19105=CARTESIAN_POINT('Ctrl Pts',(1.95804060256359,0.382765520545583,32.3473299829406));
#19106=CARTESIAN_POINT('Ctrl Pts',(1.93229126099402,0.50249418724707,32.3547696227162));
#19107=CARTESIAN_POINT('Ctrl Pts',(1.90912974723013,0.584359455018703,32.3597275441746));
#19108=CARTESIAN_POINT('Ctrl Pts',(1.84724713772239,0.759512377896457,32.3705144928822));
#19109=CARTESIAN_POINT('Ctrl Pts',(1.80652972150162,0.851839357662067,32.3763231316148));
#19110=CARTESIAN_POINT('Ctrl Pts',(1.73481793027285,0.985934443870743,32.3853599576982));
#19111=CARTESIAN_POINT('Ctrl Pts',(1.7088874064594,1.03022483231553,32.3884502268421));
#19112=CARTESIAN_POINT('Ctrl Pts',(1.66479579497099,1.09928195182521,32.3934790175597));
#19113=CARTESIAN_POINT('Ctrl Pts',(1.64771989280784,1.12471545022883,32.3953790674676));
#19114=CARTESIAN_POINT('Ctrl Pts',(1.62504771948245,1.15685922677724,32.3978475805561));
#19115=CARTESIAN_POINT('Ctrl Pts',(1.61998310947063,1.16394075550822,32.3983957000973));
#19116=CARTESIAN_POINT('Ctrl Pts',(1.61174009998203,1.17530842025117,32.3992826241084));
#19117=CARTESIAN_POINT('Ctrl Pts',(1.60859053886871,1.17961540764901,32.3996203123622));
#19118=CARTESIAN_POINT('Ctrl Pts',(1.60254961999386,1.187807109193,32.4002657634995));
#19119=CARTESIAN_POINT('Ctrl Pts',(1.59966131801297,1.19169403798347,32.4005734058732));
#19120=CARTESIAN_POINT('Ctrl Pts',(1.59302583627002,1.20055613824791,32.4012780043997));
#19121=CARTESIAN_POINT('Ctrl Pts',(1.58926946538158,1.20552433449504,32.401675319107));
#19122=CARTESIAN_POINT('Ctrl Pts',(1.57764953966693,1.22074420934558,32.4028996563797));
#19123=CARTESIAN_POINT('Ctrl Pts',(1.56970972536805,1.23093698445045,32.4037296840909));
#19124=CARTESIAN_POINT('Ctrl Pts',(1.49304891595192,1.32740275463032,32.4116834009324));
#19125=CARTESIAN_POINT('Ctrl Pts',(1.41739477913876,1.40789833920321,32.4190931509539));
#19126=CARTESIAN_POINT('Ctrl Pts',(1.20773083437981,1.59687059640301,32.4385423439482));
#19127=CARTESIAN_POINT('Ctrl Pts',(1.06561989148885,1.69501168981905,32.450813010916));
#19128=CARTESIAN_POINT('Ctrl Pts',(0.896085979347844,1.78224741857242,32.463457483311));
#19129=CARTESIAN_POINT('Ctrl Pts',(0.879369522662083,1.79055445270757,32.4646837191852));
#19130=CARTESIAN_POINT('Ctrl Pts',(0.858013506626741,1.80079581462543,32.466222122607));
#19131=CARTESIAN_POINT('Ctrl Pts',(0.853480582225938,1.80294859622175,32.4665470629523));
#19132=CARTESIAN_POINT('Ctrl Pts',(0.846218045305775,1.80636420107997,32.4670650726523));
#19133=CARTESIAN_POINT('Ctrl Pts',(0.843493654461969,1.80763797877819,32.4672588101046));
#19134=CARTESIAN_POINT('Ctrl Pts',(0.838305621625072,1.81004933929399,32.4676266196097));
#19135=CARTESIAN_POINT('Ctrl Pts',(0.835842569635021,1.81118804236173,32.4678007575777));
#19136=CARTESIAN_POINT('Ctrl Pts',(0.830175153705129,1.81379414419,32.4682003494771));
#19137=CARTESIAN_POINT('Ctrl Pts',(0.82696922151543,1.81525807819708,32.4684255883185));
#19138=CARTESIAN_POINT('Ctrl Pts',(0.816764217709754,1.8198853723048,32.4691400675413));
#19139=CARTESIAN_POINT('Ctrl Pts',(0.809750641604358,1.82301685638878,32.4696273873885));
#19140=CARTESIAN_POINT('Ctrl Pts',(0.696326753875739,1.87287563856048,32.4774512653194));
#19141=CARTESIAN_POINT('Ctrl Pts',(0.586032626659973,1.91026400213153,32.4842576744113));
#19142=CARTESIAN_POINT('Ctrl Pts',(0.37366553422335,1.96211034209167,32.4969613709237));
#19143=CARTESIAN_POINT('Ctrl Pts',(0.272519811608386,1.97869525897723,32.502852902173));
#19144=CARTESIAN_POINT('Ctrl Pts',(0.117426383721725,1.99200439431928,32.512088663048));
#19145=CARTESIAN_POINT('Ctrl Pts',(0.0641449312344817,1.99443105205114,
32.5152954628198));
#19146=CARTESIAN_POINT('Ctrl Pts',(-0.0206624008000958,1.99489163263012,
32.5204970118216));
#19147=CARTESIAN_POINT('Ctrl Pts',(-0.0521560952106073,1.99431670743821,
32.5224497923833));
#19148=CARTESIAN_POINT('Ctrl Pts',(-0.0924053732654867,1.99262793786886,
32.5249775869389));
#19149=CARTESIAN_POINT('Ctrl Pts',(-0.101186429457066,1.99220133377433,
32.5255310185995));
#19150=CARTESIAN_POINT('Ctrl Pts',(-0.115310827594806,1.99142151449313,
32.5264244672017));
#19151=CARTESIAN_POINT('Ctrl Pts',(-0.120656134923171,1.99110480174702,
32.5267633376429));
#19152=CARTESIAN_POINT('Ctrl Pts',(-0.130828596879996,1.99046096392345,
32.5274096829841));
#19153=CARTESIAN_POINT('Ctrl Pts',(-0.135655970521717,1.99013779112121,
32.5277170315977));
#19154=CARTESIAN_POINT('Ctrl Pts',(-0.146659476612136,1.98936093024505,
32.5284190447982));
#19155=CARTESIAN_POINT('Ctrl Pts',(-0.152834744385373,1.98889603859645,
32.5288140585213));
#19156=CARTESIAN_POINT('Ctrl Pts',(-0.171705819438603,1.98738696475351,
32.5300244141063));
#19157=CARTESIAN_POINT('Ctrl Pts',(-0.184393678265809,1.9862499326624,32.5308426623224));
#19158=CARTESIAN_POINT('Ctrl Pts',(-0.209671478215072,1.98374035800143,
32.5324820331688));
#19159=CARTESIAN_POINT('Ctrl Pts',(-0.222260971720968,1.9823692857021,32.5333030731097));
#19160=CARTESIAN_POINT('Ctrl Pts',(-0.381563468186005,1.96348371912612,
32.5437511959232));
#19161=CARTESIAN_POINT('Ctrl Pts',(-0.525875533563065,1.9298439829871,32.5539033747445));
#19162=CARTESIAN_POINT('Ctrl Pts',(-0.748316915354061,1.85117160846283,
32.5703567213781));
#19163=CARTESIAN_POINT('Ctrl Pts',(-0.829469932932192,1.81625864628333,
32.576532693651));
#19164=CARTESIAN_POINT('Ctrl Pts',(-0.93792137154601,1.76081141065677,32.5848375287752));
#19165=CARTESIAN_POINT('Ctrl Pts',(-0.967407486900249,1.74478547497055,
32.5871003654876));
#19166=CARTESIAN_POINT('Ctrl Pts',(-1.01282855005604,1.71859308044977,32.5905784648162));
#19167=CARTESIAN_POINT('Ctrl Pts',(-1.0290462240517,1.70893176601492,32.5918187427292));
#19168=CARTESIAN_POINT('Ctrl Pts',(-1.04941580267103,1.69640190187168,32.5933721623471));
#19169=CARTESIAN_POINT('Ctrl Pts',(-1.05369662545826,1.69374625089209,32.5936983764786));
#19170=CARTESIAN_POINT('Ctrl Pts',(-1.06052067794381,1.68947699747894,32.5942179375137));
#19171=CARTESIAN_POINT('Ctrl Pts',(-1.06307035749912,1.68787382486348,32.5944119594439));
#19172=CARTESIAN_POINT('Ctrl Pts',(-1.06790935141657,1.68481587622807,32.5947799808687));
#19173=CARTESIAN_POINT('Ctrl Pts',(-1.07019930113276,1.68336222351895,32.594954047644));
#19174=CARTESIAN_POINT('Ctrl Pts',(-1.07545096872875,1.68001343426015,32.5953530461423));
#19175=CARTESIAN_POINT('Ctrl Pts',(-1.07841064327152,1.67811513620968,32.595577764936));
#19176=CARTESIAN_POINT('Ctrl Pts',(-1.0877826054208,1.67206904366776,32.5962889424361));
#19177=CARTESIAN_POINT('Ctrl Pts',(-1.09417619705265,1.6678921840968,32.5967735056396));
#19178=CARTESIAN_POINT('Ctrl Pts',(-1.19955079536049,1.59818547145711,32.604752462756));
#19179=CARTESIAN_POINT('Ctrl Pts',(-1.29252904310272,1.52397399843088,32.6116934166522));
#19180=CARTESIAN_POINT('Ctrl Pts',(-1.45175067020464,1.3717704282141,32.6244883012895));
#19181=CARTESIAN_POINT('Ctrl Pts',(-1.51967224776997,1.2961208804621,32.630336566891));
#19182=CARTESIAN_POINT('Ctrl Pts',(-1.61338813931342,1.17419664340804,32.6394681910315));
#19183=CARTESIAN_POINT('Ctrl Pts',(-1.64359552490643,1.13152647364536,32.6426139009881));
#19184=CARTESIAN_POINT('Ctrl Pts',(-1.68901936743565,1.06169905722731,32.6477249611765));
#19185=CARTESIAN_POINT('Ctrl Pts',(-1.70533701470487,1.0352858601333,32.6496501971835));
#19186=CARTESIAN_POINT('Ctrl Pts',(-1.72545342597985,1.00095681779064,32.6521470383302));
#19187=CARTESIAN_POINT('Ctrl Pts',(-1.72982608843033,0.993380982386406,
32.6526977129275));
#19188=CARTESIAN_POINT('Ctrl Pts',(-1.73679007928916,0.981130139438561,
32.6535877751254));
#19189=CARTESIAN_POINT('Ctrl Pts',(-1.73941272486202,0.976472990774916,
32.6539260319847));
#19190=CARTESIAN_POINT('Ctrl Pts',(-1.74437477108422,0.967578239889731,
32.654571910364));
#19191=CARTESIAN_POINT('Ctrl Pts',(-1.74671752989929,0.963342546743949,
32.6548794085877));
#19192=CARTESIAN_POINT('Ctrl Pts',(-1.75203120629353,0.953652343689352,
32.6555827496625));
#19193=CARTESIAN_POINT('Ctrl Pts',(-1.7549920998638,0.948192421623277,32.6559789464901));
#19194=CARTESIAN_POINT('Ctrl Pts',(-1.76399174393227,0.931410406796379,
32.6571964794157));
#19195=CARTESIAN_POINT('Ctrl Pts',(-1.76994669050432,0.920043976410978,
32.6580207723699));
#19196=CARTESIAN_POINT('Ctrl Pts',(-1.823175507855,0.816014608763925,32.6655631253834));
#19197=CARTESIAN_POINT('Ctrl Pts',(-1.86323516851332,0.719859141452695,
32.6725342699386));
#19198=CARTESIAN_POINT('Ctrl Pts',(-1.94773814415773,0.461926119686491,
32.6911894243867));
#19199=CARTESIAN_POINT('Ctrl Pts',(-1.97962349760519,0.296898541243526,
32.7031229913283));
#19200=CARTESIAN_POINT('Ctrl Pts',(-1.99236283910541,0.101583410512929,
32.7162383097549));
#19201=CARTESIAN_POINT('Ctrl Pts',(-1.99360388671717,0.0732981554110923,
32.7181113729829));
#19202=CARTESIAN_POINT('Ctrl Pts',(-1.99437183448897,0.0392611111762049,
32.7203262884057));
#19203=CARTESIAN_POINT('Ctrl Pts',(-1.99447646588938,0.0335272730109116,
32.7206980781848));
#19204=CARTESIAN_POINT('Ctrl Pts',(-1.99460047908786,0.0246274957505847,
32.7212730016537));
#19205=CARTESIAN_POINT('Ctrl Pts',(-1.99463705283118,0.0214618857429049,
32.7214770771693));
#19206=CARTESIAN_POINT('Ctrl Pts',(-1.99469075505927,0.0156072187183045,
32.7218537091782));
#19207=CARTESIAN_POINT('Ctrl Pts',(-1.99470998215074,0.0129182376887925,
32.7220263790629));
#19208=CARTESIAN_POINT('Ctrl Pts',(-1.99474089383969,0.00689035271397881,
32.7224127566872));
#19209=CARTESIAN_POINT('Ctrl Pts',(-1.99474963291524,0.00355146445775524,
32.7226262972717));
#19210=CARTESIAN_POINT('Ctrl Pts',(-1.99475068666113,-0.00633823889024117,
32.7232574286588));
#19211=CARTESIAN_POINT('Ctrl Pts',(-1.99471911541581,-0.0128890916739229,
32.7236737035634));
#19212=CARTESIAN_POINT('Ctrl Pts',(-1.99419126645478,-0.0670500302154172,
32.7271015191955));
#19213=CARTESIAN_POINT('Ctrl Pts',(-1.99202275248162,-0.114632995312579,
32.7300246171534));
#19214=CARTESIAN_POINT('Ctrl Pts',(-1.98147383093918,-0.244017678124576,
32.7378416200914));
#19215=CARTESIAN_POINT('Ctrl Pts',(-1.96973736723722,-0.325453161411386,
32.7426199669138));
#19216=CARTESIAN_POINT('Ctrl Pts',(-1.92122278996094,-0.55886227595734,
32.7564518222252));
#19217=CARTESIAN_POINT('Ctrl Pts',(-1.87159144210308,-0.707504260175679,
32.765477840962));
#19218=CARTESIAN_POINT('Ctrl Pts',(-1.79612707593495,-0.86798806934733,
32.7764498410277));
#19219=CARTESIAN_POINT('Ctrl Pts',(-1.7868141226834,-0.887001126595059,
32.7777695626261));
#19220=CARTESIAN_POINT('Ctrl Pts',(-1.77363745489507,-0.912852290322353,
32.7795928394159));
#19221=CARTESIAN_POINT('Ctrl Pts',(-1.77003314329996,-0.919821609950433,
32.7800873026031));
#19222=CARTESIAN_POINT('Ctrl Pts',(-1.76423606829243,-0.930870618268236,
32.7808759446446));
#19223=CARTESIAN_POINT('Ctrl Pts',(-1.76207002545037,-0.934964297413323,
32.7811691777283));
#19224=CARTESIAN_POINT('Ctrl Pts',(-1.75760286506079,-0.943336276271809,
32.7817710207486));
#19225=CARTESIAN_POINT('Ctrl Pts',(-1.75530033774357,-0.947613784741125,
32.7820796792714));
#19226=CARTESIAN_POINT('Ctrl Pts',(-1.74995553255246,-0.957456749030787,
32.7827926296714));
#19227=CARTESIAN_POINT('Ctrl Pts',(-1.74690230167209,-0.963016167596326,
32.783197310371));
#19228=CARTESIAN_POINT('Ctrl Pts',(-1.73726226688231,-0.980372341362477,
32.7844670310505));
#19229=CARTESIAN_POINT('Ctrl Pts',(-1.73058220030843,-0.992116598329498,
32.7853354084742));
#19230=CARTESIAN_POINT('Ctrl Pts',(-1.6639604327434,-1.10652428336738,32.7938870200653));
#19231=CARTESIAN_POINT('Ctrl Pts',(-1.59508479454828,-1.20368418472471,
32.8019045945793));
#19232=CARTESIAN_POINT('Ctrl Pts',(-1.43637719390949,-1.3898455920855,32.8188180254318));
#19233=CARTESIAN_POINT('Ctrl Pts',(-1.34590099732977,-1.47763342105424,
32.827700295468));
#19234=CARTESIAN_POINT('Ctrl Pts',(-1.20755873497289,-1.58854794168747,
32.8398112385958));
#19235=CARTESIAN_POINT('Ctrl Pts',(-1.16611853459211,-1.61921316900989,
32.8432742835422));
#19236=CARTESIAN_POINT('Ctrl Pts',(-1.11758059817273,-1.65229932750113,
32.8471069350772));
#19237=CARTESIAN_POINT('Ctrl Pts',(-1.11160590301737,-1.65632478134333,
32.8475749726356));
#19238=CARTESIAN_POINT('Ctrl Pts',(-1.10272079340768,-1.66224139596949,
32.848265330155));
#19239=CARTESIAN_POINT('Ctrl Pts',(-1.09982712406865,-1.66415741572107,
32.8484892781032));
#19240=CARTESIAN_POINT('Ctrl Pts',(-1.09467367350379,-1.66755041868017,
32.8488865238553));
#19241=CARTESIAN_POINT('Ctrl Pts',(-1.09241588527345,-1.66903037247035,
32.8490600201042));
#19242=CARTESIAN_POINT('Ctrl Pts',(-1.0875825448234,-1.67218456124697,32.849430269065));
#19243=CARTESIAN_POINT('Ctrl Pts',(-1.08500613622704,-1.67385742622816,
32.8496269299387));
#19244=CARTESIAN_POINT('Ctrl Pts',(-1.07796794535264,-1.67840425347671,
32.8501622879692));
#19245=CARTESIAN_POINT('Ctrl Pts',(-1.07349850129062,-1.68126639726621,
32.8505002041631));
#19246=CARTESIAN_POINT('Ctrl Pts',(-1.05040334891452,-1.69592643406822,
32.8522360801427));
#19247=CARTESIAN_POINT('Ctrl Pts',(-1.0315935084831,-1.70743333596848,32.8536156240066));
#19248=CARTESIAN_POINT('Ctrl Pts',(-0.976513497681212,-1.73988587053753,
32.8575687182072));
#19249=CARTESIAN_POINT('Ctrl Pts',(-0.939768080325111,-1.7600050828664,
32.8600993798385));
#19250=CARTESIAN_POINT('Ctrl Pts',(-0.785688438822215,-1.83816542656085,
32.870390761747));
#19251=CARTESIAN_POINT('Ctrl Pts',(-0.663413815999872,-1.88574766924444,
32.8778317420061));
#19252=CARTESIAN_POINT('Ctrl Pts',(-0.435704190833042,-1.94944363914821,
32.8916870073637));
#19253=CARTESIAN_POINT('Ctrl Pts',(-0.331972647945805,-1.96976092875029,
32.8979960345232));
#19254=CARTESIAN_POINT('Ctrl Pts',(-0.214358417116515,-1.98324060158836,
32.9053862394449));
#19255=CARTESIAN_POINT('Ctrl Pts',(-0.201573367325775,-1.9845808071326,
32.9061924891071));
#19256=CARTESIAN_POINT('Ctrl Pts',(-0.182588713962379,-1.98638555135478,
32.9073943468194));
#19257=CARTESIAN_POINT('Ctrl Pts',(-0.176398279230839,-1.98694485146446,
32.9077869749619));
#19258=CARTESIAN_POINT('Ctrl Pts',(-0.16538204776158,-1.98788827050524,
32.9084870199819));
#19259=CARTESIAN_POINT('Ctrl Pts',(-0.160557255096413,-1.98828377373377,
32.9087940766024));
#19260=CARTESIAN_POINT('Ctrl Pts',(-0.15040497052267,-1.98907879406862,
32.9094411641322));
#19261=CARTESIAN_POINT('Ctrl Pts',(-0.145077225054335,-1.98947447885776,
32.9097813129042));
#19262=CARTESIAN_POINT('Ctrl Pts',(-0.131033105283022,-1.99046080387404,
32.9106794859957));
#19263=CARTESIAN_POINT('Ctrl Pts',(-0.122314404320698,-1.99101558730885,
32.9112386307938));
#19264=CARTESIAN_POINT('Ctrl Pts',(-0.0827081835528079,-1.99327465749413,
32.9137859005555));
#19265=CARTESIAN_POINT('Ctrl Pts',(-0.0517886577081614,-1.99431749228319,
32.9157946116533));
#19266=CARTESIAN_POINT('Ctrl Pts',(0.0311472345365564,-1.99518478656018,
32.9212399758421));
#19267=CARTESIAN_POINT('Ctrl Pts',(0.0831504487442948,-1.9936944850378,
32.9247153769912));
#19268=CARTESIAN_POINT('Ctrl Pts',(0.236166979560229,-1.98331238039391,
32.935116328932));
#19269=CARTESIAN_POINT('Ctrl Pts',(0.336623421845106,-1.9687519423375,32.9421785250825));
#19270=CARTESIAN_POINT('Ctrl Pts',(0.551925368442719,-1.92058123250234,
32.9575707618174));
#19271=CARTESIAN_POINT('Ctrl Pts',(0.665766651990023,-1.88414855313876,
32.9658755854131));
#19272=CARTESIAN_POINT('Ctrl Pts',(0.782011449260053,-1.83508388634968,
32.9741142567833));
#19273=CARTESIAN_POINT('Ctrl Pts',(0.788328179477207,-1.83237918059498,
32.9745611147245));
#19274=CARTESIAN_POINT('Ctrl Pts',(0.797806947325723,-1.82826246123259,
32.9752302722609));
#19275=CARTESIAN_POINT('Ctrl Pts',(0.800979409278544,-1.82687480104885,
32.9754539984321));
#19276=CARTESIAN_POINT('Ctrl Pts',(0.806465253307859,-1.82445821214568,
32.9758404395068));
#19277=CARTESIAN_POINT('Ctrl Pts',(0.808780306350825,-1.82343313255363,
32.9760033872609));
#19278=CARTESIAN_POINT('Ctrl Pts',(0.813625515008557,-1.8212766855627,32.9763441360387));
#19279=CARTESIAN_POINT('Ctrl Pts',(0.816155269449309,-1.82014445039982,
32.9765218805956));
#19280=CARTESIAN_POINT('Ctrl Pts',(0.822265327090099,-1.81739448932033,
32.9769508013742));
#19281=CARTESIAN_POINT('Ctrl Pts',(0.825843251819519,-1.81577143991545,
32.977201651383));
#19282=CARTESIAN_POINT('Ctrl Pts',(0.838302129444387,-1.81007529197663,
32.978074121406));
#19283=CARTESIAN_POINT('Ctrl Pts',(0.847158112663467,-1.80594744228603,
32.9786924626234));
#19284=CARTESIAN_POINT('Ctrl Pts',(0.971954437423615,-1.74665878507672,
32.9873850497081));
#19285=CARTESIAN_POINT('Ctrl Pts',(1.082354812598,-1.6804853714675,32.994829436277));
#19286=CARTESIAN_POINT('Ctrl Pts',(1.30847245175721,-1.51335965893541,33.0111395156997));
#19287=CARTESIAN_POINT('Ctrl Pts',(1.42045488035223,-1.40877902135488,33.0199821601658));
#19288=CARTESIAN_POINT('Ctrl Pts',(1.53277571921872,-1.27673489673572,33.0307065547587));
#19289=CARTESIAN_POINT('Ctrl Pts',(1.54590114402217,-1.26081045564831,33.0319925812937));
#19290=CARTESIAN_POINT('Ctrl Pts',(1.56386705661483,-1.23831092237548,33.0338009540979));
#19291=CARTESIAN_POINT('Ctrl Pts',(1.56891811486496,-1.23190505190047,33.0343148592367));
#19292=CARTESIAN_POINT('Ctrl Pts',(1.57681267320244,-1.22176568061353,33.0351268626001));
#19293=CARTESIAN_POINT('Ctrl Pts',(1.57968257299581,-1.21805277088309,33.0354239112952));
#19294=CARTESIAN_POINT('Ctrl Pts',(1.58518905875185,-1.21087660647659,33.035997482957));
#19295=CARTESIAN_POINT('Ctrl Pts',(1.58782746607541,-1.20741477777196,33.0362739318546));
#19296=CARTESIAN_POINT('Ctrl Pts',(1.59403663682675,-1.19921223628462,33.0369283935306));
#19297=CARTESIAN_POINT('Ctrl Pts',(1.59759759923401,-1.19446418818849,33.0373067874272));
#19298=CARTESIAN_POINT('Ctrl Pts',(1.60797608647322,-1.18049648383865,33.0384186949414));
#19299=CARTESIAN_POINT('Ctrl Pts',(1.61473527604945,-1.17123397414157,33.0391544663014));
#19300=CARTESIAN_POINT('Ctrl Pts',(1.6683507522509,-1.09641526956613,33.0450859467055));
#19301=CARTESIAN_POINT('Ctrl Pts',(1.71126925058332,-1.028141626131,33.0504312096927));
#19302=CARTESIAN_POINT('Ctrl Pts',(1.79921200468044,-0.867411001127563,
33.0628727337065));
#19303=CARTESIAN_POINT('Ctrl Pts',(1.8414569093389,-0.773691708500714,33.0700331376366));
#19304=CARTESIAN_POINT('Ctrl Pts',(1.9154757533281,-0.568593735928676,33.0852427227486));
#19305=CARTESIAN_POINT('Ctrl Pts',(1.9451628591711,-0.456830838117353,33.0932639219271));
#19306=CARTESIAN_POINT('Ctrl Pts',(1.96634193093139,-0.335538576007945,
33.10130451497));
#19307=CARTESIAN_POINT('Ctrl Pts',(1.96762117118397,-0.327953741719003,
33.101804549577));
#19308=CARTESIAN_POINT('Ctrl Pts',(1.96942287701189,-0.316880938839103,
33.102530304511));
#19309=CARTESIAN_POINT('Ctrl Pts',(1.96997999754359,-0.313398799686563,
33.1027579291361));
#19310=CARTESIAN_POINT('Ctrl Pts',(1.97094952077218,-0.30723429807065,33.1031597993702));
#19311=CARTESIAN_POINT('Ctrl Pts',(1.9713656868668,-0.304552551037628,33.1033342571552));
#19312=CARTESIAN_POINT('Ctrl Pts',(1.97223134247897,-0.298898197296047,
33.1037013114168));
#19313=CARTESIAN_POINT('Ctrl Pts',(1.97267958408598,-0.295925428827723,
33.1038938363791));
#19314=CARTESIAN_POINT('Ctrl Pts',(1.97385735468101,-0.287992774599749,
33.1044063962237));
#19315=CARTESIAN_POINT('Ctrl Pts',(1.97457491551555,-0.283031092250418,
33.1047257588138));
#19316=CARTESIAN_POINT('Ctrl Pts',(1.97786841080351,-0.259635428431879,
33.1062260641627));
#19317=CARTESIAN_POINT('Ctrl Pts',(1.98020506239208,-0.241167944528133,
33.1073940411166));
#19318=CARTESIAN_POINT('Ctrl Pts',(2.001481301371,-0.051759448188537,33.1192315031794));
#19319=CARTESIAN_POINT('Ctrl Pts',(1.9984989766766,0.120941573512309,33.1288939122785));
#19320=CARTESIAN_POINT('Ctrl Pts',(1.97027530242521,0.312246785996703,33.1402053206825));
#19321=CARTESIAN_POINT('Ctrl Pts',(1.96682271312304,0.333303481659332,33.1414579050391));
#19322=CARTESIAN_POINT('Ctrl Pts',(1.94712934879159,0.442416319655802,33.1480000358855));
#19323=CARTESIAN_POINT('Ctrl Pts',(1.92531290325817,0.529350518522361,33.153393457516));
#19324=CARTESIAN_POINT('Ctrl Pts',(1.8938662653826,0.626462894995729,33.1597678837332));
#19325=CARTESIAN_POINT('Ctrl Pts',(1.88988587120405,0.638370247031418,33.160555502763));
#19326=CARTESIAN_POINT('Ctrl Pts',(1.88378658289306,0.656059123548691,33.1617348632326));
#19327=CARTESIAN_POINT('Ctrl Pts',(1.88175284216143,0.661869853608689,33.1621237867165));
#19328=CARTESIAN_POINT('Ctrl Pts',(1.87807427352336,0.672226116991098,33.1628196869793));
#19329=CARTESIAN_POINT('Ctrl Pts',(1.87643975328666,0.676775280906877,33.1631263191619));
#19330=CARTESIAN_POINT('Ctrl Pts',(1.87295292380386,0.686370014223294,33.1637750648105));
#19331=CARTESIAN_POINT('Ctrl Pts',(1.87109672759531,0.691414120668633,33.1641173059152));
#19332=CARTESIAN_POINT('Ctrl Pts',(1.86611916461618,0.704773518840122,33.1650269177741));
#19333=CARTESIAN_POINT('Ctrl Pts',(1.86296263562231,0.713075496317366,33.1655954610281));
#19334=CARTESIAN_POINT('Ctrl Pts',(1.8480195899449,0.751600636541017,33.1682492998371));
#19335=CARTESIAN_POINT('Ctrl Pts',(1.83555294491301,0.781553006588485,33.17035734796));
#19336=CARTESIAN_POINT('Ctrl Pts',(1.79977005299998,0.86194065026131,33.1761415125654));
#19337=CARTESIAN_POINT('Ctrl Pts',(1.77506948850035,0.91172435132921,33.1798625658619));
#19338=CARTESIAN_POINT('Ctrl Pts',(1.65266449039351,1.13455006158867,33.1971522545641));
#19339=CARTESIAN_POINT('Ctrl Pts',(1.53153808410573,1.29340021235381,33.2114296567931));
#19340=CARTESIAN_POINT('Ctrl Pts',(1.37999190204386,1.44041859103112,33.2254683570575));
#19341=CARTESIAN_POINT('Ctrl Pts',(1.37095121313336,1.44902593351077,33.2262932480805));
#19342=CARTESIAN_POINT('Ctrl Pts',(1.35414598180514,1.46472755572686,33.2278025895567));
#19343=CARTESIAN_POINT('Ctrl Pts',(1.34640503328542,1.47184634067332,33.2284886688951));
#19344=CARTESIAN_POINT('Ctrl Pts',(1.33551523015057,1.48170308552749,33.2294406684291));
#19345=CARTESIAN_POINT('Ctrl Pts',(1.33241370588891,1.48449273516436,33.2297103352435));
#19346=CARTESIAN_POINT('Ctrl Pts',(1.327409875849,1.48896508817339,33.2301430061172));
#19347=CARTESIAN_POINT('Ctrl Pts',(1.32551308895486,1.49065390466338,33.230306467194));
#19348=CARTESIAN_POINT('Ctrl Pts',(1.32154473521287,1.49417359054091,33.230647294605));
#19349=CARTESIAN_POINT('Ctrl Pts',(1.31947258461452,1.49600377820404,33.2308246075698));
#19350=CARTESIAN_POINT('Ctrl Pts',(1.31447369662721,1.50040048521432,33.2312508002846));
#19351=CARTESIAN_POINT('Ctrl Pts',(1.31154321806377,1.50296277496545,33.2314993640596));
#19352=CARTESIAN_POINT('Ctrl Pts',(1.30139823581362,1.51178086286986,33.2323555263515));
#19353=CARTESIAN_POINT('Ctrl Pts',(1.29414618326472,1.517993547599,33.2329600078525));
#19354=CARTESIAN_POINT('Ctrl Pts',(1.27652810318094,1.53286856601141,33.2344112318479));
#19355=CARTESIAN_POINT('Ctrl Pts',(1.26611801278809,1.54147826409757,33.2352544762968));
#19356=CARTESIAN_POINT('Ctrl Pts',(1.22655068227239,1.573531265657,33.2384097725086));
#19357=CARTESIAN_POINT('Ctrl Pts',(1.19682173852103,1.5962597868546,33.2406801464849));
#19358=CARTESIAN_POINT('Ctrl Pts',(1.02666615247564,1.71891991245894,33.253233086772));
#19359=CARTESIAN_POINT('Ctrl Pts',(0.874388497338395,1.80116122881976,33.2628931104991));
#19360=CARTESIAN_POINT('Ctrl Pts',(0.705825483401582,1.86571813964814,33.2736446126897));
#19361=CARTESIAN_POINT('Ctrl Pts',(0.698208088731203,1.86858215026189,33.2741304319677));
#19362=CARTESIAN_POINT('Ctrl Pts',(0.670978526763432,1.87863025220074,33.2758672992567));
#19363=CARTESIAN_POINT('Ctrl Pts',(0.651271734543528,1.88555267617871,33.2771247604516));
#19364=CARTESIAN_POINT('Ctrl Pts',(0.588320847355043,1.906560888585,33.2811482278873));
#19365=CARTESIAN_POINT('Ctrl Pts',(0.544704542213219,1.91947709151793,33.2839461965681));
#19366=CARTESIAN_POINT('Ctrl Pts',(0.491586525877133,1.9332507974279,33.287381788232));
#19367=CARTESIAN_POINT('Ctrl Pts',(0.482469173488074,1.93554629238531,33.2879724517339));
#19368=CARTESIAN_POINT('Ctrl Pts',(0.467463384119336,1.93921171951324,33.288946322863));
#19369=CARTESIAN_POINT('Ctrl Pts',(0.461584273448809,1.9406195056699,33.2893283092148));
#19370=CARTESIAN_POINT('Ctrl Pts',(0.451004124934851,1.94310218372557,33.2900165546879));
#19371=CARTESIAN_POINT('Ctrl Pts',(0.446305398270003,1.94418679861605,33.2903224984778));
#19372=CARTESIAN_POINT('Ctrl Pts',(0.436402369265574,1.9464349393303,33.2909679327485));
#19373=CARTESIAN_POINT('Ctrl Pts',(0.431197248903606,1.947594653046,33.291307542953));
#19374=CARTESIAN_POINT('Ctrl Pts',(0.417423181221115,1.95060562497926,33.2922072315598));
#19375=CARTESIAN_POINT('Ctrl Pts',(0.408846647357733,1.9524212740326,33.2927684453925));
#19376=CARTESIAN_POINT('Ctrl Pts',(0.389924990092333,1.95629684007522,33.2940089406523));
#19377=CARTESIAN_POINT('Ctrl Pts',(0.379574987969912,1.95833134218392,33.2946890169339));
#19378=CARTESIAN_POINT('Ctrl Pts',(0.348741620139204,1.96413865095314,33.2967197684674));
#19379=CARTESIAN_POINT('Ctrl Pts',(0.328215290711517,1.96767274371108,33.2980779190363));
#19380=CARTESIAN_POINT('Ctrl Pts',(0.254751819115167,1.97913975476746,33.3029621034731));
#19381=CARTESIAN_POINT('Ctrl Pts',(0.201559130991383,1.9852621294249,33.3065425311369));
#19382=CARTESIAN_POINT('Ctrl Pts',(0.0324375198180166,1.99786085297244,
33.3180576294182));
#19383=CARTESIAN_POINT('Ctrl Pts',(-0.0838370256106724,1.9963634805252,
33.3261838085693));
#19384=CARTESIAN_POINT('Ctrl Pts',(-0.300765603454961,1.9745796666485,33.3413691960147));
#19385=CARTESIAN_POINT('Ctrl Pts',(-0.40130566376226,1.95662566500361,33.3484110605478));
#19386=CARTESIAN_POINT('Ctrl Pts',(-0.50762345945489,1.92909494597857,33.3555846945754));
#19387=CARTESIAN_POINT('Ctrl Pts',(-0.515192952414424,1.92708720972738,
33.3560938717393));
#19388=CARTESIAN_POINT('Ctrl Pts',(-0.526178709605743,1.92410398543749,
33.3568303787301));
#19389=CARTESIAN_POINT('Ctrl Pts',(-0.529604383265513,1.92316389809201,
33.3570596922142));
#19390=CARTESIAN_POINT('Ctrl Pts',(-0.535646358178066,1.92148846650882,
33.3574634985248));
#19391=CARTESIAN_POINT('Ctrl Pts',(-0.538263689682664,1.92075692077004,
33.3576382104472));
#19392=CARTESIAN_POINT('Ctrl Pts',(-0.543760583134392,1.91920841747427,
33.3580046820671));
#19393=CARTESIAN_POINT('Ctrl Pts',(-0.54663979712703,1.91839032888544,33.3581963745166));
#19394=CARTESIAN_POINT('Ctrl Pts',(-0.554279540014072,1.91620100631878,
33.358704345867));
#19395=CARTESIAN_POINT('Ctrl Pts',(-0.559036858850027,1.91481850231584,
33.3590199735593));
#19396=CARTESIAN_POINT('Ctrl Pts',(-0.58104470619389,1.90833388612255,33.3604771157639));
#19397=CARTESIAN_POINT('Ctrl Pts',(-0.598231537895576,1.90301609382746,
33.36160655363));
#19398=CARTESIAN_POINT('Ctrl Pts',(-0.645185362075614,1.88778905588708,
33.3646747281142));
#19399=CARTESIAN_POINT('Ctrl Pts',(-0.674795239872328,1.87740866141502,
33.3665902132715));
#19400=CARTESIAN_POINT('Ctrl Pts',(-0.7833372902581,1.83645679679908,33.3735822018617));
#19401=CARTESIAN_POINT('Ctrl Pts',(-0.860549156370975,1.80156823094579,
33.3784996505042));
#19402=CARTESIAN_POINT('Ctrl Pts',(-1.02295810536666,1.71535132457716,33.3891669631239));
#19403=CARTESIAN_POINT('Ctrl Pts',(-1.10700397635823,1.66235201070424,33.394903154773));
#19404=CARTESIAN_POINT('Ctrl Pts',(-1.19339505781599,1.59840673025072,33.4013154452251));
#19405=CARTESIAN_POINT('Ctrl Pts',(-1.20000593546468,1.59344958873478,33.4018095511411));
#19406=CARTESIAN_POINT('Ctrl Pts',(-1.21702790429884,1.58051972303505,33.4030909713356));
#19407=CARTESIAN_POINT('Ctrl Pts',(-1.22739141687754,1.57248523503708,33.4038801169651));
#19408=CARTESIAN_POINT('Ctrl Pts',(-1.27670318323539,1.53347097376726,33.4076803854793));
#19409=CARTESIAN_POINT('Ctrl Pts',(-1.31455948523975,1.50114521670288,33.4107357169756));
#19410=CARTESIAN_POINT('Ctrl Pts',(-1.3582840453595,1.46088522951964,33.4144554699272));
#19411=CARTESIAN_POINT('Ctrl Pts',(-1.36535485288055,1.45427896984817,33.4150632237763));
#19412=CARTESIAN_POINT('Ctrl Pts',(-1.37682570615761,1.44340434798724,33.4160595609246));
#19413=CARTESIAN_POINT('Ctrl Pts',(-1.38125469374114,1.43916663614045,33.4164468240244));
#19414=CARTESIAN_POINT('Ctrl Pts',(-1.3891391739411,1.43155274313149,33.4171408825983));
#19415=CARTESIAN_POINT('Ctrl Pts',(-1.39260208139003,1.42818428193993,33.4174473405043));
#19416=CARTESIAN_POINT('Ctrl Pts',(-1.39927736757128,1.42164369401301,33.4180412558098));
#19417=CARTESIAN_POINT('Ctrl Pts',(-1.40249128390312,1.41847317286848,33.418328641663));
#19418=CARTESIAN_POINT('Ctrl Pts',(-1.40944616629777,1.41156545304751,33.41895368707));
#19419=CARTESIAN_POINT('Ctrl Pts',(-1.41318308256238,1.40782424265122,33.4192915232835));
#19420=CARTESIAN_POINT('Ctrl Pts',(-1.42795826441165,1.39291397756558,33.4206352652754));
#19421=CARTESIAN_POINT('Ctrl Pts',(-1.43887910753933,1.3816298506566,33.4216463002903));
#19422=CARTESIAN_POINT('Ctrl Pts',(-1.49773489469329,1.31936152531275,33.427194792987));
#19423=CARTESIAN_POINT('Ctrl Pts',(-1.54308949701015,1.26601638188128,33.4318405247866));
#19424=CARTESIAN_POINT('Ctrl Pts',(-1.62125481303149,1.16362532963598,33.4405698861641));
#19425=CARTESIAN_POINT('Ctrl Pts',(-1.65487576150722,1.11529210529216,33.444620758554));
#19426=CARTESIAN_POINT('Ctrl Pts',(-1.76854597423252,0.935400231164669,
33.4593915017521));
#19427=CARTESIAN_POINT('Ctrl Pts',(-1.83544370345407,0.796166084685855,
33.4703016212475));
#19428=CARTESIAN_POINT('Ctrl Pts',(-1.89030717537424,0.637157036486766,
33.4813994658384));
#19429=CARTESIAN_POINT('Ctrl Pts',(-1.89480728568294,0.623647083518871,
33.4823318009305));
#19430=CARTESIAN_POINT('Ctrl Pts',(-1.90060705713279,0.605592837521602,
33.4835626369911));
#19431=CARTESIAN_POINT('Ctrl Pts',(-1.90203565852051,0.601090862772052,
33.4838683124037));
#19432=CARTESIAN_POINT('Ctrl Pts',(-1.90424035255221,0.594056610342024,
33.4843439391325));
#19433=CARTESIAN_POINT('Ctrl Pts',(-1.90502740313454,0.591527826975992,
33.4845145253664));
#19434=CARTESIAN_POINT('Ctrl Pts',(-1.90652867354078,0.586670190991764,
33.4848414342773));
#19435=CARTESIAN_POINT('Ctrl Pts',(-1.90724365556851,0.584341624737796,
33.4849977985661));
#19436=CARTESIAN_POINT('Ctrl Pts',(-1.90894323596698,0.578770049835498,
33.485371118825));
#19437=CARTESIAN_POINT('Ctrl Pts',(-1.90992383544618,0.575525839508009,
33.4855878384601));
#19438=CARTESIAN_POINT('Ctrl Pts',(-1.91284611733557,0.565768053294586,
33.4862377492209));
#19439=CARTESIAN_POINT('Ctrl Pts',(-1.91476280700752,0.559246953363802,
33.4866695039527));
#19440=CARTESIAN_POINT('Ctrl Pts',(-1.91907868441804,0.544280842726817,
33.4876547641027));
#19441=CARTESIAN_POINT('Ctrl Pts',(-1.92145554647378,0.535829471121856,
33.4882070493122));
#19442=CARTESIAN_POINT('Ctrl Pts',(-1.9707256688267,0.356095973906566,33.4998710935859));
#19443=CARTESIAN_POINT('Ctrl Pts',(-1.99459991896134,0.179306582252376,
33.5098330031497));
#19444=CARTESIAN_POINT('Ctrl Pts',(-1.99474929467395,0.0016774676722283,
33.5202191433277));
#19445=CARTESIAN_POINT('',(-1.9947497669637,-0.000964208625222721,34.3209548814384));
#19446=CARTESIAN_POINT('Ctrl Pts',(-1.99474925803387,0.00172048636055072,
33.5209548813952));
#19447=CARTESIAN_POINT('Ctrl Pts',(-1.99480900501761,-0.0675507698475596,
33.525367756855));
#19448=CARTESIAN_POINT('Ctrl Pts',(-1.9912561081305,-0.136886666161832,
33.5297806323149));
#19449=CARTESIAN_POINT('Ctrl Pts',(-1.98409705625583,-0.205879658676962,
33.5341935077747));
#19450=CARTESIAN_POINT('Ctrl Pts',(-1.9769407358986,-0.274846327096992,
33.5386046995135));
#19451=CARTESIAN_POINT('Ctrl Pts',(-1.96618104135419,-0.343469858405761,
33.5430158912523));
#19452=CARTESIAN_POINT('Ctrl Pts',(-1.95187642317062,-0.411346558476753,
33.5474270829911));
#19453=CARTESIAN_POINT('Ctrl Pts',(-1.93757225629807,-0.479221117036381,
33.5518381355567));
#19454=CARTESIAN_POINT('Ctrl Pts',(-1.9197234920193,-0.546348406239829,
33.5562491881224));
#19455=CARTESIAN_POINT('Ctrl Pts',(-1.89843956389977,-0.612335516461396,
33.560660240688));
#19456=CARTESIAN_POINT('Ctrl Pts',(-1.87713382054319,-0.678390261023937,
33.5650758144189));
#19457=CARTESIAN_POINT('Ctrl Pts',(-1.85238603593462,-0.743302020150988,
33.5694913881498));
#19458=CARTESIAN_POINT('Ctrl Pts',(-1.8243550541552,-0.806694613145749,
33.5739069618807));
#19459=CARTESIAN_POINT('Ctrl Pts',(-1.79630923971353,-0.870120750485432,
33.5783248721232));
#19460=CARTESIAN_POINT('Ctrl Pts',(-1.76497699468783,-0.932025678977947,
33.5827427823657));
#19461=CARTESIAN_POINT('Ctrl Pts',(-1.73056342603898,-0.99205735265469,
33.5871606926082));
#19462=CARTESIAN_POINT('Ctrl Pts',(-1.69608655433791,-1.05219945336132,
33.5915867295058));
#19463=CARTESIAN_POINT('Ctrl Pts',(-1.65851731041629,-1.11046100160717,
33.5960127664034));
#19464=CARTESIAN_POINT('Ctrl Pts',(-1.61810405492496,-1.16651910825987,
33.600438803301));
#19465=CARTESIAN_POINT('Ctrl Pts',(-1.58870100730711,-1.20730471583433,
33.6036590084559));
#19466=CARTESIAN_POINT('Ctrl Pts',(-1.55779340507657,-1.24692458229429,
33.6068792136108));
#19467=CARTESIAN_POINT('Ctrl Pts',(-1.52548938349084,-1.28526639392646,
33.6100994187656));
#19468=CARTESIAN_POINT('Ctrl Pts',(-1.48080783377919,-1.33829915821964,
33.6145534696747));
#19469=CARTESIAN_POINT('Ctrl Pts',(-1.43326901986471,-1.38910417913217,
33.6190075205837));
#19470=CARTESIAN_POINT('Ctrl Pts',(-1.383123640052,-1.43735749165936,33.6234615714927));
#19471=CARTESIAN_POINT('Ctrl Pts',(-1.33305363790775,-1.48553827064096,
33.6279089271494));
#19472=CARTESIAN_POINT('Ctrl Pts',(-1.2803851962972,-1.53117461743457,33.632356282806));
#19473=CARTESIAN_POINT('Ctrl Pts',(-1.22540866152179,-1.57397623068691,
33.6368036384627));
#19474=CARTESIAN_POINT('Ctrl Pts',(-1.17049694149409,-1.61672738285116,
33.6412457508963));
#19475=CARTESIAN_POINT('Ctrl Pts',(-1.11328291724205,-1.65665013985083,
33.6456878633299));
#19476=CARTESIAN_POINT('Ctrl Pts',(-1.05409177933541,-1.69349286483218,
33.6501299757635));
#19477=CARTESIAN_POINT('Ctrl Pts',(-0.994937981602122,-1.73031234792655,
33.6545692859322));
#19478=CARTESIAN_POINT('Ctrl Pts',(-0.933809959117067,-1.76405539538836,
33.6590085961009));
#19479=CARTESIAN_POINT('Ctrl Pts',(-0.871062546673523,-1.7945131936775,
33.6634479062696));
#19480=CARTESIAN_POINT('Ctrl Pts',(-0.808333396404629,-1.82496212744762,
33.6678859244097));
#19481=CARTESIAN_POINT('Ctrl Pts',(-0.743986231995407,-1.85212749647973,
33.6723239425497));
#19482=CARTESIAN_POINT('Ctrl Pts',(-0.678399611395581,-1.87584688334585,
33.6767619606897));
#19483=CARTESIAN_POINT('Ctrl Pts',(-0.612809793753564,-1.89956742642156,
33.6812001951624));
#19484=CARTESIAN_POINT('Ctrl Pts',(-0.545980861158996,-1.91984148959226,
33.6856384296351));
#19485=CARTESIAN_POINT('Ctrl Pts',(-0.478308741880752,-1.93655578539335,
33.6900766641078));
#19486=CARTESIAN_POINT('Ctrl Pts',(-0.410564937381926,-1.95328778668371,
33.6945196000118));
#19487=CARTESIAN_POINT('Ctrl Pts',(-0.341976639659408,-1.96645237650665,
33.6989625359158));
#19488=CARTESIAN_POINT('Ctrl Pts',(-0.272951303253476,-1.97598713268893,
33.7034054718197));
#19489=CARTESIAN_POINT('Ctrl Pts',(-0.203885677078493,-1.98552745426422,
33.7078510010448));
#19490=CARTESIAN_POINT('Ctrl Pts',(-0.134382992426301,-1.9914336836673,
33.7122965302699));
#19491=CARTESIAN_POINT('Ctrl Pts',(-0.0648543860996425,-1.99369543087796,
33.716742059495));
#19492=CARTESIAN_POINT('Ctrl Pts',(0.00479554274020294,-1.99596112467794,
33.7211953458549));
#19493=CARTESIAN_POINT('Ctrl Pts',(0.0744709941348924,-1.99456965162631,
33.7256486322149));
#19494=CARTESIAN_POINT('Ctrl Pts',(0.14376307234286,-1.98956270108045,33.7301019185749));
#19495=CARTESIAN_POINT('Ctrl Pts',(0.180865313670245,-1.98688174400323,
33.7324864177774));
#19496=CARTESIAN_POINT('Ctrl Pts',(0.217857760155773,-1.98316510193474,
33.7348709169799));
#19497=CARTESIAN_POINT('Ctrl Pts',(0.25467889410285,-1.97842518771839,33.7372554161824));
#19498=CARTESIAN_POINT('Ctrl Pts',(0.323458272612784,-1.96957134974426,
33.7417094988145));
#19499=CARTESIAN_POINT('Ctrl Pts',(0.391911591312129,-1.95710906248736,
33.7461635814465));
#19500=CARTESIAN_POINT('Ctrl Pts',(0.459630738094927,-1.94107370985708,
33.7506176640786));
#19501=CARTESIAN_POINT('Ctrl Pts',(0.527248098415184,-1.92506245944747,
33.7550650519229));
#19502=CARTESIAN_POINT('Ctrl Pts',(0.594133004519081,-1.90548891478166,
33.7595124397672));
#19503=CARTESIAN_POINT('Ctrl Pts',(0.659884182157403,-1.88244001993117,
33.7639598276115));
#19504=CARTESIAN_POINT('Ctrl Pts',(0.725557850587904,-1.85941829572074,
33.7684019727587));
#19505=CARTESIAN_POINT('Ctrl Pts',(0.790099985192176,-1.83292951932491,
33.7728441179059));
#19506=CARTESIAN_POINT('Ctrl Pts',(0.853122954715086,-1.80311086365709,
33.7772862630531));
#19507=CARTESIAN_POINT('Ctrl Pts',(0.916106171430466,-1.77331101661235,
33.7817256062418));
#19508=CARTESIAN_POINT('Ctrl Pts',(0.977571682500778,-1.7401856658522,33.7861649494306));
#19509=CARTESIAN_POINT('Ctrl Pts',(1.03715181149552,-1.70392009273075,33.7906042926193));
#19510=CARTESIAN_POINT('Ctrl Pts',(1.096714603681,-1.66766507227736,33.7950423440343));
#19511=CARTESIAN_POINT('Ctrl Pts',(1.15439268491689,-1.62827189781196,33.7994803954494));
#19512=CARTESIAN_POINT('Ctrl Pts',(1.20984454305707,-1.58597091528661,33.8039184468644));
#19513=CARTESIAN_POINT('Ctrl Pts',(1.26529910674263,-1.54366786885876,33.8083567148159));
#19514=CARTESIAN_POINT('Ctrl Pts',(1.31852684390637,-1.49845703151792,33.8127949827673));
#19515=CARTESIAN_POINT('Ctrl Pts',(1.36921814456832,-1.45060995277328,33.8172332507188));
#19516=CARTESIAN_POINT('Ctrl Pts',(1.41996314308366,-1.40271218909086,33.8216762201765));
#19517=CARTESIAN_POINT('Ctrl Pts',(1.46816598550494,-1.35217294681108,33.8261191896341));
#19518=CARTESIAN_POINT('Ctrl Pts',(1.51355358694689,-1.29930100513322,33.8305621590917));
#19519=CARTESIAN_POINT('Ctrl Pts',(1.55896768166696,-1.24639820147961,33.835007721963));
#19520=CARTESIAN_POINT('Ctrl Pts',(1.6015629655884,-1.19116037605976,33.8394532848343));
#19521=CARTESIAN_POINT('Ctrl Pts',(1.64110810670013,-1.13392757468152,33.8438988477056));
#19522=CARTESIAN_POINT('Ctrl Pts',(1.68072224881724,-1.07659490968604,33.8483521674921));
#19523=CARTESIAN_POINT('Ctrl Pts',(1.71727536752212,-1.01726073685655,33.8528054872787));
#19524=CARTESIAN_POINT('Ctrl Pts',(1.75058113030047,-0.956291414128532,
33.8572588070652));
#19525=CARTESIAN_POINT('Ctrl Pts',(1.76841224864826,-0.923649879497329,
33.8596430092431));
#19526=CARTESIAN_POINT('Ctrl Pts',(1.78531339333716,-0.890540044050332,
33.8620272114211));
#19527=CARTESIAN_POINT('Ctrl Pts',(1.8012617026036,-0.857020327199758,33.864411413599));
#19528=CARTESIAN_POINT('Ctrl Pts',(1.83105457641699,-0.794402486166849,
33.8688653173606));
#19529=CARTESIAN_POINT('Ctrl Pts',(1.85763737455939,-0.730105192486759,
33.8733192211222));
#19530=CARTESIAN_POINT('Ctrl Pts',(1.88081888573508,-0.664490693360145,
33.8777731248838));
#19531=CARTESIAN_POINT('Ctrl Pts',(1.90396554960781,-0.598974828369706,
33.882220333373));
#19532=CARTESIAN_POINT('Ctrl Pts',(1.92372091264796,-0.5321461457421,33.8866675418621));
#19533=CARTESIAN_POINT('Ctrl Pts',(1.93994081409499,-0.464389061357482,
33.8911147503512));
#19534=CARTESIAN_POINT('Ctrl Pts',(1.95614159485253,-0.396711851821363,
33.8955567162874));
#19535=CARTESIAN_POINT('Ctrl Pts',(1.96881507824126,-0.328108888057713,
33.8999986822235));
#19536=CARTESIAN_POINT('Ctrl Pts',(1.97786671959277,-0.258980312045775,
33.9044406481597));
#19537=CARTESIAN_POINT('Ctrl Pts',(1.98691265161891,-0.189895338902946,
33.9088798123246));
#19538=CARTESIAN_POINT('Ctrl Pts',(1.99234121005921,-0.120285895512519,
33.9133189764894));
#19539=CARTESIAN_POINT('Ctrl Pts',(1.99410910129579,-0.0505613946535523,
33.9177581406543));
#19540=CARTESIAN_POINT('Ctrl Pts',(1.99587647826414,0.0191428237954161,
33.9221960134948));
#19541=CARTESIAN_POINT('Ctrl Pts',(1.99398528954515,0.0889615440849342,
33.9266338863353));
#19542=CARTESIAN_POINT('Ctrl Pts',(1.98844429554399,0.158482951823095,33.9310717591758));
#19543=CARTESIAN_POINT('Ctrl Pts',(1.98290303029309,0.228007762861112,33.9355098492646));
#19544=CARTESIAN_POINT('Ctrl Pts',(1.97371164631804,0.29723474459686,33.9399479393535));
#19545=CARTESIAN_POINT('Ctrl Pts',(1.96093081847343,0.365756596196353,33.9443860294423));
#19546=CARTESIAN_POINT('Ctrl Pts',(1.94813644461477,0.434351072040158,33.9488288233291));
#19547=CARTESIAN_POINT('Ctrl Pts',(1.93174512355498,0.502238443828767,33.9532716172158));
#19548=CARTESIAN_POINT('Ctrl Pts',(1.91186860645616,0.5690219627988,33.9577144111025));
#19549=CARTESIAN_POINT('Ctrl Pts',(1.89198048210503,0.635844481214783,33.9621597994392));
#19550=CARTESIAN_POINT('Ctrl Pts',(1.8686032749491,0.701561402368177,33.9666051877759));
#19551=CARTESIAN_POINT('Ctrl Pts',(1.84189762901384,0.765794154282464,33.9710505761126));
#19552=CARTESIAN_POINT('Ctrl Pts',(1.81514536254822,0.830139038476509,33.9755037248443));
#19553=CARTESIAN_POINT('Ctrl Pts',(1.7850532698749,0.892994139906103,33.9799568735761));
#19554=CARTESIAN_POINT('Ctrl Pts',(1.75182848002257,0.954004475399262,33.9844100223078));
#19555=CARTESIAN_POINT('Ctrl Pts',(1.73402813618776,0.986691061351559,33.9867958185438));
#19556=CARTESIAN_POINT('Ctrl Pts',(1.71532936098203,1.0188486135646,33.9891816147798));
#19557=CARTESIAN_POINT('Ctrl Pts',(1.69576897131637,1.05042617942462,33.9915674110159));
#19558=CARTESIAN_POINT('Ctrl Pts',(1.65925073909999,1.10937985583984,33.9960215687529));
#19559=CARTESIAN_POINT('Ctrl Pts',(1.61958223217014,1.16654365376695,34.0004757264899));
#19560=CARTESIAN_POINT('Ctrl Pts',(1.57696452361047,1.22156066315759,34.0049298842269));
#19561=CARTESIAN_POINT('Ctrl Pts',(1.53441088249247,1.27649496516767,34.0093773460034));
#19562=CARTESIAN_POINT('Ctrl Pts',(1.48891713659827,1.32928850014793,34.01382480778));
#19563=CARTESIAN_POINT('Ctrl Pts',(1.44072846985315,1.37961191595847,34.0182722695565));
#19564=CARTESIAN_POINT('Ctrl Pts',(1.39259663060365,1.4298759868258,34.0227144865705));
#19565=CARTESIAN_POINT('Ctrl Pts',(1.34177651944681,1.47767537213732,34.0271567035845));
#19566=CARTESIAN_POINT('Ctrl Pts',(1.28855340351047,1.52271392218026,34.0315989205985));
#19567=CARTESIAN_POINT('Ctrl Pts',(1.23536387415241,1.56772405053537,34.0360383343405));
#19568=CARTESIAN_POINT('Ctrl Pts',(1.17977472107642,1.60997648432446,34.0404777480826));
#19569=CARTESIAN_POINT('Ctrl Pts',(1.12210675304697,1.64921314488649,34.0449171618246));
#19570=CARTESIAN_POINT('Ctrl Pts',(1.06445558341301,1.68843837600225,34.0493552823872));
#19571=CARTESIAN_POINT('Ctrl Pts',(1.00472720546485,1.72464930257842,34.0537934029498));
#19572=CARTESIAN_POINT('Ctrl Pts',(0.943272629597239,1.75763031060366,34.0582315235125));
#19573=CARTESIAN_POINT('Ctrl Pts',(0.881815076112263,1.79061291663557,34.0626698591124));
#19574=CARTESIAN_POINT('Ctrl Pts',(0.818631591127086,1.82036506402963,34.0671081947123));
#19575=CARTESIAN_POINT('Ctrl Pts',(0.754097497826226,1.84671722964622,34.0715465303122));
#19576=CARTESIAN_POINT('Ctrl Pts',(0.689495083339709,1.87309729386816,34.0759895647052));
#19577=CARTESIAN_POINT('Ctrl Pts',(0.623539660697206,1.8960700064328,34.0804325990982));
#19578=CARTESIAN_POINT('Ctrl Pts',(0.556625335339389,1.91551449969931,34.0848756334912));
#19579=CARTESIAN_POINT('Ctrl Pts',(0.489671973567971,1.93497033647526,34.0893212598572));
#19580=CARTESIAN_POINT('Ctrl Pts',(0.421759072401971,1.95089374536216,34.0937668862232));
#19581=CARTESIAN_POINT('Ctrl Pts',(0.353291928434141,1.96321480633253,34.0982125125893));
#19582=CARTESIAN_POINT('Ctrl Pts',(0.284705364897139,1.97555735754929,34.1026658929634));
#19583=CARTESIAN_POINT('Ctrl Pts',(0.215563114473331,1.98428495719858,34.1071192733375));
#19584=CARTESIAN_POINT('Ctrl Pts',(0.146275810991793,1.98937953885595,34.1115726537115));
#19585=CARTESIAN_POINT('Ctrl Pts',(0.109191134419718,1.99210631423239,34.1139562386185));
#19586=CARTESIAN_POINT('Ctrl Pts',(0.0720649142995155,1.99379322580034,
34.1163398235255));
#19587=CARTESIAN_POINT('Ctrl Pts',(0.0349597448561959,1.9944436263629,34.1187234084326));
#19588=CARTESIAN_POINT('Ctrl Pts',(-0.0343799075217012,1.99565905131826,
34.1231776920632));
#19589=CARTESIAN_POINT('Ctrl Pts',(-0.10392021778134,1.9932565351573,34.1276319756939));
#19590=CARTESIAN_POINT('Ctrl Pts',(-0.17325222182456,1.98721192381005,34.1320862593246));
#19591=CARTESIAN_POINT('Ctrl Pts',(-0.242480051178027,1.98117639478375,
34.1365338501786));
#19592=CARTESIAN_POINT('Ctrl Pts',(-0.311499711845586,1.9715096741866,34.1409814410327));
#19593=CARTESIAN_POINT('Ctrl Pts',(-0.37990153137552,1.95823961479655,34.1454290318868));
#19594=CARTESIAN_POINT('Ctrl Pts',(-0.448222751080454,1.94498519189793,
34.149871382017));
#19595=CARTESIAN_POINT('Ctrl Pts',(-0.515927097368923,1.92813595593716,
34.1543137321473));
#19596=CARTESIAN_POINT('Ctrl Pts',(-0.582611114921541,1.90777143580406,
34.1587560822775));
#19597=CARTESIAN_POINT('Ctrl Pts',(-0.649253088917247,1.8874197552822,34.1631956315537));
#19598=CARTESIAN_POINT('Ctrl Pts',(-0.714875543284826,1.86355732997129,
34.1676351808299));
#19599=CARTESIAN_POINT('Ctrl Pts',(-0.779087791852975,1.83631418201942,
34.1720747301061));
#19600=CARTESIAN_POINT('Ctrl Pts',(-0.843281368037742,1.80907895614651,
34.1765129883986));
#19601=CARTESIAN_POINT('Ctrl Pts',(-0.906065102103133,1.77846515030744,
34.1809512466911));
#19602=CARTESIAN_POINT('Ctrl Pts',(-0.967067661529605,1.74465116872218,
34.1853895049836));
#19603=CARTESIAN_POINT('Ctrl Pts',(-1.02807320373831,1.71083553376787,34.1898279802893));
#19604=CARTESIAN_POINT('Ctrl Pts',(-1.08729697143131,1.67381965180757,34.1942664555949));
#19605=CARTESIAN_POINT('Ctrl Pts',(-1.1443932222072,1.63382732118979,34.1987049309006));
#19606=CARTESIAN_POINT('Ctrl Pts',(-1.20154994366482,1.59379263466487,34.2031481069987));
#19607=CARTESIAN_POINT('Ctrl Pts',(-1.2565742490851,1.5507754889082,34.2075912830969));
#19608=CARTESIAN_POINT('Ctrl Pts',(-1.30915113609228,1.50504181515607,34.2120344591951));
#19609=CARTESIAN_POINT('Ctrl Pts',(-1.36175871028376,1.45928144835013,34.2164802286108));
#19610=CARTESIAN_POINT('Ctrl Pts',(-1.41191567077529,1.41080173799901,34.2209259980265));
#19611=CARTESIAN_POINT('Ctrl Pts',(-1.45934379181443,1.35990560694215,34.2253717674422));
#19612=CARTESIAN_POINT('Ctrl Pts',(-1.50685463944364,1.30892070021216,34.2298252913996));
#19613=CARTESIAN_POINT('Ctrl Pts',(-1.5516268317956,1.25551133426671,34.2342788153571));
#19614=CARTESIAN_POINT('Ctrl Pts',(-1.593422850475,1.20001299246472,34.2387323393145));
#19615=CARTESIAN_POINT('Ctrl Pts',(-1.61578109451182,1.17032486644569,34.2411146948261));
#19616=CARTESIAN_POINT('Ctrl Pts',(-1.63728842812581,1.14003945522088,34.2434970503377));
#19617=CARTESIAN_POINT('Ctrl Pts',(-1.65791382994515,1.10921111379963,34.2458794058494));
#19618=CARTESIAN_POINT('Ctrl Pts',(-1.69713998942199,1.05058062273872,34.2504102585352));
#19619=CARTESIAN_POINT('Ctrl Pts',(-1.733325150733,0.989758288018983,34.254941111221));
#19620=CARTESIAN_POINT('Ctrl Pts',(-1.76622165703498,0.92708609132087,34.2594719639068));
#19621=CARTESIAN_POINT('Ctrl Pts',(-1.79906366234615,0.864517726220709,
34.2639953101432));
#19622=CARTESIAN_POINT('Ctrl Pts',(-1.82862761784535,0.800105995961701,
34.2685186563796));
#19623=CARTESIAN_POINT('Ctrl Pts',(-1.85470920879811,0.734221569622887,
34.273042002616));
#19624=CARTESIAN_POINT('Ctrl Pts',(-1.8807485039618,0.668443986221841,34.2775580134678));
#19625=CARTESIAN_POINT('Ctrl Pts',(-1.90331649425586,0.601198888278888,
34.2820740243197));
#19626=CARTESIAN_POINT('Ctrl Pts',(-1.92225567913312,0.532879598540311,
34.2865900351716));
#19627=CARTESIAN_POINT('Ctrl Pts',(-1.94117680917022,0.464625437996232,
34.2911017408829));
#19628=CARTESIAN_POINT('Ctrl Pts',(-1.95647587983171,0.39529956803751,34.2956134465941));
#19629=CARTESIAN_POINT('Ctrl Pts',(-1.96804458239084,0.325312287228828,
34.3001251523054));
#19630=CARTESIAN_POINT('Ctrl Pts',(-1.97960545955663,0.255372347770581,
34.304633806173));
#19631=CARTESIAN_POINT('Ctrl Pts',(-1.98744090670197,0.184772346772902,
34.3091424600406));
#19632=CARTESIAN_POINT('Ctrl Pts',(-1.99149360991236,0.113933156623746,
34.3136511139081));
#19633=CARTESIAN_POINT('Ctrl Pts',(-1.9936819942071,0.0756813125761565,
34.3160857030705));
#19634=CARTESIAN_POINT('Ctrl Pts',(-1.99476829178972,0.0373598817098916,
34.3185202922328));
#19635=CARTESIAN_POINT('Ctrl Pts',(-1.99474976696403,-0.000964207945006128,
34.3209548813952));
#19636=CARTESIAN_POINT('',(-1.16030843567301,1.62256337213868,34.9999520653248));
#19637=CARTESIAN_POINT('Ctrl Pts',(-1.9947497669637,-0.00096420862522321,
34.3209548814384));
#19638=CARTESIAN_POINT('Ctrl Pts',(-1.99471265556682,-0.0777400726253646,
34.3258321711043));
#19639=CARTESIAN_POINT('Ctrl Pts',(-1.99023883824554,-0.154367005048329,
34.3307094607701));
#19640=CARTESIAN_POINT('Ctrl Pts',(-1.98140456893308,-0.230355153428635,
34.335586750436));
#19641=CARTESIAN_POINT('Ctrl Pts',(-1.97254063423816,-0.30659846920353,
34.3404804179887));
#19642=CARTESIAN_POINT('Ctrl Pts',(-1.95928705017002,-0.38219840303128,
34.3453740855414));
#19643=CARTESIAN_POINT('Ctrl Pts',(-1.94177087878681,-0.456676490303058,
34.3502677530941));
#19644=CARTESIAN_POINT('Ctrl Pts',(-1.92417266464279,-0.531503420239455,
34.3551843417514));
#19645=CARTESIAN_POINT('Ctrl Pts',(-1.90227198517125,-0.605197678237932,
34.3601009304088));
#19646=CARTESIAN_POINT('Ctrl Pts',(-1.87624600475734,-0.677294981623315,
34.3650175190661));
#19647=CARTESIAN_POINT('Ctrl Pts',(-1.8620984381082,-0.71648664274984,34.3676901471327));
#19648=CARTESIAN_POINT('Ctrl Pts',(-1.84673269201964,-0.755206801789487,
34.3703627751993));
#19649=CARTESIAN_POINT('Ctrl Pts',(-1.83018292208798,-0.793383913498066,
34.373035403266));
#19650=CARTESIAN_POINT('Ctrl Pts',(-1.80259560204012,-0.85702251412856,
34.377490489116));
#19651=CARTESIAN_POINT('Ctrl Pts',(-1.77163055517923,-0.91934631967445,
34.3819455749659));
#19652=CARTESIAN_POINT('Ctrl Pts',(-1.73743506938649,-0.97997292930262,
34.3864006608159));
#19653=CARTESIAN_POINT('Ctrl Pts',(-1.70329101030457,-1.0405083623603,34.3908490466467));
#19654=CARTESIAN_POINT('Ctrl Pts',(-1.66592639331255,-1.09935124275348,
34.3952974324775));
#19655=CARTESIAN_POINT('Ctrl Pts',(-1.62553614436603,-1.15614004595448,
34.3997458183083));
#19656=CARTESIAN_POINT('Ctrl Pts',(-1.58519361041228,-1.21286176174194,
34.4041889490415));
#19657=CARTESIAN_POINT('Ctrl Pts',(-1.54183282594229,-1.26753382310107,
34.4086320797747));
#19658=CARTESIAN_POINT('Ctrl Pts',(-1.49569318826118,-1.31982174898322,
34.413075210508));
#19659=CARTESIAN_POINT('Ctrl Pts',(-1.44958273259949,-1.37207660422707,
34.4175155310864));
#19660=CARTESIAN_POINT('Ctrl Pts',(-1.40069723335661,-1.4219499493231,34.4219558516647));
#19661=CARTESIAN_POINT('Ctrl Pts',(-1.34931677363553,-1.46913981869861,
34.4263961722431));
#19662=CARTESIAN_POINT('Ctrl Pts',(-1.29795137218619,-1.51631585795506,
34.4308351914794));
#19663=CARTESIAN_POINT('Ctrl Pts',(-1.24409282204039,-1.56080965193312,
34.4352742107157));
#19664=CARTESIAN_POINT('Ctrl Pts',(-1.18805724768196,-1.60235686996698,
34.439713229952));
#19665=CARTESIAN_POINT('Ctrl Pts',(-1.13201907811547,-1.64390601220124,
34.4441524547752));
#19666=CARTESIAN_POINT('Ctrl Pts',(-1.07380407864231,-1.68250801803604,
34.4485916795984));
#19667=CARTESIAN_POINT('Ctrl Pts',(-1.01375911693235,-1.71794063207567,
34.4530309044215));
#19668=CARTESIAN_POINT('Ctrl Pts',(-0.953650873833102,-1.75341058854967,
34.4574748077441));
#19669=CARTESIAN_POINT('Ctrl Pts',(-0.891709241334137,-1.78570423707937,
34.4619187110666));
#19670=CARTESIAN_POINT('Ctrl Pts',(-0.828306730700667,-1.81464473723536,
34.4663626143891));
#19671=CARTESIAN_POINT('Ctrl Pts',(-0.764867385275751,-1.84360205087833,
34.4708090994746));
#19672=CARTESIAN_POINT('Ctrl Pts',(-0.69996592770663,-1.86920215899221,
34.47525558456));
#19673=CARTESIAN_POINT('Ctrl Pts',(-0.633993340275247,-1.89131700330395,
34.4797020696455));
#19674=CARTESIAN_POINT('Ctrl Pts',(-0.567906077397025,-1.91347028827343,
34.4841562837391));
#19675=CARTESIAN_POINT('Ctrl Pts',(-0.500744439430113,-1.93212608515629,
34.4886104978327));
#19676=CARTESIAN_POINT('Ctrl Pts',(-0.432912218806348,-1.94720686453909,
34.4930647119262));
#19677=CARTESIAN_POINT('Ctrl Pts',(-0.396735307541797,-1.95524988616679,
34.4954402748451));
#19678=CARTESIAN_POINT('Ctrl Pts',(-0.360367794428594,-1.96227690747146,
34.4978158377639));
#19679=CARTESIAN_POINT('Ctrl Pts',(-0.323871455628267,-1.96828220606935,
34.5001914006828));
#19680=CARTESIAN_POINT('Ctrl Pts',(-0.255423773340099,-1.97954494594918,
34.5046466907549));
#19681=CARTESIAN_POINT('Ctrl Pts',(-0.186253044807938,-1.98725518410221,
34.509101980827));
#19682=CARTESIAN_POINT('Ctrl Pts',(-0.116760612552631,-1.99132983753479,
34.513557270899));
#19683=CARTESIAN_POINT('Ctrl Pts',(-0.047372351829141,-1.99539838292256,
34.518005882339));
#19684=CARTESIAN_POINT('Ctrl Pts',(0.0223361710133283,-1.99584213204487,
34.5224544937789));
#19685=CARTESIAN_POINT('Ctrl Pts',(0.0919553937863713,-1.99262936043149,
34.5269031052189));
#19686=CARTESIAN_POINT('Ctrl Pts',(0.161492848290692,-1.98942036224104,
34.5313464917333));
#19687=CARTESIAN_POINT('Ctrl Pts',(0.230940724665639,-1.98256339552903,
34.5357898782477));
#19688=CARTESIAN_POINT('Ctrl Pts',(0.299888137154537,-1.97207876812616,
34.5402332647621));
#19689=CARTESIAN_POINT('Ctrl Pts',(0.368792231432232,-1.96160072799448,
34.5446738595901));
#19690=CARTESIAN_POINT('Ctrl Pts',(0.43719600303466,-1.9474996220327,34.549114454418));
#19691=CARTESIAN_POINT('Ctrl Pts',(0.504693894637496,-1.92984756787049,
34.553555049246));
#19692=CARTESIAN_POINT('Ctrl Pts',(0.572172277537509,-1.91220061562585,
34.5579943606229));
#19693=CARTESIAN_POINT('Ctrl Pts',(0.638744827134744,-1.89100487635706,
34.5624336719997));
#19694=CARTESIAN_POINT('Ctrl Pts',(0.704018131739629,-1.86638314198394,
34.5668729833766));
#19695=CARTESIAN_POINT('Ctrl Pts',(0.769294714033395,-1.84176017123424,
34.5713125176728));
#19696=CARTESIAN_POINT('Ctrl Pts',(0.833271464898335,-1.81371103872464,
34.575752051969));
#19697=CARTESIAN_POINT('Ctrl Pts',(0.895573718238352,-1.78240715822753,
34.5801915862651));
#19698=CARTESIAN_POINT('Ctrl Pts',(0.957941961885542,-1.75107012078057,
34.584635822899));
#19699=CARTESIAN_POINT('Ctrl Pts',(1.01863172991866,-1.71647167455104,34.5890800595328));
#19700=CARTESIAN_POINT('Ctrl Pts',(1.07729266710847,-1.6788293754561,34.5935242961666));
#19701=CARTESIAN_POINT('Ctrl Pts',(1.13598786669948,-1.64116509042613,34.5979711285691));
#19702=CARTESIAN_POINT('Ctrl Pts',(1.19265147936601,-1.60045369941489,34.6024179609715));
#19703=CARTESIAN_POINT('Ctrl Pts',(1.24696417519628,-1.55695469050229,34.606864793374));
#19704=CARTESIAN_POINT('Ctrl Pts',(1.30137148969778,-1.51337990154673,34.611319372646));
#19705=CARTESIAN_POINT('Ctrl Pts',(1.35341934660795,-1.46700812593735,34.6157739519181));
#19706=CARTESIAN_POINT('Ctrl Pts',(1.40282397179528,-1.41813697034402,34.6202285311901));
#19707=CARTESIAN_POINT('Ctrl Pts',(1.42914182958744,-1.39210329195526,34.6226014868266));
#19708=CARTESIAN_POINT('Ctrl Pts',(1.45471028111584,-1.36536095652903,34.624974442463));
#19709=CARTESIAN_POINT('Ctrl Pts',(1.47949120731261,-1.33795864285286,34.6273473980995));
#19710=CARTESIAN_POINT('Ctrl Pts',(1.52593847306427,-1.28659807079754,34.6317950648327));
#19711=CARTESIAN_POINT('Ctrl Pts',(1.56980163759792,-1.23271251372547,34.636242731566));
#19712=CARTESIAN_POINT('Ctrl Pts',(1.61079377487083,-1.17659295312244,34.6406903982992));
#19713=CARTESIAN_POINT('Ctrl Pts',(1.65172406374089,-1.12055806498156,34.6451313544508));
#19714=CARTESIAN_POINT('Ctrl Pts',(1.68979163478545,-1.06229625582543,34.6495723106023));
#19715=CARTESIAN_POINT('Ctrl Pts',(1.72474820872218,-1.00213331399053,34.6540132667539));
#19716=CARTESIAN_POINT('Ctrl Pts',(1.75966357094895,-0.942041300665758,
34.6584489872838));
#19717=CARTESIAN_POINT('Ctrl Pts',(1.79147497428993,-0.880053028291464,
34.6628847078137));
#19718=CARTESIAN_POINT('Ctrl Pts',(1.81997711231644,-0.816523651307357,
34.6673204283436));
#19719=CARTESIAN_POINT('Ctrl Pts',(1.84846129529373,-0.753034294938201,
34.6717533545715));
#19720=CARTESIAN_POINT('Ctrl Pts',(1.87364014748911,-0.688006206665749,
34.6761862807994));
#19721=CARTESIAN_POINT('Ctrl Pts',(1.89535477332313,-0.621818177396922,
34.6806192070273));
#19722=CARTESIAN_POINT('Ctrl Pts',(1.9170631539046,-0.555649184189858,34.6850508583199));
#19723=CARTESIAN_POINT('Ctrl Pts',(1.93530913278304,-0.488321378574417,
34.6894825096125));
#19724=CARTESIAN_POINT('Ctrl Pts',(1.94998297916001,-0.420230821675738,
34.6939141609051));
#19725=CARTESIAN_POINT('Ctrl Pts',(1.96465762871941,-0.352136537796549,
34.6983460547669));
#19726=CARTESIAN_POINT('Ctrl Pts',(1.97575965651884,-0.283279900342223,
34.7027779486288));
#19727=CARTESIAN_POINT('Ctrl Pts',(1.98323035560277,-0.214067557363853,
34.7072098424907));
#19728=CARTESIAN_POINT('Ctrl Pts',(1.99070911917502,-0.144780500877922,
34.7116465205041));
#19729=CARTESIAN_POINT('Ctrl Pts',(1.9945486774022,-0.0751374617397534,
34.7160831985174));
#19730=CARTESIAN_POINT('Ctrl Pts',(1.99474228008966,-0.00554964167354013,
34.7205198765308));
#19731=CARTESIAN_POINT('Ctrl Pts',(1.99493599756775,0.0640794383063369,
34.7249591851332));
#19732=CARTESIAN_POINT('Ctrl Pts',(1.9914794819098,0.133652743457299,34.7293984937355));
#19733=CARTESIAN_POINT('Ctrl Pts',(1.9844180350377,0.202762483504982,34.7338378023379));
#19734=CARTESIAN_POINT('Ctrl Pts',(1.97734405078291,0.271994925779874,34.7382849927967));
#19735=CARTESIAN_POINT('Ctrl Pts',(1.9666524348556,0.340761674904844,34.7427321832556));
#19736=CARTESIAN_POINT('Ctrl Pts',(1.95243978435104,0.408664227677522,34.7471793737144));
#19737=CARTESIAN_POINT('Ctrl Pts',(1.94463757281088,0.445940179877938,34.749620714315));
#19738=CARTESIAN_POINT('Ctrl Pts',(1.9357751503674,0.482955942038886,34.7520620549156));
#19739=CARTESIAN_POINT('Ctrl Pts',(1.92587478566871,0.51964783500513,34.7545033955163));
#19740=CARTESIAN_POINT('Ctrl Pts',(1.90777717078887,0.586719682186929,34.7589661040452));
#19741=CARTESIAN_POINT('Ctrl Pts',(1.88613631026345,0.652975618589625,34.7634288125741));
#19742=CARTESIAN_POINT('Ctrl Pts',(1.86104327560504,0.718014964207053,34.7678915211031));
#19743=CARTESIAN_POINT('Ctrl Pts',(1.8359880405527,0.782956335957365,34.7723475071042));
#19744=CARTESIAN_POINT('Ctrl Pts',(1.80749112789103,0.846684303467218,34.7768034931053));
#19745=CARTESIAN_POINT('Ctrl Pts',(1.77569375150756,0.908812006609178,34.7812594791064));
#19746=CARTESIAN_POINT('Ctrl Pts',(1.7439343727898,0.97086546753483,34.7857101402321));
#19747=CARTESIAN_POINT('Ctrl Pts',(1.70888258594342,1.03132203083621,34.7901608013578));
#19748=CARTESIAN_POINT('Ctrl Pts',(1.6707275031139,1.08981520123312,34.7946114624835));
#19749=CARTESIAN_POINT('Ctrl Pts',(1.6325969197808,1.14827081298483,34.799059265826));
#19750=CARTESIAN_POINT('Ctrl Pts',(1.59136725968048,1.204765125754,34.8035070691685));
#19751=CARTESIAN_POINT('Ctrl Pts',(1.54727259043397,1.25895793948477,34.8079548725109));
#19752=CARTESIAN_POINT('Ctrl Pts',(1.50319140356955,1.31313418322571,34.8124013158935));
#19753=CARTESIAN_POINT('Ctrl Pts',(1.45624725429879,1.36500994711715,34.816847759276));
#19754=CARTESIAN_POINT('Ctrl Pts',(1.40671532481837,1.41427704408336,34.8212942026585));
#19755=CARTESIAN_POINT('Ctrl Pts',(1.35718188120189,1.46354564708998,34.8257407819639));
#19756=CARTESIAN_POINT('Ctrl Pts',(1.30506084762024,1.51020508270624,34.8301873612692));
#19757=CARTESIAN_POINT('Ctrl Pts',(1.25066393995028,1.55398432160947,34.8346339405746));
#19758=CARTESIAN_POINT('Ctrl Pts',(1.19621170013645,1.59780809244015,34.8390850429085));
#19759=CARTESIAN_POINT('Ctrl Pts',(1.13947934586028,1.63874551236705,34.8435361452424));
#19760=CARTESIAN_POINT('Ctrl Pts',(1.08081056994716,1.67656675214275,34.8479872475763));
#19761=CARTESIAN_POINT('Ctrl Pts',(1.02210879094863,1.71440926759,34.8524408537994));
#19762=CARTESIAN_POINT('Ctrl Pts',(0.961468844825503,1.74913187044876,34.8568944600224));
#19763=CARTESIAN_POINT('Ctrl Pts',(0.899259836826005,1.78055028246092,34.8613480662454));
#19764=CARTESIAN_POINT('Ctrl Pts',(0.83694561152002,1.81202183405516,34.8658092050826));
#19765=CARTESIAN_POINT('Ctrl Pts',(0.773057472579082,1.84017784161958,34.8702703439197));
#19766=CARTESIAN_POINT('Ctrl Pts',(0.707984590213472,1.86488213636151,34.8747314827568));
#19767=CARTESIAN_POINT('Ctrl Pts',(0.674299687442788,1.87767028614293,34.8770407861489));
#19768=CARTESIAN_POINT('Ctrl Pts',(0.640297574963375,1.88953433152249,34.8793500895409));
#19769=CARTESIAN_POINT('Ctrl Pts',(0.606033511339024,1.90046071930837,34.8816593929329));
#19770=CARTESIAN_POINT('Ctrl Pts',(0.540549617409981,1.92134272637685,34.8860728267868));
#19771=CARTESIAN_POINT('Ctrl Pts',(0.473845937994771,1.93888046061422,34.8904862606408));
#19772=CARTESIAN_POINT('Ctrl Pts',(0.406300572580434,1.95293302681398,34.8948996944947));
#19773=CARTESIAN_POINT('Ctrl Pts',(0.338868365116361,1.96696205091611,34.8993057345752));
#19774=CARTESIAN_POINT('Ctrl Pts',(0.270597756009901,1.9775173991392,34.9037117746557));
#19775=CARTESIAN_POINT('Ctrl Pts',(0.20188253232988,1.98450774894936,34.9081178147362));
#19776=CARTESIAN_POINT('Ctrl Pts',(0.13323170122176,1.99149154814995,34.9125197259463));
#19777=CARTESIAN_POINT('Ctrl Pts',(0.064137575514188,1.99491692021807,34.9169216371564));
#19778=CARTESIAN_POINT('Ctrl Pts',(-0.00499674790325566,1.99474374168974,
34.9213235483666));
#19779=CARTESIAN_POINT('Ctrl Pts',(-0.0740908315086826,1.99457066396042,
34.9257228974328));
#19780=CARTESIAN_POINT('Ctrl Pts',(-0.143224568111221,1.99080319031719,
34.9301222464991));
#19781=CARTESIAN_POINT('Ctrl Pts',(-0.211992548267063,1.98345323160876,
34.9345215955654));
#19782=CARTESIAN_POINT('Ctrl Pts',(-0.280744914779345,1.97610494169496,
34.9389199457676));
#19783=CARTESIAN_POINT('Ctrl Pts',(-0.349131193400388,1.96517583483292,
34.9433182959697));
#19784=CARTESIAN_POINT('Ctrl Pts',(-0.416750710130754,1.95072971169906,
34.9477166461719));
#19785=CARTESIAN_POINT('Ctrl Pts',(-0.4844246825355,1.93627195474386,34.9521185384746));
#19786=CARTESIAN_POINT('Ctrl Pts',(-0.551330169253238,1.91829162441387,
34.9565204307773));
#19787=CARTESIAN_POINT('Ctrl Pts',(-0.617077406011004,1.89690353932158,
34.96092232308));
#19788=CARTESIAN_POINT('Ctrl Pts',(-0.682848740161482,1.87550761516089,
34.9653258287452));
#19789=CARTESIAN_POINT('Ctrl Pts',(-0.74746051103628,1.85070162583077,34.9697293344104));
#19790=CARTESIAN_POINT('Ctrl Pts',(-0.810541566948271,1.82264915185261,
34.9741328400756));
#19791=CARTESIAN_POINT('Ctrl Pts',(-0.873734734060834,1.79454682143988,
34.9785441718988));
#19792=CARTESIAN_POINT('Ctrl Pts',(-0.935391303863738,1.76318670442566,
34.9829555037219));
#19793=CARTESIAN_POINT('Ctrl Pts',(-0.995164032288082,1.72877879190489,
34.9873668355451));
#19794=CARTESIAN_POINT('Ctrl Pts',(-1.05200654243708,1.69605764685722,34.9915619121383));
#19795=CARTESIAN_POINT('Ctrl Pts',(-1.10714529455824,1.66058077235957,34.9957569887316));
#19796=CARTESIAN_POINT('Ctrl Pts',(-1.16030843567301,1.62256337213868,34.9999520653248));
#19797=CARTESIAN_POINT('',(1.16034898466929,1.62253437445157,35.));
#19798=CARTESIAN_POINT('Origin',(0.,0.,35.));
#19799=CARTESIAN_POINT('',(-1.99474961222923,-0.00124378911175134,34.4790451185704));
#19800=CARTESIAN_POINT('Ctrl Pts',(-1.99474961222889,-0.00124378964630918,
34.4790451186047));
#19801=CARTESIAN_POINT('Ctrl Pts',(-1.99470965583835,-0.0653245566594018,
34.4831554158475));
#19802=CARTESIAN_POINT('Ctrl Pts',(-1.99158209595733,-0.129314909989991,
34.4872657130903));
#19803=CARTESIAN_POINT('Ctrl Pts',(-1.9853913538538,-0.192999312285264,
34.4913760103331));
#19804=CARTESIAN_POINT('Ctrl Pts',(-1.97866982777472,-0.262143909766435,
34.4958387176544));
#19805=CARTESIAN_POINT('Ctrl Pts',(-1.96831880424879,-0.331071626911279,
34.5003014249758));
#19806=CARTESIAN_POINT('Ctrl Pts',(-1.95436163129808,-0.399372228140521,
34.5047641322972));
#19807=CARTESIAN_POINT('Ctrl Pts',(-1.94042548309976,-0.467569942973346,
34.5092201171027));
#19808=CARTESIAN_POINT('Ctrl Pts',(-1.92289406513358,-0.535141943202289,
34.5136761019082));
#19809=CARTESIAN_POINT('Ctrl Pts',(-1.90184246552371,-0.601683304430749,
34.5181320867137));
#19810=CARTESIAN_POINT('Ctrl Pts',(-1.88081602234114,-0.668145149472913,
34.522582746667));
#19811=CARTESIAN_POINT('Ctrl Pts',(-1.85627789992849,-0.733578339405207,
34.5270334066202));
#19812=CARTESIAN_POINT('Ctrl Pts',(-1.8283537991141,-0.797590087554399,
34.5314840665735));
#19813=CARTESIAN_POINT('Ctrl Pts',(-1.80044762836177,-0.861560733767165,
34.5359318687585));
#19814=CARTESIAN_POINT('Ctrl Pts',(-1.76915998727677,-0.924111303249376,
34.5403796709435));
#19815=CARTESIAN_POINT('Ctrl Pts',(-1.73466527106065,-0.984867483408844,
34.5448274731285));
#19816=CARTESIAN_POINT('Ctrl Pts',(-1.70018110182025,-1.04560508698538,
34.5492739153701));
#19817=CARTESIAN_POINT('Ctrl Pts',(-1.66249204486713,-1.10454896679754,
34.5537203576116));
#19818=CARTESIAN_POINT('Ctrl Pts',(-1.62181835050051,-1.16134955998606,
34.5581667998532));
#19819=CARTESIAN_POINT('Ctrl Pts',(-1.58114341261805,-1.21815188973769,
34.5626133780358));
#19820=CARTESIAN_POINT('Ctrl Pts',(-1.53748394189366,-1.27281040775946,
34.5670599562184));
#19821=CARTESIAN_POINT('Ctrl Pts',(-1.49110237966126,-1.32500613427581,
34.5715065344009));
#19822=CARTESIAN_POINT('Ctrl Pts',(-1.44467363806279,-1.37725495433127,
34.5759576356467));
#19823=CARTESIAN_POINT('Ctrl Pts',(-1.39551760247024,-1.42703561726791,
34.5804087368925));
#19824=CARTESIAN_POINT('Ctrl Pts',(-1.34393508215423,-1.47406446855458,
34.5848598381383));
#19825=CARTESIAN_POINT('Ctrl Pts',(-1.2923235447832,-1.52111977529083,34.5893134432915));
#19826=CARTESIAN_POINT('Ctrl Pts',(-1.23828318225281,-1.56541987915142,
34.5937670484446));
#19827=CARTESIAN_POINT('Ctrl Pts',(-1.18214741987205,-1.60672183037073,
34.5982206535977));
#19828=CARTESIAN_POINT('Ctrl Pts',(-1.12591671166209,-1.64809363809219,
34.6026817914041));
#19829=CARTESIAN_POINT('Ctrl Pts',(-1.0675839358362,-1.68645690198636,34.6071429292105));
#19830=CARTESIAN_POINT('Ctrl Pts',(-1.00751028473955,-1.72161278708194,
34.6116040670169));
#19831=CARTESIAN_POINT('Ctrl Pts',(-0.976413083945413,-1.73981127507052,
34.6139133805946));
#19832=CARTESIAN_POINT('Ctrl Pts',(-0.944849779950104,-1.75715106896168,
34.6162226941722));
#19833=CARTESIAN_POINT('Ctrl Pts',(-0.912872618442756,-1.77360963715172,
34.6185320077498));
#19834=CARTESIAN_POINT('Ctrl Pts',(-0.851111131992418,-1.80539812582129,
34.6229922735305));
#19835=CARTESIAN_POINT('Ctrl Pts',(-0.787568603186281,-1.83401781075126,
34.6274525393112));
#19836=CARTESIAN_POINT('Ctrl Pts',(-0.722602739111021,-1.85926674899791,
34.6319128050919));
#19837=CARTESIAN_POINT('Ctrl Pts',(-0.657732762387549,-1.88447842069145,
34.6363664876757));
#19838=CARTESIAN_POINT('Ctrl Pts',(-0.591444071614061,-1.90632904581292,
34.6408201702595));
#19839=CARTESIAN_POINT('Ctrl Pts',(-0.524117845427371,-1.92466309950718,
34.6452738528433));
#19840=CARTESIAN_POINT('Ctrl Pts',(-0.456868876270491,-1.94297611482437,
34.6497224248141));
#19841=CARTESIAN_POINT('Ctrl Pts',(-0.388585205056955,-1.95778044624095,
34.6541709967849));
#19842=CARTESIAN_POINT('Ctrl Pts',(-0.319665143225316,-1.96896972010916,
34.6586195687557));
#19843=CARTESIAN_POINT('Ctrl Pts',(-0.25078728816113,-1.98015214164631,
34.6630654164132));
#19844=CARTESIAN_POINT('Ctrl Pts',(-0.181274296205601,-1.98772381995354,
34.6675112640706));
#19845=CARTESIAN_POINT('Ctrl Pts',(-0.111535216559958,-1.99162934753606,
34.6719571117281));
#19846=CARTESIAN_POINT('Ctrl Pts',(-0.041815350350925,-1.99553379912781,
34.6764017345341));
#19847=CARTESIAN_POINT('Ctrl Pts',(0.0281299930082953,-1.99577407809619,
34.6808463573401));
#19848=CARTESIAN_POINT('Ctrl Pts',(0.0978878467608373,-1.99234673989156,
34.6852909801462));
#19849=CARTESIAN_POINT('Ctrl Pts',(0.16764998223558,-1.98891919131764,34.6897358757622));
#19850=CARTESIAN_POINT('Ctrl Pts',(0.237224118103609,-1.98182360491614,
34.6941807713782));
#19851=CARTESIAN_POINT('Ctrl Pts',(0.306200262956401,-1.97110856156261,
34.6986256669942));
#19852=CARTESIAN_POINT('Ctrl Pts',(0.375249952031826,-1.96038209354139,
34.7030753018776));
#19853=CARTESIAN_POINT('Ctrl Pts',(0.443699894468999,-1.94602854096107,
34.707524936761));
#19854=CARTESIAN_POINT('Ctrl Pts',(0.511149113271741,-1.92814785390061,
34.7119745716444));
#19855=CARTESIAN_POINT('Ctrl Pts',(0.578638115626237,-1.91025662028006,
34.7164268310546));
#19856=CARTESIAN_POINT('Ctrl Pts',(0.645124754911799,-1.88883426064622,
34.7208790904648));
#19857=CARTESIAN_POINT('Ctrl Pts',(0.710224732460111,-1.86403014779857,
34.7253313498749));
#19858=CARTESIAN_POINT('Ctrl Pts',(0.775437769193194,-1.83918295762766,
34.7297913415277));
#19859=CARTESIAN_POINT('Ctrl Pts',(0.839258890766058,-1.81094248763635,
34.7342513331804));
#19860=CARTESIAN_POINT('Ctrl Pts',(0.901325948867879,-1.77950529541146,
34.7387113248332));
#19861=CARTESIAN_POINT('Ctrl Pts',(0.933689389379248,-1.76311309427401,
34.7410368849443));
#19862=CARTESIAN_POINT('Ctrl Pts',(0.965576363354185,-1.74585249339734,
34.7433624450554));
#19863=CARTESIAN_POINT('Ctrl Pts',(0.996938704649294,-1.72775599598791,
34.7456880051665));
#19864=CARTESIAN_POINT('Ctrl Pts',(1.0563508981099,-1.69347435244187,34.7500934998304));
#19865=CARTESIAN_POINT('Ctrl Pts',(1.11412509718853,-1.65604807414781,34.7544989944944));
#19866=CARTESIAN_POINT('Ctrl Pts',(1.16990273560751,-1.61565935509874,34.7589044891584));
#19867=CARTESIAN_POINT('Ctrl Pts',(1.2255952124592,-1.57533230174066,34.7633032574919));
#19868=CARTESIAN_POINT('Ctrl Pts',(1.27929677257618,-1.53205206939976,34.7677020258253));
#19869=CARTESIAN_POINT('Ctrl Pts',(1.3306744502896,-1.48604611969026,34.7721007941588));
#19870=CARTESIAN_POINT('Ctrl Pts',(1.38199285826681,-1.44009324284479,34.7764944880348));
#19871=CARTESIAN_POINT('Ctrl Pts',(1.43099233254781,-1.39142122092301,34.7808881819109));
#19872=CARTESIAN_POINT('Ctrl Pts',(1.47737142017283,-1.34029894029522,34.7852818757869));
#19873=CARTESIAN_POINT('Ctrl Pts',(1.52372217860752,-1.28920788608634,34.7896728859148));
#19874=CARTESIAN_POINT('Ctrl Pts',(1.56745538696022,-1.23566990986244,34.7940638960427));
#19875=CARTESIAN_POINT('Ctrl Pts',(1.60830629585188,-1.17999085641509,34.7984549061706));
#19876=CARTESIAN_POINT('Ctrl Pts',(1.64914684967132,-1.12432591674476,34.8028448032455));
#19877=CARTESIAN_POINT('Ctrl Pts',(1.68710625695501,-1.06652138023251,34.8072347003204));
#19878=CARTESIAN_POINT('Ctrl Pts',(1.72196116123219,-1.00691475394291,34.8116245973952));
#19879=CARTESIAN_POINT('Ctrl Pts',(1.75681968526789,-0.947301937373964,
34.8160149503706));
#19880=CARTESIAN_POINT('Ctrl Pts',(1.78857281587677,-0.885887093569423,
34.820405303346));
#19881=CARTESIAN_POINT('Ctrl Pts',(1.81704249578212,-0.823033493256425,
34.8247956563213));
#19882=CARTESIAN_POINT('Ctrl Pts',(1.84554707497725,-0.760102844447701,
34.8291913911697));
#19883=CARTESIAN_POINT('Ctrl Pts',(1.87075996451608,-0.695730377162034,
34.833587126018));
#19884=CARTESIAN_POINT('Ctrl Pts',(1.89255117354373,-0.63029962558949,34.8379828608663));
#19885=CARTESIAN_POINT('Ctrl Pts',(1.91435672909789,-0.564825796828756,
34.842381489704));
#19886=CARTESIAN_POINT('Ctrl Pts',(1.93273599313613,-0.498292781634358,
34.8467801185417));
#19887=CARTESIAN_POINT('Ctrl Pts',(1.94760963476504,-0.431096593665931,
34.8511787473793));
#19888=CARTESIAN_POINT('Ctrl Pts',(1.96251284200395,-0.363766834085676,
34.8555861197478));
#19889=CARTESIAN_POINT('Ctrl Pts',(1.97389643842135,-0.295771764791792,
34.8599934921164));
#19890=CARTESIAN_POINT('Ctrl Pts',(1.98173280701928,-0.227514052496768,
34.8644008644849));
#19891=CARTESIAN_POINT('Ctrl Pts',(1.98673681218226,-0.183927289001692,
34.867215243851));
#19892=CARTESIAN_POINT('Ctrl Pts',(1.99029545462308,-0.14023349302073,34.8700296232172));
#19893=CARTESIAN_POINT('Ctrl Pts',(1.9924126509726,-0.0965369915853482,
34.8728440025833));
#19894=CARTESIAN_POINT('Ctrl Pts',(1.99585743825963,-0.0254405376988781,
34.8774231424743));
#19895=CARTESIAN_POINT('Ctrl Pts',(1.9954980008896,0.0459551382969561,34.8820022823654));
#19896=CARTESIAN_POINT('Ctrl Pts',(1.99130272330465,0.117222125298427,34.8865814222565));
#19897=CARTESIAN_POINT('Ctrl Pts',(1.98697310365769,0.190771238760697,34.8913071963291));
#19898=CARTESIAN_POINT('Ctrl Pts',(1.97855768336608,0.264182799724639,34.8960329704018));
#19899=CARTESIAN_POINT('Ctrl Pts',(1.96607994072682,0.336982535410391,34.9007587444744));
#19900=CARTESIAN_POINT('Ctrl Pts',(1.95402968050572,0.407288181583975,34.9053226154379));
#19901=CARTESIAN_POINT('Ctrl Pts',(1.93819099945231,0.477022746940168,34.9098864864015));
#19902=CARTESIAN_POINT('Ctrl Pts',(1.91863774874258,0.545762541404237,34.914450357365));
#19903=CARTESIAN_POINT('Ctrl Pts',(1.89910305268284,0.614437106672102,34.9190098975382));
#19904=CARTESIAN_POINT('Ctrl Pts',(1.87586091671168,0.68211833980894,34.9235694377114));
#19905=CARTESIAN_POINT('Ctrl Pts',(1.84903594885902,0.748394028788993,34.9281289778847));
#19906=CARTESIAN_POINT('Ctrl Pts',(1.82222923950999,0.814624607000826,34.9326854145917));
#19907=CARTESIAN_POINT('Ctrl Pts',(1.79184471751014,0.879451120919967,34.9372418512987));
#19908=CARTESIAN_POINT('Ctrl Pts',(1.75805595896161,0.94247907544919,34.9417982880058));
#19909=CARTESIAN_POINT('Ctrl Pts',(1.72428114286142,1.00548102239372,34.9463528445643));
#19910=CARTESIAN_POINT('Ctrl Pts',(1.68710510012319,1.06668548456953,34.9509074011229));
#19911=CARTESIAN_POINT('Ctrl Pts',(1.64674780710277,1.12572164512468,34.9554619576814));
#19912=CARTESIAN_POINT('Ctrl Pts',(1.6063852328958,1.18476553119741,34.9600171102527));
#19913=CARTESIAN_POINT('Ctrl Pts',(1.56284082884428,1.24164016816606,34.9645722628241));
#19914=CARTESIAN_POINT('Ctrl Pts',(1.51637789034378,1.2960037253714,34.9691274153954));
#19915=CARTESIAN_POINT('Ctrl Pts',(1.46991192230367,1.35037082726321,34.973682864978));
#19916=CARTESIAN_POINT('Ctrl Pts',(1.42052734378007,1.40222618176822,34.9782383145605));
#19917=CARTESIAN_POINT('Ctrl Pts',(1.36852654774444,1.45126243340709,34.9827937641431));
#19918=CARTESIAN_POINT('Ctrl Pts',(1.31649062216685,1.50033181186693,34.9873522911951));
#19919=CARTESIAN_POINT('Ctrl Pts',(1.26183528935258,1.54657797917796,34.991910818247));
#19920=CARTESIAN_POINT('Ctrl Pts',(1.20489776833193,1.58973234551252,34.996469345299));
#19921=CARTESIAN_POINT('Ctrl Pts',(1.19019808398469,1.60087360266513,34.9976462301993));
#19922=CARTESIAN_POINT('Ctrl Pts',(1.1753464469573,1.61180899912977,34.9988231150997));
#19923=CARTESIAN_POINT('Ctrl Pts',(1.16034898466929,1.62253437445157,35.));
#19924=CARTESIAN_POINT('',(-1.99474967239366,-0.00114323460825715,33.6790451186519));
#19925=CARTESIAN_POINT('Ctrl Pts',(-1.99474967239366,-0.00114323460825715,
33.6790451186519));
#19926=CARTESIAN_POINT('Ctrl Pts',(-1.99470505520098,-0.0789926365181883,
33.6839926278254));
#19927=CARTESIAN_POINT('Ctrl Pts',(-1.99009895797611,-0.156676925226695,
33.6889401369989));
#19928=CARTESIAN_POINT('Ctrl Pts',(-1.98101371068683,-0.233692619846631,
33.6938876461724));
#19929=CARTESIAN_POINT('Ctrl Pts',(-1.97189090305347,-0.311026713723905,
33.6988556094009));
#19930=CARTESIAN_POINT('Ctrl Pts',(-1.95825197165493,-0.387686411871911,
33.7038235726293));
#19931=CARTESIAN_POINT('Ctrl Pts',(-1.94022999868426,-0.463179354792175,
33.7087915358577));
#19932=CARTESIAN_POINT('Ctrl Pts',(-1.922115047508,-0.539061777731016,33.7137851295932));
#19933=CARTESIAN_POINT('Ctrl Pts',(-1.8995718510703,-0.613765121854765,
33.7187787233288));
#19934=CARTESIAN_POINT('Ctrl Pts',(-1.87278362166587,-0.686810795576234,
33.7237723170643));
#19935=CARTESIAN_POINT('Ctrl Pts',(-1.8644369505841,-0.709570351771406,
33.7253282199871));
#19936=CARTESIAN_POINT('Ctrl Pts',(-1.85567850453098,-0.732169148883617,
33.7268841229099));
#19937=CARTESIAN_POINT('Ctrl Pts',(-1.84651473842679,-0.754593190581943,
33.7284400258326));
#19938=CARTESIAN_POINT('Ctrl Pts',(-1.82028118708606,-0.818787566831978,
33.7328941835165));
#19939=CARTESIAN_POINT('Ctrl Pts',(-1.79064410943348,-0.881739403773629,
33.7373483412003));
#19940=CARTESIAN_POINT('Ctrl Pts',(-1.75774259151952,-0.943063383054522,
33.7418024988842));
#19941=CARTESIAN_POINT('Ctrl Pts',(-1.72489053463828,-1.0042951736603,33.7462499606083));
#19942=CARTESIAN_POINT('Ctrl Pts',(-1.68878400713422,-1.06390353577771,
33.7506974223324));
#19943=CARTESIAN_POINT('Ctrl Pts',(-1.64961016594262,-1.12152301042768,
33.7551448840565));
#19944=CARTESIAN_POINT('Ctrl Pts',(-1.61048252131381,-1.17907453611992,
33.7595871010194));
#19945=CARTESIAN_POINT('Ctrl Pts',(-1.5682950211204,-1.23464142980895,33.7640293179822));
#19946=CARTESIAN_POINT('Ctrl Pts',(-1.52327985760852,-1.28788432629029,
33.7684715349451));
#19947=CARTESIAN_POINT('Ctrl Pts',(-1.47829310101842,-1.34109362372015,
33.7729109486368));
#19948=CARTESIAN_POINT('Ctrl Pts',(-1.43048253628969,-1.39198146031091,
33.7773503623285));
#19949=CARTESIAN_POINT('Ctrl Pts',(-1.38012171989822,-1.44024011913472,
33.7817897760202));
#19950=CARTESIAN_POINT('Ctrl Pts',(-1.32977557335486,-1.48848472045815,
33.7862278965334));
#19951=CARTESIAN_POINT('Ctrl Pts',(-1.27688100314554,-1.53410132585811,
33.7906660170466));
#19952=CARTESIAN_POINT('Ctrl Pts',(-1.22174839272104,-1.57681908517863,
33.7951041375598));
#19953=CARTESIAN_POINT('Ctrl Pts',(-1.16661311098122,-1.61953891428332,
33.7995424731112));
#19954=CARTESIAN_POINT('Ctrl Pts',(-1.10923996216822,-1.65935932051046,
33.8039808086627));
#19955=CARTESIAN_POINT('Ctrl Pts',(-1.049970950935,-1.69605087326196,33.8084191442141));
#19956=CARTESIAN_POINT('Ctrl Pts',(-0.990639192548068,-1.73278127077318,
33.8128621785604));
#19957=CARTESIAN_POINT('Ctrl Pts',(-0.929407982682463,-1.76637594508789,
33.8173052129066));
#19958=CARTESIAN_POINT('Ctrl Pts',(-0.866645918674512,-1.79665033162962,
33.8217482472529));
#19959=CARTESIAN_POINT('Ctrl Pts',(-0.803847240581718,-1.82694237961978,
33.8261938735731));
#19960=CARTESIAN_POINT('Ctrl Pts',(-0.739516382396525,-1.8539100951532,
33.8306394998934));
#19961=CARTESIAN_POINT('Ctrl Pts',(-0.67404142839136,-1.8774172991938,33.8350851262136));
#19962=CARTESIAN_POINT('Ctrl Pts',(-0.608452273729243,-1.90096550422761,
33.8395385065438));
#19963=CARTESIAN_POINT('Ctrl Pts',(-0.541715508565356,-1.92104100824494,
33.843991886874));
#19964=CARTESIAN_POINT('Ctrl Pts',(-0.474233081564563,-1.9375578821934,
33.8484452672042));
#19965=CARTESIAN_POINT('Ctrl Pts',(-0.438114422849897,-1.94639821825853,
33.8508288525526));
#19966=CARTESIAN_POINT('Ctrl Pts',(-0.401782311076133,-1.95421998611483,
33.853212437901));
#19967=CARTESIAN_POINT('Ctrl Pts',(-0.365299029535839,-1.96101610944943,
33.8555960232494));
#19968=CARTESIAN_POINT('Ctrl Pts',(-0.2971215359886,-1.97371624592918,33.860050306632));
#19969=CARTESIAN_POINT('Ctrl Pts',(-0.228146046863805,-1.98288184402868,
33.8645045900147));
#19970=CARTESIAN_POINT('Ctrl Pts',(-0.15877185441207,-1.98842124831399,
33.8689588733973));
#19971=CARTESIAN_POINT('Ctrl Pts',(-0.0895019000726365,-1.99395232937382,
33.8734064640017));
#19972=CARTESIAN_POINT('Ctrl Pts',(-0.0198349153927554,-1.99586799200378,
33.877854054606));
#19973=CARTESIAN_POINT('Ctrl Pts',(0.0498204823198855,-1.9941277496794,
33.8823016452103));
#19974=CARTESIAN_POINT('Ctrl Pts',(0.119393803054987,-1.99238955793307,
33.8867439950895));
#19975=CARTESIAN_POINT('Ctrl Pts',(0.188955076952801,-1.98700402937793,
33.8911863449687));
#19976=CARTESIAN_POINT('Ctrl Pts',(0.258093246057805,-1.97798266899368,
33.8956286948479));
#19977=CARTESIAN_POINT('Ctrl Pts',(0.327187824276703,-1.96896699648195,
33.9000682438724));
#19978=CARTESIAN_POINT('Ctrl Pts',(0.395859342642638,-1.95632010285085,
33.9045077928968));
#19979=CARTESIAN_POINT('Ctrl Pts',(0.463700960007945,-1.94010540491689,
33.9089473419213));
#19980=CARTESIAN_POINT('Ctrl Pts',(0.531522849594134,-1.92389542208246,
33.9133855999617));
#19981=CARTESIAN_POINT('Ctrl Pts',(0.598514841410656,-1.90411980826287,
33.9178238580022));
#19982=CARTESIAN_POINT('Ctrl Pts',(0.664281154596361,-1.88089290235997,
33.9222621160427));
#19983=CARTESIAN_POINT('Ctrl Pts',(0.730050683493869,-1.85766486075352,
33.9267005910963));
#19984=CARTESIAN_POINT('Ctrl Pts',(0.794593954013738,-1.83098535728792,
33.93113906615));
#19985=CARTESIAN_POINT('Ctrl Pts',(0.857532891273935,-1.80101774085748,
33.9355775412037));
#19986=CARTESIAN_POINT('Ctrl Pts',(0.9205384872393,-1.77101838568794,33.9400207170517));
#19987=CARTESIAN_POINT('Ctrl Pts',(0.981935915679973,-1.73772417761029,
33.9444638928997));
#19988=CARTESIAN_POINT('Ctrl Pts',(1.0413704272109,-1.70134511367641,33.9489070687477));
#19989=CARTESIAN_POINT('Ctrl Pts',(1.10083962847878,-1.6649448166218,33.9533528379139));
#19990=CARTESIAN_POINT('Ctrl Pts',(1.15834322883593,-1.62545635715317,33.9577986070802));
#19991=CARTESIAN_POINT('Ctrl Pts',(1.21355661016748,-1.58313231172218,33.9622443762464));
#19992=CARTESIAN_POINT('Ctrl Pts',(1.26886629759555,-1.54073444245526,33.9666978999581));
#19993=CARTESIAN_POINT('Ctrl Pts',(1.32187741951533,-1.49549143189135,33.9711514236697));
#19994=CARTESIAN_POINT('Ctrl Pts',(1.37230010035973,-1.44769471818221,33.9756049473814));
#19995=CARTESIAN_POINT('Ctrl Pts',(1.39927309362224,-1.42212645375722,33.977987305143));
#19996=CARTESIAN_POINT('Ctrl Pts',(1.42550603583875,-1.39582803407515,33.9803696629046));
#19997=CARTESIAN_POINT('Ctrl Pts',(1.45095931925126,-1.36884791572253,33.9827520206661));
#19998=CARTESIAN_POINT('Ctrl Pts',(1.49853658081032,-1.31841669524094,33.9872051223156));
#19999=CARTESIAN_POINT('Ctrl Pts',(1.54357589213584,-1.26540192235272,33.9916582239652));
#20000=CARTESIAN_POINT('Ctrl Pts',(1.58578405289311,-1.21008945954004,33.9961113256147));
#20001=CARTESIAN_POINT('Ctrl Pts',(1.62792873852477,-1.15486017887654,34.0005577304269));
#20002=CARTESIAN_POINT('Ctrl Pts',(1.66725042916285,-1.09734045249745,34.0050041352391));
#20003=CARTESIAN_POINT('Ctrl Pts',(1.70349388381983,-1.03785169956427,34.0094505400512));
#20004=CARTESIAN_POINT('Ctrl Pts',(1.73969461790375,-0.978433066702129,
34.0138917038354));
#20005=CARTESIAN_POINT('Ctrl Pts',(1.77282406866205,-0.917050433091979,
34.0183328676196));
#20006=CARTESIAN_POINT('Ctrl Pts',(1.80266937724758,-0.854055430773574,
34.0227740314037));
#20007=CARTESIAN_POINT('Ctrl Pts',(1.83249586674141,-0.79110015023325,34.0272123947924));
#20008=CARTESIAN_POINT('Ctrl Pts',(1.85904211283213,-0.726534959419857,
34.031650758181));
#20009=CARTESIAN_POINT('Ctrl Pts',(1.88214117995257,-0.660736060183446,
34.0360891215697));
#20010=CARTESIAN_POINT('Ctrl Pts',(1.90523353970721,-0.594956267228886,
34.0405261961735));
#20011=CARTESIAN_POINT('Ctrl Pts',(1.92488054539363,-0.527943938899148,
34.0449632707773));
#20012=CARTESIAN_POINT('Ctrl Pts',(1.94096406042321,-0.460093554231588,
34.0494003453812));
#20013=CARTESIAN_POINT('Ctrl Pts',(1.9570483763665,-0.392239790806103,34.0538376409388));
#20014=CARTESIAN_POINT('Ctrl Pts',(1.96956873870942,-0.323548365321683,
34.0582749364964));
#20015=CARTESIAN_POINT('Ctrl Pts',(1.97845780201861,-0.254425407795087,
34.0627122320541));
#20016=CARTESIAN_POINT('Ctrl Pts',(1.98735631033948,-0.185229004156309,
34.0671542424289));
#20017=CARTESIAN_POINT('Ctrl Pts',(1.99261575586071,-0.115600640050258,
34.0715962528037));
#20018=CARTESIAN_POINT('Ctrl Pts',(1.99422064170287,-0.0459520914235337,
34.0760382631785));
#20019=CARTESIAN_POINT('Ctrl Pts',(1.9958264667438,0.0237372163832464,34.080482873072));
#20020=CARTESIAN_POINT('Ctrl Pts',(1.99377348981726,0.0934462425034592,
34.0849274829655));
#20021=CARTESIAN_POINT('Ctrl Pts',(1.98809832646439,0.162765496372865,34.0893720928589));
#20022=CARTESIAN_POINT('Ctrl Pts',(1.9824132334389,0.232206036177869,34.0938244793605));
#20023=CARTESIAN_POINT('Ctrl Pts',(1.97309336851641,0.301254957072016,34.098276865862));
#20024=CARTESIAN_POINT('Ctrl Pts',(1.96022682995715,0.369510943838119,34.1027292523635));
#20025=CARTESIAN_POINT('Ctrl Pts',(1.95331174700821,0.406194921278941,34.10512217427));
#20026=CARTESIAN_POINT('Ctrl Pts',(1.94537307969884,0.442650080962574,34.1075150961765));
#20027=CARTESIAN_POINT('Ctrl Pts',(1.93643040766279,0.47881608032617,34.1099080180829));
#20028=CARTESIAN_POINT('Ctrl Pts',(1.91978115192599,0.546149084371742,34.114363103612));
#20029=CARTESIAN_POINT('Ctrl Pts',(1.89958287229591,0.612745779472168,34.1188181891411));
#20030=CARTESIAN_POINT('Ctrl Pts',(1.87591738645606,0.678204631134182,34.1232732746701));
#20031=CARTESIAN_POINT('Ctrl Pts',(1.8522874912097,0.743565039037421,34.127721660183));
#20032=CARTESIAN_POINT('Ctrl Pts',(1.82520090407882,0.807790543440501,34.1321700456959));
#20033=CARTESIAN_POINT('Ctrl Pts',(1.79478988370777,0.870492295106765,34.1366184312088));
#20034=CARTESIAN_POINT('Ctrl Pts',(1.76441478933691,0.933119974179799,34.14106156163));
#20035=CARTESIAN_POINT('Ctrl Pts',(1.7307232745168,0.994227037629293,34.1455046920513));
#20036=CARTESIAN_POINT('Ctrl Pts',(1.69389593896112,1.05344392848933,34.1499478224725));
#20037=CARTESIAN_POINT('Ctrl Pts',(1.65709189562652,1.11262336638427,34.1543881427427));
#20038=CARTESIAN_POINT('Ctrl Pts',(1.61715622387695,1.16991458873398,34.1588284630129));
#20039=CARTESIAN_POINT('Ctrl Pts',(1.57431503903815,1.22497335495851,34.1632687832831));
#20040=CARTESIAN_POINT('Ctrl Pts',(1.53148640979262,1.28001598494691,34.1677078022154));
#20041=CARTESIAN_POINT('Ctrl Pts',(1.48575425823248,1.33282707167784,34.1721468211478));
#20042=CARTESIAN_POINT('Ctrl Pts',(1.43738648438939,1.38309350985199,34.1765858400801));
#20043=CARTESIAN_POINT('Ctrl Pts',(1.389016470411,1.43336227609738,34.181025064604));
#20044=CARTESIAN_POINT('Ctrl Pts',(1.33801093279439,1.48108580885929,34.1854642891278));
#20045=CARTESIAN_POINT('Ctrl Pts',(1.28467506801115,1.52598739579675,34.1899035136516));
#20046=CARTESIAN_POINT('Ctrl Pts',(1.23128299244483,1.57093630461366,34.1943474166838));
#20047=CARTESIAN_POINT('Ctrl Pts',(1.17555606281593,1.61305701572653,34.198791319716));
#20048=CARTESIAN_POINT('Ctrl Pts',(1.11783229705301,1.65211334906694,34.2032352227481));
#20049=CARTESIAN_POINT('Ctrl Pts',(1.06007499560169,1.69119237290594,34.2076817075478));
#20050=CARTESIAN_POINT('Ctrl Pts',(1.0003189681262,1.72720322270235,34.2121281923476));
#20051=CARTESIAN_POINT('Ctrl Pts',(0.938928539316298,1.75995476094057,34.2165746771473));
#20052=CARTESIAN_POINT('Ctrl Pts',(0.877431399751455,1.79276322892237,34.2210288909654));
#20053=CARTESIAN_POINT('Ctrl Pts',(0.814294630900114,1.82230086868221,34.2254831047835));
#20054=CARTESIAN_POINT('Ctrl Pts',(0.749903571495696,1.84842424674586,34.2299373186015));
#20055=CARTESIAN_POINT('Ctrl Pts',(0.715561891006039,1.86235662666118,34.2323128842342));
#20056=CARTESIAN_POINT('Ctrl Pts',(0.680863721592592,1.87531869413497,34.2346884498669));
#20057=CARTESIAN_POINT('Ctrl Pts',(0.645869034668112,1.88729455903335,34.2370640154996));
#20058=CARTESIAN_POINT('Ctrl Pts',(0.580237742985919,1.90975486805078,34.2415193044206));
#20059=CARTESIAN_POINT('Ctrl Pts',(0.513304158713682,1.92883182304986,34.2459745933416));
#20060=CARTESIAN_POINT('Ctrl Pts',(0.445450283229097,1.9443769201652,34.2504298822626));
#20061=CARTESIAN_POINT('Ctrl Pts',(0.377698123176603,1.95989871461347,34.2548784925431));
#20062=CARTESIAN_POINT('Ctrl Pts',(0.309028883059356,1.97189905106972,34.2593271028237));
#20063=CARTESIAN_POINT('Ctrl Pts',(0.239841189049589,1.98027870930717,34.2637757131042));
#20064=CARTESIAN_POINT('Ctrl Pts',(0.170734756599664,1.98864852556176,34.2682190984526));
#20065=CARTESIAN_POINT('Ctrl Pts',(0.101111563046058,1.99340605122536,34.2726624838009));
#20066=CARTESIAN_POINT('Ctrl Pts',(0.0313801705448466,1.99450315803124,
34.2771058691493));
#20067=CARTESIAN_POINT('Ctrl Pts',(-0.0383074111212352,1.99559957554691,
34.2815464628077));
#20068=CARTESIAN_POINT('Ctrl Pts',(-0.108102568826947,1.99304012884137,
34.2859870564662));
#20069=CARTESIAN_POINT('Ctrl Pts',(-0.17759340119426,1.98682866557543,34.2904276501246));
#20070=CARTESIAN_POINT('Ctrl Pts',(-0.247064148813438,1.980618997592,34.2948669603303));
#20071=CARTESIAN_POINT('Ctrl Pts',(-0.31623025866382,1.97075945203409,34.2993062705359));
#20072=CARTESIAN_POINT('Ctrl Pts',(-0.384683401264078,1.95730586350011,
34.3037455807416));
#20073=CARTESIAN_POINT('Ctrl Pts',(-0.453139981230015,1.94385159939592,
34.3081851138666));
#20074=CARTESIAN_POINT('Ctrl Pts',(-0.520883043276488,1.92680303069498,
34.3126246469916));
#20075=CARTESIAN_POINT('Ctrl Pts',(-0.587514678796769,1.90626704968069,
34.3170641801166));
#20076=CARTESIAN_POINT('Ctrl Pts',(-0.654216890429641,1.88570931699099,
34.3215084155874));
#20077=CARTESIAN_POINT('Ctrl Pts',(-0.719804857395406,1.86165694359622,
34.3259526510582));
#20078=CARTESIAN_POINT('Ctrl Pts',(-0.783896991458646,1.83426635723444,
34.330396886529));
#20079=CARTESIAN_POINT('Ctrl Pts',(-0.848026560202037,1.80685977268731,
34.3348437177713));
#20080=CARTESIAN_POINT('Ctrl Pts',(-0.910658117742679,1.77611130996026,
34.3392905490136));
#20081=CARTESIAN_POINT('Ctrl Pts',(-0.971433715979074,1.74222389432561,
34.3437373802559));
#20082=CARTESIAN_POINT('Ctrl Pts',(-1.03231519222989,1.70827744295317,34.3481919583846));
#20083=CARTESIAN_POINT('Ctrl Pts',(-1.09133384074268,1.67118138300511,34.3526465365134));
#20084=CARTESIAN_POINT('Ctrl Pts',(-1.14816045382085,1.63118212802308,34.3571011146422));
#20085=CARTESIAN_POINT('Ctrl Pts',(-1.17843214780047,1.60987441424884,34.3594740807336));
#20086=CARTESIAN_POINT('Ctrl Pts',(-1.20808235829674,1.58774354703447,34.361847046825));
#20087=CARTESIAN_POINT('Ctrl Pts',(-1.23706541921401,1.56483120849658,34.3642200129164));
#20088=CARTESIAN_POINT('Ctrl Pts',(-1.29072717782349,1.52240931305536,34.3686135286305));
#20089=CARTESIAN_POINT('Ctrl Pts',(-1.34232494613137,1.47712826218427,34.3730070443447));
#20090=CARTESIAN_POINT('Ctrl Pts',(-1.39153172153462,1.4292190281629,34.3774005600589));
#20091=CARTESIAN_POINT('Ctrl Pts',(-1.44065389242058,1.38139216770868,34.3817865217061));
#20092=CARTESIAN_POINT('Ctrl Pts',(-1.48739287342646,1.3309464427752,34.3861724833533));
#20093=CARTESIAN_POINT('Ctrl Pts',(-1.53145375128017,1.2781537349591,34.3905584450005));
#20094=CARTESIAN_POINT('Ctrl Pts',(-1.57547233404685,1.22541170412177,34.3949401964585));
#20095=CARTESIAN_POINT('Ctrl Pts',(-1.61681758648526,1.17032753936153,34.3993219479166));
#20096=CARTESIAN_POINT('Ctrl Pts',(-1.65523165992728,1.11320964533837,34.4037036993747));
#20097=CARTESIAN_POINT('Ctrl Pts',(-1.69362274757341,1.05612592890003,34.4080828289279));
#20098=CARTESIAN_POINT('Ctrl Pts',(-1.72908585273544,0.997011313104283,
34.4124619584811));
#20099=CARTESIAN_POINT('Ctrl Pts',(-1.76140486097608,0.936205361141371,
34.4168410880343));
#20100=CARTESIAN_POINT('Ctrl Pts',(-1.79371621287798,0.875413814043905,
34.4212191801764));
#20101=CARTESIAN_POINT('Ctrl Pts',(-1.82288471026105,0.81293217122506,34.4255972723185));
#20102=CARTESIAN_POINT('Ctrl Pts',(-1.84873984602636,0.749125185943188,
34.4299753644606));
#20103=CARTESIAN_POINT('Ctrl Pts',(-1.87461425439687,0.685270638473024,
34.4343567200642));
#20104=CARTESIAN_POINT('Ctrl Pts',(-1.89717017614741,0.620089242522898,
34.4387380756679));
#20105=CARTESIAN_POINT('Ctrl Pts',(-1.91628549820525,0.553965208174902,
34.4431194312715));
#20106=CARTESIAN_POINT('Ctrl Pts',(-1.93540791808174,0.487816620936646,
34.4475024137412));
#20107=CARTESIAN_POINT('Ctrl Pts',(-1.95108707835117,0.420725189523249,
34.4518853962108));
#20108=CARTESIAN_POINT('Ctrl Pts',(-1.96325168347044,0.353086943755323,
34.4562683786804));
#20109=CARTESIAN_POINT('Ctrl Pts',(-1.97543605562596,0.285338788323872,
34.4606584833355));
#20110=CARTESIAN_POINT('Ctrl Pts',(-1.98409440487738,0.217042544924583,
34.4650485879906));
#20111=CARTESIAN_POINT('Ctrl Pts',(-1.98920727331645,0.1486000884419,34.4694386926456));
#20112=CARTESIAN_POINT('Ctrl Pts',(-1.9929365991361,0.0986781663031144,
34.4726408346205));
#20113=CARTESIAN_POINT('Ctrl Pts',(-1.99478074038682,0.0486785648499409,
34.4758429765955));
#20114=CARTESIAN_POINT('Ctrl Pts',(-1.99474961222923,-0.00124378911175243,
34.4790451185704));
#20115=CARTESIAN_POINT('',(-1.99475051924689,0.00023157645625902,32.0772022700356));
#20116=CARTESIAN_POINT('Ctrl Pts',(-1.99474972256505,-0.00105205830250181,
33.6805590561774));
#20117=CARTESIAN_POINT('Ctrl Pts',(-1.99477744459478,0.0515101533020236,
33.6773935162611));
#20118=CARTESIAN_POINT('Ctrl Pts',(-1.99272763643631,0.104049715830699,
33.6741765283108));
#20119=CARTESIAN_POINT('Ctrl Pts',(-1.98792330420288,0.165118763130328,
33.6703506018151));
#20120=CARTESIAN_POINT('Ctrl Pts',(-1.98718416512581,0.173788260227377,
33.6698054427645));
#20121=CARTESIAN_POINT('Ctrl Pts',(-1.9858624755907,0.188177693956954,33.6688971215239));
#20122=CARTESIAN_POINT('Ctrl Pts',(-1.98531186732526,0.1939005023272,33.6685349589675));
#20123=CARTESIAN_POINT('Ctrl Pts',(-1.9842751214132,0.2042083833691,33.6678809511091));
#20124=CARTESIAN_POINT('Ctrl Pts',(-1.98379781052901,0.208794319023396,
33.6675893845459));
#20125=CARTESIAN_POINT('Ctrl Pts',(-1.98279099217451,0.218152465343164,
33.6669931625318));
#20126=CARTESIAN_POINT('Ctrl Pts',(-1.98226014540201,0.222924498593705,
33.6666884667989));
#20127=CARTESIAN_POINT('Ctrl Pts',(-1.98107837191606,0.233209922411704,
33.66603029077));
#20128=CARTESIAN_POINT('Ctrl Pts',(-1.98042164846761,0.238722593897857,
33.665676630001));
#20129=CARTESIAN_POINT('Ctrl Pts',(-1.97858703115242,0.253593957082281,
33.6647201072701));
#20130=CARTESIAN_POINT('Ctrl Pts',(-1.97736576597867,0.262947061925106,
33.664115881357));
#20131=CARTESIAN_POINT('Ctrl Pts',(-1.97128706494602,0.307061585743987,
33.6612532805799));
#20132=CARTESIAN_POINT('Ctrl Pts',(-1.96557929425604,0.341697654986037,
33.6589682061771));
#20133=CARTESIAN_POINT('Ctrl Pts',(-1.95340753657661,0.405085004377851,
33.6547139254358));
#20134=CARTESIAN_POINT('Ctrl Pts',(-1.94721439616133,0.43387880220416,33.6527536005671));
#20135=CARTESIAN_POINT('Ctrl Pts',(-1.89984430521305,0.632606481346904,
33.6390309966897));
#20136=CARTESIAN_POINT('Ctrl Pts',(-1.83711577038384,0.796611095484098,
33.6266262800367));
#20137=CARTESIAN_POINT('Ctrl Pts',(-1.72340151515232,1.00647745140216,33.6102138885024));
#20138=CARTESIAN_POINT('Ctrl Pts',(-1.6902786233565,1.06116431148707,33.6058921517241));
#20139=CARTESIAN_POINT('Ctrl Pts',(-1.65071104683783,1.11992351436634,33.6012725129818));
#20140=CARTESIAN_POINT('Ctrl Pts',(-1.64680820314792,1.12565464671479,33.6008222054153));
#20141=CARTESIAN_POINT('Ctrl Pts',(-1.64093775524626,1.13417922668787,33.6001529598754));
#20142=CARTESIAN_POINT('Ctrl Pts',(-1.63899278084729,1.13698808243602,33.5999325326198));
#20143=CARTESIAN_POINT('Ctrl Pts',(-1.63564680361365,1.14179378447927,33.5995555745869));
#20144=CARTESIAN_POINT('Ctrl Pts',(-1.63424934863103,1.14379306659612,33.599398803704));
#20145=CARTESIAN_POINT('Ctrl Pts',(-1.63133409979684,1.14794754482382,33.5990731491221));
#20146=CARTESIAN_POINT('Ctrl Pts',(-1.62981570635026,1.15010228865044,33.5989043083394));
#20147=CARTESIAN_POINT('Ctrl Pts',(-1.62560067784433,1.15605870222888,33.5984377296933));
#20148=CARTESIAN_POINT('Ctrl Pts',(-1.62289496075444,1.159853971078,33.5981406103505));
#20149=CARTESIAN_POINT('Ctrl Pts',(-1.61217610584233,1.17477820385246,33.5969727702889));
#20150=CARTESIAN_POINT('Ctrl Pts',(-1.60406136404328,1.18583421681277,33.5961087897412));
#20151=CARTESIAN_POINT('Ctrl Pts',(-1.59382176705603,1.1994877966176,33.5950420722204));
#20152=CARTESIAN_POINT('Ctrl Pts',(-1.59180378211631,1.20216451409603,33.5948329596662));
#20153=CARTESIAN_POINT('Ctrl Pts',(-1.47626023653814,1.3546240059377,33.5829222915553));
#20154=CARTESIAN_POINT('Ctrl Pts',(-1.34212504646792,1.48764066846578,33.5724530691031));
#20155=CARTESIAN_POINT('Ctrl Pts',(-1.13828185602176,1.6394256350726,33.5575085596647));
#20156=CARTESIAN_POINT('Ctrl Pts',(-1.08330588349975,1.67626048705518,33.5535655745298));
#20157=CARTESIAN_POINT('Ctrl Pts',(-1.00592318294249,1.72270948953602,33.5480533851149));
#20158=CARTESIAN_POINT('Ctrl Pts',(-0.98501821094353,1.73474738341249,33.5465680673452));
#20159=CARTESIAN_POINT('Ctrl Pts',(-0.953627381916452,1.75207307845742,
33.5443404014604));
#20160=CARTESIAN_POINT('Ctrl Pts',(-0.9433043687139,1.7576524441856,33.5436082529417));
#20161=CARTESIAN_POINT('Ctrl Pts',(-0.926732803547868,1.7664209796327,33.5424333154536));
#20162=CARTESIAN_POINT('Ctrl Pts',(-0.920515510308838,1.76966888420559,
33.5419925899868));
#20163=CARTESIAN_POINT('Ctrl Pts',(-0.908656461074274,1.77578462969958,
33.5411520316219));
#20164=CARTESIAN_POINT('Ctrl Pts',(-0.903017924288794,1.778658551337,33.5407524177316));
#20165=CARTESIAN_POINT('Ctrl Pts',(-0.893087696208261,1.78366052709539,
33.5400486719155));
#20166=CARTESIAN_POINT('Ctrl Pts',(-0.888801815917077,1.78580005611039,
33.5397449449549));
#20167=CARTESIAN_POINT('Ctrl Pts',(-0.880410618285732,1.78995128597121,
33.53915028631));
#20168=CARTESIAN_POINT('Ctrl Pts',(-0.87630600708342,1.79196435352844,33.538859404702));
#20169=CARTESIAN_POINT('Ctrl Pts',(-0.86541758377538,1.79725812038888,33.5380877531208));
#20170=CARTESIAN_POINT('Ctrl Pts',(-0.858622090401702,1.80051449561074,
33.5376061412599));
#20171=CARTESIAN_POINT('Ctrl Pts',(-0.834466651921713,1.81192184558229,
33.5358940020932));
#20172=CARTESIAN_POINT('Ctrl Pts',(-0.817008239684935,1.81986067082694,
33.5346561912457));
#20173=CARTESIAN_POINT('Ctrl Pts',(-0.629741348865567,1.90177836237216,
33.5213709377588));
#20174=CARTESIAN_POINT('Ctrl Pts',(-0.450563670174192,1.951998153889,33.5084633464905));
#20175=CARTESIAN_POINT('Ctrl Pts',(-0.168979055491203,1.99004403649769,
33.4886738511223));
#20176=CARTESIAN_POINT('Ctrl Pts',(-0.0700036625092822,1.99597935272083,
33.4818366122368));
#20177=CARTESIAN_POINT('Ctrl Pts',(0.0386265313581515,1.99439915219946,
33.4747191374701));
#20178=CARTESIAN_POINT('Ctrl Pts',(0.0482383909166484,1.99418982392594,
33.4740927468451));
#20179=CARTESIAN_POINT('Ctrl Pts',(0.0617504847671068,1.99379780261482,
33.4732172883785));
#20180=CARTESIAN_POINT('Ctrl Pts',(0.0656520772926734,1.99367314408893,
33.472965099983));
#20181=CARTESIAN_POINT('Ctrl Pts',(0.0723185348898683,1.99344055535584,
33.4725352500913));
#20182=CARTESIAN_POINT('Ctrl Pts',(0.0750835756446354,1.99333832432936,
33.4723572710567));
#20183=CARTESIAN_POINT('Ctrl Pts',(0.0803838998658419,1.9931313126746,33.4720167059737));
#20184=CARTESIAN_POINT('Ctrl Pts',(0.0829191974956272,1.99302744782545,
33.4718540679405));
#20185=CARTESIAN_POINT('Ctrl Pts',(0.0889351760702825,1.99276948884734,
33.4714687580706));
#20186=CARTESIAN_POINT('Ctrl Pts',(0.0924156797124349,1.99261111203722,
33.4712463259399));
#20187=CARTESIAN_POINT('Ctrl Pts',(0.102843931452138,1.99210920304792,33.4705812864893));
#20188=CARTESIAN_POINT('Ctrl Pts',(0.109790405663895,1.99173844199745,33.4701401652594));
#20189=CARTESIAN_POINT('Ctrl Pts',(0.230485166904379,1.9846631286278,33.4625060940494));
#20190=CARTESIAN_POINT('Ctrl Pts',(0.343474136770502,1.96825936722014,33.4558228846101));
#20191=CARTESIAN_POINT('Ctrl Pts',(0.55484888403689,1.918801781447,33.4432020713972));
#20192=CARTESIAN_POINT('Ctrl Pts',(0.653263370067661,1.88756553938182,33.4372710009004));
#20193=CARTESIAN_POINT('Ctrl Pts',(0.799135034822772,1.82848503664878,33.4279402843683));
#20194=CARTESIAN_POINT('Ctrl Pts',(0.848592875706664,1.80606305648148,33.4246776668016));
#20195=CARTESIAN_POINT('Ctrl Pts',(0.915859543650917,1.77219392479813,33.4200601280315));
#20196=CARTESIAN_POINT('Ctrl Pts',(0.934495550001225,1.76243809172148,33.4187610803365));
#20197=CARTESIAN_POINT('Ctrl Pts',(0.962306313961244,1.74731422078209,33.4167906153672));
#20198=CARTESIAN_POINT('Ctrl Pts',(0.971598507394432,1.74216438994554,33.4161267934267));
#20199=CARTESIAN_POINT('Ctrl Pts',(0.988572405275087,1.73257924356251,33.4149039151516));
#20200=CARTESIAN_POINT('Ctrl Pts',(0.996266551343735,1.72816642435796,33.4143456683371));
#20201=CARTESIAN_POINT('Ctrl Pts',(1.00853843242336,1.72101894919219,33.4134488648567));
#20202=CARTESIAN_POINT('Ctrl Pts',(1.01313513746588,1.71831696304417,33.4131114926562));
#20203=CARTESIAN_POINT('Ctrl Pts',(1.01772692389036,1.71559303768039,33.4127730077603));
#20204=CARTESIAN_POINT('Ctrl Pts',(1.01773292994288,1.71558947474582,33.4127725650198));
#20205=CARTESIAN_POINT('Ctrl Pts',(1.01774496011206,1.7155823380752,33.4127716782022));
#20206=CARTESIAN_POINT('Ctrl Pts',(1.01775098428653,1.71557876430459,33.4127712341208));
#20207=CARTESIAN_POINT('Ctrl Pts',(1.0177630509291,1.71557160582496,33.4127703446043));
#20208=CARTESIAN_POINT('Ctrl Pts',(1.01776909334588,1.71556802114614,33.412769899173));
#20209=CARTESIAN_POINT('Ctrl Pts',(1.01778119646431,1.71556084085448,33.4127690069573));
#20210=CARTESIAN_POINT('Ctrl Pts',(1.01778725717637,1.71555724523522,33.4127685601722));
#20211=CARTESIAN_POINT('Ctrl Pts',(1.01779939689641,1.71555004305536,33.412767665248));
#20212=CARTESIAN_POINT('Ctrl Pts',(1.0178054759447,1.71554643647059,33.412767217106));
#20213=CARTESIAN_POINT('Ctrl Pts',(1.01781765245366,1.71553921228982,33.4127663194594));
#20214=CARTESIAN_POINT('Ctrl Pts',(1.01782374991602,1.71553559469256,33.4127658699547));
#20215=CARTESIAN_POINT('Ctrl Pts',(1.01783596328427,1.71552834846753,33.4127649695805));
#20216=CARTESIAN_POINT('Ctrl Pts',(1.01784207919452,1.71552471983692,33.4127645187105));
#20217=CARTESIAN_POINT('Ctrl Pts',(1.01785432967048,1.71551745141865,33.4127636155901));
#20218=CARTESIAN_POINT('Ctrl Pts',(1.0178604641518,1.71551381168079,33.4127631633459));
#20219=CARTESIAN_POINT('Ctrl Pts',(1.01787275173343,1.71550652106886,33.4127622574794));
#20220=CARTESIAN_POINT('Ctrl Pts',(1.0178789048366,1.71550287019282,33.412761803857));
#20221=CARTESIAN_POINT('Ctrl Pts',(1.0178912296432,1.71549555731484,33.4127608952356));
#20222=CARTESIAN_POINT('Ctrl Pts',(1.01789740139469,1.7154918952841,33.4127604402331));
#20223=CARTESIAN_POINT('Ctrl Pts',(1.01790976366184,1.71548455999863,33.4127595288393));
#20224=CARTESIAN_POINT('Ctrl Pts',(1.01791595415525,1.71548088675684,33.4127590724497));
#20225=CARTESIAN_POINT('Ctrl Pts',(1.01792835391224,1.71547352904487,33.4127581582812));
#20226=CARTESIAN_POINT('Ctrl Pts',(1.01793456316834,1.71546984457886,33.4127577005029));
#20227=CARTESIAN_POINT('Ctrl Pts',(1.01794700073147,1.71546246425104,33.4127567835364));
#20228=CARTESIAN_POINT('Ctrl Pts',(1.01795322891158,1.71545876846427,33.4127563243574));
#20229=CARTESIAN_POINT('Ctrl Pts',(1.01796570415503,1.71545136559359,33.412755404602));
#20230=CARTESIAN_POINT('Ctrl Pts',(1.01797195125887,1.71544765848538,33.4127549440224));
#20231=CARTESIAN_POINT('Ctrl Pts',(1.0179844644544,1.71544023290891,33.4127540214579));
#20232=CARTESIAN_POINT('Ctrl Pts',(1.01799073055532,1.71543651443489,33.4127535594723));
#20233=CARTESIAN_POINT('Ctrl Pts',(1.01800328182877,1.71542906607626,33.4127526340894));
#20234=CARTESIAN_POINT('Ctrl Pts',(1.01800956700072,1.7154253361917,33.4127521706921));
#20235=CARTESIAN_POINT('Ctrl Pts',(1.01802215646519,1.71541786498209,33.4127512424823));
#20236=CARTESIAN_POINT('Ctrl Pts',(1.01802846076987,1.71541412364953,33.4127507776689));
#20237=CARTESIAN_POINT('Ctrl Pts',(1.01804108854267,1.7154066295176,33.4127498466235));
#20238=CARTESIAN_POINT('Ctrl Pts',(1.01804741202071,1.71540287671206,33.4127493803908));
#20239=CARTESIAN_POINT('Ctrl Pts',(1.01806007831747,1.71539535952813,33.4127484464937));
#20240=CARTESIAN_POINT('Ctrl Pts',(1.01806642106507,1.71539159519165,33.4127479788347));
#20241=CARTESIAN_POINT('Ctrl Pts',(1.01807912596919,1.71538405490448,33.4127470420798));
#20242=CARTESIAN_POINT('Ctrl Pts',(1.01808548806063,1.71538027899212,33.4127465729888));
#20243=CARTESIAN_POINT('Ctrl Pts',(1.01809823173216,1.71537271550498,33.4127456333641));
#20244=CARTESIAN_POINT('Ctrl Pts',(1.0181046132738,1.71536892795272,33.4127451628333));
#20245=CARTESIAN_POINT('Ctrl Pts',(1.01811739569676,1.71536134127333,33.4127442203399));
#20246=CARTESIAN_POINT('Ctrl Pts',(1.01812379668236,1.71535754208401,33.4127437483697));
#20247=CARTESIAN_POINT('Ctrl Pts',(1.01813661813287,1.71534993204673,33.4127428029872));
#20248=CARTESIAN_POINT('Ctrl Pts',(1.01814303862253,1.71534612118378,33.4127423295731));
#20249=CARTESIAN_POINT('Ctrl Pts',(1.01815589935284,1.71533848763709,33.4127413812827));
#20250=CARTESIAN_POINT('Ctrl Pts',(1.01816233951452,1.71533466499993,33.4127409064122));
#20251=CARTESIAN_POINT('Ctrl Pts',(1.01817523930377,1.71532700807314,33.4127399552302));
#20252=CARTESIAN_POINT('Ctrl Pts',(1.01818169904741,1.71532317371432,33.41273947891));
#20253=CARTESIAN_POINT('Ctrl Pts',(1.01819463850265,1.7153154930453,33.4127385247914));
#20254=CARTESIAN_POINT('Ctrl Pts',(1.01820111804933,1.71531164683269,33.4127380470051));
#20255=CARTESIAN_POINT('Ctrl Pts',(1.01821409694964,1.71530394255075,33.4127370899661));
#20256=CARTESIAN_POINT('Ctrl Pts',(1.01822059631392,1.7153000844748,33.4127366107125));
#20257=CARTESIAN_POINT('Ctrl Pts',(1.01823361487003,1.71529235645303,33.4127356507375));
#20258=CARTESIAN_POINT('Ctrl Pts',(1.0182401340844,1.71528848649353,33.4127351700143));
#20259=CARTESIAN_POINT('Ctrl Pts',(1.01825319251392,1.71528073460091,33.4127342070871));
#20260=CARTESIAN_POINT('Ctrl Pts',(1.01825973165292,1.71527685271269,33.4127337248887));
#20261=CARTESIAN_POINT('Ctrl Pts',(1.02242343109338,1.71280508595897,33.4124266903121));
#20262=CARTESIAN_POINT('Ctrl Pts',(1.02657157532018,1.71032211439959,33.4121195893019));
#20263=CARTESIAN_POINT('Ctrl Pts',(1.03598583272414,1.7046403963131,33.4114198327033));
#20264=CARTESIAN_POINT('Ctrl Pts',(1.04124621408939,1.70143229268289,33.4110268362233));
#20265=CARTESIAN_POINT('Ctrl Pts',(1.05720194315426,1.69159980096969,33.4098286631592));
#20266=CARTESIAN_POINT('Ctrl Pts',(1.06784939839352,1.68489865735168,33.4090206649226));
#20267=CARTESIAN_POINT('Ctrl Pts',(1.2095077617466,1.59386163331758,33.3981553333141));
#20268=CARTESIAN_POINT('Ctrl Pts',(1.33023402222521,1.4945773635237,33.3875002542286));
#20269=CARTESIAN_POINT('Ctrl Pts',(1.50166665670833,1.31621567957269,33.3702572796715));
#20270=CARTESIAN_POINT('Ctrl Pts',(1.56054690280423,1.24584151482424,33.3638357873978));
#20271=CARTESIAN_POINT('Ctrl Pts',(1.63469016378132,1.1436831378983,33.3552210293849));
#20272=CARTESIAN_POINT('Ctrl Pts',(1.65426946535809,1.11517527151357,33.3528871168934));
#20273=CARTESIAN_POINT('Ctrl Pts',(1.68359869238016,1.06999758632369,33.3493123783605));
#20274=CARTESIAN_POINT('Ctrl Pts',(1.69386392221676,1.05367190005601,33.3480449229987));
#20275=CARTESIAN_POINT('Ctrl Pts',(1.70652986906523,1.03286452168446,33.3464624949052));
#20276=CARTESIAN_POINT('Ctrl Pts',(1.70915197081158,1.02851974031135,33.3461338600857));
#20277=CARTESIAN_POINT('Ctrl Pts',(1.71330806750506,1.02157336928759,33.345611353703));
#20278=CARTESIAN_POINT('Ctrl Pts',(1.7148527619035,1.01897825703279,33.3454167938415));
#20279=CARTESIAN_POINT('Ctrl Pts',(1.71777250601847,1.01404759524331,33.3450483703071));
#20280=CARTESIAN_POINT('Ctrl Pts',(1.71914867244162,1.01171278037747,33.3448744367653));
#20281=CARTESIAN_POINT('Ctrl Pts',(1.72229150276901,1.00635570092846,33.3444765500905));
#20282=CARTESIAN_POINT('Ctrl Pts',(1.72405497035828,1.0033315887291,33.3442528058552));
#20283=CARTESIAN_POINT('Ctrl Pts',(1.72959917392851,0.993766240675727,33.343547776046));
#20284=CARTESIAN_POINT('Ctrl Pts',(1.73335076937651,0.987208062286015,33.343068339897));
#20285=CARTESIAN_POINT('Ctrl Pts',(1.79755738574391,0.873473799068034,33.334818955248));
#20286=CARTESIAN_POINT('Ctrl Pts',(1.84801534220148,0.760932552141375,33.3276443188568));
#20287=CARTESIAN_POINT('Ctrl Pts',(1.92011267509742,0.549735737378889,33.3146891774949));
#20288=CARTESIAN_POINT('Ctrl Pts',(1.94526953604433,0.452733166265001,33.30891675559));
#20289=CARTESIAN_POINT('Ctrl Pts',(1.97199914774983,0.304616735853402,33.2999661453416));
#20290=CARTESIAN_POINT('Ctrl Pts',(1.97907073545238,0.25465749357308,33.296926055634));
#20291=CARTESIAN_POINT('Ctrl Pts',(1.98734265408806,0.174390708791092,33.2919718557718));
#20292=CARTESIAN_POINT('Ctrl Pts',(1.98975893930898,0.144229517552331,33.2900947644228));
#20293=CARTESIAN_POINT('Ctrl Pts',(1.99198379146869,0.105372088896581,33.2876521010948));
#20294=CARTESIAN_POINT('Ctrl Pts',(1.99242287859085,0.0967148987408133,
33.2871063456939));
#20295=CARTESIAN_POINT('Ctrl Pts',(1.99304068257595,0.0827331830997572,
33.2862223290833));
#20296=CARTESIAN_POINT('Ctrl Pts',(1.99325452290471,0.077410257784379,33.285885170752));
#20297=CARTESIAN_POINT('Ctrl Pts',(1.99362211027231,0.0672451766690467,
33.2852401199968));
#20298=CARTESIAN_POINT('Ctrl Pts',(1.9937795450106,0.0624031855658031,33.2849323454991));
#20299=CARTESIAN_POINT('Ctrl Pts',(1.99409953337463,0.0513186965914399,
33.284226577485));
#20300=CARTESIAN_POINT('Ctrl Pts',(1.99425041457987,0.045075937114839,33.283828221122));
#20301=CARTESIAN_POINT('Ctrl Pts',(1.99462511796472,0.0258318651389071,
33.2825975019978));
#20302=CARTESIAN_POINT('Ctrl Pts',(1.99475112352556,0.0128291992312109,
33.281762088333));
#20303=CARTESIAN_POINT('Ctrl Pts',(1.99473884836087,-0.128285093767944,
33.2726522640937));
#20304=CARTESIAN_POINT('Ctrl Pts',(1.98238635212579,-0.256072427776669,
33.2639855229705));
#20305=CARTESIAN_POINT('Ctrl Pts',(1.92826998706629,-0.533602193372845,
33.2443853480347));
#20306=CARTESIAN_POINT('Ctrl Pts',(1.88110331019069,-0.681477104812966,
33.2334114257033));
#20307=CARTESIAN_POINT('Ctrl Pts',(1.80985807849128,-0.838909342234719,
33.2219590437263));
#20308=CARTESIAN_POINT('Ctrl Pts',(1.80217145143339,-0.855297179481269,
33.2207705091546));
#20309=CARTESIAN_POINT('Ctrl Pts',(1.79209331013041,-0.876044392180787,
33.2192725155312));
#20310=CARTESIAN_POINT('Ctrl Pts',(1.78990742460605,-0.880501914769513,
33.2189510715677));
#20311=CARTESIAN_POINT('Ctrl Pts',(1.78637599383684,-0.887635817106282,
33.2184373227388));
#20312=CARTESIAN_POINT('Ctrl Pts',(1.78504103981864,-0.890317371290007,
33.2182443686315));
#20313=CARTESIAN_POINT('Ctrl Pts',(1.78248374249767,-0.895425402782863,
33.217877131617));
#20314=CARTESIAN_POINT('Ctrl Pts',(1.78126249717655,-0.897852360050421,
33.2177027865719));
#20315=CARTESIAN_POINT('Ctrl Pts',(1.77843519002581,-0.903442539628952,
33.217301513022));
#20316=CARTESIAN_POINT('Ctrl Pts',(1.77682564629589,-0.906603976758268,
33.2170748057109));
#20317=CARTESIAN_POINT('Ctrl Pts',(1.77248441590704,-0.915074975539426,
33.2164679121709));
#20318=CARTESIAN_POINT('Ctrl Pts',(1.76973728258311,-0.920376644805112,
33.2160886768607));
#20319=CARTESIAN_POINT('Ctrl Pts',(1.74953809025929,-0.958934065932428,
33.2133343820142));
#20320=CARTESIAN_POINT('Ctrl Pts',(1.73117238292781,-0.991705951294523,
33.2110138370989));
#20321=CARTESIAN_POINT('Ctrl Pts',(1.6683061961855,-1.09680959281878,33.2035745629473));
#20322=CARTESIAN_POINT('Ctrl Pts',(1.62010974658528,-1.16682633073641,33.1986211702758));
#20323=CARTESIAN_POINT('Ctrl Pts',(1.50528268958832,-1.31274686747913,33.1878389153347));
#20324=CARTESIAN_POINT('Ctrl Pts',(1.43706279314533,-1.38709398664308,33.1820304617162));
#20325=CARTESIAN_POINT('Ctrl Pts',(1.32607584282458,-1.49103399804107,33.1729940760045));
#20326=CARTESIAN_POINT('Ctrl Pts',(1.28729363047979,-1.52464226216208,33.1699040623753));
#20327=CARTESIAN_POINT('Ctrl Pts',(1.2233577251554,-1.57586852646034,33.1648756462386));
#20328=CARTESIAN_POINT('Ctrl Pts',(1.19901730040011,-1.59446639673979,33.1629757074807));
#20329=CARTESIAN_POINT('Ctrl Pts',(1.16722157163425,-1.61762083375273,33.1605073156984));
#20330=CARTESIAN_POINT('Ctrl Pts',(1.16015041861719,-1.62269971386889,33.159959203521));
#20331=CARTESIAN_POINT('Ctrl Pts',(1.14869231838148,-1.63081635704948,33.159072286093));
#20332=CARTESIAN_POINT('Ctrl Pts',(1.1443259805923,-1.63388312983753,33.1587345969956));
#20333=CARTESIAN_POINT('Ctrl Pts',(1.13597344148884,-1.63969977559077,33.1580891406862));
#20334=CARTESIAN_POINT('Ctrl Pts',(1.13198942221199,-1.64245272722261,33.1577814939705));
#20335=CARTESIAN_POINT('Ctrl Pts',(1.12285832893615,-1.64871329566615,33.1570768804563));
#20336=CARTESIAN_POINT('Ctrl Pts',(1.11770479147461,-1.65221135325588,33.1566795550742));
#20337=CARTESIAN_POINT('Ctrl Pts',(1.10181041759449,-1.6628915522836,33.1554551664207));
#20338=CARTESIAN_POINT('Ctrl Pts',(1.09101628313562,-1.66999340353429,33.1546250977026));
#20339=CARTESIAN_POINT('Ctrl Pts',(0.987393041226757,-1.7367374440694,33.1466687513528));
#20340=CARTESIAN_POINT('Ctrl Pts',(0.889851116694343,-1.78867534926581,
33.1392561987932));
#20341=CARTESIAN_POINT('Ctrl Pts',(0.630523295646565,-1.90027851872453,
33.1198022465785));
#20342=CARTESIAN_POINT('Ctrl Pts',(0.464387611604262,-1.94755311909873,
33.1075297798434));
#20343=CARTESIAN_POINT('Ctrl Pts',(0.275845110346863,-1.97567285512926,
33.0948884234622));
#20344=CARTESIAN_POINT('Ctrl Pts',(0.257404064695539,-1.97815999464585,
33.093666102252));
#20345=CARTESIAN_POINT('Ctrl Pts',(0.233953560237233,-1.98098925307041,
33.0921318847084));
#20346=CARTESIAN_POINT('Ctrl Pts',(0.228974690553975,-1.9815709125686,33.091807298754));
#20347=CARTESIAN_POINT('Ctrl Pts',(0.221006379669319,-1.9824713819332,33.0912897187511));
#20348=CARTESIAN_POINT('Ctrl Pts',(0.218018359687984,-1.98280220777863,
33.0910960585455));
#20349=CARTESIAN_POINT('Ctrl Pts',(0.212331477932492,-1.9834188340631,33.0907283042487));
#20350=CARTESIAN_POINT('Ctrl Pts',(0.209632814205677,-1.98370587818016,
33.0905541446227));
#20351=CARTESIAN_POINT('Ctrl Pts',(0.203425877133432,-1.98435327310112,
33.0901543813182));
#20352=CARTESIAN_POINT('Ctrl Pts',(0.199917230597112,-1.98470982799306,
33.089928993345));
#20353=CARTESIAN_POINT('Ctrl Pts',(0.188751728729845,-1.98581457692724,
33.0892135677565));
#20354=CARTESIAN_POINT('Ctrl Pts',(0.181091365915955,-1.98652779261813,
33.0887254578701));
#20355=CARTESIAN_POINT('Ctrl Pts',(0.0585593169347576,-1.99722142751281,
33.0809586496903));
#20356=CARTESIAN_POINT('Ctrl Pts',(-0.0569807634925121,-1.99726922053672,
33.0742017001674));
#20357=CARTESIAN_POINT('Ctrl Pts',(-0.274165003128792,-1.97848400321454,
33.0615312511667));
#20358=CARTESIAN_POINT('Ctrl Pts',(-0.375597679286987,-1.96175708664239,
33.0556237233778));
#20359=CARTESIAN_POINT('Ctrl Pts',(-0.546182901653154,-1.91990624639383,
33.0452056662972));
#20360=CARTESIAN_POINT('Ctrl Pts',(-0.616059833683593,-1.89863747394457,
33.0407949207249));
#20361=CARTESIAN_POINT('Ctrl Pts',(-0.700139848137715,-1.867914655736,33.0352290054685));
#20362=CARTESIAN_POINT('Ctrl Pts',(-0.715598954283094,-1.86204701302309,
33.0341947579378));
#20363=CARTESIAN_POINT('Ctrl Pts',(-0.737388080139877,-1.85346534119487,
33.0327208134592));
#20364=CARTESIAN_POINT('Ctrl Pts',(-0.743780022144838,-1.85090956788171,
33.0322864331287));
#20365=CARTESIAN_POINT('Ctrl Pts',(-0.754743667402192,-1.84645986834215,
33.0315378869697));
#20366=CARTESIAN_POINT('Ctrl Pts',(-0.759321817808162,-1.84458191066711,
33.0312242627497));
#20367=CARTESIAN_POINT('Ctrl Pts',(-0.768043386627528,-1.8409663510682,
33.030624769392));
#20368=CARTESIAN_POINT('Ctrl Pts',(-0.772188020319,-1.83923174457155,33.0303390034384));
#20369=CARTESIAN_POINT('Ctrl Pts',(-0.781844329174488,-1.83515200613445,
33.0296711503143));
#20370=CARTESIAN_POINT('Ctrl Pts',(-0.787351349343896,-1.83279603122462,
33.0292886957648));
#20371=CARTESIAN_POINT('Ctrl Pts',(-0.806243294211036,-1.82461295192599,
33.0279711950233));
#20372=CARTESIAN_POINT('Ctrl Pts',(-0.819574557554777,-1.81866385007215,
33.0270319917061));
#20373=CARTESIAN_POINT('Ctrl Pts',(-0.930510146111242,-1.76769117875129,
33.0191350537582));
#20374=CARTESIAN_POINT('Ctrl Pts',(-1.02437750385509,-1.71500003253068,
33.0119080925686));
#20375=CARTESIAN_POINT('Ctrl Pts',(-1.25623940790153,-1.55899796107296,
32.9926516570401));
#20376=CARTESIAN_POINT('Ctrl Pts',(-1.38592539259276,-1.4449303859441,32.9803804325206));
#20377=CARTESIAN_POINT('Ctrl Pts',(-1.5116644111489,-1.30163192733901,32.967737579238));
#20378=CARTESIAN_POINT('Ctrl Pts',(-1.52376124321964,-1.28744968900497,
32.966513089845));
#20379=CARTESIAN_POINT('Ctrl Pts',(-1.53885912343535,-1.26923808528586,
32.9649765561209));
#20380=CARTESIAN_POINT('Ctrl Pts',(-1.54204568383865,-1.26536470205288,
32.9646517759629));
#20381=CARTESIAN_POINT('Ctrl Pts',(-1.54711919047461,-1.25915003644248,
32.964133961802));
#20382=CARTESIAN_POINT('Ctrl Pts',(-1.54901548484136,-1.2568164670404,32.9639402605663));
#20383=CARTESIAN_POINT('Ctrl Pts',(-1.55261313179297,-1.25236871154936,
32.9635724785503));
#20384=CARTESIAN_POINT('Ctrl Pts',(-1.55431542565144,-1.25025536765374,
32.9633983320262));
#20385=CARTESIAN_POINT('Ctrl Pts',(-1.55821928052618,-1.24538855958788,
32.9629986664412));
#20386=CARTESIAN_POINT('Ctrl Pts',(-1.56041785696802,-1.24263273040667,
32.9627733627421));
#20387=CARTESIAN_POINT('Ctrl Pts',(-1.56738663284991,-1.23384998419723,
32.9620584693532));
#20388=CARTESIAN_POINT('Ctrl Pts',(-1.57212938151753,-1.22780122687483,
32.9615708033596));
#20389=CARTESIAN_POINT('Ctrl Pts',(-1.64775108555624,-1.13019898179613,
32.9537740741147));
#20390=CARTESIAN_POINT('Ctrl Pts',(-1.71057358246486,-1.03265677191458,
32.9469911646702));
#20391=CARTESIAN_POINT('Ctrl Pts',(-1.8123791974174,-0.839532200720969,
32.9343032637359));
#20392=CARTESIAN_POINT('Ctrl Pts',(-1.85311395055486,-0.745319007747131,
32.928404114423));
#20393=CARTESIAN_POINT('Ctrl Pts',(-1.90382017196381,-0.597795197695983,
32.9191500416256));
#20394=CARTESIAN_POINT('Ctrl Pts',(-1.91916796895547,-0.546519878407456,
32.9159324753358));
#20395=CARTESIAN_POINT('Ctrl Pts',(-1.94026606718953,-0.46410359594143,
32.9107149965564));
#20396=CARTESIAN_POINT('Ctrl Pts',(-1.94736887885266,-0.433334552911715,
32.9087573845429));
#20397=CARTESIAN_POINT('Ctrl Pts',(-1.95551325182578,-0.393792977147572,
32.9062241641222));
#20398=CARTESIAN_POINT('Ctrl Pts',(-1.95723127557921,-0.38516323398768,
32.9056702534992));
#20399=CARTESIAN_POINT('Ctrl Pts',(-1.95990318285128,-0.371262397022951,
32.9047762170149));
#20400=CARTESIAN_POINT('Ctrl Pts',(-1.96089304139973,-0.365998268945315,
32.9044372404049));
#20401=CARTESIAN_POINT('Ctrl Pts',(-1.96273654638875,-0.355972212920441,
32.9037908144142));
#20402=CARTESIAN_POINT('Ctrl Pts',(-1.96359409644646,-0.351211034315027,
32.9034834918385));
#20403=CARTESIAN_POINT('Ctrl Pts',(-1.96550931689918,-0.340351287357326,
32.9027817082168));
#20404=CARTESIAN_POINT('Ctrl Pts',(-1.96655593494064,-0.334250844345427,
32.9023868988679));
#20405=CARTESIAN_POINT('Ctrl Pts',(-1.96966706831472,-0.315596369129538,
32.9011777783363));
#20406=CARTESIAN_POINT('Ctrl Pts',(-1.97163985306709,-0.303027565644676,
32.9003605694334));
#20407=CARTESIAN_POINT('Ctrl Pts',(-1.98772906237007,-0.193704395418772,
32.893229323918));
#20408=CARTESIAN_POINT('Ctrl Pts',(-1.99483182175871,-0.0960674129391705,
32.8866928485967));
#20409=CARTESIAN_POINT('Ctrl Pts',(-1.99458667018612,0.194289775018152,
32.8667909497128));
#20410=CARTESIAN_POINT('Ctrl Pts',(-1.96653159115058,0.385843755610208,
32.8529671470688));
#20411=CARTESIAN_POINT('Ctrl Pts',(-1.90798583281888,0.582035260828337,
32.8394982905035));
#20412=CARTESIAN_POINT('Ctrl Pts',(-1.90440764546011,0.593638375404131,
32.8387048483445));
#20413=CARTESIAN_POINT('Ctrl Pts',(-1.89938014515719,0.609427792754021,
32.837630105199));
#20414=CARTESIAN_POINT('Ctrl Pts',(-1.89802260094675,0.613642711691862,
32.8373436924451));
#20415=CARTESIAN_POINT('Ctrl Pts',(-1.89584893659287,0.62031530513678,32.8368910845672));
#20416=CARTESIAN_POINT('Ctrl Pts',(-1.89504205704351,0.622775939156343,
32.8367243523832));
#20417=CARTESIAN_POINT('Ctrl Pts',(-1.89337435154761,0.627828468777678,
32.8363823632579));
#20418=CARTESIAN_POINT('Ctrl Pts',(-1.89251299590091,0.630420162850252,
32.8362071418891));
#20419=CARTESIAN_POINT('Ctrl Pts',(-1.89047158115592,0.636520594285752,
32.8357951599984));
#20420=CARTESIAN_POINT('Ctrl Pts',(-1.88928706551676,0.640027851517573,
32.8355586626359));
#20421=CARTESIAN_POINT('Ctrl Pts',(-1.88537086325206,0.651517808867437,
32.8347850007987));
#20422=CARTESIAN_POINT('Ctrl Pts',(-1.88259824742113,0.659486612548083,
32.8342502006518));
#20423=CARTESIAN_POINT('Ctrl Pts',(-1.84700088268742,0.759743212325898,
32.8275413083106));
#20424=CARTESIAN_POINT('Ctrl Pts',(-1.8074671327058,0.849523501464951,32.8217394379467));
#20425=CARTESIAN_POINT('Ctrl Pts',(-1.72508397598899,1.00455551351148,32.8114912688448));
#20426=CARTESIAN_POINT('Ctrl Pts',(-1.68471245572965,1.07088310121653,32.8070230681841));
#20427=CARTESIAN_POINT('Ctrl Pts',(-1.57257865582955,1.23301048307141,32.7955259223322));
#20428=CARTESIAN_POINT('Ctrl Pts',(-1.49588715298001,1.32500338217681,32.7884298300651));
#20429=CARTESIAN_POINT('Ctrl Pts',(-1.40224362705978,1.41877037674333,32.78015860791));
#20430=CARTESIAN_POINT('Ctrl Pts',(-1.39296752325565,1.42787885969652,32.779343339137));
#20431=CARTESIAN_POINT('Ctrl Pts',(-1.37910533809226,1.44122691412289,32.7781306050252));
#20432=CARTESIAN_POINT('Ctrl Pts',(-1.37458718618475,1.44553679222747,32.7777361995507));
#20433=CARTESIAN_POINT('Ctrl Pts',(-1.36652776763516,1.45315274242654,32.7770341533305));
#20434=CARTESIAN_POINT('Ctrl Pts',(-1.36299453657825,1.45646727567738,32.7767268803675));
#20435=CARTESIAN_POINT('Ctrl Pts',(-1.35555047957879,1.46339975529426,32.7760805270823));
#20436=CARTESIAN_POINT('Ctrl Pts',(-1.35163716863083,1.4670149658232,32.7757413334263));
#20437=CARTESIAN_POINT('Ctrl Pts',(-1.34131761441829,1.47647207470504,32.7748483833606));
#20438=CARTESIAN_POINT('Ctrl Pts',(-1.33488774007418,1.48228790981908,32.7742935299177));
#20439=CARTESIAN_POINT('Ctrl Pts',(-1.30583916977515,1.50822010881898,32.771793432694));
#20440=CARTESIAN_POINT('Ctrl Pts',(-1.28280327728808,1.52786105985651,32.7698285247641));
#20441=CARTESIAN_POINT('Ctrl Pts',(-1.22018509572006,1.57883619908952,32.7645303250658));
#20442=CARTESIAN_POINT('Ctrl Pts',(-1.179847362089,1.60920318525719,32.7611608117992));
#20443=CARTESIAN_POINT('Ctrl Pts',(-1.05616984104671,1.69515831966415,32.7509595429295));
#20444=CARTESIAN_POINT('Ctrl Pts',(-0.969754995040446,1.74603218611233,
32.7439905885029));
#20445=CARTESIAN_POINT('Ctrl Pts',(-0.7695630574671,1.84442785149107,32.728426890033));
#20446=CARTESIAN_POINT('Ctrl Pts',(-0.654440341313981,1.88834760546612,
32.7198526623489));
#20447=CARTESIAN_POINT('Ctrl Pts',(-0.528717321011424,1.92341951470695,
32.7113311858702));
#20448=CARTESIAN_POINT('Ctrl Pts',(-0.521428900464774,1.925408149272,32.7108401491055));
#20449=CARTESIAN_POINT('Ctrl Pts',(-0.510746862472833,1.92825762266546,
32.7101249951532));
#20450=CARTESIAN_POINT('Ctrl Pts',(-0.507362106133707,1.92915098180841,
32.7098990503031));
#20451=CARTESIAN_POINT('Ctrl Pts',(-0.501352670570711,1.9307201784862,32.7094990936864));
#20452=CARTESIAN_POINT('Ctrl Pts',(-0.498728947774156,1.93139958188479,
32.709324876637));
#20453=CARTESIAN_POINT('Ctrl Pts',(-0.493178535587645,1.93282477630955,
32.7089571862852));
#20454=CARTESIAN_POINT('Ctrl Pts',(-0.490251542820833,1.93356926665156,
32.7087637888908));
#20455=CARTESIAN_POINT('Ctrl Pts',(-0.48240154988334,1.93554696754502,32.7082464299893));
#20456=CARTESIAN_POINT('Ctrl Pts',(-0.4774754742771,1.93676805315669,32.7079231630801));
#20457=CARTESIAN_POINT('Ctrl Pts',(-0.453806412464664,1.94253939553305,
32.706376339927));
#20458=CARTESIAN_POINT('Ctrl Pts',(-0.43500196949418,1.94683664355593,32.7051667452116));
#20459=CARTESIAN_POINT('Ctrl Pts',(-0.382311365505976,1.95807605560406,
32.7018236448342));
#20460=CARTESIAN_POINT('Ctrl Pts',(-0.348301354570823,1.96441092437159,
32.6997187896802));
#20461=CARTESIAN_POINT('Ctrl Pts',(-0.22353765502545,1.98430752801679,32.6921337820842));
#20462=CARTESIAN_POINT('Ctrl Pts',(-0.132038332065827,1.99248929803095,
32.6868291011406));
#20463=CARTESIAN_POINT('Ctrl Pts',(0.115341341372458,1.99748759438773,32.6724787583385));
#20464=CARTESIAN_POINT('Ctrl Pts',(0.27078595941242,1.98240409883719,32.6634088465011));
#20465=CARTESIAN_POINT('Ctrl Pts',(0.435177502552042,1.94674247501077,32.6529045297855));
#20466=CARTESIAN_POINT('Ctrl Pts',(0.447442099548372,1.94396020503084,32.6521155942448));
#20467=CARTESIAN_POINT('Ctrl Pts',(0.465674137452995,1.93964252200997,32.650934642161));
#20468=CARTESIAN_POINT('Ctrl Pts',(0.471662262436206,1.93819509448655,32.6505454548668));
#20469=CARTESIAN_POINT('Ctrl Pts',(0.482337302224436,1.93556236295809,32.649849260063));
#20470=CARTESIAN_POINT('Ctrl Pts',(0.487026814217527,1.93438771076944,32.6495425982607));
#20471=CARTESIAN_POINT('Ctrl Pts',(0.496918656268179,1.93187170249911,32.6488939746429));
#20472=CARTESIAN_POINT('Ctrl Pts',(0.50211992237897,1.93052635529357,32.6485518858979));
#20473=CARTESIAN_POINT('Ctrl Pts',(0.515895153053796,1.92690385119931,32.6476431092774));
#20474=CARTESIAN_POINT('Ctrl Pts',(0.52445939413496,1.92459050200217,32.6470752527393));
#20475=CARTESIAN_POINT('Ctrl Pts',(0.564159881649405,1.91358204912988,32.6444293660656));
#20476=CARTESIAN_POINT('Ctrl Pts',(0.595095737681122,1.90418840715719,32.6423287491064));
#20477=CARTESIAN_POINT('Ctrl Pts',(0.678283490822216,1.87670339781152,32.6365701791737));
#20478=CARTESIAN_POINT('Ctrl Pts',(0.730030544361641,1.85718566867715,32.6328677753725));
#20479=CARTESIAN_POINT('Ctrl Pts',(0.876530592845854,1.79486012382992,32.6220428058596));
#20480=CARTESIAN_POINT('Ctrl Pts',(0.968832036150822,1.74676558141627,32.6147854299863));
#20481=CARTESIAN_POINT('Ctrl Pts',(1.11743098731727,1.65392260325258,32.6025666605976));
#20482=CARTESIAN_POINT('Ctrl Pts',(1.17583772599546,1.61292245347771,32.5976111544589));
#20483=CARTESIAN_POINT('Ctrl Pts',(1.23891312196393,1.56339398567318,32.5921716413475));
#20484=CARTESIAN_POINT('Ctrl Pts',(1.24586338088172,1.55786100768995,32.5915710314367));
#20485=CARTESIAN_POINT('Ctrl Pts',(1.2788294097961,1.53125561253455,32.5887172118988));
#20486=CARTESIAN_POINT('Ctrl Pts',(1.30435075208309,1.50957538813166,32.5864927027896));
#20487=CARTESIAN_POINT('Ctrl Pts',(1.33361554271825,1.4834184849008,32.5839356860324));
#20488=CARTESIAN_POINT('Ctrl Pts',(1.33789849084449,1.47955684152574,32.5835613035209));
#20489=CARTESIAN_POINT('Ctrl Pts',(1.3447446610922,1.47333007891937,32.5829626941665));
#20490=CARTESIAN_POINT('Ctrl Pts',(1.34731849238037,1.47097675220543,32.5827376069981));
#20491=CARTESIAN_POINT('Ctrl Pts',(1.35188025158438,1.46678378901041,32.5823386234782));
#20492=CARTESIAN_POINT('Ctrl Pts',(1.35387061739581,1.46494684204821,32.5821645253628));
#20493=CARTESIAN_POINT('Ctrl Pts',(1.35807784778132,1.46104800995269,32.5817964907846));
#20494=CARTESIAN_POINT('Ctrl Pts',(1.36029375531232,1.45898513617468,32.5816026325279));
#20495=CARTESIAN_POINT('Ctrl Pts',(1.3662355842654,1.45342835404187,32.5810827361116));
#20496=CARTESIAN_POINT('Ctrl Pts',(1.36995282803574,1.44992513682281,32.5807574044685));
#20497=CARTESIAN_POINT('Ctrl Pts',(1.38790776916931,1.43287328833316,32.5791853558575));
#20498=CARTESIAN_POINT('Ctrl Pts',(1.40195876406899,1.41912844051604,32.5779531568966));
#20499=CARTESIAN_POINT('Ctrl Pts',(1.44082602122802,1.37996722900344,32.5745310831829));
#20500=CARTESIAN_POINT('Ctrl Pts',(1.4651708705644,1.35409150782168,32.5723715256103));
#20501=CARTESIAN_POINT('Ctrl Pts',(1.55245743144667,1.25620393370509,32.5645060913675));
#20502=CARTESIAN_POINT('Ctrl Pts',(1.61089109904218,1.18034092413618,32.5589883840596));
#20503=CARTESIAN_POINT('Ctrl Pts',(1.67373258218342,1.08534791939415,32.5523810193259));
#20504=CARTESIAN_POINT('Ctrl Pts',(1.68359579711485,1.06998413503928,32.5513213420575));
#20505=CARTESIAN_POINT('Ctrl Pts',(1.72135376153569,1.00935414501893,32.5471675815331));
#20506=CARTESIAN_POINT('Ctrl Pts',(1.74764413641418,0.963116904149641,32.5440594635375));
#20507=CARTESIAN_POINT('Ctrl Pts',(1.78387497986418,0.893017527110549,32.5393790417136));
#20508=CARTESIAN_POINT('Ctrl Pts',(1.79525056135997,0.869922755341378,32.5378420817085));
#20509=CARTESIAN_POINT('Ctrl Pts',(1.82971069945764,0.796405190612958,32.5329545304335));
#20510=CARTESIAN_POINT('Ctrl Pts',(1.85113988549463,0.745240043788715,32.5295595614446));
#20511=CARTESIAN_POINT('Ctrl Pts',(1.8738882410722,0.683864501366626,32.5254650148722));
#20512=CARTESIAN_POINT('Ctrl Pts',(1.87729690813832,0.674450968649196,32.5248364416027));
#20513=CARTESIAN_POINT('Ctrl Pts',(1.88271206133806,0.659137080657604,32.5238127913894));
#20514=CARTESIAN_POINT('Ctrl Pts',(1.88476204197238,0.653252202992117,32.5234191598557));
#20515=CARTESIAN_POINT('Ctrl Pts',(1.88835609893276,0.642776991517115,32.5227179862672));
#20516=CARTESIAN_POINT('Ctrl Pts',(1.88991110405571,0.638190438105606,32.5224108087179));
#20517=CARTESIAN_POINT('Ctrl Pts',(1.89314364395616,0.628540498092129,32.5217641411323));
#20518=CARTESIAN_POINT('Ctrl Pts',(1.89481760043134,0.623475961507653,32.5214245358033));
#20519=CARTESIAN_POINT('Ctrl Pts',(1.89916790981712,0.610134803183753,32.5205293334488));
#20520=CARTESIAN_POINT('Ctrl Pts',(1.9018104495278,0.601847354257184,32.5199726293005));
#20521=CARTESIAN_POINT('Ctrl Pts',(1.91349034862977,0.564372083747713,32.5174522962384));
#20522=CARTESIAN_POINT('Ctrl Pts',(1.92191014147969,0.534997569171342,32.5154686104084));
#20523=CARTESIAN_POINT('Ctrl Pts',(1.94260750810645,0.455980269522685,32.5101074872791));
#20524=CARTESIAN_POINT('Ctrl Pts',(1.9536558206389,0.40604202030779,32.5066927600023));
#20525=CARTESIAN_POINT('Ctrl Pts',(1.98072617445345,0.256682179002209,32.4964060180972));
#20526=CARTESIAN_POINT('Ctrl Pts',(1.99115348333106,0.15641743303547,32.4893970135368));
#20527=CARTESIAN_POINT('Ctrl Pts',(1.99736456050232,-0.0655156899101971,
32.4739066187066));
#20528=CARTESIAN_POINT('Ctrl Pts',(1.98968098453288,-0.18690740954904,32.46544801048));
#20529=CARTESIAN_POINT('Ctrl Pts',(1.96983898546714,-0.314355673926472,
32.457026571927));
#20530=CARTESIAN_POINT('Ctrl Pts',(1.96862913945504,-0.321845357539484,
32.4565334404044));
#20531=CARTESIAN_POINT('Ctrl Pts',(1.96679763103281,-0.332786624761421,
32.4558158170144));
#20532=CARTESIAN_POINT('Ctrl Pts',(1.96620956877452,-0.336243648531386,
32.4555894797688));
#20533=CARTESIAN_POINT('Ctrl Pts',(1.9651507038387,-0.342370593862699,32.4551890773148));
#20534=CARTESIAN_POINT('Ctrl Pts',(1.96468357112867,-0.345041125126671,
32.4550148052127));
#20535=CARTESIAN_POINT('Ctrl Pts',(1.96368510715721,-0.350681428011536,
32.4546472685231));
#20536=CARTESIAN_POINT('Ctrl Pts',(1.96315248420269,-0.353650941025623,
32.4544540788045));
#20537=CARTESIAN_POINT('Ctrl Pts',(1.96170843947949,-0.36159807527564,32.4539378628263));
#20538=CARTESIAN_POINT('Ctrl Pts',(1.96078480258814,-0.366573497211493,
32.4536155258246));
#20539=CARTESIAN_POINT('Ctrl Pts',(1.95628006668931,-0.390335253572446,
32.4520799206508));
#20540=CARTESIAN_POINT('Ctrl Pts',(1.9524477086605,-0.409073733944282,32.4508803702721));
#20541=CARTESIAN_POINT('Ctrl Pts',(1.9410174927103,-0.461136287084059,32.4475721556635));
#20542=CARTESIAN_POINT('Ctrl Pts',(1.93283157793759,-0.494325761173943,
32.4454914222752));
#20543=CARTESIAN_POINT('Ctrl Pts',(1.89987849515198,-0.614553661226869,
32.4380035581232));
#20544=CARTESIAN_POINT('Ctrl Pts',(1.87004930999941,-0.700094498784596,
32.4327682761755));
#20545=CARTESIAN_POINT('Ctrl Pts',(1.77261486071114,-0.928283444794056,
32.4183783679804));
#20546=CARTESIAN_POINT('Ctrl Pts',(1.69376389168123,-1.06537698320112,32.4092040329626));
#20547=CARTESIAN_POINT('Ctrl Pts',(1.59212644424844,-1.20179772962198,32.3985801178017));
#20548=CARTESIAN_POINT('Ctrl Pts',(1.58455013849633,-1.211769468417,32.3977944612093));
#20549=CARTESIAN_POINT('Ctrl Pts',(1.5731139943908,-1.22653077697972,32.396617472141));
#20550=CARTESIAN_POINT('Ctrl Pts',(1.56932498464801,-1.23137503523889,32.3962289408024));
#20551=CARTESIAN_POINT('Ctrl Pts',(1.56251839258574,-1.23999483679082,32.3955334762726));
#20552=CARTESIAN_POINT('Ctrl Pts',(1.55950936336184,-1.24377709713176,32.3952268860175));
#20553=CARTESIAN_POINT('Ctrl Pts',(1.55312289836002,-1.25174508281412,32.3945779517426));
#20554=CARTESIAN_POINT('Ctrl Pts',(1.54974222519764,-1.255928152509,32.3942354790177));
#20555=CARTESIAN_POINT('Ctrl Pts',(1.54072384522464,-1.26699517270886,32.3933246037741));
#20556=CARTESIAN_POINT('Ctrl Pts',(1.53505697500883,-1.27385509934689,32.392755022962));
#20557=CARTESIAN_POINT('Ctrl Pts',(1.50840775381711,-1.30567877213289,32.390089146776));
#20558=CARTESIAN_POINT('Ctrl Pts',(1.48686218613045,-1.33016226002758,32.3879698469219));
#20559=CARTESIAN_POINT('Ctrl Pts',(1.42673759741959,-1.39519864078846,32.3821468587206));
#20560=CARTESIAN_POINT('Ctrl Pts',(1.38703875512352,-1.43467137173626,32.3783974910547));
#20561=CARTESIAN_POINT('Ctrl Pts',(1.26863394464928,-1.54288886120904,32.3674851580711));
#20562=CARTESIAN_POINT('Ctrl Pts',(1.18612097049716,-1.60718759128474,32.3601878530912));
#20563=CARTESIAN_POINT('Ctrl Pts',(1.00713807874719,-1.7253424130091,32.3452343891684));
#20564=CARTESIAN_POINT('Ctrl Pts',(0.91044412816499,-1.77826637002954,32.3376063418241));
#20565=CARTESIAN_POINT('Ctrl Pts',(0.80347504740806,-1.8257886886864,32.3299616370584));
#20566=CARTESIAN_POINT('Ctrl Pts',(0.79706782121218,-1.82859491944787,32.3295066736343));
#20567=CARTESIAN_POINT('Ctrl Pts',(0.787438329915628,-1.8327522049802,32.3288274446735));
#20568=CARTESIAN_POINT('Ctrl Pts',(0.784227144523292,-1.83412855452577,
32.3286016931392));
#20569=CARTESIAN_POINT('Ctrl Pts',(0.77867523675752,-1.83649091723438,32.3282127060926));
#20570=CARTESIAN_POINT('Ctrl Pts',(0.776336230200448,-1.83748090365047,
32.3280492305237));
#20571=CARTESIAN_POINT('Ctrl Pts',(0.771501824193918,-1.8395161910968,32.3277121918679));
#20572=CARTESIAN_POINT('Ctrl Pts',(0.769006186141714,-1.84056088402972,
32.3275386681908));
#20573=CARTESIAN_POINT('Ctrl Pts',(0.763025081623626,-1.84305033109771,
32.3271238903255));
#20574=CARTESIAN_POINT('Ctrl Pts',(0.759537602938234,-1.84449028960265,
32.3268829272453));
#20575=CARTESIAN_POINT('Ctrl Pts',(0.75209367916114,-1.84753914756337,32.3263704435451));
#20576=CARTESIAN_POINT('Ctrl Pts',(0.748136101459601,-1.84914525619373,
32.3260990881553));
#20577=CARTESIAN_POINT('Ctrl Pts',(0.737253603402887,-1.85352105772802,
32.3253558757013));
#20578=CARTESIAN_POINT('Ctrl Pts',(0.73031817850206,-1.85626467653479,32.3248855050298));
#20579=CARTESIAN_POINT('Ctrl Pts',(0.669533444691139,-1.87991740342202,
32.3207902417237));
#20580=CARTESIAN_POINT('Ctrl Pts',(0.614809294862489,-1.89851925552571,
32.3172895199227));
#20581=CARTESIAN_POINT('Ctrl Pts',(0.457864477697418,-1.94436772459396,
32.3075665543522));
#20582=CARTESIAN_POINT('Ctrl Pts',(0.354178327847693,-1.96590073236273,
32.3015058179901));
#20583=CARTESIAN_POINT('Ctrl Pts',(0.122283269115748,-1.99510794679716,
32.2879034992953));
#20584=CARTESIAN_POINT('Ctrl Pts',(-0.0059277955016167,-1.99884135601865,
32.2803384516671));
#20585=CARTESIAN_POINT('Ctrl Pts',(-0.146593543900511,-1.98939875770172,
32.2715392050502));
#20586=CARTESIAN_POINT('Ctrl Pts',(-0.159575257583097,-1.9883995596025,
32.2707227133513));
#20587=CARTESIAN_POINT('Ctrl Pts',(-0.178770558302684,-1.98673291787286,
32.269508505695));
#20588=CARTESIAN_POINT('Ctrl Pts',(-0.184992465790764,-1.98616323237375,
32.2691138605299));
#20589=CARTESIAN_POINT('Ctrl Pts',(-0.1960343002,-1.98509989430986,32.2684115443737));
#20590=CARTESIAN_POINT('Ctrl Pts',(-0.20085531983028,-1.98461789195329,
32.2681042421835));
#20591=CARTESIAN_POINT('Ctrl Pts',(-0.210971802636704,-1.98356921329467,
32.267457986733));
#20592=CARTESIAN_POINT('Ctrl Pts',(-0.216266841089597,-1.98299888501643,
32.2671189207444));
#20593=CARTESIAN_POINT('Ctrl Pts',(-0.230166976232471,-1.98144536634449,
32.2662266669185));
#20594=CARTESIAN_POINT('Ctrl Pts',(-0.238767990847383,-1.98042733251649,
32.2656723851528));
#20595=CARTESIAN_POINT('Ctrl Pts',(-0.277311643169661,-1.97561048932814,
32.2631784968194));
#20596=CARTESIAN_POINT('Ctrl Pts',(-0.30717102911427,-1.97118856169952,
32.2612193457107));
#20597=CARTESIAN_POINT('Ctrl Pts',(-0.386471177699078,-1.95759936866033,
32.2559403858176));
#20598=CARTESIAN_POINT('Ctrl Pts',(-0.435682453834954,-1.94723787575538,
32.2525846785828));
#20599=CARTESIAN_POINT('Ctrl Pts',(-0.588928634873387,-1.90887174965014,
32.2418865279852));
#20600=CARTESIAN_POINT('Ctrl Pts',(-0.691111943997745,-1.87429682493267,
32.2343758941744));
#20601=CARTESIAN_POINT('Ctrl Pts',(-0.896020780072597,-1.78591908084901,
32.2188098426077));
#20602=CARTESIAN_POINT('Ctrl Pts',(-0.997889855101148,-1.73106406845087,
32.210784181256));
#20603=CARTESIAN_POINT('Ctrl Pts',(-1.10088223226489,-1.66347379643079,
32.2027394434066));
#20604=CARTESIAN_POINT('Ctrl Pts',(-1.10729042317245,-1.65921508073954,
32.2022392577582));
#20605=CARTESIAN_POINT('Ctrl Pts',(-1.11659991485968,-1.65295028087775,
32.2015133251425));
#20606=CARTESIAN_POINT('Ctrl Pts',(-1.11952069255584,-1.65097347656691,
32.201285672576));
#20607=CARTESIAN_POINT('Ctrl Pts',(-1.12461832191774,-1.64750361459868,
32.2008885528908));
#20608=CARTESIAN_POINT('Ctrl Pts',(-1.12679747047572,-1.64601397046622,
32.2007188564654));
#20609=CARTESIAN_POINT('Ctrl Pts',(-1.12898097269192,-1.64451498195596,
32.2005488901526));
#20610=CARTESIAN_POINT('Ctrl Pts',(-1.12898825439329,-1.64450998294956,
32.2005483233375));
#20611=CARTESIAN_POINT('Ctrl Pts',(-1.12900278842142,-1.64450000496019,
32.2005471919951));
#20612=CARTESIAN_POINT('Ctrl Pts',(-1.1290100235002,-1.64449503781967,32.2005466288105));
#20613=CARTESIAN_POINT('Ctrl Pts',(-1.12902444250486,-1.64448513851689,
32.2005455064246));
#20614=CARTESIAN_POINT('Ctrl Pts',(-1.12903162588245,-1.64448020673208,
32.200544947266));
#20615=CARTESIAN_POINT('Ctrl Pts',(-1.12904594255831,-1.64447037740662,
32.2005438328484));
#20616=CARTESIAN_POINT('Ctrl Pts',(-1.12905307499812,-1.64446548045636,
32.2005432776562));
#20617=CARTESIAN_POINT('Ctrl Pts',(-1.12906729000837,-1.64445572065878,
32.2005421711552));
#20618=CARTESIAN_POINT('Ctrl Pts',(-1.12907437195736,-1.64445085823911,
32.2005416198947));
#20619=CARTESIAN_POINT('Ctrl Pts',(-1.12908848677094,-1.64444116696661,
32.2005405211958));
#20620=CARTESIAN_POINT('Ctrl Pts',(-1.12909551887482,-1.64443633863705,
32.2005399738167));
#20621=CARTESIAN_POINT('Ctrl Pts',(-1.1291095343607,-1.64442671529867,32.2005388828523));
#20622=CARTESIAN_POINT('Ctrl Pts',(-1.12911651708822,-1.64442192074018,
32.200538339318));
#20623=CARTESIAN_POINT('Ctrl Pts',(-1.1291304345631,-1.64441236443739,32.2005372559856));
#20624=CARTESIAN_POINT('Ctrl Pts',(-1.12913736850178,-1.64440760324931,
32.2005367162504));
#20625=CARTESIAN_POINT('Ctrl Pts',(-1.12915118900127,-1.64439811327649,
32.2005356404692));
#20626=CARTESIAN_POINT('Ctrl Pts',(-1.12915807471961,-1.64439338507116,
32.2005351044888));
#20627=CARTESIAN_POINT('Ctrl Pts',(-1.12917179923596,-1.64438396075233,
32.2005340361815));
#20628=CARTESIAN_POINT('Ctrl Pts',(-1.12917863724504,-1.64437926518148,
32.2005335039161));
#20629=CARTESIAN_POINT('Ctrl Pts',(-1.12919226686039,-1.64436990577884,
32.2005324429986));
#20630=CARTESIAN_POINT('Ctrl Pts',(-1.12919905767014,-1.6443652424949,32.2005319144084));
#20631=CARTESIAN_POINT('Ctrl Pts',(-1.12921259344222,-1.64435594728726,
32.2005308607981));
#20632=CARTESIAN_POINT('Ctrl Pts',(-1.12921933755909,-1.64435131594502,
32.2005303358438));
#20633=CARTESIAN_POINT('Ctrl Pts',(-1.12923278057776,-1.64434208418906,
32.2005292894559));
#20634=CARTESIAN_POINT('Ctrl Pts',(-1.12923947855604,-1.64433748441039,
32.2005287680943));
#20635=CARTESIAN_POINT('Ctrl Pts',(-1.12925282977169,-1.64432831545842,
32.2005277288548));
#20636=CARTESIAN_POINT('Ctrl Pts',(-1.12925948214429,-1.64432374687984,
32.2005272110442));
#20637=CARTESIAN_POINT('Ctrl Pts',(-1.12927274232323,-1.64431464021051,
32.2005261788934));
#20638=CARTESIAN_POINT('Ctrl Pts',(-1.12927934941847,-1.64431010260896,
32.2005256646084));
#20639=CARTESIAN_POINT('Ctrl Pts',(-1.12929252005907,-1.64430105719805,
32.2005246394296));
#20640=CARTESIAN_POINT('Ctrl Pts',(-1.12929908254952,-1.64429655011401,
32.2005241286178));
#20641=CARTESIAN_POINT('Ctrl Pts',(-1.12931216417362,-1.64428756560787,
32.2005231103702));
#20642=CARTESIAN_POINT('Ctrl Pts',(-1.12931868246514,-1.64428308876495,
32.200522603));
#20643=CARTESIAN_POINT('Ctrl Pts',(-1.12933167610801,-1.6442741644572,32.2005215916031));
#20644=CARTESIAN_POINT('Ctrl Pts',(-1.12933815060729,-1.64426971757838,
32.2005210876428));
#20645=CARTESIAN_POINT('Ctrl Pts',(-1.1293510574228,-1.64426085268109,32.2005200830067));
#20646=CARTESIAN_POINT('Ctrl Pts',(-1.12935748867744,-1.64425643539254,
32.2005195824136));
#20647=CARTESIAN_POINT('Ctrl Pts',(-1.12937030945367,-1.64424762936891,
32.200518584477));
#20648=CARTESIAN_POINT('Ctrl Pts',(-1.12937669794717,-1.64424324134075,
32.2005180872135));
#20649=CARTESIAN_POINT('Ctrl Pts',(-1.12938943349152,-1.64423449364064,
32.2005170959134));
#20650=CARTESIAN_POINT('Ctrl Pts',(-1.12939577961846,-1.64423013460404,
32.2005166019487));
#20651=CARTESIAN_POINT('Ctrl Pts',(-1.12940843097335,-1.64422144451578,
32.200515617204));
#20652=CARTESIAN_POINT('Ctrl Pts',(-1.12941473520491,-1.64421711414925,
32.2005151265015));
#20653=CARTESIAN_POINT('Ctrl Pts',(-1.12942730314356,-1.64420848114597,
32.2005141482518));
#20654=CARTESIAN_POINT('Ctrl Pts',(-1.12943356585409,-1.64420417919449,
32.2005136607823));
#20655=CARTESIAN_POINT('Ctrl Pts',(-1.12944605151944,-1.6441956024953,32.2005126889388));
#20656=CARTESIAN_POINT('Ctrl Pts',(-1.1294522732779,-1.64419132857012,32.2005122046579));
#20657=CARTESIAN_POINT('Ctrl Pts',(-1.12946467714457,-1.64418280785311,
32.2005112391835));
#20658=CARTESIAN_POINT('Ctrl Pts',(-1.12947085825948,-1.64417856174433,
32.2005107580673));
#20659=CARTESIAN_POINT('Ctrl Pts',(-1.12948318152058,-1.64417009619397,
32.2005097988691));
#20660=CARTESIAN_POINT('Ctrl Pts',(-1.12948932251604,-1.64416587754357,
32.2005093208767));
#20661=CARTESIAN_POINT('Ctrl Pts',(-1.12950156574171,-1.64415746677216,
32.2005083679103));
#20662=CARTESIAN_POINT('Ctrl Pts',(-1.12950766696792,-1.64415327534155,
32.2005078930144));
#20663=CARTESIAN_POINT('Ctrl Pts',(-1.12951983107695,-1.64414491872184,
32.2005069462082));
#20664=CARTESIAN_POINT('Ctrl Pts',(-1.12952589290254,-1.64414075425971,
32.2005064743802));
#20665=CARTESIAN_POINT('Ctrl Pts',(-1.12953797887576,-1.64413245112173,
32.2005055336579));
#20666=CARTESIAN_POINT('Ctrl Pts',(-1.1295440017855,-1.64412831329696,32.2005050648599));
#20667=CARTESIAN_POINT('Ctrl Pts',(-1.12955601025092,-1.64412006321304,
32.2005041301725));
#20668=CARTESIAN_POINT('Ctrl Pts',(-1.12956199462572,-1.64411595176581,
32.200503664375));
#20669=CARTESIAN_POINT('Ctrl Pts',(-1.12957394363968,-1.64410774233429,
32.2005027343171));
#20670=CARTESIAN_POINT('Ctrl Pts',(-1.12957990721702,-1.64410364507931,
32.2005022701392));
#20671=CARTESIAN_POINT('Ctrl Pts',(-1.1295917289717,-1.64409552289097,32.2005013499885));
#20672=CARTESIAN_POINT('Ctrl Pts',(-1.12959763785162,-1.64409146312224,
32.2005008900692));
#20673=CARTESIAN_POINT('Ctrl Pts',(-1.12960941827893,-1.64408336914108,
32.2004999731372));
#20674=CARTESIAN_POINT('Ctrl Pts',(-1.1296152898331,-1.64407933492457,32.2004995161241));
#20675=CARTESIAN_POINT('Ctrl Pts',(-1.1321009175131,-1.64237149488527,32.200306047197));
#20676=CARTESIAN_POINT('Ctrl Pts',(-1.13457683593976,-1.64066206705954,
32.2001134205673));
#20677=CARTESIAN_POINT('Ctrl Pts',(-1.13967419220664,-1.63712568472626,
32.199717003506));
#20678=CARTESIAN_POINT('Ctrl Pts',(-1.14229512909805,-1.63529801881902,
32.199513261818));
#20679=CARTESIAN_POINT('Ctrl Pts',(-1.14887271143428,-1.63068772397597,
32.199002132005));
#20680=CARTESIAN_POINT('Ctrl Pts',(-1.15282367462965,-1.62789696742885,
32.1986952814134));
#20681=CARTESIAN_POINT('Ctrl Pts',(-1.16401445556548,-1.61993120340002,
32.1978265156498));
#20682=CARTESIAN_POINT('Ctrl Pts',(-1.17122995375882,-1.614722006613,32.1972667944543));
#20683=CARTESIAN_POINT('Ctrl Pts',(-1.24446582675881,-1.56110049638963,
32.1915874758735));
#20684=CARTESIAN_POINT('Ctrl Pts',(-1.30748957121274,-1.50870946941751,
32.1867131744928));
#20685=CARTESIAN_POINT('Ctrl Pts',(-1.44765094977023,-1.37679474645003,
32.1754366363088));
#20686=CARTESIAN_POINT('Ctrl Pts',(-1.52173848995551,-1.29443790360402,
32.1691098508864));
#20687=CARTESIAN_POINT('Ctrl Pts',(-1.64701158555818,-1.12947014584585,
32.1569270686873));
#20688=CARTESIAN_POINT('Ctrl Pts',(-1.69973627328369,-1.04844779328467,
32.151130689616));
#20689=CARTESIAN_POINT('Ctrl Pts',(-1.75252351357761,-0.952811781841404,
32.1443103111423));
#20690=CARTESIAN_POINT('Ctrl Pts',(-1.75855608767532,-0.941631261088707,
32.1435134312328));
#20691=CARTESIAN_POINT('Ctrl Pts',(-1.76736660344698,-0.924922222399464,
32.1423228823436));
#20692=CARTESIAN_POINT('Ctrl Pts',(-1.77022636685033,-0.919437021864666,
32.1419321112741));
#20693=CARTESIAN_POINT('Ctrl Pts',(-1.77527689745009,-0.909638884477386,
32.1412341480227));
#20694=CARTESIAN_POINT('Ctrl Pts',(-1.77747758669201,-0.905331094630736,
32.1409273082408));
#20695=CARTESIAN_POINT('Ctrl Pts',(-1.78208293023251,-0.896234737610973,
32.1402794100404));
#20696=CARTESIAN_POINT('Ctrl Pts',(-1.78448399889495,-0.891444407627698,
32.1399382289148));
#20697=CARTESIAN_POINT('Ctrl Pts',(-1.79078082460493,-0.878754336242574,
32.139034413736));
#20698=CARTESIAN_POINT('Ctrl Pts',(-1.79464357499126,-0.870838434987936,
32.1384706336672));
#20699=CARTESIAN_POINT('Ctrl Pts',(-1.81215283604656,-0.834345569413666,
32.1358713832743));
#20700=CARTESIAN_POINT('Ctrl Pts',(-1.82516939072008,-0.805473111825947,
32.133814284664));
#20701=CARTESIAN_POINT('Ctrl Pts',(-1.85840050842208,-0.726815907048204,
32.1282047784031));
#20702=CARTESIAN_POINT('Ctrl Pts',(-1.87729889687107,-0.676507060522405,
32.1246106897333));
#20703=CARTESIAN_POINT('Ctrl Pts',(-1.92407777126974,-0.534851104395849,
32.114479852037));
#20704=CARTESIAN_POINT('Ctrl Pts',(-1.94746455250535,-0.442176494784212,
32.1078338879887));
#20705=CARTESIAN_POINT('Ctrl Pts',(-1.98451431995775,-0.233181474814436,
32.093024626058));
#20706=CARTESIAN_POINT('Ctrl Pts',(-1.99476346756107,-0.11659257845761,
32.0848797877451));
#20707=CARTESIAN_POINT('Ctrl Pts',(-1.99474998671879,0.000230185530924812,
32.0772014385531));
#20708=CARTESIAN_POINT('',(-1.99474934552561,0.000704641662985501,30.4808452152674));
#20709=CARTESIAN_POINT('Ctrl Pts',(-1.99474998656482,0.000231515990512227,
32.0772013511067));
#20710=CARTESIAN_POINT('Ctrl Pts',(-1.99474932987922,0.00588954239274279,
32.0768294691232));
#20711=CARTESIAN_POINT('Ctrl Pts',(-1.994724600045,0.0115476292319622,32.0764587444995));
#20712=CARTESIAN_POINT('Ctrl Pts',(-1.99462718926037,0.0228406201405742,
32.0757212328955));
#20713=CARTESIAN_POINT('Ctrl Pts',(-1.99455470408963,0.0284754680534856,
32.0753544397563));
#20714=CARTESIAN_POINT('Ctrl Pts',(-1.99440133338182,0.0374432595348793,
32.0747726862233));
#20715=CARTESIAN_POINT('Ctrl Pts',(-1.99433597042751,0.0407763869072901,
32.0745568997712));
#20716=CARTESIAN_POINT('Ctrl Pts',(-1.99420454227825,0.0467184856729034,
32.0741730088618));
#20717=CARTESIAN_POINT('Ctrl Pts',(-1.99414171269055,0.049327510029208,
32.0740047271924));
#20718=CARTESIAN_POINT('Ctrl Pts',(-1.99400421729553,0.0546065791285882,
32.073664794882));
#20719=CARTESIAN_POINT('Ctrl Pts',(-1.99392930885807,0.0572765976941349,
32.0734931603565));
#20720=CARTESIAN_POINT('Ctrl Pts',(-1.99375553841236,0.0630562843716036,
32.0731222703868));
#20721=CARTESIAN_POINT('Ctrl Pts',(-1.99365476469498,0.066165863417449,
32.0729231237206));
#20722=CARTESIAN_POINT('Ctrl Pts',(-1.99336115179429,0.0746152199705355,
32.0723830554699));
#20723=CARTESIAN_POINT('Ctrl Pts',(-1.9931541304564,0.0799545268342738,
32.0720429198772));
#20724=CARTESIAN_POINT('Ctrl Pts',(-1.99217525128507,0.102826663548703,
32.0705905258563));
#20725=CARTESIAN_POINT('Ctrl Pts',(-1.99119345952562,0.120350371331074,
32.0694894798816));
#20726=CARTESIAN_POINT('Ctrl Pts',(-1.97561090389686,0.345282062007617,
32.0554811198056));
#20727=CARTESIAN_POINT('Ctrl Pts',(-1.92889957127704,0.549212799457698,
32.0440269275762));
#20728=CARTESIAN_POINT('Ctrl Pts',(-1.83237428774714,0.78998399887494,32.0286128687338));
#20729=CARTESIAN_POINT('Ctrl Pts',(-1.81140904770275,0.836939007320726,
32.0255168011908));
#20730=CARTESIAN_POINT('Ctrl Pts',(-1.77507594953448,0.91053494018854,32.0204793993337));
#20731=CARTESIAN_POINT('Ctrl Pts',(-1.76086491394984,0.937722292929969,
32.0185767066792));
#20732=CARTESIAN_POINT('Ctrl Pts',(-1.74182122376156,0.972194559216066,
32.0161052199152));
#20733=CARTESIAN_POINT('Ctrl Pts',(-1.73755934879876,0.979791274731646,
32.0155568306202));
#20734=CARTESIAN_POINT('Ctrl Pts',(-1.73060635186003,0.991996823480004,
32.0146695752303));
#20735=CARTESIAN_POINT('Ctrl Pts',(-1.72794621815228,0.996623253372562,
32.014331826881));
#20736=CARTESIAN_POINT('Ctrl Pts',(-1.72283701144074,1.00542709480778,32.0136863307224));
#20737=CARTESIAN_POINT('Ctrl Pts',(-1.72039122622048,1.00960637826224,32.0133787037177));
#20738=CARTESIAN_POINT('Ctrl Pts',(-1.71476576295487,1.01913920116737,32.0126742388898));
#20739=CARTESIAN_POINT('Ctrl Pts',(-1.71157619948137,1.02448682035149,32.0122770429992));
#20740=CARTESIAN_POINT('Ctrl Pts',(-1.70169628416991,1.04087655746113,32.0110534303641));
#20741=CARTESIAN_POINT('Ctrl Pts',(-1.69492382970594,1.0518685516234,32.0102240136365));
#20742=CARTESIAN_POINT('Ctrl Pts',(-1.61418203494577,1.1801114931882,32.0004419309435));
#20743=CARTESIAN_POINT('Ctrl Pts',(-1.52830547945784,1.28938546386611,31.9910249156142));
#20744=CARTESIAN_POINT('Ctrl Pts',(-1.36087498114351,1.46199469660722,31.9743119575535));
#20745=CARTESIAN_POINT('Ctrl Pts',(-1.28443323552939,1.52958856444278,31.9671500677009));
#20746=CARTESIAN_POINT('Ctrl Pts',(-1.17207749735467,1.61455275352589,31.9574998582312));
#20747=CARTESIAN_POINT('Ctrl Pts',(-1.14030973197873,1.63714396882882,31.9548598208094));
#20748=CARTESIAN_POINT('Ctrl Pts',(-1.09634345469721,1.66650882697449,31.9513441312956));
#20749=CARTESIAN_POINT('Ctrl Pts',(-1.0847077501933,1.67410566041631,31.9504264001781));
#20750=CARTESIAN_POINT('Ctrl Pts',(-1.06737772965087,1.68516370659574,31.9490792947103));
#20751=CARTESIAN_POINT('Ctrl Pts',(-1.06174420241356,1.68871880056284,31.9486444337705));
#20752=CARTESIAN_POINT('Ctrl Pts',(-1.0527423915626,1.6943366304862,31.9479545399262));
#20753=CARTESIAN_POINT('Ctrl Pts',(-1.04938566701543,1.69641766169301,31.9476983757351));
#20754=CARTESIAN_POINT('Ctrl Pts',(-1.04300600898862,1.7003466058827,31.9472136235588));
#20755=CARTESIAN_POINT('Ctrl Pts',(-1.03998429523219,1.70219645783603,31.9469849121348));
#20756=CARTESIAN_POINT('Ctrl Pts',(-1.03467837933972,1.70542526444898,31.9465848919186));
#20757=CARTESIAN_POINT('Ctrl Pts',(-1.03239631937592,1.70680769900328,31.9464133553995));
#20758=CARTESIAN_POINT('Ctrl Pts',(-1.02756386012961,1.70972188567511,31.9460511995249));
#20759=CARTESIAN_POINT('Ctrl Pts',(-1.0250128102914,1.71125250972027,31.9458606541848));
#20760=CARTESIAN_POINT('Ctrl Pts',(-1.01827427440553,1.71527514102252,31.9453589835437));
#20761=CARTESIAN_POINT('Ctrl Pts',(-1.01408103210372,1.71775754076702,31.9450484810027));
#20762=CARTESIAN_POINT('Ctrl Pts',(-0.998711409218007,1.72678046409516,
31.9439163434955));
#20763=CARTESIAN_POINT('Ctrl Pts',(-0.987480213083196,1.73322765377137,
31.9431005227049));
#20764=CARTESIAN_POINT('Ctrl Pts',(-0.819987389136426,1.82721910786742,
31.9310911721451));
#20765=CARTESIAN_POINT('Ctrl Pts',(-0.652667827218758,1.89345083260286,
31.9210544744051));
#20766=CARTESIAN_POINT('Ctrl Pts',(-0.452517921620162,1.94293183270706,
31.9089894693175));
#20767=CARTESIAN_POINT('Ctrl Pts',(-0.426178454825232,1.94887876559413,
31.9074021201945));
#20768=CARTESIAN_POINT('Ctrl Pts',(-0.344629904279162,1.96555856505706,
31.9024745610374));
#20769=CARTESIAN_POINT('Ctrl Pts',(-0.289084820663625,1.97449219896898,
31.8990991878472));
#20770=CARTESIAN_POINT('Ctrl Pts',(-0.200738904723304,1.98489354711158,
31.8936488041727));
#20771=CARTESIAN_POINT('Ctrl Pts',(-0.168150524710556,1.98791944227067,
31.8916211236522));
#20772=CARTESIAN_POINT('Ctrl Pts',(-0.126615798296741,1.99074743904478,
31.8890092960904));
#20773=CARTESIAN_POINT('Ctrl Pts',(-0.11772389657387,1.99129304886842,31.8884485562656));
#20774=CARTESIAN_POINT('Ctrl Pts',(-0.10345596619214,1.99207263386072,31.8875461302064));
#20775=CARTESIAN_POINT('Ctrl Pts',(-0.0980820570298916,1.99234445432535,
31.8872056326682));
#20776=CARTESIAN_POINT('Ctrl Pts',(-0.0878796428655608,1.99281913032875,
31.8865580190796));
#20777=CARTESIAN_POINT('Ctrl Pts',(-0.0830513642794613,1.99302618850091,
31.8862510371584));
#20778=CARTESIAN_POINT('Ctrl Pts',(-0.0720812443907305,1.99345670351143,
31.8855524005117));
#20779=CARTESIAN_POINT('Ctrl Pts',(-0.065939049774496,1.99366932435777,
31.8851604090009));
#20780=CARTESIAN_POINT('Ctrl Pts',(-0.0500708889735416,1.99414521335601,
31.8841455393411));
#20781=CARTESIAN_POINT('Ctrl Pts',(-0.0403438936627081,1.99436571133372,
31.883521328235));
#20782=CARTESIAN_POINT('Ctrl Pts',(0.0200043326713027,1.99529205690601,
31.8796351459475));
#20783=CARTESIAN_POINT('Ctrl Pts',(0.0706314838680484,1.99414166668733,
31.8763155430744));
#20784=CARTESIAN_POINT('Ctrl Pts',(0.13409283830146,1.99028004094122,31.8720756688003));
#20785=CARTESIAN_POINT('Ctrl Pts',(0.147020947832433,1.98936682378843,31.8712078650238));
#20786=CARTESIAN_POINT('Ctrl Pts',(0.3242919908657,1.97510732536553,31.8592530943559));
#20787=CARTESIAN_POINT('Ctrl Pts',(0.486360859213983,1.94155965709629,31.8475927555112));
#20788=CARTESIAN_POINT('Ctrl Pts',(0.704559251501132,1.86733280074355,31.8316820308599));
#20789=CARTESIAN_POINT('Ctrl Pts',(0.765623194195359,1.84313821951995,31.827214800699));
#20790=CARTESIAN_POINT('Ctrl Pts',(0.832633692061753,1.81268089633509,31.8223765657941));
#20791=CARTESIAN_POINT('Ctrl Pts',(0.83985911683253,1.80934451277659,31.8218557556634));
#20792=CARTESIAN_POINT('Ctrl Pts',(0.851111242574038,1.80406684850361,31.8210462878835));
#20793=CARTESIAN_POINT('Ctrl Pts',(0.855151620779874,1.80215516743265,31.8207559483549));
#20794=CARTESIAN_POINT('Ctrl Pts',(0.861932017097704,1.79891912586887,31.8202692962759));
#20795=CARTESIAN_POINT('Ctrl Pts',(0.864675467753168,1.79760205809845,31.820072550747));
#20796=CARTESIAN_POINT('Ctrl Pts',(0.870027459364532,1.79501760241953,31.8196890655342));
#20797=CARTESIAN_POINT('Ctrl Pts',(0.872636270319368,1.79375079457314,31.8195022909254));
#20798=CARTESIAN_POINT('Ctrl Pts',(0.877614082183783,1.79132019796685,31.8191462183624));
#20799=CARTESIAN_POINT('Ctrl Pts',(0.879983531011061,1.79015739925545,31.8189768622947));
#20800=CARTESIAN_POINT('Ctrl Pts',(0.88554676306466,1.78741354832691,31.8185795362488));
#20801=CARTESIAN_POINT('Ctrl Pts',(0.888738647033779,1.78582862561535,31.8183518081015));
#20802=CARTESIAN_POINT('Ctrl Pts',(0.898726561545294,1.78083573908963,31.8176398980057));
#20803=CARTESIAN_POINT('Ctrl Pts',(0.905507467644321,1.77739742110228,31.8171575744244));
#20804=CARTESIAN_POINT('Ctrl Pts',(1.01453463699822,1.72132834689195,31.8094160083485));
#20805=CARTESIAN_POINT('Ctrl Pts',(1.1120785330888,1.65998241239724,31.8026757435883));
#20806=CARTESIAN_POINT('Ctrl Pts',(1.28573768120921,1.52854991539803,31.7900165540472));
#20807=CARTESIAN_POINT('Ctrl Pts',(1.36275497706805,1.46030277563428,31.7841037038883));
#20808=CARTESIAN_POINT('Ctrl Pts',(1.47159155681531,1.34771828524721,31.7748167041358));
#20809=CARTESIAN_POINT('Ctrl Pts',(1.50742722730279,1.30751243014434,31.7715797750089));
#20810=CARTESIAN_POINT('Ctrl Pts',(1.561719604958,1.24139656868197,31.7663336591272));
#20811=CARTESIAN_POINT('Ctrl Pts',(1.58125975683932,1.21640904722309,31.764367372882));
#20812=CARTESIAN_POINT('Ctrl Pts',(1.60545683242319,1.18389762598168,31.7618244111468));
#20813=CARTESIAN_POINT('Ctrl Pts',(1.61067159959475,1.17679319501088,31.7612696413601));
#20814=CARTESIAN_POINT('Ctrl Pts',(1.61898167184888,1.16531310503677,31.7603745490021));
#20815=CARTESIAN_POINT('Ctrl Pts',(1.6221067578795,1.16095906546276,31.7600353806108));
#20816=CARTESIAN_POINT('Ctrl Pts',(1.62801890286672,1.15265147049618,31.7593888060741));
#20817=CARTESIAN_POINT('Ctrl Pts',(1.63080920635282,1.14870026217724,31.7590815276597));
#20818=CARTESIAN_POINT('Ctrl Pts',(1.63713393948355,1.13967463275887,31.7583801476378));
#20819=CARTESIAN_POINT('Ctrl Pts',(1.64065918552692,1.13459386561254,31.7579856992061));
#20820=CARTESIAN_POINT('Ctrl Pts',(1.65134865273557,1.11903366082132,31.7567787651803));
#20821=CARTESIAN_POINT('Ctrl Pts',(1.65843640410259,1.10850231759122,31.7559633971537));
#20822=CARTESIAN_POINT('Ctrl Pts',(1.7489937813781,0.971134835711256,31.7453456141375));
#20823=CARTESIAN_POINT('Ctrl Pts',(1.81779951396931,0.835265570101009,31.7349781352055));
#20824=CARTESIAN_POINT('Ctrl Pts',(1.90336458059826,0.604291428588858,31.7178187847069));
#20825=CARTESIAN_POINT('Ctrl Pts',(1.92986256383391,0.513416539776491,31.7111890253457));
#20826=CARTESIAN_POINT('Ctrl Pts',(1.95724109497874,0.386616581873011,31.7023309743702));
#20827=CARTESIAN_POINT('Ctrl Pts',(1.96375525272594,0.352037931230871,31.6999551804326));
#20828=CARTESIAN_POINT('Ctrl Pts',(1.97245684607242,0.298031201910524,31.6963236815515));
#20829=CARTESIAN_POINT('Ctrl Pts',(1.97527902302628,0.278713937229114,31.6950403770361));
#20830=CARTESIAN_POINT('Ctrl Pts',(1.97847987220997,0.254304790513559,31.6934410545095));
#20831=CARTESIAN_POINT('Ctrl Pts',(1.97912309243677,0.249249508709049,31.6931110254362));
#20832=CARTESIAN_POINT('Ctrl Pts',(1.98011723139521,0.241189680478594,31.6925868190158));
#20833=CARTESIAN_POINT('Ctrl Pts',(1.98048069557435,0.238186747730455,31.6923919457197));
#20834=CARTESIAN_POINT('Ctrl Pts',(1.98115674019984,0.232492736804073,31.6920232772764));
#20835=CARTESIAN_POINT('Ctrl Pts',(1.9814706652022,0.229801881924157,31.691849410787));
#20836=CARTESIAN_POINT('Ctrl Pts',(1.98217671359029,0.223640859504411,31.6914521303368));
#20837=CARTESIAN_POINT('Ctrl Pts',(1.98256520631736,0.220170300206956,31.6912289230298));
#20838=CARTESIAN_POINT('Ctrl Pts',(1.98357278248761,0.210950274180009,31.6906374504553));
#20839=CARTESIAN_POINT('Ctrl Pts',(1.98417598827319,0.205199052488333,31.690270061884));
#20840=CARTESIAN_POINT('Ctrl Pts',(1.98813200801416,0.165831213238705,31.687765391635));
#20841=CARTESIAN_POINT('Ctrl Pts',(1.99065559639091,0.132134391251426,31.6856721203616));
#20842=CARTESIAN_POINT('Ctrl Pts',(1.99562692760634,0.031466058776295,31.6795259671994));
#20843=CARTESIAN_POINT('Ctrl Pts',(1.99555809048951,-0.035584830233128,
31.6755729127611));
#20844=CARTESIAN_POINT('Ctrl Pts',(1.99107210310318,-0.122762840000178,
31.6704768439513));
#20845=CARTESIAN_POINT('Ctrl Pts',(1.98972112004744,-0.142998997611173,
31.6692970713786));
#20846=CARTESIAN_POINT('Ctrl Pts',(1.97976899638068,-0.264224974468188,
31.6622321539425));
#20847=CARTESIAN_POINT('Ctrl Pts',(1.9637895730272,-0.364457916836624,31.6563926683583));
#20848=CARTESIAN_POINT('Ctrl Pts',(1.92818124007526,-0.513667176439659,
31.6472820783049));
#20849=CARTESIAN_POINT('Ctrl Pts',(1.91412251887782,-0.563800688808152,
31.6441486884623));
#20850=CARTESIAN_POINT('Ctrl Pts',(1.88860327018468,-0.642777820640292,
31.639055897928));
#20851=CARTESIAN_POINT('Ctrl Pts',(1.87840241391484,-0.672004349617054,
31.6371362431469));
#20852=CARTESIAN_POINT('Ctrl Pts',(1.86445542762859,-0.709161389761481,
31.6346456773719));
#20853=CARTESIAN_POINT('Ctrl Pts',(1.86133103675602,-0.717321884537835,
31.6340955661206));
#20854=CARTESIAN_POINT('Ctrl Pts',(1.85621005210657,-0.730438464894457,
31.6332061958353));
#20855=CARTESIAN_POINT('Ctrl Pts',(1.8542469632508,-0.735407578766996,31.6328680643335));
#20856=CARTESIAN_POINT('Ctrl Pts',(1.85046720699997,-0.744863821553946,
31.6322222805818));
#20857=CARTESIAN_POINT('Ctrl Pts',(1.84865411983734,-0.749352347945748,
31.631914751015));
#20858=CARTESIAN_POINT('Ctrl Pts',(1.84447605377035,-0.759588227052796,
31.6312111348816));
#20859=CARTESIAN_POINT('Ctrl Pts',(1.84210052650984,-0.76533119392625,31.6308146933366));
#20860=CARTESIAN_POINT('Ctrl Pts',(1.83473065726099,-0.782915148664882,
31.6295956728241));
#20861=CARTESIAN_POINT('Ctrl Pts',(1.82964877136552,-0.794718865569783,
31.6287701264769));
#20862=CARTESIAN_POINT('Ctrl Pts',(1.78188328349275,-0.902776993825045,
31.6211444719937));
#20863=CARTESIAN_POINT('Ctrl Pts',(1.73176238653417,-0.995543496451416,
31.6140847890614));
#20864=CARTESIAN_POINT('Ctrl Pts',(1.60324587333483,-1.19409242715677,31.5978204037459));
#20865=CARTESIAN_POINT('Ctrl Pts',(1.52123133386611,-1.29696072433048,31.5885470917199));
#20866=CARTESIAN_POINT('Ctrl Pts',(1.40054849237707,-1.42099976620114,31.5766648428988));
#20867=CARTESIAN_POINT('Ctrl Pts',(1.37044861020676,-1.45005086325532,31.5738255520883));
#20868=CARTESIAN_POINT('Ctrl Pts',(1.32313420684551,-1.49292617800254,31.5695747720104));
#20869=CARTESIAN_POINT('Ctrl Pts',(1.3065680269435,-1.50744578453689,31.5681239517869));
#20870=CARTESIAN_POINT('Ctrl Pts',(1.28571660851249,-1.52511918017284,31.5663473636237));
#20871=CARTESIAN_POINT('Ctrl Pts',(1.28165557607537,-1.52853351190485,31.5660036373573));
#20872=CARTESIAN_POINT('Ctrl Pts',(1.27522208916417,-1.53389882967076,31.5654627654761));
#20873=CARTESIAN_POINT('Ctrl Pts',(1.27285870498995,-1.53586057759228,31.5652648466817));
#20874=CARTESIAN_POINT('Ctrl Pts',(1.26840950490099,-1.53953635185446,31.5648937209171));
#20875=CARTESIAN_POINT('Ctrl Pts',(1.26632476502626,-1.54125158244618,31.5647204283514));
#20876=CARTESIAN_POINT('Ctrl Pts',(1.2615515846922,-1.54516251899288,31.5643250302089));
#20877=CARTESIAN_POINT('Ctrl Pts',(1.25886089618895,-1.54735543926808,31.5641031273757));
#20878=CARTESIAN_POINT('Ctrl Pts',(1.25056586835105,-1.55407995765512,31.5634220123758));
#20879=CARTESIAN_POINT('Ctrl Pts',(1.24494260511389,-1.5585882777907,31.562964448366));
#20880=CARTESIAN_POINT('Ctrl Pts',(1.19884777812114,-1.59513509121953,31.5592464479872));
#20881=CARTESIAN_POINT('Ctrl Pts',(1.15716698768159,-1.6256252873362,31.5560891392314));
#20882=CARTESIAN_POINT('Ctrl Pts',(1.05664667721089,-1.69332953472336,31.5488208749054));
#20883=CARTESIAN_POINT('Ctrl Pts',(0.996950117854174,-1.72914970939522,
31.5447640587105));
#20884=CARTESIAN_POINT('Ctrl Pts',(0.846401056888334,-1.80909092962046,
31.5348654168885));
#20885=CARTESIAN_POINT('Ctrl Pts',(0.753842344734532,-1.84957437193072,
31.5290506260312));
#20886=CARTESIAN_POINT('Ctrl Pts',(0.610053791048967,-1.89987092979403,
31.5199991077975));
#20887=CARTESIAN_POINT('Ctrl Pts',(0.560848489754028,-1.91497350872426,
31.5169002616554));
#20888=CARTESIAN_POINT('Ctrl Pts',(0.481446276305041,-1.93602150297413,
31.5118587339682));
#20889=CARTESIAN_POINT('Ctrl Pts',(0.451599283421843,-1.94320037663654,
31.5099547756967));
#20890=CARTESIAN_POINT('Ctrl Pts',(0.413083940313299,-1.95152892133551,
31.5074818649995));
#20891=CARTESIAN_POINT('Ctrl Pts',(0.404556263970177,-1.95331454147972,
31.506933346721));
#20892=CARTESIAN_POINT('Ctrl Pts',(0.390786345207502,-1.95610380097916,
31.5060459329258));
#20893=CARTESIAN_POINT('Ctrl Pts',(0.38555122999224,-1.95714238009246,31.5057081558867));
#20894=CARTESIAN_POINT('Ctrl Pts',(0.375558622648085,-1.95908313525623,
31.5050626382961));
#20895=CARTESIAN_POINT('Ctrl Pts',(0.370801883327998,-1.95998902357429,
31.5047550186901));
#20896=CARTESIAN_POINT('Ctrl Pts',(0.359921917649469,-1.96202001400915,
31.5040506178922));
#20897=CARTESIAN_POINT('Ctrl Pts',(0.353796651658854,-1.96313378301105,
31.5036534788658));
#20898=CARTESIAN_POINT('Ctrl Pts',(0.334957564206822,-1.9664682975837,31.502430212694));
#20899=CARTESIAN_POINT('Ctrl Pts',(0.322227523103384,-1.96859430700155,
31.5016010880314));
#20900=CARTESIAN_POINT('Ctrl Pts',(0.170028513222552,-1.9924968368546,31.4916563390715));
#20901=CARTESIAN_POINT('Ctrl Pts',(0.0286774136200812,-1.99952892784342,
31.4820580445661));
#20902=CARTESIAN_POINT('Ctrl Pts',(-0.210491895795797,-1.98605432024905,
31.4654002604322));
#20903=CARTESIAN_POINT('Ctrl Pts',(-0.308235481518195,-1.9732486449967,
31.4584850060521));
#20904=CARTESIAN_POINT('Ctrl Pts',(-0.46157151644206,-1.9414839997497,31.4477517363439));
#20905=CARTESIAN_POINT('Ctrl Pts',(-0.517971100143095,-1.92720414045988,
31.4438316777563));
#20906=CARTESIAN_POINT('Ctrl Pts',(-0.580203089146887,-1.90851734176708,
31.4395952660623));
#20907=CARTESIAN_POINT('Ctrl Pts',(-0.58672453187955,-1.90652259243112,
31.4391524400644));
#20908=CARTESIAN_POINT('Ctrl Pts',(-0.59647594995493,-1.9034850987971,31.4384920996695));
#20909=CARTESIAN_POINT('Ctrl Pts',(-0.599713618008486,-1.90246751799136,
31.4382731532227));
#20910=CARTESIAN_POINT('Ctrl Pts',(-0.605271195297765,-1.90070520570508,
31.4378978582564));
#20911=CARTESIAN_POINT('Ctrl Pts',(-0.607592345539976,-1.899964484072,31.4377412756485));
#20912=CARTESIAN_POINT('Ctrl Pts',(-0.612431723787028,-1.89841037424143,
31.4374151559839));
#20913=CARTESIAN_POINT('Ctrl Pts',(-0.614949681751742,-1.89759623061437,
31.4372456647642));
#20914=CARTESIAN_POINT('Ctrl Pts',(-0.621947166007032,-1.89531830935224,
31.436775154913));
#20915=CARTESIAN_POINT('Ctrl Pts',(-0.62642317359611,-1.89384365240303,
31.4364747725742));
#20916=CARTESIAN_POINT('Ctrl Pts',(-0.644326673098439,-1.8878747823889,
31.4352754612713));
#20917=CARTESIAN_POINT('Ctrl Pts',(-0.657711771778033,-1.88325338396664,
31.4343837518552));
#20918=CARTESIAN_POINT('Ctrl Pts',(-0.787200198933685,-1.83699663954138,
31.4257948963618));
#20919=CARTESIAN_POINT('Ctrl Pts',(-0.89927260918478,-1.78481330801568,
31.4186463048127));
#20920=CARTESIAN_POINT('Ctrl Pts',(-1.07591327940762,-1.68167375565586,
31.4067818551141));
#20921=CARTESIAN_POINT('Ctrl Pts',(-1.14344308049151,-1.63650639793599,
31.4020835874523));
#20922=CARTESIAN_POINT('Ctrl Pts',(-1.25308478655208,-1.55306520834449,
31.3939293295779));
#20923=CARTESIAN_POINT('Ctrl Pts',(-1.29665512215616,-1.51687762805256,
31.3905321066451));
#20924=CARTESIAN_POINT('Ctrl Pts',(-1.3630040696393,-1.45682145119373,31.3850495607634));
#20925=CARTESIAN_POINT('Ctrl Pts',(-1.38683242177852,-1.43415636259705,
31.3830122891388));
#20926=CARTESIAN_POINT('Ctrl Pts',(-1.41640029398225,-1.40460577948084,
31.3803897148444));
#20927=CARTESIAN_POINT('Ctrl Pts',(-1.42266941292446,-1.39825567258185,
31.3798280586367));
#20928=CARTESIAN_POINT('Ctrl Pts',(-1.43265244285895,-1.38800703482086,
31.3789245068296));
#20929=CARTESIAN_POINT('Ctrl Pts',(-1.43639359200502,-1.38413510852872,
31.3785838052613));
#20930=CARTESIAN_POINT('Ctrl Pts',(-1.44346251219736,-1.37675956053643,
31.3779360297551));
#20931=CARTESIAN_POINT('Ctrl Pts',(-1.44679332282461,-1.37325889474734,
31.377629090922));
#20932=CARTESIAN_POINT('Ctrl Pts',(-1.45432767863913,-1.36528248638433,
31.3769308636938));
#20933=CARTESIAN_POINT('Ctrl Pts',(-1.45852332814274,-1.36079938431561,
31.3765392400153));
#20934=CARTESIAN_POINT('Ctrl Pts',(-1.46930089936719,-1.34917631541821,
31.3755259408891));
#20935=CARTESIAN_POINT('Ctrl Pts',(-1.47585144033371,-1.34200759442334,
31.374902939348));
#20936=CARTESIAN_POINT('Ctrl Pts',(-1.51602220034926,-1.29739605753985,
31.3710376558577));
#20937=CARTESIAN_POINT('Ctrl Pts',(-1.5482652143614,-1.25874298781197,31.3677384518195));
#20938=CARTESIAN_POINT('Ctrl Pts',(-1.581718129923,-1.21540732136719,31.3640884223525));
#20939=CARTESIAN_POINT('Ctrl Pts',(-1.58441424422324,-1.21189054851352,
31.3637925590055));
#20940=CARTESIAN_POINT('Ctrl Pts',(-1.70256778802969,-1.05670453392889,
31.3507520080083));
#20941=CARTESIAN_POINT('Ctrl Pts',(-1.79569444202854,-0.889281258320573,
31.3371804596772));
#20942=CARTESIAN_POINT('Ctrl Pts',(-1.88362453382085,-0.658883659700334,
31.3202981224338));
#20943=CARTESIAN_POINT('Ctrl Pts',(-1.90139569462875,-0.605693662426969,
31.3165239749815));
#20944=CARTESIAN_POINT('Ctrl Pts',(-1.91877776054363,-0.545312145725606,
31.3124276778312));
#20945=CARTESIAN_POINT('Ctrl Pts',(-1.92061818384855,-0.538794233186789,
31.3119879274492));
#20946=CARTESIAN_POINT('Ctrl Pts',(-1.92332844373332,-0.529005400046055,
31.3113312597949));
#20947=CARTESIAN_POINT('Ctrl Pts',(-1.92422318698944,-0.525741517116593,
31.3111129335879));
#20948=CARTESIAN_POINT('Ctrl Pts',(-1.92574748754049,-0.520125088124526,
31.3107383365297));
#20949=CARTESIAN_POINT('Ctrl Pts',(-1.92638104533116,-0.517773658554759,
31.3105818341014));
#20950=CARTESIAN_POINT('Ctrl Pts',(-1.92769521510163,-0.512860357549892,
31.3102555155233));
#20951=CARTESIAN_POINT('Ctrl Pts',(-1.92837502452724,-0.510298298696599,
31.3100857464631));
#20952=CARTESIAN_POINT('Ctrl Pts',(-1.93025483769002,-0.503156277813248,
31.3096135656816));
#20953=CARTESIAN_POINT('Ctrl Pts',(-1.93144365571775,-0.498573348893381,
31.3093117978475));
#20954=CARTESIAN_POINT('Ctrl Pts',(-1.93616370941818,-0.480107139642457,
31.3081006307306));
#20955=CARTESIAN_POINT('Ctrl Pts',(-1.93956177019594,-0.466189814395688,
31.3071986315439));
#20956=CARTESIAN_POINT('Ctrl Pts',(-1.97718139378684,-0.304575809792007,
31.2968363213099));
#20957=CARTESIAN_POINT('Ctrl Pts',(-1.99461257580312,-0.153453721871375,
31.2882019858445));
#20958=CARTESIAN_POINT('Ctrl Pts',(-1.99487121963617,0.133668057474652,
31.2715168899994));
#20959=CARTESIAN_POINT('Ctrl Pts',(-1.98119470743788,0.268771501879354,
31.2635403645652));
#20960=CARTESIAN_POINT('Ctrl Pts',(-1.95133019524141,0.414132853595452,
31.2542776850415));
#20961=CARTESIAN_POINT('Ctrl Pts',(-1.94859819998239,0.426802757355567,
31.2534648555655));
#20962=CARTESIAN_POINT('Ctrl Pts',(-1.94436908622295,0.445528127312583,
31.2522550623641));
#20963=CARTESIAN_POINT('Ctrl Pts',(-1.94296668611304,0.45160481718661,31.2518611367817));
#20964=CARTESIAN_POINT('Ctrl Pts',(-1.94042451122363,0.46238916426216,31.2511596319364));
#20965=CARTESIAN_POINT('Ctrl Pts',(-1.93929603746011,0.467099455574493,
31.2508524184245));
#20966=CARTESIAN_POINT('Ctrl Pts',(-1.93688937859238,0.476985873508292,
31.2502058714525));
#20967=CARTESIAN_POINT('Ctrl Pts',(-1.93560757595444,0.48216107207886,31.2498664234468));
#20968=CARTESIAN_POINT('Ctrl Pts',(-1.93218260267122,0.495755410904218,
31.2489720813532));
#20969=CARTESIAN_POINT('Ctrl Pts',(-1.9300051697685,0.504165724948014,31.2484160839992));
#20970=CARTESIAN_POINT('Ctrl Pts',(-1.91994968956288,0.541984961347442,
31.2459034973414));
#20971=CARTESIAN_POINT('Ctrl Pts',(-1.9114542615777,0.571224075328402,31.2439270019532));
#20972=CARTESIAN_POINT('Ctrl Pts',(-1.88698276339085,0.648777597626214,
31.2385900023989));
#20973=CARTESIAN_POINT('Ctrl Pts',(-1.86982248342857,0.69669179870545,31.2351926199528));
#20974=CARTESIAN_POINT('Ctrl Pts',(-1.81338337256306,0.837115439473,31.2249386276497));
#20975=CARTESIAN_POINT('Ctrl Pts',(-1.76892972803691,0.927364986613652,
31.217944942651));
#20976=CARTESIAN_POINT('Ctrl Pts',(-1.65588155766603,1.11890984876398,31.2024266984386));
#20977=CARTESIAN_POINT('Ctrl Pts',(-1.58437974691568,1.21805219834673,31.1939240981901));
#20978=CARTESIAN_POINT('Ctrl Pts',(-1.49928348244099,1.31576366149377,31.1854643857727));
#20979=CARTESIAN_POINT('Ctrl Pts',(-1.49427467463566,1.32144927062638,31.1849718807926));
#20980=CARTESIAN_POINT('Ctrl Pts',(-1.48690172279494,1.32972294602694,31.1842549959714));
#20981=CARTESIAN_POINT('Ctrl Pts',(-1.48456303651856,1.33233345582291,31.1840287760579));
#20982=CARTESIAN_POINT('Ctrl Pts',(-1.48040331528074,1.33695210651232,31.1836285070402));
#20983=CARTESIAN_POINT('Ctrl Pts',(-1.47858505458397,1.33896271333984,31.1834542515238));
#20984=CARTESIAN_POINT('Ctrl Pts',(-1.47473392016223,1.34320383212994,31.1830866693572));
#20985=CARTESIAN_POINT('Ctrl Pts',(-1.47270008725653,1.34543343321652,31.1828934178857));
#20986=CARTESIAN_POINT('Ctrl Pts',(-1.46723944392326,1.3513924774604,31.1823768619727));
#20987=CARTESIAN_POINT('Ctrl Pts',(-1.46380344807836,1.35511353055324,31.1820542483759));
#20988=CARTESIAN_POINT('Ctrl Pts',(-1.44729278073818,1.37285788253193,31.1805153151586));
#20989=CARTESIAN_POINT('Ctrl Pts',(-1.43403001288442,1.38670586166615,31.1793127854054));
#20990=CARTESIAN_POINT('Ctrl Pts',(-1.39649113896128,1.42478644227771,31.1759942359655));
#20991=CARTESIAN_POINT('Ctrl Pts',(-1.37178577288711,1.44858827409231,31.1739063592736));
#20992=CARTESIAN_POINT('Ctrl Pts',(-1.27943566401587,1.53307814529466,31.1663891734738));
#20993=CARTESIAN_POINT('Ctrl Pts',(-1.20827658467783,1.58976544085981,31.1611328268029));
#20994=CARTESIAN_POINT('Ctrl Pts',(-1.00427663326607,1.73064046305574,31.1467547390443));
#20995=CARTESIAN_POINT('Ctrl Pts',(-0.864994056850914,1.80429041889654,
31.1376118454133));
#20996=CARTESIAN_POINT('Ctrl Pts',(-0.706829202964467,1.86536250699166,
31.1270239583355));
#20997=CARTESIAN_POINT('Ctrl Pts',(-0.695089231941632,1.86976890359345,
31.1262372926929));
#20998=CARTESIAN_POINT('Ctrl Pts',(-0.677527660102893,1.87617208587096,
31.125059083945));
#20999=CARTESIAN_POINT('Ctrl Pts',(-0.671736945297046,1.87825315145487,
31.124670350614));
#21000=CARTESIAN_POINT('Ctrl Pts',(-0.661380479736466,1.88192103633594,
31.1239746613554));
#21001=CARTESIAN_POINT('Ctrl Pts',(-0.65681839603707,1.88351812307009,31.1236680492174));
#21002=CARTESIAN_POINT('Ctrl Pts',(-0.647169566926578,1.88685665105511,
31.1230192112892));
#21003=CARTESIAN_POINT('Ctrl Pts',(-0.642081502978429,1.88859413654348,
31.1226768573425));
#21004=CARTESIAN_POINT('Ctrl Pts',(-0.628562317584801,1.89314975662326,
31.1217666312155));
#21005=CARTESIAN_POINT('Ctrl Pts',(-0.620119350879211,1.89593211231607,
31.1211975837239));
#21006=CARTESIAN_POINT('Ctrl Pts',(-0.580702160949729,1.90863047499537,
31.118537907081));
#21007=CARTESIAN_POINT('Ctrl Pts',(-0.549508511316975,1.91784396608568,
31.1164244034177));
#21008=CARTESIAN_POINT('Ctrl Pts',(-0.464265799246307,1.9407712876464,31.1106214276322));
#21009=CARTESIAN_POINT('Ctrl Pts',(-0.409847701835213,1.95298741129955,
31.1068866598826));
#21010=CARTESIAN_POINT('Ctrl Pts',(-0.252367685644169,1.98146779719222,
31.0960014792073));
#21011=CARTESIAN_POINT('Ctrl Pts',(-0.148451425910998,1.99194955617663,
31.0887165774201));
#21012=CARTESIAN_POINT('Ctrl Pts',(0.032268284277143,1.99595513123105,31.0761123235167));
#21013=CARTESIAN_POINT('Ctrl Pts',(0.108778141130885,1.99325037343932,31.0707999761076));
#21014=CARTESIAN_POINT('Ctrl Pts',(0.220692408511845,1.98282907905133,31.0632120929522));
#21015=CARTESIAN_POINT('Ctrl Pts',(0.256343178529391,1.97853604150312,31.0608229424961));
#21016=CARTESIAN_POINT('Ctrl Pts',(0.297688003581043,1.97242087520728,31.0580994640606));
#21017=CARTESIAN_POINT('Ctrl Pts',(0.303511012869209,1.97153324182182,31.0577169879956));
#21018=CARTESIAN_POINT('Ctrl Pts',(0.312811317087408,1.97007336409897,31.0571079603871));
#21019=CARTESIAN_POINT('Ctrl Pts',(0.31629112000322,1.9695176840805,31.056880501021));
#21020=CARTESIAN_POINT('Ctrl Pts',(0.322447836978754,1.96851779718032,31.056478819528));
#21021=CARTESIAN_POINT('Ctrl Pts',(0.325125337342351,1.96807734623456,31.0563043859038));
#21022=CARTESIAN_POINT('Ctrl Pts',(0.330768766717762,1.96713716644237,31.0559372710552));
#21023=CARTESIAN_POINT('Ctrl Pts',(0.333734459130286,1.9666361940424,31.0557446617724));
#21024=CARTESIAN_POINT('Ctrl Pts',(0.341646190442853,1.96528131197251,31.0552316393335));
#21025=CARTESIAN_POINT('Ctrl Pts',(0.346590199238606,1.9644154320669,31.0549119006035));
#21026=CARTESIAN_POINT('Ctrl Pts',(0.369915499791155,1.96023950331184,31.0534071835543));
#21027=CARTESIAN_POINT('Ctrl Pts',(0.388253722277744,1.95668993340963,31.052235263747));
#21028=CARTESIAN_POINT('Ctrl Pts',(0.574894127910444,1.91783618901617,31.040396187309));
#21029=CARTESIAN_POINT('Ctrl Pts',(0.738034696196257,1.86116153261909,31.030735067415));
#21030=CARTESIAN_POINT('Ctrl Pts',(0.990544070261842,1.73493869467138,31.0142218044359));
#21031=CARTESIAN_POINT('Ctrl Pts',(1.0849157119771,1.67754062608221,31.0076452878914));
#21032=CARTESIAN_POINT('Ctrl Pts',(1.18449948506942,1.6050406427909,30.9999563093416));
#21033=CARTESIAN_POINT('Ctrl Pts',(1.19487045530749,1.59733499231193,30.9991460128382));
#21034=CARTESIAN_POINT('Ctrl Pts',(1.21012883259697,1.58576623898341,30.9979392738313));
#21035=CARTESIAN_POINT('Ctrl Pts',(1.21507432037646,1.58198000958115,30.9975458469874));
#21036=CARTESIAN_POINT('Ctrl Pts',(1.22383322617909,1.57520895366687,30.9968449037336));
#21037=CARTESIAN_POINT('Ctrl Pts',(1.22765367697921,1.57223327211136,30.9965377509617));
#21038=CARTESIAN_POINT('Ctrl Pts',(1.2356607821859,1.56594970033123,30.995890998397));
#21039=CARTESIAN_POINT('Ctrl Pts',(1.23984506976345,1.56263886892361,30.9955512827896));
#21040=CARTESIAN_POINT('Ctrl Pts',(1.25082172300252,1.55388171311349,30.9946554779236));
#21041=CARTESIAN_POINT('Ctrl Pts',(1.25759174484254,1.54840768546309,30.9940982788395));
#21042=CARTESIAN_POINT('Ctrl Pts',(1.28801830622811,1.52347454594009,30.9915725084775));
#21043=CARTESIAN_POINT('Ctrl Pts',(1.31125946526838,1.50351730634742,30.9895837740622));
#21044=CARTESIAN_POINT('Ctrl Pts',(1.37217644151777,1.44872076027496,30.9842056921162));
#21045=CARTESIAN_POINT('Ctrl Pts',(1.408980924493,1.41295152995392,30.9807787636526));
#21046=CARTESIAN_POINT('Ctrl Pts',(1.51389366465317,1.30281091363879,30.9704690127331));
#21047=CARTESIAN_POINT('Ctrl Pts',(1.5777848604126,1.22465584098359,30.9634492639706));
#21048=CARTESIAN_POINT('Ctrl Pts',(1.68418416071839,1.07228040907223,30.9504827827202));
#21049=CARTESIAN_POINT('Ctrl Pts',(1.72837114410311,0.999498183239119,30.9445554114429));
#21050=CARTESIAN_POINT('Ctrl Pts',(1.78509501797916,0.890988459725063,30.9362791772635));
#21051=CARTESIAN_POINT('Ctrl Pts',(1.80147806444191,0.857380828877979,30.9337891843463));
#21052=CARTESIAN_POINT('Ctrl Pts',(1.81936909496831,0.817899265772309,30.930964167749));
#21053=CARTESIAN_POINT('Ctrl Pts',(1.82180574160099,0.812457355640775,30.9305769553645));
#21054=CARTESIAN_POINT('Ctrl Pts',(1.82565217337184,0.803762571578491,30.9299618398451));
#21055=CARTESIAN_POINT('Ctrl Pts',(1.82707772717558,0.800516776178691,30.9297330005675));
#21056=CARTESIAN_POINT('Ctrl Pts',(1.82958038317483,0.794777052715037,30.9293297395611));
#21057=CARTESIAN_POINT('Ctrl Pts',(1.83066105254867,0.792284704548647,30.9291551006747));
#21058=CARTESIAN_POINT('Ctrl Pts',(1.83292316594254,0.78703825245408,30.9287884733284));
#21059=CARTESIAN_POINT('Ctrl Pts',(1.83410349336,0.784283698039193,30.9285965532947));
#21060=CARTESIAN_POINT('Ctrl Pts',(1.83722494496853,0.776953517322683,30.9280873220005));
#21061=CARTESIAN_POINT('Ctrl Pts',(1.83915519845539,0.772373241231321,30.9277706677287));
#21062=CARTESIAN_POINT('Ctrl Pts',(1.84805774962005,0.751025872773029,30.9263017705579));
#21063=CARTESIAN_POINT('Ctrl Pts',(1.85481827948457,0.73417062994929,30.9251618433078));
#21064=CARTESIAN_POINT('Ctrl Pts',(1.91739337045346,0.57177519373274,30.9143467231604));
#21065=CARTESIAN_POINT('Ctrl Pts',(1.95620574354421,0.420235728504764,30.9055066279835));
#21066=CARTESIAN_POINT('Ctrl Pts',(1.99386810558418,0.140008305319292,30.8890469952164));
#21067=CARTESIAN_POINT('Ctrl Pts',(1.9987336623906,0.0130076470548837,30.8815461973256));
#21068=CARTESIAN_POINT('Ctrl Pts',(1.99077283241317,-0.126571232251853,
30.8728202581421));
#21069=CARTESIAN_POINT('Ctrl Pts',(1.9899051972352,-0.139549419073874,30.8720045704407));
#21070=CARTESIAN_POINT('Ctrl Pts',(1.98843319239388,-0.158745101669556,
30.8707913317783));
#21071=CARTESIAN_POINT('Ctrl Pts',(1.98792643058039,-0.164969915671555,
30.8703968444273));
#21072=CARTESIAN_POINT('Ctrl Pts',(1.98697466582404,-0.176019065659548,
30.8696947062967));
#21073=CARTESIAN_POINT('Ctrl Pts',(1.98654130222136,-0.180844375064161,
30.8693874236488));
#21074=CARTESIAN_POINT('Ctrl Pts',(1.98559454126165,-0.190971874618354,
30.8687411047432));
#21075=CARTESIAN_POINT('Ctrl Pts',(1.98507747519386,-0.196273675651231,
30.8684019553599));
#21076=CARTESIAN_POINT('Ctrl Pts',(1.98366337838926,-0.210195809776485,
30.8675092456928));
#21077=CARTESIAN_POINT('Ctrl Pts',(1.98273140001984,-0.218812405163402,
30.8669545894451));
#21078=CARTESIAN_POINT('Ctrl Pts',(1.97829564619371,-0.257465237872614,
30.8644566319803));
#21079=CARTESIAN_POINT('Ctrl Pts',(1.97416543968721,-0.287424185108046,
30.8624937078472));
#21080=CARTESIAN_POINT('Ctrl Pts',(1.9613384907093,-0.367041932504719,30.8572021400294));
#21081=CARTESIAN_POINT('Ctrl Pts',(1.95143808899274,-0.416481837387152,
30.8538373863261));
#21082=CARTESIAN_POINT('Ctrl Pts',(1.91632034008428,-0.562815839647878,
30.8436451402717));
#21083=CARTESIAN_POINT('Ctrl Pts',(1.88567379545211,-0.658237294143165,
30.836680429423));
#21084=CARTESIAN_POINT('Ctrl Pts',(1.80165789901835,-0.864991354912337,
30.8211092979026));
#21085=CARTESIAN_POINT('Ctrl Pts',(1.74485211177816,-0.9745151567217,30.8125231318297));
#21086=CARTESIAN_POINT('Ctrl Pts',(1.6742202599273,-1.08446814209581,30.8039911124005));
#21087=CARTESIAN_POINT('Ctrl Pts',(1.67010119751613,-1.09080090963307,30.8035000978645));
#21088=CARTESIAN_POINT('Ctrl Pts',(1.6640208755196,-1.10003379141174,30.8027849704285));
#21089=CARTESIAN_POINT('Ctrl Pts',(1.66208786158366,-1.10295229146523,30.802559030048));
#21090=CARTESIAN_POINT('Ctrl Pts',(1.65864463900939,-1.10812132427727,30.8021590787325));
#21091=CARTESIAN_POINT('Ctrl Pts',(1.65713751623782,-1.1103738831854,30.8019848625321));
#21092=CARTESIAN_POINT('Ctrl Pts',(1.65394118904495,-1.11513013915709,30.8016171709741));
#21093=CARTESIAN_POINT('Ctrl Pts',(1.65225089273359,-1.1176330667237,30.8014237715359));
#21094=CARTESIAN_POINT('Ctrl Pts',(1.64770496279773,-1.12433165746063,30.8009064012472));
#21095=CARTESIAN_POINT('Ctrl Pts',(1.64483896661605,-1.12852031247112,30.8005831250485));
#21096=CARTESIAN_POINT('Ctrl Pts',(1.63100394090725,-1.1485755400944,30.7990361888016));
#21097=CARTESIAN_POINT('Ctrl Pts',(1.61982068588802,-1.16429405182188,30.7978264927564));
#21098=CARTESIAN_POINT('Ctrl Pts',(1.58795084166033,-1.20774013418534,30.7944830396632));
#21099=CARTESIAN_POINT('Ctrl Pts',(1.56676767591454,-1.23509653497835,30.7923779404633));
#21100=CARTESIAN_POINT('Ctrl Pts',(1.48682514277101,-1.33296706467308,30.7847911657475));
#21101=CARTESIAN_POINT('Ctrl Pts',(1.42392781617646,-1.39995787477465,30.77948505607));
#21102=CARTESIAN_POINT('Ctrl Pts',(1.24254851037312,-1.56822154143298,30.7651359416259));
#21103=CARTESIAN_POINT('Ctrl Pts',(1.11648618569916,-1.66032976765912,30.7560686331889));
#21104=CARTESIAN_POINT('Ctrl Pts',(0.970052269822594,-1.7430388865462,30.7455667809738));
#21105=CARTESIAN_POINT('Ctrl Pts',(0.959035509866836,-1.74912459403028,
30.7447772446136));
#21106=CARTESIAN_POINT('Ctrl Pts',(0.942539923947373,-1.75803413816186,
30.7435955664146));
#21107=CARTESIAN_POINT('Ctrl Pts',(0.937104260467197,-1.76093757493176,
30.7432062589891));
#21108=CARTESIAN_POINT('Ctrl Pts',(0.927493176188584,-1.76601419214855,
30.7425180091939));
#21109=CARTESIAN_POINT('Ctrl Pts',(0.923323334104867,-1.76819787886469,
30.7422194415545));
#21110=CARTESIAN_POINT('Ctrl Pts',(0.914513090343158,-1.77277201511575,
30.7415886675316));
#21111=CARTESIAN_POINT('Ctrl Pts',(0.909870963007115,-1.77515904634179,
30.7412563434684));
#21112=CARTESIAN_POINT('Ctrl Pts',(0.900362678696656,-1.78000121243852,
30.7405756982464));
#21113=CARTESIAN_POINT('Ctrl Pts',(0.895495724887295,-1.78245467690037,
30.7402273218416));
#21114=CARTESIAN_POINT('Ctrl Pts',(0.883475391576953,-1.78845255136964,
30.7393669311408));
#21115=CARTESIAN_POINT('Ctrl Pts',(0.876310720792331,-1.79197399913212,
30.7388541197062));
#21116=CARTESIAN_POINT('Ctrl Pts',(0.856413061815055,-1.80160586549991,
30.737429912066));
#21117=CARTESIAN_POINT('Ctrl Pts',(0.843636220407204,-1.80762411402532,
30.73651534913));
#21118=CARTESIAN_POINT('Ctrl Pts',(0.727691293483214,-1.86074038350987,
30.7282144376432));
#21119=CARTESIAN_POINT('Ctrl Pts',(0.620763014543473,-1.89908792487588,
30.7205294409812));
#21120=CARTESIAN_POINT('Ctrl Pts',(0.378262314537477,-1.96337770096241,
30.7031559857211));
#21121=CARTESIAN_POINT('Ctrl Pts',(0.24206481084392,-1.98477715771986,30.6934277198737));
#21122=CARTESIAN_POINT('Ctrl Pts',(0.0689977362471238,-1.99387774352911,
30.6817290272623));
#21123=CARTESIAN_POINT('Ctrl Pts',(0.0332009877801101,-1.99479503505999,
30.6793466729204));
#21124=CARTESIAN_POINT('Ctrl Pts',(-0.00848886137459782,-1.99474061907471,
30.6766300481064));
#21125=CARTESIAN_POINT('Ctrl Pts',(-0.0143740897827916,-1.99470689220335,
30.6762478964795));
#21126=CARTESIAN_POINT('Ctrl Pts',(-0.0237813886347323,-1.99461134443465,
30.6756392861305));
#21127=CARTESIAN_POINT('Ctrl Pts',(-0.0273035380444403,-1.99456624033171,
30.6754119215116));
#21128=CARTESIAN_POINT('Ctrl Pts',(-0.0335385166585083,-1.99446987747866,
30.6750103482055));
#21129=CARTESIAN_POINT('Ctrl Pts',(-0.0362513810617108,-1.99442241313016,
30.6748359284097));
#21130=CARTESIAN_POINT('Ctrl Pts',(-0.0419720574307192,-1.99431064772598,
30.6744687788403));
#21131=CARTESIAN_POINT('Ctrl Pts',(-0.044979815531504,-1.99424507764888,
30.6742761212528));
#21132=CARTESIAN_POINT('Ctrl Pts',(-0.0530085863773872,-1.99405187465097,
30.6737628330784));
#21133=CARTESIAN_POINT('Ctrl Pts',(-0.0580293260474644,-1.99391208122831,
30.6734428781467));
#21134=CARTESIAN_POINT('Ctrl Pts',(-0.0817539013258678,-1.99316182603325,
30.6719356161514));
#21135=CARTESIAN_POINT('Ctrl Pts',(-0.100449825557757,-1.99230711966565,
30.6707614212645));
#21136=CARTESIAN_POINT('Ctrl Pts',(-0.290777119355789,-1.98091994285634,
30.6589213061435));
#21137=CARTESIAN_POINT('Ctrl Pts',(-0.460399861992667,-1.94849830957342,
30.6492608441593));
#21138=CARTESIAN_POINT('Ctrl Pts',(-0.728479717704918,-1.86024060531193,
30.632751225846));
#21139=CARTESIAN_POINT('Ctrl Pts',(-0.830127548660997,-1.81715736612486,
30.6261778860915));
#21140=CARTESIAN_POINT('Ctrl Pts',(-0.939139613169537,-1.75988966870218,
30.6184915545002));
#21141=CARTESIAN_POINT('Ctrl Pts',(-0.95053105845854,-1.75376325465686,
30.6176803843634));
#21142=CARTESIAN_POINT('Ctrl Pts',(-0.9673208429311,-1.74452193375066,30.6164725918652));
#21143=CARTESIAN_POINT('Ctrl Pts',(-0.972765617208123,-1.74149172925181,
30.6160789929091));
#21144=CARTESIAN_POINT('Ctrl Pts',(-0.982303783523599,-1.73612472340922,
30.6153860594975));
#21145=CARTESIAN_POINT('Ctrl Pts',(-0.986403278291313,-1.73379882059854,
30.6150871184092));
#21146=CARTESIAN_POINT('Ctrl Pts',(-0.99499212705771,-1.72888550185399,
30.6144584342802));
#21147=CARTESIAN_POINT('Ctrl Pts',(-0.999479713997759,-1.72629508251038,
30.614128584336));
#21148=CARTESIAN_POINT('Ctrl Pts',(-1.00862206488894,-1.72097014411957,
30.6134537725302));
#21149=CARTESIAN_POINT('Ctrl Pts',(-1.01327591955092,-1.71823415652256,
30.6131087592285));
#21150=CARTESIAN_POINT('Ctrl Pts',(-1.024676310235,-1.71146947612557,30.6122598599228));
#21151=CARTESIAN_POINT('Ctrl Pts',(-1.03141021294671,-1.70741977209982,
30.6117552101457));
#21152=CARTESIAN_POINT('Ctrl Pts',(-1.04991210181841,-1.69614352220084,
30.6103596302375));
#21153=CARTESIAN_POINT('Ctrl Pts',(-1.06162906584482,-1.68883450345156,
30.6094656904831));
#21154=CARTESIAN_POINT('Ctrl Pts',(-1.09871067489991,-1.66516468560231,
30.6066036430285));
#21155=CARTESIAN_POINT('Ctrl Pts',(-1.12377931177294,-1.648350227588,30.6046190089808));
#21156=CARTESIAN_POINT('Ctrl Pts',(-1.22435195382162,-1.57753167824948,
30.5964487928782));
#21157=CARTESIAN_POINT('Ctrl Pts',(-1.29641617636026,-1.51886314082391,
30.5900965347656));
#21158=CARTESIAN_POINT('Ctrl Pts',(-1.47601651483654,-1.35052590813613,
30.5730074456338));
#21159=CARTESIAN_POINT('Ctrl Pts',(-1.57544416212508,-1.23309622233248,
30.5621420012456));
#21160=CARTESIAN_POINT('Ctrl Pts',(-1.66832844720924,-1.09357691558635,
30.5510836096127));
#21161=CARTESIAN_POINT('Ctrl Pts',(-1.67609176887542,-1.08164073916261,
30.5501513403544));
#21162=CARTESIAN_POINT('Ctrl Pts',(-1.68625943840324,-1.06563547965153,
30.5489205786209));
#21163=CARTESIAN_POINT('Ctrl Pts',(-1.68877785640327,-1.06163987393523,
30.5486149127207));
#21164=CARTESIAN_POINT('Ctrl Pts',(-1.69268628263736,-1.05538984500868,
30.5481392979288));
#21165=CARTESIAN_POINT('Ctrl Pts',(-1.69408601153855,-1.05314156792276,
30.5479687141645));
#21166=CARTESIAN_POINT('Ctrl Pts',(-1.69676457817262,-1.04882003339374,
30.5476418056303));
#21167=CARTESIAN_POINT('Ctrl Pts',(-1.6980440809281,-1.04674724527474,30.5474854392649));
#21168=CARTESIAN_POINT('Ctrl Pts',(-1.70109479113365,-1.04178479595711,
30.547112109566));
#21169=CARTESIAN_POINT('Ctrl Pts',(-1.70286243200226,-1.0388929625332,30.5468953825897));
#21170=CARTESIAN_POINT('Ctrl Pts',(-1.70815290045356,-1.03018805697164,
30.546245439563));
#21171=CARTESIAN_POINT('Ctrl Pts',(-1.71165344012901,-1.02436139529044,
30.5458136600655));
#21172=CARTESIAN_POINT('Ctrl Pts',(-1.74429482901721,-0.969395161345221,
30.5417699113467));
#21173=CARTESIAN_POINT('Ctrl Pts',(-1.77134493247479,-0.919037520493393,
30.5382857105938));
#21174=CARTESIAN_POINT('Ctrl Pts',(-1.89070397722454,-0.67192278166108,
30.5218885323362));
#21175=CARTESIAN_POINT('Ctrl Pts',(-1.9526085886087,-0.462140684089348,
30.5098589377122));
#21176=CARTESIAN_POINT('Ctrl Pts',(-1.98309007347306,-0.217355163286339,
30.4947211034775));
#21177=CARTESIAN_POINT('Ctrl Pts',(-1.9860741285533,-0.188146013438282,
30.492901088329));
#21178=CARTESIAN_POINT('Ctrl Pts',(-1.98916000561039,-0.149526372181063,
30.4904724526059));
#21179=CARTESIAN_POINT('Ctrl Pts',(-1.98984156439777,-0.140164930181504,
30.4898820354191));
#21180=CARTESIAN_POINT('Ctrl Pts',(-1.99082037799331,-0.12526967788181,
30.488939749249));
#21181=CARTESIAN_POINT('Ctrl Pts',(-1.99116069125404,-0.119738758240396,
30.4885892329797));
#21182=CARTESIAN_POINT('Ctrl Pts',(-1.9917525402028,-0.109418384663465,
30.4879339941431));
#21183=CARTESIAN_POINT('Ctrl Pts',(-1.99200985814323,-0.104629291822345,
30.4876294553304));
#21184=CARTESIAN_POINT('Ctrl Pts',(-1.99248084347473,-0.095230988806741,
30.4870308563351));
#21185=CARTESIAN_POINT('Ctrl Pts',(-1.99269579434065,-0.0906218708114643,
30.4867368384174));
#21186=CARTESIAN_POINT('Ctrl Pts',(-1.99314311831427,-0.0802574011244163,
30.4860746484356));
#21187=CARTESIAN_POINT('Ctrl Pts',(-1.99336655748497,-0.0745017239083139,
30.4857061984316));
#21188=CARTESIAN_POINT('Ctrl Pts',(-1.9939167460376,-0.0585466240891084,
30.4846828054902));
#21189=CARTESIAN_POINT('Ctrl Pts',(-1.99419015864603,-0.0483456517303464,
30.4840261989168));
#21190=CARTESIAN_POINT('Ctrl Pts',(-1.99463292928769,-0.0251945900154945,
30.482530679838));
#21191=CARTESIAN_POINT('Ctrl Pts',(-1.99475445956689,-0.0122441981611814,
30.4816903058683));
#21192=CARTESIAN_POINT('Ctrl Pts',(-1.99474987500568,0.00070616204988155,
30.4808460358741));
#21193=CARTESIAN_POINT('',(-1.99474947325114,-0.00144964281222297,28.8790451185423));
#21194=CARTESIAN_POINT('Ctrl Pts',(-1.99474987552217,0.000704701547650649,
30.4808461310883));
#21195=CARTESIAN_POINT('Ctrl Pts',(-1.99466568051133,0.239029688859807,
30.4653090678252));
#21196=CARTESIAN_POINT('Ctrl Pts',(-1.95186213000554,0.475413415424764,
30.4482388704665));
#21197=CARTESIAN_POINT('Ctrl Pts',(-1.85744162136749,0.727958154770136,
30.4298945696681));
#21198=CARTESIAN_POINT('Ctrl Pts',(-1.84575844615724,0.757092096227795,
30.4277820813544));
#21199=CARTESIAN_POINT('Ctrl Pts',(-1.82630218246401,0.802478468634954,
30.4245098135911));
#21200=CARTESIAN_POINT('Ctrl Pts',(-1.8189886130018,0.818921141463728,30.4233282834959));
#21201=CARTESIAN_POINT('Ctrl Pts',(-1.80937863218933,0.839762510989474,
30.4218378076276));
#21202=CARTESIAN_POINT('Ctrl Pts',(-1.80728725145465,0.844254050328181,
30.4215170209616));
#21203=CARTESIAN_POINT('Ctrl Pts',(-1.80390555593749,0.851446573282073,
30.4210040706918));
#21204=CARTESIAN_POINT('Ctrl Pts',(-1.8026258754975,0.854152489414659,30.4208112613892));
#21205=CARTESIAN_POINT('Ctrl Pts',(-1.80017273746489,0.859309643353357,
30.42044412703));
#21206=CARTESIAN_POINT('Ctrl Pts',(-1.79900037577071,0.861761333506452,
30.4202697405456));
#21207=CARTESIAN_POINT('Ctrl Pts',(-1.79628409260997,0.867412034805799,
30.4198681396871));
#21208=CARTESIAN_POINT('Ctrl Pts',(-1.79473663470469,0.870609322265508,
30.4196411476917));
#21209=CARTESIAN_POINT('Ctrl Pts',(-1.79055825375805,0.879184019487755,
30.4190329917603));
#21210=CARTESIAN_POINT('Ctrl Pts',(-1.78791162481773,0.884553799526985,
30.4186527849619));
#21211=CARTESIAN_POINT('Ctrl Pts',(-1.76834119322049,0.92381380110481,30.4158771060142));
#21212=CARTESIAN_POINT('Ctrl Pts',(-1.75047792899269,0.957230372849213,
30.4135371024245));
#21213=CARTESIAN_POINT('Ctrl Pts',(-1.68968699356754,1.06355075706345,30.4061000826566));
#21214=CARTESIAN_POINT('Ctrl Pts',(-1.64306980890241,1.13424263085786,30.4011655783765));
#21215=CARTESIAN_POINT('Ctrl Pts',(-1.49632628831981,1.32864867189428,30.3870218590609));
#21216=CARTESIAN_POINT('Ctrl Pts',(-1.38574046017786,1.44361234050747,30.3778726511871));
#21217=CARTESIAN_POINT('Ctrl Pts',(-1.24979288024212,1.55477419618601,30.3670421843246));
#21218=CARTESIAN_POINT('Ctrl Pts',(-1.236766032734,1.56515647753784,30.3660087802714));
#21219=CARTESIAN_POINT('Ctrl Pts',(-1.21651986280806,1.58088190739906,30.3644084793133));
#21220=CARTESIAN_POINT('Ctrl Pts',(-1.20939173367485,1.58634164418815,30.3638461432804));
#21221=CARTESIAN_POINT('Ctrl Pts',(-1.19754619333474,1.59528840247737,30.3629133082341));
#21222=CARTESIAN_POINT('Ctrl Pts',(-1.19284977722775,1.59880310858834,30.3625438915353));
#21223=CARTESIAN_POINT('Ctrl Pts',(-1.18370561852511,1.60558370045337,30.3618254027196));
#21224=CARTESIAN_POINT('Ctrl Pts',(-1.17925968858737,1.60885194979654,30.3614764266885));
#21225=CARTESIAN_POINT('Ctrl Pts',(-1.17477665416828,1.61211890882029,30.3611248798015));
#21226=CARTESIAN_POINT('Ctrl Pts',(-1.17475301654721,1.61213613366491,30.3611230262156));
#21227=CARTESIAN_POINT('Ctrl Pts',(-1.17470501832466,1.61217110857708,30.3611192623693));
#21228=CARTESIAN_POINT('Ctrl Pts',(-1.17468065827152,1.6121888581958,30.3611173521525));
#21229=CARTESIAN_POINT('Ctrl Pts',(-1.17463118657791,1.6122249033504,30.3611134728031));
#21230=CARTESIAN_POINT('Ctrl Pts',(-1.17460607548248,1.61224319843639,30.3611115037137));
#21231=CARTESIAN_POINT('Ctrl Pts',(-1.17455507163147,1.61228035627505,30.3611075042629));
#21232=CARTESIAN_POINT('Ctrl Pts',(-1.1745291793961,1.61229921859214,30.3611054739429));
#21233=CARTESIAN_POINT('Ctrl Pts',(-1.17447658165263,1.61233753375047,30.3611013495539));
#21234=CARTESIAN_POINT('Ctrl Pts',(-1.17444987661594,1.61235698618758,30.3610992555226));
#21235=CARTESIAN_POINT('Ctrl Pts',(-1.17439561991206,1.6123965056997,30.3610950010975));
#21236=CARTESIAN_POINT('Ctrl Pts',(-1.17436806870536,1.61241657237407,30.3610928407406));
#21237=CARTESIAN_POINT('Ctrl Pts',(-1.17431208451571,1.61245734576052,30.3610884509108));
#21238=CARTESIAN_POINT('Ctrl Pts',(-1.17428365196805,1.61247805208547,30.3610862214729));
#21239=CARTESIAN_POINT('Ctrl Pts',(-1.1742258680442,1.61252013154369,30.3610816905783));
#21240=CARTESIAN_POINT('Ctrl Pts',(-1.17419651706862,1.61254150430984,30.3610793891539));
#21241=CARTESIAN_POINT('Ctrl Pts',(-1.17413685713103,1.6125849449352,30.3610747112187));
#21242=CARTESIAN_POINT('Ctrl Pts',(-1.17410654855901,1.61260701242928,30.3610723347395));
#21243=CARTESIAN_POINT('Ctrl Pts',(-1.17404493213218,1.61265187233141,30.3610675034594));
#21244=CARTESIAN_POINT('Ctrl Pts',(-1.17401362461838,1.61267466440375,30.3610650486865));
#21245=CARTESIAN_POINT('Ctrl Pts',(-1.1739499665713,1.61272100503713,30.3610600573928));
#21246=CARTESIAN_POINT('Ctrl Pts',(-1.17391761637694,1.61274455325718,30.3610575208998));
#21247=CARTESIAN_POINT('Ctrl Pts',(-1.17385182676162,1.61279243953418,30.3610523625466));
#21248=CARTESIAN_POINT('Ctrl Pts',(-1.1738183876307,1.61281677727829,30.3610497407103));
#21249=CARTESIAN_POINT('Ctrl Pts',(-1.17375037124547,1.6128662778822,30.3610444078403));
#21250=CARTESIAN_POINT('Ctrl Pts',(-1.17371579423155,1.61289144045715,30.3610416968268));
#21251=CARTESIAN_POINT('Ctrl Pts',(-1.17364545012493,1.61294262819773,30.3610361815328));
#21252=CARTESIAN_POINT('Ctrl Pts',(-1.17360968330331,1.61296865304726,30.361033377275));
#21253=CARTESIAN_POINT('Ctrl Pts',(-1.17353690462833,1.61302160496073,30.3610276711881));
#21254=CARTESIAN_POINT('Ctrl Pts',(-1.1734998929798,1.613048531747,30.3610247693767));
#21255=CARTESIAN_POINT('Ctrl Pts',(-1.17342456627785,1.61310332961044,30.3610188636106));
#21256=CARTESIAN_POINT('Ctrl Pts',(-1.17338625139744,1.61313120042238,30.3610158596712));
#21257=CARTESIAN_POINT('Ctrl Pts',(-1.17330825620532,1.61318793103211,30.3610097447912));
#21258=CARTESIAN_POINT('Ctrl Pts',(-1.17326857604437,1.61321679056911,30.3610066338643));
#21259=CARTESIAN_POINT('Ctrl Pts',(-1.17318778435371,1.61327554612565,30.3610002998454));
#21260=CARTESIAN_POINT('Ctrl Pts',(-1.17314667294667,1.61330544189189,30.3609970767649));
#21261=CARTESIAN_POINT('Ctrl Pts',(-1.17306294856002,1.61336632045898,30.3609905129408));
#21262=CARTESIAN_POINT('Ctrl Pts',(-1.17302033568964,1.61339730300204,30.3609871722079));
#21263=CARTESIAN_POINT('Ctrl Pts',(-1.17293353364606,1.61346040891404,30.3609803672267));
#21264=CARTESIAN_POINT('Ctrl Pts',(-1.17288934453556,1.61349253204329,30.3609769029857));
#21265=CARTESIAN_POINT('Ctrl Pts',(-1.17279931030378,1.61355797648023,30.3609698447465));
#21266=CARTESIAN_POINT('Ctrl Pts',(-1.17275346521908,1.61359129754987,30.3609662507537));
#21267=CARTESIAN_POINT('Ctrl Pts',(-1.17266003397574,1.61365919904923,30.3609589263502));
#21268=CARTESIAN_POINT('Ctrl Pts',(-1.17261244783259,1.61369377923703,30.3609551959434));
#21269=CARTESIAN_POINT('Ctrl Pts',(-1.17251914935189,1.61376157163806,30.3609478820975));
#21270=CARTESIAN_POINT('Ctrl Pts',(-1.17247343729051,1.61379478389938,30.360944298677));
#21271=CARTESIAN_POINT('Ctrl Pts',(-1.16859673567131,1.61661116363172,30.3606404026141));
#21272=CARTESIAN_POINT('Ctrl Pts',(-1.16475587701931,1.61938066288131,30.3603395636112));
#21273=CARTESIAN_POINT('Ctrl Pts',(-1.15583163972442,1.6257674213605,30.3596411150445));
#21274=CARTESIAN_POINT('Ctrl Pts',(-1.15074110011931,1.62937454465798,30.359243119517));
#21275=CARTESIAN_POINT('Ctrl Pts',(-1.13501272429323,1.64040909782194,30.3580146282341));
#21276=CARTESIAN_POINT('Ctrl Pts',(-1.12431944900311,1.64775655237485,30.3571810976589));
#21277=CARTESIAN_POINT('Ctrl Pts',(-1.01789323044253,1.7193647499095,30.34890045313));
#21278=CARTESIAN_POINT('Ctrl Pts',(-0.91684810955211,1.77530359854768,30.341139356087));
#21279=CARTESIAN_POINT('Ctrl Pts',(-0.66521501300496,1.88737377633127,30.3221230288653));
#21280=CARTESIAN_POINT('Ctrl Pts',(-0.511559342251409,1.93468320884565,
30.3107290315539));
#21281=CARTESIAN_POINT('Ctrl Pts',(-0.329817526449159,1.96744675655863,
30.2984025546668));
#21282=CARTESIAN_POINT('Ctrl Pts',(-0.305656538455194,1.97134485983718,
30.2967878261163));
#21283=CARTESIAN_POINT('Ctrl Pts',(-0.275996518025113,1.97557171257568,
30.2948397746447));
#21284=CARTESIAN_POINT('Ctrl Pts',(-0.270561168326607,1.9763234364378,30.2944841850787));
#21285=CARTESIAN_POINT('Ctrl Pts',(-0.2620387437074,1.97746629330736,30.2939289010564));
#21286=CARTESIAN_POINT('Ctrl Pts',(-0.258953789495453,1.97787263988403,
30.293728363844));
#21287=CARTESIAN_POINT('Ctrl Pts',(-0.253196166089922,1.97861732565822,
30.2933549732022));
#21288=CARTESIAN_POINT('Ctrl Pts',(-0.25052379089714,1.97895746549567,30.2931820222134));
#21289=CARTESIAN_POINT('Ctrl Pts',(-0.244466599660409,1.97971595835107,
30.2927908129422));
#21290=CARTESIAN_POINT('Ctrl Pts',(-0.241081403439257,1.98013104400671,
30.2925727411421));
#21291=CARTESIAN_POINT('Ctrl Pts',(-0.231062947396517,1.98133341369536,
30.2919289842313));
#21292=CARTESIAN_POINT('Ctrl Pts',(-0.224426696722137,1.98209607303317,
30.291504663611));
#21293=CARTESIAN_POINT('Ctrl Pts',(-0.1777111085203,1.98722715034128,30.288531692265));
#21294=CARTESIAN_POINT('Ctrl Pts',(-0.137507988255322,1.99041329263624,
30.2860456553246));
#21295=CARTESIAN_POINT('Ctrl Pts',(-0.0563548842666095,1.99437375319577,
30.2811235913442));
#21296=CARTESIAN_POINT('Ctrl Pts',(-0.0154231428127811,1.99511027609926,
30.2786900443058));
#21297=CARTESIAN_POINT('Ctrl Pts',(0.0696939432603636,1.99402190705517,
30.2736801147433));
#21298=CARTESIAN_POINT('Ctrl Pts',(0.113853778871762,1.99198848396273,30.2711091737496));
#21299=CARTESIAN_POINT('Ctrl Pts',(0.200626784587728,1.98509763953635,30.2660566993938));
#21300=CARTESIAN_POINT('Ctrl Pts',(0.243222513348809,1.98032990487091,30.2635761672926));
#21301=CARTESIAN_POINT('Ctrl Pts',(0.401846263907804,1.95737982017132,30.2542512439538));
#21302=CARTESIAN_POINT('Ctrl Pts',(0.516333895195177,1.93033941821418,30.2473275949846));
#21303=CARTESIAN_POINT('Ctrl Pts',(0.641414689460609,1.88886774831417,30.2391736180503));
#21304=CARTESIAN_POINT('Ctrl Pts',(0.655008731771161,1.88419683660323,30.2382796204874));
#21305=CARTESIAN_POINT('Ctrl Pts',(0.676166651754766,1.87667033913496,30.2368753883034));
#21306=CARTESIAN_POINT('Ctrl Pts',(0.683765837338168,1.87391493386405,30.2363684362566));
#21307=CARTESIAN_POINT('Ctrl Pts',(0.696499459218093,1.86921005413598,30.2355144867702));
#21308=CARTESIAN_POINT('Ctrl Pts',(0.701643016338607,1.8672854093101,30.2351683146824));
#21309=CARTESIAN_POINT('Ctrl Pts',(0.711690686803729,1.86347833965617,30.2344896399933));
#21310=CARTESIAN_POINT('Ctrl Pts',(0.716595444989848,1.86159773404717,30.2341572003642));
#21311=CARTESIAN_POINT('Ctrl Pts',(0.72150063993698,1.85969470320895,30.233823568999));
#21312=CARTESIAN_POINT('Ctrl Pts',(0.721508600135357,1.85969161489308,30.2338230275757));
#21313=CARTESIAN_POINT('Ctrl Pts',(0.721524537637443,1.85968543150725,30.2338219435594));
#21314=CARTESIAN_POINT('Ctrl Pts',(0.721532514982225,1.8596823364211,30.2338214009637));
#21315=CARTESIAN_POINT('Ctrl Pts',(0.721548487002828,1.85967613940639,30.2338203145873));
#21316=CARTESIAN_POINT('Ctrl Pts',(0.721556481614404,1.8596730375025,30.233819770811));
#21317=CARTESIAN_POINT('Ctrl Pts',(0.721572488237506,1.85966682682479,30.2338186820686));
#21318=CARTESIAN_POINT('Ctrl Pts',(0.721580500204912,1.85966371806784,30.2338181371056));
#21319=CARTESIAN_POINT('Ctrl Pts',(0.721596541552215,1.85965749367835,30.2338170459889));
#21320=CARTESIAN_POINT('Ctrl Pts',(0.721604570938548,1.85965437804307,30.2338164998348));
#21321=CARTESIAN_POINT('Ctrl Pts',(0.72162064720136,1.85964813986603,30.2338154063306));
#21322=CARTESIAN_POINT('Ctrl Pts',(0.721628694086015,1.85964501732084,30.23381485898));
#21323=CARTESIAN_POINT('Ctrl Pts',(0.721644805413988,1.85963876529659,30.2338137630782));
#21324=CARTESIAN_POINT('Ctrl Pts',(0.721652869866033,1.85963563581389,30.2338132145264));
#21325=CARTESIAN_POINT('Ctrl Pts',(0.721669016452481,1.85962936986585,30.2338121162136));
#21326=CARTESIAN_POINT('Ctrl Pts',(0.721677098562723,1.85962623340962,30.2338115664543));
#21327=CARTESIAN_POINT('Ctrl Pts',(0.726093489696471,1.8579123140468,30.2335111540689));
#21328=CARTESIAN_POINT('Ctrl Pts',(0.730495670037904,1.85618587374475,30.2332107665123));
#21329=CARTESIAN_POINT('Ctrl Pts',(0.740619760255113,1.85217383023168,30.2325177457645));
#21330=CARTESIAN_POINT('Ctrl Pts',(0.74633727925959,1.84987734481367,30.2321247477341));
#21331=CARTESIAN_POINT('Ctrl Pts',(0.763696412171434,1.84281133809574,30.2309265669909));
#21332=CARTESIAN_POINT('Ctrl Pts',(0.775303449601213,1.83795821137453,30.2301185625849));
#21333=CARTESIAN_POINT('Ctrl Pts',(0.930030426104529,1.77153742094551,30.219253746891));
#21334=CARTESIAN_POINT('Ctrl Pts',(1.0654731073403,1.69353140090503,30.2085992605668));
#21335=CARTESIAN_POINT('Ctrl Pts',(1.26397311294647,1.54589729249184,30.1913569259095));
#21336=CARTESIAN_POINT('Ctrl Pts',(1.33365559086546,1.4862000157858,30.1849354583402));
#21337=CARTESIAN_POINT('Ctrl Pts',(1.42363398434183,1.39767278890527,30.1763208342768));
#21338=CARTESIAN_POINT('Ctrl Pts',(1.44764665256479,1.37278636874968,30.1739870317407));
#21339=CARTESIAN_POINT('Ctrl Pts',(1.48402522927104,1.33306732363768,30.1704124377485));
#21340=CARTESIAN_POINT('Ctrl Pts',(1.49684256813808,1.31865907834359,30.1691450204073));
#21341=CARTESIAN_POINT('Ctrl Pts',(1.51276706525988,1.30022656510334,30.1675626282775));
#21342=CARTESIAN_POINT('Ctrl Pts',(1.51606997812326,1.2963738415834,30.1672339926103));
#21343=CARTESIAN_POINT('Ctrl Pts',(1.52131506047581,1.29020818864268,30.1667114827525));
#21344=CARTESIAN_POINT('Ctrl Pts',(1.52326671426154,1.28790341283503,30.1665169202843));
#21345=CARTESIAN_POINT('Ctrl Pts',(1.52695989579606,1.28352186768229,30.1661484902583));
#21346=CARTESIAN_POINT('Ctrl Pts',(1.52870240371332,1.28144600711636,30.1659745528368));
#21347=CARTESIAN_POINT('Ctrl Pts',(1.53268600418052,1.27668062987651,30.1655766549996));
#21348=CARTESIAN_POINT('Ctrl Pts',(1.534924248718,1.27398876339921,30.1653529034966));
#21349=CARTESIAN_POINT('Ctrl Pts',(1.54197073156149,1.26546865327324,30.1646478420626));
#21350=CARTESIAN_POINT('Ctrl Pts',(1.54675302050689,1.25961888972123,30.1641683817167));
#21351=CARTESIAN_POINT('Ctrl Pts',(1.62886865214448,1.15800103505688,30.1559162981046));
#21352=CARTESIAN_POINT('Ctrl Pts',(1.69722065669643,1.05528742763423,30.1487393801663));
#21353=CARTESIAN_POINT('Ctrl Pts',(1.80316997393057,0.858846372859983,30.135782691383));
#21354=CARTESIAN_POINT('Ctrl Pts',(1.84397285642237,0.767334328811819,30.130011044752));
#21355=CARTESIAN_POINT('Ctrl Pts',(1.89475235165458,0.625686499903933,30.1210623121413));
#21356=CARTESIAN_POINT('Ctrl Pts',(1.90996133925146,0.57759603000583,30.1180233262793));
#21357=CARTESIAN_POINT('Ctrl Pts',(1.93135261642658,0.499819485274614,30.1130707630029));
#21358=CARTESIAN_POINT('Ctrl Pts',(1.93870903581534,0.470478020351055,30.1111941718594));
#21359=CARTESIAN_POINT('Ctrl Pts',(1.94731138664546,0.432528673478925,30.1087520657233));
#21360=CARTESIAN_POINT('Ctrl Pts',(1.94917240423737,0.42406323193522,30.1082063554833));
#21361=CARTESIAN_POINT('Ctrl Pts',(1.95208802314533,0.410375792195459,30.1073223902778));
#21362=CARTESIAN_POINT('Ctrl Pts',(1.95317699424345,0.405161164460992,30.1069852378996));
#21363=CARTESIAN_POINT('Ctrl Pts',(1.95521640718318,0.395195944799523,30.1063401839851));
#21364=CARTESIAN_POINT('Ctrl Pts',(1.95617045725483,0.39044612328369,30.1060324003162));
#21365=CARTESIAN_POINT('Ctrl Pts',(1.95831470495417,0.379565646867008,30.1053265906224));
#21366=CARTESIAN_POINT('Ctrl Pts',(1.95949342957825,0.373432807737394,30.1049282016409));
#21367=CARTESIAN_POINT('Ctrl Pts',(1.96303802874306,0.354511498117409,30.1036973058093));
#21368=CARTESIAN_POINT('Ctrl Pts',(1.96530761165989,0.341705549883269,30.1028617468941));
#21369=CARTESIAN_POINT('Ctrl Pts',(1.98835204356511,0.203846740700948,30.0938385779487));
#21370=CARTESIAN_POINT('Ctrl Pts',(1.99728239456358,0.0771318025587282,
30.0852673401902));
#21371=CARTESIAN_POINT('Ctrl Pts',(1.9902602694282,-0.205460999781071,30.0656800467879));
#21372=CARTESIAN_POINT('Ctrl Pts',(1.9681157817375,-0.36038107897085,30.054611354457));
#21373=CARTESIAN_POINT('Ctrl Pts',(1.92349535757947,-0.52869937830307,30.0430699986609));
#21374=CARTESIAN_POINT('Ctrl Pts',(1.91860167385474,-0.546191447865313,
30.0418772846926));
#21375=CARTESIAN_POINT('Ctrl Pts',(1.91206510591828,-0.568383057686739,
30.0403748014609));
#21376=CARTESIAN_POINT('Ctrl Pts',(1.91064282657059,-0.573145932639903,
30.0400529613236));
#21377=CARTESIAN_POINT('Ctrl Pts',(1.90833452214748,-0.580771809805676,
30.0395387277533));
#21378=CARTESIAN_POINT('Ctrl Pts',(1.90745983425723,-0.583638179415678,
30.0393456829692));
#21379=CARTESIAN_POINT('Ctrl Pts',(1.90577995688558,-0.589099056214416,
30.0389783796749));
#21380=CARTESIAN_POINT('Ctrl Pts',(1.90497593704651,-0.591693857879293,
30.0388040585938));
#21381=CARTESIAN_POINT('Ctrl Pts',(1.90311049600848,-0.597670953478845,
30.0384029780734));
#21382=CARTESIAN_POINT('Ctrl Pts',(1.90204535819706,-0.601052064704276,
30.038176439128));
#21383=CARTESIAN_POINT('Ctrl Pts',(1.89916467344168,-0.610111998177867,
30.0375702883828));
#21384=CARTESIAN_POINT('Ctrl Pts',(1.89733265355348,-0.61578560481305,30.0371916238709));
#21385=CARTESIAN_POINT('Ctrl Pts',(1.88383338224745,-0.656959460811448,
30.0344497780979));
#21386=CARTESIAN_POINT('Ctrl Pts',(1.87119516144548,-0.692136581925847,
30.0321405607066));
#21387=CARTESIAN_POINT('Ctrl Pts',(1.82656844291455,-0.806172713941301,
30.0247006622978));
#21388=CARTESIAN_POINT('Ctrl Pts',(1.79052151244,-0.883346979058934,30.0197369165592));
#21389=CARTESIAN_POINT('Ctrl Pts',(1.70125728344307,-1.04637754464846,30.0089438351228));
#21390=CARTESIAN_POINT('Ctrl Pts',(1.64623431731441,-1.13097027787818,30.0031348664401));
#21391=CARTESIAN_POINT('Ctrl Pts',(1.55390433102242,-1.25181553033917,29.9940972528022));
#21392=CARTESIAN_POINT('Ctrl Pts',(1.52119051994729,-1.29137120457922,29.9910065241158));
#21393=CARTESIAN_POINT('Ctrl Pts',(1.46656997161629,-1.35245649742028,29.9859770507631));
#21394=CARTESIAN_POINT('Ctrl Pts',(1.44562755267283,-1.37481885299057,29.9840767912153));
#21395=CARTESIAN_POINT('Ctrl Pts',(1.41808315652934,-1.402905388239,29.9816080421236));
#21396=CARTESIAN_POINT('Ctrl Pts',(1.41194640158631,-1.40908151728623,29.981059901067));
#21397=CARTESIAN_POINT('Ctrl Pts',(1.40198388105152,-1.41897753002168,29.9801729505615));
#21398=CARTESIAN_POINT('Ctrl Pts',(1.3981832320712,-1.42272263006079,29.9798352574502));
#21399=CARTESIAN_POINT('Ctrl Pts',(1.39090469115614,-1.42983745689816,29.9791898025587));
#21400=CARTESIAN_POINT('Ctrl Pts',(1.38742946003484,-1.43320986103817,29.9788821613116));
#21401=CARTESIAN_POINT('Ctrl Pts',(1.37945653546241,-1.44089070407277,29.9781775731668));
#21402=CARTESIAN_POINT('Ctrl Pts',(1.3749508917345,-1.4451907826226,29.977780267753));
#21403=CARTESIAN_POINT('Ctrl Pts',(1.36103738448895,-1.45834553981789,29.9765559875253));
#21404=CARTESIAN_POINT('Ctrl Pts',(1.35156372418896,-1.4671298381135,29.9757260079733));
#21405=CARTESIAN_POINT('Ctrl Pts',(1.26044409600532,-1.5499874632589,29.967776057998));
#21406=CARTESIAN_POINT('Ctrl Pts',(1.17288938503415,-1.61725183938662,29.9603703392054));
#21407=CARTESIAN_POINT('Ctrl Pts',(0.935667596511906,-1.77006464507373,
29.9409268967729));
#21408=CARTESIAN_POINT('Ctrl Pts',(0.779661265895116,-1.84410734432581,
29.9286576484827));
#21409=CARTESIAN_POINT('Ctrl Pts',(0.598277101336207,-1.90300891659655,
29.9160090894163));
#21410=CARTESIAN_POINT('Ctrl Pts',(0.580380124860129,-1.90854326648443,
29.9147784256211));
#21411=CARTESIAN_POINT('Ctrl Pts',(0.557586649798532,-1.91524148176705,
29.913235285106));
#21412=CARTESIAN_POINT('Ctrl Pts',(0.552760837188338,-1.91663983672436,
29.9129099414633));
#21413=CARTESIAN_POINT('Ctrl Pts',(0.54503665523231,-1.91884643989487,29.9123914405375));
#21414=CARTESIAN_POINT('Ctrl Pts',(0.542141691221527,-1.91966637788402,
29.9121976129662));
#21415=CARTESIAN_POINT('Ctrl Pts',(0.53663268622214,-1.92121323230813,29.9118297365021));
#21416=CARTESIAN_POINT('Ctrl Pts',(0.534019049742052,-1.92194135667876,
29.9116556212613));
#21417=CARTESIAN_POINT('Ctrl Pts',(0.528009453264891,-1.92360234512286,
29.9112562181817));
#21418=CARTESIAN_POINT('Ctrl Pts',(0.524612505404947,-1.92453154937436,
29.9110311447455));
#21419=CARTESIAN_POINT('Ctrl Pts',(0.515534613523457,-1.92698890307561,
29.9104314651091));
#21420=CARTESIAN_POINT('Ctrl Pts',(0.509849286799737,-1.92850094040665,
29.9100577747491));
#21421=CARTESIAN_POINT('Ctrl Pts',(0.469566370420368,-1.93902376589892,
29.9074227588315));
#21422=CARTESIAN_POINT('Ctrl Pts',(0.434736163110228,-1.94712880776038,
29.9052107850648));
#21423=CARTESIAN_POINT('Ctrl Pts',(0.386656507434843,-1.95696235935127,
29.9022243398097));
#21424=CARTESIAN_POINT('Ctrl Pts',(0.373581970546604,-1.95950030801102,
29.9014189537047));
#21425=CARTESIAN_POINT('Ctrl Pts',(0.336881953554389,-1.96624360463748,
29.899174636119));
#21426=CARTESIAN_POINT('Ctrl Pts',(0.313204132028088,-1.97015395452307,
29.8977456068746));
#21427=CARTESIAN_POINT('Ctrl Pts',(0.18450760265531,-1.98902906657953,29.8900537795893));
#21428=CARTESIAN_POINT('Ctrl Pts',(0.0784906052197476,-1.99602619720032,
29.8839799332439));
#21429=CARTESIAN_POINT('Ctrl Pts',(-0.145681996287054,-1.99292607095643,
29.8709016394709));
#21430=CARTESIAN_POINT('Ctrl Pts',(-0.263384832330395,-1.9808079286306,
29.8638892917108));
#21431=CARTESIAN_POINT('Ctrl Pts',(-0.39255818662144,-1.95578822709646,
29.8556816097451));
#21432=CARTESIAN_POINT('Ctrl Pts',(-0.405774564570033,-1.95308896562998,
29.8548360114642));
#21433=CARTESIAN_POINT('Ctrl Pts',(-0.42515941144419,-1.94892463013027,
29.8535867749573));
#21434=CARTESIAN_POINT('Ctrl Pts',(-0.431350086775581,-1.94756382185559,
29.8531864729945));
#21435=CARTESIAN_POINT('Ctrl Pts',(-0.44227311022526,-1.94510813366725,
29.852477737646));
#21436=CARTESIAN_POINT('Ctrl Pts',(-0.447008164803977,-1.94402542565722,
29.8521696971042));
#21437=CARTESIAN_POINT('Ctrl Pts',(-0.456251663323227,-1.94187626934649,
29.8515667574413));
#21438=CARTESIAN_POINT('Ctrl Pts',(-0.460760442578518,-1.94081138694474,
29.851271910462));
#21439=CARTESIAN_POINT('Ctrl Pts',(-0.472902267712806,-1.93789903870934,
29.8504758744366));
#21440=CARTESIAN_POINT('Ctrl Pts',(-0.480528118888391,-1.93602220107952,
29.8499737416978));
#21441=CARTESIAN_POINT('Ctrl Pts',(-0.508515430137787,-1.92895855597037,
29.8481227675753));
#21442=CARTESIAN_POINT('Ctrl Pts',(-0.528805068106709,-1.92349530727224,
29.8467650347883));
#21443=CARTESIAN_POINT('Ctrl Pts',(-0.702168349245475,-1.87386475958351,
29.835023170862));
#21444=CARTESIAN_POINT('Ctrl Pts',(-0.849498380171197,-1.8118339125268,
29.8240271018646));
#21445=CARTESIAN_POINT('Ctrl Pts',(-1.05351260044327,-1.69553850004089,
29.8076424475808));
#21446=CARTESIAN_POINT('Ctrl Pts',(-1.11699486635934,-1.65440717737234,
29.8023685791579));
#21447=CARTESIAN_POINT('Ctrl Pts',(-1.20588760888744,-1.58935757225439,
29.7948510907989));
#21448=CARTESIAN_POINT('Ctrl Pts',(-1.2332495311162,-1.56822138432968,29.7925178193457));
#21449=CARTESIAN_POINT('Ctrl Pts',(-1.27499571825495,-1.53420506201687,
29.78894394596));
#21450=CARTESIAN_POINT('Ctrl Pts',(-1.289764900205,-1.52181004868533,29.7876767303591));
#21451=CARTESIAN_POINT('Ctrl Pts',(-1.30819190051769,-1.50588421300893,
29.786094553357));
#21452=CARTESIAN_POINT('Ctrl Pts',(-1.31201846812658,-1.502551447451,29.7857659354969));
#21453=CARTESIAN_POINT('Ctrl Pts',(-1.31810208379111,-1.49721193543508,
29.7852434473215));
#21454=CARTESIAN_POINT('Ctrl Pts',(-1.32036733210652,-1.49521463058243,
29.7850488888265));
#21455=CARTESIAN_POINT('Ctrl Pts',(-1.32465691245024,-1.49141509063294,
29.7846804618319));
#21456=CARTESIAN_POINT('Ctrl Pts',(-1.32668208225354,-1.48961389661295,
29.7845065234876));
#21457=CARTESIAN_POINT('Ctrl Pts',(-1.33131480846138,-1.48547659007489,
29.784108617686));
#21458=CARTESIAN_POINT('Ctrl Pts',(-1.33391988743018,-1.48313773914112,
29.7838848591704));
#21459=CARTESIAN_POINT('Ctrl Pts',(-1.34212810592106,-1.47572924534879,
29.7831797535112));
#21460=CARTESIAN_POINT('Ctrl Pts',(-1.34770868755247,-1.47063454201164,
29.7827002562826));
#21461=CARTESIAN_POINT('Ctrl Pts',(-1.44350876425442,-1.3821720934168,29.7744641282722));
#21462=CARTESIAN_POINT('Ctrl Pts',(-1.52588213403983,-1.29066298475416,
29.7673007549229));
#21463=CARTESIAN_POINT('Ctrl Pts',(-1.65917078808642,-1.11184925662339,
29.7543532894403));
#21464=CARTESIAN_POINT('Ctrl Pts',(-1.71288817501726,-1.02716571279457,
29.748577090161));
#21465=CARTESIAN_POINT('Ctrl Pts',(-1.78379968354245,-0.894225745179675,
29.7396175415534));
#21466=CARTESIAN_POINT('Ctrl Pts',(-1.80587759752339,-0.848755862964658,
29.7365722738101));
#21467=CARTESIAN_POINT('Ctrl Pts',(-1.83839194569144,-0.774764712321493,
29.7316103664774));
#21468=CARTESIAN_POINT('Ctrl Pts',(-1.84994556731505,-0.746757356213623,
29.7297308933589));
#21469=CARTESIAN_POINT('Ctrl Pts',(-1.86398024165095,-0.710408636922516,
29.7272855418833));
#21470=CARTESIAN_POINT('Ctrl Pts',(-1.86705115570611,-0.702298192243683,
29.7267395340787));
#21471=CARTESIAN_POINT('Ctrl Pts',(-1.87192324721275,-0.689172916463398,
29.7258552034461));
#21472=CARTESIAN_POINT('Ctrl Pts',(-1.87375741228224,-0.684170381747702,
29.7255179848849));
#21473=CARTESIAN_POINT('Ctrl Pts',(-1.87722090542567,-0.674605590966897,
29.7248728821735));
#21474=CARTESIAN_POINT('Ctrl Pts',(-1.87885370165506,-0.670044624057021,
29.7245651162179));
#21475=CARTESIAN_POINT('Ctrl Pts',(-1.88255262427622,-0.659592415705384,
29.7238594573999));
#21476=CARTESIAN_POINT('Ctrl Pts',(-1.88460773234966,-0.653697354842725,
29.7234612021293));
#21477=CARTESIAN_POINT('Ctrl Pts',(-1.89085517223222,-0.635502278453995,
29.7222311237586));
#21478=CARTESIAN_POINT('Ctrl Pts',(-1.8949549442572,-0.623171063373311,
29.7213962544618));
#21479=CARTESIAN_POINT('Ctrl Pts',(-1.93511570973685,-0.498314278954933,
29.7129293291086));
#21480=CARTESIAN_POINT('Ctrl Pts',(-1.9612246098998,-0.382856239917268,
29.7049666528438));
#21481=CARTESIAN_POINT('Ctrl Pts',(-1.98887518461848,-0.177185840241624,
29.6906262161521));
#21482=CARTESIAN_POINT('Ctrl Pts',(-1.99481690558367,-0.0878868767612705,
29.6843555906316));
#21483=CARTESIAN_POINT('Ctrl Pts',(-1.99468269335407,0.0899240126054698,
29.6720070532425));
#21484=CARTESIAN_POINT('Ctrl Pts',(-1.98873717617692,0.178252204240259,
29.6659421718432));
#21485=CARTESIAN_POINT('Ctrl Pts',(-1.97590266168009,0.273674450671789,
29.659653047608));
#21486=CARTESIAN_POINT('Ctrl Pts',(-1.97481170536337,0.281438744108537,
29.6591432579223));
#21487=CARTESIAN_POINT('Ctrl Pts',(-1.9731597213127,0.292713012403177,29.6584060316065));
#21488=CARTESIAN_POINT('Ctrl Pts',(-1.97263506419656,0.29622811720631,29.6581766059426));
#21489=CARTESIAN_POINT('Ctrl Pts',(-1.97169260979237,0.302428837526234,
29.6577726716034));
#21490=CARTESIAN_POINT('Ctrl Pts',(-1.97127871491979,0.305115023790714,
29.657597943365));
#21491=CARTESIAN_POINT('Ctrl Pts',(-1.97039760502827,0.310756808663185,
29.6572315131497));
#21492=CARTESIAN_POINT('Ctrl Pts',(-1.9699292305424,0.31371219768379,29.6570398781321));
#21493=CARTESIAN_POINT('Ctrl Pts',(-1.96866837429776,0.321553880574816,
29.6565322143381));
#21494=CARTESIAN_POINT('Ctrl Pts',(-1.96786434482808,0.326438336739092,
29.6562168353945));
#21495=CARTESIAN_POINT('Ctrl Pts',(-1.96406089804911,0.34901935900467,29.6547624873377));
#21496=CARTESIAN_POINT('Ctrl Pts',(-1.9608407825424,0.366678611527238,29.6536355387752));
#21497=CARTESIAN_POINT('Ctrl Pts',(-1.95135780568296,0.414979847897621,
29.6505757688381));
#21498=CARTESIAN_POINT('Ctrl Pts',(-1.94461183516986,0.445522833706953,
29.6486660442634));
#21499=CARTESIAN_POINT('Ctrl Pts',(-1.91836248795739,0.552371595047287,
29.6420339473941));
#21500=CARTESIAN_POINT('Ctrl Pts',(-1.89506135114121,0.627672866895404,
29.6374463997027));
#21501=CARTESIAN_POINT('Ctrl Pts',(-1.81072224382273,0.852211318433263,
29.6235232603464));
#21502=CARTESIAN_POINT('Ctrl Pts',(-1.73602666167702,0.995581932743773,
29.614238060434));
#21503=CARTESIAN_POINT('Ctrl Pts',(-1.63819113968824,1.13819963853713,29.603535906655));
#21504=CARTESIAN_POINT('Ctrl Pts',(-1.63138520232766,1.14793333410339,29.6027978258839));
#21505=CARTESIAN_POINT('Ctrl Pts',(-1.61697564899362,1.16815457204016,29.6012479664391));
#21506=CARTESIAN_POINT('Ctrl Pts',(-1.6093560098812,1.17862995654739,29.6004356104254));
#21507=CARTESIAN_POINT('Ctrl Pts',(-1.59791849996567,1.19403639163864,29.5992263880552));
#21508=CARTESIAN_POINT('Ctrl Pts',(-1.59417855627439,1.19902508996725,29.5988325556329));
#21509=CARTESIAN_POINT('Ctrl Pts',(-1.58749192040203,1.20785778294067,29.5981311557343));
#21510=CARTESIAN_POINT('Ctrl Pts',(-1.58455448751181,1.21170875072365,29.5978239536142));
#21511=CARTESIAN_POINT('Ctrl Pts',(-1.57835367276,1.21977689777012,29.5971773684635));
#21512=CARTESIAN_POINT('Ctrl Pts',(-1.57508735206549,1.22399176022619,29.5968378706508));
#21513=CARTESIAN_POINT('Ctrl Pts',(-1.5664529748821,1.23504177061498,29.5959432562952));
#21514=CARTESIAN_POINT('Ctrl Pts',(-1.56105712497378,1.24185496185503,29.5953870352665));
#21515=CARTESIAN_POINT('Ctrl Pts',(-1.53653758136221,1.2724027940613,29.5928720001395));
#21516=CARTESIAN_POINT('Ctrl Pts',(-1.51691679507018,1.29573140545769,29.5908932323507));
#21517=CARTESIAN_POINT('Ctrl Pts',(-1.46308431817299,1.35683774807051,29.5855486130291));
#21518=CARTESIAN_POINT('Ctrl Pts',(-1.42794830067102,1.39376730676925,29.5821457534618));
#21519=CARTESIAN_POINT('Ctrl Pts',(-1.31940463850189,1.49943512045892,29.5718814143154));
#21520=CARTESIAN_POINT('Ctrl Pts',(-1.24217729250116,1.56400976385522,29.5648828858498));
#21521=CARTESIAN_POINT('Ctrl Pts',(-1.06136825096233,1.69332661587501,29.5493732462378));
#21522=CARTESIAN_POINT('Ctrl Pts',(-0.956024337976294,1.75495937265301,
29.5408843601799));
#21523=CARTESIAN_POINT('Ctrl Pts',(-0.838841317786708,1.80981497286336,
29.5324367075282));
#21524=CARTESIAN_POINT('Ctrl Pts',(-0.831959469096917,1.81298881372095,
29.5319441211451));
#21525=CARTESIAN_POINT('Ctrl Pts',(-0.821868361964223,1.81757317423066,
29.5312271403572));
#21526=CARTESIAN_POINT('Ctrl Pts',(-0.818673311137647,1.81901452940124,
29.531000905191));
#21527=CARTESIAN_POINT('Ctrl Pts',(-0.813000479095079,1.82155569010856,
29.5306006188287));
#21528=CARTESIAN_POINT('Ctrl Pts',(-0.810524237857629,1.82265887411017,
29.5304263611579));
#21529=CARTESIAN_POINT('Ctrl Pts',(-0.805286672135983,1.82497946422341,
29.5300587849174));
#21530=CARTESIAN_POINT('Ctrl Pts',(-0.802524839234077,1.82619564994166,
29.529865541486));
#21531=CARTESIAN_POINT('Ctrl Pts',(-0.795120924133763,1.8294359579301,29.5293490298217));
#21532=CARTESIAN_POINT('Ctrl Pts',(-0.790473837363793,1.83144869487509,
29.5290264522268));
#21533=CARTESIAN_POINT('Ctrl Pts',(-0.768202472402139,1.8409942637053,29.5274879525778));
#21534=CARTESIAN_POINT('Ctrl Pts',(-0.750477170208798,1.84829083219049,
29.5262858109905));
#21535=CARTESIAN_POINT('Ctrl Pts',(-0.700762706701203,1.86792249549073,
29.5229686086327));
#21536=CARTESIAN_POINT('Ctrl Pts',(-0.668555464807695,1.87969058560893,
29.5208816631549));
#21537=CARTESIAN_POINT('Ctrl Pts',(-0.549982384435761,1.91958191382647,
29.5133682219611));
#21538=CARTESIAN_POINT('Ctrl Pts',(-0.462022617878833,1.9426303534154,29.5081145492054));
#21539=CARTESIAN_POINT('Ctrl Pts',(-0.218449517138189,1.98896744515433,
29.493734928394));
#21540=CARTESIAN_POINT('Ctrl Pts',(-0.0612028394111058,1.99998914096932,
29.4845880091085));
#21541=CARTESIAN_POINT('Ctrl Pts',(0.108221522271149,1.99185161473854,29.4739955096605));
#21542=CARTESIAN_POINT('Ctrl Pts',(0.120738466222123,1.9911320810915,29.4732089718794));
#21543=CARTESIAN_POINT('Ctrl Pts',(0.139386752225096,1.98988360319602,29.4720309176832));
#21544=CARTESIAN_POINT('Ctrl Pts',(0.145523941327363,1.98944419426288,29.4716422099475));
#21545=CARTESIAN_POINT('Ctrl Pts',(0.156478485427015,1.98860891306648,29.4709465491798));
#21546=CARTESIAN_POINT('Ctrl Pts',(0.161296640220893,1.98822391060676,29.4706399398293));
#21547=CARTESIAN_POINT('Ctrl Pts',(0.171471438358703,1.98737364838928,29.4699910897493));
#21548=CARTESIAN_POINT('Ctrl Pts',(0.176827687050827,1.98690423539829,29.4696487207939));
#21549=CARTESIAN_POINT('Ctrl Pts',(0.191035449280268,1.98560118446814,29.4687384126165));
#21550=CARTESIAN_POINT('Ctrl Pts',(0.199883320149152,1.98473002212479,29.4681692977063));
#21551=CARTESIAN_POINT('Ctrl Pts',(0.241080165248053,1.98039550721082,29.4655088380872));
#21552=CARTESIAN_POINT('Ctrl Pts',(0.273345546375769,1.97620039863636,29.4633946024729));
#21553=CARTESIAN_POINT('Ctrl Pts',(0.360613604713349,1.96267590587993,29.4575891008301));
#21554=CARTESIAN_POINT('Ctrl Pts',(0.415347551650833,1.95182589837783,29.4538524908469));
#21555=CARTESIAN_POINT('Ctrl Pts',(0.570931040727586,1.91414370410869,29.4429638838575));
#21556=CARTESIAN_POINT('Ctrl Pts',(0.6702219243729,1.88167683896254,29.4356774166701));
#21557=CARTESIAN_POINT('Ctrl Pts',(0.837265265202727,1.81215010657783,29.4230613258358));
#21558=CARTESIAN_POINT('Ctrl Pts',(0.90626945205378,1.77864511198752,29.4177387087298));
#21559=CARTESIAN_POINT('Ctrl Pts',(1.00434662604989,1.72383013431698,29.4101549621578));
#21560=CARTESIAN_POINT('Ctrl Pts',(1.03504405586912,1.70557517293847,29.4077789588422));
#21561=CARTESIAN_POINT('Ctrl Pts',(1.07020890669867,1.68336420291293,29.4050687400411));
#21562=CARTESIAN_POINT('Ctrl Pts',(1.0751669282844,1.68020183967615,29.4046868922337));
#21563=CARTESIAN_POINT('Ctrl Pts',(1.08307115893924,1.67511098882462,29.4040786726542));
#21564=CARTESIAN_POINT('Ctrl Pts',(1.08602632523621,1.6731965758895,29.403851396787));
#21565=CARTESIAN_POINT('Ctrl Pts',(1.09124954002506,1.66979321013697,29.4034499247904));
#21566=CARTESIAN_POINT('Ctrl Pts',(1.09351963681289,1.66830744393357,29.4032755179165));
#21567=CARTESIAN_POINT('Ctrl Pts',(1.09830119694076,1.66516398542629,29.4029083356749));
#21568=CARTESIAN_POINT('Ctrl Pts',(1.10081193618029,1.66350524466242,29.402715632723));
#21569=CARTESIAN_POINT('Ctrl Pts',(1.10750597897225,1.65906097775051,29.4022020949817));
#21570=CARTESIAN_POINT('Ctrl Pts',(1.1116825593925,1.65626528968634,29.4018819370027));
#21571=CARTESIAN_POINT('Ctrl Pts',(1.13138916337494,1.64296610587366,29.4003722807648));
#21572=CARTESIAN_POINT('Ctrl Pts',(1.14678179656807,1.63225936567296,29.3991959452767));
#21573=CARTESIAN_POINT('Ctrl Pts',(1.18903581765834,1.60197565289214,29.3959678785352));
#21574=CARTESIAN_POINT('Ctrl Pts',(1.21556333250924,1.5819412811859,29.3939424630068));
#21575=CARTESIAN_POINT('Ctrl Pts',(1.30966758123519,1.50710526837466,29.3867125361567));
#21576=CARTESIAN_POINT('Ctrl Pts',(1.3741456414647,1.44855835576325,29.381669042052));
#21577=CARTESIAN_POINT('Ctrl Pts',(1.53846118282463,1.27847941958292,29.3679530908451));
#21578=CARTESIAN_POINT('Ctrl Pts',(1.62989688063555,1.15965574372557,29.3592842263497));
#21579=CARTESIAN_POINT('Ctrl Pts',(1.71480370255174,1.01916234515257,29.3491293066863));
#21580=CARTESIAN_POINT('Ctrl Pts',(1.72226702145372,1.00649883905141,29.3482152320256));
#21581=CARTESIAN_POINT('Ctrl Pts',(1.73472791365769,0.984811154490312,29.3466512271324));
#21582=CARTESIAN_POINT('Ctrl Pts',(1.73979675418513,0.975828464525246,29.3460038599903));
#21583=CARTESIAN_POINT('Ctrl Pts',(1.74782723583675,0.961335862312169,29.344959886108));
#21584=CARTESIAN_POINT('Ctrl Pts',(1.75083306420175,0.955850546032718,29.3445648620706));
#21585=CARTESIAN_POINT('Ctrl Pts',(1.75612871361583,0.946077760408783,29.3438612313486));
#21586=CARTESIAN_POINT('Ctrl Pts',(1.75842876675791,0.941795869113549,29.3435529919384));
#21587=CARTESIAN_POINT('Ctrl Pts',(1.76319051860419,0.932852905361689,29.3429093053458));
#21588=CARTESIAN_POINT('Ctrl Pts',(1.76564943456453,0.928190401415687,29.3425737625582));
#21589=CARTESIAN_POINT('Ctrl Pts',(1.77198615028136,0.916058662110182,29.341700785273));
#21590=CARTESIAN_POINT('Ctrl Pts',(1.77583518122866,0.908574595026239,29.3411623416014));
#21591=CARTESIAN_POINT('Ctrl Pts',(1.79221870899521,0.876216575432168,29.3388345617276));
#21592=CARTESIAN_POINT('Ctrl Pts',(1.804278300622,0.851106968125027,29.3370287374579));
#21593=CARTESIAN_POINT('Ctrl Pts',(1.83446293809845,0.784731885145469,29.3322538886938));
#21594=CARTESIAN_POINT('Ctrl Pts',(1.85172134675272,0.743092143853861,29.3292568521593));
#21595=CARTESIAN_POINT('Ctrl Pts',(1.93290702330323,0.526774165873512,29.3136804573127));
#21596=CARTESIAN_POINT('Ctrl Pts',(1.97357526088913,0.344391154345442,29.3004112078428));
#21597=CARTESIAN_POINT('Ctrl Pts',(1.98903093849333,0.151149127975669,29.2872158370067));
#21598=CARTESIAN_POINT('Ctrl Pts',(1.9896146876436,0.143260361243321,29.2866788402576));
#21599=CARTESIAN_POINT('Ctrl Pts',(1.99280073243957,0.0964198891996078,
29.2835010760387));
#21600=CARTESIAN_POINT('Ctrl Pts',(1.99430625162311,0.0573988624375412,
29.2808976380761));
#21601=CARTESIAN_POINT('Ctrl Pts',(1.99472650006532,0.0117317454929255,
29.277920722126));
#21602=CARTESIAN_POINT('Ctrl Pts',(1.99475446156921,0.00510734466025873,
29.2774906188408));
#21603=CARTESIAN_POINT('Ctrl Pts',(1.99474683809922,-0.00491576492343968,
29.2768425789152));
#21604=CARTESIAN_POINT('Ctrl Pts',(1.99473556759528,-0.00831436368357211,
29.2766233191499));
#21605=CARTESIAN_POINT('Ctrl Pts',(1.99469979830948,-0.0144058748249083,
29.2762311985545));
#21606=CARTESIAN_POINT('Ctrl Pts',(1.99467853223731,-0.0170987698666067,
29.2760581590104));
#21607=CARTESIAN_POINT('Ctrl Pts',(1.99462085554161,-0.0229115665326558,
29.2756853059508));
#21608=CARTESIAN_POINT('Ctrl Pts',(1.99458257860969,-0.0260314170960715,
29.2754855985625));
#21609=CARTESIAN_POINT('Ctrl Pts',(1.99445623140718,-0.0346761467921984,
29.2749333398556));
#21610=CARTESIAN_POINT('Ctrl Pts',(1.99435252395427,-0.0402008221434106,
29.2745816545407));
#21611=CARTESIAN_POINT('Ctrl Pts',(1.99365218038771,-0.0707451848983417,
29.2726438590587));
#21612=CARTESIAN_POINT('Ctrl Pts',(1.99260765508568,-0.0957537034461689,
29.2710816526476));
#21613=CARTESIAN_POINT('Ctrl Pts',(1.98129094390957,-0.282378853568761,
29.2595619515875));
#21614=CARTESIAN_POINT('Ctrl Pts',(1.95184123842895,-0.442246226024752,
29.2504300232227));
#21615=CARTESIAN_POINT('Ctrl Pts',(1.86958648990062,-0.704577793124424,
29.2343627628488));
#21616=CARTESIAN_POINT('Ctrl Pts',(1.82670905431181,-0.80926638931887,29.2276365199524));
#21617=CARTESIAN_POINT('Ctrl Pts',(1.76930240973371,-0.921284060672225,
29.2197798315951));
#21618=CARTESIAN_POINT('Ctrl Pts',(1.7632829307337,-0.932753253072947,29.2189675141049));
#21619=CARTESIAN_POINT('Ctrl Pts',(1.75420119853841,-0.949654985046272,
29.2177583381817));
#21620=CARTESIAN_POINT('Ctrl Pts',(1.75122439982988,-0.955133255406537,
29.2173645133408));
#21621=CARTESIAN_POINT('Ctrl Pts',(1.74588959366236,-0.964842239821923,
29.2166631219817));
#21622=CARTESIAN_POINT('Ctrl Pts',(1.74354175804883,-0.969078509856197,
29.2163559207877));
#21623=CARTESIAN_POINT('Ctrl Pts',(1.73857666037765,-0.977960731986841,
29.2157093325255));
#21624=CARTESIAN_POINT('Ctrl Pts',(1.73595615400385,-0.982604817708438,
29.2153698306559));
#21625=CARTESIAN_POINT('Ctrl Pts',(1.7290155555785,-0.994790586581263,29.2144751941241));
#21626=CARTESIAN_POINT('Ctrl Pts',(1.72466477671083,-1.0023145746672,29.2139189548768));
#21627=CARTESIAN_POINT('Ctrl Pts',(1.70483345895507,-1.03609828577954,29.2114037202105));
#21628=CARTESIAN_POINT('Ctrl Pts',(1.6888020874888,-1.06202830414087,29.2094247672188));
#21629=CARTESIAN_POINT('Ctrl Pts',(1.64439607954055,-1.13030375973011,29.204079526719));
#21630=CARTESIAN_POINT('Ctrl Pts',(1.61498357460313,-1.17194384135886,29.2006762205873));
#21631=CARTESIAN_POINT('Ctrl Pts',(1.52290448083161,-1.29224504771991,29.1904110380524));
#21632=CARTESIAN_POINT('Ctrl Pts',(1.45585454405651,-1.36734032141634,29.1834121149305));
#21633=CARTESIAN_POINT('Ctrl Pts',(1.2957328348618,-1.5214877184818,29.1679047352846));
#21634=CARTESIAN_POINT('Ctrl Pts',(1.20047171591933,-1.59772446057512,29.1594185247704));
#21635=CARTESIAN_POINT('Ctrl Pts',(1.09313300079835,-1.66857262417747,29.1510212467001));
#21636=CARTESIAN_POINT('Ctrl Pts',(1.08740423646716,-1.67231169026018,29.150576386859));
#21637=CARTESIAN_POINT('Ctrl Pts',(1.07875334735924,-1.67789472695013,29.149909714621));
#21638=CARTESIAN_POINT('Ctrl Pts',(1.07584555489214,-1.67976065009983,29.1496864901218));
#21639=CARTESIAN_POINT('Ctrl Pts',(1.07080017794599,-1.68297978050172,29.1493006786138));
#21640=CARTESIAN_POINT('Ctrl Pts',(1.06866485186282,-1.68433648575218,29.149137860532));
#21641=CARTESIAN_POINT('Ctrl Pts',(1.0642315057073,-1.68714144130097,29.1488007952327));
#21642=CARTESIAN_POINT('Ctrl Pts',(1.06193310394885,-1.68858906296089,29.1486265918141));
#21643=CARTESIAN_POINT('Ctrl Pts',(1.05641288901803,-1.69205017789126,29.1482094800557));
#21644=CARTESIAN_POINT('Ctrl Pts',(1.05318824484642,-1.69405918376061,29.1479668686416));
#21645=CARTESIAN_POINT('Ctrl Pts',(1.04628075485438,-1.69833531648587,29.1474493591027));
#21646=CARTESIAN_POINT('Ctrl Pts',(1.04259622788232,-1.70059970940683,29.1471746368819));
#21647=CARTESIAN_POINT('Ctrl Pts',(1.03242275924415,-1.70680650822678,29.1464196460598));
#21648=CARTESIAN_POINT('Ctrl Pts',(1.02591854938596,-1.71072392413257,29.1459409242689));
#21649=CARTESIAN_POINT('Ctrl Pts',(0.967963137306254,-1.74518043883418,
29.141708940551));
#21650=CARTESIAN_POINT('Ctrl Pts',(0.91517909713262,-1.77343060331604,29.138088701647));
#21651=CARTESIAN_POINT('Ctrl Pts',(0.7373153419182,-1.85856314200701,29.1263810362761));
#21652=CARTESIAN_POINT('Ctrl Pts',(0.607635294874978,-1.90490776991815,
29.1185892814105));
#21653=CARTESIAN_POINT('Ctrl Pts',(0.382335811180314,-1.96004968451904,
29.1049355028131));
#21654=CARTESIAN_POINT('Ctrl Pts',(0.28898325439819,-1.97597077470157,29.0992513680315));
#21655=CARTESIAN_POINT('Ctrl Pts',(0.182263431093813,-1.98644603354663,
29.0925557835163));
#21656=CARTESIAN_POINT('Ctrl Pts',(0.169654133564061,-1.98756264447166,
29.0917617304716));
#21657=CARTESIAN_POINT('Ctrl Pts',(0.1508775158442,-1.9890454223966,29.0905745955482));
#21658=CARTESIAN_POINT('Ctrl Pts',(0.144717573471841,-1.98950308863245,
29.090184387057));
#21659=CARTESIAN_POINT('Ctrl Pts',(0.133731026157236,-1.990268063626,29.089487052718));
#21660=CARTESIAN_POINT('Ctrl Pts',(0.128905221234699,-1.99058644517388,
29.0891802768922));
#21661=CARTESIAN_POINT('Ctrl Pts',(0.118725365463809,-1.99122088572276,
29.0885321246352));
#21662=CARTESIAN_POINT('Ctrl Pts',(0.113371110068733,-1.9915329067375,29.088190624007));
#21663=CARTESIAN_POINT('Ctrl Pts',(0.0991983455425936,-1.99230148953258,
29.0872850624796));
#21664=CARTESIAN_POINT('Ctrl Pts',(0.0903780290164882,-1.99272109053517,
29.0867198476139));
#21665=CARTESIAN_POINT('Ctrl Pts',(0.0496833626137043,-1.99438628389095,
29.0841042826778));
#21666=CARTESIAN_POINT('Ctrl Pts',(0.0177863390575472,-1.99492569689813,
29.082031971538));
#21667=CARTESIAN_POINT('Ctrl Pts',(-0.068374917324342,-1.99431628173908,
29.0763705137672));
#21668=CARTESIAN_POINT('Ctrl Pts',(-0.122598623136321,-1.99171816591562,
29.0727387323324));
#21669=CARTESIAN_POINT('Ctrl Pts',(-0.352674846251479,-1.97126340031703,
29.0570458634451));
#21670=CARTESIAN_POINT('Ctrl Pts',(-0.525820179741654,-1.93229452706614,
29.0444416512425));
#21671=CARTESIAN_POINT('Ctrl Pts',(-0.702560740995732,-1.86696908936891,
29.031659069985));
#21672=CARTESIAN_POINT('Ctrl Pts',(-0.71352819186916,-1.86280506394832,
29.0308666179083));
#21673=CARTESIAN_POINT('Ctrl Pts',(-0.753443472610029,-1.84724613329007,
29.0279868409863));
#21674=CARTESIAN_POINT('Ctrl Pts',(-0.782162225180227,-1.83527051486149,
29.0259231268357));
#21675=CARTESIAN_POINT('Ctrl Pts',(-0.815741446972016,-1.82033657015145,
29.0235296790506));
#21676=CARTESIAN_POINT('Ctrl Pts',(-0.82088227714723,-1.81802409936181,
29.0231638026675));
#21677=CARTESIAN_POINT('Ctrl Pts',(-0.829186504529237,-1.81424625018304,
29.0225737585325));
#21678=CARTESIAN_POINT('Ctrl Pts',(-0.832355938761917,-1.81279433672401,
29.0223487897179));
#21679=CARTESIAN_POINT('Ctrl Pts',(-0.837974475018411,-1.81020265125403,
29.021950412703));
#21680=CARTESIAN_POINT('Ctrl Pts',(-0.840425079500347,-1.80906620814867,
29.021776801773));
#21681=CARTESIAN_POINT('Ctrl Pts',(-0.845166886736786,-1.80685552808274,
29.0214411619055));
#21682=CARTESIAN_POINT('Ctrl Pts',(-0.847458339547273,-1.8057819161533,
29.021279095258));
#21683=CARTESIAN_POINT('Ctrl Pts',(-0.853903828548873,-1.80274704726758,
29.0208235755316));
#21684=CARTESIAN_POINT('Ctrl Pts',(-0.858053176041891,-1.80077578086284,
29.0205307375961));
#21685=CARTESIAN_POINT('Ctrl Pts',(-0.875450133658827,-1.79243707481151,
29.0193045169851));
#21686=CARTESIAN_POINT('Ctrl Pts',(-0.888634385470293,-1.78593744659649,
29.0183790373044));
#21687=CARTESIAN_POINT('Ctrl Pts',(-0.923084770713577,-1.76847797905721,
29.0159676801844));
#21688=CARTESIAN_POINT('Ctrl Pts',(-0.944228247774239,-1.7572799951707,
29.0144947471362));
#21689=CARTESIAN_POINT('Ctrl Pts',(-1.04221221354983,-1.70310654137577,
29.007677939762));
#21690=CARTESIAN_POINT('Ctrl Pts',(-1.1163609292893,-1.65545136752319,29.0025431818502));
#21691=CARTESIAN_POINT('Ctrl Pts',(-1.31824026067784,-1.50595140882999,
28.9879573301493));
#21692=CARTESIAN_POINT('Ctrl Pts',(-1.43693250606842,-1.39314924625441,
28.9785636495392));
#21693=CARTESIAN_POINT('Ctrl Pts',(-1.55383371680727,-1.25102550456506,
28.9671751700723));
#21694=CARTESIAN_POINT('Ctrl Pts',(-1.56685051354219,-1.23468354204676,
28.9658726103616));
#21695=CARTESIAN_POINT('Ctrl Pts',(-1.58437523995888,-1.21195858301741,
28.9640692189897));
#21696=CARTESIAN_POINT('Ctrl Pts',(-1.58910622951228,-1.20574868711128,
28.9635772177295));
#21697=CARTESIAN_POINT('Ctrl Pts',(-1.59658100181716,-1.19581689488158,
28.9627915283571));
#21698=CARTESIAN_POINT('Ctrl Pts',(-1.59934854018609,-1.19211290902519,
28.9624987731733));
#21699=CARTESIAN_POINT('Ctrl Pts',(-1.60499926881264,-1.18449505725215,
28.9618971913992));
#21700=CARTESIAN_POINT('Ctrl Pts',(-1.60788107797538,-1.18058020987352,
28.9615883137886));
#21701=CARTESIAN_POINT('Ctrl Pts',(-1.61450359065645,-1.17151450795343,
28.9608736566693));
#21702=CARTESIAN_POINT('Ctrl Pts',(-1.61823398907472,-1.16635622416048,
28.9604674821747));
#21703=CARTESIAN_POINT('Ctrl Pts',(-1.62987545786151,-1.15009538984348,
28.9591884390637));
#21704=CARTESIAN_POINT('Ctrl Pts',(-1.63769730572518,-1.13892973152651,
28.9583121625329));
#21705=CARTESIAN_POINT('Ctrl Pts',(-1.71507399433766,-1.02602949122731,
28.9494700392553));
#21706=CARTESIAN_POINT('Ctrl Pts',(-1.77516054061037,-0.918155869470301,
28.941143523288));
#21707=CARTESIAN_POINT('Ctrl Pts',(-1.85838563392994,-0.729592615704861,
28.926872576684));
#21708=CARTESIAN_POINT('Ctrl Pts',(-1.88710310707098,-0.65172383881565,
28.9210596919052));
#21709=CARTESIAN_POINT('Ctrl Pts',(-1.91766546543442,-0.549676532124244,
28.9136608865835));
#21710=CARTESIAN_POINT('Ctrl Pts',(-1.92403797609486,-0.526937415471637,
28.9120261167439));
#21711=CARTESIAN_POINT('Ctrl Pts',(-1.93382961471452,-0.489448252179756,
28.9093583934285));
#21712=CARTESIAN_POINT('Ctrl Pts',(-1.9374871849228,-0.474763094905207,
28.9083202475327));
#21713=CARTESIAN_POINT('Ctrl Pts',(-1.95275747153124,-0.41033512349148,
28.9037991070087));
#21714=CARTESIAN_POINT('Ctrl Pts',(-1.96262537178659,-0.360193481078364,
28.9003671221817));
#21715=CARTESIAN_POINT('Ctrl Pts',(-1.97167414499397,-0.302622375618298,
28.8965648626167));
#21716=CARTESIAN_POINT('Ctrl Pts',(-1.97275191725003,-0.295514996350605,
28.8960978494781));
#21717=CARTESIAN_POINT('Ctrl Pts',(-1.97429258291513,-0.284970844872324,
28.8954087084629));
#21718=CARTESIAN_POINT('Ctrl Pts',(-1.97478495940073,-0.2815385407945,28.8951849607858));
#21719=CARTESIAN_POINT('Ctrl Pts',(-1.97564471693772,-0.275432026133444,
28.8947879362226));
#21720=CARTESIAN_POINT('Ctrl Pts',(-1.97601562117872,-0.272758343161151,
28.8946144617332));
#21721=CARTESIAN_POINT('Ctrl Pts',(-1.9767239862926,-0.267574770195167,
28.894278840156));
#21722=CARTESIAN_POINT('Ctrl Pts',(-1.97706209261052,-0.265065006682137,
28.8941166562815));
#21723=CARTESIAN_POINT('Ctrl Pts',(-1.97779457991747,-0.25954837468441,
28.8937608461641));
#21724=CARTESIAN_POINT('Ctrl Pts',(-1.9781868862003,-0.256541230041903,
28.893567336597));
#21725=CARTESIAN_POINT('Ctrl Pts',(-1.97913716695173,-0.249125241262451,
28.8930911874896));
#21726=CARTESIAN_POINT('Ctrl Pts',(-1.97968727218915,-0.244715378902829,
28.892808980054));
#21727=CARTESIAN_POINT('Ctrl Pts',(-1.9823636691879,-0.22266052620991,28.8914020755545));
#21728=CARTESIAN_POINT('Ctrl Pts',(-1.98426889701555,-0.204988836130511,
28.8902891269955));
#21729=CARTESIAN_POINT('Ctrl Pts',(-1.99176151272927,-0.125541967397613,
28.8853404638821));
#21730=CARTESIAN_POINT('Ctrl Pts',(-1.99470237642068,-0.063547662994927,
28.8816269784329));
#21731=CARTESIAN_POINT('Ctrl Pts',(-1.99474942627385,-0.00151290453868526,
28.8779715341069));
#21732=CARTESIAN_POINT('',(-1.99456009906478,-0.000760494884442119,28.0790451186048));
#21733=CARTESIAN_POINT('Ctrl Pts',(-1.99474985500375,-0.000760567235443675,
28.0790451186048));
#21734=CARTESIAN_POINT('Ctrl Pts',(-1.99472090390775,-0.0766909937140657,
28.0838673953792));
#21735=CARTESIAN_POINT('Ctrl Pts',(-1.99035228629733,-0.152487659476892,
28.0886896721536));
#21736=CARTESIAN_POINT('Ctrl Pts',(-1.98171477759731,-0.227671040653933,
28.093511948928));
#21737=CARTESIAN_POINT('Ctrl Pts',(-1.97305323617513,-0.30306360961574,
28.0983476430478));
#21738=CARTESIAN_POINT('Ctrl Pts',(-1.96009914796827,-0.377839146982171,
28.1031833371677));
#21739=CARTESIAN_POINT('Ctrl Pts',(-1.9429741886226,-0.451529472843513,
28.1080190312875));
#21740=CARTESIAN_POINT('Ctrl Pts',(-1.92577546389587,-0.525537218142682,
28.1128755550521));
#21741=CARTESIAN_POINT('Ctrl Pts',(-1.90437000772297,-0.598450062555347,
28.1177320788166));
#21742=CARTESIAN_POINT('Ctrl Pts',(-1.87892964315567,-0.669814122403307,
28.1225886025812));
#21743=CARTESIAN_POINT('Ctrl Pts',(-1.85974397604313,-0.72363281247828,
28.1262511148862));
#21744=CARTESIAN_POINT('Ctrl Pts',(-1.83826454851322,-0.776571052191794,
28.1299136271912));
#21745=CARTESIAN_POINT('Ctrl Pts',(-1.81458234810635,-0.828443398453306,
28.1335761394962));
#21746=CARTESIAN_POINT('Ctrl Pts',(-1.78578205236523,-0.891526173172308,
28.1380301782142));
#21747=CARTESIAN_POINT('Ctrl Pts',(-1.75363125164456,-0.95323025320993,
28.1424842169322));
#21748=CARTESIAN_POINT('Ctrl Pts',(-1.71828444602139,-1.0131762556737,28.1469382556501));
#21749=CARTESIAN_POINT('Ctrl Pts',(-1.682990772139,-1.07303214998177,28.1513855992559));
#21750=CARTESIAN_POINT('Ctrl Pts',(-1.64451087491594,-1.13113479347519,
28.1558329428617));
#21751=CARTESIAN_POINT('Ctrl Pts',(-1.60304648564627,-1.18712658438649,
28.1602802864674));
#21752=CARTESIAN_POINT('Ctrl Pts',(-1.5616309786294,-1.24305236673174,28.1647223871122));
#21753=CARTESIAN_POINT('Ctrl Pts',(-1.51723825751373,-1.29687184739755,
28.169164487757));
#21754=CARTESIAN_POINT('Ctrl Pts',(-1.4701140003193,-1.34825531282661,28.1736065884018));
#21755=CARTESIAN_POINT('Ctrl Pts',(-1.42301946931509,-1.39960636533803,
28.1780458869498));
#21756=CARTESIAN_POINT('Ctrl Pts',(-1.37319715052399,-1.44852409100623,
28.1824851854978));
#21757=CARTESIAN_POINT('Ctrl Pts',(-1.3209327762968,-1.49471206692287,28.1869244840459));
#21758=CARTESIAN_POINT('Ctrl Pts',(-1.2686836111094,-1.54088660204405,28.1913624907489));
#21759=CARTESIAN_POINT('Ctrl Pts',(-1.21399416787632,-1.58433264032543,
28.195800497452));
#21760=CARTESIAN_POINT('Ctrl Pts',(-1.15718548899295,-1.6247920810258,28.2002385041551));
#21761=CARTESIAN_POINT('Ctrl Pts',(-1.10037403838995,-1.66525349575951,
28.2046767273904));
#21762=CARTESIAN_POINT('Ctrl Pts',(-1.04144354700391,-1.70272774155636,
28.2091149506257));
#21763=CARTESIAN_POINT('Ctrl Pts',(-0.980744981797496,-1.73699937915332,
28.213553173861));
#21764=CARTESIAN_POINT('Ctrl Pts',(-0.919982113159806,-1.77130732376818,
28.217996098904));
#21765=CARTESIAN_POINT('Ctrl Pts',(-0.857447859277962,-1.80240564711765,
28.222439023947));
#21766=CARTESIAN_POINT('Ctrl Pts',(-0.793517948224323,-1.83012481223163,
28.2268819489901));
#21767=CARTESIAN_POINT('Ctrl Pts',(-0.729550718650175,-1.85786015816324,
28.2313274675513));
#21768=CARTESIAN_POINT('Ctrl Pts',(-0.664186669228553,-1.88221224874948,
28.2357729861126));
#21769=CARTESIAN_POINT('Ctrl Pts',(-0.597819046438306,-1.90306067959369,
28.2402185046738));
#21770=CARTESIAN_POINT('Ctrl Pts',(-0.531335610293624,-1.92394549153171,
28.2446717807891));
#21771=CARTESIAN_POINT('Ctrl Pts',(-0.463845579006982,-1.94131431711732,
28.2491250569043));
#21772=CARTESIAN_POINT('Ctrl Pts',(-0.395754024367098,-1.95509752050818,
28.2535783330196));
#21773=CARTESIAN_POINT('Ctrl Pts',(-0.359292954951652,-1.96247802956337,
28.2559629343174));
#21774=CARTESIAN_POINT('Ctrl Pts',(-0.322659533583422,-1.96883132014021,
28.2583475356152));
#21775=CARTESIAN_POINT('Ctrl Pts',(-0.285916359981321,-1.97415283035408,
28.260732136913));
#21776=CARTESIAN_POINT('Ctrl Pts',(-0.217286221267569,-1.98409252658445,
28.265186175631));
#21777=CARTESIAN_POINT('Ctrl Pts',(-0.148001227391612,-1.99046881891421,
28.2696402143489));
#21778=CARTESIAN_POINT('Ctrl Pts',(-0.0784639955463822,-1.99320620205309,
28.2740942530669));
#21779=CARTESIAN_POINT('Ctrl Pts',(-0.00903128896481908,-1.9959394704798,
28.2785415966727));
#21780=CARTESIAN_POINT('Ctrl Pts',(0.0606524178666762,-1.99504466690194,
28.2829889402785));
#21781=CARTESIAN_POINT('Ctrl Pts',(0.130177248859435,-1.99049778858942,
28.2874362838842));
#21782=CARTESIAN_POINT('Ctrl Pts',(0.199620117222928,-1.98595627057906,
28.291878384529));
#21783=CARTESIAN_POINT('Ctrl Pts',(0.268903995586189,-1.97777126073603,
28.2963204851738));
#21784=CARTESIAN_POINT('Ctrl Pts',(0.337618661805003,-1.96597080387807,
28.3007625858186));
#21785=CARTESIAN_POINT('Ctrl Pts',(0.406289982507969,-1.95417779080057,
28.3052018843666));
#21786=CARTESIAN_POINT('Ctrl Pts',(0.474392321983942,-1.93877393764083,
28.3096411829146));
#21787=CARTESIAN_POINT('Ctrl Pts',(0.541521761563122,-1.9198389891482,28.3140804814626));
#21788=CARTESIAN_POINT('Ctrl Pts',(0.608631666338052,-1.90090955076432,
28.3185184881657));
#21789=CARTESIAN_POINT('Ctrl Pts',(0.674768762310941,-1.87845118974319,
28.3229564948688));
#21790=CARTESIAN_POINT('Ctrl Pts',(0.739542233185855,-1.85259408609508,
28.3273945015718));
#21791=CARTESIAN_POINT('Ctrl Pts',(0.804318864386049,-1.82673572086786,
28.3318327248071));
#21792=CARTESIAN_POINT('Ctrl Pts',(0.867731284613089,-1.79747846751092,
28.3362709480424));
#21793=CARTESIAN_POINT('Ctrl Pts',(0.929408344014541,-1.76500076276928,
28.3407091712778));
#21794=CARTESIAN_POINT('Ctrl Pts',(0.991150743453881,-1.73248865148364,
28.3451520963208));
#21795=CARTESIAN_POINT('Ctrl Pts',(1.05115367862411,-1.69674950775209,28.3495950213638));
#21796=CARTESIAN_POINT('Ctrl Pts',(1.10907118641276,-1.65800743845406,28.3540379464068));
#21797=CARTESIAN_POINT('Ctrl Pts',(1.16702250303466,-1.61924275381551,28.3584834649681));
#21798=CARTESIAN_POINT('Ctrl Pts',(1.22288557708541,-1.57747194785833,28.3629289835293));
#21799=CARTESIAN_POINT('Ctrl Pts',(1.2763462693605,-1.5329604571513,28.3673745020906));
#21800=CARTESIAN_POINT('Ctrl Pts',(1.32990025203595,-1.48837129265046,28.3718277782058));
#21801=CARTESIAN_POINT('Ctrl Pts',(1.3810431252692,-1.44103222904822,28.3762810543211));
#21802=CARTESIAN_POINT('Ctrl Pts',(1.42949703153687,-1.39124613182833,28.3807343304363));
#21803=CARTESIAN_POINT('Ctrl Pts',(1.45544270496476,-1.36458710845505,28.3831189317341));
#21804=CARTESIAN_POINT('Ctrl Pts',(1.48061805011818,-1.33722703062777,28.3855035330319));
#21805=CARTESIAN_POINT('Ctrl Pts',(1.50498533932892,-1.30921605967274,28.3878881343298));
#21806=CARTESIAN_POINT('Ctrl Pts',(1.55049938383449,-1.25689622353235,28.3923421730477));
#21807=CARTESIAN_POINT('Ctrl Pts',(1.59337201604558,-1.20209654390236,28.3967962117657));
#21808=CARTESIAN_POINT('Ctrl Pts',(1.63332177260354,-1.145114644758,28.4012502504837));
#21809=CARTESIAN_POINT('Ctrl Pts',(1.67321147847031,-1.08821839826146,28.4056975940895));
#21810=CARTESIAN_POINT('Ctrl Pts',(1.71018675001396,-1.02914684025344,28.4101449376952));
#21811=CARTESIAN_POINT('Ctrl Pts',(1.74400549498859,-0.968231581776595,
28.414592281301));
#21812=CARTESIAN_POINT('Ctrl Pts',(1.77778437113911,-0.907388136128027,
28.4190343819458));
#21813=CARTESIAN_POINT('Ctrl Pts',(1.80841387505166,-0.844705732877582,
28.4234764825906));
#21814=CARTESIAN_POINT('Ctrl Pts',(1.83569548648917,-0.780544453175667,
28.4279185832353));
#21815=CARTESIAN_POINT('Ctrl Pts',(1.86295988856532,-0.716423646693214,
28.4323578817834));
#21816=CARTESIAN_POINT('Ctrl Pts',(1.8868803965012,-0.650826263861637,28.4367971803314));
#21817=CARTESIAN_POINT('Ctrl Pts',(1.90730536994191,-0.58413507709326,28.4412364788794));
#21818=CARTESIAN_POINT('Ctrl Pts',(1.92772439967357,-0.51746329759665,28.4456744855825));
#21819=CARTESIAN_POINT('Ctrl Pts',(1.94464977094004,-0.449698813897798,
28.4501124922855));
#21820=CARTESIAN_POINT('Ctrl Pts',(1.9579793409919,-0.381240688737356,28.4545504989886));
#21821=CARTESIAN_POINT('Ctrl Pts',(1.97130956139916,-0.312779223475779,
28.4589887222239));
#21822=CARTESIAN_POINT('Ctrl Pts',(1.98104354105954,-0.243624530554679,
28.4634269454592));
#21823=CARTESIAN_POINT('Ctrl Pts',(1.98713035708185,-0.174185264772244,
28.4678651686945));
#21824=CARTESIAN_POINT('Ctrl Pts',(1.993223621414,-0.104672435750919,28.4723080937375));
#21825=CARTESIAN_POINT('Ctrl Pts',(1.99566196737844,-0.0348749208047779,
28.4767510187806));
#21826=CARTESIAN_POINT('Ctrl Pts',(1.9944465059925,0.0347950748572986,28.4811939438236));
#21827=CARTESIAN_POINT('Ctrl Pts',(1.99323033509171,0.104505739763558,28.4856394623848));
#21828=CARTESIAN_POINT('Ctrl Pts',(1.98835614581087,0.174088248712013,28.4900849809461));
#21829=CARTESIAN_POINT('Ctrl Pts',(1.97987702725532,0.24313477630037,28.4945304995074));
#21830=CARTESIAN_POINT('Ctrl Pts',(1.9713831124012,0.312301792006778,28.4989837756226));
#21831=CARTESIAN_POINT('Ctrl Pts',(1.95927179597492,0.380930477260881,28.5034370517378));
#21832=CARTESIAN_POINT('Ctrl Pts',(1.94364727905563,0.448623246298778,28.5078903278531));
#21833=CARTESIAN_POINT('Ctrl Pts',(1.93528079955626,0.484870777492008,28.5102749291509));
#21834=CARTESIAN_POINT('Ctrl Pts',(1.92590783839721,0.520850208579681,28.5126595304487));
#21835=CARTESIAN_POINT('Ctrl Pts',(1.91555014288437,0.556502661804665,28.5150441317464));
#21836=CARTESIAN_POINT('Ctrl Pts',(1.89620368992137,0.62309551621691,28.5194981704644));
#21837=CARTESIAN_POINT('Ctrl Pts',(1.87334219798095,0.688810200013788,28.5239522091824));
#21838=CARTESIAN_POINT('Ctrl Pts',(1.84706350906263,0.753248933613074,28.5284062479004));
#21839=CARTESIAN_POINT('Ctrl Pts',(1.82082432109675,0.817590805783743,28.5328535915062));
#21840=CARTESIAN_POINT('Ctrl Pts',(1.79117831434442,0.880660084793923,28.5373009351119));
#21841=CARTESIAN_POINT('Ctrl Pts',(1.75827322167461,0.942073691619719,28.5417482787177));
#21842=CARTESIAN_POINT('Ctrl Pts',(1.72540692072673,1.00341489811577,28.5461903793625));
#21843=CARTESIAN_POINT('Ctrl Pts',(1.68928939490203,1.06310387964073,28.5506324800073));
#21844=CARTESIAN_POINT('Ctrl Pts',(1.65011590392848,1.12077877661129,28.555074580652));
#21845=CARTESIAN_POINT('Ctrl Pts',(1.61096712376658,1.17841729200133,28.5595138792001));
#21846=CARTESIAN_POINT('Ctrl Pts',(1.56876647703001,1.23404383916435,28.5639531777481));
#21847=CARTESIAN_POINT('Ctrl Pts',(1.52375368261948,1.28732368781265,28.5683924762961));
#21848=CARTESIAN_POINT('Ctrl Pts',(1.47875398702419,1.34058803191603,28.5728304829992));
#21849=CARTESIAN_POINT('Ctrl Pts',(1.43094408406991,1.39150665938169,28.5772684897022));
#21850=CARTESIAN_POINT('Ctrl Pts',(1.38060418746342,1.43977763562936,28.5817064964053));
#21851=CARTESIAN_POINT('Ctrl Pts',(1.3302618347519,1.48805096703855,28.5861447196406));
#21852=CARTESIAN_POINT('Ctrl Pts',(1.2773895983274,1.53367605365235,28.5905829428759));
#21853=CARTESIAN_POINT('Ctrl Pts',(1.22230348752928,1.57638883111806,28.5950211661112));
#21854=CARTESIAN_POINT('Ctrl Pts',(1.16715901907598,1.61914685805777,28.5994640911542));
#21855=CARTESIAN_POINT('Ctrl Pts',(1.1097963826876,1.65898611721601,28.6039070161973));
#21856=CARTESIAN_POINT('Ctrl Pts',(1.05056274451245,1.69568436990569,28.6083499412403));
#21857=CARTESIAN_POINT('Ctrl Pts',(0.991294529224582,1.73240404487601,28.6127954598015));
#21858=CARTESIAN_POINT('Ctrl Pts',(0.930153567536852,1.76597882822019,28.6172409783628));
#21859=CARTESIAN_POINT('Ctrl Pts',(0.867511484794862,1.79623255349885,28.6216864969241));
#21860=CARTESIAN_POINT('Ctrl Pts',(0.804760089869839,1.82653907237266,28.6261397730393));
#21861=CARTESIAN_POINT('Ctrl Pts',(0.740502796257915,1.85351277517669,28.6305930491545));
#21862=CARTESIAN_POINT('Ctrl Pts',(0.675130292879802,1.87702601210959,28.6350463252698));
#21863=CARTESIAN_POINT('Ctrl Pts',(0.640125197223682,1.88961667432212,28.6374309265676));
#21864=CARTESIAN_POINT('Ctrl Pts',(0.604800587654434,1.90121597693428,28.6398155278654));
#21865=CARTESIAN_POINT('Ctrl Pts',(0.56921774033835,1.91181032704191,28.6422001291632));
#21866=CARTESIAN_POINT('Ctrl Pts',(0.502754898190598,1.9315988114374,28.6466541678812));
#21867=CARTESIAN_POINT('Ctrl Pts',(0.435127300851099,1.94795654839455,28.6511082065992));
#21868=CARTESIAN_POINT('Ctrl Pts',(0.366722357313723,1.96075043673239,28.6555622453172));
#21869=CARTESIAN_POINT('Ctrl Pts',(0.298420237034797,1.97352509386824,28.6600095889229));
#21870=CARTESIAN_POINT('Ctrl Pts',(0.229343566979604,1.982746445467,28.6644569325287));
#21871=CARTESIAN_POINT('Ctrl Pts',(0.159894408044754,1.98833129552799,28.6689042761344));
#21872=CARTESIAN_POINT('Ctrl Pts',(0.0905271225295731,1.99390956162483,
28.6733463767792));
#21873=CARTESIAN_POINT('Ctrl Pts',(0.0207887059247658,1.99585980177506,
28.677788477424));
#21874=CARTESIAN_POINT('Ctrl Pts',(-0.0489108896728576,1.99415026699881,
28.6822305780688));
#21875=CARTESIAN_POINT('Ctrl Pts',(-0.118566518456798,1.99244181060466,
28.6866698766168));
#21876=CARTESIAN_POINT('Ctrl Pts',(-0.18818288653511,1.98707817099578,28.6911091751649));
#21877=CARTESIAN_POINT('Ctrl Pts',(-0.257348780247559,1.97807966669826,
28.6955484737129));
#21878=CARTESIAN_POINT('Ctrl Pts',(-0.326494546543439,1.96908378098389,
28.6999864804159));
#21879=CARTESIAN_POINT('Ctrl Pts',(-0.395189613484428,1.95645519351512,
28.704424487119));
#21880=CARTESIAN_POINT('Ctrl Pts',(-0.463028416280303,1.94026602511536,
28.7088624938221));
#21881=CARTESIAN_POINT('Ctrl Pts',(-0.530870528960365,1.92407606683915,
28.7133007170574));
#21882=CARTESIAN_POINT('Ctrl Pts',(-0.597855818918246,1.90432529869434,
28.7177389402927));
#21883=CARTESIAN_POINT('Ctrl Pts',(-0.663591180862934,1.88113644034157,
28.722177163528));
#21884=CARTESIAN_POINT('Ctrl Pts',(-0.729396182169134,1.85792301595246,
28.726620088571));
#21885=CARTESIAN_POINT('Ctrl Pts',(-0.793948149902581,1.83126439473065,
28.7310630136141));
#21886=CARTESIAN_POINT('Ctrl Pts',(-0.856872275349802,1.80133213656917,
28.7355059386571));
#21887=CARTESIAN_POINT('Ctrl Pts',(-0.919833132199041,1.77138240571657,
28.7399514572184));
#21888=CARTESIAN_POINT('Ctrl Pts',(-0.981163824840807,1.73815546765738,
28.7443969757796));
#21889=CARTESIAN_POINT('Ctrl Pts',(-1.04051503765132,1.70186839059942,28.7488424943409));
#21890=CARTESIAN_POINT('Ctrl Pts',(-1.09996981998501,1.66551799157902,28.7532957704561));
#21891=CARTESIAN_POINT('Ctrl Pts',(-1.15743782352383,1.62609707080648,28.7577490465713));
#21892=CARTESIAN_POINT('Ctrl Pts',(-1.21260020212703,1.58386499181638,28.7622023226866));
#21893=CARTESIAN_POINT('Ctrl Pts',(-1.2421380695763,1.56125092797605,28.7645869239844));
#21894=CARTESIAN_POINT('Ctrl Pts',(-1.27101543260124,1.53783149657783,28.7669715252822));
#21895=CARTESIAN_POINT('Ctrl Pts',(-1.29918768722305,1.51365085666016,28.76935612658));
#21896=CARTESIAN_POINT('Ctrl Pts',(-1.35318319536139,1.46730575730648,28.7739265012451));
#21897=CARTESIAN_POINT('Ctrl Pts',(-1.40482250508354,1.41795863007694,28.7784968759102));
#21898=CARTESIAN_POINT('Ctrl Pts',(-1.45374853911666,1.36588533468816,28.7830672505753));
#21899=CARTESIAN_POINT('Ctrl Pts',(-1.50065853549726,1.31595776245616,28.7874492991765));
#21900=CARTESIAN_POINT('Ctrl Pts',(-1.54507405645156,1.26352467347088,28.7918313477777));
#21901=CARTESIAN_POINT('Ctrl Pts',(-1.58671329490916,1.20887074671302,28.7962133963789));
#21902=CARTESIAN_POINT('Ctrl Pts',(-1.62831315497145,1.15426850639357,28.8005913008591));
#21903=CARTESIAN_POINT('Ctrl Pts',(-1.66714163101419,1.0974499897678,28.8049692053393));
#21904=CARTESIAN_POINT('Ctrl Pts',(-1.70295563913342,1.03873464062949,28.8093471098196));
#21905=CARTESIAN_POINT('Ctrl Pts',(-1.73874877114827,0.980053516863378,
28.8137224624047));
#21906=CARTESIAN_POINT('Ctrl Pts',(-1.77153065696791,0.919478183176294,
28.8180978149899));
#21907=CARTESIAN_POINT('Ctrl Pts',(-1.8011013554795,0.857357259134092,28.822473167575));
#21908=CARTESIAN_POINT('Ctrl Pts',(-1.83066554242213,0.795250014331845,
28.8268475566925));
#21909=CARTESIAN_POINT('Ctrl Pts',(-1.85701973001042,0.73159831112045,28.8312219458101));
#21910=CARTESIAN_POINT('Ctrl Pts',(-1.88001071204681,0.666773788543948,
28.8355963349276));
#21911=CARTESIAN_POINT('Ctrl Pts',(-1.90301678880371,0.601906705451793,
28.8399735960487));
#21912=CARTESIAN_POINT('Ctrl Pts',(-1.9226550823902,0.535865742243995,28.8443508571697));
#21913=CARTESIAN_POINT('Ctrl Pts',(-1.93882166625638,0.4690395601171,28.8487281182908));
#21914=CARTESIAN_POINT('Ctrl Pts',(-1.95499461229697,0.402187079309592,
28.8531071020329));
#21915=CARTESIAN_POINT('Ctrl Pts',(-1.96769303523254,0.334549260828964,
28.8574860857751));
#21916=CARTESIAN_POINT('Ctrl Pts',(-1.97686429343349,0.266524159970012,
28.8618650695173));
#21917=CARTESIAN_POINT('Ctrl Pts',(-1.98604794688615,0.198407120989854,
28.8662499715974));
#21918=CARTESIAN_POINT('Ctrl Pts',(-1.99169488580679,0.129902258227077,
28.8706348736776));
#21919=CARTESIAN_POINT('Ctrl Pts',(-1.99380447786887,0.0614106385737057,
28.8750197757577));
#21920=CARTESIAN_POINT('Ctrl Pts',(-1.99445001346885,0.0404521890321277,
28.8763615566859));
#21921=CARTESIAN_POINT('Ctrl Pts',(-1.99476469430693,0.0194949600558917,
28.8777033376141));
#21922=CARTESIAN_POINT('Ctrl Pts',(-1.99474947325114,-0.00144964281222297,
28.8790451185423));
#21923=CARTESIAN_POINT('',(-1.99382862437974,0.00178311505610039,27.2790451186048));
#21924=CARTESIAN_POINT('Ctrl Pts',(-1.99382862437974,0.00178311505610039,
27.2790451186048));
#21925=CARTESIAN_POINT('Ctrl Pts',(-1.9897025744846,-0.476968105037969,
27.3095767974018));
#21926=CARTESIAN_POINT('Ctrl Pts',(-1.57649467124548,-1.62673224728373,
27.3824938086711));
#21927=CARTESIAN_POINT('Ctrl Pts',(0.346093998518022,-2.33304570413791,
27.4977961524125));
#21928=CARTESIAN_POINT('Ctrl Pts',(2.1489051180945,-0.97215744961082,27.6249521498293));
#21929=CARTESIAN_POINT('Ctrl Pts',(1.98079137716424,1.28037058446309,27.752108147246));
#21930=CARTESIAN_POINT('Ctrl Pts',(-0.00405728419479211,2.35857305416888,
27.8792641446628));
#21931=CARTESIAN_POINT('Ctrl Pts',(-1.70198164629091,1.42865299045872,27.9882431351157));
#21932=CARTESIAN_POINT('Ctrl Pts',(-1.99043493990472,0.379843564099569,
28.0548367930963));
#21933=CARTESIAN_POINT('Ctrl Pts',(-1.99173494636544,-0.000759417697459401,
28.0790451186048));
#21934=CARTESIAN_POINT('',(-1.99474927319053,-0.00170282290822489,25.6790451186048));
#21935=CARTESIAN_POINT('Ctrl Pts',(-1.99474916919083,0.00182058025913,27.2795743230551));
#21936=CARTESIAN_POINT('Ctrl Pts',(-1.99460679985945,0.157809916119892,
27.2687736719809));
#21937=CARTESIAN_POINT('Ctrl Pts',(-1.97616814764425,0.31325218485814,27.257698223344));
#21938=CARTESIAN_POINT('Ctrl Pts',(-1.9366719416301,0.478026890473197,27.2464400873559));
#21939=CARTESIAN_POINT('Ctrl Pts',(-1.93340965083876,0.49105504968079,27.2455536757105));
#21940=CARTESIAN_POINT('Ctrl Pts',(-1.92837363507333,0.510338051726765,
27.2442482324704));
#21941=CARTESIAN_POINT('Ctrl Pts',(-1.92670058705654,0.516618480185472,
27.2438240871158));
#21942=CARTESIAN_POINT('Ctrl Pts',(-1.92359632482327,0.528046671149623,
27.2430543177036));
#21943=CARTESIAN_POINT('Ctrl Pts',(-1.92217507498526,0.533197046587033,
27.2427081563871));
#21944=CARTESIAN_POINT('Ctrl Pts',(-1.91990197759731,0.541307161942427,
27.2421643244256));
#21945=CARTESIAN_POINT('Ctrl Pts',(-1.91906395256792,0.544270698662273,
27.2419658665239));
#21946=CARTESIAN_POINT('Ctrl Pts',(-1.91747880769462,0.549827123364246,
27.2415942849693));
#21947=CARTESIAN_POINT('Ctrl Pts',(-1.916733298736,0.552420406188063,27.2414210732377));
#21948=CARTESIAN_POINT('Ctrl Pts',(-1.91502036904709,0.558333687439218,
27.2410265859094));
#21949=CARTESIAN_POINT('Ctrl Pts',(-1.91404957783869,0.56165268130021,27.2408055095512));
#21950=CARTESIAN_POINT('Ctrl Pts',(-1.91104766060861,0.57181762234811,27.2401294254953));
#21951=CARTESIAN_POINT('Ctrl Pts',(-1.90898837277144,0.578655295219941,
27.2396760308093));
#21952=CARTESIAN_POINT('Ctrl Pts',(-1.89229171892375,0.633035665688997,
27.2360801415041));
#21953=CARTESIAN_POINT('Ctrl Pts',(-1.87591589196118,0.680031342406879,
27.233033363773));
#21954=CARTESIAN_POINT('Ctrl Pts',(-1.85116402537216,0.743337907443125,
27.2289504846696));
#21955=CARTESIAN_POINT('Ctrl Pts',(-1.84429744256836,0.760214751048216,
27.2278641730061));
#21956=CARTESIAN_POINT('Ctrl Pts',(-1.80294357986268,0.857995667637109,
27.2215701409892));
#21957=CARTESIAN_POINT('Ctrl Pts',(-1.76336597820338,0.93664501430885,27.2165031169297));
#21958=CARTESIAN_POINT('Ctrl Pts',(-1.68864944448531,1.06348579843691,27.2079559484914));
#21959=CARTESIAN_POINT('Ctrl Pts',(-1.65631440973545,1.11317614552078,27.2045027073776));
#21960=CARTESIAN_POINT('Ctrl Pts',(-1.57672341043266,1.22432420945706,27.1964089487888));
#21961=CARTESIAN_POINT('Ctrl Pts',(-1.5280056341374,1.2846101233949,27.1917349277779));
#21962=CARTESIAN_POINT('Ctrl Pts',(-1.46531419190174,1.35356196891362,27.1859368631662));
#21963=CARTESIAN_POINT('Ctrl Pts',(-1.45458015558808,1.36509055859065,27.1849512328303));
#21964=CARTESIAN_POINT('Ctrl Pts',(-1.44005880385412,1.38032105497168,27.1836266436172));
#21965=CARTESIAN_POINT('Ctrl Pts',(-1.43639145787625,1.38413697018114,27.1832928559376));
#21966=CARTESIAN_POINT('Ctrl Pts',(-1.42956740734128,1.39118114440309,27.1826730875579));
#21967=CARTESIAN_POINT('Ctrl Pts',(-1.42641483695275,1.39441337524033,27.1823872877461));
#21968=CARTESIAN_POINT('Ctrl Pts',(-1.41986715172456,1.40108106942304,27.1817947560018));
#21969=CARTESIAN_POINT('Ctrl Pts',(-1.41647048159474,1.40451495746349,27.1814879567318));
#21970=CARTESIAN_POINT('Ctrl Pts',(-1.40874079147721,1.41227278397408,27.1807910766158));
#21971=CARTESIAN_POINT('Ctrl Pts',(-1.40440028780705,1.41658916562026,27.1804006654354));
#21972=CARTESIAN_POINT('Ctrl Pts',(-1.39316664946732,1.42765799821397,27.1793925385091));
#21973=CARTESIAN_POINT('Ctrl Pts',(-1.38624432530855,1.43438047189903,27.1787735191574));
#21974=CARTESIAN_POINT('Ctrl Pts',(-1.34363916263484,1.47515912622825,27.1749766115967));
#21975=CARTESIAN_POINT('Ctrl Pts',(-1.3067548080363,1.50792964144487,27.1717440914835));
#21976=CARTESIAN_POINT('Ctrl Pts',(-1.23917019810692,1.56363321087344,27.1659089241363));
#21977=CARTESIAN_POINT('Ctrl Pts',(-1.20895134501141,1.58711308664897,27.1633289037337));
#21978=CARTESIAN_POINT('Ctrl Pts',(-1.10163276113008,1.66565502008231,27.1542712093847));
#21979=CARTESIAN_POINT('Ctrl Pts',(-1.02130482323748,1.71608140769274,27.1476655744769));
#21980=CARTESIAN_POINT('Ctrl Pts',(-0.872022788501079,1.79558954503728,
27.1358663647506));
#21981=CARTESIAN_POINT('Ctrl Pts',(-0.804430309719816,1.82687127517369,
27.1306847785493));
#21982=CARTESIAN_POINT('Ctrl Pts',(-0.707129944025984,1.86545155570333,
27.1235715257642));
#21983=CARTESIAN_POINT('Ctrl Pts',(-0.678763766444861,1.87595901448863,
27.1215378019557));
#21984=CARTESIAN_POINT('Ctrl Pts',(-0.633669838145158,1.89150591951069,
27.1183788083664));
#21985=CARTESIAN_POINT('Ctrl Pts',(-0.617096991088353,1.89697745426736,
27.1172333335376));
#21986=CARTESIAN_POINT('Ctrl Pts',(-0.595738540309857,1.90371941289554,
27.1157788054274));
#21987=CARTESIAN_POINT('Ctrl Pts',(-0.591017709481509,1.90519030015296,
27.1154586657663));
#21988=CARTESIAN_POINT('Ctrl Pts',(-0.583432496204787,1.90752274718303,
27.1149465036827));
#21989=CARTESIAN_POINT('Ctrl Pts',(-0.580571598435654,1.90839543282521,
27.1147538390233));
#21990=CARTESIAN_POINT('Ctrl Pts',(-0.57510695190225,1.91004893794979,27.1143868076051));
#21991=CARTESIAN_POINT('Ctrl Pts',(-0.572503601830494,1.91083086050498,
27.1142123801221));
#21992=CARTESIAN_POINT('Ctrl Pts',(-0.566490368498008,1.91262355770618,
27.1138104559202));
#21993=CARTESIAN_POINT('Ctrl Pts',(-0.563079375545609,1.9136305360251,27.1135831827497));
#21994=CARTESIAN_POINT('Ctrl Pts',(-0.552127353515837,1.91683192529738,
27.1128556991488));
#21995=CARTESIAN_POINT('Ctrl Pts',(-0.544575933696427,1.9189909592504,27.112357509485));
#21996=CARTESIAN_POINT('Ctrl Pts',(-0.443617997709538,1.94721200556986,
27.1057400168433));
#21997=CARTESIAN_POINT('Ctrl Pts',(-0.348430252232567,1.9664774098224,27.0999883637565));
#21998=CARTESIAN_POINT('Ctrl Pts',(-0.0721855841925019,2.00168696613813,
27.0837221410369));
#21999=CARTESIAN_POINT('Ctrl Pts',(0.110105217391063,1.99995861702493,27.0734183590793));
#22000=CARTESIAN_POINT('Ctrl Pts',(0.306738966596962,1.97110049161639,27.0611718749675));
#22001=CARTESIAN_POINT('Ctrl Pts',(0.323795820453936,1.9683704376302,27.0601009726926));
#22002=CARTESIAN_POINT('Ctrl Pts',(0.353735505063498,1.96317872925446,27.0582049368789));
#22003=CARTESIAN_POINT('Ctrl Pts',(0.366633679381107,1.96081086865013,27.0573827662986));
#22004=CARTESIAN_POINT('Ctrl Pts',(0.385654884983612,1.9571246981102,27.0561620208309));
#22005=CARTESIAN_POINT('Ctrl Pts',(0.391796739459875,1.95590441682651,27.0557665693331));
#22006=CARTESIAN_POINT('Ctrl Pts',(0.402699531751236,1.95368480420153,27.0550622630596));
#22007=CARTESIAN_POINT('Ctrl Pts',(0.407462772644021,1.95269693379777,27.0547537766876));
#22008=CARTESIAN_POINT('Ctrl Pts',(0.416738749694144,1.95073772843451,27.0541514728172));
#22009=CARTESIAN_POINT('Ctrl Pts',(0.421251824923678,1.94976813237951,27.0538577127876));
#22010=CARTESIAN_POINT('Ctrl Pts',(0.433349820505624,1.94712501583074,27.0530682923024));
#22011=CARTESIAN_POINT('Ctrl Pts',(0.440928339461058,1.94542285656315,27.0525717161052));
#22012=CARTESIAN_POINT('Ctrl Pts',(0.4685984680652,1.93903806999769,27.0507509835917));
#22013=CARTESIAN_POINT('Ctrl Pts',(0.488626475890427,1.93408822835178,27.0494182754833));
#22014=CARTESIAN_POINT('Ctrl Pts',(0.671058754418088,1.88598638384895,27.0371383524665));
#22015=CARTESIAN_POINT('Ctrl Pts',(0.827447741541594,1.82279224832791,27.025501814765));
#22016=CARTESIAN_POINT('Ctrl Pts',(1.03861266980297,1.70463717140479,27.0086216873806));
#22017=CARTESIAN_POINT('Ctrl Pts',(1.1011370423934,1.66493320945291,27.0034697841364));
#22018=CARTESIAN_POINT('Ctrl Pts',(1.19763801000848,1.59583419625229,26.995404636848));
#22019=CARTESIAN_POINT('Ctrl Pts',(1.23308217854283,1.56860850895439,26.9924161919143));
#22020=CARTESIAN_POINT('Ctrl Pts',(1.272664747017,1.53603231929917,26.9890754019891));
#22021=CARTESIAN_POINT('Ctrl Pts',(1.27772389726021,1.53182652071015,26.988648345017));
#22022=CARTESIAN_POINT('Ctrl Pts',(1.28532359894526,1.52544485158716,26.9880068601596));
#22023=CARTESIAN_POINT('Ctrl Pts',(1.28787957481,1.52328754686328,26.9877911169253));
#22024=CARTESIAN_POINT('Ctrl Pts',(1.29228366208294,1.51955138356075,26.987419405886));
#22025=CARTESIAN_POINT('Ctrl Pts',(1.2941343169128,1.51797557311783,26.9872632169682));
#22026=CARTESIAN_POINT('Ctrl Pts',(1.29831035626929,1.51440653768285,26.9869107965521));
#22027=CARTESIAN_POINT('Ctrl Pts',(1.30063402763084,1.51241134254242,26.9867147133901));
#22028=CARTESIAN_POINT('Ctrl Pts',(1.30694051471286,1.50697106295087,26.9861825485773));
#22029=CARTESIAN_POINT('Ctrl Pts',(1.31091433360489,1.50351551539601,26.9858472322528));
#22030=CARTESIAN_POINT('Ctrl Pts',(1.32901417061324,1.48764997402661,26.9843197336432));
#22031=CARTESIAN_POINT('Ctrl Pts',(1.34297853469373,1.47505587292216,26.9831406530443));
#22032=CARTESIAN_POINT('Ctrl Pts',(1.36414978678315,1.4554121245445,26.9813482976862));
#22033=CARTESIAN_POINT('Ctrl Pts',(1.37148435928995,1.44850259010828,26.9807264521344));
#22034=CARTESIAN_POINT('Ctrl Pts',(1.5219094480837,1.30462770661271,26.9679463144279));
#22035=CARTESIAN_POINT('Ctrl Pts',(1.64387870841392,1.1471472277165,26.9569813693188));
#22036=CARTESIAN_POINT('Ctrl Pts',(1.76534526605985,0.930129337140123,26.942193020355));
#22037=CARTESIAN_POINT('Ctrl Pts',(1.78835387866926,0.88508435395895,26.9391457441888));
#22038=CARTESIAN_POINT('Ctrl Pts',(1.82237676931385,0.811719859633889,26.934180849798));
#22039=CARTESIAN_POINT('Ctrl Pts',(1.83449937217942,0.783937573250285,26.9323004557604));
#22040=CARTESIAN_POINT('Ctrl Pts',(1.84927073273663,0.747863995754283,26.9298540673233));
#22041=CARTESIAN_POINT('Ctrl Pts',(1.85250518945258,0.739815732682226,26.9293079645264));
#22042=CARTESIAN_POINT('Ctrl Pts',(1.85764171375973,0.726789666378497,26.9284235172365));
#22043=CARTESIAN_POINT('Ctrl Pts',(1.85957653018366,0.721824828712571,26.9280862775469));
#22044=CARTESIAN_POINT('Ctrl Pts',(1.86323233010537,0.712331604214012,26.9274411592409));
#22045=CARTESIAN_POINT('Ctrl Pts',(1.86495675816197,0.707804577420693,26.9271333989234));
#22046=CARTESIAN_POINT('Ctrl Pts',(1.86886548573625,0.697429800048986,26.9264277881906));
#22047=CARTESIAN_POINT('Ctrl Pts',(1.87103885145382,0.691578010537166,26.9260295755416));
#22048=CARTESIAN_POINT('Ctrl Pts',(1.87765064034761,0.673516453456321,26.9247997576797));
#22049=CARTESIAN_POINT('Ctrl Pts',(1.8819972083418,0.661273645922266,26.9239651081388));
#22050=CARTESIAN_POINT('Ctrl Pts',(1.92763843406612,0.528621935544873,26.9149090043765));
#22051=CARTESIAN_POINT('Ctrl Pts',(1.95742857562902,0.404590235290474,26.9063005177591));
#22052=CARTESIAN_POINT('Ctrl Pts',(1.99691470390854,0.12463226314581,26.8867069778729));
#22053=CARTESIAN_POINT('Ctrl Pts',(2.00055582696806,-0.0313380870244883,
26.8756739806269));
#22054=CARTESIAN_POINT('Ctrl Pts',(1.98435228346906,-0.204212107640017,
26.8641661205944));
#22055=CARTESIAN_POINT('Ctrl Pts',(1.98241324781325,-0.222248378817915,
26.8629749732254));
#22056=CARTESIAN_POINT('Ctrl Pts',(1.97962995826503,-0.245188652906416,
26.8614741712327));
#22057=CARTESIAN_POINT('Ctrl Pts',(1.97901311340757,-0.250118662688979,
26.8611524780768));
#22058=CARTESIAN_POINT('Ctrl Pts',(1.97799474047609,-0.258018113938238,
26.8606384235504));
#22059=CARTESIAN_POINT('Ctrl Pts',(1.97760493531469,-0.260989004714034,
26.8604454116184));
#22060=CARTESIAN_POINT('Ctrl Pts',(1.97684894350177,-0.26665182818081,26.8600781319914));
#22061=CARTESIAN_POINT('Ctrl Pts',(1.97648395620222,-0.269343858014512,
26.8599038018848));
#22062=CARTESIAN_POINT('Ctrl Pts',(1.97562989414417,-0.275547921533612,
26.8595026492185));
#22063=CARTESIAN_POINT('Ctrl Pts',(1.9751369539273,-0.279059401208969,26.8592760474144));
#22064=CARTESIAN_POINT('Ctrl Pts',(1.97378961891658,-0.28847476144236,26.8586696185915));
#22065=CARTESIAN_POINT('Ctrl Pts',(1.97291809153942,-0.294376211637407,
26.8582907402236));
#22066=CARTESIAN_POINT('Ctrl Pts',(1.96638433329972,-0.337286064338147,
26.8555442252955));
#22067=CARTESIAN_POINT('Ctrl Pts',(1.95970723516138,-0.37413530337609,26.8532307589938));
#22068=CARTESIAN_POINT('Ctrl Pts',(1.93448831525661,-0.493974477653454,
26.8457909822654));
#22069=CARTESIAN_POINT('Ctrl Pts',(1.91167774270641,-0.575974372203325,
26.8408310162175));
#22070=CARTESIAN_POINT('Ctrl Pts',(1.85054944419298,-0.751430752443487,
26.8300419323936));
#22071=CARTESIAN_POINT('Ctrl Pts',(1.81023517969291,-0.843936550597181,
26.8242331946577));
#22072=CARTESIAN_POINT('Ctrl Pts',(1.73910795866076,-0.978347448872652,
26.8151961323744));
#22073=CARTESIAN_POINT('Ctrl Pts',(1.71336992197817,-1.02275272047976,26.8121057254511));
#22074=CARTESIAN_POINT('Ctrl Pts',(1.66957838426229,-1.0920045469544,26.8070767299766));
#22075=CARTESIAN_POINT('Ctrl Pts',(1.65261308554818,-1.11751319535862,26.8051766171205));
#22076=CARTESIAN_POINT('Ctrl Pts',(1.63008075361425,-1.14975653931474,26.8027080330895));
#22077=CARTESIAN_POINT('Ctrl Pts',(1.62504703464881,-1.1568601878827,26.8021599070082));
#22078=CARTESIAN_POINT('Ctrl Pts',(1.61685363524085,-1.16826382083532,26.8012729748947));
#22079=CARTESIAN_POINT('Ctrl Pts',(1.61372288483648,-1.17258453124573,26.8009352851152));
#22080=CARTESIAN_POINT('Ctrl Pts',(1.60771775859644,-1.18080253296128,26.8002898327103));
#22081=CARTESIAN_POINT('Ctrl Pts',(1.60484644835808,-1.18470202568707,26.7999821906016));
#22082=CARTESIAN_POINT('Ctrl Pts',(1.598249729667,-1.19359296127723,26.7992775950071));
#22083=CARTESIAN_POINT('Ctrl Pts',(1.59451510002529,-1.198577469306,26.7988802829783));
#22084=CARTESIAN_POINT('Ctrl Pts',(1.58296185977137,-1.21384770030322,26.7976559624247));
#22085=CARTESIAN_POINT('Ctrl Pts',(1.57506673642062,-1.22407485546644,26.7968259488745));
#22086=CARTESIAN_POINT('Ctrl Pts',(1.49883835472969,-1.32086068868532,26.7888733501473));
#22087=CARTESIAN_POINT('Ctrl Pts',(1.42354897002234,-1.40167409221848,26.7814647968924));
#22088=CARTESIAN_POINT('Ctrl Pts',(1.21473376378135,-1.5915493224345,26.7620173305601));
#22089=CARTESIAN_POINT('Ctrl Pts',(1.07306056622204,-1.69031041188822,26.7497471057844));
#22090=CARTESIAN_POINT('Ctrl Pts',(0.903899811883599,-1.77829744931058,
26.7371014203918));
#22091=CARTESIAN_POINT('Ctrl Pts',(0.887202112564299,-1.78668664345683,
26.735873854914));
#22092=CARTESIAN_POINT('Ctrl Pts',(0.865871430225537,-1.79703072552548,
26.7343340288122));
#22093=CARTESIAN_POINT('Ctrl Pts',(0.861346277993833,-1.79920408872352,
26.7340089671626));
#22094=CARTESIAN_POINT('Ctrl Pts',(0.854096671865346,-1.80265234716841,
26.7334908096801));
#22095=CARTESIAN_POINT('Ctrl Pts',(0.851377492694039,-1.80393818488103,
26.7332970450913));
#22096=CARTESIAN_POINT('Ctrl Pts',(0.846199760827307,-1.80637230107773,
26.732929215386));
#22097=CARTESIAN_POINT('Ctrl Pts',(0.843741804024056,-1.80752169932998,
26.7327550842244));
#22098=CARTESIAN_POINT('Ctrl Pts',(0.838086633390827,-1.81015214076514,
26.7323555490711));
#22099=CARTESIAN_POINT('Ctrl Pts',(0.83488783779947,-1.81162972942749,26.7321303599627));
#22100=CARTESIAN_POINT('Ctrl Pts',(0.824707677684042,-1.81629946248286,
26.7314161971569));
#22101=CARTESIAN_POINT('Ctrl Pts',(0.817711688158443,-1.81945983486432,
26.7309291415866));
#22102=CARTESIAN_POINT('Ctrl Pts',(0.704192853961239,-1.86995388408844,
26.7230834950702));
#22103=CARTESIAN_POINT('Ctrl Pts',(0.593722365550085,-1.90790922564198,
26.7162582654751));
#22104=CARTESIAN_POINT('Ctrl Pts',(0.381331703983508,-1.96062878259491,
26.7035419080329));
#22105=CARTESIAN_POINT('Ctrl Pts',(0.280367517858031,-1.97759252206167,
26.6976564886392));
#22106=CARTESIAN_POINT('Ctrl Pts',(0.125593572910727,-1.99150215547713,
26.6884354119564));
#22107=CARTESIAN_POINT('Ctrl Pts',(0.0724717364806699,-1.99414186156437,
26.6852372413083));
#22108=CARTESIAN_POINT('Ctrl Pts',(-0.0121201715123191,-1.99496081668052,
26.6800484637605));
#22109=CARTESIAN_POINT('Ctrl Pts',(-0.0435524338473951,-1.99452214133124,
26.6780995607384));
#22110=CARTESIAN_POINT('Ctrl Pts',(-0.083738947343184,-1.99301092113365,
26.6755761218088));
#22111=CARTESIAN_POINT('Ctrl Pts',(-0.0925155966413155,-1.99262279507719,
26.6750230758507));
#22112=CARTESIAN_POINT('Ctrl Pts',(-0.106635705332029,-1.99190487899414,
26.6741301009403));
#22113=CARTESIAN_POINT('Ctrl Pts',(-0.111980967619995,-1.99161152903668,
26.6737913162781));
#22114=CARTESIAN_POINT('Ctrl Pts',(-0.122155072704288,-1.99101208229963,
26.6731450364761));
#22115=CARTESIAN_POINT('Ctrl Pts',(-0.126984116495725,-1.99070992541116,
26.6728376672052));
#22116=CARTESIAN_POINT('Ctrl Pts',(-0.137993752388975,-1.98998082119529,
26.6721354697561));
#22117=CARTESIAN_POINT('Ctrl Pts',(-0.144173527124846,-1.98954264519977,
26.6717402917702));
#22118=CARTESIAN_POINT('Ctrl Pts',(-0.163066403830353,-1.98811456236324,
26.6705289414675));
#22119=CARTESIAN_POINT('Ctrl Pts',(-0.17577194331572,-1.98703154895143,
26.6697098558245));
#22120=CARTESIAN_POINT('Ctrl Pts',(-0.287350873418209,-1.97644208926666,
26.6624764334676));
#22121=CARTESIAN_POINT('Ctrl Pts',(-0.385380687577209,-1.9596862162087,
26.65583225197));
#22122=CARTESIAN_POINT('Ctrl Pts',(-0.616787739014875,-1.90209546357603,
26.6394756916763));
#22123=CARTESIAN_POINT('Ctrl Pts',(-0.74793506557626,-1.85444983353104,
26.629630275672));
#22124=CARTESIAN_POINT('Ctrl Pts',(-0.926498968511898,-1.76752954014019,
26.6160078528213));
#22125=CARTESIAN_POINT('Ctrl Pts',(-0.978762556778147,-1.73913381651503,
26.6119972700661));
#22126=CARTESIAN_POINT('Ctrl Pts',(-1.0355491879007,-1.70490830422718,26.6076741718831));
#22127=CARTESIAN_POINT('Ctrl Pts',(-1.04139545693419,-1.70134357258578,
26.6072295335165));
#22128=CARTESIAN_POINT('Ctrl Pts',(-1.05011658572411,-1.69596411358556,
26.6065670299919));
#22129=CARTESIAN_POINT('Ctrl Pts',(-1.05300527414928,-1.69417207249398,
26.6063477190831));
#22130=CARTESIAN_POINT('Ctrl Pts',(-1.05795712487784,-1.69108255985268,
26.6059720131795));
#22131=CARTESIAN_POINT('Ctrl Pts',(-1.06002249834409,-1.68978868666051,
26.6058153826207));
#22132=CARTESIAN_POINT('Ctrl Pts',(-1.06432336690025,-1.68708337746436,
26.6054893763965));
#22133=CARTESIAN_POINT('Ctrl Pts',(-1.06655841983701,-1.68567128738697,
26.605320045839));
#22134=CARTESIAN_POINT('Ctrl Pts',(-1.07275900920254,-1.68173653102068,
26.604850502667));
#22135=CARTESIAN_POINT('Ctrl Pts',(-1.07671848014454,-1.67920426607269,
26.6045509219677));
#22136=CARTESIAN_POINT('Ctrl Pts',(-1.09135159271219,-1.66977267578,26.6034445466298));
#22137=CARTESIAN_POINT('Ctrl Pts',(-1.10196845470289,-1.66278520333276,
26.6026433980875));
#22138=CARTESIAN_POINT('Ctrl Pts',(-1.12418832813985,-1.64785492368984,
26.600968377322));
#22139=CARTESIAN_POINT('Ctrl Pts',(-1.13577564304281,-1.63988992283795,
26.6000958687759));
#22140=CARTESIAN_POINT('Ctrl Pts',(-1.31505183333017,-1.51384549806041,
26.5865958649654));
#22141=CARTESIAN_POINT('Ctrl Pts',(-1.46365152895638,-1.37070760257481,
26.5752812872329));
#22142=CARTESIAN_POINT('Ctrl Pts',(-1.61694016391936,-1.16912155139533,
26.5601911800423));
#22143=CARTESIAN_POINT('Ctrl Pts',(-1.64465578330973,-1.1297997781298,26.55728756095));
#22144=CARTESIAN_POINT('Ctrl Pts',(-1.68688208749409,-1.06504001305279,
26.5525368107231));
#22145=CARTESIAN_POINT('Ctrl Pts',(-1.70230170220518,-1.04021641126892,
26.5507229007947));
#22146=CARTESIAN_POINT('Ctrl Pts',(-1.72152687731665,-1.00769344647638,
26.5483514616334));
#22147=CARTESIAN_POINT('Ctrl Pts',(-1.72583627845885,-1.00029496033239,
26.5478123339418));
#22148=CARTESIAN_POINT('Ctrl Pts',(-1.73273771173502,-0.988269049228014,
26.5469364513506));
#22149=CARTESIAN_POINT('Ctrl Pts',(-1.73535918492558,-0.983658573763605,
26.5466007621425));
#22150=CARTESIAN_POINT('Ctrl Pts',(-1.74034307807082,-0.974811296802802,
26.5459567662677));
#22151=CARTESIAN_POINT('Ctrl Pts',(-1.74270849414668,-0.97057621931986,
26.5456485701755));
#22152=CARTESIAN_POINT('Ctrl Pts',(-1.74805615038108,-0.960919117117224,
26.5449459529696));
#22153=CARTESIAN_POINT('Ctrl Pts',(-1.75102864427979,-0.955491779143886,
26.5445511869786));
#22154=CARTESIAN_POINT('Ctrl Pts',(-1.76019452973022,-0.938569797468603,
26.5433206194059));
#22155=CARTESIAN_POINT('Ctrl Pts',(-1.76630024818284,-0.927028298922435,
26.5424817174519));
#22156=CARTESIAN_POINT('Ctrl Pts',(-1.77788070048859,-0.90460824395497,
26.5408525887931));
#22157=CARTESIAN_POINT('Ctrl Pts',(-1.78336999617227,-0.893737828460682,
26.540062921269));
#22158=CARTESIAN_POINT('Ctrl Pts',(-1.85354314901331,-0.751553508897692,
26.5297358685534));
#22159=CARTESIAN_POINT('Ctrl Pts',(-1.90366914354141,-0.613582078641405,
26.5196835777378));
#22160=CARTESIAN_POINT('Ctrl Pts',(-1.96803445699008,-0.34893188742608,
26.5006927911525));
#22161=CARTESIAN_POINT('Ctrl Pts',(-1.98614825525813,-0.223906023392428,
26.4918495679565));
#22162=CARTESIAN_POINT('Ctrl Pts',(-1.99288065852635,-0.0870330910302871,
26.4827851965441));
#22163=CARTESIAN_POINT('Ctrl Pts',(-1.99332947186261,-0.0760638362088492,
26.4820631776488));
#22164=CARTESIAN_POINT('Ctrl Pts',(-1.99395253335949,-0.0569799828751236,
26.4808153551949));
#22165=CARTESIAN_POINT('Ctrl Pts',(-1.99416785543449,-0.0488671009836684,
26.4802874960542));
#22166=CARTESIAN_POINT('Ctrl Pts',(-1.99440810146639,-0.037110146430956,
26.4795265400302));
#22167=CARTESIAN_POINT('Ctrl Pts',(-1.99447255989448,-0.0334670959027242,
26.4792913042332));
#22168=CARTESIAN_POINT('Ctrl Pts',(-1.99456773336815,-0.0271021885634675,
26.4788813116109));
#22169=CARTESIAN_POINT('Ctrl Pts',(-1.99460285948886,-0.0243804204677668,
26.4787063089989));
#22170=CARTESIAN_POINT('Ctrl Pts',(-1.99466073430711,-0.0190504690719636,
26.4783642390629));
#22171=CARTESIAN_POINT('Ctrl Pts',(-1.99468393876935,-0.0164423224033568,
26.478197145991));
#22172=CARTESIAN_POINT('Ctrl Pts',(-1.99473339151064,-0.00931187333839594,
26.4777411151937));
#22173=CARTESIAN_POINT('Ctrl Pts',(-1.99474937674971,-0.0047894801152562,
26.4774527494229));
#22174=CARTESIAN_POINT('Ctrl Pts',(-1.99475185659427,0.0137361181896936,
26.47627488716));
#22175=CARTESIAN_POINT('Ctrl Pts',(-1.9946062781266,0.0277393604116115,
26.4753925230793));
#22176=CARTESIAN_POINT('Ctrl Pts',(-1.99241474663792,0.132448529288717,
26.468846486816));
#22177=CARTESIAN_POINT('Ctrl Pts',(-1.98432958457099,0.222933759005454,
26.4634783153668));
#22178=CARTESIAN_POINT('Ctrl Pts',(-1.95880133593162,0.383839807844613,
26.4539688877398));
#22179=CARTESIAN_POINT('Ctrl Pts',(-1.94363352561543,0.454449734028068,
26.4498087069397));
#22180=CARTESIAN_POINT('Ctrl Pts',(-1.89190203917916,0.644431498507619,
26.4383407757964));
#22181=CARTESIAN_POINT('Ctrl Pts',(-1.84792148585435,0.761422867130402,
26.4309560836767));
#22182=CARTESIAN_POINT('Ctrl Pts',(-1.78761479324789,0.885228867718535,
26.4223607905538));
#22183=CARTESIAN_POINT('Ctrl Pts',(-1.78180376652631,0.896867951321353,
26.4215449831546));
#22184=CARTESIAN_POINT('Ctrl Pts',(-1.77303495211782,0.914009645017655,
26.4203316002231));
#22185=CARTESIAN_POINT('Ctrl Pts',(-1.7701644123944,0.919556699865657,26.4199370893696));
#22186=CARTESIAN_POINT('Ctrl Pts',(-1.76502105930991,0.929382426540547,
26.4192349247278));
#22187=CARTESIAN_POINT('Ctrl Pts',(-1.76275861020527,0.933666490797689,
26.4189276391711));
#22188=CARTESIAN_POINT('Ctrl Pts',(-1.75797590985675,0.942643430729684,
26.4182813297268));
#22189=CARTESIAN_POINT('Ctrl Pts',(-1.75545242613107,0.947334532157192,
26.4179421927728));
#22190=CARTESIAN_POINT('Ctrl Pts',(-1.7487742582021,0.95963079154519,26.4170495510533));
#22191=CARTESIAN_POINT('Ctrl Pts',(-1.74458878643574,0.967219015809541,
26.4164949506273));
#22192=CARTESIAN_POINT('Ctrl Pts',(-1.7255808327729,1.00115547518758,26.4139976001845));
#22193=CARTESIAN_POINT('Ctrl Pts',(-1.7102106353266,1.02719078649811,26.4120352389543));
#22194=CARTESIAN_POINT('Ctrl Pts',(-1.66765988422647,1.09566281040562,26.406745552761));
#22195=CARTESIAN_POINT('Ctrl Pts',(-1.6394543682798,1.13743357580766,26.4033821493995));
#22196=CARTESIAN_POINT('Ctrl Pts',(-1.55059729495721,1.25884478170398,26.3931924628638));
#22197=CARTESIAN_POINT('Ctrl Pts',(-1.4855063352444,1.33503174736399,26.3862289557524));
#22198=CARTESIAN_POINT('Ctrl Pts',(-1.32818174023148,1.49336051102167,26.3706557698497));
#22199=CARTESIAN_POINT('Ctrl Pts',(-1.23346858964307,1.57249961726009,26.3620662708068));
#22200=CARTESIAN_POINT('Ctrl Pts',(-1.12583008763503,1.64669099971828,26.3535312768325));
#22201=CARTESIAN_POINT('Ctrl Pts',(-1.11958546507842,1.65094307157835,26.3530402414235));
#22202=CARTESIAN_POINT('Ctrl Pts',(-1.11041204981948,1.65711342292827,26.3523250893724));
#22203=CARTESIAN_POINT('Ctrl Pts',(-1.10750221808766,1.65905956922099,26.3520991450738));
#22204=CARTESIAN_POINT('Ctrl Pts',(-1.10233047906725,1.66249884896086,26.3516991893072));
#22205=CARTESIAN_POINT('Ctrl Pts',(-1.10007063648844,1.66399504295032,26.3515249725581));
#22206=CARTESIAN_POINT('Ctrl Pts',(-1.09528607307665,1.66714879419957,26.3511572825438));
#22207=CARTESIAN_POINT('Ctrl Pts',(-1.09276064212373,1.66880522026967,26.3509638851877));
#22208=CARTESIAN_POINT('Ctrl Pts',(-1.08598143671414,1.67322970270345,26.3504465263594));
#22209=CARTESIAN_POINT('Ctrl Pts',(-1.08172080870011,1.67598729478594,26.3501232594853));
#22210=CARTESIAN_POINT('Ctrl Pts',(-1.06121794808537,1.68914653892736,26.348576436171));
#22211=CARTESIAN_POINT('Ctrl Pts',(-1.04483527341616,1.69932895040902,26.3473668412685));
#22212=CARTESIAN_POINT('Ctrl Pts',(-0.998669686648428,1.72710239342899,
26.3440237401053));
#22213=CARTESIAN_POINT('Ctrl Pts',(-0.968572048685566,1.74415948255465,
26.3419188843811));
#22214=CARTESIAN_POINT('Ctrl Pts',(-0.857072985933626,1.80357183198289,
26.3343338739697));
#22215=CARTESIAN_POINT('Ctrl Pts',(-0.773215844155963,1.84108255915724,
26.3290291909821));
#22216=CARTESIAN_POINT('Ctrl Pts',(-0.540926164620284,1.9263071435606,26.3146788441818));
#22217=CARTESIAN_POINT('Ctrl Pts',(-0.389033331272474,1.96262684333847,
26.3056089302712));
#22218=CARTESIAN_POINT('Ctrl Pts',(-0.221984301227528,1.98239973084691,
26.2951046108969));
#22219=CARTESIAN_POINT('Ctrl Pts',(-0.20948183725367,1.98375983202795,26.2943156750733));
#22220=CARTESIAN_POINT('Ctrl Pts',(-0.190837078200525,1.98560991261882,
26.2931347225811));
#22221=CARTESIAN_POINT('Ctrl Pts',(-0.184703855599289,1.98618981969231,
26.292745535163));
#22222=CARTESIAN_POINT('Ctrl Pts',(-0.173753098931749,1.98717407255697,
26.2920493401442));
#22223=CARTESIAN_POINT('Ctrl Pts',(-0.168936575170822,1.98758933558376,
26.2917426782509));
#22224=CARTESIAN_POINT('Ctrl Pts',(-0.158764373488071,1.9884291034863,26.2910940544471));
#22225=CARTESIAN_POINT('Ctrl Pts',(-0.15340840288067,1.98884948824057,26.290751965607));
#22226=CARTESIAN_POINT('Ctrl Pts',(-0.139204106616541,1.98990665043685,
26.2898431887471));
#22227=CARTESIAN_POINT('Ctrl Pts',(-0.130353198129671,1.99050604125467,
26.2892753320646));
#22228=CARTESIAN_POINT('Ctrl Pts',(-0.0892312018048569,1.99301540984878,
26.2866294448014));
#22229=CARTESIAN_POINT('Ctrl Pts',(-0.0569222911537299,1.99419965905707,
26.284528827396));
#22230=CARTESIAN_POINT('Ctrl Pts',(0.0306817334046424,1.99528012333654,
26.2787702558293));
#22231=CARTESIAN_POINT('Ctrl Pts',(0.0859636232140479,1.99366332694163,
26.2750678508332));
#22232=CARTESIAN_POINT('Ctrl Pts',(0.244771471743728,1.98240149380513,26.2642428765634));
#22233=CARTESIAN_POINT('Ctrl Pts',(0.347699623840962,1.96695970827862,26.2569854971615));
#22234=CARTESIAN_POINT('Ctrl Pts',(0.518424920590111,1.92752378182725,26.2447665599753));
#22235=CARTESIAN_POINT('Ctrl Pts',(0.58699673550787,1.90776004002007,26.2398108903183));
#22236=CARTESIAN_POINT('Ctrl Pts',(0.662727332694286,1.88146176734226,26.2343734404213));
#22237=CARTESIAN_POINT('Ctrl Pts',(0.671069080322281,1.87850264672185,26.2337750311104));
#22238=CARTESIAN_POINT('Ctrl Pts',(0.710894065166959,1.86407614292352,26.2309215021966));
#22239=CARTESIAN_POINT('Ctrl Pts',(0.74210697676578,1.85187143207115,26.228695138789));
#22240=CARTESIAN_POINT('Ctrl Pts',(0.778317152497066,1.83665000582119,26.2261362416073));
#22241=CARTESIAN_POINT('Ctrl Pts',(0.783624929106467,1.8343916719782,26.2257617646161));
#22242=CARTESIAN_POINT('Ctrl Pts',(0.79212643437708,1.83073084857593,26.2251630334546));
#22243=CARTESIAN_POINT('Ctrl Pts',(0.795326361449667,1.82934297145295,26.224937918412));
#22244=CARTESIAN_POINT('Ctrl Pts',(0.801004702247619,1.82686243751916,26.2245389032379));
#22245=CARTESIAN_POINT('Ctrl Pts',(0.803484546826355,1.82577311898268,26.2243648012286));
#22246=CARTESIAN_POINT('Ctrl Pts',(0.808731333047573,1.82345560887289,26.2239967778307));
#22247=CARTESIAN_POINT('Ctrl Pts',(0.811497691986622,1.82222617223619,26.2238029345731));
#22248=CARTESIAN_POINT('Ctrl Pts',(0.818923149510501,1.81890585691757,26.2232831209708));
#22249=CARTESIAN_POINT('Ctrl Pts',(0.823577074781566,1.81680335876355,26.2229578567514));
#22250=CARTESIAN_POINT('Ctrl Pts',(0.846091617724544,1.80652770123288,26.2213866397609));
#22251=CARTESIAN_POINT('Ctrl Pts',(0.86383969047805,1.7981085675307,26.2201551864568));
#22252=CARTESIAN_POINT('Ctrl Pts',(0.91329673198017,1.77374633450444,26.2167357284304));
#22253=CARTESIAN_POINT('Ctrl Pts',(0.944710020340432,1.75721662622919,26.2145779848323));
#22254=CARTESIAN_POINT('Ctrl Pts',(1.0589970846477,1.69312734096632,26.2067195810789));
#22255=CARTESIAN_POINT('Ctrl Pts',(1.13886760514968,1.64046884265803,26.2012068375491));
#22256=CARTESIAN_POINT('Ctrl Pts',(1.22293719960101,1.57593180041014,26.1950585883482));
#22257=CARTESIAN_POINT('Ctrl Pts',(1.23116382018762,1.5695133260715,26.1944531002979));
#22258=CARTESIAN_POINT('Ctrl Pts',(1.34869327843517,1.47632326267751,26.1857424046758));
#22259=CARTESIAN_POINT('Ctrl Pts',(1.44862871503805,1.37839423452942,26.1775421761836));
#22260=CARTESIAN_POINT('Ctrl Pts',(1.54574829324497,1.26089512000377,26.16802657748));
#22261=CARTESIAN_POINT('Ctrl Pts',(1.55387767494147,1.25086308145653,26.167216774584));
#22262=CARTESIAN_POINT('Ctrl Pts',(1.56578212778264,1.23587728561667,26.1660106308452));
#22263=CARTESIAN_POINT('Ctrl Pts',(1.56963242968722,1.23098349746558,26.16561730129));
#22264=CARTESIAN_POINT('Ctrl Pts',(1.57643609614817,1.22225212050456,26.1649164675145));
#22265=CARTESIAN_POINT('Ctrl Pts',(1.57939853241792,1.21842163737982,26.1646093265203));
#22266=CARTESIAN_POINT('Ctrl Pts',(1.58559633456413,1.21034718369656,26.1639625335058));
#22267=CARTESIAN_POINT('Ctrl Pts',(1.58882867148446,1.20610094644759,26.1636227654224));
#22268=CARTESIAN_POINT('Ctrl Pts',(1.59729163250779,1.19489031519034,26.162726673718));
#22269=CARTESIAN_POINT('Ctrl Pts',(1.60249370412724,1.18790460427443,26.1621692389836));
#22270=CARTESIAN_POINT('Ctrl Pts',(1.62580514522594,1.15616855123185,26.159640875042));
#22271=CARTESIAN_POINT('Ctrl Pts',(1.6433871858039,1.13103778559928,26.1576497319203));
#22272=CARTESIAN_POINT('Ctrl Pts',(1.68886413643025,1.06273544179683,26.15226355236));
#22273=CARTESIAN_POINT('Ctrl Pts',(1.71568008045751,1.01887673064159,26.1488307955993));
#22274=CARTESIAN_POINT('Ctrl Pts',(1.79002954141133,0.88600118239082,26.1385100615273));
#22275=CARTESIAN_POINT('Ctrl Pts',(1.8325351114359,0.794364910200626,26.131485189322));
#22276=CARTESIAN_POINT('Ctrl Pts',(1.89528980754297,0.626886221083859,26.1190069485199));
#22277=CARTESIAN_POINT('Ctrl Pts',(1.91834950455345,0.552309976563445,26.1135718554628));
#22278=CARTESIAN_POINT('Ctrl Pts',(1.94744166928258,0.434067354181813,26.1052995602191));
#22279=CARTESIAN_POINT('Ctrl Pts',(1.95649839041601,0.391226604846006,26.1023717119027));
#22280=CARTESIAN_POINT('Ctrl Pts',(1.96534497275748,0.341312874227525,26.0990661093336));
#22281=CARTESIAN_POINT('Ctrl Pts',(1.9665158984502,0.334500470266664,26.0986172135613));
#22282=CARTESIAN_POINT('Ctrl Pts',(1.96821198039782,0.324315906977759,26.0979496318969));
#22283=CARTESIAN_POINT('Ctrl Pts',(1.96876391735158,0.320948353261616,26.0977294678346));
#22284=CARTESIAN_POINT('Ctrl Pts',(1.96973613618521,0.31491963178232,26.0973363681478));
#22285=CARTESIAN_POINT('Ctrl Pts',(1.97015966938895,0.312259024031686,26.0971632499953));
#22286=CARTESIAN_POINT('Ctrl Pts',(1.97106054339876,0.306524991128492,26.0967909430602));
#22287=CARTESIAN_POINT('Ctrl Pts',(1.97153608513815,0.303451316114563,26.0965918575256));
#22288=CARTESIAN_POINT('Ctrl Pts',(1.97282976192237,0.294958187562228,26.0960430586312));
#22289=CARTESIAN_POINT('Ctrl Pts',(1.97363276078984,0.289536403895955,26.0956941935494));
#22290=CARTESIAN_POINT('Ctrl Pts',(1.97788617700363,0.259977558639935,26.0937999116733));
#22291=CARTESIAN_POINT('Ctrl Pts',(1.98091635127636,0.235780831643728,26.0922771517358));
#22292=CARTESIAN_POINT('Ctrl Pts',(1.98865181483683,0.163247059783556,26.087779333982));
#22293=CARTESIAN_POINT('Ctrl Pts',(1.99203682554155,0.114785151720892,26.0848625697586));
#22294=CARTESIAN_POINT('Ctrl Pts',(1.99446808830493,0.0416156628385256,
26.0805283161669));
#22295=CARTESIAN_POINT('Ctrl Pts',(1.99483001390177,0.016973098859942,26.0790804906789));
#22296=CARTESIAN_POINT('Ctrl Pts',(1.99426672636337,-0.129514519424248,
26.0705137595227));
#22297=CARTESIAN_POINT('Ctrl Pts',(1.98263568426723,-0.251056740084457,
26.0635525048635));
#22298=CARTESIAN_POINT('Ctrl Pts',(1.95414678151079,-0.401653202858875,
26.054471602337));
#22299=CARTESIAN_POINT('Ctrl Pts',(1.94757752788801,-0.432384765997712,
26.0525952119452));
#22300=CARTESIAN_POINT('Ctrl Pts',(1.92815637048739,-0.513781890406775,
26.0475466650199));
#22301=CARTESIAN_POINT('Ctrl Pts',(1.91403526826719,-0.564116187350478,
26.044342077686));
#22302=CARTESIAN_POINT('Ctrl Pts',(1.89492958659536,-0.623190261119388,
26.0404573063918));
#22303=CARTESIAN_POINT('Ctrl Pts',(1.89183480609136,-0.632522964511125,
26.0398398722316));
#22304=CARTESIAN_POINT('Ctrl Pts',(1.88668358510471,-0.647681072158943,
26.038830829571));
#22305=CARTESIAN_POINT('Ctrl Pts',(1.88466883283597,-0.65352055107582,26.0384405988675));
#22306=CARTESIAN_POINT('Ctrl Pts',(1.88102838348234,-0.663915034764084,
26.0377432397127));
#22307=CARTESIAN_POINT('Ctrl Pts',(1.87941317640742,-0.668473682745276,
26.0374364613772));
#22308=CARTESIAN_POINT('Ctrl Pts',(1.87597189274502,-0.678075057548505,
26.0367883192272));
#22309=CARTESIAN_POINT('Ctrl Pts',(1.87414202797496,-0.683116376681361,
26.0364468312747));
#22310=CARTESIAN_POINT('Ctrl Pts',(1.86924588554003,-0.696437607244069,
26.0355413390327));
#22311=CARTESIAN_POINT('Ctrl Pts',(1.8661449524954,-0.704704571795733,26.0349761810928));
#22312=CARTESIAN_POINT('Ctrl Pts',(1.85159155344792,-0.74273361280262,26.0323612654904));
#22313=CARTESIAN_POINT('Ctrl Pts',(1.83948186027241,-0.772237522004765,
26.0302895600559));
#22314=CARTESIAN_POINT('Ctrl Pts',(1.80487611604055,-0.851112455191398,
26.0246301739942));
#22315=CARTESIAN_POINT('Ctrl Pts',(1.78106603532669,-0.899873934694573,
26.0209998968339));
#22316=CARTESIAN_POINT('Ctrl Pts',(1.66142325844926,-1.12149566569647,26.0038893855869));
#22317=CARTESIAN_POINT('Ctrl Pts',(1.54224236576821,-1.280451718441,25.9896970254888));
#22318=CARTESIAN_POINT('Ctrl Pts',(1.38522509308509,-1.43551814194517,25.9749814697341));
#22319=CARTESIAN_POINT('Ctrl Pts',(1.36851196018866,-1.4514599626903,25.9734582545449));
#22320=CARTESIAN_POINT('Ctrl Pts',(1.34740476751152,-1.47090425795328,25.9715914848922));
#22321=CARTESIAN_POINT('Ctrl Pts',(1.3432686367981,-1.47468244541253,25.9712283276274));
#22322=CARTESIAN_POINT('Ctrl Pts',(1.33676644565324,-1.48057187824255,25.9706616422081));
#22323=CARTESIAN_POINT('Ctrl Pts',(1.33441121429464,-1.48269495459303,25.970457235715));
#22324=CARTESIAN_POINT('Ctrl Pts',(1.33006865634126,-1.48659073845232,25.9700819462337));
#22325=CARTESIAN_POINT('Ctrl Pts',(1.32808285889487,-1.48836506755106,25.9699109424082));
#22326=CARTESIAN_POINT('Ctrl Pts',(1.3236131314964,-1.49234274377136,25.9695274054526));
#22327=CARTESIAN_POINT('Ctrl Pts',(1.32112725814866,-1.49454386182717,25.9693150401472));
#22328=CARTESIAN_POINT('Ctrl Pts',(1.31378795609195,-1.50100983112605,25.9686907795093));
#22329=CARTESIAN_POINT('Ctrl Pts',(1.30891923113949,-1.50525737195677,25.9682801573117));
#22330=CARTESIAN_POINT('Ctrl Pts',(1.27017412859174,-1.53872898422214,25.9650392407669));
#22331=CARTESIAN_POINT('Ctrl Pts',(1.23534087024433,-1.5668321096658,25.9622869323671));
#22332=CARTESIAN_POINT('Ctrl Pts',(1.14075002505497,-1.63802939553656,25.9551395550182));
#22333=CARTESIAN_POINT('Ctrl Pts',(1.07949952888634,-1.67902745923303,25.9508358995551));
#22334=CARTESIAN_POINT('Ctrl Pts',(0.871070435635749,-1.80240808538269,
25.9367611815496));
#22335=CARTESIAN_POINT('Ctrl Pts',(0.715745215872706,-1.86952946016563,
25.927084225882));
#22336=CARTESIAN_POINT('Ctrl Pts',(0.534048661929887,-1.92204158425444,
25.9153763170266));
#22337=CARTESIAN_POINT('Ctrl Pts',(0.514174080390318,-1.92745344699057,
25.9140918647329));
#22338=CARTESIAN_POINT('Ctrl Pts',(0.486700466777882,-1.9344793761117,25.9123096860271));
#22339=CARTESIAN_POINT('Ctrl Pts',(0.479170039166781,-1.93635840478393,
25.9118205193527));
#22340=CARTESIAN_POINT('Ctrl Pts',(0.467144859729687,-1.9392845433052,25.9110382278996));
#22341=CARTESIAN_POINT('Ctrl Pts',(0.462657055146897,-1.94036009766553,
25.9107460213456));
#22342=CARTESIAN_POINT('Ctrl Pts',(0.453430501075795,-1.94253751906237,
25.9101447275935));
#22343=CARTESIAN_POINT('Ctrl Pts',(0.448691375477951,-1.94363764142218,
25.9098355865409));
#22344=CARTESIAN_POINT('Ctrl Pts',(0.437839937350715,-1.94611484974783,
25.90912703822));
#22345=CARTESIAN_POINT('Ctrl Pts',(0.431725090198839,-1.94748049134259,
25.9087272666594));
#22346=CARTESIAN_POINT('Ctrl Pts',(0.412745591548754,-1.9516254411941,25.9074848318487));
#22347=CARTESIAN_POINT('Ctrl Pts',(0.399860001809734,-1.95430620712455,
25.9066390268469));
#22348=CARTESIAN_POINT('Ctrl Pts',(0.369943586681603,-1.96022187505819,
25.9046696988374));
#22349=CARTESIAN_POINT('Ctrl Pts',(0.352895446308533,-1.96336263315835,
25.9035432508486));
#22350=CARTESIAN_POINT('Ctrl Pts',(0.156884942412084,-1.99683805978584,
25.890541251457));
#22351=CARTESIAN_POINT('Ctrl Pts',(-0.0253425947507,-2.00282435706728,25.8778530385365));
#22352=CARTESIAN_POINT('Ctrl Pts',(-0.302140482888902,-1.97411182075522,
25.8584881907062));
#22353=CARTESIAN_POINT('Ctrl Pts',(-0.397625518859958,-1.95711654969343,
25.851816954888));
#22354=CARTESIAN_POINT('Ctrl Pts',(-0.499120079866885,-1.93131260899514,
25.8449762414664));
#22355=CARTESIAN_POINT('Ctrl Pts',(-0.506720581867318,-1.92933239869856,
25.8444655548407));
#22356=CARTESIAN_POINT('Ctrl Pts',(-0.517745621579041,-1.92639032460175,
25.8437272749049));
#22357=CARTESIAN_POINT('Ctrl Pts',(-0.521179476180026,-1.92546414286883,
25.8434976846837));
#22358=CARTESIAN_POINT('Ctrl Pts',(-0.527233418461934,-1.92381388751366,
25.843093561166));
#22359=CARTESIAN_POINT('Ctrl Pts',(-0.52985452524474,-1.92309363624678,
25.8429188076313));
#22360=CARTESIAN_POINT('Ctrl Pts',(-0.535356654722064,-1.92156960862007,
25.8425524316907));
#22361=CARTESIAN_POINT('Ctrl Pts',(-0.53823733783313,-1.92076471150913,
25.8423608758351));
#22362=CARTESIAN_POINT('Ctrl Pts',(-0.545875317515864,-1.91861203693715,
25.8418536473996));
#22363=CARTESIAN_POINT('Ctrl Pts',(-0.550629469953649,-1.91725303458705,
25.8415386226704));
#22364=CARTESIAN_POINT('Ctrl Pts',(-0.572562116066159,-1.91089514939675,
25.8400882889479));
#22365=CARTESIAN_POINT('Ctrl Pts',(-0.589678584363909,-1.90568278310088,
25.8389649197564));
#22366=CARTESIAN_POINT('Ctrl Pts',(-0.636381000070517,-1.89077127956367,
25.8359172318337));
#22367=CARTESIAN_POINT('Ctrl Pts',(-0.665814658580627,-1.88060837802264,
25.8340157877586));
#22368=CARTESIAN_POINT('Ctrl Pts',(-0.775617918319599,-1.83979390981897,
25.826953416595));
#22369=CARTESIAN_POINT('Ctrl Pts',(-0.854219509873379,-1.80464289395786,
25.821958583593));
#22370=CARTESIAN_POINT('Ctrl Pts',(-1.02000801428476,-1.7172341610937,25.8110864151556));
#22371=CARTESIAN_POINT('Ctrl Pts',(-1.10596515850756,-1.66317436496698,
25.805222666529));
#22372=CARTESIAN_POINT('Ctrl Pts',(-1.24076967279879,-1.56330545228823,
25.7951955490725));
#22373=CARTESIAN_POINT('Ctrl Pts',(-1.29209339290553,-1.52115960602932,
25.7911529841031));
#22374=CARTESIAN_POINT('Ctrl Pts',(-1.34901745654908,-1.46945244906522,
25.786345818397));
#22375=CARTESIAN_POINT('Ctrl Pts',(-1.35676093838173,-1.46230583238358,
25.7856845890357));
#22376=CARTESIAN_POINT('Ctrl Pts',(-1.36905807138593,-1.45077479695036,
25.7846225509277));
#22377=CARTESIAN_POINT('Ctrl Pts',(-1.37364820636982,-1.44642943759363,
25.7842234146424));
#22378=CARTESIAN_POINT('Ctrl Pts',(-1.38173868762547,-1.43869714834417,
25.7835150417119));
#22379=CARTESIAN_POINT('Ctrl Pts',(-1.38524744344229,-1.43531906044685,
25.7832061895234));
#22380=CARTESIAN_POINT('Ctrl Pts',(-1.3919773898818,-1.42879207725204,25.7826106135402));
#22381=CARTESIAN_POINT('Ctrl Pts',(-1.39520035867988,-1.42564505138953,
25.7823239724779));
#22382=CARTESIAN_POINT('Ctrl Pts',(-1.40207890421909,-1.4188829201228,25.7817091491221));
#22383=CARTESIAN_POINT('Ctrl Pts',(-1.40573121329794,-1.41526455117506,
25.7813808240291));
#22384=CARTESIAN_POINT('Ctrl Pts',(-1.41945116733061,-1.4015665884746,25.7801403429386));
#22385=CARTESIAN_POINT('Ctrl Pts',(-1.42942452537626,-1.39139355579345,
25.7792240441544));
#22386=CARTESIAN_POINT('Ctrl Pts',(-1.48777662855196,-1.33058364036823,
25.7737748262578));
#22387=CARTESIAN_POINT('Ctrl Pts',(-1.53356512403361,-1.27753987903736,
25.7691321964156));
#22388=CARTESIAN_POINT('Ctrl Pts',(-1.61272772427735,-1.17543158055717,
25.7603866729488));
#22389=CARTESIAN_POINT('Ctrl Pts',(-1.6468875298684,-1.12707175312899,25.7563163230258));
#22390=CARTESIAN_POINT('Ctrl Pts',(-1.7629874576479,-0.946138305508907,
25.7414007200954));
#22391=CARTESIAN_POINT('Ctrl Pts',(-1.83148052572356,-0.805597278227731,
25.7303520866869));
#22392=CARTESIAN_POINT('Ctrl Pts',(-1.88759140389618,-0.645156132111088,
25.7191393419408));
#22393=CARTESIAN_POINT('Ctrl Pts',(-1.89212008276404,-0.631751029274498,
25.7182129962918));
#22394=CARTESIAN_POINT('Ctrl Pts',(-1.897966173964,-0.613819321714616,25.7169888378195));
#22395=CARTESIAN_POINT('Ctrl Pts',(-1.89941059427398,-0.609335008582619,
25.7166839462945));
#22396=CARTESIAN_POINT('Ctrl Pts',(-1.90164144578985,-0.602324144809895,
25.7162092576138));
#22397=CARTESIAN_POINT('Ctrl Pts',(-1.9024387477851,-0.599801112780958,
25.716038829642));
#22398=CARTESIAN_POINT('Ctrl Pts',(-1.90396060015198,-0.594951705963677,
25.7157120365177));
#22399=CARTESIAN_POINT('Ctrl Pts',(-1.90468589985617,-0.592625617336767,
25.7155556304472));
#22400=CARTESIAN_POINT('Ctrl Pts',(-1.90641144447034,-0.587055780126092,
25.7151819326798));
#22401=CARTESIAN_POINT('Ctrl Pts',(-1.9074076724485,-0.583810805046987,
25.7149648786783));
#22402=CARTESIAN_POINT('Ctrl Pts',(-1.91038134201225,-0.574035922213185,
25.7143129891375));
#22403=CARTESIAN_POINT('Ctrl Pts',(-1.91233359552819,-0.56749831238639,
25.7138796029367));
#22404=CARTESIAN_POINT('Ctrl Pts',(-1.9306447282768,-0.505011309619001,
25.7097609785098));
#22405=CARTESIAN_POINT('Ctrl Pts',(-1.94457906799819,-0.448373973983803,
25.706208800238));
#22406=CARTESIAN_POINT('Ctrl Pts',(-1.98166579443634,-0.262939890188768,
25.6949197026938));
#22407=CARTESIAN_POINT('Ctrl Pts',(-1.99464064461358,-0.132464691104114,
25.6874821624276));
#22408=CARTESIAN_POINT('Ctrl Pts',(-1.99474931168317,-0.00165711783231753,
25.6798260142406));
#22409=CARTESIAN_POINT('',(-1.99466367889413,0.000990252434004168,24.8790450931555));
#22410=CARTESIAN_POINT('Ctrl Pts',(-1.99474975438214,0.000989895140400634,
24.8790451186048));
#22411=CARTESIAN_POINT('Ctrl Pts',(-1.99478493408844,-0.0699011595160849,
24.8835489941164));
#22412=CARTESIAN_POINT('Ctrl Pts',(-1.99103669367566,-0.140785882431073,
24.8880528696279));
#22413=CARTESIAN_POINT('Ctrl Pts',(-1.98353341726112,-0.211240964560431,
24.8925567451395));
#22414=CARTESIAN_POINT('Ctrl Pts',(-1.97602707455192,-0.281724838917365,
24.8970624612082));
#22415=CARTESIAN_POINT('Ctrl Pts',(-1.96476269732732,-0.351778257317102,
24.9015681772769));
#22416=CARTESIAN_POINT('Ctrl Pts',(-1.94982031519319,-0.420984917734511,
24.9060738933457));
#22417=CARTESIAN_POINT('Ctrl Pts',(-1.93485533688121,-0.490296233888402,
24.910586423051));
#22418=CARTESIAN_POINT('Ctrl Pts',(-1.91620135044852,-0.558757776505707,
24.9150989527564));
#22419=CARTESIAN_POINT('Ctrl Pts',(-1.89398901392024,-0.625965795910172,
24.9196114824617));
#22420=CARTESIAN_POINT('Ctrl Pts',(-1.87175843849076,-0.693229000883427,
24.9241277174766));
#22421=CARTESIAN_POINT('Ctrl Pts',(-1.84596386614983,-0.759236196406817,
24.9286439524916));
#22422=CARTESIAN_POINT('Ctrl Pts',(-1.81678410869231,-0.82360370622229,
24.9331601875065));
#22423=CARTESIAN_POINT('Ctrl Pts',(-1.78754438766915,-0.88810348942644,
24.937685703255));
#22424=CARTESIAN_POINT('Ctrl Pts',(-1.75490580504173,-0.950956441190844,
24.9422112190035));
#22425=CARTESIAN_POINT('Ctrl Pts',(-1.71909291508943,-1.01180388998527,
24.946736734752));
#22426=CARTESIAN_POINT('Ctrl Pts',(-1.69814978896887,-1.04738705001267,
24.9493832245273));
#22427=CARTESIAN_POINT('Ctrl Pts',(-1.67612192428506,-1.08228490824662,
24.9520297143025));
#22428=CARTESIAN_POINT('Ctrl Pts',(-1.65306071014841,-1.11643085368671,
24.9546762040778));
#22429=CARTESIAN_POINT('Ctrl Pts',(-1.61424871789799,-1.17389843375214,
24.9591302427958));
#22430=CARTESIAN_POINT('Ctrl Pts',(-1.57235955514502,-1.22945350124489,
24.9635842815138));
#22431=CARTESIAN_POINT('Ctrl Pts',(-1.52760818907699,-1.28274735749676,
24.9680383202318));
#22432=CARTESIAN_POINT('Ctrl Pts',(-1.48292409126539,-1.33596110480217,
24.9724856638375));
#22433=CARTESIAN_POINT('Ctrl Pts',(-1.43538664146035,-1.38692001508527,
24.9769330074433));
#22434=CARTESIAN_POINT('Ctrl Pts',(-1.3852537979361,-1.43530466375735,24.981380351049));
#22435=CARTESIAN_POINT('Ctrl Pts',(-1.33518005588115,-1.48363227190217,
24.9858224516938));
#22436=CARTESIAN_POINT('Ctrl Pts',(-1.28251734762013,-1.529391307576,24.9902645523386));
#22437=CARTESIAN_POINT('Ctrl Pts',(-1.22756237558356,-1.57229710187091,
24.9947066529834));
#22438=CARTESIAN_POINT('Ctrl Pts',(-1.17264206938682,-1.61517583100068,
24.9991459515314));
#22439=CARTESIAN_POINT('Ctrl Pts',(-1.11543275287161,-1.65520458863969,
25.0035852500794));
#22440=CARTESIAN_POINT('Ctrl Pts',(-1.05626514235829,-1.69213814788829,
25.0080245486275));
#22441=CARTESIAN_POINT('Ctrl Pts',(-0.99711474974064,-1.72906095939562,
25.0124625553305));
#22442=CARTESIAN_POINT('Ctrl Pts',(-0.936007609482037,-1.76289010146123,
25.0169005620336));
#22443=CARTESIAN_POINT('Ctrl Pts',(-0.873302942494188,-1.79342396915258,
25.0213385687367));
#22444=CARTESIAN_POINT('Ctrl Pts',(-0.81059521611902,-1.8239593266043,25.025776791972));
#22445=CARTESIAN_POINT('Ctrl Pts',(-0.746290249464193,-1.85119887829924,
25.0302150152072));
#22446=CARTESIAN_POINT('Ctrl Pts',(-0.680769740515363,-1.87498803273478,
25.0346532384425));
#22447=CARTESIAN_POINT('Ctrl Pts',(-0.615179819817879,-1.89880238915418,
25.0390961634856));
#22448=CARTESIAN_POINT('Ctrl Pts',(-0.548372247658953,-1.91915888506903,
25.0435390885286));
#22449=CARTESIAN_POINT('Ctrl Pts',(-0.480745571768988,-1.93595228704752,
25.0479820135716));
#22450=CARTESIAN_POINT('Ctrl Pts',(-0.413079419404771,-1.95275549202596,
25.0524275321329));
#22451=CARTESIAN_POINT('Ctrl Pts',(-0.34459369243018,-1.96599137029154,
25.0568730506941));
#22452=CARTESIAN_POINT('Ctrl Pts',(-0.275696111969152,-1.97560603773756,
25.0613185692554));
#22453=CARTESIAN_POINT('Ctrl Pts',(-0.206678303306874,-1.98523748304667,
25.0657718453706));
#22454=CARTESIAN_POINT('Ctrl Pts',(-0.137247694206113,-1.99123506132352,
25.0702251214858));
#22455=CARTESIAN_POINT('Ctrl Pts',(-0.0678152942088697,-1.99359691220953,
25.0746783976011));
#22456=CARTESIAN_POINT('Ctrl Pts',(-0.0306362406624794,-1.99486161543976,
25.0770629988989));
#22457=CARTESIAN_POINT('Ctrl Pts',(0.00654335154922504,-1.99508474164078,
25.0794476001968));
#22458=CARTESIAN_POINT('Ctrl Pts',(0.0436609877908849,-1.99427211800324,
25.0818322014946));
#22459=CARTESIAN_POINT('Ctrl Pts',(0.112990560449697,-1.99275427216962,
25.0862862402126));
#22460=CARTESIAN_POINT('Ctrl Pts',(0.182378190338787,-1.98761381512302,
25.0907402789306));
#22461=CARTESIAN_POINT('Ctrl Pts',(0.251414320647691,-1.97884269255372,
25.0951943176486));
#22462=CARTESIAN_POINT('Ctrl Pts',(0.320346678926507,-1.97008475434442,
25.0996416612543));
#22463=CARTESIAN_POINT('Ctrl Pts',(0.388928104586969,-1.95770704350507,
25.1040890048601));
#22464=CARTESIAN_POINT('Ctrl Pts',(0.456750377337522,-1.94175350013899,
25.1085363484659));
#22465=CARTESIAN_POINT('Ctrl Pts',(0.524492694599824,-1.92581876436071,
25.1129784491106));
#22466=CARTESIAN_POINT('Ctrl Pts',(0.591477162207732,-1.90631668020356,
25.1174205497554));
#22467=CARTESIAN_POINT('Ctrl Pts',(0.657303804424595,-1.883342579349,25.1218626504002));
#22468=CARTESIAN_POINT('Ctrl Pts',(0.723088922903924,-1.86038297065905,
25.1263019489482));
#22469=CARTESIAN_POINT('Ctrl Pts',(0.787717203715071,-1.8339558509964,25.1307412474963));
#22470=CARTESIAN_POINT('Ctrl Pts',(0.850803416763638,-1.80420650384686,
25.1351805460443));
#22471=CARTESIAN_POINT('Ctrl Pts',(0.913871271595267,-1.77446581381815,
25.1396185527474));
#22472=CARTESIAN_POINT('Ctrl Pts',(0.975397506923356,-1.74140502420487,
25.1440565594504));
#22473=CARTESIAN_POINT('Ctrl Pts',(1.03501813542709,-1.70521700139221,25.1484945661535));
#22474=CARTESIAN_POINT('Ctrl Pts',(1.09464167284673,-1.66902721295046,25.1529327893888));
#22475=CARTESIAN_POINT('Ctrl Pts',(1.15235900159095,-1.62971014444717,25.1573710126241));
#22476=CARTESIAN_POINT('Ctrl Pts',(1.20783349187974,-1.58750301366441,25.1618092358594));
#22477=CARTESIAN_POINT('Ctrl Pts',(1.26336675126887,-1.54525116908453,25.1662521609025));
#22478=CARTESIAN_POINT('Ctrl Pts',(1.31665203935131,-1.50010344823748,25.1706950859455));
#22479=CARTESIAN_POINT('Ctrl Pts',(1.36738510186496,-1.45233795849924,25.1751380109885));
#22480=CARTESIAN_POINT('Ctrl Pts',(1.41814777935539,-1.4045445860786,25.1795835295498));
#22481=CARTESIAN_POINT('Ctrl Pts',(1.46635492747801,-1.35413075719609,25.184029048111));
#22482=CARTESIAN_POINT('Ctrl Pts',(1.51174049771817,-1.30141009296026,25.1884745666723));
#22483=CARTESIAN_POINT('Ctrl Pts',(1.55720526704536,-1.24859742969361,25.1929278427875));
#22484=CARTESIAN_POINT('Ctrl Pts',(1.59983833037512,-1.1934702826931,25.1973811189028));
#22485=CARTESIAN_POINT('Ctrl Pts',(1.63941559816193,-1.13637320410302,25.201834395018));
#22486=CARTESIAN_POINT('Ctrl Pts',(1.66060808694645,-1.10579936044693,25.2042189963158));
#22487=CARTESIAN_POINT('Ctrl Pts',(1.68092515364768,-1.07466114176135,25.2066035976136));
#22488=CARTESIAN_POINT('Ctrl Pts',(1.70033786218408,-1.04301424579114,25.2089881989113));
#22489=CARTESIAN_POINT('Ctrl Pts',(1.73659757382767,-0.983903106294958,
25.2134422376293));
#22490=CARTESIAN_POINT('Ctrl Pts',(1.76984298071321,-0.922781830119846,
25.2178962763473));
#22491=CARTESIAN_POINT('Ctrl Pts',(1.79984557221022,-0.859990394536619,
25.2223503150653));
#22492=CARTESIAN_POINT('Ctrl Pts',(1.82980306515073,-0.797293344236958,
25.226797658671));
#22493=CARTESIAN_POINT('Ctrl Pts',(1.85652720794401,-0.732931555392873,
25.2312450022768));
#22494=CARTESIAN_POINT('Ctrl Pts',(1.87983392826067,-0.667272031978011,
25.2356923458826));
#22495=CARTESIAN_POINT('Ctrl Pts',(1.90311317234972,-0.601689914392275,
25.2401344465274));
#22496=CARTESIAN_POINT('Ctrl Pts',(1.92298283267127,-0.534813559932045,
25.2445765471722));
#22497=CARTESIAN_POINT('Ctrl Pts',(1.93930650845159,-0.467030864908624,
25.249018647817));
#22498=CARTESIAN_POINT('Ctrl Pts',(1.9556198871849,-0.399290927509548,25.253457946365));
#22499=CARTESIAN_POINT('Ctrl Pts',(1.96839160436379,-0.330646258564595,
25.257897244913));
#22500=CARTESIAN_POINT('Ctrl Pts',(1.97753524003519,-0.261499401374021,
25.262336543461));
#22501=CARTESIAN_POINT('Ctrl Pts',(1.9866762148899,-0.19237266606033,25.2667745501641));
#22502=CARTESIAN_POINT('Ctrl Pts',(1.99219113997979,-0.122744517695394,
25.2712125568671));
#22503=CARTESIAN_POINT('Ctrl Pts',(1.99404510212167,-0.0530254015031812,
25.2756505635702));
#22504=CARTESIAN_POINT('Ctrl Pts',(1.99589915471916,0.0166971163145512,
25.2800887868055));
#22505=CARTESIAN_POINT('Ctrl Pts',(1.99409187911962,0.0865101213204753,
25.2845270100408));
#22506=CARTESIAN_POINT('Ctrl Pts',(1.98864046260717,0.156002156977167,25.2889652332761));
#22507=CARTESIAN_POINT('Ctrl Pts',(1.98318327092055,0.225567811776531,25.2934081583192));
#22508=CARTESIAN_POINT('Ctrl Pts',(1.97407427118063,0.294811329505175,25.2978510833622));
#22509=CARTESIAN_POINT('Ctrl Pts',(1.96138255739416,0.363326335475374,25.3022940084052));
#22510=CARTESIAN_POINT('Ctrl Pts',(1.94868343493193,0.431881336474788,25.3067395269665));
#22511=CARTESIAN_POINT('Ctrl Pts',(1.93239755011193,0.499706503104474,25.3111850455277));
#22512=CARTESIAN_POINT('Ctrl Pts',(1.912644540423,0.566408354890803,25.315630564089));
#22513=CARTESIAN_POINT('Ctrl Pts',(1.89285706118077,0.633226603270421,25.3200838402042));
#22514=CARTESIAN_POINT('Ctrl Pts',(1.8695905431547,0.698917162441658,25.3245371163195));
#22515=CARTESIAN_POINT('Ctrl Pts',(1.84301334641758,0.763105082820636,25.3289903924347));
#22516=CARTESIAN_POINT('Ctrl Pts',(1.82878202183952,0.797475868345489,25.3313749937325));
#22517=CARTESIAN_POINT('Ctrl Pts',(1.81360223082304,0.831416195494785,25.3337595950303));
#22518=CARTESIAN_POINT('Ctrl Pts',(1.79750513532881,0.864871580621396,25.3361441963281));
#22519=CARTESIAN_POINT('Ctrl Pts',(1.76743843753571,0.927360677149058,25.3405982350461));
#22520=CARTESIAN_POINT('Ctrl Pts',(1.73404972190266,0.98840378608566,25.3450522737641));
#22521=CARTESIAN_POINT('Ctrl Pts',(1.69750110851537,1.04762471767761,25.3495063124821));
#22522=CARTESIAN_POINT('Ctrl Pts',(1.66100743337272,1.10675663100796,25.3539536560879));
#22523=CARTESIAN_POINT('Ctrl Pts',(1.62136354270157,1.16407139004667,25.3584009996936));
#22524=CARTESIAN_POINT('Ctrl Pts',(1.57877833891398,1.219215534299,25.3628483432994));
#22525=CARTESIAN_POINT('Ctrl Pts',(1.53624333870432,1.27429466927355,25.3672904439441));
#22526=CARTESIAN_POINT('Ctrl Pts',(1.49077421006266,1.32720788622117,25.3717325445889));
#22527=CARTESIAN_POINT('Ctrl Pts',(1.44262323073612,1.37763049350705,25.3761746452337));
#22528=CARTESIAN_POINT('Ctrl Pts',(1.39450262526062,1.42802129398891,25.3806139437817));
#22529=CARTESIAN_POINT('Ctrl Pts',(1.34370386240992,1.47592424825168,25.3850532423298));
#22530=CARTESIAN_POINT('Ctrl Pts',(1.29051859470568,1.52104875635821,25.3894925408778));
#22531=CARTESIAN_POINT('Ctrl Pts',(1.2373488040231,1.56616013314062,25.3939305475808));
#22532=CARTESIAN_POINT('Ctrl Pts',(1.18179426024702,1.6084943522703,25.3983685542839));
#22533=CARTESIAN_POINT('Ctrl Pts',(1.12418114587633,1.64779984031926,25.402806560987));
#22534=CARTESIAN_POINT('Ctrl Pts',(1.06656522053736,1.68710724609965,25.4072447842223));
#22535=CARTESIAN_POINT('Ctrl Pts',(1.00689093095456,1.72338535348979,25.4116830074576));
#22536=CARTESIAN_POINT('Ctrl Pts',(0.945513517706415,1.75642584538444,25.4161212306928));
#22537=CARTESIAN_POINT('Ctrl Pts',(0.88407108186231,1.78950134003403,25.4205641557359));
#22538=CARTESIAN_POINT('Ctrl Pts',(0.820922353042827,1.8193321407639,25.4250070807789));
#22539=CARTESIAN_POINT('Ctrl Pts',(0.756446402137609,1.84575632280999,25.4294500058219));
#22540=CARTESIAN_POINT('Ctrl Pts',(0.691932813965891,1.87219592973881,25.4338955243832));
#22541=CARTESIAN_POINT('Ctrl Pts',(0.626090923900176,1.89522479825833,25.4383410429444));
#22542=CARTESIAN_POINT('Ctrl Pts',(0.559316326762558,1.91473047949753,25.4427865615057));
#22543=CARTESIAN_POINT('Ctrl Pts',(0.492425206088981,1.93427019869498,25.4472398376209));
#22544=CARTESIAN_POINT('Ctrl Pts',(0.424598605789145,1.95027434556549,25.4516931137362));
#22545=CARTESIAN_POINT('Ctrl Pts',(0.356242919684316,1.9626814679603,25.4561463898514));
#22546=CARTESIAN_POINT('Ctrl Pts',(0.319640415465156,1.96932512521373,25.4585309911492));
#22547=CARTESIAN_POINT('Ctrl Pts',(0.282886311397865,1.97493829690981,25.460915592447));
#22548=CARTESIAN_POINT('Ctrl Pts',(0.246043286473326,1.97951768460941,25.4633001937448));
#22549=CARTESIAN_POINT('Ctrl Pts',(0.177226642091959,1.9880712193817,25.4677542324628));
#22550=CARTESIAN_POINT('Ctrl Pts',(0.107827142843297,1.99304886785181,25.4722082711807));
#22551=CARTESIAN_POINT('Ctrl Pts',(0.0382488468277091,1.99438326011235,
25.4766623098987));
#22552=CARTESIAN_POINT('Ctrl Pts',(-0.0312248621984024,1.99571564657399,
25.4811096535045));
#22553=CARTESIAN_POINT('Ctrl Pts',(-0.100876349089344,1.99341563677056,
25.4855569971102));
#22554=CARTESIAN_POINT('Ctrl Pts',(-0.170295337034419,1.98746749927749,
25.490004340716));
#22555=CARTESIAN_POINT('Ctrl Pts',(-0.239632487128338,1.98152637402712,
25.4944464413608));
#22556=CARTESIAN_POINT('Ctrl Pts',(-0.308737197238971,1.9719457045458,25.4988885420056));
#22557=CARTESIAN_POINT('Ctrl Pts',(-0.377199894270806,1.95876180334978,
25.5033306426503));
#22558=CARTESIAN_POINT('Ctrl Pts',(-0.445619404730034,1.94558621861705,
25.5077699411984));
#22559=CARTESIAN_POINT('Ctrl Pts',(-0.51339722589405,1.9288120035081,25.5122092397464));
#22560=CARTESIAN_POINT('Ctrl Pts',(-0.58013112954922,1.90852703282609,25.5166485382944));
#22561=CARTESIAN_POINT('Ctrl Pts',(-0.646845613501994,1.88824796511202,
25.5210865449975));
#22562=CARTESIAN_POINT('Ctrl Pts',(-0.712516314841297,1.86446031224138,
25.5255245517006));
#22563=CARTESIAN_POINT('Ctrl Pts',(-0.776755122245963,1.83730210976983,
25.5299625584036));
#22564=CARTESIAN_POINT('Ctrl Pts',(-0.840997063889379,1.81014258223802,
25.5344007816389));
#22565=CARTESIAN_POINT('Ctrl Pts',(-0.903806522907634,1.77961237144815,
25.5388390048742));
#22566=CARTESIAN_POINT('Ctrl Pts',(-0.964816023669794,1.74589736324047,
25.5432772281095));
#22567=CARTESIAN_POINT('Ctrl Pts',(-1.02589015726518,1.71214663770227,25.5477201531526));
#22568=CARTESIAN_POINT('Ctrl Pts',(-1.08516009726805,1.6752046177823,25.5521630781956));
#22569=CARTESIAN_POINT('Ctrl Pts',(-1.14228447074454,1.63530234219726,25.5566060032386));
#22570=CARTESIAN_POINT('Ctrl Pts',(-1.19944219006916,1.59537677401153,25.5610515217999));
#22571=CARTESIAN_POINT('Ctrl Pts',(-1.25445146379816,1.55248781183562,25.5654970403611));
#22572=CARTESIAN_POINT('Ctrl Pts',(-1.30700356997422,1.50690717384139,25.5699425589224));
#22573=CARTESIAN_POINT('Ctrl Pts',(-1.35964738104254,1.46124699636148,25.5743958350376));
#22574=CARTESIAN_POINT('Ctrl Pts',(-1.40982511283057,1.41288610660636,25.5788491111529));
#22575=CARTESIAN_POINT('Ctrl Pts',(-1.45726507255276,1.36213291231723,25.5833023872681));
#22576=CARTESIAN_POINT('Ctrl Pts',(-1.48266780676331,1.33495603627405,25.5856869885659));
#22577=CARTESIAN_POINT('Ctrl Pts',(-1.50728623044283,1.3070937844297,25.5880715898637));
#22578=CARTESIAN_POINT('Ctrl Pts',(-1.53108363525564,1.2785970688033,25.5904561911615));
#22579=CARTESIAN_POINT('Ctrl Pts',(-1.57528287205678,1.22566973946071,25.5948851429009));
#22580=CARTESIAN_POINT('Ctrl Pts',(-1.61682821605232,1.17033542805466,25.5993140946403));
#22581=CARTESIAN_POINT('Ctrl Pts',(-1.65544488032248,1.11289254230321,25.6037430463797));
#22582=CARTESIAN_POINT('Ctrl Pts',(-1.69400648819274,1.05553155379868,25.6081656836913));
#22583=CARTESIAN_POINT('Ctrl Pts',(-1.72964742212998,0.996068358787369,
25.6125883210028));
#22584=CARTESIAN_POINT('Ctrl Pts',(-1.76213257527141,0.934834931775307,
25.6170109583144));
#22585=CARTESIAN_POINT('Ctrl Pts',(-1.79458275594071,0.873667426703344,
25.6214288343568));
#22586=CARTESIAN_POINT('Ctrl Pts',(-1.82388366463736,0.81073390527048,25.6258467103991));
#22587=CARTESIAN_POINT('Ctrl Pts',(-1.84984406934354,0.74639432045973,25.6302645864415));
#22588=CARTESIAN_POINT('Ctrl Pts',(-1.87578918887268,0.682092618030071,
25.634679861291));
#22589=CARTESIAN_POINT('Ctrl Pts',(-1.89839751658755,0.616386950766104,
25.6390951361406));
#22590=CARTESIAN_POINT('Ctrl Pts',(-1.9175250249787,0.549659295455327,25.6435104109902));
#22591=CARTESIAN_POINT('Ctrl Pts',(-1.93664550425373,0.482956161709385,
25.6479240632824));
#22592=CARTESIAN_POINT('Ctrl Pts',(-1.95228757073861,0.415232262406829,
25.6523377155746));
#22593=CARTESIAN_POINT('Ctrl Pts',(-1.96435699506207,0.346884935462325,
25.6567513678668));
#22594=CARTESIAN_POINT('Ctrl Pts',(-1.97643122831788,0.278510376260323,
25.6611667787313));
#22595=CARTESIAN_POINT('Ctrl Pts',(-1.98492988835067,0.209512381281266,
25.6655821895958));
#22596=CARTESIAN_POINT('Ctrl Pts',(-1.98981009553343,0.140297349273715,
25.6699976004603));
#22597=CARTESIAN_POINT('Ctrl Pts',(-1.99314340277558,0.0930216991187449,
25.6730134398418));
#22598=CARTESIAN_POINT('Ctrl Pts',(-1.99478969175973,0.045644973009116,
25.6760292792233));
#22599=CARTESIAN_POINT('Ctrl Pts',(-1.99474927319053,-0.00170282290822489,
25.6790451186048));
#22600=CARTESIAN_POINT('',(-1.99474960167085,0.00126060858432954,24.0790451186048));
#22601=CARTESIAN_POINT('Ctrl Pts',(-1.99701539600246,0.00124451192682707,
24.0790462410754));
#22602=CARTESIAN_POINT('Ctrl Pts',(-1.99268113066523,-0.585369854447445,
24.116610900576));
#22603=CARTESIAN_POINT('Ctrl Pts',(-1.40931803204236,-1.84136072419047,
24.196560892549));
#22604=CARTESIAN_POINT('Ctrl Pts',(0.72621645117898,-2.24399041429405,24.3188962169942));
#22605=CARTESIAN_POINT('Ctrl Pts',(2.27983401216692,-0.604351048955341,
24.4460522144109));
#22606=CARTESIAN_POINT('Ctrl Pts',(1.74244183309103,1.58958477965188,24.5732082118277));
#22607=CARTESIAN_POINT('Ctrl Pts',(-0.393076711783321,2.32559111024706,
24.7003642092444));
#22608=CARTESIAN_POINT('Ctrl Pts',(-1.81615388819116,1.20559137819909,24.8023095681518));
#22609=CARTESIAN_POINT('Ctrl Pts',(-1.99314839518148,0.270951615543583,
24.861869594587));
#22610=CARTESIAN_POINT('Ctrl Pts',(-1.99194231462318,0.00100154863538889,
24.87904428855));
#22611=CARTESIAN_POINT('',(-1.9947492845807,-0.00168942735291895,23.2790451186048));
#22612=CARTESIAN_POINT('Ctrl Pts',(-1.9947492845807,-0.00168942735291895,
23.2790451186048));
#22613=CARTESIAN_POINT('Ctrl Pts',(-1.99465920403236,-0.10804979203561,
23.2858496230972));
#22614=CARTESIAN_POINT('Ctrl Pts',(-1.98605925402385,-0.214061270660987,
23.2926541275897));
#22615=CARTESIAN_POINT('Ctrl Pts',(-1.96913368264437,-0.318653577377403,
23.2994586320821));
#22616=CARTESIAN_POINT('Ctrl Pts',(-1.96731820264146,-0.329872415255579,
23.3001885006082));
#22617=CARTESIAN_POINT('Ctrl Pts',(-1.96540697249395,-0.341074954761223,
23.3009183691343));
#22618=CARTESIAN_POINT('Ctrl Pts',(-1.96340024706976,-0.352259893127804,
23.3016482376603));
#22619=CARTESIAN_POINT('Ctrl Pts',(-1.95115416107432,-0.420516225279579,
23.3061022763783));
#22620=CARTESIAN_POINT('Ctrl Pts',(-1.93532024986766,-0.488268381969719,
23.3105563150963));
#22621=CARTESIAN_POINT('Ctrl Pts',(-1.91595404076151,-0.555110508087934,
23.3150103538143));
#22622=CARTESIAN_POINT('Ctrl Pts',(-1.89661694207666,-0.621852160105046,
23.31945769742));
#22623=CARTESIAN_POINT('Ctrl Pts',(-1.87375821884304,-0.687686030136642,
23.3239050410258));
#22624=CARTESIAN_POINT('Ctrl Pts',(-1.84748455717621,-0.752215642947846,
23.3283523846315));
#22625=CARTESIAN_POINT('Ctrl Pts',(-1.82124186945576,-0.816669181978649,
23.3327944852763));
#22626=CARTESIAN_POINT('Ctrl Pts',(-1.79159242289082,-0.879821066396918,
23.3372365859211));
#22627=CARTESIAN_POINT('Ctrl Pts',(-1.75869239605651,-0.941290931940295,
23.3416786865659));
#22628=CARTESIAN_POINT('Ctrl Pts',(-1.72581312270487,-1.00272202202017,
23.3461179851139));
#22629=CARTESIAN_POINT('Ctrl Pts',(-1.68968756724518,-1.06247276742969,
23.3505572836619));
#22630=CARTESIAN_POINT('Ctrl Pts',(-1.65051897062473,-1.12018511421455,
23.35499658221));
#22631=CARTESIAN_POINT('Ctrl Pts',(-1.61136177214606,-1.1778806665884,23.359434588913));
#22632=CARTESIAN_POINT('Ctrl Pts',(-1.56916356520635,-1.23353859301894,
23.3638725956161));
#22633=CARTESIAN_POINT('Ctrl Pts',(-1.5241713057499,-1.28682920126512,23.3683106023191));
#22634=CARTESIAN_POINT('Ctrl Pts',(-1.47917685110192,-1.34012240958282,
23.3727488255544));
#22635=CARTESIAN_POINT('Ctrl Pts',(-1.43138839093273,-1.39104769787549,
23.3771870487897));
#22636=CARTESIAN_POINT('Ctrl Pts',(-1.38109245590606,-1.43930927556914,
23.381625272025));
#22637=CARTESIAN_POINT('Ctrl Pts',(-1.33074323788676,-1.48762198107834,
23.3860681970681));
#22638=CARTESIAN_POINT('Ctrl Pts',(-1.2778815969231,-1.53326500396611,23.3905111221111));
#22639=CARTESIAN_POINT('Ctrl Pts',(-1.22282944061413,-1.57598087604747,
23.3949540471541));
#22640=CARTESIAN_POINT('Ctrl Pts',(-1.16774514809551,-1.61872168314158,
23.3993995657154));
#22641=CARTESIAN_POINT('Ctrl Pts',(-1.11046819725744,-1.65853165896925,
23.4038450842766));
#22642=CARTESIAN_POINT('Ctrl Pts',(-1.05134965802129,-1.69519658419857,
23.4082906028379));
#22643=CARTESIAN_POINT('Ctrl Pts',(-0.992127955283884,-1.73192549074592,
23.4127438789531));
#22644=CARTESIAN_POINT('Ctrl Pts',(-0.931058678142455,-1.76549815544073,
23.4171971550683));
#22645=CARTESIAN_POINT('Ctrl Pts',(-0.868516949756957,-1.79574660531069,
23.4216504311836));
#22646=CARTESIAN_POINT('Ctrl Pts',(-0.835027652705715,-1.81194378036781,
23.4240350324814));
#22647=CARTESIAN_POINT('Ctrl Pts',(-0.801116498800482,-1.82718863205936,
23.4264196337792));
#22648=CARTESIAN_POINT('Ctrl Pts',(-0.766842997888278,-1.84146120759839,
23.428804235077));
#22649=CARTESIAN_POINT('Ctrl Pts',(-0.702825797107145,-1.86812000549261,
23.4332582737949));
#22650=CARTESIAN_POINT('Ctrl Pts',(-0.63728999456594,-1.8914893457816,23.4377123125129));
#22651=CARTESIAN_POINT('Ctrl Pts',(-0.570606879146275,-1.91139617870575,
23.4421663512309));
#22652=CARTESIAN_POINT('Ctrl Pts',(-0.504023998809854,-1.93127308856703,
23.4466136948367));
#22653=CARTESIAN_POINT('Ctrl Pts',(-0.436297693757557,-1.94769768217472,
23.4510610384424));
#22654=CARTESIAN_POINT('Ctrl Pts',(-0.367819064652596,-1.96054500029407,
23.4555083820482));
#22655=CARTESIAN_POINT('Ctrl Pts',(-0.299421164812397,-1.97337717274594,
23.4599504826929));
#22656=CARTESIAN_POINT('Ctrl Pts',(-0.230273181283642,-1.98264035584297,
23.4643925833377));
#22657=CARTESIAN_POINT('Ctrl Pts',(-0.160779465112124,-1.9882599241795,
23.4688346839825));
#22658=CARTESIAN_POINT('Ctrl Pts',(-0.0913295858846346,-1.99387594766742,
23.4732739825305));
#22659=CARTESIAN_POINT('Ctrl Pts',(-0.0215348934897767,-1.99585287654051,
23.4777132810786));
#22660=CARTESIAN_POINT('Ctrl Pts',(0.0481935384601513,-1.99416773250163,
23.4821525796266));
#22661=CARTESIAN_POINT('Ctrl Pts',(0.117901679293752,-1.99248307884312,
23.4865905863297));
#22662=CARTESIAN_POINT('Ctrl Pts',(0.187543108792388,-1.98713847961906,
23.4910285930327));
#22663=CARTESIAN_POINT('Ctrl Pts',(0.256706930850311,-1.97816306561249,
23.4954665997358));
#22664=CARTESIAN_POINT('Ctrl Pts',(0.325874127440659,-1.96918721369164,
23.4999048229711));
#22665=CARTESIAN_POINT('Ctrl Pts',(0.394563185144293,-1.95658026065646,
23.5043430462064));
#22666=CARTESIAN_POINT('Ctrl Pts',(0.462370284715168,-1.94042296479722,
23.5087812694417));
#22667=CARTESIAN_POINT('Ctrl Pts',(0.530249218424936,-1.92424855206611,
23.5132241944847));
#22668=CARTESIAN_POINT('Ctrl Pts',(0.597243851932029,-1.90451640304601,
23.5176671195277));
#22669=CARTESIAN_POINT('Ctrl Pts',(0.662963432335407,-1.88135776764709,
23.5221100445708));
#22670=CARTESIAN_POINT('Ctrl Pts',(0.728721375962942,-1.85818561359946,
23.526555563132));
#22671=CARTESIAN_POINT('Ctrl Pts',(0.793202332343888,-1.83158317880671,
23.5310010816933));
#22672=CARTESIAN_POINT('Ctrl Pts',(0.856036121549,-1.80172964706233,23.5354466002545));
#22673=CARTESIAN_POINT('Ctrl Pts',(0.918979557470293,-1.77182402007169,
23.5398998763698));
#22674=CARTESIAN_POINT('Ctrl Pts',(0.980269657979123,-1.73865620427228,
23.544353152485));
#22675=CARTESIAN_POINT('Ctrl Pts',(1.03956210241269,-1.7024506447258,23.5488064286002));
#22676=CARTESIAN_POINT('Ctrl Pts',(1.07131150134714,-1.68306360874395,23.5511910298981));
#22677=CARTESIAN_POINT('Ctrl Pts',(1.10248862554588,-1.66280629428665,23.5535756311959));
#22678=CARTESIAN_POINT('Ctrl Pts',(1.13304448021701,-1.64171793203028,23.5559602324937));
#22679=CARTESIAN_POINT('Ctrl Pts',(1.19011773598109,-1.60232837786275,23.5604142712117));
#22680=CARTESIAN_POINT('Ctrl Pts',(1.24524754449985,-1.55988109652507,23.5648683099297));
#22681=CARTESIAN_POINT('Ctrl Pts',(1.29808739268708,-1.51459456074781,23.5693223486477));
#22682=CARTESIAN_POINT('Ctrl Pts',(1.35084781437262,-1.46937609767012,23.5737696922535));
#22683=CARTESIAN_POINT('Ctrl Pts',(1.40132473888279,-1.42132716674313,23.5782170358592));
#22684=CARTESIAN_POINT('Ctrl Pts',(1.44920135926868,-1.3707089343817,23.582664379465));
#22685=CARTESIAN_POINT('Ctrl Pts',(1.49702153804036,-1.32015037571318,23.5871064801098));
#22686=CARTESIAN_POINT('Ctrl Pts',(1.54224716635718,-1.26702888542403,23.5915485807546));
#22687=CARTESIAN_POINT('Ctrl Pts',(1.58459658190161,-1.21164402161928,23.5959906813993));
#22688=CARTESIAN_POINT('Ctrl Pts',(1.62691928324711,-1.15629409483195,23.6004299799474));
#22689=CARTESIAN_POINT('Ctrl Pts',(1.66636907435181,-1.09868401484527,23.6048692784954));
#22690=CARTESIAN_POINT('Ctrl Pts',(1.70270407591608,-1.03914695416903,23.6093085770434));
#22691=CARTESIAN_POINT('Ctrl Pts',(1.73902850392055,-0.979627218899252,
23.6137465837465));
#22692=CARTESIAN_POINT('Ctrl Pts',(1.77223968684989,-0.91818203379965,23.6181845904496));
#22693=CARTESIAN_POINT('Ctrl Pts',(1.80213965260977,-0.85517263461335,23.6226225971526));
#22694=CARTESIAN_POINT('Ctrl Pts',(1.83204107720174,-0.792160161171581,
23.6270608203879));
#22695=CARTESIAN_POINT('Ctrl Pts',(1.85863075615744,-0.727583765436892,
23.6314990436233));
#22696=CARTESIAN_POINT('Ctrl Pts',(1.88175795509335,-0.6618266849734,23.6359372668586));
#22697=CARTESIAN_POINT('Ctrl Pts',(1.90490965474427,-0.595999942139985,
23.6403801919016));
#22698=CARTESIAN_POINT('Ctrl Pts',(1.92459139023972,-0.528990480781164,
23.6448231169446));
#22699=CARTESIAN_POINT('Ctrl Pts',(1.94070195267942,-0.461197889594338,
23.6492660419877));
#22700=CARTESIAN_POINT('Ctrl Pts',(1.95682191951755,-0.393365725081634,
23.6537115605489));
#22701=CARTESIAN_POINT('Ctrl Pts',(1.96936647599005,-0.324750002571239,
23.6581570791102));
#22702=CARTESIAN_POINT('Ctrl Pts',(1.9782858524203,-0.255758965852019,23.6626025976714));
#22703=CARTESIAN_POINT('Ctrl Pts',(1.9872207934114,-0.186647537847844,23.6670558737867));
#22704=CARTESIAN_POINT('Ctrl Pts',(1.99251788924153,-0.117159976363346,
23.6715091499019));
#22705=CARTESIAN_POINT('Ctrl Pts',(1.99417942449901,-0.0477072888013889,
23.6759624260172));
#22706=CARTESIAN_POINT('Ctrl Pts',(1.99506912884897,-0.0105173718484036,
23.6783470273149));
#22707=CARTESIAN_POINT('Ctrl Pts',(1.99491730370229,0.026662579891606,23.6807316286127));
#22708=CARTESIAN_POINT('Ctrl Pts',(1.99373040618449,0.0637701337258532,
23.6831162299105));
#22709=CARTESIAN_POINT('Ctrl Pts',(1.99151347897597,0.133080874125654,23.6875702686285));
#22710=CARTESIAN_POINT('Ctrl Pts',(1.98567353928422,0.202413136346486,23.6920243073465));
#22711=CARTESIAN_POINT('Ctrl Pts',(1.97620666341123,0.271357303179857,23.6964783460644));
#22712=CARTESIAN_POINT('Ctrl Pts',(1.96675401772357,0.340197836218457,23.7009256896702));
#22713=CARTESIAN_POINT('Ctrl Pts',(1.95368532247587,0.408650950652678,23.705373033276));
#22714=CARTESIAN_POINT('Ctrl Pts',(1.93704863226097,0.476308890065993,23.7098203768817));
#22715=CARTESIAN_POINT('Ctrl Pts',(1.92043155499376,0.543887067723278,23.7142624775265));
#22716=CARTESIAN_POINT('Ctrl Pts',(1.90025495333303,0.610671459107838,23.7187045781713));
#22717=CARTESIAN_POINT('Ctrl Pts',(1.87661818769376,0.676263070200494,23.7231466788161));
#22718=CARTESIAN_POINT('Ctrl Pts',(1.85299633223096,0.74181330581431,23.7275859773641));
#22719=CARTESIAN_POINT('Ctrl Pts',(1.82591880832445,0.806171794247129,23.7320252759121));
#22720=CARTESIAN_POINT('Ctrl Pts',(1.79553477695009,0.868954790114415,23.7364645744602));
#22721=CARTESIAN_POINT('Ctrl Pts',(1.76515958739101,0.931719516001482,23.7409025811632));
#22722=CARTESIAN_POINT('Ctrl Pts',(1.73148001363771,0.992909219018232,23.7453405878663));
#22723=CARTESIAN_POINT('Ctrl Pts',(1.69469258292169,1.05216187532633,23.7497785945693));
#22724=CARTESIAN_POINT('Ctrl Pts',(1.65790335733123,1.11141742259679,23.7542168178046));
#22725=CARTESIAN_POINT('Ctrl Pts',(1.61800623398767,1.16873532086556,23.7586550410399));
#22726=CARTESIAN_POINT('Ctrl Pts',(1.57524181337524,1.22378134970847,23.7630932642752));
#22727=CARTESIAN_POINT('Ctrl Pts',(1.53243208857855,1.27888569374419,23.7675361893183));
#22728=CARTESIAN_POINT('Ctrl Pts',(1.48674930458348,1.33171297713226,23.7719791143613));
#22729=CARTESIAN_POINT('Ctrl Pts',(1.4384746228959,1.38196176567389,23.7764220394043));
#22730=CARTESIAN_POINT('Ctrl Pts',(1.39017176128957,1.4322398865017,23.7808675579656));
#22731=CARTESIAN_POINT('Ctrl Pts',(1.33927434787408,1.47993618174905,23.7853130765268));
#22732=CARTESIAN_POINT('Ctrl Pts',(1.28609867079362,1.52478777916236,23.7897585950881));
#22733=CARTESIAN_POINT('Ctrl Pts',(1.23283020067228,1.56971764386517,23.7942118712033));
#22734=CARTESIAN_POINT('Ctrl Pts',(1.17727592103198,1.61179260600342,23.7986651473186));
#22735=CARTESIAN_POINT('Ctrl Pts',(1.11978262634189,1.65079206208501,23.8031184234338));
#22736=CARTESIAN_POINT('Ctrl Pts',(1.08899662035741,1.67167514931789,23.8055030247316));
#22737=CARTESIAN_POINT('Ctrl Pts',(1.05765509629277,1.69167716750663,23.8078876260294));
#22738=CARTESIAN_POINT('Ctrl Pts',(1.02581404086839,1.71076974372862,23.8102722273273));
#22739=CARTESIAN_POINT('Ctrl Pts',(0.966340243797557,1.74643150143895,23.8147262660453));
#22740=CARTESIAN_POINT('Ctrl Pts',(0.904886810215522,1.77905883631686,23.8191803047632));
#22741=CARTESIAN_POINT('Ctrl Pts',(0.841796004535295,1.80842667787456,23.8236343434812));
#22742=CARTESIAN_POINT('Ctrl Pts',(0.778800034138541,1.83775037500346,23.828081687087));
#22743=CARTESIAN_POINT('Ctrl Pts',(0.714172016778803,1.86382409823917,23.8325290306927));
#22744=CARTESIAN_POINT('Ctrl Pts',(0.648280794056694,1.88646748568779,23.8369763742985));
#22745=CARTESIAN_POINT('Ctrl Pts',(0.582467250313252,1.90908417891011,23.8414184749433));
#22746=CARTESIAN_POINT('Ctrl Pts',(0.515393919675886,1.92827840992859,23.8458605755881));
#22747=CARTESIAN_POINT('Ctrl Pts',(0.447450054273597,1.94391769667097,23.8503026762328));
#22748=CARTESIAN_POINT('Ctrl Pts',(0.379549048162587,1.95954711808198,23.8547419747809));
#22749=CARTESIAN_POINT('Ctrl Pts',(0.310779072626706,1.97162593421012,23.8591812733289));
#22750=CARTESIAN_POINT('Ctrl Pts',(0.241543522004278,1.98007178897074,23.8636205718769));
#22751=CARTESIAN_POINT('Ctrl Pts',(0.172328119068684,1.98851518597035,23.86805857858));
#22752=CARTESIAN_POINT('Ctrl Pts',(0.102647895712263,1.99332766105929,23.872496585283));
#22753=CARTESIAN_POINT('Ctrl Pts',(0.032913628371883,1.99447844199114,23.8769345919861));
#22754=CARTESIAN_POINT('Ctrl Pts',(-0.036824041333096,1.99562927907008,
23.8813728152214));
#22755=CARTESIAN_POINT('Ctrl Pts',(-0.106615270724014,1.99311806160853,
23.8858110384567));
#22756=CARTESIAN_POINT('Ctrl Pts',(-0.176048797512498,1.98696612537668,
23.890249261692));
#22757=CARTESIAN_POINT('Ctrl Pts',(-0.245555881460078,1.9808076718473,23.894692186735));
#22758=CARTESIAN_POINT('Ctrl Pts',(-0.314704017823341,1.97100084457308,
23.8991351117781));
#22759=CARTESIAN_POINT('Ctrl Pts',(-0.383087549361908,1.95761883215908,
23.9035780368211));
#22760=CARTESIAN_POINT('Ctrl Pts',(-0.451510999182559,1.94422900811363,
23.9080235553823));
#22761=CARTESIAN_POINT('Ctrl Pts',(-0.519168480809031,1.92725996416102,
23.9124690739436));
#22762=CARTESIAN_POINT('Ctrl Pts',(-0.585667740268369,1.90683529978573,
23.9169145925048));
#22763=CARTESIAN_POINT('Ctrl Pts',(-0.652283042791804,1.88637499380095,
23.9213678686201));
#22764=CARTESIAN_POINT('Ctrl Pts',(-0.717735628858871,1.86244719819799,
23.9258211447353));
#22765=CARTESIAN_POINT('Ctrl Pts',(-0.781652265790118,1.83522404569175,
23.9302744208505));
#22766=CARTESIAN_POINT('Ctrl Pts',(-0.815877786829699,1.82064683037504,
23.9326590221483));
#22767=CARTESIAN_POINT('Ctrl Pts',(-0.849663306511639,1.80512553783525,
23.9350436234461));
#22768=CARTESIAN_POINT('Ctrl Pts',(-0.882954658214134,1.78869187789232,
23.9374282247439));
#22769=CARTESIAN_POINT('Ctrl Pts',(-0.945137367581059,1.75799653367205,
23.9418822634619));
#22770=CARTESIAN_POINT('Ctrl Pts',(-1.00584066178244,1.72399392269352,23.9463363021799));
#22771=CARTESIAN_POINT('Ctrl Pts',(-1.06469000510462,1.68684995050844,23.9507903408979));
#22772=CARTESIAN_POINT('Ctrl Pts',(-1.1234508887202,1.64976181148471,23.9552376845036));
#22773=CARTESIAN_POINT('Ctrl Pts',(-1.1803629418952,1.6095419423325,23.9596850281094));
#22774=CARTESIAN_POINT('Ctrl Pts',(-1.2350748287984,1.5664027993363,23.9641323717151));
#22775=CARTESIAN_POINT('Ctrl Pts',(-1.28972221601077,1.52331451295543,23.9685744723599));
#22776=CARTESIAN_POINT('Ctrl Pts',(-1.34217420592638,1.47731408968489,23.9730165730047));
#22777=CARTESIAN_POINT('Ctrl Pts',(-1.39210866753241,1.42865706881712,23.9774586736495));
#22778=CARTESIAN_POINT('Ctrl Pts',(-1.44201163025885,1.38003074101367,23.9818979721975));
#22779=CARTESIAN_POINT('Ctrl Pts',(-1.48939986522325,1.32875148086676,23.9863372707455));
#22780=CARTESIAN_POINT('Ctrl Pts',(-1.53398572845433,1.27511385664122,23.9907765692935));
#22781=CARTESIAN_POINT('Ctrl Pts',(-1.57855861710803,1.22149184107403,23.9952145759966));
#22782=CARTESIAN_POINT('Ctrl Pts',(-1.62033044013214,1.16551320010519,23.9996525826996));
#22783=CARTESIAN_POINT('Ctrl Pts',(-1.65905292629981,1.10750663665553,24.0040905894027));
#22784=CARTESIAN_POINT('Ctrl Pts',(-1.69777730175411,1.04949724304087,24.008528812638));
#22785=CARTESIAN_POINT('Ctrl Pts',(-1.73345177515224,0.989460139006743,
24.0129670358733));
#22786=CARTESIAN_POINT('Ctrl Pts',(-1.76587162242856,0.927752647854771,
24.0174052591086));
#22787=CARTESIAN_POINT('Ctrl Pts',(-1.79832581495525,0.86597978442588,24.0218481841516));
#22788=CARTESIAN_POINT('Ctrl Pts',(-1.82751827133476,0.802533436113121,
24.0262911091947));
#22789=CARTESIAN_POINT('Ctrl Pts',(-1.85329089780187,0.737794287470932,
24.0307340342377));
#22790=CARTESIAN_POINT('Ctrl Pts',(-1.87907856881188,0.673017347922943,
24.0351795527989));
#22791=CARTESIAN_POINT('Ctrl Pts',(-1.90144227950406,0.606946569837811,
24.0396250713602));
#22792=CARTESIAN_POINT('Ctrl Pts',(-1.92027357612706,0.539978661919344,
24.0440705899214));
#22793=CARTESIAN_POINT('Ctrl Pts',(-1.93913773388834,0.472893893132154,
24.0485238660367));
#22794=CARTESIAN_POINT('Ctrl Pts',(-1.95445706520358,0.404909346996058,
24.0529771421519));
#22795=CARTESIAN_POINT('Ctrl Pts',(-1.96617421935367,0.336432016385155,
24.0574304182671));
#22796=CARTESIAN_POINT('Ctrl Pts',(-1.97244841845348,0.299764375030206,
24.059815019565));
#22797=CARTESIAN_POINT('Ctrl Pts',(-1.97769065557813,0.262955533534279,
24.0621996208628));
#22798=CARTESIAN_POINT('Ctrl Pts',(-1.98189826454658,0.226068200964329,
24.0645842221607));
#22799=CARTESIAN_POINT('Ctrl Pts',(-1.99040364133292,0.151503129803286,
24.0694045209754));
#22800=CARTESIAN_POINT('Ctrl Pts',(-1.99470208524478,0.0764491906303517,
24.0742248197901));
#22801=CARTESIAN_POINT('Ctrl Pts',(-1.99474960167085,0.00126060858432954,
24.0790451186048));
#22802=CARTESIAN_POINT('',(-1.99474912756561,0.0018398000541739,21.6791185974309));
#22803=CARTESIAN_POINT('Ctrl Pts',(-1.9947492527556,-0.00172659519609434,
23.2784073370651));
#22804=CARTESIAN_POINT('Ctrl Pts',(-1.99489940380178,0.171744110531787,
23.268297843062));
#22805=CARTESIAN_POINT('Ctrl Pts',(-1.9724229427003,0.34448348214041,23.2584065746183));
#22806=CARTESIAN_POINT('Ctrl Pts',(-1.92332896953422,0.529290084831314,
23.246631304765));
#22807=CARTESIAN_POINT('Ctrl Pts',(-1.9185455129571,0.546374782313945,23.2455319505099));
#22808=CARTESIAN_POINT('Ctrl Pts',(-1.90971110003626,0.576380405088859,
23.2435808450283));
#22809=CARTESIAN_POINT('Ctrl Pts',(-1.90575523383637,0.589328288229115,
23.2427321761686));
#22810=CARTESIAN_POINT('Ctrl Pts',(-1.89975144105552,0.608286380862188,
23.2414792501397));
#22811=CARTESIAN_POINT('Ctrl Pts',(-1.89780607460701,0.614328870074552,
23.2410783578602));
#22812=CARTESIAN_POINT('Ctrl Pts',(-1.89432090012929,0.624979596461161,
23.2403689486663));
#22813=CARTESIAN_POINT('Ctrl Pts',(-1.89279302839988,0.629591708662053,
23.2400608271127));
#22814=CARTESIAN_POINT('Ctrl Pts',(-1.8897764060195,0.63858760680647,23.2394580112928));
#22815=CARTESIAN_POINT('Ctrl Pts',(-1.88828921254927,0.642971885457949,
23.2391633701656));
#22816=CARTESIAN_POINT('Ctrl Pts',(-1.88424340314484,0.654763912780786,
23.2383685847191));
#22817=CARTESIAN_POINT('Ctrl Pts',(-1.88165639167996,0.662161766126466,
23.2378675020128));
#22818=CARTESIAN_POINT('Ctrl Pts',(-1.87194155807373,0.689425726641019,
23.2360115650513));
#22819=CARTESIAN_POINT('Ctrl Pts',(-1.86454237218534,0.709193002487699,
23.2346477202322));
#22820=CARTESIAN_POINT('Ctrl Pts',(-1.79906142641129,0.876016041837107,
23.2229778612225));
#22821=CARTESIAN_POINT('Ctrl Pts',(-1.72400944119378,1.01577462395414,23.2120702178011));
#22822=CARTESIAN_POINT('Ctrl Pts',(-1.60078695790284,1.19151625634831,23.1970949015526));
#22823=CARTESIAN_POINT('Ctrl Pts',(-1.56634159124751,1.23644822130391,23.19314549444));
#22824=CARTESIAN_POINT('Ctrl Pts',(-1.48694712872525,1.33136207722755,23.1846095837393));
#22825=CARTESIAN_POINT('Ctrl Pts',(-1.44128408651554,1.38066613017713,23.1800466557328));
#22826=CARTESIAN_POINT('Ctrl Pts',(-1.38659486276273,1.43403899504209,23.1750421574157));
#22827=CARTESIAN_POINT('Ctrl Pts',(-1.37992883832855,1.44045463722598,23.1744394788972));
#22828=CARTESIAN_POINT('Ctrl Pts',(-1.37102780217901,1.44890284305928,23.1736446659523));
#22829=CARTESIAN_POINT('Ctrl Pts',(-1.36883260332173,1.45097690793098,23.1734494396446));
#22830=CARTESIAN_POINT('Ctrl Pts',(-1.36478958420291,1.45477948685112,23.1730913486875));
#22831=CARTESIAN_POINT('Ctrl Pts',(-1.36294317406247,1.45650948124739,23.1729283713201));
#22832=CARTESIAN_POINT('Ctrl Pts',(-1.35911850477873,1.46007936463732,23.1725919430775));
#22833=CARTESIAN_POINT('Ctrl Pts',(-1.3571398246329,1.46191872467962,23.1724185357982));
#22834=CARTESIAN_POINT('Ctrl Pts',(-1.35259735941805,1.46612418191959,23.1720219043132));
#22835=CARTESIAN_POINT('Ctrl Pts',(-1.35003110422235,1.46848757284468,23.1717988875741));
#22836=CARTESIAN_POINT('Ctrl Pts',(-1.34329596290318,1.47465771927889,23.1712163046297));
#22837=CARTESIAN_POINT('Ctrl Pts',(-1.33911705735108,1.47845356421404,23.1708575521151));
#22838=CARTESIAN_POINT('Ctrl Pts',(-1.31169434007647,1.50315091091942,23.1685206146643));
#22839=CARTESIAN_POINT('Ctrl Pts',(-1.2879765415313,1.52352269268791,23.1665800338312));
#22840=CARTESIAN_POINT('Ctrl Pts',(-1.25485206696472,1.55064736521741,23.1639622597975));
#22841=CARTESIAN_POINT('Ctrl Pts',(-1.24585244230854,1.55788724361022,23.1632600706656));
#22842=CARTESIAN_POINT('Ctrl Pts',(-1.20586560996043,1.58948710719907,23.160177205957));
#22843=CARTESIAN_POINT('Ctrl Pts',(-1.1742218390596,1.61300480819376,23.1578346519009));
#22844=CARTESIAN_POINT('Ctrl Pts',(-1.01796422495945,1.72209864162488,23.1466195989385));
#22845=CARTESIAN_POINT('Ctrl Pts',(-0.884597707779442,1.79425837661051,
23.1380571550944));
#22846=CARTESIAN_POINT('Ctrl Pts',(-0.702479546861747,1.8675083986285,23.1263301953977));
#22847=CARTESIAN_POINT('Ctrl Pts',(-0.66004342976242,1.88292521663852,23.1235989852721));
#22848=CARTESIAN_POINT('Ctrl Pts',(-0.599569372779141,1.90259950449145,
23.1196866433448));
#22849=CARTESIAN_POINT('Ctrl Pts',(-0.581937742373893,1.9080662296082,23.1185436625259));
#22850=CARTESIAN_POINT('Ctrl Pts',(-0.550829658827688,1.9172400812361,23.1165215890655));
#22851=CARTESIAN_POINT('Ctrl Pts',(-0.537385210810333,1.9210517852363,23.1156459040899));
#22852=CARTESIAN_POINT('Ctrl Pts',(-0.517697594082466,1.92641068091167,
23.1143605636898));
#22853=CARTESIAN_POINT('Ctrl Pts',(-0.511485028323538,1.92806949425546,
23.1139545301397));
#22854=CARTESIAN_POINT('Ctrl Pts',(-0.500552758359396,1.93093195691401,
23.1132392233061));
#22855=CARTESIAN_POINT('Ctrl Pts',(-0.495836439353296,1.93214841843303,
23.1129303673742));
#22856=CARTESIAN_POINT('Ctrl Pts',(-0.486654093840431,1.93448095010188,
23.1123285145661));
#22857=CARTESIAN_POINT('Ctrl Pts',(-0.482188562561224,1.93559885898617,
23.1120355793078));
#22858=CARTESIAN_POINT('Ctrl Pts',(-0.470241675788623,1.93854575513296,
23.1112512004687));
#22859=CARTESIAN_POINT('Ctrl Pts',(-0.462753588287392,1.94034687418592,
23.1107588622567));
#22860=CARTESIAN_POINT('Ctrl Pts',(-0.435554129207192,1.9467227920117,23.1089678398856));
#22861=CARTESIAN_POINT('Ctrl Pts',(-0.415784414017754,1.95104082460511,
23.1076609571303));
#22862=CARTESIAN_POINT('Ctrl Pts',(-0.225437569174109,1.98959131143251,
23.0950250351925));
#22863=CARTESIAN_POINT('Ctrl Pts',(-0.0511697036647404,2.00166225353009,
23.0829504625356));
#22864=CARTESIAN_POINT('Ctrl Pts',(0.224179776813687,1.98473372414726,23.063712973047));
#22865=CARTESIAN_POINT('Ctrl Pts',(0.325335266638371,1.97068162455681,23.0566362422489));
#22866=CARTESIAN_POINT('Ctrl Pts',(0.439424508758674,1.94580373550329,23.0489285950421));
#22867=CARTESIAN_POINT('Ctrl Pts',(0.453832404026459,1.94249382408422,23.0479604855709));
#22868=CARTESIAN_POINT('Ctrl Pts',(0.472692289274206,1.93793985818632,23.0467013352492));
#22869=CARTESIAN_POINT('Ctrl Pts',(0.477178172348412,1.9368401811095,23.0464024466736));
#22870=CARTESIAN_POINT('Ctrl Pts',(0.484117246615384,1.93511355342052,23.0459410846895));
#22871=CARTESIAN_POINT('Ctrl Pts',(0.48657309400842,1.93449750515866,23.0457779917306));
#22872=CARTESIAN_POINT('Ctrl Pts',(0.491645179992134,1.93321490485597,23.0454415571628));
#22873=CARTESIAN_POINT('Ctrl Pts',(0.494261205674138,1.93254772568213,23.0452682583259));
#22874=CARTESIAN_POINT('Ctrl Pts',(0.500238552677646,1.93101035942966,23.0448727910667));
#22875=CARTESIAN_POINT('Ctrl Pts',(0.503598955437186,1.93013670768135,23.0446508256534));
#22876=CARTESIAN_POINT('Ctrl Pts',(0.513932494918911,1.92742132631619,23.0439693288622));
#22877=CARTESIAN_POINT('Ctrl Pts',(0.520898034804708,1.92555052378309,23.0435114483241));
#22878=CARTESIAN_POINT('Ctrl Pts',(0.577772648559834,1.90994395083988,23.0397838888185));
#22879=CARTESIAN_POINT('Ctrl Pts',(0.627144861339185,1.89430660604481,23.0366179298728));
#22880=CARTESIAN_POINT('Ctrl Pts',(0.846498534727965,1.81531332104591,23.022637599023));
#22881=CARTESIAN_POINT('Ctrl Pts',(1.00796759534284,1.73087643441346,23.0125057537943));
#22882=CARTESIAN_POINT('Ctrl Pts',(1.19198945924644,1.60004977177471,22.9990079625898));
#22883=CARTESIAN_POINT('Ctrl Pts',(1.22729861822341,1.57312931180532,22.9963205015641));
#22884=CARTESIAN_POINT('Ctrl Pts',(1.2758069467884,1.53351782076213,22.9924665092481));
#22885=CARTESIAN_POINT('Ctrl Pts',(1.2897759067463,1.52178787908598,22.9913368281267));
#22886=CARTESIAN_POINT('Ctrl Pts',(1.31405888529558,1.50082257618495,22.9893363654208));
#22887=CARTESIAN_POINT('Ctrl Pts',(1.32444141570741,1.49166822055837,22.9884688904352));
#22888=CARTESIAN_POINT('Ctrl Pts',(1.33948782066421,1.47812075616335,22.987193391538));
#22889=CARTESIAN_POINT('Ctrl Pts',(1.34422729453372,1.47381191832117,22.9867889104323));
#22890=CARTESIAN_POINT('Ctrl Pts',(1.3525312540081,1.46618909311492,22.986075389714));
#22891=CARTESIAN_POINT('Ctrl Pts',(1.35610453573722,1.46288473137947,22.9857667607986));
#22892=CARTESIAN_POINT('Ctrl Pts',(1.3630395892598,1.45642435519384,22.9851646383765));
#22893=CARTESIAN_POINT('Ctrl Pts',(1.36640258384193,1.4532696936815,22.984871203965));
#22894=CARTESIAN_POINT('Ctrl Pts',(1.37538231926807,1.44478751675164,22.9840837715075));
#22895=CARTESIAN_POINT('Ctrl Pts',(1.38097899105617,1.43943895882334,22.9835888660634));
#22896=CARTESIAN_POINT('Ctrl Pts',(1.40127097731044,1.41981929355098,22.9817791982691));
#22897=CARTESIAN_POINT('Ctrl Pts',(1.41577694970131,1.40535502803365,22.9804560145121));
#22898=CARTESIAN_POINT('Ctrl Pts',(1.54887832470058,1.26848393434861,22.9680313866217));
#22899=CARTESIAN_POINT('Ctrl Pts',(1.65152682314986,1.13159648599117,22.9562182900774));
#22900=CARTESIAN_POINT('Ctrl Pts',(1.79182953512,0.8839822124736,22.9363669834231));
#22901=CARTESIAN_POINT('Ctrl Pts',(1.83951143776093,0.779924285922606,22.9284292754728));
#22902=CARTESIAN_POINT('Ctrl Pts',(1.88074322445812,0.664753712432432,22.9204356373407));
#22903=CARTESIAN_POINT('Ctrl Pts',(1.8834149230623,0.657145956000921,22.9199112257996));
#22904=CARTESIAN_POINT('Ctrl Pts',(1.88722373872034,0.646086161423059,22.9191543151094));
#22905=CARTESIAN_POINT('Ctrl Pts',(1.88839762505644,0.642647008992073,22.9189197082477));
#22906=CARTESIAN_POINT('Ctrl Pts',(1.8904338942683,0.636627563955998,22.9185104379808));
#22907=CARTESIAN_POINT('Ctrl Pts',(1.89130040459761,0.634048691915502,22.9183355314295));
#22908=CARTESIAN_POINT('Ctrl Pts',(1.89310615953207,0.628637839473811,22.9179694702294));
#22909=CARTESIAN_POINT('Ctrl Pts',(1.89404432517614,0.625805528124738,22.917778379715));
#22910=CARTESIAN_POINT('Ctrl Pts',(1.89651003194754,0.618305251623333,22.9172737104863));
#22911=CARTESIAN_POINT('Ctrl Pts',(1.89802670573874,0.613633694480815,22.9169607680206));
#22912=CARTESIAN_POINT('Ctrl Pts',(1.90336686457588,0.59697606646518,22.9158496824772));
#22913=CARTESIAN_POINT('Ctrl Pts',(1.90709428842756,0.584959177526419,22.9150569551356));
#22914=CARTESIAN_POINT('Ctrl Pts',(1.96288578613714,0.398888545053495,22.9029063986842));
#22915=CARTESIAN_POINT('Ctrl Pts',(1.99105536719381,0.218527942337301,22.8927409605768));
#22916=CARTESIAN_POINT('Ctrl Pts',(1.99632964599413,-0.0671472086073016,
22.8760074279757));
#22917=CARTESIAN_POINT('Ctrl Pts',(1.99011646855187,-0.171093040492514,
22.8698000834706));
#22918=CARTESIAN_POINT('Ctrl Pts',(1.97379153888453,-0.288782021070179,
22.8623993525615));
#22919=CARTESIAN_POINT('Ctrl Pts',(1.97158699706026,-0.303467936998391,
22.8614693729235));
#22920=CARTESIAN_POINT('Ctrl Pts',(1.96816756465189,-0.324634321716895,
22.8601191420597));
#22921=CARTESIAN_POINT('Ctrl Pts',(1.96708416367084,-0.331135767817606,
22.8597030570557));
#22922=CARTESIAN_POINT('Ctrl Pts',(1.96513981691095,-0.342457350024902,
22.8589760877232));
#22923=CARTESIAN_POINT('Ctrl Pts',(1.96429330374573,-0.34727993428171,22.8586656641692));
#22924=CARTESIAN_POINT('Ctrl Pts',(1.96262447290281,-0.356585919235362,
22.8580651598019));
#22925=CARTESIAN_POINT('Ctrl Pts',(1.96180452575304,-0.361069718476592,
22.8577751562371));
#22926=CARTESIAN_POINT('Ctrl Pts',(1.95982398034336,-0.371694207110537,
22.8570863786607));
#22927=CARTESIAN_POINT('Ctrl Pts',(1.95864988385309,-0.377832302138153,
22.8566871764839));
#22928=CARTESIAN_POINT('Ctrl Pts',(1.95441074102143,-0.399443395158241,
22.8552771021699));
#22929=CARTESIAN_POINT('Ctrl Pts',(1.95119109208131,-0.414885127426448,
22.8542613117072));
#22930=CARTESIAN_POINT('Ctrl Pts',(1.94624691363325,-0.437266054436639,
22.8527766881474));
#22931=CARTESIAN_POINT('Ctrl Pts',(1.94466761536991,-0.444237002862461,
22.8523125252483));
#22932=CARTESIAN_POINT('Ctrl Pts',(1.90638520058454,-0.6090969456747,22.841293411604));
#22933=CARTESIAN_POINT('Ctrl Pts',(1.85061664949302,-0.761905991173004,
22.8300934346233));
#22934=CARTESIAN_POINT('Ctrl Pts',(1.74153493599781,-0.975795969344882,
22.8133413262106));
#22935=CARTESIAN_POINT('Ctrl Pts',(1.70201483118059,-1.04320108220321,22.8078978346983));
#22936=CARTESIAN_POINT('Ctrl Pts',(1.64136094097861,-1.13398841818731,22.800471181571));
#22937=CARTESIAN_POINT('Ctrl Pts',(1.62347421338004,-1.1594512392648,22.7983774952092));
#22938=CARTESIAN_POINT('Ctrl Pts',(1.59437972844739,-1.19887472761427,22.7951311061));
#22939=CARTESIAN_POINT('Ctrl Pts',(1.58356786047875,-1.21312003409577,22.7939570466494));
#22940=CARTESIAN_POINT('Ctrl Pts',(1.56952398704838,-1.23111593934856,22.7924745981308));
#22941=CARTESIAN_POINT('Ctrl Pts',(1.56646802467499,-1.23500199634667,22.7921545206208));
#22942=CARTESIAN_POINT('Ctrl Pts',(1.56154011609277,-1.24122075925653,22.791642434251));
#22943=CARTESIAN_POINT('Ctrl Pts',(1.55967734029929,-1.24356065466187,22.7914497834867));
#22944=CARTESIAN_POINT('Ctrl Pts',(1.55611145585771,-1.24801926619274,22.7910827619239));
#22945=CARTESIAN_POINT('Ctrl Pts',(1.55440929976673,-1.25013866459532,22.790908330469));
#22946=CARTESIAN_POINT('Ctrl Pts',(1.55046984493898,-1.25502329622993,22.7905063750542));
#22947=CARTESIAN_POINT('Ctrl Pts',(1.54822947924408,-1.2577860287917,22.7902790747557));
#22948=CARTESIAN_POINT('Ctrl Pts',(1.54101720620963,-1.26663145824277,22.7895514167534));
#22949=CARTESIAN_POINT('Ctrl Pts',(1.53601667299004,-1.27269087607779,22.7890530811784));
#22950=CARTESIAN_POINT('Ctrl Pts',(1.47057524992667,-1.35104225745904,22.7826087275976));
#22951=CARTESIAN_POINT('Ctrl Pts',(1.40511221180769,-1.41900371886646,22.777009669299));
#22952=CARTESIAN_POINT('Ctrl Pts',(1.20784053647726,-1.59670788465467,22.7614854606171));
#22953=CARTESIAN_POINT('Ctrl Pts',(1.06638254649067,-1.69445589350048,22.7517663922293));
#22954=CARTESIAN_POINT('Ctrl Pts',(0.881410211152412,-1.78983321367631,
22.7390576890241));
#22955=CARTESIAN_POINT('Ctrl Pts',(0.848180547462305,-1.80581737135943,
22.7367781174496));
#22956=CARTESIAN_POINT('Ctrl Pts',(0.806063898861428,-1.82465737695657,
22.7338849767244));
#22957=CARTESIAN_POINT('Ctrl Pts',(0.797572963830665,-1.82838478308745,
22.7333015208749));
#22958=CARTESIAN_POINT('Ctrl Pts',(0.784040115038235,-1.83421331694995,
22.7323711900482));
#22959=CARTESIAN_POINT('Ctrl Pts',(0.779014957207658,-1.83635320391942,
22.7320256389008));
#22960=CARTESIAN_POINT('Ctrl Pts',(0.7695391704228,-1.84034242887845,22.7313738445211));
#22961=CARTESIAN_POINT('Ctrl Pts',(0.765090495865998,-1.84219633123379,
22.7310677591127));
#22962=CARTESIAN_POINT('Ctrl Pts',(0.755074872781552,-1.84632761889957,
22.7303784410754));
#22963=CARTESIAN_POINT('Ctrl Pts',(0.749504273242664,-1.84859597611245,
22.7299949061505));
#22964=CARTESIAN_POINT('Ctrl Pts',(0.735291845640043,-1.85430849844004,
22.7290159778119));
#22965=CARTESIAN_POINT('Ctrl Pts',(0.726636100967313,-1.85771743748934,
22.7284194044127));
#22966=CARTESIAN_POINT('Ctrl Pts',(0.702825541053477,-1.86690301181164,
22.726777139125));
#22967=CARTESIAN_POINT('Ctrl Pts',(0.68762389157369,-1.87255546101241,22.7257273310065));
#22968=CARTESIAN_POINT('Ctrl Pts',(0.521421943171681,-1.93205784487764,
22.7142330279155));
#22969=CARTESIAN_POINT('Ctrl Pts',(0.364554065561413,-1.96769114330824,
22.7031638822829));
#22970=CARTESIAN_POINT('Ctrl Pts',(0.126266568804543,-1.99232873994268,
22.6864494637566));
#22971=CARTESIAN_POINT('Ctrl Pts',(0.0469604868819839,-1.99577379931077,
22.6809167662677));
#22972=CARTESIAN_POINT('Ctrl Pts',(-0.0637430796203894,-1.99397857876174,
22.6733835679092));
#22973=CARTESIAN_POINT('Ctrl Pts',(-0.095128121130232,-1.99272793566527,
22.6712696456375));
#22974=CARTESIAN_POINT('Ctrl Pts',(-0.144438823931425,-1.98959520698629,
22.6679954054893));
#22975=CARTESIAN_POINT('Ctrl Pts',(-0.16238986498644,-1.988210564608,22.6668133067906));
#22976=CARTESIAN_POINT('Ctrl Pts',(-0.185255482074356,-1.98613507194462,
22.6653222201655));
#22977=CARTESIAN_POINT('Ctrl Pts',(-0.190188887105685,-1.98566873021372,
22.6650013797042));
#22978=CARTESIAN_POINT('Ctrl Pts',(-0.19809962093472,-1.98489119681239,
22.6644883639014));
#22979=CARTESIAN_POINT('Ctrl Pts',(-0.20107803616472,-1.98459168260386,
22.6642955425731));
#22980=CARTESIAN_POINT('Ctrl Pts',(-0.206759082776146,-1.98400746703817,
22.6639283996267));
#22981=CARTESIAN_POINT('Ctrl Pts',(-0.209461773434491,-1.98372395083625,
22.6637540165225));
#22982=CARTESIAN_POINT('Ctrl Pts',(-0.215695447291557,-1.98305714766182,
22.6633524424185));
#22983=CARTESIAN_POINT('Ctrl Pts',(-0.219225990961452,-1.98266995292684,
22.6631254737005));
#22984=CARTESIAN_POINT('Ctrl Pts',(-0.230534283410593,-1.98139919754019,
22.6623999455805));
#22985=CARTESIAN_POINT('Ctrl Pts',(-0.238307993341783,-1.98047927053248,
22.6619033917045));
#22986=CARTESIAN_POINT('Ctrl Pts',(-0.331322086997792,-1.96891655200613,
22.6559862032511));
#22987=CARTESIAN_POINT('Ctrl Pts',(-0.41580669748798,-1.95282246036435,
22.6508534983321));
#22988=CARTESIAN_POINT('Ctrl Pts',(-0.594183396951104,-1.90673497566668,
22.6400436085755));
#22989=CARTESIAN_POINT('Ctrl Pts',(-0.687419122200089,-1.87513940891472,
22.6344058274439));
#22990=CARTESIAN_POINT('Ctrl Pts',(-0.871823303580205,-1.79703794755343,
22.6226977915133));
#22991=CARTESIAN_POINT('Ctrl Pts',(-0.962501982539506,-1.75014491569914,
22.6166345067782));
#22992=CARTESIAN_POINT('Ctrl Pts',(-1.06610356363666,-1.68607416129696,
22.6090857557789));
#22993=CARTESIAN_POINT('Ctrl Pts',(-1.08285599885455,-1.67536435641059,
22.6078448309455));
#22994=CARTESIAN_POINT('Ctrl Pts',(-1.10562645089442,-1.66032303942571,
22.6061287763047));
#22995=CARTESIAN_POINT('Ctrl Pts',(-1.11178495434079,-1.65620549965024,
22.6056616556944));
#22996=CARTESIAN_POINT('Ctrl Pts',(-1.12210492745288,-1.64922212683239,
22.6048737645673));
#22997=CARTESIAN_POINT('Ctrl Pts',(-1.12627873728325,-1.64637459195147,
22.6045536874333));
#22998=CARTESIAN_POINT('Ctrl Pts',(-1.13449316927295,-1.64072453262732,
22.60392091027));
#22999=CARTESIAN_POINT('Ctrl Pts',(-1.13853433774948,-1.6379228626968,22.6036082442668));
#23000=CARTESIAN_POINT('Ctrl Pts',(-1.14739679455849,-1.63173003374059,
22.602919523392));
#23001=CARTESIAN_POINT('Ctrl Pts',(-1.1522134807747,-1.62833239870155,22.6025432222784));
#23002=CARTESIAN_POINT('Ctrl Pts',(-1.16892298976981,-1.61643444073414,
22.6012308146831));
#23003=CARTESIAN_POINT('Ctrl Pts',(-1.18073714609981,-1.60782493764149,
22.6002905104766));
#23004=CARTESIAN_POINT('Ctrl Pts',(-1.19992835209821,-1.59351385715911,
22.5987422928034));
#23005=CARTESIAN_POINT('Ctrl Pts',(-1.20736208790122,-1.58788892776655,
22.5981373915182));
#23006=CARTESIAN_POINT('Ctrl Pts',(-1.34300582784669,-1.48374736444706,
22.5870032120367));
#23007=CARTESIAN_POINT('Ctrl Pts',(-1.45878315193137,-1.37007366965008,
22.5758333061371));
#23008=CARTESIAN_POINT('Ctrl Pts',(-1.60840515543387,-1.1824546710807,22.5590898808915));
#23009=CARTESIAN_POINT('Ctrl Pts',(-1.65360654159593,-1.11837063565539,
22.5536259534026));
#23010=CARTESIAN_POINT('Ctrl Pts',(-1.71136257825583,-1.02529887140285,
22.5461748860087));
#23011=CARTESIAN_POINT('Ctrl Pts',(-1.72717988718325,-0.998423514920038,
22.5440765580716));
#23012=CARTESIAN_POINT('Ctrl Pts',(-1.75108126929563,-0.955543150079855,
22.540823777461));
#23013=CARTESIAN_POINT('Ctrl Pts',(-1.7595903382555,-0.939782006625218,
22.5396478711321));
#23014=CARTESIAN_POINT('Ctrl Pts',(-1.77017731447375,-0.919523955079091,
22.5381634376108));
#23015=CARTESIAN_POINT('Ctrl Pts',(-1.77245201926606,-0.915131613110703,
22.5378431843751));
#23016=CARTESIAN_POINT('Ctrl Pts',(-1.77607615698756,-0.908069378160911,
22.5373308839325));
#23017=CARTESIAN_POINT('Ctrl Pts',(-1.7774359447346,-0.905404867243701,
22.5371381938817));
#23018=CARTESIAN_POINT('Ctrl Pts',(-1.78001986208449,-0.90031341289305,
22.5367711444385));
#23019=CARTESIAN_POINT('Ctrl Pts',(-1.78124501000241,-0.897887055965062,
22.5365967241986));
#23020=CARTESIAN_POINT('Ctrl Pts',(-1.78406139681554,-0.892280862686914,
22.5361948569657));
#23021=CARTESIAN_POINT('Ctrl Pts',(-1.78564909528378,-0.889099271462731,
22.5359676333153));
#23022=CARTESIAN_POINT('Ctrl Pts',(-1.7907144497849,-0.878880502161535,
22.5352404680016));
#23023=CARTESIAN_POINT('Ctrl Pts',(-1.79415913260376,-0.871826926368618,
22.5347425446204));
#23024=CARTESIAN_POINT('Ctrl Pts',(-1.83693946489664,-0.782899451156252,
22.5285129520476));
#23025=CARTESIAN_POINT('Ctrl Pts',(-1.87068570914006,-0.698439549331201,
22.523103492427));
#23026=CARTESIAN_POINT('Ctrl Pts',(-1.93625134309907,-0.495027903713703,
22.5105906628112));
#23027=CARTESIAN_POINT('Ctrl Pts',(-1.96305870021421,-0.374863490957609,
22.5035765390543));
#23028=CARTESIAN_POINT('Ctrl Pts',(-1.98936137568163,-0.169154360979053,
22.4913011048295));
#23029=CARTESIAN_POINT('Ctrl Pts',(-1.99474073217265,-0.0847262876506961,
22.4861927592061));
#23030=CARTESIAN_POINT('Ctrl Pts',(-1.99475112955633,0.0102038276302703,
22.4802577665153));
#23031=CARTESIAN_POINT('Ctrl Pts',(-1.99467058831744,0.0206258208173814,
22.4796036818783));
#23032=CARTESIAN_POINT('Ctrl Pts',(-1.99441052938746,0.0373326605575081,
22.4785509509724));
#23033=CARTESIAN_POINT('Ctrl Pts',(-1.99428296314659,0.0436182153457306,
22.4781539306143));
#23034=CARTESIAN_POINT('Ctrl Pts',(-1.99400396820605,0.0547668623345773,
22.4774480020702));
#23035=CARTESIAN_POINT('Ctrl Pts',(-1.99386445633228,0.059630223203031,
22.4771394694905));
#23036=CARTESIAN_POINT('Ctrl Pts',(-1.99353720471725,0.0697467317808887,
22.4764964356248));
#23037=CARTESIAN_POINT('Ctrl Pts',(-1.99334649055535,0.0749997393650962,
22.4761618434785));
#23038=CARTESIAN_POINT('Ctrl Pts',(-1.99279910155984,0.0885946860519297,
22.4752940762535));
#23039=CARTESIAN_POINT('Ctrl Pts',(-1.99241081214924,0.0969351829329676,
22.4747599144674));
#23040=CARTESIAN_POINT('Ctrl Pts',(-1.99053186476983,0.132488562882764,
22.4724751231784));
#23041=CARTESIAN_POINT('Ctrl Pts',(-1.98853601091771,0.159670707486427,
22.4707087513756));
#23042=CARTESIAN_POINT('Ctrl Pts',(-1.98188605987933,0.230369475588433,
22.4660610626453));
#23043=CARTESIAN_POINT('Ctrl Pts',(-1.97635590473971,0.273786974072694,
22.4631535490953));
#23044=CARTESIAN_POINT('Ctrl Pts',(-1.9413764756979,0.491111472763187,22.4483315183634));
#23045=CARTESIAN_POINT('Ctrl Pts',(-1.89037919748841,0.660745567678301,
22.4357970051439));
#23046=CARTESIAN_POINT('Ctrl Pts',(-1.79409402071138,0.873819015165399,
22.4197682710196));
#23047=CARTESIAN_POINT('Ctrl Pts',(-1.76816196099366,0.925169023630686,
22.4158906578821));
#23048=CARTESIAN_POINT('Ctrl Pts',(-1.73679187187874,0.981134962362514,
22.4117032482282));
#23049=CARTESIAN_POINT('Ctrl Pts',(-1.73350998349171,0.986921962846886,
22.4112707450058));
#23050=CARTESIAN_POINT('Ctrl Pts',(-1.72850361193248,0.995647746023252,
22.4106194652532));
#23051=CARTESIAN_POINT('Ctrl Pts',(-1.72680049077688,0.998598636139177,
22.4103993645986));
#23052=CARTESIAN_POINT('Ctrl Pts',(-1.7238256741348,1.00372254465682,22.4100174629333));
#23053=CARTESIAN_POINT('Ctrl Pts',(-1.72255741631258,1.00589753411517,22.4098554418575));
#23054=CARTESIAN_POINT('Ctrl Pts',(-1.71987735310241,1.01047375609972,22.4095147413663));
#23055=CARTESIAN_POINT('Ctrl Pts',(-1.71846463131751,1.01287444066157,22.4093361242915));
#23056=CARTESIAN_POINT('Ctrl Pts',(-1.71501102697897,1.01871523953045,22.4089018131834));
#23057=CARTESIAN_POINT('Ctrl Pts',(-1.71296480278288,1.02215221323185,22.4086464657524));
#23058=CARTESIAN_POINT('Ctrl Pts',(-1.70565529567986,1.03434615105033,22.4077412223584));
#23059=CARTESIAN_POINT('Ctrl Pts',(-1.70033497730051,1.04306899265292,22.4070949435868));
#23060=CARTESIAN_POINT('Ctrl Pts',(-1.66843593103339,1.09447586278817,22.4032914218129));
#23061=CARTESIAN_POINT('Ctrl Pts',(-1.64031559347395,1.13618729273205,22.4002266274959));
#23062=CARTESIAN_POINT('Ctrl Pts',(-1.55172778104536,1.25743495250759,22.3912420917059));
#23063=CARTESIAN_POINT('Ctrl Pts',(-1.48683278847187,1.33354134809347,22.3854943850943));
#23064=CARTESIAN_POINT('Ctrl Pts',(-1.3160535036731,1.50578419587836,22.3714138056933));
#23065=CARTESIAN_POINT('Ctrl Pts',(-1.20503807378247,1.59601307294226,22.3630441238972));
#23066=CARTESIAN_POINT('Ctrl Pts',(-1.07456233244342,1.68062754313318,22.3533364246023));
#23067=CARTESIAN_POINT('Ctrl Pts',(-1.06369868729427,1.68752429177564,22.3525293779118));
#23068=CARTESIAN_POINT('Ctrl Pts',(-1.04748761789267,1.69759710144086,22.3513265585637));
#23069=CARTESIAN_POINT('Ctrl Pts',(-1.04219069416228,1.7008541336746,22.3509337728373));
#23070=CARTESIAN_POINT('Ctrl Pts',(-1.0327428142645,1.70660284787424,22.350233550599));
#23071=CARTESIAN_POINT('Ctrl Pts',(-1.0285978345157,1.70910429609778,22.3499264750104));
#23072=CARTESIAN_POINT('Ctrl Pts',(-1.01986088817699,1.71433364861487,22.3492794537948));
#23073=CARTESIAN_POINT('Ctrl Pts',(-1.01526699569827,1.71705824494605,22.3489393907102));
#23074=CARTESIAN_POINT('Ctrl Pts',(-1.00313538583759,1.72418768697949,22.3480416865375));
#23075=CARTESIAN_POINT('Ctrl Pts',(-0.995579662025072,1.72856151605712,
22.3474829270845));
#23076=CARTESIAN_POINT('Ctrl Pts',(-0.961174433151073,1.74817747608927,
22.3449399319126));
#23077=CARTESIAN_POINT('Ctrl Pts',(-0.934003225952079,1.76284388845325,
22.3429351945449));
#23078=CARTESIAN_POINT('Ctrl Pts',(-0.860300200539954,1.80044481261374,
22.3375032371334));
#23079=CARTESIAN_POINT('Ctrl Pts',(-0.8131984648607,1.82220345600647,22.3340375032315));
#23080=CARTESIAN_POINT('Ctrl Pts',(-0.671797997957731,1.88094866216494,
22.3236547158045));
#23081=CARTESIAN_POINT('Ctrl Pts',(-0.575475403203092,1.91261736277786,
22.3166009573889));
#23082=CARTESIAN_POINT('Ctrl Pts',(-0.41590012443275,1.95193163595939,22.3051349263968));
#23083=CARTESIAN_POINT('Ctrl Pts',(-0.353941300566931,1.96411206290793,
22.3007373953101));
#23084=CARTESIAN_POINT('Ctrl Pts',(-0.235281884923783,1.98164080282252,
22.2925179264074));
#23085=CARTESIAN_POINT('Ctrl Pts',(-0.178720983214047,1.9875406967794,22.2886861387096));
#23086=CARTESIAN_POINT('Ctrl Pts',(-0.114627291754193,1.99146740079931,
22.2844952308409));
#23087=CARTESIAN_POINT('Ctrl Pts',(-0.107272226548183,1.99187712923906,
22.284016553547));
#23088=CARTESIAN_POINT('Ctrl Pts',(-0.0964544870976982,1.99241965939637,
22.2833159936367));
#23089=CARTESIAN_POINT('Ctrl Pts',(-0.0929935734136764,1.99258419219363,
22.2830923862285));
#23090=CARTESIAN_POINT('Ctrl Pts',(-0.0868293905717075,1.99286114404596,
22.2826950735144));
#23091=CARTESIAN_POINT('Ctrl Pts',(-0.084126305969816,1.992977081529,22.2825211725213));
#23092=CARTESIAN_POINT('Ctrl Pts',(-0.0783849786478261,1.99321163007509,
22.2821525075817));
#23093=CARTESIAN_POINT('Ctrl Pts',(-0.0753467073484952,1.99332879403751,
22.2819578259026));
#23094=CARTESIAN_POINT('Ctrl Pts',(-0.0671452677217028,1.99362628544087,
22.2814333935126));
#23095=CARTESIAN_POINT('Ctrl Pts',(-0.0619816028323414,1.99379350368177,
22.2811043708301));
#23096=CARTESIAN_POINT('Ctrl Pts',(-0.0364988061753795,1.99451963518245,
22.2794861154271));
#23097=CARTESIAN_POINT('Ctrl Pts',(-0.0161717109281678,1.99478803175302,
22.2782124501692));
#23098=CARTESIAN_POINT('Ctrl Pts',(0.041415696194476,1.9946680245351,22.2746438133625));
#23099=CARTESIAN_POINT('Ctrl Pts',(0.0786674710410893,1.99354648149933,
22.2723823904248));
#23100=CARTESIAN_POINT('Ctrl Pts',(0.215010420764463,1.98561338880275,22.2642077895884));
#23101=CARTESIAN_POINT('Ctrl Pts',(0.313589617462195,1.9724487477969,22.2584903442219));
#23102=CARTESIAN_POINT('Ctrl Pts',(0.551468306609822,1.92238890172888,22.2443805624144));
#23103=CARTESIAN_POINT('Ctrl Pts',(0.688517929913839,1.87766636357191,22.2359514793444));
#23104=CARTESIAN_POINT('Ctrl Pts',(0.831278386553244,1.81333089533958,22.2261763621779));
#23105=CARTESIAN_POINT('Ctrl Pts',(0.842942442268593,1.80793825078633,22.2253704091527));
#23106=CARTESIAN_POINT('Ctrl Pts',(0.860168933230003,1.79977098314399,22.2241689091766));
#23107=CARTESIAN_POINT('Ctrl Pts',(0.865771973903007,1.79708237797969,22.2237763395186));
#23108=CARTESIAN_POINT('Ctrl Pts',(0.87571689947265,1.79225302583458,22.2230763600458));
#23109=CARTESIAN_POINT('Ctrl Pts',(0.880063747065188,1.79012256481499,22.2227693102396));
#23110=CARTESIAN_POINT('Ctrl Pts',(0.889191862383118,1.78560744324897,22.222122197365));
#23111=CARTESIAN_POINT('Ctrl Pts',(0.893971383646201,1.7832193566189,22.2217820162824));
#23112=CARTESIAN_POINT('Ctrl Pts',(0.90654259092734,1.77687491297745,22.220883667149));
#23113=CARTESIAN_POINT('Ctrl Pts',(0.914317905637967,1.77288654147205,22.2203243778276));
#23114=CARTESIAN_POINT('Ctrl Pts',(0.94951787304008,1.75453746343677,22.2177755058577));
#23115=CARTESIAN_POINT('Ctrl Pts',(0.976630877052434,1.73959128897639,22.2157653053747));
#23116=CARTESIAN_POINT('Ctrl Pts',(1.04837939618225,1.69783349617416,22.2103149144964));
#23117=CARTESIAN_POINT('Ctrl Pts',(1.09232882632352,1.66989666927832,22.206835888048));
#23118=CARTESIAN_POINT('Ctrl Pts',(1.21852016881137,1.58256748347739,22.1964281286322));
#23119=CARTESIAN_POINT('Ctrl Pts',(1.29737946524444,1.51858962973985,22.1893627730914));
#23120=CARTESIAN_POINT('Ctrl Pts',(1.45756737938829,1.3670113913473,22.1739768007585));
#23121=CARTESIAN_POINT('Ctrl Pts',(1.53660883203062,1.27752229590784,22.1656815236915));
#23122=CARTESIAN_POINT('Ctrl Pts',(1.61171713907721,1.1753525802301,22.1574015376432));
#23123=CARTESIAN_POINT('Ctrl Pts',(1.61620292735164,1.16917660190197,22.156905362334));
#23124=CARTESIAN_POINT('Ctrl Pts',(1.62270276408493,1.16011881277242,22.1561841521045));
#23125=CARTESIAN_POINT('Ctrl Pts',(1.62474475266373,1.1572572788599,22.1559572459319));
#23126=CARTESIAN_POINT('Ctrl Pts',(1.62834881367573,1.15217839760242,22.155556195608));
#23127=CARTESIAN_POINT('Ctrl Pts',(1.62991393982904,1.14996324637169,22.1553818422289));
#23128=CARTESIAN_POINT('Ctrl Pts',(1.63320772413744,1.14528126044184,22.1550145223358));
#23129=CARTESIAN_POINT('Ctrl Pts',(1.63493530976434,1.14281370698911,22.1548216291984));
#23130=CARTESIAN_POINT('Ctrl Pts',(1.63953814260921,1.13620756732195,22.1543070451041));
#23131=CARTESIAN_POINT('Ctrl Pts',(1.64240333127733,1.13206194877011,22.1539860358096));
#23132=CARTESIAN_POINT('Ctrl Pts',(1.65593643393266,1.11232148647098,22.152466297353));
#23133=CARTESIAN_POINT('Ctrl Pts',(1.66639856674365,1.09658581167,22.1512809451576));
#23134=CARTESIAN_POINT('Ctrl Pts',(1.69483935913605,1.05246189552209,22.1480218283361));
#23135=CARTESIAN_POINT('Ctrl Pts',(1.71232739913355,1.02376347123415,22.1459749988323));
#23136=CARTESIAN_POINT('Ctrl Pts',(1.77317277487014,0.91798931282505,22.138640469828));
#23137=CARTESIAN_POINT('Ctrl Pts',(1.81212052145354,0.838491164759395,22.133518311605));
#23138=CARTESIAN_POINT('Ctrl Pts',(1.90161886261521,0.620186069472018,22.1198347949095));
#23139=CARTESIAN_POINT('Ctrl Pts',(1.94225405921951,0.477940508038958,22.1112715833456));
#23140=CARTESIAN_POINT('Ctrl Pts',(1.96915222389969,0.3188411085778,22.1012899361543));
#23141=CARTESIAN_POINT('Ctrl Pts',(1.97132262070656,0.305134795598925,22.1004272378053));
#23142=CARTESIAN_POINT('Ctrl Pts',(1.97492353201607,0.280750163991763,22.0988869070206));
#23143=CARTESIAN_POINT('Ctrl Pts',(1.9764108921075,0.270080710512796,22.0982110685707));
#23144=CARTESIAN_POINT('Ctrl Pts',(1.9786426483581,0.253064536842356,22.0971300215973));
#23145=CARTESIAN_POINT('Ctrl Pts',(1.97944310948491,0.246725281395549,22.096726582603));
#23146=CARTESIAN_POINT('Ctrl Pts',(1.98080137446067,0.235536214890278,22.0960132126866));
#23147=CARTESIAN_POINT('Ctrl Pts',(1.98137186105829,0.230687973467998,22.0957036842872));
#23148=CARTESIAN_POINT('Ctrl Pts',(1.98251467891323,0.22065874214856,22.0950624862996));
#23149=CARTESIAN_POINT('Ctrl Pts',(1.98308451013029,0.215477510251902,22.0947307404343));
#23150=CARTESIAN_POINT('Ctrl Pts',(1.98449327061911,0.202189145803423,22.0938786113204));
#23151=CARTESIAN_POINT('Ctrl Pts',(1.9853028251675,0.194079058443926,22.0933573077001));
#23152=CARTESIAN_POINT('Ctrl Pts',(1.98844201081966,0.160553171225484,22.0911970510066));
#23153=CARTESIAN_POINT('Ctrl Pts',(1.99033336811422,0.135099720064538,22.0895444119469));
#23154=CARTESIAN_POINT('Ctrl Pts',(2.00177901562873,-0.0728653863915378,
22.0759329134262));
#23155=CARTESIAN_POINT('Ctrl Pts',(1.98669331201354,-0.255832244915403,
22.0631559690902));
#23156=CARTESIAN_POINT('Ctrl Pts',(1.92596453455098,-0.528177844569036,
22.0437408037614));
#23157=CARTESIAN_POINT('Ctrl Pts',(1.89820549146989,-0.620590021843092,
22.0371051157657));
#23158=CARTESIAN_POINT('Ctrl Pts',(1.86107222929613,-0.717982881631027,
22.0302965103033));
#23159=CARTESIAN_POINT('Ctrl Pts',(1.85823050557929,-0.725305903791294,
22.0297857685802));
#23160=CARTESIAN_POINT('Ctrl Pts',(1.8540392792451,-0.735920215445776,22.0290474239287));
#23161=CARTESIAN_POINT('Ctrl Pts',(1.85272415845232,-0.73922486812476,22.0288178236047));
#23162=CARTESIAN_POINT('Ctrl Pts',(1.8503883465027,-0.745048937041736,22.0284136884696));
#23163=CARTESIAN_POINT('Ctrl Pts',(1.84937133576502,-0.747569805618463,
22.0282389333788));
#23164=CARTESIAN_POINT('Ctrl Pts',(1.84722448041796,-0.752860031488306,
22.0278725607555));
#23165=CARTESIAN_POINT('Ctrl Pts',(1.84609356197069,-0.755628922691078,
22.0276810097483));
#23166=CARTESIAN_POINT('Ctrl Pts',(1.84307666529403,-0.762968159888389,
22.0271738079769));
#23167=CARTESIAN_POINT('Ctrl Pts',(1.84117990044613,-0.767534092147903,
22.0268588049421));
#23168=CARTESIAN_POINT('Ctrl Pts',(1.83234260697776,-0.788586135251535,
22.0254087167105));
#23169=CARTESIAN_POINT('Ctrl Pts',(1.82519723301195,-0.804986109541091,
22.0242855663869));
#23170=CARTESIAN_POINT('Ctrl Pts',(1.80501732476475,-0.849652124632118,
22.0212386167411));
#23171=CARTESIAN_POINT('Ctrl Pts',(1.79153990051543,-0.87771366771119,22.0193376785394));
#23172=CARTESIAN_POINT('Ctrl Pts',(1.74195140755976,-0.975056562181382,
22.0127513654253));
#23173=CARTESIAN_POINT('Ctrl Pts',(1.70243142066826,-1.04252528738825,22.0081988487639));
#23174=CARTESIAN_POINT('Ctrl Pts',(1.56910603169086,-1.24224784100677,21.9942579734009));
#23175=CARTESIAN_POINT('Ctrl Pts',(1.46309281346152,-1.36551296241946,21.9849247614131));
#23176=CARTESIAN_POINT('Ctrl Pts',(1.33792028993777,-1.47954410902969,21.9744464321081));
#23177=CARTESIAN_POINT('Ctrl Pts',(1.33246531706927,-1.48445870585632,21.973990871058));
#23178=CARTESIAN_POINT('Ctrl Pts',(1.31530487183876,-1.49974841777872,21.9725609606724));
#23179=CARTESIAN_POINT('Ctrl Pts',(1.30350464069281,-1.51001584501153,21.9715823204737));
#23180=CARTESIAN_POINT('Ctrl Pts',(1.2868397337514,-1.52417513345275,21.9702060379645));
#23181=CARTESIAN_POINT('Ctrl Pts',(1.28207551594959,-1.52818477540374,21.9698132341926));
#23182=CARTESIAN_POINT('Ctrl Pts',(1.27379594441695,-1.53508702643795,21.9691316782757));
#23183=CARTESIAN_POINT('Ctrl Pts',(1.27028929886817,-1.53799004657729,21.968843352552));
#23184=CARTESIAN_POINT('Ctrl Pts',(1.26298756397207,-1.54399287147642,21.9682436575304));
#23185=CARTESIAN_POINT('Ctrl Pts',(1.25919093226656,-1.54709074372227,21.9679322128274));
#23186=CARTESIAN_POINT('Ctrl Pts',(1.25024316354679,-1.5543369445752,21.9671990651403));
#23187=CARTESIAN_POINT('Ctrl Pts',(1.24508275742025,-1.55847368623881,21.9667769004715));
#23188=CARTESIAN_POINT('Ctrl Pts',(1.22843564821211,-1.57168307159329,21.9654170696229));
#23189=CARTESIAN_POINT('Ctrl Pts',(1.21686983509291,-1.58065480253422,21.9644754058082));
#23190=CARTESIAN_POINT('Ctrl Pts',(1.18947054010425,-1.60142979294396,21.962251376562));
#23191=CARTESIAN_POINT('Ctrl Pts',(1.1735586707043,-1.61312663715536,21.9609649824225));
#23192=CARTESIAN_POINT('Ctrl Pts',(1.11705121195152,-1.65338679037229,21.9564136388948));
#23193=CARTESIAN_POINT('Ctrl Pts',(1.07556837204327,-1.6806675094283,21.9531021070919));
#23194=CARTESIAN_POINT('Ctrl Pts',(0.89032584162857,-1.79282170299353,21.9384452458201));
#23195=CARTESIAN_POINT('Ctrl Pts',(0.737274205600266,-1.86099586565288,
21.9265950596769));
#23196=CARTESIAN_POINT('Ctrl Pts',(0.522204827353338,-1.92605067653363,
21.9111891200183));
#23197=CARTESIAN_POINT('Ctrl Pts',(0.466167120640786,-1.94037592805868,
21.9072897016726));
#23198=CARTESIAN_POINT('Ctrl Pts',(0.403062289609456,-1.95361529297327,
21.9030813074586));
#23199=CARTESIAN_POINT('Ctrl Pts',(0.396536969877108,-1.95495021849559,
21.9026483029122));
#23200=CARTESIAN_POINT('Ctrl Pts',(0.386661744634067,-1.95691897614008,
21.9019963978943));
#23201=CARTESIAN_POINT('Ctrl Pts',(0.38331677988225,-1.95757692840498,21.9017761697802));
#23202=CARTESIAN_POINT('Ctrl Pts',(0.377498005163986,-1.95870599121408,
21.9013941089536));
#23203=CARTESIAN_POINT('Ctrl Pts',(0.375024972632849,-1.95918099572151,
21.9012320557287));
#23204=CARTESIAN_POINT('Ctrl Pts',(0.369815058781727,-1.96017145701136,
21.9008913558898));
#23205=CARTESIAN_POINT('Ctrl Pts',(0.367077988510799,-1.9606858670086,21.9007127714055));
#23206=CARTESIAN_POINT('Ctrl Pts',(0.360409763285189,-1.96192465287333,
21.90027865878));
#23207=CARTESIAN_POINT('Ctrl Pts',(0.356477463871933,-1.96264295261523,
21.9000234764867));
#23208=CARTESIAN_POINT('Ctrl Pts',(0.342994459046092,-1.96506398819669,
21.8991512272462));
#23209=CARTESIAN_POINT('Ctrl Pts',(0.333433316318281,-1.96670890304321,
21.8985373579226));
#23210=CARTESIAN_POINT('Ctrl Pts',(0.209132038555653,-1.98716136380694,
21.8906126699653));
#23211=CARTESIAN_POINT('Ctrl Pts',(0.092954056282022,-1.99597455346449,
21.8838179988577));
#23212=CARTESIAN_POINT('Ctrl Pts',(-0.13839933914818,-1.99326679365454,
21.8703798108761));
#23213=CARTESIAN_POINT('Ctrl Pts',(-0.253114545077029,-1.98196824158015,
21.8637553110501));
#23214=CARTESIAN_POINT('Ctrl Pts',(-0.384208110501742,-1.95748481326619,
21.8557727631345));
#23215=CARTESIAN_POINT('Ctrl Pts',(-0.402155310732573,-1.95387659408648,
21.8546711864521));
#23216=CARTESIAN_POINT('Ctrl Pts',(-0.466372986767495,-1.94004360540612,
21.8506941267411));
#23217=CARTESIAN_POINT('Ctrl Pts',(-0.512322527213875,-1.9284185286809,
21.847781558384));
#23218=CARTESIAN_POINT('Ctrl Pts',(-0.566958514744587,-1.91250525790726,
21.8442194085392));
#23219=CARTESIAN_POINT('Ctrl Pts',(-0.576085736579041,-1.90977578213628,
21.8436209887834));
#23220=CARTESIAN_POINT('Ctrl Pts',(-0.591008981218374,-1.90519630443585,
21.8426369181211));
#23221=CARTESIAN_POINT('Ctrl Pts',(-0.596816782435865,-1.90338495874766,
21.842252532972));
#23222=CARTESIAN_POINT('Ctrl Pts',(-0.607216729445446,-1.90008912867734,
21.8415616567058));
#23223=CARTESIAN_POINT('Ctrl Pts',(-0.611811964410745,-1.89861448771706,
21.8412554910312));
#23224=CARTESIAN_POINT('Ctrl Pts',(-0.62155427073647,-1.89544907659638,
21.8406044578399));
#23225=CARTESIAN_POINT('Ctrl Pts',(-0.626699887532937,-1.89375398704581,
21.8402594500284));
#23226=CARTESIAN_POINT('Ctrl Pts',(-0.639904168049234,-1.88934447051319,
21.8393711262455));
#23227=CARTESIAN_POINT('Ctrl Pts',(-0.647952431057276,-1.88659945826284,
21.8388268032043));
#23228=CARTESIAN_POINT('Ctrl Pts',(-0.685029326964789,-1.87368844557313,
21.836305714693));
#23229=CARTESIAN_POINT('Ctrl Pts',(-0.713836594352723,-1.86290383829853,
21.8343085239392));
#23230=CARTESIAN_POINT('Ctrl Pts',(-0.790478718656267,-1.83217253765312,
21.8288875984377));
#23231=CARTESIAN_POINT('Ctrl Pts',(-0.837802100439806,-1.81102172129554,
21.8254252955133));
#23232=CARTESIAN_POINT('Ctrl Pts',(-0.980442748138354,-1.74048173800657,
21.8146352932242));
#23233=CARTESIAN_POINT('Ctrl Pts',(-1.07263676033614,-1.68522735339636,
21.8071466913429));
#23234=CARTESIAN_POINT('Ctrl Pts',(-1.17425054468235,-1.6125982230581,21.7984354376002));
#23235=CARTESIAN_POINT('Ctrl Pts',(-1.18843416884133,-1.60217402439918,
21.7972086818905));
#23236=CARTESIAN_POINT('Ctrl Pts',(-1.27878421140073,-1.53391162155286,
21.7893307632562));
#23237=CARTESIAN_POINT('Ctrl Pts',(-1.35085598275733,-1.47083880874594,
21.7827466800504));
#23238=CARTESIAN_POINT('Ctrl Pts',(-1.4236556634689,-1.39724508503005,21.7759847301797));
#23239=CARTESIAN_POINT('Ctrl Pts',(-1.42914739877409,-1.39162746211556,
21.7754739266258));
#23240=CARTESIAN_POINT('Ctrl Pts',(-1.43707726103172,-1.38341937226122,
21.7747355093503));
#23241=CARTESIAN_POINT('Ctrl Pts',(-1.43954178635455,-1.38085468444104,
21.7745058976897));
#23242=CARTESIAN_POINT('Ctrl Pts',(-1.44387767942877,-1.37631834923807,
21.7741017495179));
#23243=CARTESIAN_POINT('Ctrl Pts',(-1.44575189273671,-1.37434945214526,
21.7739269926804));
#23244=CARTESIAN_POINT('Ctrl Pts',(-1.44967977958317,-1.3702062049999,21.7735606237776));
#23245=CARTESIAN_POINT('Ctrl Pts',(-1.45173258486281,-1.36803107051301,
21.7733690782093));
#23246=CARTESIAN_POINT('Ctrl Pts',(-1.45590620702771,-1.36358876372386,
21.7729794720103));
#23247=CARTESIAN_POINT('Ctrl Pts',(-1.45802663978856,-1.361321239898,21.7727814408053));
#23248=CARTESIAN_POINT('Ctrl Pts',(-1.46705016042496,-1.35162650342268,
21.7719382861313));
#23249=CARTESIAN_POINT('Ctrl Pts',(-1.47390201309046,-1.34415149596916,
21.7712969706654));
#23250=CARTESIAN_POINT('Ctrl Pts',(-1.55687083527858,-1.25223961221706,
21.7635131944535));
#23251=CARTESIAN_POINT('Ctrl Pts',(-1.62570413458052,-1.16148387067856,
21.7568613529895));
#23252=CARTESIAN_POINT('Ctrl Pts',(-1.71020123021507,-1.02772530334523,
21.7476691445891));
#23253=CARTESIAN_POINT('Ctrl Pts',(-1.73270050868412,-0.989321230798476,
21.745094368668));
#23254=CARTESIAN_POINT('Ctrl Pts',(-1.77380547893419,-0.913448674272355,
21.7400788966662));
#23255=CARTESIAN_POINT('Ctrl Pts',(-1.79255400984957,-0.87608465676867,
21.7376408523234));
#23256=CARTESIAN_POINT('Ctrl Pts',(-1.84922249582413,-0.753701777756611,
21.7296964005963));
#23257=CARTESIAN_POINT('Ctrl Pts',(-1.88236647669968,-0.666620718928333,
21.7240995234148));
#23258=CARTESIAN_POINT('Ctrl Pts',(-1.91296509429747,-0.565465780779629,
21.7175005481069));
#23259=CARTESIAN_POINT('Ctrl Pts',(-1.91650612760227,-0.553345509072535,
21.7167084626777));
#23260=CARTESIAN_POINT('Ctrl Pts',(-1.92160594335428,-0.535253433520577,
21.7155237045835));
#23261=CARTESIAN_POINT('Ctrl Pts',(-1.92325251424397,-0.529306531882967,
21.7151338882961));
#23262=CARTESIAN_POINT('Ctrl Pts',(-1.92614013589272,-0.518685957228025,
21.7144369919139));
#23263=CARTESIAN_POINT('Ctrl Pts',(-1.9273918406919,-0.514015210944063,
21.7141302601834));
#23264=CARTESIAN_POINT('Ctrl Pts',(-1.92999691070707,-0.504151058822975,
21.7134819284136));
#23265=CARTESIAN_POINT('Ctrl Pts',(-1.93134632271255,-0.49895665770441,
21.713140203132));
#23266=CARTESIAN_POINT('Ctrl Pts',(-1.93404538683843,-0.488391918446066,
21.7124445080554));
#23267=CARTESIAN_POINT('Ctrl Pts',(-1.93539367155762,-0.483021282579187,
21.7120904973733));
#23268=CARTESIAN_POINT('Ctrl Pts',(-1.93868131223518,-0.469690804783977,
21.7112109066444));
#23269=CARTESIAN_POINT('Ctrl Pts',(-1.94059401121295,-0.461724552977374,
21.7106844725305));
#23270=CARTESIAN_POINT('Ctrl Pts',(-1.94955530046714,-0.423361918956064,
21.7081453760436));
#23271=CARTESIAN_POINT('Ctrl Pts',(-1.95593876719981,-0.392816165863748,
21.7061115732804));
#23272=CARTESIAN_POINT('Ctrl Pts',(-1.98377047680234,-0.242057975678065,
21.6960092438615));
#23273=CARTESIAN_POINT('Ctrl Pts',(-1.99486174452552,-0.120222041741954,
21.6876218107719));
#23274=CARTESIAN_POINT('Ctrl Pts',(-1.99474915136507,0.00184000770332437,
21.6791186215938));
#23275=CARTESIAN_POINT('',(-1.99474949799968,-0.00141517844896885,20.0802123525403));
#23276=CARTESIAN_POINT('Ctrl Pts',(-1.99474915155411,0.00183980275410899,
21.6791186358711));
#23277=CARTESIAN_POINT('Ctrl Pts',(-1.99462759772053,0.133630781894563,
21.6699377018992));
#23278=CARTESIAN_POINT('Ctrl Pts',(-1.98144558057616,0.265099377212311,
21.6606648776704));
#23279=CARTESIAN_POINT('Ctrl Pts',(-1.95303028307935,0.406007963953111,
21.6511398820363));
#23280=CARTESIAN_POINT('Ctrl Pts',(-1.9505682576785,0.41767600052295,21.6503545061792));
#23281=CARTESIAN_POINT('Ctrl Pts',(-1.94671784351141,0.43514685143171,21.6491842770525));
#23282=CARTESIAN_POINT('Ctrl Pts',(-1.94540786422072,0.440966425620485,
21.6487954298911));
#23283=CARTESIAN_POINT('Ctrl Pts',(-1.94325117019873,0.450350835919816,
21.6481700354034));
#23284=CARTESIAN_POINT('Ctrl Pts',(-1.94242071682887,0.453919315783123,
21.6479326100637));
#23285=CARTESIAN_POINT('Ctrl Pts',(-1.94080367432097,0.460782086162704,
21.6474767699827));
#23286=CARTESIAN_POINT('Ctrl Pts',(-1.9400185186105,0.464076697380762,21.6472582758597));
#23287=CARTESIAN_POINT('Ctrl Pts',(-1.93865430964199,0.469737120445104,
21.6468834900377));
#23288=CARTESIAN_POINT('Ctrl Pts',(-1.93807931257185,0.472103879499661,
21.6467269660816));
#23289=CARTESIAN_POINT('Ctrl Pts',(-1.93686976671853,0.477043068363232,
21.6464007020923));
#23290=CARTESIAN_POINT('Ctrl Pts',(-1.93623442988505,0.479615278145238,
21.646231008808));
#23291=CARTESIAN_POINT('Ctrl Pts',(-1.93445094332048,0.486774557272059,
21.6457592836481));
#23292=CARTESIAN_POINT('Ctrl Pts',(-1.93329159566434,0.491358859654482,
21.6454578935852));
#23293=CARTESIAN_POINT('Ctrl Pts',(-1.9285656395357,0.509770588137588,21.6442499687596));
#23294=CARTESIAN_POINT('Ctrl Pts',(-1.92486679127725,0.523564076647532,
21.6433507844798));
#23295=CARTESIAN_POINT('Ctrl Pts',(-1.88703483710921,0.65882114891643,21.6345794691881));
#23296=CARTESIAN_POINT('Ctrl Pts',(-1.841593303974,0.776845759596387,21.6272805479765));
#23297=CARTESIAN_POINT('Ctrl Pts',(-1.75721828361801,0.946136240089996,
21.6163102568148));
#23298=CARTESIAN_POINT('Ctrl Pts',(-1.72648908104309,1.00111189485545,21.6126629290317));
#23299=CARTESIAN_POINT('Ctrl Pts',(-1.64525247806218,1.13154856728356,21.6036318904546));
#23300=CARTESIAN_POINT('Ctrl Pts',(-1.59210035721319,1.20518515254058,21.5981991448856));
#23301=CARTESIAN_POINT('Ctrl Pts',(-1.52279643770028,1.28857783195248,21.5914664353033));
#23302=CARTESIAN_POINT('Ctrl Pts',(-1.51128509631546,1.3020595782912,21.5903586761523));
#23303=CARTESIAN_POINT('Ctrl Pts',(-1.49598191381535,1.31950585898312,21.5888987743151));
#23304=CARTESIAN_POINT('Ctrl Pts',(-1.49235100810189,1.32361099496857,21.5885533090356));
#23305=CARTESIAN_POINT('Ctrl Pts',(-1.48515745745297,1.33167686343929,21.587870643137));
#23306=CARTESIAN_POINT('Ctrl Pts',(-1.4815957705789,1.33563839183819,21.5875334842059));
#23307=CARTESIAN_POINT('Ctrl Pts',(-1.47476481155392,1.34317526185204,21.5868884254635));
#23308=CARTESIAN_POINT('Ctrl Pts',(-1.47149829490288,1.34675305860667,21.586580643552));
#23309=CARTESIAN_POINT('Ctrl Pts',(-1.46399139605767,1.35491540460037,21.5858748488138));
#23310=CARTESIAN_POINT('Ctrl Pts',(-1.45974247003781,1.35949199374472,21.5854764730848));
#23311=CARTESIAN_POINT('Ctrl Pts',(-1.44657949648695,1.37353719917973,21.5842456582888));
#23312=CARTESIAN_POINT('Ctrl Pts',(-1.43759443334741,1.38293850516904,21.5834101677385));
#23313=CARTESIAN_POINT('Ctrl Pts',(-1.34398365286598,1.47898778041756,21.5747517918442));
#23314=CARTESIAN_POINT('Ctrl Pts',(-1.25174131841775,1.55782889500527,21.5665805912205));
#23315=CARTESIAN_POINT('Ctrl Pts',(-1.06112392158137,1.69283842659526,21.5504230932594));
#23316=CARTESIAN_POINT('Ctrl Pts',(-0.963976243073012,1.74998151417476,
21.5424977399265));
#23317=CARTESIAN_POINT('Ctrl Pts',(-0.823115605134974,1.81753102802609,
21.5317570132323));
#23318=CARTESIAN_POINT('Ctrl Pts',(-0.783087369271146,1.83513297866075,
21.5287849896786));
#23319=CARTESIAN_POINT('Ctrl Pts',(-0.728556341170191,1.8570027612317,21.5248706935772));
#23320=CARTESIAN_POINT('Ctrl Pts',(-0.714538960654169,1.86244132843294,
21.5238762144651));
#23321=CARTESIAN_POINT('Ctrl Pts',(-0.690828942538745,1.87133341752682,
21.5222152715546));
#23322=CARTESIAN_POINT('Ctrl Pts',(-0.681168869294488,1.87487129421083,
21.5215444259801));
#23323=CARTESIAN_POINT('Ctrl Pts',(-0.668558241381134,1.87937943977441,
21.5206766900429));
#23324=CARTESIAN_POINT('Ctrl Pts',(-0.665632410930428,1.8804176915253,21.5204759228869));
#23325=CARTESIAN_POINT('Ctrl Pts',(-0.659883136138226,1.88244276262535,
21.5200825273207));
#23326=CARTESIAN_POINT('Ctrl Pts',(-0.65705987365359,1.88343007054796,21.5198898706161));
#23327=CARTESIAN_POINT('Ctrl Pts',(-0.651666434277915,1.88530257787059,
21.5195228448407));
#23328=CARTESIAN_POINT('Ctrl Pts',(-0.649096700003978,1.88618886271008,
21.5193484150846));
#23329=CARTESIAN_POINT('Ctrl Pts',(-0.643160385905131,1.88822269100933,
21.5189464730168));
#23330=CARTESIAN_POINT('Ctrl Pts',(-0.639792543807331,1.88936648488526,
21.5187191843183));
#23331=CARTESIAN_POINT('Ctrl Pts',(-0.628977040069291,1.89300743482387,
21.5179916008935));
#23332=CARTESIAN_POINT('Ctrl Pts',(-0.621517564887757,1.89546964804969,
21.5174933277134));
#23333=CARTESIAN_POINT('Ctrl Pts',(-0.525362643226921,1.9265796610077,21.5111135710746));
#23334=CARTESIAN_POINT('Ctrl Pts',(-0.434766279784053,1.94902498030959,
21.5055714981401));
#23335=CARTESIAN_POINT('Ctrl Pts',(-0.210135339865238,1.98822523236754,
21.4922336607228));
#23336=CARTESIAN_POINT('Ctrl Pts',(-0.0753480564502597,1.99787856835567,
21.4845497530724));
#23337=CARTESIAN_POINT('Ctrl Pts',(0.127077534222631,1.99184976507782,21.4724709923917));
#23338=CARTESIAN_POINT('Ctrl Pts',(0.194618998963505,1.98638770982028,21.4683552932056));
#23339=CARTESIAN_POINT('Ctrl Pts',(0.274603870970788,1.97580071609844,21.4633203341471));
#23340=CARTESIAN_POINT('Ctrl Pts',(0.287443516497159,1.97397364923387,21.4625071843974));
#23341=CARTESIAN_POINT('Ctrl Pts',(0.306530047981177,1.97106749333816,21.4612907473473));
#23342=CARTESIAN_POINT('Ctrl Pts',(0.312791257224153,1.97008359251791,21.4608904722861));
#23343=CARTESIAN_POINT('Ctrl Pts',(0.323842302991212,1.96829299594639,21.4601817676285));
#23344=CARTESIAN_POINT('Ctrl Pts',(0.328634104398711,1.96749860987008,21.4598737307615));
#23345=CARTESIAN_POINT('Ctrl Pts',(0.337990731419987,1.96591233084261,21.4592707853869));
#23346=CARTESIAN_POINT('Ctrl Pts',(0.34255579679748,1.96512201976582,21.4589759289756));
#23347=CARTESIAN_POINT('Ctrl Pts',(0.354852389765219,1.96294906511074,21.4581798356736));
#23348=CARTESIAN_POINT('Ctrl Pts',(0.362578510546136,1.96153666076045,21.4576776548471));
#23349=CARTESIAN_POINT('Ctrl Pts',(0.391142134159139,1.95614045110115,21.4558136008388));
#23350=CARTESIAN_POINT('Ctrl Pts',(0.411923414949782,1.95187004586243,21.4544426357739));
#23351=CARTESIAN_POINT('Ctrl Pts',(0.582951299979936,1.91387214823501,21.4430331003788));
#23352=CARTESIAN_POINT('Ctrl Pts',(0.728868893390707,1.86318835959631,21.4324270674748));
#23353=CARTESIAN_POINT('Ctrl Pts',(0.97475916852336,1.74443854889997,21.4133776461433));
#23354=CARTESIAN_POINT('Ctrl Pts',(1.07719425592596,1.68311596531382,21.4050433423637));
#23355=CARTESIAN_POINT('Ctrl Pts',(1.18219795034365,1.60672023660532,21.3964589178389));
#23356=CARTESIAN_POINT('Ctrl Pts',(1.19079447555452,1.60035947246432,21.3957559180322));
#23357=CARTESIAN_POINT('Ctrl Pts',(1.20563218159969,1.58919495946227,21.3945427639548));
#23358=CARTESIAN_POINT('Ctrl Pts',(1.21189674950765,1.58442287600956,21.3940306361421));
#23359=CARTESIAN_POINT('Ctrl Pts',(1.22101616044616,1.5773903620465,21.3932854333068));
#23360=CARTESIAN_POINT('Ctrl Pts',(1.22389323897372,1.57515908988853,21.3930503748909));
#23361=CARTESIAN_POINT('Ctrl Pts',(1.22891025291307,1.57124618048337,21.3926405861212));
#23362=CARTESIAN_POINT('Ctrl Pts',(1.23105287549119,1.56956802576634,21.3924656107257));
#23363=CARTESIAN_POINT('Ctrl Pts',(1.23553471527144,1.56604291535272,21.392099683946));
#23364=CARTESIAN_POINT('Ctrl Pts',(1.23787322491147,1.5641951044229,21.3919087956394));
#23365=CARTESIAN_POINT('Ctrl Pts',(1.24404320656702,1.55929729207249,21.3914052385379));
#23366=CARTESIAN_POINT('Ctrl Pts',(1.2478676335518,1.55623838637607,21.3910932009757));
#23367=CARTESIAN_POINT('Ctrl Pts',(1.26382983014862,1.54337460815747,21.3897910242636));
#23368=CARTESIAN_POINT('Ctrl Pts',(1.27586401227092,1.53344125386396,21.388809751128));
#23369=CARTESIAN_POINT('Ctrl Pts',(1.44891848972545,1.38714939549097,21.374684755799));
#23370=CARTESIAN_POINT('Ctrl Pts',(1.58744919667585,1.22620795374632,21.3630788430112));
#23371=CARTESIAN_POINT('Ctrl Pts',(1.72510128599185,1.00283842887616,21.3474864507092));
#23372=CARTESIAN_POINT('Ctrl Pts',(1.7503189590019,0.958145238245635,21.3443965305516));
#23373=CARTESIAN_POINT('Ctrl Pts',(1.78779648616265,0.885296228959564,21.3393682580237));
#23374=CARTESIAN_POINT('Ctrl Pts',(1.8011783755114,0.857742379244277,21.3374683670956));
#23375=CARTESIAN_POINT('Ctrl Pts',(1.8175420926116,0.821975728509637,21.335000032784));
#23376=CARTESIAN_POINT('Ctrl Pts',(1.82111220174292,0.814035442389179,21.3344519293608));
#23377=CARTESIAN_POINT('Ctrl Pts',(1.82678630487332,0.801191505402095,21.333565025075));
#23378=CARTESIAN_POINT('Ctrl Pts',(1.82892282846319,0.796302278425035,21.3332273403366));
#23379=CARTESIAN_POINT('Ctrl Pts',(1.83296096734602,0.786959405261308,21.3325818916934));
#23380=CARTESIAN_POINT('Ctrl Pts',(1.8348660337925,0.782507284757336,21.3322742482807));
#23381=CARTESIAN_POINT('Ctrl Pts',(1.83918429535329,0.772313074634138,21.331569641413));
#23382=CARTESIAN_POINT('Ctrl Pts',(1.84158683632246,0.766566553114736,21.3311723193739));
#23383=CARTESIAN_POINT('Ctrl Pts',(1.84889046704608,0.748864841194824,21.3299479377961));
#23384=CARTESIAN_POINT('Ctrl Pts',(1.85370226684932,0.736873396404387,21.3291178727971));
#23385=CARTESIAN_POINT('Ctrl Pts',(1.89849228752855,0.622036917646174,21.3211612599407));
#23386=CARTESIAN_POINT('Ctrl Pts',(1.92998181685044,0.516106215679385,21.3137484108569));
#23387=CARTESIAN_POINT('Ctrl Pts',(1.98774568646514,0.239756896093602,21.2942944754034));
#23388=CARTESIAN_POINT('Ctrl Pts',(2.00101357841623,0.0675416382083606,
21.2820223710285));
#23389=CARTESIAN_POINT('Ctrl Pts',(1.99105200394158,-0.122824311525504,
21.2693810509212));
#23390=CARTESIAN_POINT('Ctrl Pts',(1.98981942828649,-0.141395184833082,
21.2681584811593));
#23391=CARTESIAN_POINT('Ctrl Pts',(1.98792511663006,-0.164943695799032,
21.2666240010388));
#23392=CARTESIAN_POINT('Ctrl Pts',(1.98750431918883,-0.169939032133866,
21.266299395568));
#23393=CARTESIAN_POINT('Ctrl Pts',(1.98680104824651,-0.177927499136992,
21.2657817936845));
#23394=CARTESIAN_POINT('Ctrl Pts',(1.98653063528956,-0.180921628372104,
21.2655881309913));
#23395=CARTESIAN_POINT('Ctrl Pts',(1.98600323401925,-0.186617475299121,
21.2652203767007));
#23396=CARTESIAN_POINT('Ctrl Pts',(1.98574750424957,-0.189319246431959,
21.2650462195482));
#23397=CARTESIAN_POINT('Ctrl Pts',(1.985146785305,-0.195530661356432,21.2646464696675));
#23398=CARTESIAN_POINT('Ctrl Pts',(1.98479800262249,-0.199039915570191,
21.2644210926037));
#23399=CARTESIAN_POINT('Ctrl Pts',(1.98365882239871,-0.210200883880464,
21.2637057346359));
#23400=CARTESIAN_POINT('Ctrl Pts',(1.98283345749588,-0.21784907554564,21.2632176809555));
#23401=CARTESIAN_POINT('Ctrl Pts',(1.96892322175888,-0.340112967079147,
21.2554473958506));
#23402=CARTESIAN_POINT('Ctrl Pts',(1.94596178663907,-0.453405713915335,
21.2486874262964));
#23403=CARTESIAN_POINT('Ctrl Pts',(1.88430469459147,-0.662538632997183,
21.2360149422177));
#23404=CARTESIAN_POINT('Ctrl Pts',(1.84772715469179,-0.758594137701845,
21.2301083824523));
#23405=CARTESIAN_POINT('Ctrl Pts',(1.7810072939806,-0.899957090405861,21.2208365044465));
#23406=CARTESIAN_POINT('Ctrl Pts',(1.75614376346414,-0.947559046685419,
21.2176084702422));
#23407=CARTESIAN_POINT('Ctrl Pts',(1.71361803042075,-1.02153936378006,21.2123755073278));
#23408=CARTESIAN_POINT('Ctrl Pts',(1.69719374588583,-1.04860032397429,21.210413202833));
#23409=CARTESIAN_POINT('Ctrl Pts',(1.67538616342487,-1.08267553855334,21.2078747119729));
#23410=CARTESIAN_POINT('Ctrl Pts',(1.67059002181998,-1.09006150898332,21.2073203357143));
#23411=CARTESIAN_POINT('Ctrl Pts',(1.66279743383105,-1.10188972476269,21.2064257267486));
#23412=CARTESIAN_POINT('Ctrl Pts',(1.6598316857201,-1.10635213456587,21.2060866459606));
#23413=CARTESIAN_POINT('Ctrl Pts',(1.65415421708014,-1.11482051901102,21.2054401389211));
#23414=CARTESIAN_POINT('Ctrl Pts',(1.65144582860549,-1.11882869019175,21.2051328399763));
#23415=CARTESIAN_POINT('Ctrl Pts',(1.64524054119214,-1.12794033431591,21.2044312743641));
#23416=CARTESIAN_POINT('Ctrl Pts',(1.64173443928362,-1.13303745110376,21.2040366601949));
#23417=CARTESIAN_POINT('Ctrl Pts',(1.63095449358012,-1.14855408109221,21.2028287236886));
#23418=CARTESIAN_POINT('Ctrl Pts',(1.62360486005962,-1.15892030929244,21.2020125119208));
#23419=CARTESIAN_POINT('Ctrl Pts',(1.60896633975525,-1.17915451440288,21.2004008141663));
#23420=CARTESIAN_POINT('Ctrl Pts',(1.60168445985505,-1.18902688412987,21.1996056227899));
#23421=CARTESIAN_POINT('Ctrl Pts',(1.49754528885855,-1.32752038600383,21.1883234883692));
#23422=CARTESIAN_POINT('Ctrl Pts',(1.38557209789052,-1.44399505643734,21.1772032650752));
#23423=CARTESIAN_POINT('Ctrl Pts',(1.19977609088203,-1.59554929898323,21.160474158432));
#23424=CARTESIAN_POINT('Ctrl Pts',(1.13579576672833,-1.64170932126844,21.1549763778008));
#23425=CARTESIAN_POINT('Ctrl Pts',(1.04283439308263,-1.70073602086015,21.147484875551));
#23426=CARTESIAN_POINT('Ctrl Pts',(1.01602744180602,-1.7168852761824,21.1453788666931));
#23427=CARTESIAN_POINT('Ctrl Pts',(0.973256065471496,-1.7412991120906,21.1421155135832));
#23428=CARTESIAN_POINT('Ctrl Pts',(0.957541837256029,-1.74998961487602,
21.1409365548075));
#23429=CARTESIAN_POINT('Ctrl Pts',(0.937347408219849,-1.76080433576715,
21.139448841269));
#23430=CARTESIAN_POINT('Ctrl Pts',(0.932974331977045,-1.76312534146083,
21.1391282981912));
#23431=CARTESIAN_POINT('Ctrl Pts',(0.925944222278671,-1.76682308512656,
21.1386156446599));
#23432=CARTESIAN_POINT('Ctrl Pts',(0.923292688525903,-1.768210148289,21.1384228898119));
#23433=CARTESIAN_POINT('Ctrl Pts',(0.918226948231438,-1.77084562307642,
21.1380557942818));
#23434=CARTESIAN_POINT('Ctrl Pts',(0.915813341110429,-1.77209505206391,
21.1378813924368));
#23435=CARTESIAN_POINT('Ctrl Pts',(0.910237887162976,-1.77496681099306,
21.1374796701835));
#23436=CARTESIAN_POINT('Ctrl Pts',(0.90707425423622,-1.77658562673838,21.1372525725932));
#23437=CARTESIAN_POINT('Ctrl Pts',(0.896918523092782,-1.78174806620431,
21.1365262171337));
#23438=CARTESIAN_POINT('Ctrl Pts',(0.889909748127897,-1.78525898780979,
21.1360289712314));
#23439=CARTESIAN_POINT('Ctrl Pts',(0.804656508339471,-1.82733826626339,
21.130027154693));
#23440=CARTESIAN_POINT('Ctrl Pts',(0.723972819034145,-1.86078069982627,
21.124819563072));
#23441=CARTESIAN_POINT('Ctrl Pts',(0.474973529853891,-1.94532763661055,
21.1093997423195));
#23442=CARTESIAN_POINT('Ctrl Pts',(0.30187637386104,-1.97958816458617,21.0994639507241));
#23443=CARTESIAN_POINT('Ctrl Pts',(0.0874915008619739,-1.99321419909783,
21.0863690198997));
#23444=CARTESIAN_POINT('Ctrl Pts',(0.0483922330984359,-1.99454643307504,
21.0839532755294));
#23445=CARTESIAN_POINT('Ctrl Pts',(-0.000171845794752117,-1.99477239096135,
21.0809087559399));
#23446=CARTESIAN_POINT('Ctrl Pts',(-0.00962477993409601,-1.9947491771997,
21.0803140891755));
#23447=CARTESIAN_POINT('Ctrl Pts',(-0.0245785091961187,-1.99460615863495,
21.079369990997));
#23448=CARTESIAN_POINT('Ctrl Pts',(-0.0300796686829023,-1.99453078284649,
21.0790219523416));
#23449=CARTESIAN_POINT('Ctrl Pts',(-0.0403944688794591,-1.99434676824405,
21.0783679838135));
#23450=CARTESIAN_POINT('Ctrl Pts',(-0.0452081745988543,-1.99424345690376,
21.0780622231253));
#23451=CARTESIAN_POINT('Ctrl Pts',(-0.0559766656579116,-1.99397333548177,
21.0773769320759));
#23452=CARTESIAN_POINT('Ctrl Pts',(-0.0619311534704512,-1.9937972767231,
21.0769971145785));
#23453=CARTESIAN_POINT('Ctrl Pts',(-0.0769963065174997,-1.99328428698191,
21.0760338822824));
#23454=CARTESIAN_POINT('Ctrl Pts',(-0.0861055402092911,-1.99291156635405,
21.0754493516363));
#23455=CARTESIAN_POINT('Ctrl Pts',(-0.111777499128371,-1.99168481518693,
21.073795923307));
#23456=CARTESIAN_POINT('Ctrl Pts',(-0.12833227512816,-1.990686668436,21.072722546437));
#23457=CARTESIAN_POINT('Ctrl Pts',(-0.304700458161688,-1.97784369888403,
21.0612084888847));
#23458=CARTESIAN_POINT('Ctrl Pts',(-0.462512780334678,-1.94698992303224,
21.0501439821441));
#23459=CARTESIAN_POINT('Ctrl Pts',(-0.690386557842399,-1.87314987845886,
21.0334308960687));
#23460=CARTESIAN_POINT('Ctrl Pts',(-0.764350001830473,-1.84420563727078,
21.027895021836));
#23461=CARTESIAN_POINT('Ctrl Pts',(-0.864914836788747,-1.79775880778824,
21.0203580303438));
#23462=CARTESIAN_POINT('Ctrl Pts',(-0.893120643696821,-1.78391427880746,
21.0182433884816));
#23463=CARTESIAN_POINT('Ctrl Pts',(-0.936962053657687,-1.76109452492476,
21.0149681586175));
#23464=CARTESIAN_POINT('Ctrl Pts',(-0.95282226985633,-1.75256429090815,
21.0137857746432));
#23465=CARTESIAN_POINT('Ctrl Pts',(-0.97289778490481,-1.74141379972355,
21.012294381605));
#23466=CARTESIAN_POINT('Ctrl Pts',(-0.977221180689317,-1.73899134185101,
21.0119735141634));
#23467=CARTESIAN_POINT('Ctrl Pts',(-0.984141587061875,-1.73507978495682,
21.0114604654936));
#23468=CARTESIAN_POINT('Ctrl Pts',(-0.986744316557314,-1.73360092800587,
21.0112676381339));
#23469=CARTESIAN_POINT('Ctrl Pts',(-0.991703454122104,-1.73076838615294,
21.0109004908793));
#23470=CARTESIAN_POINT('Ctrl Pts',(-0.994060396106565,-1.72941576157809,
21.0107261094687));
#23471=CARTESIAN_POINT('Ctrl Pts',(-0.999491271377177,-1.72628426801765,
21.0103245487756));
#23472=CARTESIAN_POINT('Ctrl Pts',(-1.0025632222725,-1.72450200388051,21.0100975917262));
#23473=CARTESIAN_POINT('Ctrl Pts',(-1.0123897695024,-1.71876577078851,21.0093721384879));
#23474=CARTESIAN_POINT('Ctrl Pts',(-1.019125965867,-1.71478018730684,21.0088756472427));
#23475=CARTESIAN_POINT('Ctrl Pts',(-1.11528037265996,-1.65712207192996,
21.0017977001473));
#23476=CARTESIAN_POINT('Ctrl Pts',(-1.20039270675749,-1.59654873091424,
20.9956420182105));
#23477=CARTESIAN_POINT('Ctrl Pts',(-1.29377619001345,-1.51837927406437,
20.9885452433897));
#23478=CARTESIAN_POINT('Ctrl Pts',(-1.30701776024503,-1.5069960291394,20.9875303175385));
#23479=CARTESIAN_POINT('Ctrl Pts',(-1.3899443047319,-1.43379216216006,20.9811081521863));
#23480=CARTESIAN_POINT('Ctrl Pts',(-1.45537482442311,-1.36732893258698,
20.9757342648897));
#23481=CARTESIAN_POINT('Ctrl Pts',(-1.55205386191034,-1.25429143651024,
20.9669245740612));
#23482=CARTESIAN_POINT('Ctrl Pts',(-1.5864038286869,-1.21055373530019,20.9635863570589));
#23483=CARTESIAN_POINT('Ctrl Pts',(-1.6378434426487,-1.13910045151353,20.9581907134116));
#23484=CARTESIAN_POINT('Ctrl Pts',(-1.65615962067804,-1.11230216370038,
20.9561794040305));
#23485=CARTESIAN_POINT('Ctrl Pts',(-1.67864536384126,-1.07761598895925,
20.9535859272684));
#23486=CARTESIAN_POINT('Ctrl Pts',(-1.68342768934117,-1.07012975281281,
20.9530267616563));
#23487=CARTESIAN_POINT('Ctrl Pts',(-1.69102317021305,-1.05806289645685,
20.9521262694408));
#23488=CARTESIAN_POINT('Ctrl Pts',(-1.69386812959824,-1.05350235579467,
20.9517861223918));
#23489=CARTESIAN_POINT('Ctrl Pts',(-1.69923646171272,-1.0448188244254,20.9511387854643));
#23490=CARTESIAN_POINT('Ctrl Pts',(-1.70176335234649,-1.04069804488252,
20.9508317280353));
#23491=CARTESIAN_POINT('Ctrl Pts',(-1.70747406450607,-1.03130876813957,
20.9501323809005));
#23492=CARTESIAN_POINT('Ctrl Pts',(-1.71064851455176,-1.02603465558443,
20.9497397518054));
#23493=CARTESIAN_POINT('Ctrl Pts',(-1.72022151452973,-1.00996190778892,
20.9485437920162));
#23494=CARTESIAN_POINT('Ctrl Pts',(-1.72654250038892,-0.99911765904418,
20.947737654936));
#23495=CARTESIAN_POINT('Ctrl Pts',(-1.81033636397372,-0.852191380164005,
20.9368241495545));
#23496=CARTESIAN_POINT('Ctrl Pts',(-1.87160893655554,-0.707536373281423,
20.9261124747945));
#23497=CARTESIAN_POINT('Ctrl Pts',(-1.95127313492434,-0.433717375003955,
20.9062345092853));
#23498=CARTESIAN_POINT('Ctrl Pts',(-1.97518037440777,-0.306994850058432,
20.8971983706322));
#23499=CARTESIAN_POINT('Ctrl Pts',(-1.9877100826093,-0.167806434641161,
20.8879527101568));
#23500=CARTESIAN_POINT('Ctrl Pts',(-1.98861169041916,-0.156760739973835,
20.8872237365665));
#23501=CARTESIAN_POINT('Ctrl Pts',(-1.99001844698862,-0.137553594038412,
20.8859650277712));
#23502=CARTESIAN_POINT('Ctrl Pts',(-1.9905655464046,-0.129395601328476,
20.8854331896449));
#23503=CARTESIAN_POINT('Ctrl Pts',(-1.99128459973133,-0.117586401925617,
20.8846675682353));
#23504=CARTESIAN_POINT('Ctrl Pts',(-1.99149669446991,-0.113937857985663,
20.8844316097618));
#23505=CARTESIAN_POINT('Ctrl Pts',(-1.99184935179946,-0.10756923578421,
20.8840207856241));
#23506=CARTESIAN_POINT('Ctrl Pts',(-1.99199437218206,-0.104849426857585,
20.8838456711378));
#23507=CARTESIAN_POINT('Ctrl Pts',(-1.99228609676488,-0.0991590471834062,
20.8834800033512));
#23508=CARTESIAN_POINT('Ctrl Pts',(-1.99243172798125,-0.0961884484689376,
20.8832895110457));
#23509=CARTESIAN_POINT('Ctrl Pts',(-1.99279825623071,-0.0883537246479702,
20.8827881321422));
#23510=CARTESIAN_POINT('Ctrl Pts',(-1.99300799016818,-0.0834890593249809,
20.8824778669979));
#23511=CARTESIAN_POINT('Ctrl Pts',(-1.99380596780158,-0.0632593994759704,
20.881191802085));
#23512=CARTESIAN_POINT('Ctrl Pts',(-1.99423437709987,-0.0478881272889963,
20.8802245984657));
#23513=CARTESIAN_POINT('Ctrl Pts',(-1.99465762594903,-0.0219241560307305,
20.8786054361783));
#23514=CARTESIAN_POINT('Ctrl Pts',(-1.99474591466741,-0.0113339883133201,
20.8779491026436));
#23515=CARTESIAN_POINT('Ctrl Pts',(-1.99476839307396,0.0489829932903482,
20.8742316625552));
#23516=CARTESIAN_POINT('Ctrl Pts',(-1.99292749800584,0.0986965464004528,
20.8712478548543));
#23517=CARTESIAN_POINT('Ctrl Pts',(-1.97716860906682,0.310089536787109,
20.8587101942019));
#23518=CARTESIAN_POINT('Ctrl Pts',(-1.94541358639662,0.469808908423853,
20.8495614641394));
#23519=CARTESIAN_POINT('Ctrl Pts',(-1.87426142568092,0.685876115117961,
20.8359556299183));
#23520=CARTESIAN_POINT('Ctrl Pts',(-1.85083560043257,0.746785209467117,
20.8319809491297));
#23521=CARTESIAN_POINT('Ctrl Pts',(-1.82023019411856,0.816026726300142,
20.8272483949835));
#23522=CARTESIAN_POINT('Ctrl Pts',(-1.81591426640882,0.825586426708788,
20.8265901799074));
#23523=CARTESIAN_POINT('Ctrl Pts',(-1.80888297791147,0.840838692181028,
20.825532067556));
#23524=CARTESIAN_POINT('Ctrl Pts',(-1.80621562482331,0.846553276059964,
20.8251338230302));
#23525=CARTESIAN_POINT('Ctrl Pts',(-1.80144122255652,0.856656748938176,
20.8244264813752));
#23526=CARTESIAN_POINT('Ctrl Pts',(-1.79934511091369,0.861050773746821,
20.82411776497));
#23527=CARTESIAN_POINT('Ctrl Pts',(-1.79495618607249,0.87016515167175,20.8234751114212));
#23528=CARTESIAN_POINT('Ctrl Pts',(-1.7926607915261,0.874884213345639,20.8231410862755));
#23529=CARTESIAN_POINT('Ctrl Pts',(-1.7866825027129,0.887052564697577,20.8222764291821));
#23530=CARTESIAN_POINT('Ctrl Pts',(-1.78297166095314,0.89448793776662,20.8217448238506));
#23531=CARTESIAN_POINT('Ctrl Pts',(-1.7670515179887,0.925894252489792,20.8194853286888));
#23532=CARTESIAN_POINT('Ctrl Pts',(-1.75440491070679,0.949639155452578,
20.8177421267536));
#23533=CARTESIAN_POINT('Ctrl Pts',(-1.72030565117904,1.01065571662531,20.8131686401678));
#23534=CARTESIAN_POINT('Ctrl Pts',(-1.69812200845352,1.04750069154125,20.810313186436));
#23535=CARTESIAN_POINT('Ctrl Pts',(-1.58360842852719,1.22448839014269,20.7961285278988));
#23536=CARTESIAN_POINT('Ctrl Pts',(-1.47503968637752,1.35330402724302,20.7842427318938));
#23537=CARTESIAN_POINT('Ctrl Pts',(-1.33863747803025,1.47898301608038,20.7714649813158));
#23538=CARTESIAN_POINT('Ctrl Pts',(-1.32545672513084,1.49080701554177,20.7702502186491));
#23539=CARTESIAN_POINT('Ctrl Pts',(-1.27455623573207,1.53525931890152,20.7656395087198));
#23540=CARTESIAN_POINT('Ctrl Pts',(-1.2357715660454,1.56664749845943,20.7622910888135));
#23541=CARTESIAN_POINT('Ctrl Pts',(-1.19012835875964,1.60083512877261,20.758570727107));
#23542=CARTESIAN_POINT('Ctrl Pts',(-1.18438623236307,1.60508812100165,20.758106534246));
#23543=CARTESIAN_POINT('Ctrl Pts',(-1.17583070523126,1.61135398944276,20.7574207439316));
#23544=CARTESIAN_POINT('Ctrl Pts',(-1.17303480173822,1.61339049241423,20.7571975491157));
#23545=CARTESIAN_POINT('Ctrl Pts',(-1.16804832328875,1.61700277005376,20.7568011344654));
#23546=CARTESIAN_POINT('Ctrl Pts',(-1.16585984014542,1.61858137804516,20.7566277193502));
#23547=CARTESIAN_POINT('Ctrl Pts',(-1.16116721392099,1.62195183186857,20.7562570880976));
#23548=CARTESIAN_POINT('Ctrl Pts',(-1.1586621317819,1.62374231584814,20.7560599659928));
#23549=CARTESIAN_POINT('Ctrl Pts',(-1.15180117775299,1.62862215593435,20.7555220570549));
#23550=CARTESIAN_POINT('Ctrl Pts',(-1.14743699056448,1.63169986031115,20.7551820637712));
#23551=CARTESIAN_POINT('Ctrl Pts',(-1.12464448547164,1.64763688477039,20.7534173536551));
#23552=CARTESIAN_POINT('Ctrl Pts',(-1.10601130715639,1.66020228136474,20.7520117899838));
#23553=CARTESIAN_POINT('Ctrl Pts',(-1.05106997858262,1.69591663626929,20.7479618943836));
#23554=CARTESIAN_POINT('Ctrl Pts',(-1.01421825613947,1.71820929582388,20.7453630016253));
#23555=CARTESIAN_POINT('Ctrl Pts',(-0.904317707491192,1.77992213952994,
20.7378636936592));
#23556=CARTESIAN_POINT('Ctrl Pts',(-0.829495670003397,1.81599879998697,
20.733068334897));
#23557=CARTESIAN_POINT('Ctrl Pts',(-0.611778883570966,1.9047020594815,20.7194317446622));
#23558=CARTESIAN_POINT('Ctrl Pts',(-0.464838532057203,1.9457850376763,20.7105528282108));
#23559=CARTESIAN_POINT('Ctrl Pts',(-0.302143524173006,1.9717752702888,20.7002656777771));
#23560=CARTESIAN_POINT('Ctrl Pts',(-0.289600578998553,1.97365648442812,
20.6994700978053));
#23561=CARTESIAN_POINT('Ctrl Pts',(-0.270918873800382,1.97627648397204,
20.6982811187106));
#23562=CARTESIAN_POINT('Ctrl Pts',(-0.264793072890843,1.97710657386833,
20.6978906062086));
#23563=CARTESIAN_POINT('Ctrl Pts',(-0.253867515447367,1.97853537815539,
20.6971929321118));
#23564=CARTESIAN_POINT('Ctrl Pts',(-0.249069232536893,1.97914513736109,
20.6968861218239));
#23565=CARTESIAN_POINT('Ctrl Pts',(-0.238948475413551,1.98039388140843,
20.6962381073448));
#23566=CARTESIAN_POINT('Ctrl Pts',(-0.233625555871817,1.98102887362625,
20.6958967797632));
#23567=CARTESIAN_POINT('Ctrl Pts',(-0.219539843419446,1.98265165417861,
20.6949921641047));
#23568=CARTESIAN_POINT('Ctrl Pts',(-0.210773025808216,1.9836027959536,20.6944277263706));
#23569=CARTESIAN_POINT('Ctrl Pts',(-0.170390079741878,1.98771334512583,
20.6918210112972));
#23570=CARTESIAN_POINT('Ctrl Pts',(-0.138709114305952,1.99017504498136,
20.6897569537459));
#23571=CARTESIAN_POINT('Ctrl Pts',(-0.0530896116608339,1.99477369023793,
20.6841237031214));
#23572=CARTESIAN_POINT('Ctrl Pts',(0.000895923536202471,1.9954796182546,
20.6805123946312));
#23573=CARTESIAN_POINT('Ctrl Pts',(0.157708187939494,1.99116689184892,20.6698571293759));
#23574=CARTESIAN_POINT('Ctrl Pts',(0.260195852412431,1.98038186095124,20.6626775326176));
#23575=CARTESIAN_POINT('Ctrl Pts',(0.474134462384115,1.94097089468312,20.6475040564342));
#23576=CARTESIAN_POINT('Ctrl Pts',(0.584898793153921,1.91051605508487,20.6395384356151));
#23577=CARTESIAN_POINT('Ctrl Pts',(0.699578850912882,1.86806714959347,20.6315527121247));
#23578=CARTESIAN_POINT('Ctrl Pts',(0.706698718336567,1.86538531409833,20.63105808478));
#23579=CARTESIAN_POINT('Ctrl Pts',(0.717131907084739,1.86138714344612,20.6303351702207));
#23580=CARTESIAN_POINT('Ctrl Pts',(0.720457215266392,1.8601025970093,20.6301050437164));
#23581=CARTESIAN_POINT('Ctrl Pts',(0.726313246717226,1.85782238810294,20.6297003030155));
#23582=CARTESIAN_POINT('Ctrl Pts',(0.728845399198117,1.85683045605249,20.6295254663805));
#23583=CARTESIAN_POINT('Ctrl Pts',(0.734154485792772,1.85473816893816,20.6291592641874));
#23584=CARTESIAN_POINT('Ctrl Pts',(0.73693097329095,1.8536367565459,20.6289679638558));
#23585=CARTESIAN_POINT('Ctrl Pts',(0.744280144748954,1.85070227154632,20.628462140696));
#23586=CARTESIAN_POINT('Ctrl Pts',(0.748848566360184,1.84885847421659,20.6281482593375));
#23587=CARTESIAN_POINT('Ctrl Pts',(0.769803995391451,1.84031053020935,20.6267108055312));
#23588=CARTESIAN_POINT('Ctrl Pts',(0.786108748360493,1.83340506353455,20.6255989157678));
#23589=CARTESIAN_POINT('Ctrl Pts',(0.830413390364009,1.81394121223263,20.6225898718312));
#23590=CARTESIAN_POINT('Ctrl Pts',(0.858219814201922,1.80095199397567,20.6207148897967));
#23591=CARTESIAN_POINT('Ctrl Pts',(0.954049267081981,1.75346329264872,20.6142633617162));
#23592=CARTESIAN_POINT('Ctrl Pts',(1.02038839779694,1.71570763020122,20.6098139422606));
#23593=CARTESIAN_POINT('Ctrl Pts',(1.22263834661753,1.58471046030953,20.595819758751));
#23594=CARTESIAN_POINT('Ctrl Pts',(1.34923259786795,1.4784167294981,20.5863451595544));
#23595=CARTESIAN_POINT('Ctrl Pts',(1.47549067428435,1.34253050423435,20.5748652196335));
#23596=CARTESIAN_POINT('Ctrl Pts',(1.48941989450352,1.3270603646162,20.5735673037745));
#23597=CARTESIAN_POINT('Ctrl Pts',(1.50822859696124,1.30550175172249,20.5717693601583));
#23598=CARTESIAN_POINT('Ctrl Pts',(1.51331859777057,1.29959806990368,20.571278093037));
#23599=CARTESIAN_POINT('Ctrl Pts',(1.52137097679652,1.29014699598195,20.5704932838955));
#23600=CARTESIAN_POINT('Ctrl Pts',(1.52435589162585,1.28661883841277,20.570200670987));
#23601=CARTESIAN_POINT('Ctrl Pts',(1.53045599836644,1.27935751080579,20.5695991651803));
#23602=CARTESIAN_POINT('Ctrl Pts',(1.53356985316342,1.27562326263333,20.569290220531));
#23603=CARTESIAN_POINT('Ctrl Pts',(1.54073341918444,1.26696831329434,20.5685750462435));
#23604=CARTESIAN_POINT('Ctrl Pts',(1.54477324709192,1.26203953559078,20.5681684197521));
#23605=CARTESIAN_POINT('Ctrl Pts',(1.55740397678857,1.24647794827303,20.5668865474606));
#23606=CARTESIAN_POINT('Ctrl Pts',(1.5659090940346,1.23577632126464,20.5660078722085));
#23607=CARTESIAN_POINT('Ctrl Pts',(1.65082204766596,1.12664977283399,20.557074940533));
#23608=CARTESIAN_POINT('Ctrl Pts',(1.71794396909565,1.02137709226249,20.5486515452287));
#23609=CARTESIAN_POINT('Ctrl Pts',(1.83576437377644,0.791727453541646,20.5307727742091));
#23610=CARTESIAN_POINT('Ctrl Pts',(1.88463965623471,0.667081514609771,20.5213313932871));
#23611=CARTESIAN_POINT('Ctrl Pts',(1.9311279464309,0.50126505474854,20.5096788883549));
#23612=CARTESIAN_POINT('Ctrl Pts',(1.94047977290186,0.463746200616541,20.5071016419899));
#23613=CARTESIAN_POINT('Ctrl Pts',(1.95014580237329,0.419526519009288,20.5041512691031));
#23614=CARTESIAN_POINT('Ctrl Pts',(1.95152367408803,0.41306961049691,20.5037226188492));
#23615=CARTESIAN_POINT('Ctrl Pts',(1.95356127096199,0.403283325922952,20.5030763332975));
#23616=CARTESIAN_POINT('Ctrl Pts',(1.95424458204713,0.39995899080945,20.5028573853821));
#23617=CARTESIAN_POINT('Ctrl Pts',(1.95545480467101,0.393994060232259,20.5024656012927));
#23618=CARTESIAN_POINT('Ctrl Pts',(1.95598485445028,0.391354138935763,20.5022925877211));
#23619=CARTESIAN_POINT('Ctrl Pts',(1.95711824032035,0.385649468091649,20.5019195410964));
#23620=CARTESIAN_POINT('Ctrl Pts',(1.95771972172431,0.382584383284932,20.5017196151784));
#23621=CARTESIAN_POINT('Ctrl Pts',(1.95936828162208,0.374077806464852,20.5011661392954));
#23622=CARTESIAN_POINT('Ctrl Pts',(1.96039989938741,0.368633292800868,20.5008134616092));
#23623=CARTESIAN_POINT('Ctrl Pts',(1.9660075460108,0.33834871726512,20.4988600707724));
#23624=CARTESIAN_POINT('Ctrl Pts',(1.97013439630459,0.313426436307198,20.4972837169013));
#23625=CARTESIAN_POINT('Ctrl Pts',(1.99733693981883,0.127274438934472,20.4856956322969));
#23626=CARTESIAN_POINT('Ctrl Pts',(2.00106448360066,-0.0361804509339467,
20.4765163451083));
#23627=CARTESIAN_POINT('Ctrl Pts',(1.98378470925755,-0.209153196562604,
20.4663531028269));
#23628=CARTESIAN_POINT('Ctrl Pts',(1.98260989290247,-0.220011003369011,
20.4657134456306));
#23629=CARTESIAN_POINT('Ctrl Pts',(1.96965121070298,-0.331229036817398,
20.4591406867822));
#23630=CARTESIAN_POINT('Ctrl Pts',(1.95034846566181,-0.430552195970423,
20.4530876079861));
#23631=CARTESIAN_POINT('Ctrl Pts',(1.92021939793493,-0.540322974101999,
20.4459812336882));
#23632=CARTESIAN_POINT('Ctrl Pts',(1.91671222826163,-0.55263520916391,20.4451782800329));
#23633=CARTESIAN_POINT('Ctrl Pts',(1.91132953098247,-0.570863811689611,
20.443980399156));
#23634=CARTESIAN_POINT('Ctrl Pts',(1.90954446543396,-0.576806727266043,
20.443588422871));
#23635=CARTESIAN_POINT('Ctrl Pts',(1.90631785433562,-0.587369750298536,
20.4428891094832));
#23636=CARTESIAN_POINT('Ctrl Pts',(1.90488716289222,-0.591993142947174,
20.4425821298778));
#23637=CARTESIAN_POINT('Ctrl Pts',(1.90184013570277,-0.601714435377332,
20.441934762351));
#23638=CARTESIAN_POINT('Ctrl Pts',(1.90022009778173,-0.606811125952121,
20.441594254879));
#23639=CARTESIAN_POINT('Ctrl Pts',(1.89589202236301,-0.620240084236888,
20.4406941217714));
#23640=CARTESIAN_POINT('Ctrl Pts',(1.89314957491207,-0.628561059485576,
20.4401333668126));
#23641=CARTESIAN_POINT('Ctrl Pts',(1.88039524767662,-0.666418732549545,
20.4375681658284));
#23642=CARTESIAN_POINT('Ctrl Pts',(1.86974680414694,-0.695734805670041,
20.435542777292));
#23643=CARTESIAN_POINT('Ctrl Pts',(1.83930489877027,-0.773790364627192,
20.4300410282625));
#23644=CARTESIAN_POINT('Ctrl Pts',(1.81826469385884,-0.822013826381631,
20.4265249259601));
#23645=CARTESIAN_POINT('Ctrl Pts',(1.7087984447378,-1.04807990322145,20.4094829484785));
#23646=CARTESIAN_POINT('Ctrl Pts',(1.596062681537,-1.21286214527536,20.3952207082234));
#23647=CARTESIAN_POINT('Ctrl Pts',(1.45746392762335,-1.36192928909657,20.3816285451081));
#23648=CARTESIAN_POINT('Ctrl Pts',(1.45405057768791,-1.36557292276706,20.381295918343));
#23649=CARTESIAN_POINT('Ctrl Pts',(1.4368148253314,-1.38383360048671,20.3796270793348));
#23650=CARTESIAN_POINT('Ctrl Pts',(1.42278490794068,-1.39825443273459,20.3783032452223));
#23651=CARTESIAN_POINT('Ctrl Pts',(1.40476520045535,-1.41622409659852,20.3766488773825));
#23652=CARTESIAN_POINT('Ctrl Pts',(1.40097671208021,-1.41997190605658,20.376303570256));
#23653=CARTESIAN_POINT('Ctrl Pts',(1.39495503138068,-1.42588137016206,20.3757587407628));
#23654=CARTESIAN_POINT('Ctrl Pts',(1.39273176216352,-1.42805303134533,20.3755584451444));
#23655=CARTESIAN_POINT('Ctrl Pts',(1.3885899436377,-1.43207983475016,20.37518691942));
#23656=CARTESIAN_POINT('Ctrl Pts',(1.38667276724863,-1.43393630310631,20.375015586868));
#23657=CARTESIAN_POINT('Ctrl Pts',(1.3823027627939,-1.43815096966422,20.3746264987679));
#23658=CARTESIAN_POINT('Ctrl Pts',(1.3798476291947,-1.44050673729787,20.3744089331239));
#23659=CARTESIAN_POINT('Ctrl Pts',(1.37242243489901,-1.44759501250875,20.3737539921292));
#23660=CARTESIAN_POINT('Ctrl Pts',(1.36743390309245,-1.45230822624932,20.3733180862744));
#23661=CARTESIAN_POINT('Ctrl Pts',(1.31845255320753,-1.4981101619401,20.3690767800569));
#23662=CARTESIAN_POINT('Ctrl Pts',(1.27264042127202,-1.53721799577438,20.3654133496719));
#23663=CARTESIAN_POINT('Ctrl Pts',(1.11777788709031,-1.65774028460213,20.3537152904472));
#23664=CARTESIAN_POINT('Ctrl Pts',(1.00216337446197,-1.73008756024586,20.34599524919));
#23665=CARTESIAN_POINT('Ctrl Pts',(0.788899591332623,-1.83493551619263,
20.3320483638324));
#23666=CARTESIAN_POINT('Ctrl Pts',(0.69444015082306,-1.87272515311601,20.3259635917708));
#23667=CARTESIAN_POINT('Ctrl Pts',(0.585316550302441,-1.9069860392324,20.3188231148549));
#23668=CARTESIAN_POINT('Ctrl Pts',(0.573074841999933,-1.91070050798264,
20.3180207303827));
#23669=CARTESIAN_POINT('Ctrl Pts',(0.554845239319503,-1.91604091958289,
20.3168235364142));
#23670=CARTESIAN_POINT('Ctrl Pts',(0.548883955707449,-1.91775713969889,
20.3164316728657));
#23671=CARTESIAN_POINT('Ctrl Pts',(0.538258022312406,-1.92076268305258,
20.3157324859282));
#23672=CARTESIAN_POINT('Ctrl Pts',(0.533596482817148,-1.92206289596355,
20.3154255195595));
#23673=CARTESIAN_POINT('Ctrl Pts',(0.528922010563834,-1.92334840039834,
20.3151174546899));
#23674=CARTESIAN_POINT('Ctrl Pts',(0.528913729745517,-1.92335067760937,
20.3151169089528));
#23675=CARTESIAN_POINT('Ctrl Pts',(0.52889718726741,-1.92335522664796,20.3151158187397));
#23676=CARTESIAN_POINT('Ctrl Pts',(0.52888892554063,-1.92335749849421,20.3151152742593));
#23677=CARTESIAN_POINT('Ctrl Pts',(0.528872420928399,-1.92336203689124,
20.3151141865386));
#23678=CARTESIAN_POINT('Ctrl Pts',(0.528864178114277,-1.92336430342267,
20.3151136433031));
#23679=CARTESIAN_POINT('Ctrl Pts',(0.528847711516913,-1.92336883113876,
20.3151125580847));
#23680=CARTESIAN_POINT('Ctrl Pts',(0.528839487629902,-1.9233710923522,20.315112016095));
#23681=CARTESIAN_POINT('Ctrl Pts',(0.523767067259621,-1.92476575370058,
20.3147777211988));
#23682=CARTESIAN_POINT('Ctrl Pts',(0.518697431709371,-1.92613813648773,
20.3144433197822));
#23683=CARTESIAN_POINT('Ctrl Pts',(0.505457657848107,-1.92966616711681,
20.3135692166355));
#23684=CARTESIAN_POINT('Ctrl Pts',(0.497279205034542,-1.93178993397027,
20.313028487511));
#23685=CARTESIAN_POINT('Ctrl Pts',(0.479334254635,-1.93632834181821,20.3118402354014));
#23686=CARTESIAN_POINT('Ctrl Pts',(0.469562531243437,-1.93872117594944,
20.3111920237576));
#23687=CARTESIAN_POINT('Ctrl Pts',(0.440789658567927,-1.945536593528,20.3092797784676));
#23688=CARTESIAN_POINT('Ctrl Pts',(0.421741682996167,-1.94975436091704,
20.3080092606781));
#23689=CARTESIAN_POINT('Ctrl Pts',(0.354850016223437,-1.96354003302606,
20.3035305146353));
#23690=CARTESIAN_POINT('Ctrl Pts',(0.306722968757956,-1.97163088840184,
20.3002773240443));
#23691=CARTESIAN_POINT('Ctrl Pts',(0.140755785821808,-1.99330878218816,
20.2889567147697));
#23692=CARTESIAN_POINT('Ctrl Pts',(0.0220349285774205,-1.99814947960201,
20.280666795027));
#23693=CARTESIAN_POINT('Ctrl Pts',(-0.168616295561586,-1.9889252680014,
20.2673631480476));
#23694=CARTESIAN_POINT('Ctrl Pts',(-0.240595802031494,-1.98150706759378,
20.2623478731941));
#23695=CARTESIAN_POINT('Ctrl Pts',(-0.347871859377439,-1.96451787710126,
20.2550130235649));
#23696=CARTESIAN_POINT('Ctrl Pts',(-0.383567143313866,-1.95786158239877,
20.2525964775362));
#23697=CARTESIAN_POINT('Ctrl Pts',(-0.424841584467101,-1.94899259072776,
20.2498453854307));
#23698=CARTESIAN_POINT('Ctrl Pts',(-0.43061423656448,-1.94772530712237,
20.2494616083487));
#23699=CARTESIAN_POINT('Ctrl Pts',(-0.439825434810796,-1.94566019848988,
20.2488509078089));
#23700=CARTESIAN_POINT('Ctrl Pts',(-0.443267588076611,-1.94487888232808,
20.2486230687879));
#23701=CARTESIAN_POINT('Ctrl Pts',(-0.449353041137022,-1.94348058244005,
20.2482209534395));
#23702=CARTESIAN_POINT('Ctrl Pts',(-0.451997175836633,-1.94286733548465,
20.2480464640574));
#23703=CARTESIAN_POINT('Ctrl Pts',(-0.457565648197978,-1.94156387170542,
20.2476794867065));
#23704=CARTESIAN_POINT('Ctrl Pts',(-0.46048967322923,-1.94087244595429,
20.2474870697029));
#23705=CARTESIAN_POINT('Ctrl Pts',(-0.468280741678794,-1.93901154326947,
20.2469751049772));
#23706=CARTESIAN_POINT('Ctrl Pts',(-0.473145004033291,-1.93783033943265,
20.2466562267975));
#23707=CARTESIAN_POINT('Ctrl Pts',(-0.495995807457831,-1.93219023791108,
20.2451615946121));
#23708=CARTESIAN_POINT('Ctrl Pts',(-0.513924815307466,-1.92749897545502,
20.2439986876174));
#23709=CARTESIAN_POINT('Ctrl Pts',(-0.69758776825939,-1.87669713630335,
20.2321624478231));
#23710=CARTESIAN_POINT('Ctrl Pts',(-0.856784875385627,-1.80957429655429,
20.2224976794698));
#23711=CARTESIAN_POINT('Ctrl Pts',(-1.10075895629859,-1.66719678253958,
20.2059745180876));
#23712=CARTESIAN_POINT('Ctrl Pts',(-1.19131131641182,-1.60374173462483,
20.1993914283463));
#23713=CARTESIAN_POINT('Ctrl Pts',(-1.28607029642266,-1.52486641012604,
20.1916954683965));
#23714=CARTESIAN_POINT('Ctrl Pts',(-1.29591634532761,-1.5165075632808,20.1908854579668));
#23715=CARTESIAN_POINT('Ctrl Pts',(-1.31038844883627,-1.50397754574264,
20.1896790639482));
#23716=CARTESIAN_POINT('Ctrl Pts',(-1.31507739280921,-1.49987925995224,
20.1892856934848));
#23717=CARTESIAN_POINT('Ctrl Pts',(-1.32337814949308,-1.49255528726999,
20.1885848136784));
#23718=CARTESIAN_POINT('Ctrl Pts',(-1.3269975680024,-1.48933826444883,20.1882776677347));
#23719=CARTESIAN_POINT('Ctrl Pts',(-1.33396468447799,-1.48310017088257,
20.1876834355184));
#23720=CARTESIAN_POINT('Ctrl Pts',(-1.33731392619724,-1.48008086216766,
20.1873964245369));
#23721=CARTESIAN_POINT('Ctrl Pts',(-1.34613466737381,-1.47207466731663,
20.1866369381957));
#23722=CARTESIAN_POINT('Ctrl Pts',(-1.35158865232037,-1.4670686696032,20.1861636538531));
#23723=CARTESIAN_POINT('Ctrl Pts',(-1.37260448857279,-1.44756240238564,
20.1843254945044));
#23724=CARTESIAN_POINT('Ctrl Pts',(-1.38796142418423,-1.43284438008474,
20.1829513084693));
#23725=CARTESIAN_POINT('Ctrl Pts',(-1.42564730543416,-1.39555198626953,
20.1794993852665));
#23726=CARTESIAN_POINT('Ctrl Pts',(-1.44767750056089,-1.37268541596079,
20.1774090697715));
#23727=CARTESIAN_POINT('Ctrl Pts',(-1.51759834108046,-1.29655407288879,
20.170531412078));
#23728=CARTESIAN_POINT('Ctrl Pts',(-1.56316425510684,-1.24123845635288,
20.1656569067693));
#23729=CARTESIAN_POINT('Ctrl Pts',(-1.66315172134245,-1.10559670011308,
20.1540240149303));
#23730=CARTESIAN_POINT('Ctrl Pts',(-1.71488863749726,-1.02351049239724,
20.147219639307));
#23731=CARTESIAN_POINT('Ctrl Pts',(-1.79990051468839,-0.863957834649184,
20.1346810595498));
#23732=CARTESIAN_POINT('Ctrl Pts',(-1.83464356822001,-0.787497024447547,
20.1289402964422));
#23733=CARTESIAN_POINT('Ctrl Pts',(-1.8672508331969,-0.701757111122103,
20.1229486288768));
#23734=CARTESIAN_POINT('Ctrl Pts',(-1.86998767853476,-0.694431281061299,
20.1224401652213));
#23735=CARTESIAN_POINT('Ctrl Pts',(-1.87390431070599,-0.683756390259391,
20.1217044969201));
#23736=CARTESIAN_POINT('Ctrl Pts',(-1.87511830784384,-0.680420090069961,
20.1214753148594));
#23737=CARTESIAN_POINT('Ctrl Pts',(-1.87724574121125,-0.674524553558618,
20.1210716603941));
#23738=CARTESIAN_POINT('Ctrl Pts',(-1.8781628629766,-0.671966670859111,
20.1208969694257));
#23739=CARTESIAN_POINT('Ctrl Pts',(-1.88007954767483,-0.666586394718117,
20.1205304580266));
#23740=CARTESIAN_POINT('Ctrl Pts',(-1.88107798144244,-0.663763629035798,
20.1203387051626));
#23741=CARTESIAN_POINT('Ctrl Pts',(-1.88371299589392,-0.656260236447226,
20.1198303932575));
#23742=CARTESIAN_POINT('Ctrl Pts',(-1.88533849955046,-0.651575699536349,
20.119514487004));
#23743=CARTESIAN_POINT('Ctrl Pts',(-1.89279531171783,-0.629824377485894,
20.118054141564));
#23744=CARTESIAN_POINT('Ctrl Pts',(-1.8984126836074,-0.612684401991071,
20.116921844109));
#23745=CARTESIAN_POINT('Ctrl Pts',(-1.9495871232946,-0.44907285613511,20.1062669395526));
#23746=CARTESIAN_POINT('Ctrl Pts',(-1.97834520572389,-0.297860487836512,
20.0975545876577));
#23747=CARTESIAN_POINT('Ctrl Pts',(-1.9929598869966,-0.0971002446200696,
20.0858436778963));
#23748=CARTESIAN_POINT('Ctrl Pts',(-1.99471555080441,-0.0492650808880827,
20.0830456991473));
#23749=CARTESIAN_POINT('Ctrl Pts',(-1.99474949799968,-0.00141517844896885,
20.0802123525403));
#23750=CARTESIAN_POINT('',(-1.9947498118588,0.000866365563832799,18.4790451186048));
#23751=CARTESIAN_POINT('Ctrl Pts',(-1.99474949974525,-0.00141271585688734,
20.0802122067223));
#23752=CARTESIAN_POINT('Ctrl Pts',(-1.99479157143496,0.0579923524695157,
20.0766946401339));
#23753=CARTESIAN_POINT('Ctrl Pts',(-1.99217996997649,0.117366413478714,
20.0731252228154));
#23754=CARTESIAN_POINT('Ctrl Pts',(-1.98462482765162,0.202401326950034,
20.0678812145986));
#23755=CARTESIAN_POINT('Ctrl Pts',(-1.98182164648267,0.228221095170741,
20.0662715292149));
#23756=CARTESIAN_POINT('Ctrl Pts',(-1.97754983490082,0.261498970957234,
20.064171466487));
#23757=CARTESIAN_POINT('Ctrl Pts',(-1.97654150200027,0.269014404190812,
20.0636955134407));
#23758=CARTESIAN_POINT('Ctrl Pts',(-1.97475763923998,0.281758346576112,
20.0628855115214));
#23759=CARTESIAN_POINT('Ctrl Pts',(-1.97400412832825,0.286989895422397,
20.0625521569281));
#23760=CARTESIAN_POINT('Ctrl Pts',(-1.97256852378058,0.296683940159797,
20.0619328696202));
#23761=CARTESIAN_POINT('Ctrl Pts',(-1.97189205527009,0.30114724500578,20.0616471162348));
#23762=CARTESIAN_POINT('Ctrl Pts',(-1.97046024938845,0.310382522488708,
20.0610545403539));
#23763=CARTESIAN_POINT('Ctrl Pts',(-1.96970271482704,0.315154119780667,
20.0607476500414));
#23764=CARTESIAN_POINT('Ctrl Pts',(-1.96794411801215,0.325977197581678,
20.0600498874106));
#23765=CARTESIAN_POINT('Ctrl Pts',(-1.96693246733654,0.332026885222133,
20.0596586815144));
#23766=CARTESIAN_POINT('Ctrl Pts',(-1.96425073004043,0.347621232672551,
20.0586471653638));
#23767=CARTESIAN_POINT('Ctrl Pts',(-1.96253898574749,0.357158474328952,
20.0580255367881));
#23768=CARTESIAN_POINT('Ctrl Pts',(-1.95157086246802,0.41580817921827,20.0541839222342));
#23769=CARTESIAN_POINT('Ctrl Pts',(-1.94054169223333,0.464566970840847,
20.0509078124423));
#23770=CARTESIAN_POINT('Ctrl Pts',(-1.92434694564427,0.525438773852179,
20.0467091832994));
#23771=CARTESIAN_POINT('Ctrl Pts',(-1.92087652530502,0.537987392652589,
20.0458377796828));
#23772=CARTESIAN_POINT('Ctrl Pts',(-1.90906629775885,0.579120031182964,
20.0429622371476));
#23773=CARTESIAN_POINT('Ctrl Pts',(-1.9002095833829,0.607550448750966,20.0409439823474));
#23774=CARTESIAN_POINT('Ctrl Pts',(-1.8550898910222,0.741731967202147,20.0312772633244));
#23775=CARTESIAN_POINT('Ctrl Pts',(-1.8106167829739,0.844504880364251,20.0234362259177));
#23776=CARTESIAN_POINT('Ctrl Pts',(-1.71323201346121,1.02603195526923,20.0091069977932));
#23777=CARTESIAN_POINT('Ctrl Pts',(-1.66285586473625,1.10581211996945,20.002621886709));
#23778=CARTESIAN_POINT('Ctrl Pts',(-1.60206958213234,1.18847401564678,19.995913648131));
#23779=CARTESIAN_POINT('Ctrl Pts',(-1.59707524053649,1.19517702198866,19.9953698050596));
#23780=CARTESIAN_POINT('Ctrl Pts',(-1.58981689601905,1.20479184897804,19.9945901300848));
#23781=CARTESIAN_POINT('Ctrl Pts',(-1.58758680638758,1.20772898240941,19.9943520118123));
#23782=CARTESIAN_POINT('Ctrl Pts',(-1.58369238853638,1.2128286883807,19.9939386934998));
#23783=CARTESIAN_POINT('Ctrl Pts',(-1.58203175133413,1.21499405225157,19.993763235557));
#23784=CARTESIAN_POINT('Ctrl Pts',(-1.57878391994185,1.2192110665583,19.9934216190243));
#23785=CARTESIAN_POINT('Ctrl Pts',(-1.57719717225079,1.22126302274253,19.9932554298611));
#23786=CARTESIAN_POINT('Ctrl Pts',(-1.57287736067164,1.22682687189651,19.9928048957413));
#23787=CARTESIAN_POINT('Ctrl Pts',(-1.57013651944046,1.23033275034268,19.9925210989883));
#23788=CARTESIAN_POINT('Ctrl Pts',(-1.55978582814503,1.24348165599816,19.9914569347669));
#23789=CARTESIAN_POINT('Ctrl Pts',(-1.55209849417305,1.25306374177308,19.9906818951945));
#23790=CARTESIAN_POINT('Ctrl Pts',(-1.54252308387722,1.26477594219974,19.9897342668684));
#23791=CARTESIAN_POINT('Ctrl Pts',(-1.54071854731388,1.26697356185253,19.9895564455782));
#23792=CARTESIAN_POINT('Ctrl Pts',(-1.44341994067265,1.38495148938827,19.9800090486742));
#23793=CARTESIAN_POINT('Ctrl Pts',(-1.3351531459121,1.48960804179835,19.9714545660136));
#23794=CARTESIAN_POINT('Ctrl Pts',(-1.14510025738833,1.63578985610729,19.9575242873846));
#23795=CARTESIAN_POINT('Ctrl Pts',(-1.07044784642207,1.68558670192604,19.9522779572911));
#23796=CARTESIAN_POINT('Ctrl Pts',(-0.963364394474653,1.74702629618186,
19.944820631185));
#23797=CARTESIAN_POINT('Ctrl Pts',(-0.933601571033613,1.76311081517892,
19.9427554660563));
#23798=CARTESIAN_POINT('Ctrl Pts',(-0.883517736577203,1.78855348389122,
19.9392826660378));
#23799=CARTESIAN_POINT('Ctrl Pts',(-0.863421987155416,1.79834078095296,
19.9378898853884));
#23800=CARTESIAN_POINT('Ctrl Pts',(-0.836164322159506,1.81105397147456,
19.9359998281854));
#23801=CARTESIAN_POINT('Ctrl Pts',(-0.829143171850048,1.814279156885,19.9355129020865));
#23802=CARTESIAN_POINT('Ctrl Pts',(-0.817995593756372,1.81932160409208,
19.9347396096534));
#23803=CARTESIAN_POINT('Ctrl Pts',(-0.813881387141164,1.82116582925369,
19.9344541713745));
#23804=CARTESIAN_POINT('Ctrl Pts',(-0.80533365341709,1.8249626675538,19.9338610380314));
#23805=CARTESIAN_POINT('Ctrl Pts',(-0.800899199043685,1.82691310783573,
19.9335532709729));
#23806=CARTESIAN_POINT('Ctrl Pts',(-0.790733790151156,1.83134011389263,
19.9328476027526));
#23807=CARTESIAN_POINT('Ctrl Pts',(-0.784998248123695,1.83380595718764,
19.9324493391482));
#23808=CARTESIAN_POINT('Ctrl Pts',(-0.76728841705765,1.84132151742653,19.9312192098373));
#23809=CARTESIAN_POINT('Ctrl Pts',(-0.755276473047177,1.84628109492061,
19.9303842975684));
#23810=CARTESIAN_POINT('Ctrl Pts',(-0.627497203455606,1.89758387336553,
19.9214953793794));
#23811=CARTESIAN_POINT('Ctrl Pts',(-0.50769808320323,1.93308287286196,19.9130708865235));
#23812=CARTESIAN_POINT('Ctrl Pts',(-0.230437029749444,1.98767902824605,
19.8935022627038));
#23813=CARTESIAN_POINT('Ctrl Pts',(-0.0724058547523233,1.99968255789331,
19.8822860173317));
#23814=CARTESIAN_POINT('Ctrl Pts',(0.103631904175656,1.99213989303651,19.8706063160622));
#23815=CARTESIAN_POINT('Ctrl Pts',(0.121862603145181,1.99110785474312,19.8694071947563));
#23816=CARTESIAN_POINT('Ctrl Pts',(0.145044833564224,1.98947590009342,19.867897837713));
#23817=CARTESIAN_POINT('Ctrl Pts',(0.150011067178842,1.98910759935675,19.8675753983959));
#23818=CARTESIAN_POINT('Ctrl Pts',(0.157965748569112,1.9884877113156,19.8670604349542));
#23819=CARTESIAN_POINT('Ctrl Pts',(0.160955058130292,1.98824797883173,19.866867256255));
#23820=CARTESIAN_POINT('Ctrl Pts',(0.166650600758536,1.98777828646641,19.8664998561568));
#23821=CARTESIAN_POINT('Ctrl Pts',(0.169356871456463,1.98754954379765,19.8663255715384));
#23822=CARTESIAN_POINT('Ctrl Pts',(0.17559035852282,1.98700984548761,19.8659247836223));
#23823=CARTESIAN_POINT('Ctrl Pts',(0.179117218275992,1.98669502507574,19.8656984997581));
#23824=CARTESIAN_POINT('Ctrl Pts',(0.188566409893344,1.98582618875558,19.8650934770131));
#23825=CARTESIAN_POINT('Ctrl Pts',(0.194487189884171,1.98525506623446,19.8647156799015));
#23826=CARTESIAN_POINT('Ctrl Pts',(0.237300289343633,1.98093191365155,19.8619927018668));
#23827=CARTESIAN_POINT('Ctrl Pts',(0.27408699710948,1.97617798229358,19.8597006549321));
#23828=CARTESIAN_POINT('Ctrl Pts',(0.32219531135202,1.96859153769233,19.8567408622568));
#23829=CARTESIAN_POINT('Ctrl Pts',(0.33365230809027,1.96668213197125,19.8560388145315));
#23830=CARTESIAN_POINT('Ctrl Pts',(0.377995416626657,1.95889332325865,19.8533303504125));
#23831=CARTESIAN_POINT('Ctrl Pts',(0.410749608172277,1.95228802240549,19.8513483611052));
#23832=CARTESIAN_POINT('Ctrl Pts',(0.576764093016468,1.91444569063303,19.8413301455033));
#23833=CARTESIAN_POINT('Ctrl Pts',(0.706718720786841,1.8703767146194,19.8335526180792));
#23834=CARTESIAN_POINT('Ctrl Pts',(0.880394668499987,1.79077314887592,19.8222249415291));
#23835=CARTESIAN_POINT('Ctrl Pts',(0.928705719902529,1.7662016396177,19.8189682357586));
#23836=CARTESIAN_POINT('Ctrl Pts',(0.994274895496613,1.72941790086039,19.8143585047188));
#23837=CARTESIAN_POINT('Ctrl Pts',(1.01243156762269,1.71885168471277,19.8130611367147));
#23838=CARTESIAN_POINT('Ctrl Pts',(1.03950541482379,1.70251834205102,19.8110929985837));
#23839=CARTESIAN_POINT('Ctrl Pts',(1.04854930467336,1.69696333528007,19.810429802151));
#23840=CARTESIAN_POINT('Ctrl Pts',(1.0650587620294,1.68664040516485,19.8092083021186));
#23841=CARTESIAN_POINT('Ctrl Pts',(1.07253776448059,1.68189439698195,19.8086508079343));
#23842=CARTESIAN_POINT('Ctrl Pts',(1.08446750711907,1.67421211796774,19.8077547809032));
#23843=CARTESIAN_POINT('Ctrl Pts',(1.08893857363858,1.67130750368955,19.8074174275886));
#23844=CARTESIAN_POINT('Ctrl Pts',(1.0934037171669,1.66838121358215,19.8070789639158));
#23845=CARTESIAN_POINT('Ctrl Pts',(1.09340952810014,1.66837740526779,19.8070785234369));
#23846=CARTESIAN_POINT('Ctrl Pts',(1.09342116748771,1.66836977706933,19.8070776411456));
#23847=CARTESIAN_POINT('Ctrl Pts',(1.0934269959196,1.66836595719968,19.8070771993349));
#23848=CARTESIAN_POINT('Ctrl Pts',(1.09343867034859,1.66835830586093,19.8070763143767));
#23849=CARTESIAN_POINT('Ctrl Pts',(1.09344451631787,1.66835447440981,19.8070758712313));
#23850=CARTESIAN_POINT('Ctrl Pts',(1.09345622602696,1.66834679977276,19.8070749835881));
#23851=CARTESIAN_POINT('Ctrl Pts',(1.09346208966169,1.66834295665544,19.8070745390982));
#23852=CARTESIAN_POINT('Ctrl Pts',(1.09347383460968,1.66833525874551,19.8070736487729));
#23853=CARTESIAN_POINT('Ctrl Pts',(1.09347971593568,1.66833140394427,19.8070732029365));
#23854=CARTESIAN_POINT('Ctrl Pts',(1.09349149631307,1.66832368263498,19.8070723099146));
#23855=CARTESIAN_POINT('Ctrl Pts',(1.0934973953828,1.66831981611463,19.8070718627277));
#23856=CARTESIAN_POINT('Ctrl Pts',(1.09350921136434,1.66831207128983,19.8070709669958));
#23857=CARTESIAN_POINT('Ctrl Pts',(1.09351512826697,1.66830819299112,19.8070705184516));
#23858=CARTESIAN_POINT('Ctrl Pts',(1.09352697988898,1.66830042462538,19.807069620007));
#23859=CARTESIAN_POINT('Ctrl Pts',(1.09353291464791,1.66829653453215,19.8070691701036));
#23860=CARTESIAN_POINT('Ctrl Pts',(1.09354480215066,1.66828874246634,19.8070682689279));
#23861=CARTESIAN_POINT('Ctrl Pts',(1.093550754861,1.66828484051543,19.807067817658));
#23862=CARTESIAN_POINT('Ctrl Pts',(1.09356267832501,1.66827702469512,19.807066913745));
#23863=CARTESIAN_POINT('Ctrl Pts',(1.09356864906477,1.66827311083456,19.8070664611028));
#23864=CARTESIAN_POINT('Ctrl Pts',(1.09358060852437,1.66826527123559,19.8070655544498));
#23865=CARTESIAN_POINT('Ctrl Pts',(1.0935865972904,1.66826134546661,19.8070651004354));
#23866=CARTESIAN_POINT('Ctrl Pts',(1.09359859308495,1.66825348186485,19.8070641910165));
#23867=CARTESIAN_POINT('Ctrl Pts',(1.09360460001615,1.66824954409558,19.8070637356194));
#23868=CARTESIAN_POINT('Ctrl Pts',(1.09361663211126,1.66824165651189,19.8070628234371));
#23869=CARTESIAN_POINT('Ctrl Pts',(1.093622657256,1.66823770670976,19.8070623666535));
#23870=CARTESIAN_POINT('Ctrl Pts',(1.09363472582534,1.66822979502859,19.8070614516947));
#23871=CARTESIAN_POINT('Ctrl Pts',(1.09364076925832,1.66822583314379,19.8070609935188));
#23872=CARTESIAN_POINT('Ctrl Pts',(1.09365287435609,1.66821789732792,19.8070600757792));
#23873=CARTESIAN_POINT('Ctrl Pts',(1.09365893608432,1.66821392335499,19.8070596162105));
#23874=CARTESIAN_POINT('Ctrl Pts',(1.09367107797674,1.66820596322817,19.8070586956698));
#23875=CARTESIAN_POINT('Ctrl Pts',(1.09367715808327,1.66820197711181,19.807058234702));
#23876=CARTESIAN_POINT('Ctrl Pts',(1.09368933694926,1.66819399255502,19.8070573113464));
#23877=CARTESIAN_POINT('Ctrl Pts',(1.0936954355811,1.66818999419798,19.8070568489683));
#23878=CARTESIAN_POINT('Ctrl Pts',(1.09370765132625,1.66818198527137,19.8070559228051));
#23879=CARTESIAN_POINT('Ctrl Pts',(1.09371376848406,1.66817797467233,19.8070554590165));
#23880=CARTESIAN_POINT('Ctrl Pts',(1.09372602140024,1.6681699411828,19.8070545300233));
#23881=CARTESIAN_POINT('Ctrl Pts',(1.09373215717773,1.66816591827947,19.8070540648171));
#23882=CARTESIAN_POINT('Ctrl Pts',(1.09374444728044,1.66815786021508,19.8070531329926));
#23883=CARTESIAN_POINT('Ctrl Pts',(1.09375060168012,1.66815382500492,19.8070526663687));
#23884=CARTESIAN_POINT('Ctrl Pts',(1.09376292930712,1.66814574214245,19.8070517316872));
#23885=CARTESIAN_POINT('Ctrl Pts',(1.09376910247076,1.66814169453161,19.8070512636346));
#23886=CARTESIAN_POINT('Ctrl Pts',(1.09378146754851,1.6681335869175,19.8070503261016));
#23887=CARTESIAN_POINT('Ctrl Pts',(1.09378765948411,1.66812952689984,19.8070498566197));
#23888=CARTESIAN_POINT('Ctrl Pts',(1.09380006232053,1.66812139433039,19.8070489162118));
#23889=CARTESIAN_POINT('Ctrl Pts',(1.09380627314936,1.6681173218255,19.8070484452913));
#23890=CARTESIAN_POINT('Ctrl Pts',(1.09381871373432,1.66810916430553,19.8070475020091));
#23891=CARTESIAN_POINT('Ctrl Pts',(1.09382494348527,1.66810507929355,19.8070470296478));
#23892=CARTESIAN_POINT('Ctrl Pts',(1.09383742204899,1.66809689667029,19.8070460834737));
#23893=CARTESIAN_POINT('Ctrl Pts',(1.09384367080592,1.66809279909532,19.8070456096652));
#23894=CARTESIAN_POINT('Ctrl Pts',(1.09385618753842,1.66808459124233,19.8070446605848));
#23895=CARTESIAN_POINT('Ctrl Pts',(1.09386245545394,1.66808048100337,19.8070441853174));
#23896=CARTESIAN_POINT('Ctrl Pts',(1.09387501015858,1.66807224804775,19.8070432333454));
#23897=CARTESIAN_POINT('Ctrl Pts',(1.09388129713543,1.66806812520767,19.8070427566265));
#23898=CARTESIAN_POINT('Ctrl Pts',(1.09389389036947,1.66805986678213,19.8070418017205));
#23899=CARTESIAN_POINT('Ctrl Pts',(1.09390019656389,1.66805573123752,19.8070413235382));
#23900=CARTESIAN_POINT('Ctrl Pts',(1.09391282823227,1.66804744740253,19.8070403657053));
#23901=CARTESIAN_POINT('Ctrl Pts',(1.09391915365422,1.66804329914594,19.8070398860588));
#23902=CARTESIAN_POINT('Ctrl Pts',(1.09796816187908,1.66538789788568,19.8067328542644));
#23903=CARTESIAN_POINT('Ctrl Pts',(1.10200116314678,1.66272197636024,19.8064257534902));
#23904=CARTESIAN_POINT('Ctrl Pts',(1.11115195608395,1.65662514042144,19.805726002304));
#23905=CARTESIAN_POINT('Ctrl Pts',(1.11626360378344,1.65318513507896,19.8053330110232));
#23906=CARTESIAN_POINT('Ctrl Pts',(1.13176342872066,1.64264949576233,19.8041348709326));
#23907=CARTESIAN_POINT('Ctrl Pts',(1.14210033438136,1.6354793299428,19.8033269007101));
#23908=CARTESIAN_POINT('Ctrl Pts',(1.27951916456512,1.5382210272217,19.7924638250715));
#23909=CARTESIAN_POINT('Ctrl Pts',(1.39566344971092,1.43366554211868,19.7818112632814));
#23910=CARTESIAN_POINT('Ctrl Pts',(1.55895069241756,1.24783916483241,19.7645695358436));
#23911=CARTESIAN_POINT('Ctrl Pts',(1.61464019877761,1.17489068577311,19.7581467393732));
#23912=CARTESIAN_POINT('Ctrl Pts',(1.68415777014259,1.06950267054128,19.7495304071077));
#23913=CARTESIAN_POINT('Ctrl Pts',(1.70244608518529,1.04014469324449,19.7471961918098));
#23914=CARTESIAN_POINT('Ctrl Pts',(1.72973041537877,0.993696206687807,19.7436210377723));
#23915=CARTESIAN_POINT('Ctrl Pts',(1.73925674948538,0.976926552352003,19.7423534636509));
#23916=CARTESIAN_POINT('Ctrl Pts',(1.75098119170168,0.955572175605586,19.7407709043396));
#23917=CARTESIAN_POINT('Ctrl Pts',(1.75340662556756,0.951114358672792,19.7404422548359));
#23918=CARTESIAN_POINT('Ctrl Pts',(1.75724830381259,0.943988920647067,19.7399197281302));
#23919=CARTESIAN_POINT('Ctrl Pts',(1.75867552758812,0.941327292984444,19.7397251625747));
#23920=CARTESIAN_POINT('Ctrl Pts',(1.76137208005775,0.936270956357053,19.739356730193));
#23921=CARTESIAN_POINT('Ctrl Pts',(1.76264255735098,0.933876931519931,19.7391827934883));
#23922=CARTESIAN_POINT('Ctrl Pts',(1.76554288860533,0.928384686433786,19.7387849018384));
#23923=CARTESIAN_POINT('Ctrl Pts',(1.76716946692051,0.925284763275979,19.7385611557832));
#23924=CARTESIAN_POINT('Ctrl Pts',(1.77228065763994,0.915481246707695,19.7378561287058));
#23925=CARTESIAN_POINT('Ctrl Pts',(1.77573540232728,0.908762030357327,19.7373766970123));
#23926=CARTESIAN_POINT('Ctrl Pts',(1.83477626388655,0.792309746267034,19.7291299761734));
#23927=CARTESIAN_POINT('Ctrl Pts',(1.8801426111822,0.677666914298953,19.7219575789469));
#23928=CARTESIAN_POINT('Ctrl Pts',(1.94273573170084,0.463489822721087,19.7090039508161));
#23929=CARTESIAN_POINT('Ctrl Pts',(1.96354075558599,0.365446936121691,19.7032307645136));
#23930=CARTESIAN_POINT('Ctrl Pts',(1.98363512103785,0.216253246808749,19.6942783748981));
#23931=CARTESIAN_POINT('Ctrl Pts',(1.98847018085168,0.166010602037781,19.6912372655598));
#23932=CARTESIAN_POINT('Ctrl Pts',(1.99314958321106,0.0854292211807199,
19.6862815434851));
#23933=CARTESIAN_POINT('Ctrl Pts',(1.9942161759429,0.0551824483347266,19.6844039778784));
#23934=CARTESIAN_POINT('Ctrl Pts',(1.99470260121952,0.0162557870631466,
19.6819607743806));
#23935=CARTESIAN_POINT('Ctrl Pts',(1.99475440981777,0.00758673939837224,
19.6814149634779));
#23936=CARTESIAN_POINT('Ctrl Pts',(1.99474681594471,-0.0064097607796518,
19.6805308746529));
#23937=CARTESIAN_POINT('Ctrl Pts',(1.99472258280768,-0.0117371842216121,
19.6801936998861));
#23938=CARTESIAN_POINT('Ctrl Pts',(1.99463556452769,-0.0219088464717725,
19.6795486294732));
#23939=CARTESIAN_POINT('Ctrl Pts',(1.99457647247869,-0.0267530855502447,
19.6792408518053));
#23940=CARTESIAN_POINT('Ctrl Pts',(1.99440082234015,-0.0378406527751516,
19.6785350931934));
#23941=CARTESIAN_POINT('Ctrl Pts',(1.99427259401908,-0.0440837207153039,
19.6781367494784));
#23942=CARTESIAN_POINT('Ctrl Pts',(1.99378702809095,-0.0633237524418409,
19.6769061304251));
#23943=CARTESIAN_POINT('Ctrl Pts',(1.9933319358954,-0.0763176980658115,
19.6760708050093));
#23944=CARTESIAN_POINT('Ctrl Pts',(1.98700944955615,-0.217395919012639,
19.6669541803501));
#23945=CARTESIAN_POINT('Ctrl Pts',(1.96893395600265,-0.344608745056516,
19.6582798602198));
#23946=CARTESIAN_POINT('Ctrl Pts',(1.9024249421722,-0.619439137984203,19.6386786546724));
#23947=CARTESIAN_POINT('Ctrl Pts',(1.84872032789869,-0.764959432134436,
19.6277122284852));
#23948=CARTESIAN_POINT('Ctrl Pts',(1.7705574685612,-0.918956594275065,19.6162668674067));
#23949=CARTESIAN_POINT('Ctrl Pts',(1.76214841711091,-0.934980205399458,
19.6150786590688));
#23950=CARTESIAN_POINT('Ctrl Pts',(1.75115574934955,-0.9552516666789,19.6135810118025));
#23951=CARTESIAN_POINT('Ctrl Pts',(1.74877305555854,-0.959606693709444,
19.6132595949053));
#23952=CARTESIAN_POINT('Ctrl Pts',(1.74492659525316,-0.966575249003801,
19.6127458769035));
#23953=CARTESIAN_POINT('Ctrl Pts',(1.74347317568109,-0.969194418463121,
19.612552926721));
#23954=CARTESIAN_POINT('Ctrl Pts',(1.74069018800519,-0.974183049423307,
19.6121856914928));
#23955=CARTESIAN_POINT('Ctrl Pts',(1.73936169498908,-0.976553039258202,
19.6120113443352));
#23956=CARTESIAN_POINT('Ctrl Pts',(1.73628729209446,-0.982011501101211,
19.611610055672));
#23957=CARTESIAN_POINT('Ctrl Pts',(1.7345379827498,-0.985098033627859,19.6113833354147));
#23958=CARTESIAN_POINT('Ctrl Pts',(1.7298220860889,-0.993367391619987,19.6107763824562));
#23959=CARTESIAN_POINT('Ctrl Pts',(1.72684041544024,-0.998541639609193,
19.6103971009775));
#23960=CARTESIAN_POINT('Ctrl Pts',(1.70493005716401,-1.03617216623934,19.6076417653366));
#23961=CARTESIAN_POINT('Ctrl Pts',(1.6851094953953,-1.06810378153494,19.6053202724379));
#23962=CARTESIAN_POINT('Ctrl Pts',(1.61760687655192,-1.1702914838794,19.597881117897));
#23963=CARTESIAN_POINT('Ctrl Pts',(1.56633846232174,-1.23807124751812,19.5929286551491));
#23964=CARTESIAN_POINT('Ctrl Pts',(1.44511601339076,-1.37870225203595,19.5821473603529));
#23965=CARTESIAN_POINT('Ctrl Pts',(1.37364234597441,-1.44992613011785,19.5763389418498));
#23966=CARTESIAN_POINT('Ctrl Pts',(1.25812265930164,-1.54880173355664,19.5673026416673));
#23967=CARTESIAN_POINT('Ctrl Pts',(1.21787804872935,-1.58064287192584,19.5642126794812));
#23968=CARTESIAN_POINT('Ctrl Pts',(1.1517180177734,-1.62896019463947,19.5591843445321));
#23969=CARTESIAN_POINT('Ctrl Pts',(1.12657123985685,-1.64645157545625,19.5572844344416));
#23970=CARTESIAN_POINT('Ctrl Pts',(1.09377309736181,-1.66816179332454,19.554816078568));
#23971=CARTESIAN_POINT('Ctrl Pts',(1.08648214965273,-1.67291957123913,19.5542679731884));
#23972=CARTESIAN_POINT('Ctrl Pts',(1.07467294820859,-1.68051601791366,19.5533810664996));
#23973=CARTESIAN_POINT('Ctrl Pts',(1.07017398654208,-1.68338458757999,19.5530433813259));
#23974=CARTESIAN_POINT('Ctrl Pts',(1.06156997405131,-1.68882213495668,19.5523979323579));
#23975=CARTESIAN_POINT('Ctrl Pts',(1.0574669654597,-1.69139428567346,19.5520902890578));
#23976=CARTESIAN_POINT('Ctrl Pts',(1.04806534420248,-1.69724052262482,19.5513856831637));
#23977=CARTESIAN_POINT('Ctrl Pts',(1.04276070179288,-1.70050477056073,19.550988361989));
#23978=CARTESIAN_POINT('Ctrl Pts',(1.02640513071954,-1.71046397663756,19.5497639856811));
#23979=CARTESIAN_POINT('Ctrl Pts',(1.01530454588711,-1.71707634477404,19.5489339251251));
#23980=CARTESIAN_POINT('Ctrl Pts',(0.908727680369466,-1.77916696609252,
19.540971996476));
#23981=CARTESIAN_POINT('Ctrl Pts',(0.808880720206796,-1.8267253765563,19.5335533776178));
#23982=CARTESIAN_POINT('Ctrl Pts',(0.544645531775835,-1.92665793510056,
19.5140864951871));
#23983=CARTESIAN_POINT('Ctrl Pts',(0.376465286938706,-1.96644969776647,
19.5018072687979));
#23984=CARTESIAN_POINT('Ctrl Pts',(0.186905103903939,-1.98606011123713,
19.4891718365038));
#23985=CARTESIAN_POINT('Ctrl Pts',(0.168518165702547,-1.98770469921553,
19.487959357438));
#23986=CARTESIAN_POINT('Ctrl Pts',(0.145125675942604,-1.98947005210635,
19.4864356824495));
#23987=CARTESIAN_POINT('Ctrl Pts',(0.140139633368759,-1.98982748863274,
19.4861120040694));
#23988=CARTESIAN_POINT('Ctrl Pts',(0.132156018878052,-1.99036965609028,
19.485595531373));
#23989=CARTESIAN_POINT('Ctrl Pts',(0.129159322958782,-1.99056636432869,
19.4854020757962));
#23990=CARTESIAN_POINT('Ctrl Pts',(0.123452854956208,-1.99092800597406,
19.4850344738957));
#23991=CARTESIAN_POINT('Ctrl Pts',(0.120743223897487,-1.99109417314495,
19.4848602630147));
#23992=CARTESIAN_POINT('Ctrl Pts',(0.114506810000172,-1.99146384154836,
19.4844600726191));
#23993=CARTESIAN_POINT('Ctrl Pts',(0.110979822084166,-1.99166350603977,
19.4842343103695));
#23994=CARTESIAN_POINT('Ctrl Pts',(0.101540914186302,-1.99217269615232,
19.4836315920804));
#23995=CARTESIAN_POINT('Ctrl Pts',(0.0956280593895489,-1.99246527822371,
19.4832555665839));
#23996=CARTESIAN_POINT('Ctrl Pts',(0.0532467157259226,-1.99437331027754,
19.4805708004221));
#23997=CARTESIAN_POINT('Ctrl Pts',(0.016738509186272,-1.99501387047296,
19.478313533195));
#23998=CARTESIAN_POINT('Ctrl Pts',(-0.025042684057217,-1.99459976855038,
19.475772774299));
#23999=CARTESIAN_POINT('Ctrl Pts',(-0.0303157837360414,-1.9945265921917,
19.4754528874787));
#24000=CARTESIAN_POINT('Ctrl Pts',(-0.0562843266006999,-1.99406321050778,
19.4738810893639));
#24001=CARTESIAN_POINT('Ctrl Pts',(-0.0769736919264156,-1.99337179522832,
19.4726399389276));
#24002=CARTESIAN_POINT('Ctrl Pts',(-0.117953404069742,-1.99136330454254,
19.4701972135433));
#24003=CARTESIAN_POINT('Ctrl Pts',(-0.138241716373127,-1.9900578080192,
19.4689954774902));
#24004=CARTESIAN_POINT('Ctrl Pts',(-0.290718815688208,-1.97790322979042,
19.4599988095077));
#24005=CARTESIAN_POINT('Ctrl Pts',(-0.421549135273346,-1.9542047333214,
19.4524539155032));
#24006=CARTESIAN_POINT('Ctrl Pts',(-0.603446190942141,-1.9021252370702,
19.4412558505582));
#24007=CARTESIAN_POINT('Ctrl Pts',(-0.65714014702683,-1.8842488615606,19.437861326509));
#24008=CARTESIAN_POINT('Ctrl Pts',(-0.740710073361018,-1.85241899800003,
19.4323827522007));
#24009=CARTESIAN_POINT('Ctrl Pts',(-0.771125909358189,-1.83996526954877,
19.4303466638326));
#24010=CARTESIAN_POINT('Ctrl Pts',(-0.80938916826633,-1.82318302168074,
19.4277254151994));
#24011=CARTESIAN_POINT('Ctrl Pts',(-0.817535152294955,-1.81954484057154,
19.4271638718119));
#24012=CARTESIAN_POINT('Ctrl Pts',(-0.830557190515278,-1.81362380324245,
19.426260458601));
#24013=CARTESIAN_POINT('Ctrl Pts',(-0.835448948732386,-1.81137560973404,
19.4259197821513));
#24014=CARTESIAN_POINT('Ctrl Pts',(-0.844713972374017,-1.80707200113342,
19.4252720266124));
#24015=CARTESIAN_POINT('Ctrl Pts',(-0.849088994313327,-1.80502044073333,
19.4249650825078));
#24016=CARTESIAN_POINT('Ctrl Pts',(-0.859006929183904,-1.80032562851777,
19.4242668050363));
#24017=CARTESIAN_POINT('Ctrl Pts',(-0.864545156779075,-1.7976726463903,
19.4238751362015));
#24018=CARTESIAN_POINT('Ctrl Pts',(-0.878811447988021,-1.79075747837467,
19.4228616443093));
#24019=CARTESIAN_POINT('Ctrl Pts',(-0.887520708249872,-1.78645707878797,
19.4222384943168));
#24020=CARTESIAN_POINT('Ctrl Pts',(-0.941188485771207,-1.7594680544678,
19.4183706474784));
#24021=CARTESIAN_POINT('Ctrl Pts',(-0.985302229741203,-1.73514908758266,
19.4150689417449));
#24022=CARTESIAN_POINT('Ctrl Pts',(-1.03949759437698,-1.70253889354015,
19.4108517883081));
#24023=CARTESIAN_POINT('Ctrl Pts',(-1.05048459455819,-1.69578183665368,
19.4099882975104));
#24024=CARTESIAN_POINT('Ctrl Pts',(-1.21378403095503,-1.59315591259754,
19.3970262251595));
#24025=CARTESIAN_POINT('Ctrl Pts',(-1.35249488239145,-1.47721307504617,
19.3842306262316));
#24026=CARTESIAN_POINT('Ctrl Pts',(-1.50040696629637,-1.3150556292171,19.3691873195122));
#24027=CARTESIAN_POINT('Ctrl Pts',(-1.52619187384494,-1.28504130596986,
19.3665062562997));
#24028=CARTESIAN_POINT('Ctrl Pts',(-1.5643955915988,-1.23779772350961,19.3624651413257));
#24029=CARTESIAN_POINT('Ctrl Pts',(-1.57745967271579,-1.22110517232585,
19.3610699616955));
#24030=CARTESIAN_POINT('Ctrl Pts',(-1.59341847787732,-1.20003023397758,
19.3593520096872));
#24031=CARTESIAN_POINT('Ctrl Pts',(-1.59656469005466,-1.19584121022814,
19.3590126415179));
#24032=CARTESIAN_POINT('Ctrl Pts',(-1.60152041240154,-1.1891884940077,19.358477069564));
#24033=CARTESIAN_POINT('Ctrl Pts',(-1.60334079786851,-1.18673299095385,
19.3582801175319));
#24034=CARTESIAN_POINT('Ctrl Pts',(-1.6067599080722,-1.1820987534504,19.3579097942538));
#24035=CARTESIAN_POINT('Ctrl Pts',(-1.60835983042557,-1.1799209808587,19.3577363418937));
#24036=CARTESIAN_POINT('Ctrl Pts',(-1.61201908326103,-1.17491882922439,
19.3573392419842));
#24037=CARTESIAN_POINT('Ctrl Pts',(-1.61407541557882,-1.17209228874836,
19.3571158036888));
#24038=CARTESIAN_POINT('Ctrl Pts',(-1.62042168983933,-1.16332061665698,
19.3564252859873));
#24039=CARTESIAN_POINT('Ctrl Pts',(-1.62468635515522,-1.15735714514718,
19.3559599214556));
#24040=CARTESIAN_POINT('Ctrl Pts',(-1.66100861095637,-1.10596969260325,
19.3519835329336));
#24041=CARTESIAN_POINT('Ctrl Pts',(-1.691190436754,-1.05924254363261,19.3485923049423));
#24042=CARTESIAN_POINT('Ctrl Pts',(-1.79926534056818,-0.875498635045534,
19.3358488056662));
#24043=CARTESIAN_POINT('Ctrl Pts',(-1.86277848868227,-0.730695713326674,
19.3269721050195));
#24044=CARTESIAN_POINT('Ctrl Pts',(-1.92526121514925,-0.525056752820484,
19.3142592322411));
#24045=CARTESIAN_POINT('Ctrl Pts',(-1.93955657242489,-0.46950488603592,
19.3108203998264));
#24046=CARTESIAN_POINT('Ctrl Pts',(-1.95831577760277,-0.380956545213267,
19.305276662275));
#24047=CARTESIAN_POINT('Ctrl Pts',(-1.96438137454597,-0.348330573188435,
19.3032211990962));
#24048=CARTESIAN_POINT('Ctrl Pts',(-1.97104627070201,-0.306731612706796,
19.3005782496893));
#24049=CARTESIAN_POINT('Ctrl Pts',(-1.97240280100466,-0.29788398726114,
19.3000148671833));
#24050=CARTESIAN_POINT('Ctrl Pts',(-1.97448073327285,-0.283694291599757,
19.2991091946587));
#24051=CARTESIAN_POINT('Ctrl Pts',(-1.97524011983714,-0.278357836619679,
19.2987681087472));
#24052=CARTESIAN_POINT('Ctrl Pts',(-1.97663906170083,-0.268232958463942,
19.2981200265467));
#24053=CARTESIAN_POINT('Ctrl Pts',(-1.97728287060039,-0.263445154071275,
19.297813167195));
#24054=CARTESIAN_POINT('Ctrl Pts',(-1.97870408228964,-0.252577292333428,
19.2971157030705));
#24055=CARTESIAN_POINT('Ctrl Pts',(-1.97947086238014,-0.246495917763622,
19.2967247658164));
#24056=CARTESIAN_POINT('Ctrl Pts',(-1.9813757684695,-0.230805659066627,
19.2957143956943));
#24057=CARTESIAN_POINT('Ctrl Pts',(-1.98247201927359,-0.221191942553078,
19.2950936494894));
#24058=CARTESIAN_POINT('Ctrl Pts',(-1.98877561114035,-0.162095104333968,
19.2912671989161));
#24059=CARTESIAN_POINT('Ctrl Pts',(-1.99219954051521,-0.112443369334408,
19.2880058791133));
#24060=CARTESIAN_POINT('Ctrl Pts',(-1.99417609289829,-0.049611094148558,
19.2838163002837));
#24061=CARTESIAN_POINT('Ctrl Pts',(-1.99445915274093,-0.0364996679966243,
19.2829386585307));
#24062=CARTESIAN_POINT('Ctrl Pts',(-1.99470984793476,-0.015118232770998,
19.2815019836021));
#24063=CARTESIAN_POINT('Ctrl Pts',(-1.99475537897725,-0.0068493957490642,
19.2809450477984));
#24064=CARTESIAN_POINT('Ctrl Pts',(-1.99461006220623,0.197369450072887,
19.267157738017));
#24065=CARTESIAN_POINT('Ctrl Pts',(-1.96560205707574,0.392193566079999,
19.2531195237202));
#24066=CARTESIAN_POINT('Ctrl Pts',(-1.89853482476783,0.613033893187592,
19.2375520550565));
#24067=CARTESIAN_POINT('Ctrl Pts',(-1.88752055048928,0.646151354663908,
19.2352314493102));
#24068=CARTESIAN_POINT('Ctrl Pts',(-1.87365455818853,0.68445617931814,19.2325771609461));
#24069=CARTESIAN_POINT('Ctrl Pts',(-1.87164272395583,0.689938534037558,
19.2321979911347));
#24070=CARTESIAN_POINT('Ctrl Pts',(-1.86838349219207,0.698700938786822,
19.2315932171183));
#24071=CARTESIAN_POINT('Ctrl Pts',(-1.8671514840325,0.701986618031553,19.2313667246304));
#24072=CARTESIAN_POINT('Ctrl Pts',(-1.86495215544196,0.707805320714476,
19.2309661455131));
#24073=CARTESIAN_POINT('Ctrl Pts',(-1.86398833392307,0.710339640925739,
19.2307918513531));
#24074=CARTESIAN_POINT('Ctrl Pts',(-1.86194163956103,0.715688470714734,
19.2304243744203));
#24075=CARTESIAN_POINT('Ctrl Pts',(-1.86085755392363,0.718502484718369,
19.2302312661074));
#24076=CARTESIAN_POINT('Ctrl Pts',(-1.85793931853889,0.726026583394934,
19.229715498019));
#24077=CARTESIAN_POINT('Ctrl Pts',(-1.85609362545229,0.730732212284432,
19.2293935254134));
#24078=CARTESIAN_POINT('Ctrl Pts',(-1.8472025353795,0.753149175914821,19.2278622921471));
#24079=CARTESIAN_POINT('Ctrl Pts',(-1.83992111112095,0.770766668630898,
19.226666654914));
#24080=CARTESIAN_POINT('Ctrl Pts',(-1.81894526820849,0.819525975530581,
19.2233719970962));
#24081=CARTESIAN_POINT('Ctrl Pts',(-1.80470463389051,0.850427056715048,
19.221300630423));
#24082=CARTESIAN_POINT('Ctrl Pts',(-1.74995615012824,0.961650383299276,
19.213853071179));
#24083=CARTESIAN_POINT('Ctrl Pts',(-1.70481689534721,1.03957662077931,19.2086471321123));
#24084=CARTESIAN_POINT('Ctrl Pts',(-1.57339007178949,1.23474434592281,19.1950011373688));
#24085=CARTESIAN_POINT('Ctrl Pts',(-1.47929198794705,1.3460453583392,19.186554212404));
#24086=CARTESIAN_POINT('Ctrl Pts',(-1.36524161323755,1.45440264437956,19.1768226476289));
#24087=CARTESIAN_POINT('Ctrl Pts',(-1.35646305430518,1.46259347978206,19.1760767531766));
#24088=CARTESIAN_POINT('Ctrl Pts',(-1.33790116351703,1.47960180040547,19.174505696094));
#24089=CARTESIAN_POINT('Ctrl Pts',(-1.32810340846043,1.48840261162717,19.1736798991539));
#24090=CARTESIAN_POINT('Ctrl Pts',(-1.31355887954949,1.50120924355131,19.1724587285113));
#24091=CARTESIAN_POINT('Ctrl Pts',(-1.3088792584224,1.50529107099677,19.1720665288867));
#24092=CARTESIAN_POINT('Ctrl Pts',(-1.30050788916851,1.51252449688049,19.1713661343983));
#24093=CARTESIAN_POINT('Ctrl Pts',(-1.296823537006,1.51568460988363,19.1710582950493));
#24094=CARTESIAN_POINT('Ctrl Pts',(-1.28909763732421,1.52226241448382,19.1704136127561));
#24095=CARTESIAN_POINT('Ctrl Pts',(-1.28505395263735,1.52567752655203,19.1700766673073));
#24096=CARTESIAN_POINT('Ctrl Pts',(-1.27447067911,1.5345437534886,19.1691960107829));
#24097=CARTESIAN_POINT('Ctrl Pts',(-1.26790975353078,1.53996912191667,19.1686512570793));
#24098=CARTESIAN_POINT('Ctrl Pts',(-1.23903347662685,1.56353789934106,19.1662586704155));
#24099=CARTESIAN_POINT('Ctrl Pts',(-1.21636290925108,1.58123870686895,19.1643931900431));
#24100=CARTESIAN_POINT('Ctrl Pts',(-1.15560330552658,1.62659883882741,19.1594240963888));
#24101=CARTESIAN_POINT('Ctrl Pts',(-1.11690611935303,1.6534094807499,19.1562895636654));
#24102=CARTESIAN_POINT('Ctrl Pts',(-0.910374383655349,1.78594059534205,
19.1397166619385));
#24103=CARTESIAN_POINT('Ctrl Pts',(-0.728439497648743,1.86754500433499,
19.1254933413746));
#24104=CARTESIAN_POINT('Ctrl Pts',(-0.506480137557737,1.92964803793909,
19.1099846034438));
#24105=CARTESIAN_POINT('Ctrl Pts',(-0.47527420373088,1.93757023199523,19.1078476939812));
#24106=CARTESIAN_POINT('Ctrl Pts',(-0.438333702445592,1.94600194919867,
19.1053796566277));
#24107=CARTESIAN_POINT('Ctrl Pts',(-0.432773830374164,1.94724596151668,
19.1050098254619));
#24108=CARTESIAN_POINT('Ctrl Pts',(-0.42382216271563,1.94920864873533,19.1044170828593));
#24109=CARTESIAN_POINT('Ctrl Pts',(-0.42043374060486,1.94994232020364,19.104193337312));
#24110=CARTESIAN_POINT('Ctrl Pts',(-0.414397369740995,1.95123286767823,
19.1037958690282));
#24111=CARTESIAN_POINT('Ctrl Pts',(-0.411750185403053,1.95179319322462,
19.1036219500371));
#24112=CARTESIAN_POINT('Ctrl Pts',(-0.40612716640827,1.95297146018727,19.1032533458392));
#24113=CARTESIAN_POINT('Ctrl Pts',(-0.403151066177744,1.95358798566721,
19.1030587425155));
#24114=CARTESIAN_POINT('Ctrl Pts',(-0.395117745364777,1.95523302006747,
19.1025347419746));
#24115=CARTESIAN_POINT('Ctrl Pts',(-0.390057880004449,1.95624871811876,
19.102206070726));
#24116=CARTESIAN_POINT('Ctrl Pts',(-0.365113371823572,1.96115535402875,
19.1005922780309));
#24117=CARTESIAN_POINT('Ctrl Pts',(-0.345173315211025,1.96476297719361,
19.0993226209827));
#24118=CARTESIAN_POINT('Ctrl Pts',(-0.288587915204649,1.97411250321723,
19.0957682478155));
#24119=CARTESIAN_POINT('Ctrl Pts',(-0.251831096599224,1.97913734026269,
19.093516757889));
#24120=CARTESIAN_POINT('Ctrl Pts',(-0.116506031913427,1.99380531516961,
19.0853679186858));
#24121=CARTESIAN_POINT('Ctrl Pts',(-0.0173946315439436,1.99713124639425,
19.0796659123627));
#24122=CARTESIAN_POINT('Ctrl Pts',(0.225767770818578,1.9871807813714,19.0655408954649));
#24123=CARTESIAN_POINT('Ctrl Pts',(0.368886777911649,1.96564813038824,19.0570812090882));
#24124=CARTESIAN_POINT('Ctrl Pts',(0.520827983858679,1.92559871343667,19.0472719488605));
#24125=CARTESIAN_POINT('Ctrl Pts',(0.533203014934197,1.92220881450737,19.0464671995945));
#24126=CARTESIAN_POINT('Ctrl Pts',(0.551518390679827,1.91700120053913,19.0452671519696));
#24127=CARTESIAN_POINT('Ctrl Pts',(0.557484504398185,1.91527469676413,19.0448748203123));
#24128=CARTESIAN_POINT('Ctrl Pts',(0.568085704878433,1.91215313821748,19.0441751081117));
#24129=CARTESIAN_POINT('Ctrl Pts',(0.572723980589902,1.91076901625044,19.0438680865696));
#24130=CARTESIAN_POINT('Ctrl Pts',(0.582473317147373,1.90782099944126,19.0432208720734));
#24131=CARTESIAN_POINT('Ctrl Pts',(0.587583214849239,1.90625341856959,19.0428805604902));
#24132=CARTESIAN_POINT('Ctrl Pts',(0.60103932313367,1.90206619658716,19.0419814980655));
#24133=CARTESIAN_POINT('Ctrl Pts',(0.609374636300733,1.89941218084499,19.0414216227364));
#24134=CARTESIAN_POINT('Ctrl Pts',(0.647214929698922,1.88708887816328,19.0388662349133));
#24135=CARTESIAN_POINT('Ctrl Pts',(0.676507759714877,1.87678679386743,19.0368499753536));
#24136=CARTESIAN_POINT('Ctrl Pts',(0.754442624496422,1.84731603909029,19.0313791154287));
#24137=CARTESIAN_POINT('Ctrl Pts',(0.80258868846046,1.82691292122322,19.027885319443));
#24138=CARTESIAN_POINT('Ctrl Pts',(0.941771155316311,1.76136667329637,19.0174498386052));
#24139=CARTESIAN_POINT('Ctrl Pts',(1.03022058744348,1.71113637966265,19.010371626379));
#24140=CARTESIAN_POINT('Ctrl Pts',(1.2128522065243,1.58810997310483,18.9950090905732));
#24141=CARTESIAN_POINT('Ctrl Pts',(1.30515473629979,1.51316950178545,18.9867505880825));
#24142=CARTESIAN_POINT('Ctrl Pts',(1.39573411221792,1.4251358515359,18.978502861267));
#24143=CARTESIAN_POINT('Ctrl Pts',(1.40118117169572,1.41978069996848,18.9780063288439));
#24144=CARTESIAN_POINT('Ctrl Pts',(1.4090907674789,1.41191470581817,18.9772846979359));
#24145=CARTESIAN_POINT('Ctrl Pts',(1.41157755612636,1.40942851220125,18.9770577251521));
#24146=CARTESIAN_POINT('Ctrl Pts',(1.41597089706986,1.40501293172964,18.9766565988912));
#24147=CARTESIAN_POINT('Ctrl Pts',(1.41788010241651,1.40308621802148,18.9764822359132));
#24148=CARTESIAN_POINT('Ctrl Pts',(1.42190083927048,1.39901202128495,18.9761149410083));
#24149=CARTESIAN_POINT('Ctrl Pts',(1.42401143370464,1.39686365454584,18.9759220822845));
#24150=CARTESIAN_POINT('Ctrl Pts',(1.4296389010258,1.3911094655672,18.9754076875339));
#24151=CARTESIAN_POINT('Ctrl Pts',(1.4331470247017,1.38749505924799,18.9750868322905));
#24152=CARTESIAN_POINT('Ctrl Pts',(1.44973118123455,1.37027846197375,18.9735689235499));
#24153=CARTESIAN_POINT('Ctrl Pts',(1.46262801538567,1.35650393020353,18.97238520801));
#24154=CARTESIAN_POINT('Ctrl Pts',(1.49789735416319,1.31774639711915,18.9691317346888));
#24155=CARTESIAN_POINT('Ctrl Pts',(1.51983908278505,1.29237822784512,18.9670887988578));
#24156=CARTESIAN_POINT('Ctrl Pts',(1.59710989032198,1.19834934614082,18.9597729581381));
#24157=CARTESIAN_POINT('Ctrl Pts',(1.64851391667944,1.1265900598515,18.9546647941645));
#24158=CARTESIAN_POINT('Ctrl Pts',(1.77294945459313,0.926032284283776,18.9409762194831));
#24159=CARTESIAN_POINT('Ctrl Pts',(1.83667716449269,0.792146101301501,18.9323948795123));
#24160=CARTESIAN_POINT('Ctrl Pts',(1.88919017415651,0.64042956496315,18.9224634004611));
#24161=CARTESIAN_POINT('Ctrl Pts',(1.89323776887667,0.628363175833703,18.9216725170902));
#24162=CARTESIAN_POINT('Ctrl Pts',(1.90109239201868,0.604182515390935,18.9200850961987));
#24163=CARTESIAN_POINT('Ctrl Pts',(1.90489976053855,0.592068986955557,18.9192886131363));
#24164=CARTESIAN_POINT('Ctrl Pts',(1.91038918202794,0.574002601069587,18.9180985434496));
#24165=CARTESIAN_POINT('Ctrl Pts',(1.9121596666601,0.568076773546139,18.9177078512868));
#24166=CARTESIAN_POINT('Ctrl Pts',(1.91526573475889,0.557501683026,18.9170099762887));
#24167=CARTESIAN_POINT('Ctrl Pts',(1.91661202436701,0.552855594793642,18.9167031455198));
#24168=CARTESIAN_POINT('Ctrl Pts',(1.91941420156649,0.543051936148847,18.9160552119053));
#24169=CARTESIAN_POINT('Ctrl Pts',(1.92086622844552,0.537893311004489,18.9157139861444));
#24170=CARTESIAN_POINT('Ctrl Pts',(1.92465060806694,0.524237767392702,18.9148099270281));
#24171=CARTESIAN_POINT('Ctrl Pts',(1.9269474594287,0.515731213290482,18.914245946548));
#24172=CARTESIAN_POINT('Ctrl Pts',(1.93724832997663,0.47655154249783,18.9116444239032));
#24173=CARTESIAN_POINT('Ctrl Pts',(1.94457643436697,0.44570703750624,18.909585207267));
#24174=CARTESIAN_POINT('Ctrl Pts',(1.96235091474038,0.362078484325791,18.9039684778908));
#24175=CARTESIAN_POINT('Ctrl Pts',(1.97140123123206,0.309027931035628,18.9003691522594));
#24176=CARTESIAN_POINT('Ctrl Pts',(1.99146903999612,0.15375560306599,18.8897362459326));
#24177=CARTESIAN_POINT('Ctrl Pts',(1.99674440567768,0.0509728397950796,
18.8825669248224));
#24178=CARTESIAN_POINT('Ctrl Pts',(1.99109407008832,-0.166755160266121,
18.8673747184937));
#24179=CARTESIAN_POINT('Ctrl Pts',(1.97816540034085,-0.281302786902861,
18.8593799506066));
#24180=CARTESIAN_POINT('Ctrl Pts',(1.95392706126697,-0.401565012017354,
18.8513683713491));
#24181=CARTESIAN_POINT('Ctrl Pts',(1.95238157855035,-0.409012953193088,
18.8508738493201));
#24182=CARTESIAN_POINT('Ctrl Pts',(1.95004933951711,-0.419937901509884,
18.8501510599525));
#24183=CARTESIAN_POINT('Ctrl Pts',(1.94929582944013,-0.423421819805583,
18.8499209542114));
#24184=CARTESIAN_POINT('Ctrl Pts',(1.94795098143183,-0.429560160825977,
18.8495162374245));
#24185=CARTESIAN_POINT('Ctrl Pts',(1.94736354889718,-0.432215416915608,
18.8493414040255));
#24186=CARTESIAN_POINT('Ctrl Pts',(1.94611946991086,-0.437784757717157,
18.8489751951939));
#24187=CARTESIAN_POINT('Ctrl Pts',(1.94546170880826,-0.440698564899252,
18.8487838850386));
#24188=CARTESIAN_POINT('Ctrl Pts',(1.94370166973369,-0.448414604701606,
18.848278007853));
#24189=CARTESIAN_POINT('Ctrl Pts',(1.94258813162305,-0.453214287904757,
18.8479640825371));
#24190=CARTESIAN_POINT('Ctrl Pts',(1.93738991134168,-0.475249010483119,
18.8465261357435));
#24191=CARTESIAN_POINT('Ctrl Pts',(1.93309341349026,-0.492433952564051,
18.8454138067364));
#24192=CARTESIAN_POINT('Ctrl Pts',(1.92072558088926,-0.539243370099406,
18.8424032870651));
#24193=CARTESIAN_POINT('Ctrl Pts',(1.91219805498775,-0.568743335661869,
18.8405272951433));
#24194=CARTESIAN_POINT('Ctrl Pts',(1.88010699102037,-0.670859298463815,
18.8340705385269));
#24195=CARTESIAN_POINT('Ctrl Pts',(1.85305859298422,-0.742313937661483,
18.8296171210869));
#24196=CARTESIAN_POINT('Ctrl Pts',(1.75497613771495,-0.962380372455703,
18.8156250605066));
#24197=CARTESIAN_POINT('Ctrl Pts',(1.66963537035923,-1.10382417610636,18.8061559707903));
#24198=CARTESIAN_POINT('Ctrl Pts',(1.5550256090783,-1.2495425009449,18.7946822542834));
#24199=CARTESIAN_POINT('Ctrl Pts',(1.54189833058624,-1.26570557138382,18.7933840105735));
#24200=CARTESIAN_POINT('Ctrl Pts',(1.5235118748498,-1.28763345119319,18.7915856821536));
#24201=CARTESIAN_POINT('Ctrl Pts',(1.51846800873429,-1.29357769040101,18.7910943629948));
#24202=CARTESIAN_POINT('Ctrl Pts',(1.51037870863932,-1.3029984951137,18.7903094914647));
#24203=CARTESIAN_POINT('Ctrl Pts',(1.5073557766421,-1.30649434894155,18.7900168684755));
#24204=CARTESIAN_POINT('Ctrl Pts',(1.50112772443305,-1.31364635942377,18.7894153573153));
#24205=CARTESIAN_POINT('Ctrl Pts',(1.49792133310086,-1.31730136333421,18.7891064174451));
#24206=CARTESIAN_POINT('Ctrl Pts',(1.49048178673474,-1.32571950764206,18.7883912799448));
#24207=CARTESIAN_POINT('Ctrl Pts',(1.48623912395737,-1.33047413894105,18.7879846855945));
#24208=CARTESIAN_POINT('Ctrl Pts',(1.47282560273044,-1.34536206819126,18.7867030146092));
#24209=CARTESIAN_POINT('Ctrl Pts',(1.46357349766461,-1.35542131902214,18.7858245100569));
#24210=CARTESIAN_POINT('Ctrl Pts',(1.36899728609609,-1.45615083413938,18.7768980821716));
#24211=CARTESIAN_POINT('Ctrl Pts',(1.27548158567696,-1.53872189519491,18.7684816303936));
#24212=CARTESIAN_POINT('Ctrl Pts',(1.07045483877802,-1.6881520385075,18.7509086163256));
#24213=CARTESIAN_POINT('Ctrl Pts',(0.958860150551927,-1.75394382086196,
18.741778678217));
#24214=CARTESIAN_POINT('Ctrl Pts',(0.802919105054839,-1.82652039212361,
18.7301026545817));
#24215=CARTESIAN_POINT('Ctrl Pts',(0.763580023330528,-1.84331278477983,
18.727244406527));
#24216=CARTESIAN_POINT('Ctrl Pts',(0.717405499615434,-1.8612906676147,18.7240134497637));
#24217=CARTESIAN_POINT('Ctrl Pts',(0.711070091785226,-1.8637201850121,18.7235728061334));
#24218=CARTESIAN_POINT('Ctrl Pts',(0.701510634610369,-1.86733022731593,
18.7229120555581));
#24219=CARTESIAN_POINT('Ctrl Pts',(0.698295813288188,-1.86853480189628,
18.7226905481327));
#24220=CARTESIAN_POINT('Ctrl Pts',(0.692620798080142,-1.87064450500476,
18.7223007845031));
#24221=CARTESIAN_POINT('Ctrl Pts',(0.690161921447034,-1.87155308674783,
18.7221323230139));
#24222=CARTESIAN_POINT('Ctrl Pts',(0.684878408046122,-1.87349357398586,
18.7217712372957));
#24223=CARTESIAN_POINT('Ctrl Pts',(0.682053236102053,-1.87452393662761,
18.7215787059357));
#24224=CARTESIAN_POINT('Ctrl Pts',(0.676223443005217,-1.87663518390325,
18.7211825186632));
#24225=CARTESIAN_POINT('Ctrl Pts',(0.67321853247528,-1.87771525163079,18.7209789113052));
#24226=CARTESIAN_POINT('Ctrl Pts',(0.665659937021267,-1.88041159291514,
18.7204682391235));
#24227=CARTESIAN_POINT('Ctrl Pts',(0.661102918091184,-1.88201855552993,
18.7201617103954));
#24228=CARTESIAN_POINT('Ctrl Pts',(0.648149342013863,-1.88653358048644,
18.7192940971228));
#24229=CARTESIAN_POINT('Ctrl Pts',(0.639739008739433,-1.88940216132828,
18.718735199416));
#24230=CARTESIAN_POINT('Ctrl Pts',(0.553880700907586,-1.91804752617227,
18.7130717745536));
#24231=CARTESIAN_POINT('Ctrl Pts',(0.474929194967297,-1.93910692519503,
18.7082111276932));
#24232=CARTESIAN_POINT('Ctrl Pts',(0.291248040574525,-1.97620449762924,
18.6972312546363));
#24233=CARTESIAN_POINT('Ctrl Pts',(0.186095166723978,-1.98886367971497,
18.6911757432887));
#24234=CARTESIAN_POINT('Ctrl Pts',(-0.0210114533441814,-1.99722154622232,
18.679010748956));
#24235=CARTESIAN_POINT('Ctrl Pts',(-0.122606996735743,-1.99356430198719,
18.6729303255419));
#24236=CARTESIAN_POINT('Ctrl Pts',(-0.23618474553309,-1.98075943428324,
18.665794719991));
#24237=CARTESIAN_POINT('Ctrl Pts',(-0.248880837784266,-1.97920425599955,
18.664992450444));
#24238=CARTESIAN_POINT('Ctrl Pts',(-0.26771037722805,-1.97671373610716,
18.6637953951755));
#24239=CARTESIAN_POINT('Ctrl Pts',(-0.273856005556042,-1.97587168798964,
18.6634035543951));
#24240=CARTESIAN_POINT('Ctrl Pts',(-0.284789085921504,-1.97432169600112,
18.6627043929912));
#24241=CARTESIAN_POINT('Ctrl Pts',(-0.289578098481244,-1.97362496613828,
18.6623974292919));
#24242=CARTESIAN_POINT('Ctrl Pts',(-0.299655081873104,-1.97212144855169,
18.6617500030035));
#24243=CARTESIAN_POINT('Ctrl Pts',(-0.304942430259469,-1.97131080482971,
18.6614094205114));
#24244=CARTESIAN_POINT('Ctrl Pts',(-0.318886241762849,-1.96911553210243,
18.6605088773625));
#24245=CARTESIAN_POINT('Ctrl Pts',(-0.327536872891857,-1.96769510005466,
18.6599477855285));
#24246=CARTESIAN_POINT('Ctrl Pts',(-0.366971436970498,-1.96095270177919,
18.6573788159813));
#24247=CARTESIAN_POINT('Ctrl Pts',(-0.397635637482324,-1.95496528099559,
18.6553499204388));
#24248=CARTESIAN_POINT('Ctrl Pts',(-0.479637898766279,-1.93694465454788,
18.6498362892341));
#24249=CARTESIAN_POINT('Ctrl Pts',(-0.530657549781949,-1.92359269514701,
18.6463116005113));
#24250=CARTESIAN_POINT('Ctrl Pts',(-0.67620728268537,-1.87927075147409,
18.6359874324675));
#24251=CARTESIAN_POINT('Ctrl Pts',(-0.769023283211464,-1.84323491135177,
18.6290610423482));
#24252=CARTESIAN_POINT('Ctrl Pts',(-0.894923591927749,-1.78318391182548,
18.6193291659809));
#24253=CARTESIAN_POINT('Ctrl Pts',(-0.930562084471992,-1.76484770213853,
18.6165354953556));
#24254=CARTESIAN_POINT('Ctrl Pts',(-1.03542380158946,-1.70683570473254,
18.6082354042682));
#24255=CARTESIAN_POINT('Ctrl Pts',(-1.10285314113458,-1.6640639145745,18.602788488158));
#24256=CARTESIAN_POINT('Ctrl Pts',(-1.17385887229917,-1.61280610191208,
18.5970687043649));
#24257=CARTESIAN_POINT('Ctrl Pts',(-1.18014471967242,-1.60821224342719,
18.5965625235583));
#24258=CARTESIAN_POINT('Ctrl Pts',(-1.18925251748062,-1.60147387454476,
18.5958295384597));
#24259=CARTESIAN_POINT('Ctrl Pts',(-1.19209580591436,-1.59935853115591,
18.5956007766812));
#24260=CARTESIAN_POINT('Ctrl Pts',(-1.19706405034536,-1.59564165836322,
18.5952011801115));
#24261=CARTESIAN_POINT('Ctrl Pts',(-1.19919145713552,-1.59404344106643,
18.5950301157123));
#24262=CARTESIAN_POINT('Ctrl Pts',(-1.20364684836035,-1.59068235479456,
18.594671956812));
#24263=CARTESIAN_POINT('Ctrl Pts',(-1.2059741566668,-1.5889186332671,18.5944849241815));
#24264=CARTESIAN_POINT('Ctrl Pts',(-1.21200616676444,-1.58432646221614,
18.5940002828221));
#24265=CARTESIAN_POINT('Ctrl Pts',(-1.21570486977454,-1.58149010677236,
18.5937032260741));
#24266=CARTESIAN_POINT('Ctrl Pts',(-1.22383104042245,-1.57521318743955,
18.5930507531277));
#24267=CARTESIAN_POINT('Ctrl Pts',(-1.22825402925024,-1.57176685382326,
18.5926957312136));
#24268=CARTESIAN_POINT('Ctrl Pts',(-1.24126494099582,-1.56154046616931,
18.5916515147872));
#24269=CARTESIAN_POINT('Ctrl Pts',(-1.24981183389738,-1.55470822767957,
18.5909657428702));
#24270=CARTESIAN_POINT('Ctrl Pts',(-1.2798047220425,-1.53032524696298,18.5885581026482));
#24271=CARTESIAN_POINT('Ctrl Pts',(-1.30094170527475,-1.51239754366509,
18.5868593029022));
#24272=CARTESIAN_POINT('Ctrl Pts',(-1.40677906570725,-1.41876838842703,
18.5783018875312));
#24273=CARTESIAN_POINT('Ctrl Pts',(-1.48528173685675,-1.33636589834739,
18.5717737066171));
#24274=CARTESIAN_POINT('Ctrl Pts',(-1.64618998778756,-1.13565679721318,
18.5568419694347));
#24275=CARTESIAN_POINT('Ctrl Pts',(-1.7236523006194,-1.01423474826733,18.5484201721396));
#24276=CARTESIAN_POINT('Ctrl Pts',(-1.79311044995909,-0.874041015284506,
18.5386532471053));
#24277=CARTESIAN_POINT('Ctrl Pts',(-1.79870524800957,-0.862468666454245,
18.5378470762196));
#24278=CARTESIAN_POINT('Ctrl Pts',(-1.80683884768547,-0.845221611485181,
18.5366453134103));
#24279=CARTESIAN_POINT('Ctrl Pts',(-1.80946366991463,-0.839587648709466,
18.5362527006984));
#24280=CARTESIAN_POINT('Ctrl Pts',(-1.81408594877558,-0.829543951768758,
18.5355526728614));
#24281=CARTESIAN_POINT('Ctrl Pts',(-1.8160937731473,-0.825139020965405,
18.5352456179272));
#24282=CARTESIAN_POINT('Ctrl Pts',(-1.82028369669915,-0.815857444135958,
18.5345985233619));
#24283=CARTESIAN_POINT('Ctrl Pts',(-1.82246227531362,-0.810979259761785,
18.5342583658277));
#24284=CARTESIAN_POINT('Ctrl Pts',(-1.8281518787571,-0.79810062343403,18.5333601454061));
#24285=CARTESIAN_POINT('Ctrl Pts',(-1.83162995298638,-0.790085823327649,
18.5328009618283));
#24286=CARTESIAN_POINT('Ctrl Pts',(-1.84718554666243,-0.753585053916015,
18.5302532637896));
#24287=CARTESIAN_POINT('Ctrl Pts',(-1.85865138710598,-0.724844617589241,
18.5282441547314));
#24288=CARTESIAN_POINT('Ctrl Pts',(-1.88759139078703,-0.647095572828773,
18.52279744819));
#24289=CARTESIAN_POINT('Ctrl Pts',(-1.90382342613669,-0.597653339737001,
18.519321079174));
#24290=CARTESIAN_POINT('Ctrl Pts',(-1.96903110870473,-0.369262700635089,
18.5032132497618));
#24291=CARTESIAN_POINT('Ctrl Pts',(-1.9948202059118,-0.184693437491307,
18.4899526768026));
#24292=CARTESIAN_POINT('Ctrl Pts',(-1.99474985647572,0.000756696823254535,
18.4774220616698));
#24293=CARTESIAN_POINT('',(-1.99474917376081,-0.00181556617865773,17.6790451186048));
#24294=CARTESIAN_POINT('Ctrl Pts',(-1.99474917376081,-0.00181556617865773,
17.6790451186048));
#24295=CARTESIAN_POINT('Ctrl Pts',(-1.9946619313494,-0.0976681603296343,
17.6851684928657));
#24296=CARTESIAN_POINT('Ctrl Pts',(-1.98766217964683,-0.193217564775626,
17.6912918671266));
#24297=CARTESIAN_POINT('Ctrl Pts',(-1.97390131051665,-0.287647664410234,
17.6974152413876));
#24298=CARTESIAN_POINT('Ctrl Pts',(-1.96688300708852,-0.335808800579352,
17.700538278033));
#24299=CARTESIAN_POINT('Ctrl Pts',(-1.95810674035759,-0.383679286233765,
17.7036613146785));
#24300=CARTESIAN_POINT('Ctrl Pts',(-1.94759707343738,-0.431153339356385,
17.706784351324));
#24301=CARTESIAN_POINT('Ctrl Pts',(-1.93260830811386,-0.498860284458797,
17.711238390042));
#24302=CARTESIAN_POINT('Ctrl Pts',(-1.9140549686818,-0.565918774422324,
17.71569242876));
#24303=CARTESIAN_POINT('Ctrl Pts',(-1.89200890460737,-0.631925523607358,
17.7201464674779));
#24304=CARTESIAN_POINT('Ctrl Pts',(-1.86999597919259,-0.697833054392723,
17.7245938110837));
#24305=CARTESIAN_POINT('Ctrl Pts',(-1.84450090312234,-0.762691521591686,
17.7290411546895));
#24306=CARTESIAN_POINT('Ctrl Pts',(-1.81564626477699,-0.826109074941892,
17.7334884982952));
#24307=CARTESIAN_POINT('Ctrl Pts',(-1.78682564308431,-0.889451865515344,
17.73793059894));
#24308=CARTESIAN_POINT('Ctrl Pts',(-1.75465352709317,-0.951356672597149,
17.7423726995848));
#24309=CARTESIAN_POINT('Ctrl Pts',(-1.71930130765783,-1.01144973972317,
17.7468148002296));
#24310=CARTESIAN_POINT('Ctrl Pts',(-1.68397138855911,-1.07150489987627,
17.7512540987776));
#24311=CARTESIAN_POINT('Ctrl Pts',(-1.64546559316361,-1.12975016625242,
17.7556933973256));
#24312=CARTESIAN_POINT('Ctrl Pts',(-1.60400143668215,-1.18583597247748,
17.7601326958736));
#24313=CARTESIAN_POINT('Ctrl Pts',(-1.56254934635505,-1.24190545761819,
17.7645707025767));
#24314=CARTESIAN_POINT('Ctrl Pts',(-1.51814089482739,-1.29581633663531,
17.7690087092798));
#24315=CARTESIAN_POINT('Ctrl Pts',(-1.47103613297335,-1.34724914473411,
17.7734467159828));
#24316=CARTESIAN_POINT('Ctrl Pts',(-1.42392907285789,-1.39868446226157,
17.7778849392181));
#24317=CARTESIAN_POINT('Ctrl Pts',(-1.37412577364437,-1.44764110941488,
17.7823231624534));
#24318=CARTESIAN_POINT('Ctrl Pts',(-1.32192446154567,-1.49383509145661,
17.7867613856887));
#24319=CARTESIAN_POINT('Ctrl Pts',(-1.26966784791765,-1.54007801092443,
17.7912043107318));
#24320=CARTESIAN_POINT('Ctrl Pts',(-1.2150085181826,-1.58355209857006,17.7956472357748));
#24321=CARTESIAN_POINT('Ctrl Pts',(-1.15827850124395,-1.62401307755081,
17.8000901608178));
#24322=CARTESIAN_POINT('Ctrl Pts',(-1.10151536865938,-1.66449767527039,
17.8045356793791));
#24323=CARTESIAN_POINT('Ctrl Pts',(-1.04267955606598,-1.70196540043725,
17.8089811979403));
#24324=CARTESIAN_POINT('Ctrl Pts',(-0.982130486825968,-1.73621636593686,
17.8134267165016));
#24325=CARTESIAN_POINT('Ctrl Pts',(-0.921475757769878,-1.77052710032739,
17.8178799926168));
#24326=CARTESIAN_POINT('Ctrl Pts',(-0.859102242251811,-1.80160965149693,
17.822333268732));
#24327=CARTESIAN_POINT('Ctrl Pts',(-0.795391532281774,-1.82931131108799,
17.8267865448473));
#24328=CARTESIAN_POINT('Ctrl Pts',(-0.7612762792085,-1.84414475318812,17.829171146145));
#24329=CARTESIAN_POINT('Ctrl Pts',(-0.72677791776351,-1.85800963399779,
17.8315557474428));
#24330=CARTESIAN_POINT('Ctrl Pts',(-0.69195671403833,-1.87088841687506,
17.8339403487406));
#24331=CARTESIAN_POINT('Ctrl Pts',(-0.626916495472786,-1.89494384183414,
17.8383943874586));
#24332=CARTESIAN_POINT('Ctrl Pts',(-0.560491567793676,-1.91565124300101,
17.8428484261766));
#24333=CARTESIAN_POINT('Ctrl Pts',(-0.49305989658857,-1.9328526847321,17.8473024648945));
#24334=CARTESIAN_POINT('Ctrl Pts',(-0.425729585662315,-1.95002827002362,
17.8517498085003));
#24335=CARTESIAN_POINT('Ctrl Pts',(-0.357396005222441,-1.9637082355019,
17.8561971521061));
#24336=CARTESIAN_POINT('Ctrl Pts',(-0.288454977126301,-1.97378349589591,
17.8606444957118));
#24337=CARTESIAN_POINT('Ctrl Pts',(-0.219595223415858,-1.98384687859354,
17.8650865963566));
#24338=CARTESIAN_POINT('Ctrl Pts',(-0.150129926427493,-1.99031392594899,
17.8695286970014));
#24339=CARTESIAN_POINT('Ctrl Pts',(-0.0804661177590715,-1.993126379935,
17.8739707976462));
#24340=CARTESIAN_POINT('Ctrl Pts',(-0.0108462533297702,-1.99593705981257,
17.8784100961942));
#24341=CARTESIAN_POINT('Ctrl Pts',(0.0589713863406405,-1.99509769986978,
17.8828493947422));
#24342=CARTESIAN_POINT('Ctrl Pts',(0.128575135381385,-1.99060191828041,
17.8872886932902));
#24343=CARTESIAN_POINT('Ctrl Pts',(0.198158629588811,-1.98610744497268,
17.8917266999933));
#24344=CARTESIAN_POINT('Ctrl Pts',(0.26752786843497,-1.97795869381767,17.8961647066964));
#24345=CARTESIAN_POINT('Ctrl Pts',(0.336273464866386,-1.96620134251982,
17.9006027133994));
#24346=CARTESIAN_POINT('Ctrl Pts',(0.405022415424763,-1.9544434175758,17.9050409366347));
#24347=CARTESIAN_POINT('Ctrl Pts',(0.473147181007539,-1.9390766278222,17.90947915987));
#24348=CARTESIAN_POINT('Ctrl Pts',(0.540247527698153,-1.92019795107589,
17.9139173831053));
#24349=CARTESIAN_POINT('Ctrl Pts',(0.607418959801008,-1.90129927445498,
17.9183603081484));
#24350=CARTESIAN_POINT('Ctrl Pts',(0.673563334683393,-1.87888141784204,
17.9228032331914));
#24351=CARTESIAN_POINT('Ctrl Pts',(0.738295510370425,-1.85309128265903,
17.9272461582344));
#24352=CARTESIAN_POINT('Ctrl Pts',(0.803065472892864,-1.82728609271255,
17.9316916767957));
#24353=CARTESIAN_POINT('Ctrl Pts',(0.866421150631294,-1.79810491091656,
17.9361371953569));
#24354=CARTESIAN_POINT('Ctrl Pts',(0.927999890924212,-1.765741703915,17.9405827139182));
#24355=CARTESIAN_POINT('Ctrl Pts',(0.989686087837908,-1.73332202221381,
17.9450359900334));
#24356=CARTESIAN_POINT('Ctrl Pts',(1.0495887367749,-1.69770948122588,17.9494892661486));
#24357=CARTESIAN_POINT('Ctrl Pts',(1.10737284860007,-1.65914222919054,17.9539425422639));
#24358=CARTESIAN_POINT('Ctrl Pts',(1.13831457879753,-1.63849057479555,17.9563271435617));
#24359=CARTESIAN_POINT('Ctrl Pts',(1.16864940321442,-1.6169924285982,17.9587117448595));
#24360=CARTESIAN_POINT('Ctrl Pts',(1.1983299490112,-1.59468896522263,17.9610963461574));
#24361=CARTESIAN_POINT('Ctrl Pts',(1.25376827334243,-1.55302980420884,17.9655503848754));
#24362=CARTESIAN_POINT('Ctrl Pts',(1.30714141940108,-1.50839377884732,17.9700044235934));
#24363=CARTESIAN_POINT('Ctrl Pts',(1.35811196655997,-1.46101315832083,17.9744584623113));
#24364=CARTESIAN_POINT('Ctrl Pts',(1.40900589706705,-1.41370375822865,17.9789058059171));
#24365=CARTESIAN_POINT('Ctrl Pts',(1.45750404091836,-1.36365828176769,17.9833531495229));
#24366=CARTESIAN_POINT('Ctrl Pts',(1.50330038120899,-1.31115045908428,17.9878004931286));
#24367=CARTESIAN_POINT('Ctrl Pts',(1.54904273232183,-1.25870453772652,17.9922425937734));
#24368=CARTESIAN_POINT('Ctrl Pts',(1.59208928574462,-1.20380240274425,17.9966846944182));
#24369=CARTESIAN_POINT('Ctrl Pts',(1.63217068887368,-1.14675472742937,18.001126795063));
#24370=CARTESIAN_POINT('Ctrl Pts',(1.6722268084761,-1.08974303804079,18.005566093611));
#24371=CARTESIAN_POINT('Ctrl Pts',(1.70932120749868,-1.03058889283162,18.0100053921591));
#24372=CARTESIAN_POINT('Ctrl Pts',(1.74322563959379,-0.969634947783344,
18.0144446907071));
#24373=CARTESIAN_POINT('Ctrl Pts',(1.77712020542982,-0.908698740457763,
18.0188826974101));
#24374=CARTESIAN_POINT('Ctrl Pts',(1.80782640928376,-0.845964200622262,
18.0233207041132));
#24375=CARTESIAN_POINT('Ctrl Pts',(1.83516100802873,-0.781800253972191,
18.0277587108163));
#24376=CARTESIAN_POINT('Ctrl Pts',(1.86249694044043,-0.717633176735796,
18.0321969340516));
#24377=CARTESIAN_POINT('Ctrl Pts',(1.88646075147374,-0.652037005553244,
18.0366351572869));
#24378=CARTESIAN_POINT('Ctrl Pts',(1.90691728457396,-0.585400745039742,
18.0410733805222));
#24379=CARTESIAN_POINT('Ctrl Pts',(1.92739548911345,-0.51869389076208,18.0455163055652));
#24380=CARTESIAN_POINT('Ctrl Pts',(1.94435885565362,-0.450945216831616,
18.0499592306083));
#24381=CARTESIAN_POINT('Ctrl Pts',(1.95772237224233,-0.382558068431269,
18.0544021556513));
#24382=CARTESIAN_POINT('Ctrl Pts',(1.97109368966573,-0.314130999637519,
18.0588476742125));
#24383=CARTESIAN_POINT('Ctrl Pts',(1.98086090600766,-0.245065199434764,
18.0632931927738));
#24384=CARTESIAN_POINT('Ctrl Pts',(1.98699075573615,-0.175770586615263,
18.0677387113351));
#24385=CARTESIAN_POINT('Ctrl Pts',(1.99313130222353,-0.106355052762036,
18.0721919874503));
#24386=CARTESIAN_POINT('Ctrl Pts',(1.99562179424232,-0.0367103984459924,
18.0766452635655));
#24387=CARTESIAN_POINT('Ctrl Pts',(1.99448108963014,0.0327527954193907,
18.0810985396808));
#24388=CARTESIAN_POINT('Ctrl Pts',(1.99387027511332,0.069948338195728,18.0834831409786));
#24389=CARTESIAN_POINT('Ctrl Pts',(1.99221918026625,0.107091921061017,18.0858677422763));
#24390=CARTESIAN_POINT('Ctrl Pts',(1.98953677474741,0.144121422514747,18.0882523435741));
#24391=CARTESIAN_POINT('Ctrl Pts',(1.98452648726271,0.21328637404612,18.0927063822921));
#24392=CARTESIAN_POINT('Ctrl Pts',(1.97589526670082,0.282326721031587,18.0971604210101));
#24393=CARTESIAN_POINT('Ctrl Pts',(1.96365571159974,0.350833021253317,18.1016144597281));
#24394=CARTESIAN_POINT('Ctrl Pts',(1.95143455445166,0.419236345861818,18.1060618033338));
#24395=CARTESIAN_POINT('Ctrl Pts',(1.93561591323597,0.487106738974794,18.1105091469396));
#24396=CARTESIAN_POINT('Ctrl Pts',(1.91626424745491,0.554038713833296,18.1149564905453));
#24397=CARTESIAN_POINT('Ctrl Pts',(1.89693539529866,0.620891782773368,18.1193985911901));
#24398=CARTESIAN_POINT('Ctrl Pts',(1.87408192625443,0.686808162678716,18.1238406918349));
#24399=CARTESIAN_POINT('Ctrl Pts',(1.84781921053907,0.751393191120845,18.1282827924797));
#24400=CARTESIAN_POINT('Ctrl Pts',(1.82157306146113,0.815937479040921,18.1327220910277));
#24401=CARTESIAN_POINT('Ctrl Pts',(1.79192211592647,0.879151629064188,18.1371613895757));
#24402=CARTESIAN_POINT('Ctrl Pts',(1.75903088925285,0.940658223349132,18.1416006881237));
#24403=CARTESIAN_POINT('Ctrl Pts',(1.72614923399345,1.00214691908934,18.1460386948268));
#24404=CARTESIAN_POINT('Ctrl Pts',(1.69002940019957,1.06192861403172,18.1504767015299));
#24405=CARTESIAN_POINT('Ctrl Pts',(1.65088235492533,1.11964950439689,18.1549147082329));
#24406=CARTESIAN_POINT('Ctrl Pts',(1.61173339965005,1.17737321098893,18.1593529314682));
#24407=CARTESIAN_POINT('Ctrl Pts',(1.56955721642649,1.23303550955568,18.1637911547035));
#24408=CARTESIAN_POINT('Ctrl Pts',(1.52460768845155,1.2863121545,18.1682293779388));
#24409=CARTESIAN_POINT('Ctrl Pts',(1.47961054141226,1.33964524017013,18.1726723029819));
#24410=CARTESIAN_POINT('Ctrl Pts',(1.43183450173105,1.39058725285202,18.1771152280249));
#24411=CARTESIAN_POINT('Ctrl Pts',(1.38157265842686,1.43884834224714,18.1815581530679));
#24412=CARTESIAN_POINT('Ctrl Pts',(1.33128147521591,1.4871376036266,18.1860036716292));
#24413=CARTESIAN_POINT('Ctrl Pts',(1.27850197074633,1.53274250665963,18.1904491901904));
#24414=CARTESIAN_POINT('Ctrl Pts',(1.22356077697345,1.57541314820974,18.1948947087517));
#24415=CARTESIAN_POINT('Ctrl Pts',(1.16852370928375,1.61815825122051,18.1993479848669));
#24416=CARTESIAN_POINT('Ctrl Pts',(1.11131782411176,1.65795859201021,18.2038012609821));
#24417=CARTESIAN_POINT('Ctrl Pts',(1.05229853030599,1.6946077320772,18.2082545370974));
#24418=CARTESIAN_POINT('Ctrl Pts',(1.02069539567785,1.71423229267183,18.2106391383952));
#24419=CARTESIAN_POINT('Ctrl Pts',(0.988572726641358,1.73295409804132,18.213023739693));
#24420=CARTESIAN_POINT('Ctrl Pts',(0.955987608594783,1.75074705617723,18.2154083409909));
#24421=CARTESIAN_POINT('Ctrl Pts',(0.895124026266901,1.78398134340042,18.2198623797088));
#24422=CARTESIAN_POINT('Ctrl Pts',(0.832404790085185,1.81410384152131,18.2243164184268));
#24423=CARTESIAN_POINT('Ctrl Pts',(0.768180962672243,1.84090346598836,18.2287704571448));
#24424=CARTESIAN_POINT('Ctrl Pts',(0.704053673650548,1.86766280645589,18.2332178007506));
#24425=CARTESIAN_POINT('Ctrl Pts',(0.638426730301333,1.89110899970459,18.2376651443563));
#24426=CARTESIAN_POINT('Ctrl Pts',(0.571675947805817,1.91107670521105,18.2421124879621));
#24427=CARTESIAN_POINT('Ctrl Pts',(0.505003857621541,1.9310208708452,18.2465545886069));
#24428=CARTESIAN_POINT('Ctrl Pts',(0.437211026452579,1.94749455377516,18.2509966892517));
#24429=CARTESIAN_POINT('Ctrl Pts',(0.36869173250688,1.96038107746455,18.2554387898964));
#24430=CARTESIAN_POINT('Ctrl Pts',(0.300215660835344,1.97325947227772,18.2598780884445));
#24431=CARTESIAN_POINT('Ctrl Pts',(0.231014515470778,1.98255510644078,18.2643173869925));
#24432=CARTESIAN_POINT('Ctrl Pts',(0.16149468384471,1.98820195895435,18.2687566855405));
#24433=CARTESIAN_POINT('Ctrl Pts',(0.0919950826318286,1.99384716822228,
18.2731946922436));
#24434=CARTESIAN_POINT('Ctrl Pts',(0.0221774669620181,1.9958456640726,18.2776326989466));
#24435=CARTESIAN_POINT('Ctrl Pts',(-0.04754647991321,1.9941832650857,18.2820707056497));
#24436=CARTESIAN_POINT('Ctrl Pts',(-0.117273828649554,1.99252078498964,
18.286508928885));
#24437=CARTESIAN_POINT('Ctrl Pts',(-0.186907010153732,1.98719706949691,
18.2909471521203));
#24438=CARTESIAN_POINT('Ctrl Pts',(-0.25603595713023,1.97825002240779,18.2953853753556));
#24439=CARTESIAN_POINT('Ctrl Pts',(-0.325238138597088,1.96929349690966,
18.2998283003986));
#24440=CARTESIAN_POINT('Ctrl Pts',(-0.393934532857344,1.95670604127559,
18.3042712254417));
#24441=CARTESIAN_POINT('Ctrl Pts',(-0.461722764225033,1.94057714391786,
18.3087141504847));
#24442=CARTESIAN_POINT('Ctrl Pts',(-0.529550566373594,1.92443883145886,
18.3131596690459));
#24443=CARTESIAN_POINT('Ctrl Pts',(-0.5964686806551,1.90475510077308,18.3176051876072));
#24444=CARTESIAN_POINT('Ctrl Pts',(-0.662090156717492,1.88166526961567,
18.3220507061684));
#24445=CARTESIAN_POINT('Ctrl Pts',(-0.727826144087432,1.85853514605834,
18.3265039822837));
#24446=CARTESIAN_POINT('Ctrl Pts',(-0.792260523944197,1.83198724373524,
18.3309572583989));
#24447=CARTESIAN_POINT('Ctrl Pts',(-0.855027309003584,1.80220860705915,
18.3354105345142));
#24448=CARTESIAN_POINT('Ctrl Pts',(-0.888637117431817,1.78626300345702,
18.337795135812));
#24449=CARTESIAN_POINT('Ctrl Pts',(-0.921769209696405,1.7693918350193,18.3401797371097));
#24450=CARTESIAN_POINT('Ctrl Pts',(-0.954370742034073,1.75162897020155,
18.3425643384075));
#24451=CARTESIAN_POINT('Ctrl Pts',(-1.01526498352919,1.71845089229238,18.3470183771255));
#24452=CARTESIAN_POINT('Ctrl Pts',(-1.07454763790588,1.68202789996184,18.3514724158435));
#24453=CARTESIAN_POINT('Ctrl Pts',(-1.1318511647767,1.6425408680741,18.3559264545615));
#24454=CARTESIAN_POINT('Ctrl Pts',(-1.18906855554323,1.6031131913305,18.3603737981672));
#24455=CARTESIAN_POINT('Ctrl Pts',(-1.24431232347915,1.56063089177578,18.364821141773));
#24456=CARTESIAN_POINT('Ctrl Pts',(-1.29723998650435,1.51532042153275,18.3692684853788));
#24457=CARTESIAN_POINT('Ctrl Pts',(-1.35010525325527,1.47006336767668,18.3737105860235));
#24458=CARTESIAN_POINT('Ctrl Pts',(-1.40065946801004,1.42198508195742,18.3781526866683));
#24459=CARTESIAN_POINT('Ctrl Pts',(-1.44859106720036,1.37135388668547,18.3825947873131));
#24460=CARTESIAN_POINT('Ctrl Pts',(-1.49649243092557,1.32075462979579,18.3870340858611));
#24461=CARTESIAN_POINT('Ctrl Pts',(-1.54177412516799,1.26760601268498,18.3914733844091));
#24462=CARTESIAN_POINT('Ctrl Pts',(-1.584160619306,1.21221396409217,18.3959126829572));
#24463=CARTESIAN_POINT('Ctrl Pts',(-1.62653477888753,1.15683803469877,18.4003506896602));
#24464=CARTESIAN_POINT('Ctrl Pts',(-1.66601511352324,1.09922035841337,18.4047886963633));
#24465=CARTESIAN_POINT('Ctrl Pts',(-1.70236680988852,1.03969938303819,18.4092267030663));
#24466=CARTESIAN_POINT('Ctrl Pts',(-1.73872027986857,0.980175503609246,
18.4136649263016));
#24467=CARTESIAN_POINT('Ctrl Pts',(-1.77194455539026,0.918748559772755,
18.4181031495369));
#24468=CARTESIAN_POINT('Ctrl Pts',(-1.80184948906721,0.855783840258872,
18.4225413727722));
#24469=CARTESIAN_POINT('Ctrl Pts',(-1.83178610372115,0.792752416573324,
18.4269842978153));
#24470=CARTESIAN_POINT('Ctrl Pts',(-1.8583961473623,0.728180408697531,18.4314272228583));
#24471=CARTESIAN_POINT('Ctrl Pts',(-1.88153700708338,0.662454567103078,
18.4358701479013));
#24472=CARTESIAN_POINT('Ctrl Pts',(-1.90469137507678,0.596690358629536,
18.4403156664626));
#24473=CARTESIAN_POINT('Ctrl Pts',(-1.92437239023596,0.529771445645212,
18.4447611850238));
#24474=CARTESIAN_POINT('Ctrl Pts',(-1.94048768550706,0.462098587852696,
18.4492067035851));
#24475=CARTESIAN_POINT('Ctrl Pts',(-1.95663110241826,0.394307639034258,
18.4536599797003));
#24476=CARTESIAN_POINT('Ctrl Pts',(-1.96919629039305,0.325760600612199,
18.4581132558155));
#24477=CARTESIAN_POINT('Ctrl Pts',(-1.9781423585773,0.256866447209936,18.4625665319308));
#24478=CARTESIAN_POINT('Ctrl Pts',(-1.9829327208299,0.219975609236646,18.4649511332286));
#24479=CARTESIAN_POINT('Ctrl Pts',(-1.98668626629364,0.182985302955157,
18.4673357345265));
#24480=CARTESIAN_POINT('Ctrl Pts',(-1.98940285988789,0.145958293940053,
18.4697203358243));
#24481=CARTESIAN_POINT('Ctrl Pts',(-1.99294386346392,0.0976946259368988,
18.4728285967512));
#24482=CARTESIAN_POINT('Ctrl Pts',(-1.99472877578325,0.0493005479635618,
18.475936857678));
#24483=CARTESIAN_POINT('Ctrl Pts',(-1.9947498118588,0.000866365563832799,
18.4790451186048));
#24484=CARTESIAN_POINT('',(-1.99474923905823,0.00174234801668578,16.07864965537));
#24485=CARTESIAN_POINT('Ctrl Pts',(-1.99474916465594,-0.00182554222757092,
17.6788731275167));
#24486=CARTESIAN_POINT('Ctrl Pts',(-1.99487395459297,0.134530998253091,
17.670963424711));
#24487=CARTESIAN_POINT('Ctrl Pts',(-1.98101782634591,0.27053147043171,17.6630747226269));
#24488=CARTESIAN_POINT('Ctrl Pts',(-1.94710945436344,0.434461068927948,
17.6528395731388));
#24489=CARTESIAN_POINT('Ctrl Pts',(-1.94011125517069,0.46471475362475,17.650921029371));
#24490=CARTESIAN_POINT('Ctrl Pts',(-1.93038367435289,0.502705853059274,
17.6484692026851));
#24491=CARTESIAN_POINT('Ctrl Pts',(-1.92830865321938,0.51060752018063,17.6479569106788));
#24492=CARTESIAN_POINT('Ctrl Pts',(-1.924748354045,0.523833839833939,17.6470953706912));
#24493=CARTESIAN_POINT('Ctrl Pts',(-1.9232893632645,0.529165515045873,17.6467469715466));
#24494=CARTESIAN_POINT('Ctrl Pts',(-1.920371999549,0.539655146275757,17.6460593176069));
#24495=CARTESIAN_POINT('Ctrl Pts',(-1.91891495969128,0.544813426882911,
17.6457201085009));
#24496=CARTESIAN_POINT('Ctrl Pts',(-1.91610356314825,0.554615267053036,
17.6450735025496));
#24497=CARTESIAN_POINT('Ctrl Pts',(-1.91475307020975,0.559259902552393,
17.6447662336324));
#24498=CARTESIAN_POINT('Ctrl Pts',(-1.91163787743441,0.569830163452721,
17.6440649396523));
#24499=CARTESIAN_POINT('Ctrl Pts',(-1.90986250055745,0.575752565920685,
17.6436705680794));
#24500=CARTESIAN_POINT('Ctrl Pts',(-1.90435976063781,0.59380338157505,17.6424640987922));
#24501=CARTESIAN_POINT('Ctrl Pts',(-1.90054424364274,0.60590438147918,17.6416491218866));
#24502=CARTESIAN_POINT('Ctrl Pts',(-1.84952423406113,0.762490573328746,
17.6310212559867));
#24503=CARTESIAN_POINT('Ctrl Pts',(-1.78608076665082,0.90112636964128,17.6206419784212));
#24504=CARTESIAN_POINT('Ctrl Pts',(-1.6759606198772,1.08347319351912,17.6058018110514));
#24505=CARTESIAN_POINT('Ctrl Pts',(-1.64200105005281,1.13427986927447,17.6015290705849));
#24506=CARTESIAN_POINT('Ctrl Pts',(-1.55831260082218,1.24783264721737,17.5917470438183));
#24507=CARTESIAN_POINT('Ctrl Pts',(-1.50702614473421,1.3093126943296,17.5862718391463));
#24508=CARTESIAN_POINT('Ctrl Pts',(-1.44522760426659,1.37493548182497,17.580360339955));
#24509=CARTESIAN_POINT('Ctrl Pts',(-1.43821863299528,1.38226538027678,17.579699067453));
#24510=CARTESIAN_POINT('Ctrl Pts',(-1.4289912435603,1.39176909963981,17.5788407833141));
#24511=CARTESIAN_POINT('Ctrl Pts',(-1.42682338372019,1.39399147517855,17.5786400149043));
#24512=CARTESIAN_POINT('Ctrl Pts',(-1.42255686880042,1.3983449013131,17.5782466172185));
#24513=CARTESIAN_POINT('Ctrl Pts',(-1.42045859245903,1.40047631018831,17.5780539596466));
#24514=CARTESIAN_POINT('Ctrl Pts',(-1.41644414634149,1.40453584217814,17.577686933256));
#24515=CARTESIAN_POINT('Ctrl Pts',(-1.41452885263436,1.40646474424731,17.5775125037478));
#24516=CARTESIAN_POINT('Ctrl Pts',(-1.4100983845802,1.41090848691685,17.5771105636285));
#24517=CARTESIAN_POINT('Ctrl Pts',(-1.40758042355766,1.41342051928855,17.5768832766234));
#24518=CARTESIAN_POINT('Ctrl Pts',(-1.39948007435782,1.42145868192833,17.5761557040853));
#24519=CARTESIAN_POINT('Ctrl Pts',(-1.39387167195694,1.42695866442534,17.5756574400135));
#24520=CARTESIAN_POINT('Ctrl Pts',(-1.31909689409082,1.49942641378923,17.5690840964259));
#24521=CARTESIAN_POINT('Ctrl Pts',(-1.24519239302094,1.56134477679806,17.5633713287119));
#24522=CARTESIAN_POINT('Ctrl Pts',(-1.09137028803074,1.67232089231421,17.552289429932));
#24523=CARTESIAN_POINT('Ctrl Pts',(-1.01190424536467,1.72156796591944,17.546926926072));
#24524=CARTESIAN_POINT('Ctrl Pts',(-0.864738636181897,1.79904835912485,
17.5371847851522));
#24525=CARTESIAN_POINT('Ctrl Pts',(-0.798386657545375,1.82946036537168,
17.5328555983323));
#24526=CARTESIAN_POINT('Ctrl Pts',(-0.706536243996306,1.86560943166117,
17.5268390736166));
#24527=CARTESIAN_POINT('Ctrl Pts',(-0.682370196143658,1.87458337773705,
17.5252542883188));
#24528=CARTESIAN_POINT('Ctrl Pts',(-0.640982683262154,1.88904609805361,
17.5225329154798));
#24529=CARTESIAN_POINT('Ctrl Pts',(-0.623847806683709,1.89477382321997,
17.5214041780342));
#24530=CARTESIAN_POINT('Ctrl Pts',(-0.601396601373318,1.90194110359519,
17.5199216863733));
#24531=CARTESIAN_POINT('Ctrl Pts',(-0.59614841915814,1.90359262843793,17.519574889705));
#24532=CARTESIAN_POINT('Ctrl Pts',(-0.58579112517895,1.90680488219416,17.5188899614425));
#24533=CARTESIAN_POINT('Ctrl Pts',(-0.580682441201451,1.90836684174517,
17.5185518733498));
#24534=CARTESIAN_POINT('Ctrl Pts',(-0.570932421228476,1.91130509569048,
17.5179061223116));
#24535=CARTESIAN_POINT('Ctrl Pts',(-0.56629222205078,1.9126850543119,17.5175985818367));
#24536=CARTESIAN_POINT('Ctrl Pts',(-0.555682341862649,1.91579835549853,
17.5168948701816));
#24537=CARTESIAN_POINT('Ctrl Pts',(-0.549709512588068,1.91752070505459,
17.5164983436752));
#24538=CARTESIAN_POINT('Ctrl Pts',(-0.531357805844762,1.92271988844064,
17.5152788064337));
#24539=CARTESIAN_POINT('Ctrl Pts',(-0.51895347607888,1.9261049203074,17.5144528246592));
#24540=CARTESIAN_POINT('Ctrl Pts',(-0.404234574888088,1.95622207876314,
17.5067972944854));
#24541=CARTESIAN_POINT('Ctrl Pts',(-0.299995801873904,1.97489400501435,
17.4997058203022));
#24542=CARTESIAN_POINT('Ctrl Pts',(-0.0624775108408705,1.99819855041709,
17.483290746562));
#24543=CARTESIAN_POINT('Ctrl Pts',(0.0707869734158899,1.997920917267,17.4738939159684));
#24544=CARTESIAN_POINT('Ctrl Pts',(0.243123709943663,1.98028855865138,17.4620133766614));
#24545=CARTESIAN_POINT('Ctrl Pts',(0.283086946734378,1.97497193298334,17.4592801937768));
#24546=CARTESIAN_POINT('Ctrl Pts',(0.343984641105148,1.96498351243578,17.4551743703625));
#24547=CARTESIAN_POINT('Ctrl Pts',(0.365049075388629,1.96117946707962,17.4537651450919));
#24548=CARTESIAN_POINT('Ctrl Pts',(0.391199455421058,1.95602098801509,17.4520327417419));
#24549=CARTESIAN_POINT('Ctrl Pts',(0.396345722642714,1.95498470304402,17.4516926410067));
#24550=CARTESIAN_POINT('Ctrl Pts',(0.404507720269038,1.95330759764672,17.4511546199647));
#24551=CARTESIAN_POINT('Ctrl Pts',(0.407526113864646,1.95268008993195,17.4509559541228));
#24552=CARTESIAN_POINT('Ctrl Pts',(0.413183155429322,1.95149033329523,17.4505841952418));
#24553=CARTESIAN_POINT('Ctrl Pts',(0.415822087194919,1.95092973548234,17.4504110131692));
#24554=CARTESIAN_POINT('Ctrl Pts',(0.421836151923533,1.9496393889866,17.4500168701501));
#24555=CARTESIAN_POINT('Ctrl Pts',(0.425210525409237,1.9489062306018,17.4497961071131));
#24556=CARTESIAN_POINT('Ctrl Pts',(0.4355326280605,1.94663543763054,17.4491219248841));
#24557=CARTESIAN_POINT('Ctrl Pts',(0.442474142468444,1.94506936484769,17.4486701055179));
#24558=CARTESIAN_POINT('Ctrl Pts',(0.497199082655915,1.93241476572177,17.4451193580921));
#24559=CARTESIAN_POINT('Ctrl Pts',(0.544571677684162,1.91960317864502,17.4421134787008));
#24560=CARTESIAN_POINT('Ctrl Pts',(0.762228981851611,1.85203111125313,17.4284160925313));
#24561=CARTESIAN_POINT('Ctrl Pts',(0.925130804134118,1.7762757317428,17.4184207779021));
#24562=CARTESIAN_POINT('Ctrl Pts',(1.116064141616,1.65400087529898,17.4049080011937));
#24563=CARTESIAN_POINT('Ctrl Pts',(1.15542269983746,1.6267501171322,17.4020181171983));
#24564=CARTESIAN_POINT('Ctrl Pts',(1.21701323180001,1.58074307968851,17.3972935852474));
#24565=CARTESIAN_POINT('Ctrl Pts',(1.23988233875269,1.56286964916456,17.395491904199));
#24566=CARTESIAN_POINT('Ctrl Pts',(1.26876742393338,1.53926132518276,17.3931503896267));
#24567=CARTESIAN_POINT('Ctrl Pts',(1.27514954346977,1.53397843586224,17.3926287898682));
#24568=CARTESIAN_POINT('Ctrl Pts',(1.28562526378452,1.52519646023876,17.3917654928271));
#24569=CARTESIAN_POINT('Ctrl Pts',(1.28973797752693,1.52172024682695,17.3914247306714));
#24570=CARTESIAN_POINT('Ctrl Pts',(1.29751415308781,1.51509337414078,17.3907769069641));
#24571=CARTESIAN_POINT('Ctrl Pts',(1.30118034743469,1.51194596881081,17.3904699808064));
#24572=CARTESIAN_POINT('Ctrl Pts',(1.30947807645864,1.50476988641005,17.3897718745778));
#24573=CARTESIAN_POINT('Ctrl Pts',(1.31410250587305,1.50073310299943,17.3893803596675));
#24574=CARTESIAN_POINT('Ctrl Pts',(1.32599016035539,1.49025898771593,17.3883675248174));
#24575=CARTESIAN_POINT('Ctrl Pts',(1.33322510246685,1.48378993676585,17.38774488081));
#24576=CARTESIAN_POINT('Ctrl Pts',(1.35184711078189,1.46689309459556,17.3861258747288));
#24577=CARTESIAN_POINT('Ctrl Pts',(1.36316065166095,1.45638558677678,17.3851261552643));
#24578=CARTESIAN_POINT('Ctrl Pts',(1.49057017060994,1.33526809529004,17.373680142492));
#24579=CARTESIAN_POINT('Ctrl Pts',(1.59302136640857,1.21119898262068,17.3626082962276));
#24580=CARTESIAN_POINT('Ctrl Pts',(1.72227981449997,1.00948786995335,17.3458928314113));
#24581=CARTESIAN_POINT('Ctrl Pts',(1.76104082694941,0.940239339496951,17.3403617362564));
#24582=CARTESIAN_POINT('Ctrl Pts',(1.8092549393652,0.840600968220298,17.3328304511581));
#24583=CARTESIAN_POINT('Ctrl Pts',(1.82226292602302,0.81201692345694,17.3307168918657));
#24584=CARTESIAN_POINT('Ctrl Pts',(1.8416583609076,0.76658076250785,17.3274431509721));
#24585=CARTESIAN_POINT('Ctrl Pts',(1.84850126083855,0.749929815619094,17.3262611961893));
#24586=CARTESIAN_POINT('Ctrl Pts',(1.85693939906319,0.728579565859989,17.3247702641461));
#24587=CARTESIAN_POINT('Ctrl Pts',(1.85874353850996,0.723964484563416,17.3244494372982));
#24588=CARTESIAN_POINT('Ctrl Pts',(1.86160994577561,0.716550718727087,17.3239364380792));
#24589=CARTESIAN_POINT('Ctrl Pts',(1.86268312895095,0.713756319853589,17.3237436197941));
#24590=CARTESIAN_POINT('Ctrl Pts',(1.8647186077025,0.708420399012569,17.3233764790212));
#24591=CARTESIAN_POINT('Ctrl Pts',(1.86568198801607,0.705879357482266,17.323202095062));
#24592=CARTESIAN_POINT('Ctrl Pts',(1.86789251884577,0.700012653868794,17.3228005141895));
#24593=CARTESIAN_POINT('Ctrl Pts',(1.86913598160927,0.696685625133023,17.3225735395823));
#24594=CARTESIAN_POINT('Ctrl Pts',(1.87245107034768,0.687742959324083,17.3219654606523));
#24595=CARTESIAN_POINT('Ctrl Pts',(1.8745063380064,0.682121235493444,17.3215853130878));
#24596=CARTESIAN_POINT('Ctrl Pts',(1.88937630048065,0.640873007640733,17.3188109393327));
#24597=CARTESIAN_POINT('Ctrl Pts',(1.90120068030406,0.604894570267783,17.3164721232632));
#24598=CARTESIAN_POINT('Ctrl Pts',(1.93611125092309,0.487502755861741,17.3090349507673));
#24599=CARTESIAN_POINT('Ctrl Pts',(1.95504617159904,0.404947620795662,17.3040992794347));
#24600=CARTESIAN_POINT('Ctrl Pts',(1.98491677013169,0.2219993225217,17.2933351849493));
#24601=CARTESIAN_POINT('Ctrl Pts',(1.99359467703481,0.121480170666097,17.2875272621031));
#24602=CARTESIAN_POINT('Ctrl Pts',(1.9951754586604,-0.030546742864486,17.2784921451381));
#24603=CARTESIAN_POINT('Ctrl Pts',(1.99373045716577,-0.0818319821665538,
17.2754028734052));
#24604=CARTESIAN_POINT('Ctrl Pts',(1.9882691649609,-0.163557695667005,17.2703755639381));
#24605=CARTESIAN_POINT('Ctrl Pts',(1.98552399341436,-0.194061084227873,
17.2684759686639));
#24606=CARTESIAN_POINT('Ctrl Pts',(1.9810981674322,-0.233138154838589,17.2660079670331));
#24607=CARTESIAN_POINT('Ctrl Pts',(1.98006185204967,-0.241781733039885,
17.2654598937993));
#24608=CARTESIAN_POINT('Ctrl Pts',(1.97829918292811,-0.255711504780833,
17.2645730265905));
#24609=CARTESIAN_POINT('Ctrl Pts',(1.97760813234482,-0.261002116528721,
17.2642353485687));
#24610=CARTESIAN_POINT('Ctrl Pts',(1.97624940029182,-0.271089139291165,
17.263589904937));
#24611=CARTESIAN_POINT('Ctrl Pts',(1.97558546139651,-0.275886022905429,
17.2632822597861));
#24612=CARTESIAN_POINT('Ctrl Pts',(1.97402761864393,-0.286847208341354,
17.2625776378948));
#24613=CARTESIAN_POINT('Ctrl Pts',(1.97312229944541,-0.293009812256648,
17.2621803025157));
#24614=CARTESIAN_POINT('Ctrl Pts',(1.97025015004233,-0.311943717804821,
17.2609558396116));
#24615=CARTESIAN_POINT('Ctrl Pts',(1.96818810476172,-0.324700027764395,
17.2601257060466));
#24616=CARTESIAN_POINT('Ctrl Pts',(1.94732285168643,-0.446267489545338,
17.2521637323949));
#24617=CARTESIAN_POINT('Ctrl Pts',(1.91964228926552,-0.553341642130039,
17.2447451458188));
#24618=CARTESIAN_POINT('Ctrl Pts',(1.8265155066649,-0.820056361734216,17.2252779390862));
#24619=CARTESIAN_POINT('Ctrl Pts',(1.74898854175703,-0.974521106123854,
17.212998329644));
#24620=CARTESIAN_POINT('Ctrl Pts',(1.64226299508886,-1.13240467184797,17.2003629896625));
#24621=CARTESIAN_POINT('Ctrl Pts',(1.63171652882727,-1.14754926495797,17.1991508671861));
#24622=CARTESIAN_POINT('Ctrl Pts',(1.61804796396616,-1.16660761668881,17.1976275742049));
#24623=CARTESIAN_POINT('Ctrl Pts',(1.61511967513087,-1.17065835380331,17.1973039287264));
#24624=CARTESIAN_POINT('Ctrl Pts',(1.61040769947528,-1.17712515137752,17.1967874961048));
#24625=CARTESIAN_POINT('Ctrl Pts',(1.60863375268652,-1.17954823154703,17.1965940478792));
#24626=CARTESIAN_POINT('Ctrl Pts',(1.60524571220301,-1.18415418590358,17.1962264513651));
#24627=CARTESIAN_POINT('Ctrl Pts',(1.6036326541947,-1.1863377440762,17.1960522385548));
#24628=CARTESIAN_POINT('Ctrl Pts',(1.59991018454899,-1.19135529740016,17.1956520324233));
#24629=CARTESIAN_POINT('Ctrl Pts',(1.59779769967947,-1.1941869847874,17.1954262564242));
#24630=CARTESIAN_POINT('Ctrl Pts',(1.59212477184885,-1.20174927842679,17.1948234774285));
#24631=CARTESIAN_POINT('Ctrl Pts',(1.58855073766808,-1.20646971504061,17.1944474052699));
#24632=CARTESIAN_POINT('Ctrl Pts',(1.562781877784,-1.24019112326695,17.191761637912));
#24633=CARTESIAN_POINT('Ctrl Pts',(1.53981368369376,-1.26859585657837,17.189503459316));
#24634=CARTESIAN_POINT('Ctrl Pts',(1.46672571093517,-1.35407158985838,17.1826648983127));
#24635=CARTESIAN_POINT('Ctrl Pts',(1.41411493503509,-1.40892689903081,17.1782126288713));
#24636=CARTESIAN_POINT('Ctrl Pts',(1.28219160979058,-1.53162405966886,17.1677309272256));
#24637=CARTESIAN_POINT('Ctrl Pts',(1.20044138780058,-1.59650472294606,17.1617414827155));
#24638=CARTESIAN_POINT('Ctrl Pts',(1.0677793481733,-1.68581706743439,17.152270370152));
#24639=CARTESIAN_POINT('Ctrl Pts',(1.02028056041973,-1.71498068526348,17.1489250403128));
#24640=CARTESIAN_POINT('Ctrl Pts',(0.94323528179161,-1.75795094732029,17.1435189131193));
#24641=CARTESIAN_POINT('Ctrl Pts',(0.914462973075244,-1.77308815665554,
17.1415044638148));
#24642=CARTESIAN_POINT('Ctrl Pts',(0.877370034870741,-1.79145984757148,
17.1389074667355));
#24643=CARTESIAN_POINT('Ctrl Pts',(0.86937901241561,-1.79535141189792,17.1383479982075));
#24644=CARTESIAN_POINT('Ctrl Pts',(0.856513166103216,-1.80151093890031,
17.1374471338763));
#24645=CARTESIAN_POINT('Ctrl Pts',(0.851654654282618,-1.8038128549274,17.1371069193846));
#24646=CARTESIAN_POINT('Ctrl Pts',(0.842410439321841,-1.80814700129685,
17.1364595293659));
#24647=CARTESIAN_POINT('Ctrl Pts',(0.838026532360741,-1.8101829899104,17.1361524866121));
#24648=CARTESIAN_POINT('Ctrl Pts',(0.828044589280915,-1.81477480444193,
17.1354532768966));
#24649=CARTESIAN_POINT('Ctrl Pts',(0.822442059805473,-1.81732068978892,
17.1350607710491));
#24650=CARTESIAN_POINT('Ctrl Pts',(0.805385313501111,-1.82497653954453,
17.1338655526949));
#24651=CARTESIAN_POINT('Ctrl Pts',(0.793894774412921,-1.8300043574555,17.1330600389029));
#24652=CARTESIAN_POINT('Ctrl Pts',(0.637986768271091,-1.89647898274159,
17.1221242777255));
#24653=CARTESIAN_POINT('Ctrl Pts',(0.486887043540393,-1.94076798098162,
17.1113867182223));
#24654=CARTESIAN_POINT('Ctrl Pts',(0.242529791646867,-1.98203842136501,
17.0941118802415));
#24655=CARTESIAN_POINT('Ctrl Pts',(0.151929380314377,-1.99103383645298,
17.0877416606701));
#24656=CARTESIAN_POINT('Ctrl Pts',(0.0267245857756098,-1.99486621604645,
17.079194783896));
#24657=CARTESIAN_POINT('Ctrl Pts',(-0.00760291807186951,-1.99503080479141,
17.0768786512938));
#24658=CARTESIAN_POINT('Ctrl Pts',(-0.0610969171456245,-1.99390638240001,
17.0733280452297));
#24659=CARTESIAN_POINT('Ctrl Pts',(-0.0802683271625168,-1.99322666997899,
17.0720673510286));
#24660=CARTESIAN_POINT('Ctrl Pts',(-0.10448702612464,-1.99201799273349,
17.0704921300935));
#24661=CARTESIAN_POINT('Ctrl Pts',(-0.109545337950104,-1.99174622939305,
17.0701640894029));
#24662=CARTESIAN_POINT('Ctrl Pts',(-0.117615670421557,-1.99128180453433,
17.0696423040222));
#24663=CARTESIAN_POINT('Ctrl Pts',(-0.1206283415547,-1.99110157312717,17.0694478743199));
#24664=CARTESIAN_POINT('Ctrl Pts',(-0.126346204418445,-1.99074647998349,
17.0690795453665));
#24665=CARTESIAN_POINT('Ctrl Pts',(-0.129051415203062,-1.99057294346532,
17.0689055768848));
#24666=CARTESIAN_POINT('Ctrl Pts',(-0.135253177172652,-1.99016241101559,
17.0685074119068));
#24667=CARTESIAN_POINT('Ctrl Pts',(-0.138749459774596,-1.98992171504951,
17.0682834252993));
#24668=CARTESIAN_POINT('Ctrl Pts',(-0.149801121824968,-1.98913161237082,
17.0675768802434));
#24669=CARTESIAN_POINT('Ctrl Pts',(-0.157354128014693,-1.98854837261846,
17.0670961824657));
#24670=CARTESIAN_POINT('Ctrl Pts',(-0.286482863122264,-1.97783677806641,
17.0589124133052));
#24671=CARTESIAN_POINT('Ctrl Pts',(-0.406901684643899,-1.95661738195584,
17.0517943432779));
#24672=CARTESIAN_POINT('Ctrl Pts',(-0.621531346165174,-1.89810735803976,
17.0388781698789));
#24673=CARTESIAN_POINT('Ctrl Pts',(-0.716285588654842,-1.8644158780333,
17.033087291115));
#24674=CARTESIAN_POINT('Ctrl Pts',(-0.854615041238981,-1.80312218717505,
17.0240928161145));
#24675=CARTESIAN_POINT('Ctrl Pts',(-0.900325623519345,-1.78073851799526,
17.0210272342319));
#24676=CARTESIAN_POINT('Ctrl Pts',(-0.971940425098654,-1.7422073283255,
17.0160351231518));
#24677=CARTESIAN_POINT('Ctrl Pts',(-0.998417648215627,-1.72717011550998,
17.014146346494));
#24678=CARTESIAN_POINT('Ctrl Pts',(-1.03199354265398,-1.70707128356579,
17.0116905206944));
#24679=CARTESIAN_POINT('Ctrl Pts',(-1.03941845771678,-1.70256051439148,
17.0111435552908));
#24680=CARTESIAN_POINT('Ctrl Pts',(-1.05135203865993,-1.6952034920557,17.0102580486427));
#24681=CARTESIAN_POINT('Ctrl Pts',(-1.05587922910271,-1.69238737921352,
17.009920617077));
#24682=CARTESIAN_POINT('Ctrl Pts',(-1.06449756588004,-1.68697835053265,
17.0092753567829));
#24683=CARTESIAN_POINT('Ctrl Pts',(-1.06859067038259,-1.68438861353955,
17.0089676473002));
#24684=CARTESIAN_POINT('Ctrl Pts',(-1.07793221066091,-1.67843039902162,
17.0082624714675));
#24685=CARTESIAN_POINT('Ctrl Pts',(-1.08317434253265,-1.67505217750344,
17.0078646444645));
#24686=CARTESIAN_POINT('Ctrl Pts',(-1.09926199179173,-1.66457760979476,
17.0066371822756));
#24687=CARTESIAN_POINT('Ctrl Pts',(-1.11005408478666,-1.65740021156439,
17.0058045196354));
#24688=CARTESIAN_POINT('Ctrl Pts',(-1.21483242039514,-1.5862338189017,16.997628101887));
#24689=CARTESIAN_POINT('Ctrl Pts',(-1.30323839566535,-1.51443623268288,
16.9899794504521));
#24690=CARTESIAN_POINT('Ctrl Pts',(-1.50117195367957,-1.32346250925512,
16.9710030059021));
#24691=CARTESIAN_POINT('Ctrl Pts',(-1.60327818044759,-1.19773546977313,
16.9595208354585));
#24692=CARTESIAN_POINT('Ctrl Pts',(-1.70234762257109,-1.04002801779976,
16.9470843822573));
#24693=CARTESIAN_POINT('Ctrl Pts',(-1.71517890682172,-1.01872820959655,
16.9454432824012));
#24694=CARTESIAN_POINT('Ctrl Pts',(-1.73036593826448,-0.9924170944778,16.9434678090384));
#24695=CARTESIAN_POINT('Ctrl Pts',(-1.73310279663216,-0.987629823252238,
16.943110434944));
#24696=CARTESIAN_POINT('Ctrl Pts',(-1.73735586504191,-0.980118298975971,
16.9425529850741));
#24697=CARTESIAN_POINT('Ctrl Pts',(-1.738885573803,-0.977401781935186,16.9423520558596));
#24698=CARTESIAN_POINT('Ctrl Pts',(-1.74172491401848,-0.97233180554543,
16.9419783156686));
#24699=CARTESIAN_POINT('Ctrl Pts',(-1.74303613400936,-0.969979304860729,
16.9418054053613));
#24700=CARTESIAN_POINT('Ctrl Pts',(-1.74599288891186,-0.964649142550532,
16.9414147751311));
#24701=CARTESIAN_POINT('Ctrl Pts',(-1.7476355689051,-0.96166993041941,16.9411972394111));
#24702=CARTESIAN_POINT('Ctrl Pts',(-1.75246201799881,-0.95286333343815,
16.9405565178862));
#24703=CARTESIAN_POINT('Ctrl Pts',(-1.75562435909795,-0.947024165203018,
16.9401346774769));
#24704=CARTESIAN_POINT('Ctrl Pts',(-1.77737473607163,-0.906379360006077,
16.9372182765079));
#24705=CARTESIAN_POINT('Ctrl Pts',(-1.79495710862953,-0.871041893896169,
16.934783657536));
#24706=CARTESIAN_POINT('Ctrl Pts',(-1.8399626010414,-0.773429025800144,
16.9282666564147));
#24707=CARTESIAN_POINT('Ctrl Pts',(-1.86526793285316,-0.710233566745033,
16.9242705175052));
#24708=CARTESIAN_POINT('Ctrl Pts',(-1.91109806899398,-0.576312227966323,
16.9160255300904));
#24709=CARTESIAN_POINT('Ctrl Pts',(-1.93103697188816,-0.505497630126043,
16.9117879118472));
#24710=CARTESIAN_POINT('Ctrl Pts',(-1.97224754543779,-0.320508651458527,
16.9007249439881));
#24711=CARTESIAN_POINT('Ctrl Pts',(-1.98754375892155,-0.205305254166047,
16.8938296732041));
#24712=CARTESIAN_POINT('Ctrl Pts',(-1.99334611033523,-0.0760207855470938,
16.8857561467659));
#24713=CARTESIAN_POINT('Ctrl Pts',(-1.99381268095662,-0.0626007560284189,
16.8849143368068));
#24714=CARTESIAN_POINT('Ctrl Pts',(-1.99429969228872,-0.0428524027725935,
16.8836696537673));
#24715=CARTESIAN_POINT('Ctrl Pts',(-1.99442557588602,-0.0365268646384565,
16.8832700817958));
#24716=CARTESIAN_POINT('Ctrl Pts',(-1.99459487867349,-0.0253458037629439,
16.8825621787351));
#24717=CARTESIAN_POINT('Ctrl Pts',(-1.99465066581256,-0.0204904975402112,
16.88225423738));
#24718=CARTESIAN_POINT('Ctrl Pts',(-1.99473016565131,-0.010348079090638,
16.8816098216231));
#24719=CARTESIAN_POINT('Ctrl Pts',(-1.99475058642307,-0.00506098584367161,
16.8812732465272));
#24720=CARTESIAN_POINT('Ctrl Pts',(-1.99474902518492,0.00871386445208958,
16.8803946168026));
#24721=CARTESIAN_POINT('Ctrl Pts',(-1.99469388920883,0.0172014409270973,
16.8798515284149));
#24722=CARTESIAN_POINT('Ctrl Pts',(-1.99421732835034,0.0542043160928534,
16.8774762172676));
#24723=CARTESIAN_POINT('Ctrl Pts',(-1.99323860307682,0.0827078689679757,
16.8756266602739));
#24724=CARTESIAN_POINT('Ctrl Pts',(-1.98905591326439,0.157635832937072,
16.870709647773));
#24725=CARTESIAN_POINT('Ctrl Pts',(-1.98483815122889,0.203983878561712,
16.8676120683846));
#24726=CARTESIAN_POINT('Ctrl Pts',(-1.95455254570461,0.44359184664207,16.8513090825775));
#24727=CARTESIAN_POINT('Ctrl Pts',(-1.90187537957457,0.632378623373003,
16.8373450918898));
#24728=CARTESIAN_POINT('Ctrl Pts',(-1.80804112401136,0.843391916970157,
16.8217536975807));
#24729=CARTESIAN_POINT('Ctrl Pts',(-1.79253047780147,0.875875286437578,
16.8193585417887));
#24730=CARTESIAN_POINT('Ctrl Pts',(-1.77346527155746,0.913172074935447,
16.8166290083371));
#24731=CARTESIAN_POINT('Ctrl Pts',(-1.77075905014548,0.918408784968108,
16.8162462461532));
#24732=CARTESIAN_POINT('Ctrl Pts',(-1.76639736463288,0.92675797233013,16.8156368505928));
#24733=CARTESIAN_POINT('Ctrl Pts',(-1.76475681977809,0.929878140712621,
16.8154093076938));
#24734=CARTESIAN_POINT('Ctrl Pts',(-1.76183875727002,0.935392495029688,
16.8150075307899));
#24735=CARTESIAN_POINT('Ctrl Pts',(-1.76056461578253,0.937788441167372,
16.814833084945));
#24736=CARTESIAN_POINT('Ctrl Pts',(-1.75786828019294,0.94283387406216,16.8144660005724));
#24737=CARTESIAN_POINT('Ctrl Pts',(-1.75644498695282,0.945482740556031,
16.8142734337706));
#24738=CARTESIAN_POINT('Ctrl Pts',(-1.75263145533975,0.952541708355605,
16.8137606450252));
#24739=CARTESIAN_POINT('Ctrl Pts',(-1.7502305430359,0.956946065326368,16.8134410964274));
#24740=CARTESIAN_POINT('Ctrl Pts',(-1.73882755632265,0.977677814769204,
16.811938613708));
#24741=CARTESIAN_POINT('Ctrl Pts',(-1.72961310970501,0.993888188676363,
16.8107686910807));
#24742=CARTESIAN_POINT('Ctrl Pts',(-1.63309981005563,1.15826919894595,16.7989304673217));
#24743=CARTESIAN_POINT('Ctrl Pts',(-1.52720201954448,1.29471042660096,16.789268721702));
#24744=CARTESIAN_POINT('Ctrl Pts',(-1.32679708232649,1.49358806558945,16.7727534125305));
#24745=CARTESIAN_POINT('Ctrl Pts',(-1.24219968321856,1.56465030482708,16.7661753680787));
#24746=CARTESIAN_POINT('Ctrl Pts',(-1.14162358880379,1.63581480788914,16.7584846795465));
#24747=CARTESIAN_POINT('Ctrl Pts',(-1.13100420926848,1.64317496643819,16.7576743612264));
#24748=CARTESIAN_POINT('Ctrl Pts',(-1.11516086709462,1.65392944152406,16.7564675959102));
#24749=CARTESIAN_POINT('Ctrl Pts',(-1.10999115429502,1.65740338873693,16.7560741647671));
#24750=CARTESIAN_POINT('Ctrl Pts',(-1.10077329405929,1.66353514191372,16.7553732166747));
#24751=CARTESIAN_POINT('Ctrl Pts',(-1.09673156066048,1.6662025376495,16.7550660633818));
#24752=CARTESIAN_POINT('Ctrl Pts',(-1.08821620834786,1.67177795059815,16.7544193126021));
#24753=CARTESIAN_POINT('Ctrl Pts',(-1.08374056044535,1.67468278457462,16.7540795993115));
#24754=CARTESIAN_POINT('Ctrl Pts',(-1.07193160259281,1.68227999977469,16.7531838071098));
#24755=CARTESIAN_POINT('Ctrl Pts',(-1.06457919674939,1.68694234879012,16.75262661843));
#24756=CARTESIAN_POINT('Ctrl Pts',(-1.03122235534646,1.7077898595469,16.7501009625148));
#24757=CARTESIAN_POINT('Ctrl Pts',(-1.00487893758587,1.72342214729797,16.748112334381));
#24758=CARTESIAN_POINT('Ctrl Pts',(-0.933475519307544,1.76359947295092,
16.7427346096397));
#24759=CARTESIAN_POINT('Ctrl Pts',(-0.887813403303553,1.78702161455461,
16.7393079382413));
#24760=CARTESIAN_POINT('Ctrl Pts',(-0.749899513418087,1.85117271657148,
16.7289986718655));
#24761=CARTESIAN_POINT('Ctrl Pts',(-0.655412418530284,1.88669577792285,
16.7219791492113));
#24762=CARTESIAN_POINT('Ctrl Pts',(-0.476956327253535,1.93875809696486,
16.7090092913177));
#24763=CARTESIAN_POINT('Ctrl Pts',(-0.393810818413432,1.95734136191275,
16.7030783286534));
#24764=CARTESIAN_POINT('Ctrl Pts',(-0.272842241311096,1.97635493653421,
16.6948015506274));
#24765=CARTESIAN_POINT('Ctrl Pts',(-0.235798083935167,1.98111620808697,
16.69231423842));
#24766=CARTESIAN_POINT('Ctrl Pts',(-0.192708432024769,1.98542855584353,
16.6894919171655));
#24767=CARTESIAN_POINT('Ctrl Pts',(-0.186774830721642,1.98599553245411,
16.6891048287576));
#24768=CARTESIAN_POINT('Ctrl Pts',(-0.177308823081423,1.98685724372613,
16.688489872511));
#24769=CARTESIAN_POINT('Ctrl Pts',(-0.173778075906166,1.98716916906953,
16.6882610692757));
#24770=CARTESIAN_POINT('Ctrl Pts',(-0.167539948455341,1.98770352599418,
16.6878578496154));
#24771=CARTESIAN_POINT('Ctrl Pts',(-0.164832923342684,1.98792984014027,
16.6876832161804));
#24772=CARTESIAN_POINT('Ctrl Pts',(-0.159138273187571,1.98839421512925,
16.6873165765256));
#24773=CARTESIAN_POINT('Ctrl Pts',(-0.156150578533138,1.98863107233771,
16.6871246388226));
#24774=CARTESIAN_POINT('Ctrl Pts',(-0.148205450236327,1.98924292721306,
16.6866153103506));
#24775=CARTESIAN_POINT('Ctrl Pts',(-0.143247089177238,1.98960612978326,
16.6862985770149));
#24776=CARTESIAN_POINT('Ctrl Pts',(-0.120159096986449,1.99121058022812,
16.6848287729036));
#24777=CARTESIAN_POINT('Ctrl Pts',(-0.102013691133315,1.99222263982331,
16.683688036299));
#24778=CARTESIAN_POINT('Ctrl Pts',(0.0721460156645393,1.99955052407448,
16.6728557317881));
#24779=CARTESIAN_POINT('Ctrl Pts',(0.228403099608374,1.98777619380485,16.6640019459702));
#24780=CARTESIAN_POINT('Ctrl Pts',(0.50590133044061,1.93367590241801,16.6475426380116));
#24781=CARTESIAN_POINT('Ctrl Pts',(0.627493249398118,1.89770493173866,16.6400579838682));
#24782=CARTESIAN_POINT('Ctrl Pts',(0.756922220350272,1.84560712280681,16.6313498888973));
#24783=CARTESIAN_POINT('Ctrl Pts',(0.768945850515908,1.84063010015916,16.6305338378908));
#24784=CARTESIAN_POINT('Ctrl Pts',(0.786667694623885,1.83309042886999,16.62932016135));
#24785=CARTESIAN_POINT('Ctrl Pts',(0.792404115428017,1.8306180100148,16.6289256026702));
#24786=CARTESIAN_POINT('Ctrl Pts',(0.802568954494305,1.82618019614825,16.6282233840759));
#24787=CARTESIAN_POINT('Ctrl Pts',(0.807002023284808,1.82422552587605,16.6279160925957));
#24788=CARTESIAN_POINT('Ctrl Pts',(0.816293690844209,1.82008805920375,16.6272698023845));
#24789=CARTESIAN_POINT('Ctrl Pts',(0.821150749369042,1.81790191673574,16.6269306907076));
#24790=CARTESIAN_POINT('Ctrl Pts',(0.833885483514078,1.8121086148904,16.6260381871712));
#24791=CARTESIAN_POINT('Ctrl Pts',(0.841748447561085,1.80846956813637,16.6254837002685));
#24792=CARTESIAN_POINT('Ctrl Pts',(0.876923885565738,1.79191097582611,16.6229875838446));
#24793=CARTESIAN_POINT('Ctrl Pts',(0.903963184978954,1.77842369529033,16.621026366889));
#24794=CARTESIAN_POINT('Ctrl Pts',(0.975216622861375,1.74083744706297,16.6157405050005));
#24795=CARTESIAN_POINT('Ctrl Pts',(1.01883988620459,1.71567101973835,16.6123798458872));
#24796=CARTESIAN_POINT('Ctrl Pts',(1.14616265451037,1.63564877102358,16.6021953620248));
#24797=CARTESIAN_POINT('Ctrl Pts',(1.22673195346038,1.57612218113352,16.5952343024069));
#24798=CARTESIAN_POINT('Ctrl Pts',(1.39582834956368,1.43034194230574,16.5796569751341));
#24799=CARTESIAN_POINT('Ctrl Pts',(1.48152095304375,1.34138658966505,16.571060734088));
#24800=CARTESIAN_POINT('Ctrl Pts',(1.56317761729671,1.23917730211983,16.5625196994939));
#24801=CARTESIAN_POINT('Ctrl Pts',(1.56786016493216,1.23324740297999,16.5620286009859));
#24802=CARTESIAN_POINT('Ctrl Pts',(1.57466290057864,1.22453116238265,16.5613133745241));
#24803=CARTESIAN_POINT('Ctrl Pts',(1.57680955639181,1.22176570644128,16.5610874183815));
#24804=CARTESIAN_POINT('Ctrl Pts',(1.58060518470355,1.21684927501266,16.56068744916));
#24805=CARTESIAN_POINT('Ctrl Pts',(1.58225706517009,1.2147005754837,16.5605132307513));
#24806=CARTESIAN_POINT('Ctrl Pts',(1.58574039489923,1.210150438276,16.5601455454016));
#24807=CARTESIAN_POINT('Ctrl Pts',(1.58757076632006,1.20774821279019,16.5599521543381));
#24808=CARTESIAN_POINT('Ctrl Pts',(1.59246207078364,1.20129840900599,16.5594348301449));
#24809=CARTESIAN_POINT('Ctrl Pts',(1.59551305137694,1.19724325791056,16.559111591451));
#24810=CARTESIAN_POINT('Ctrl Pts',(1.61008247427344,1.17772399069686,16.5575651093825));
#24811=CARTESIAN_POINT('Ctrl Pts',(1.62139224091025,1.16210440161631,16.5563558200972));
#24812=CARTESIAN_POINT('Ctrl Pts',(1.65234311573005,1.11802736188042,16.5530137822637));
#24813=CARTESIAN_POINT('Ctrl Pts',(1.67147423263653,1.08921859010369,16.5509096621664));
#24814=CARTESIAN_POINT('Ctrl Pts',(1.73855751124592,0.982267155972074,16.5433300297437));
#24815=CARTESIAN_POINT('Ctrl Pts',(1.78185931372507,0.901338251149441,16.5380297012983));
#24816=CARTESIAN_POINT('Ctrl Pts',(1.88329840287108,0.675632396680486,16.5236780642973));
#24817=CARTESIAN_POINT('Ctrl Pts',(1.93028262906167,0.526584949104312,16.5146027167588));
#24818=CARTESIAN_POINT('Ctrl Pts',(1.96180648783979,0.361249165216293,16.5040921799395));
#24819=CARTESIAN_POINT('Ctrl Pts',(1.96404452339453,0.348876416062155,16.5033034114031));
#24820=CARTESIAN_POINT('Ctrl Pts',(1.967204507576,0.330411764749167,16.5021226610736));
#24821=CARTESIAN_POINT('Ctrl Pts',(1.96821547469222,0.324335247407431,16.5017335070935));
#24822=CARTESIAN_POINT('Ctrl Pts',(1.96996957076929,0.313481775671792,16.5010373493372));
#24823=CARTESIAN_POINT('Ctrl Pts',(1.97072351406344,0.308706598372016,16.5007306911271));
#24824=CARTESIAN_POINT('Ctrl Pts',(1.97227870383174,0.298618726014456,16.5000820516492));
#24825=CARTESIAN_POINT('Ctrl Pts',(1.97307585824194,0.293305447965371,16.4997399433618));
#24826=CARTESIAN_POINT('Ctrl Pts',(1.97513249277483,0.279209456726481,16.4988310601912));
#24827=CARTESIAN_POINT('Ctrl Pts',(1.97635484610452,0.270421527989015,16.4982631161582));
#24828=CARTESIAN_POINT('Ctrl Pts',(1.98176037521902,0.229563433203964,16.4956162199731));
#24829=CARTESIAN_POINT('Ctrl Pts',(1.98522162593979,0.197404271554775,16.4935146600132));
#24830=CARTESIAN_POINT('Ctrl Pts',(1.99248029288389,0.110046301160344,16.4877528446617));
#24831=CARTESIAN_POINT('Ctrl Pts',(1.99476539556015,0.0547538797841763,
16.4840480770293));
#24832=CARTESIAN_POINT('Ctrl Pts',(1.99472084027156,-0.10451324661133,16.4732187062672));
#24833=CARTESIAN_POINT('Ctrl Pts',(1.98656541957888,-0.208299905003579,
16.4659593160153));
#24834=CARTESIAN_POINT('Ctrl Pts',(1.95915199036361,-0.381997002730529,
16.4536967920309));
#24835=CARTESIAN_POINT('Ctrl Pts',(1.94410890929081,-0.45237156257599,16.4486997142241));
#24836=CARTESIAN_POINT('Ctrl Pts',(1.92459299505438,-0.524382125772988,
16.4436417649834));
#24837=CARTESIAN_POINT('Ctrl Pts',(1.92388351040222,-0.526979173191117,
16.4434594296823));
#24838=CARTESIAN_POINT('Ctrl Pts',(1.91293774660489,-0.566729084893602,
16.4406699224326));
#24839=CARTESIAN_POINT('Ctrl Pts',(1.90163131762015,-0.603582217110363,
16.4381007443645));
#24840=CARTESIAN_POINT('Ctrl Pts',(1.88714598452739,-0.646336701726393,
16.4351583548678));
#24841=CARTESIAN_POINT('Ctrl Pts',(1.88499767986217,-0.652575550262991,
16.4347299615342));
#24842=CARTESIAN_POINT('Ctrl Pts',(1.88169783505153,-0.662006293164019,
16.4340839862395));
#24843=CARTESIAN_POINT('Ctrl Pts',(1.88056906917945,-0.665206021538717,
16.4338650935147));
#24844=CARTESIAN_POINT('Ctrl Pts',(1.87852991603475,-0.670939763930992,
16.4334733689175));
#24845=CARTESIAN_POINT('Ctrl Pts',(1.87762256133708,-0.673474817428733,
16.4333003598805));
#24846=CARTESIAN_POINT('Ctrl Pts',(1.87565131169209,-0.678947331998111,
16.4329272787143));
#24847=CARTESIAN_POINT('Ctrl Pts',(1.87458565187466,-0.681884122702154,
16.4327273138992));
#24848=CARTESIAN_POINT('Ctrl Pts',(1.87160974587897,-0.690025549173345,
16.4321736212907));
#24849=CARTESIAN_POINT('Ctrl Pts',(1.86968467614099,-0.695224793106826,
16.4318207668955));
#24850=CARTESIAN_POINT('Ctrl Pts',(1.85885457118732,-0.724104483546334,
16.4298645832112));
#24851=CARTESIAN_POINT('Ctrl Pts',(1.84952084996295,-0.747623161211341,
16.428285695259));
#24852=CARTESIAN_POINT('Ctrl Pts',(1.77672383453969,-0.921338842276807,
16.416684432423));
#24853=CARTESIAN_POINT('Ctrl Pts',(1.69549817495256,-1.06344406120452,16.4074958847814));
#24854=CARTESIAN_POINT('Ctrl Pts',(1.53109063619255,-1.28344569354573,16.3914373817416));
#24855=CARTESIAN_POINT('Ctrl Pts',(1.45694606875831,-1.36703117385271,16.3847893560265));
#24856=CARTESIAN_POINT('Ctrl Pts',(1.36684771192279,-1.45290131940669,16.377020310384));
#24857=CARTESIAN_POINT('Ctrl Pts',(1.35739682432387,-1.4617348460928,16.3762090142992));
#24858=CARTESIAN_POINT('Ctrl Pts',(1.34326708546068,-1.47468638448044,16.3750010699312));
#24859=CARTESIAN_POINT('Ctrl Pts',(1.33865364862301,-1.47887551979562,16.3746074461707));
#24860=CARTESIAN_POINT('Ctrl Pts',(1.33042006700895,-1.48628175739307,16.3739062812565));
#24861=CARTESIAN_POINT('Ctrl Pts',(1.32680767682032,-1.48950743707856,16.3735991045751));
#24862=CARTESIAN_POINT('Ctrl Pts',(1.31919196574312,-1.4962581904967,16.3729524335373));
#24863=CARTESIAN_POINT('Ctrl Pts',(1.31518618598601,-1.49978042072497,16.3726128238682));
#24864=CARTESIAN_POINT('Ctrl Pts',(1.3046107003509,-1.50900435832209,16.3717175980776));
#24865=CARTESIAN_POINT('Ctrl Pts',(1.2980177976398,-1.51467918251336,16.3711608747291));
#24866=CARTESIAN_POINT('Ctrl Pts',(1.26852136370655,-1.53973415632697,16.3686759776842));
#24867=CARTESIAN_POINT('Ctrl Pts',(1.24522045446381,-1.55863837338692,16.3667285285644));
#24868=CARTESIAN_POINT('Ctrl Pts',(1.18191512173939,-1.60767275111424,16.361474987186));
#24869=CARTESIAN_POINT('Ctrl Pts',(1.14118962099465,-1.63683248155291,16.3581331919109));
#24870=CARTESIAN_POINT('Ctrl Pts',(0.940859195913623,-1.76915779898231,
16.3418771199799));
#24871=CARTESIAN_POINT('Ctrl Pts',(0.768181440041581,-1.85068066275807,
16.3282787648916));
#24872=CARTESIAN_POINT('Ctrl Pts',(0.552643582820447,-1.91699625236617,
16.3130598137048));
#24873=CARTESIAN_POINT('Ctrl Pts',(0.518414043724896,-1.92653492724311,
16.3106961606288));
#24874=CARTESIAN_POINT('Ctrl Pts',(0.478249379526924,-1.936579347296,16.3079984024909));
#24875=CARTESIAN_POINT('Ctrl Pts',(0.47254691662802,-1.93797870242915,16.3076171472811));
#24876=CARTESIAN_POINT('Ctrl Pts',(0.463417600623498,-1.94017629841859,
16.3070096899712));
#24877=CARTESIAN_POINT('Ctrl Pts',(0.459994724238379,-1.94099067376742,
16.3067825872857));
#24878=CARTESIAN_POINT('Ctrl Pts',(0.453929000806524,-1.94241689228135,
16.3063813128865));
#24879=CARTESIAN_POINT('Ctrl Pts',(0.451287040924777,-1.94303240535023,
16.3062069311387));
#24880=CARTESIAN_POINT('Ctrl Pts',(0.445710351368644,-1.9443196518877,16.3058396847283));
#24881=CARTESIAN_POINT('Ctrl Pts',(0.442775361837196,-1.94499012986654,
16.3056468929308));
#24882=CARTESIAN_POINT('Ctrl Pts',(0.435029168150651,-1.9467412515557,16.3051393265999));
#24883=CARTESIAN_POINT('Ctrl Pts',(0.430215417522592,-1.94781071293563,
16.3048251890987));
#24884=CARTESIAN_POINT('Ctrl Pts',(0.408050631234795,-1.95264884271615,
16.3033844350071));
#24885=CARTESIAN_POINT('Ctrl Pts',(0.390653063184677,-1.9562037362078,16.3022695623201));
#24886=CARTESIAN_POINT('Ctrl Pts',(0.204956648586496,-1.99157131492097,
16.2905171868948));
#24887=CARTESIAN_POINT('Ctrl Pts',(0.0332514037991786,-2.00181830485268,
16.2808883729642));
#24888=CARTESIAN_POINT('Ctrl Pts',(-0.249338889014082,-1.98226811197165,
16.264328044652));
#24889=CARTESIAN_POINT('Ctrl Pts',(-0.360141236352017,-1.96515894840319,
16.2576585183495));
#24890=CARTESIAN_POINT('Ctrl Pts',(-0.481493555491101,-1.93580964672997,
16.2498653864549));
#24891=CARTESIAN_POINT('Ctrl Pts',(-0.494041783208733,-1.93264526911354,
16.2490538005373));
#24892=CARTESIAN_POINT('Ctrl Pts',(-0.5125863130384,-1.92777635594111,16.247845506692));
#24893=CARTESIAN_POINT('Ctrl Pts',(-0.518607017057288,-1.9261654049605,
16.2474518258592));
#24894=CARTESIAN_POINT('Ctrl Pts',(-0.529292625670624,-1.92325254051255,
16.2467505966836));
#24895=CARTESIAN_POINT('Ctrl Pts',(-0.53396054535643,-1.92196179813806,
16.2464434130549));
#24896=CARTESIAN_POINT('Ctrl Pts',(-0.543759189451278,-1.91921388957568,
16.2457967655598));
#24897=CARTESIAN_POINT('Ctrl Pts',(-0.548888855698729,-1.91775312103295,
16.2454571865261));
#24898=CARTESIAN_POINT('Ctrl Pts',(-0.562367154549118,-1.91385641555012,
16.2445621281949));
#24899=CARTESIAN_POINT('Ctrl Pts',(-0.570705750864116,-1.91138644387144,
16.2440055424214));
#24900=CARTESIAN_POINT('Ctrl Pts',(-0.604991665118755,-1.90098626950671,
16.2417051015714));
#24901=CARTESIAN_POINT('Ctrl Pts',(-0.630790990500136,-1.89258191824386,
16.2399458025394));
#24902=CARTESIAN_POINT('Ctrl Pts',(-0.69868726747648,-1.86892163983815,
16.235237989733));
#24903=CARTESIAN_POINT('Ctrl Pts',(-0.740453738240495,-1.85277082832396,
16.2322611246372));
#24904=CARTESIAN_POINT('Ctrl Pts',(-0.909452116101657,-1.78079306677736,
16.2198810089001));
#24905=CARTESIAN_POINT('Ctrl Pts',(-1.03121785739565,-1.71315745230085,
16.2101286245708));
#24906=CARTESIAN_POINT('Ctrl Pts',(-1.22072406736468,-1.5803235492986,16.1940397857979));
#24907=CARTESIAN_POINT('Ctrl Pts',(-1.29271860449864,-1.52199632896768,
16.1876793772745));
#24908=CARTESIAN_POINT('Ctrl Pts',(-1.36615419918655,-1.45351709666854,
16.1811204156262));
#24909=CARTESIAN_POINT('Ctrl Pts',(-1.37186663311428,-1.44812678732777,
16.1806097353838));
#24910=CARTESIAN_POINT('Ctrl Pts',(-1.38011943987973,-1.44024669516089,
16.1798714629457));
#24911=CARTESIAN_POINT('Ctrl Pts',(-1.38268513607195,-1.43778372025244,
16.1796418738949));
#24912=CARTESIAN_POINT('Ctrl Pts',(-1.38720015235866,-1.43342620619791,
16.1792377517232));
#24913=CARTESIAN_POINT('Ctrl Pts',(-1.38915220363405,-1.43153452868563,
16.1790629983688));
#24914=CARTESIAN_POINT('Ctrl Pts',(-1.393244066615,-1.42755296904277,16.1786966220437));
#24915=CARTESIAN_POINT('Ctrl Pts',(-1.39538304170685,-1.42546226740192,
16.1785050656263));
#24916=CARTESIAN_POINT('Ctrl Pts',(-1.39973271281647,-1.42119158962664,
16.1781154329696));
#24917=CARTESIAN_POINT('Ctrl Pts',(-1.40194303892925,-1.41901124649057,
16.1779173861771));
#24918=CARTESIAN_POINT('Ctrl Pts',(-1.41135220939285,-1.40968626725036,
16.1770740501836));
#24919=CARTESIAN_POINT('Ctrl Pts',(-1.41850176033607,-1.40249178154965,
16.1764325710668));
#24920=CARTESIAN_POINT('Ctrl Pts',(-1.47692330683751,-1.34279927855359,
16.171182004695));
#24921=CARTESIAN_POINT('Ctrl Pts',(-1.52532375702421,-1.28755674990014,
16.1667748554819));
#24922=CARTESIAN_POINT('Ctrl Pts',(-1.60653714581684,-1.18383647792672,
16.1590105881081));
#24923=CARTESIAN_POINT('Ctrl Pts',(-1.64046912714042,-1.13635023349188,
16.155627454503));
#24924=CARTESIAN_POINT('Ctrl Pts',(-1.75326817084982,-0.962887791352267,
16.1436270980803));
#24925=CARTESIAN_POINT('Ctrl Pts',(-1.82008480465106,-0.829690516503707,
16.1350066792169));
#24926=CARTESIAN_POINT('Ctrl Pts',(-1.87616581456879,-0.677651586910031,
16.1249820646661));
#24927=CARTESIAN_POINT('Ctrl Pts',(-1.88070923261675,-0.664938046384692,
16.1241428609167));
#24928=CARTESIAN_POINT('Ctrl Pts',(-1.88906350256649,-0.640790054421439,
16.1225465352056));
#24929=CARTESIAN_POINT('Ctrl Pts',(-1.89290047274669,-0.629365236313066,
16.1217903017965));
#24930=CARTESIAN_POINT('Ctrl Pts',(-1.89853488634873,-0.612070682169828,
16.1206437757707));
#24931=CARTESIAN_POINT('Ctrl Pts',(-1.90040919696285,-0.606226127270713,
16.1202560150732));
#24932=CARTESIAN_POINT('Ctrl Pts',(-1.90371075307071,-0.595765287401171,
16.1195614071961));
#24933=CARTESIAN_POINT('Ctrl Pts',(-1.90514826186818,-0.591152271971093,
16.1192548996995));
#24934=CARTESIAN_POINT('Ctrl Pts',(-1.90815252441948,-0.581386712413458,
16.1186055937766));
#24935=CARTESIAN_POINT('Ctrl Pts',(-1.90971519795699,-0.576232962935452,
16.1182626645406));
#24936=CARTESIAN_POINT('Ctrl Pts',(-1.91381341614365,-0.5625171188833,16.1173492931216));
#24937=CARTESIAN_POINT('Ctrl Pts',(-1.91631234757277,-0.553944296014019,
16.1167776611458));
#24938=CARTESIAN_POINT('Ctrl Pts',(-1.92164650677388,-0.535176822822759,
16.1155245166883));
#24939=CARTESIAN_POINT('Ctrl Pts',(-1.92445833166587,-0.524975857713881,
16.1148422612552));
#24940=CARTESIAN_POINT('Ctrl Pts',(-1.9325869588191,-0.494543020349167,
16.1128033552907));
#24941=CARTESIAN_POINT('Ctrl Pts',(-1.93766667681076,-0.474249878078136,
16.1114391585396));
#24942=CARTESIAN_POINT('Ctrl Pts',(-1.97733363940674,-0.304491487802693,
16.0999861661938));
#24943=CARTESIAN_POINT('Ctrl Pts',(-1.99488318252704,-0.151604532131688,
16.0893478098941));
#24944=CARTESIAN_POINT('Ctrl Pts',(-1.99474923905823,0.00174234801668578,
16.07864965537));
#24945=CARTESIAN_POINT('',(-1.99474965194692,-0.00117837076332067,14.4790451186048));
#24946=CARTESIAN_POINT('Ctrl Pts',(-1.9947492380933,0.00174345238502811,
16.0786495783244));
#24947=CARTESIAN_POINT('Ctrl Pts',(-1.9946527896329,0.11209375190194,16.0709510549627));
#24948=CARTESIAN_POINT('Ctrl Pts',(-1.98539954860549,0.222261577203071,
16.0632697882811));
#24949=CARTESIAN_POINT('Ctrl Pts',(-1.9655023144666,0.340467667316,16.0553715701984));
#24950=CARTESIAN_POINT('Ctrl Pts',(-1.96386065344918,0.349812696704146,
16.0547496030639));
#24951=CARTESIAN_POINT('Ctrl Pts',(-1.96129914989705,0.363807178115647,
16.05382221121));
#24952=CARTESIAN_POINT('Ctrl Pts',(-1.96042934144709,0.368465488915019,
16.0535141827204));
#24953=CARTESIAN_POINT('Ctrl Pts',(-1.95895289923287,0.376219418966858,
16.0530026250845));
#24954=CARTESIAN_POINT('Ctrl Pts',(-1.95835551364941,0.379316747734227,
16.0527985926566));
#24955=CARTESIAN_POINT('Ctrl Pts',(-1.95717074648686,0.385382129463518,
16.0523996700488));
#24956=CARTESIAN_POINT('Ctrl Pts',(-1.95658395450499,0.388350287610403,
16.0522047473525));
#24957=CARTESIAN_POINT('Ctrl Pts',(-1.9554589819207,0.393973439400101,16.05183604079));
#24958=CARTESIAN_POINT('Ctrl Pts',(-1.95492215286741,0.396628638958936,
16.051662185347));
#24959=CARTESIAN_POINT('Ctrl Pts',(-1.95368115633524,0.402702977214842,
16.0512650019972));
#24960=CARTESIAN_POINT('Ctrl Pts',(-1.9529734222032,0.406121362524119,16.0510418803883));
#24961=CARTESIAN_POINT('Ctrl Pts',(-1.95107042847056,0.41519288496285,16.0504507838302));
#24962=CARTESIAN_POINT('Ctrl Pts',(-1.94985956284539,0.420842768420181,
16.0500836838035));
#24963=CARTESIAN_POINT('Ctrl Pts',(-1.94141985332776,0.459403865390753,
16.0475848259531));
#24964=CARTESIAN_POINT('Ctrl Pts',(-1.93338214728715,0.492134896974623,
16.0454968477282));
#24965=CARTESIAN_POINT('Ctrl Pts',(-1.90440331593729,0.598435132671208,
16.0387775753409));
#24966=CARTESIAN_POINT('Ctrl Pts',(-1.88005956466325,0.671010158128769,
16.0342867013603));
#24967=CARTESIAN_POINT('Ctrl Pts',(-1.83717276310179,0.778029089459532,
16.0275748916603));
#24968=CARTESIAN_POINT('Ctrl Pts',(-1.82169186239954,0.813616508858517,
16.0253276451676));
#24969=CARTESIAN_POINT('Ctrl Pts',(-1.79087764297408,0.879155964903707,
16.021126216155));
#24970=CARTESIAN_POINT('Ctrl Pts',(-1.77580566660233,0.909215117337312,
16.019173682129));
#24971=CARTESIAN_POINT('Ctrl Pts',(-1.71656009196387,1.02027431471765,16.0118236242065));
#24972=CARTESIAN_POINT('Ctrl Pts',(-1.66754930610852,1.09855121425934,16.0063595150894));
#24973=CARTESIAN_POINT('Ctrl Pts',(-1.59534772278531,1.19784189395358,15.9988244739383));
#24974=CARTESIAN_POINT('Ctrl Pts',(-1.5768296120453,1.22211610589529,15.9969308793983));
#24975=CARTESIAN_POINT('Ctrl Pts',(-1.55228919322179,1.25279791189754,15.9944654766801));
#24976=CARTESIAN_POINT('Ctrl Pts',(-1.54677090018576,1.25960474984806,15.9939138364973));
#24977=CARTESIAN_POINT('Ctrl Pts',(-1.53781261269245,1.2705071960211,15.993022588298));
#24978=CARTESIAN_POINT('Ctrl Pts',(-1.534400640192,1.27462576522166,15.992684116532));
#24979=CARTESIAN_POINT('Ctrl Pts',(-1.52786973029459,1.28244495861365,15.9920380752596));
#24980=CARTESIAN_POINT('Ctrl Pts',(-1.5247538032281,1.28614805659659,15.9917306300986));
#24981=CARTESIAN_POINT('Ctrl Pts',(-1.51761242078122,1.29457274822584,15.9910277573812));
#24982=CARTESIAN_POINT('Ctrl Pts',(-1.51357836523474,1.29928695483865,15.9906319775548));
#24983=CARTESIAN_POINT('Ctrl Pts',(-1.50115565219921,1.31366779802462,15.98941697728));
#24984=CARTESIAN_POINT('Ctrl Pts',(-1.49269602799819,1.32327243264591,15.9885948178463));
#24985=CARTESIAN_POINT('Ctrl Pts',(-1.38641376929217,1.44162392391303,15.9783282797106));
#24986=CARTESIAN_POINT('Ctrl Pts',(-1.27703009480913,1.53935057847327,15.9683627390451));
#24987=CARTESIAN_POINT('Ctrl Pts',(-1.0719773452698,1.68554050706017,15.9508342938042));
#24988=CARTESIAN_POINT('Ctrl Pts',(-0.981243680039204,1.73992661279771,
15.9434139653585));
#24989=CARTESIAN_POINT('Ctrl Pts',(-0.858568647998133,1.80079665636824,
15.9340969595623));
#24990=CARTESIAN_POINT('Ctrl Pts',(-0.830183715831587,1.81405731706274,
15.9319885889391));
#24991=CARTESIAN_POINT('Ctrl Pts',(-0.785101274697649,1.83383862768064,
15.9287263239504));
#24992=CARTESIAN_POINT('Ctrl Pts',(-0.768609077783679,1.84081184928874,
15.9275506864571));
#24993=CARTESIAN_POINT('Ctrl Pts',(-0.747450918990749,1.84942398324726,
15.9260670172339));
#24994=CARTESIAN_POINT('Ctrl Pts',(-0.74287034719889,1.85126864464043,15.9257472721007));
#24995=CARTESIAN_POINT('Ctrl Pts',(-0.735484679104377,1.85421113206303,
15.92523411598));
#24996=CARTESIAN_POINT('Ctrl Pts',(-0.732683900219955,1.8553196323324,15.9250400712032));
#24997=CARTESIAN_POINT('Ctrl Pts',(-0.727356374601661,1.85741423044616,
15.9246720326447));
#24998=CARTESIAN_POINT('Ctrl Pts',(-0.72483015885912,1.85840150667947,15.924497971473));
#24999=CARTESIAN_POINT('Ctrl Pts',(-0.719025013418015,1.86065659134515,
15.9240990200988));
#25000=CARTESIAN_POINT('Ctrl Pts',(-0.715744743324225,1.86192088545769,
15.9238743426542));
#25001=CARTESIAN_POINT('Ctrl Pts',(-0.706986211038732,1.86527006555698,
15.9232764076172));
#25002=CARTESIAN_POINT('Ctrl Pts',(-0.701502021424044,1.86733950744365,
15.922904057475));
#25003=CARTESIAN_POINT('Ctrl Pts',(-0.662903884023204,1.88171035290446,
15.9202972708386));
#25004=CARTESIAN_POINT('Ctrl Pts',(-0.629474994211099,1.89315530668457,
15.9181110025674));
#25005=CARTESIAN_POINT('Ctrl Pts',(-0.553101616402828,1.91705604216219,
15.9132389124869));
#25006=CARTESIAN_POINT('Ctrl Pts',(-0.510006666211071,1.92896836226965,
15.9105756461925));
#25007=CARTESIAN_POINT('Ctrl Pts',(-0.318539430504791,1.97502750518257,
15.8989755521283));
#25008=CARTESIAN_POINT('Ctrl Pts',(-0.166947111196137,1.99357250333605,
15.8903578065403));
#25009=CARTESIAN_POINT('Ctrl Pts',(0.0308947069436403,1.99503224802059,
15.8785432503216));
#25010=CARTESIAN_POINT('Ctrl Pts',(0.076502358957742,1.99380417752586,15.8757843444004));
#25011=CARTESIAN_POINT('Ctrl Pts',(0.149566215485059,1.9893262291711,15.8712818122131));
#25012=CARTESIAN_POINT('Ctrl Pts',(0.177067746360322,1.98706713395893,15.8695682414089));
#25013=CARTESIAN_POINT('Ctrl Pts',(0.213168027956534,1.98334633067129,15.8672907144756));
#25014=CARTESIAN_POINT('Ctrl Pts',(0.221817456240314,1.98239761091768,15.8667429017418));
#25015=CARTESIAN_POINT('Ctrl Pts',(0.235759212858958,1.98077601320342,15.8658563544656));
#25016=CARTESIAN_POINT('Ctrl Pts',(0.241055597976108,1.98013843422936,15.8655187343998));
#25017=CARTESIAN_POINT('Ctrl Pts',(0.251155104954563,1.97888153486538,15.8648733339777));
#25018=CARTESIAN_POINT('Ctrl Pts',(0.255958660534206,1.97826595259428,15.8645656737954));
#25019=CARTESIAN_POINT('Ctrl Pts',(0.266936986544989,1.97681841037125,15.8638609221095));
#25020=CARTESIAN_POINT('Ctrl Pts',(0.273110172181634,1.97597500357755,15.863463471495));
#25021=CARTESIAN_POINT('Ctrl Pts',(0.292082868441552,1.97329226695444,15.8622383059418));
#25022=CARTESIAN_POINT('Ctrl Pts',(0.30486832411298,1.97135741678673,15.8614075799533));
#25023=CARTESIAN_POINT('Ctrl Pts',(0.427356031565815,1.95160102150611,15.8533986795703));
#25024=CARTESIAN_POINT('Ctrl Pts',(0.535387807585934,1.92476804107169,15.8459298438467));
#25025=CARTESIAN_POINT('Ctrl Pts',(0.803614244301825,1.83380972905258,15.8264073746937));
#25026=CARTESIAN_POINT('Ctrl Pts',(0.958776542691533,1.75766969616028,15.8141277909881));
#25027=CARTESIAN_POINT('Ctrl Pts',(1.11705388713816,1.65273535286599,15.8015462129111));
#25028=CARTESIAN_POINT('Ctrl Pts',(1.1317379193471,1.64271509069432,15.8003791619288));
#25029=CARTESIAN_POINT('Ctrl Pts',(1.15031234244297,1.62967275051754,15.7989051495937));
#25030=CARTESIAN_POINT('Ctrl Pts',(1.15432761621008,1.62683112665772,15.7985866448457));
#25031=CARTESIAN_POINT('Ctrl Pts',(1.16078112047955,1.62222803568393,15.7980750051395));
#25032=CARTESIAN_POINT('Ctrl Pts',(1.16322591832389,1.62047587845511,15.7978812429672));
#25033=CARTESIAN_POINT('Ctrl Pts',(1.16786870923725,1.61713252498481,15.7975134150538));
#25034=CARTESIAN_POINT('Ctrl Pts',(1.17006739149406,1.61554239338464,15.7973392832791));
#25035=CARTESIAN_POINT('Ctrl Pts',(1.17511379968564,1.61187702262572,15.7969397430485));
#25036=CARTESIAN_POINT('Ctrl Pts',(1.1779592742476,1.60979872249933,15.7967145494943));
#25037=CARTESIAN_POINT('Ctrl Pts',(1.18698659570309,1.60316852465207,15.7960003584327));
#25038=CARTESIAN_POINT('Ctrl Pts',(1.19314777312266,1.59858840634351,15.7955132792673));
#25039=CARTESIAN_POINT('Ctrl Pts',(1.29240348122505,1.52390981996341,15.7876695668171));
#25040=CARTESIAN_POINT('Ctrl Pts',(1.37922156662505,1.44580929534614,15.7808460090613));
#25041=CARTESIAN_POINT('Ctrl Pts',(1.52592618006905,1.28851930502849,15.7683474311591));
#25042=CARTESIAN_POINT('Ctrl Pts',(1.58769000148148,1.21159908831075,15.7626743779119));
#25043=CARTESIAN_POINT('Ctrl Pts',(1.67506154760631,1.0845712865334,15.7535434302963));
#25044=CARTESIAN_POINT('Ctrl Pts',(1.70467098150482,1.03741127910021,15.7502011343208));
#25045=CARTESIAN_POINT('Ctrl Pts',(1.74837606466245,0.960866295521648,15.7447994784433));
#25046=CARTESIAN_POINT('Ctrl Pts',(1.76379158248398,0.932267110694594,15.7427863680743));
#25047=CARTESIAN_POINT('Ctrl Pts',(1.78252529368759,0.895382657920932,15.7401908720983));
#25048=CARTESIAN_POINT('Ctrl Pts',(1.78649628533786,0.887433121480815,15.7396315326831));
#25049=CARTESIAN_POINT('Ctrl Pts',(1.79278409236191,0.874632299828052,15.7387308269601));
#25050=CARTESIAN_POINT('Ctrl Pts',(1.79513467342641,0.869797657543339,15.7383906412148));
#25051=CARTESIAN_POINT('Ctrl Pts',(1.79956164346505,0.86059794262176,15.7377432738338));
#25052=CARTESIAN_POINT('Ctrl Pts',(1.80164176844044,0.856234702059272,15.7374362248336));
#25053=CARTESIAN_POINT('Ctrl Pts',(1.80633437719127,0.846298741859406,15.7367369565868));
#25054=CARTESIAN_POINT('Ctrl Pts',(1.80893695998885,0.840721425966304,15.73634439824));
#25055=CARTESIAN_POINT('Ctrl Pts',(1.8167664242427,0.823738268821107,15.7351488640905));
#25056=CARTESIAN_POINT('Ctrl Pts',(1.82191146607867,0.812295250257209,15.7343430848305));
#25057=CARTESIAN_POINT('Ctrl Pts',(1.88989435921471,0.657199727624472,15.7234167719473));
#25058=CARTESIAN_POINT('Ctrl Pts',(1.93567601962903,0.506705313167106,15.7126902034601));
#25059=CARTESIAN_POINT('Ctrl Pts',(1.97945196496466,0.262839467641361,15.6954194193815));
#25060=CARTESIAN_POINT('Ctrl Pts',(1.98938424300913,0.172238990371814,15.6890421884122));
#25061=CARTESIAN_POINT('Ctrl Pts',(1.99449324686085,0.0469503072085415,
15.6804862282634));
#25062=CARTESIAN_POINT('Ctrl Pts',(1.99500609791161,0.0125938935330608,
15.6781678503751));
#25063=CARTESIAN_POINT('Ctrl Pts',(1.99442191280116,-0.0409538870161705,
15.6746141948049));
#25064=CARTESIAN_POINT('Ctrl Pts',(1.99393549374277,-0.0601440042439693,
15.6733526450537));
#25065=CARTESIAN_POINT('Ctrl Pts',(1.99297063706869,-0.0843876386238216,
15.6717765113325));
#25066=CARTESIAN_POINT('Ctrl Pts',(1.99274986015056,-0.0894495947839769,
15.6714483947513));
#25067=CARTESIAN_POINT('Ctrl Pts',(1.99236679001827,-0.0975256202009443,
15.6709265169602));
#25068=CARTESIAN_POINT('Ctrl Pts',(1.99221694051022,-0.100540214864414,
15.6707320703219));
#25069=CARTESIAN_POINT('Ctrl Pts',(1.99191952422333,-0.106261562206286,
15.6703637285011));
#25070=CARTESIAN_POINT('Ctrl Pts',(1.99177328422832,-0.108968320642123,
15.6701897640073));
#25071=CARTESIAN_POINT('Ctrl Pts',(1.99142535289544,-0.115173367869909,
15.6697916332221));
#25072=CARTESIAN_POINT('Ctrl Pts',(1.99121996124137,-0.118671425514473,
15.6695676766948));
#25073=CARTESIAN_POINT('Ctrl Pts',(1.99054155550235,-0.129727503069359,
15.6688613215636));
#25074=CARTESIAN_POINT('Ctrl Pts',(1.99003471233042,-0.137283492685096,
15.6683807822093));
#25075=CARTESIAN_POINT('Ctrl Pts',(1.98056400084957,-0.267373832261972,
15.6601425066931));
#25076=CARTESIAN_POINT('Ctrl Pts',(1.96033950833219,-0.388846396194774,
15.6529781055579));
#25077=CARTESIAN_POINT('Ctrl Pts',(1.90357408724273,-0.604531993860171,
15.640030409639));
#25078=CARTESIAN_POINT('Ctrl Pts',(1.87083552266274,-0.699304305055512,
15.6342550555598));
#25079=CARTESIAN_POINT('Ctrl Pts',(1.80095385045338,-0.861032883307637,
15.6237783634448));
#25080=CARTESIAN_POINT('Ctrl Pts',(1.76682041958583,-0.929061847995357,
15.6191632092025));
#25081=CARTESIAN_POINT('Ctrl Pts',(1.72324031379163,-1.00478787356553,15.6136991452631));
#25082=CARTESIAN_POINT('Ctrl Pts',(1.7175073480908,-1.01455623340083,15.6129878679163));
#25083=CARTESIAN_POINT('Ctrl Pts',(1.70865903278578,-1.02934287345655,15.6119011188232));
#25084=CARTESIAN_POINT('Ctrl Pts',(1.70560400508463,-1.03439712783591,15.6115278465016));
#25085=CARTESIAN_POINT('Ctrl Pts',(1.70026028019183,-1.04314977729231,15.6108782548688));
#25086=CARTESIAN_POINT('Ctrl Pts',(1.69798183714066,-1.04685441132577,15.6106023133194));
#25087=CARTESIAN_POINT('Ctrl Pts',(1.69321261452415,-1.05455239570988,15.6100268316828));
#25088=CARTESIAN_POINT('Ctrl Pts',(1.69071978357449,-1.05854443746359,15.6097272170927));
#25089=CARTESIAN_POINT('Ctrl Pts',(1.683830829649,-1.06949005500667,15.6089024440314));
#25090=CARTESIAN_POINT('Ctrl Pts',(1.67940581963778,-1.07642525529635,15.6083762170346));
#25091=CARTESIAN_POINT('Ctrl Pts',(1.66382617558005,-1.10051290341008,15.606535597904));
#25092=CARTESIAN_POINT('Ctrl Pts',(1.6524509506281,-1.11752046827208,15.6052129933034));
#25093=CARTESIAN_POINT('Ctrl Pts',(1.55330359300697,-1.26093536098684,15.593858476359));
#25094=CARTESIAN_POINT('Ctrl Pts',(1.45145305901874,-1.37694444188002,15.5832591368896));
#25095=CARTESIAN_POINT('Ctrl Pts',(1.24285062431285,-1.56542559607305,15.5636462757614));
#25096=CARTESIAN_POINT('Ctrl Pts',(1.14042526210469,-1.64154573577819,15.5547373637761));
#25097=CARTESIAN_POINT('Ctrl Pts',(1.02307456070021,-1.71243725620804,15.545753233086));
#25098=CARTESIAN_POINT('Ctrl Pts',(1.01467932594733,-1.71742504584792,15.545116898694));
#25099=CARTESIAN_POINT('Ctrl Pts',(1.00285609771061,-1.72433251957279,15.5442300170998));
#25100=CARTESIAN_POINT('Ctrl Pts',(0.999458716866094,-1.72630393172737,
15.5439762401445));
#25101=CARTESIAN_POINT('Ctrl Pts',(0.993654372562984,-1.72964916408859,
15.5435445137915));
#25102=CARTESIAN_POINT('Ctrl Pts',(0.991250339306147,-1.73102802060276,
15.5433662399579));
#25103=CARTESIAN_POINT('Ctrl Pts',(0.986644401699797,-1.73365705899902,
15.543025720391));
#25104=CARTESIAN_POINT('Ctrl Pts',(0.984442988645295,-1.73490805978474,
15.5428634204495));
#25105=CARTESIAN_POINT('Ctrl Pts',(0.979224792440551,-1.73786028303442,
15.5424797612027));
#25106=CARTESIAN_POINT('Ctrl Pts',(0.976205936405182,-1.73955785406685,
15.5422586367755));
#25107=CARTESIAN_POINT('Ctrl Pts',(0.967182060644392,-1.74460129501744,
15.5416000910584));
#25108=CARTESIAN_POINT('Ctrl Pts',(0.961164074127508,-1.74792403808091,
15.5411641158733));
#25109=CARTESIAN_POINT('Ctrl Pts',(0.850582025185871,-1.80823649187624,
15.5332092985703));
#25110=CARTESIAN_POINT('Ctrl Pts',(0.741120812905381,-1.85579044322479,
15.5262479098748));
#25111=CARTESIAN_POINT('Ctrl Pts',(0.5318166317685,-1.92522196653055,15.5134390977038));
#25112=CARTESIAN_POINT('Ctrl Pts',(0.433286066257205,-1.94976169912284,
15.5075974330694));
#25113=CARTESIAN_POINT('Ctrl Pts',(0.281950476477381,-1.97541040930895,
15.4984816239273));
#25114=CARTESIAN_POINT('Ctrl Pts',(0.230261369932737,-1.98210025667364,
15.4953451779851));
#25115=CARTESIAN_POINT('Ctrl Pts',(0.147521013839934,-1.98952873710777,
15.4902478548551));
#25116=CARTESIAN_POINT('Ctrl Pts',(0.11661067700174,-1.99157948136775,15.4883268147675));
#25117=CARTESIAN_POINT('Ctrl Pts',(0.0769340281574682,-1.99328500543427,
15.4858346912803));
#25118=CARTESIAN_POINT('Ctrl Pts',(0.0681994057471645,-1.99360296817505,
15.4852844400508));
#25119=CARTESIAN_POINT('Ctrl Pts',(0.054122111901267,-1.99402279597857,
15.484394897841));
#25120=CARTESIAN_POINT('Ctrl Pts',(0.0487805619729641,-1.99416061784053,
15.4840567351901));
#25121=CARTESIAN_POINT('Ctrl Pts',(0.0385989265556293,-1.99438239026013,
15.4834109279476));
#25122=CARTESIAN_POINT('Ctrl Pts',(0.0337589560308472,-1.99447018727277,
15.4831034061917));
#25123=CARTESIAN_POINT('Ctrl Pts',(0.0227054358960415,-1.99463045175091,
15.4823998585181));
#25124=CARTESIAN_POINT('Ctrl Pts',(0.0164917950282941,-1.99469150374779,
15.4820034778714));
#25125=CARTESIAN_POINT('Ctrl Pts',(-0.00256814825675998,-1.99478971215964,
15.4807848276505));
#25126=CARTESIAN_POINT('Ctrl Pts',(-0.0154144068904503,-1.99473180511758,
15.4799595933177));
#25127=CARTESIAN_POINT('Ctrl Pts',(-0.172186242844886,-1.99251064736297,
15.4698397636446));
#25128=CARTESIAN_POINT('Ctrl Pts',(-0.315439739389119,-1.97489966395824,
15.4600417566724));
#25129=CARTESIAN_POINT('Ctrl Pts',(-0.552153552281778,-1.91937618556936,
15.443125276818));
#25130=CARTESIAN_POINT('Ctrl Pts',(-0.646958137923274,-1.88953026217246,
15.4361545250006));
#25131=CARTESIAN_POINT('Ctrl Pts',(-0.773694013565491,-1.83896939126179,
15.4268206040582));
#25132=CARTESIAN_POINT('Ctrl Pts',(-0.807849099097985,-1.82422340795237,
15.4243045975179));
#25133=CARTESIAN_POINT('Ctrl Pts',(-0.859980016618908,-1.79996502099589,
15.4204840902258));
#25134=CARTESIAN_POINT('Ctrl Pts',(-0.878255171450998,-1.79111910233697,
15.4191486291234));
#25135=CARTESIAN_POINT('Ctrl Pts',(-0.901006263085567,-1.77967467376247,
15.417493875022));
#25136=CARTESIAN_POINT('Ctrl Pts',(-0.905610618276656,-1.77733610779197,
15.4171593917827));
#25137=CARTESIAN_POINT('Ctrl Pts',(-0.912910986896972,-1.77359249384027,
15.4166297634478));
#25138=CARTESIAN_POINT('Ctrl Pts',(-0.915612919647041,-1.77219913832591,
15.4164338976519));
#25139=CARTESIAN_POINT('Ctrl Pts',(-0.920713598177809,-1.76955399843327,
15.4160644517662));
#25140=CARTESIAN_POINT('Ctrl Pts',(-0.923112952984117,-1.7683035258027,
15.4158907956441));
#25141=CARTESIAN_POINT('Ctrl Pts',(-0.928579806906484,-1.76544020435438,
15.4154954140523));
#25142=CARTESIAN_POINT('Ctrl Pts',(-0.931645647368408,-1.76382424326482,
15.4152738882577));
#25143=CARTESIAN_POINT('Ctrl Pts',(-0.939736486170129,-1.75953269589332,
15.414689779883));
#25144=CARTESIAN_POINT('Ctrl Pts',(-0.944754313838724,-1.75684355015778,
15.4143280395755));
#25145=CARTESIAN_POINT('Ctrl Pts',(-0.977997018819345,-1.73884456492324,
15.411934509218));
#25146=CARTESIAN_POINT('Ctrl Pts',(-1.00586211039976,-1.72287558727561,
15.4099424259101));
#25147=CARTESIAN_POINT('Ctrl Pts',(-1.04233473098311,-1.70078707165599,
15.407337654787));
#25148=CARTESIAN_POINT('Ctrl Pts',(-1.05129497982961,-1.69526317363566,
15.4066979594962));
#25149=CARTESIAN_POINT('Ctrl Pts',(-1.2148860731785,-1.59261515995388,15.3950149053074));
#25150=CARTESIAN_POINT('Ctrl Pts',(-1.35551254325261,-1.47477798037274,
15.3848314364103));
#25151=CARTESIAN_POINT('Ctrl Pts',(-1.51202120881655,-1.30206133511899,
15.3709704128747));
#25152=CARTESIAN_POINT('Ctrl Pts',(-1.54445932552945,-1.26341468593201,
15.3679303989625));
#25153=CARTESIAN_POINT('Ctrl Pts',(-1.59395470238153,-1.19968800996751,
15.3629763063732));
#25154=CARTESIAN_POINT('Ctrl Pts',(-1.61196617601303,-1.17537560299963,
15.3610992434239));
#25155=CARTESIAN_POINT('Ctrl Pts',(-1.63441739605989,-1.14358317535177,
15.3586566059735));
#25156=CARTESIAN_POINT('Ctrl Pts',(-1.63937145067098,-1.13646994962209,
15.3581108469893));
#25157=CARTESIAN_POINT('Ctrl Pts',(-1.64729497341312,-1.12493342618513,
15.3572268219234));
#25158=CARTESIAN_POINT('Ctrl Pts',(-1.65029339674597,-1.12053007391104,
15.3568896587039));
#25159=CARTESIAN_POINT('Ctrl Pts',(-1.65598483837359,-1.11209947772614,
15.3562445968015));
#25160=CARTESIAN_POINT('Ctrl Pts',(-1.65868089840397,-1.10807432506637,
15.3559368160397));
#25161=CARTESIAN_POINT('Ctrl Pts',(-1.66481855884391,-1.09883835289982,
15.3552310310868));
#25162=CARTESIAN_POINT('Ctrl Pts',(-1.66825039304214,-1.09362113381343,
15.354832664029));
#25163=CARTESIAN_POINT('Ctrl Pts',(-1.67875281166043,-1.07749044385639,
15.3536019022532));
#25164=CARTESIAN_POINT('Ctrl Pts',(-1.68574110892564,-1.06652405487339,
15.3527664564327));
#25165=CARTESIAN_POINT('Ctrl Pts',(-1.75653313051831,-0.952999470751862,
15.3441295571548));
#25166=CARTESIAN_POINT('Ctrl Pts',(-1.81099189664738,-0.844935107726615,
15.335981802361));
#25167=CARTESIAN_POINT('Ctrl Pts',(-1.89669597090157,-0.627894553412535,
15.3198424509148));
#25168=CARTESIAN_POINT('Ctrl Pts',(-1.92910947416793,-0.519849367004161,
15.3119103611211));
#25169=CARTESIAN_POINT('Ctrl Pts',(-1.96124541729301,-0.36670096513606,
15.3011502115146));
#25170=CARTESIAN_POINT('Ctrl Pts',(-1.96883818353093,-0.3234655111744,15.2981662913259));
#25171=CARTESIAN_POINT('Ctrl Pts',(-1.97819466860347,-0.257471726116805,
15.2937253378715));
#25172=CARTESIAN_POINT('Ctrl Pts',(-1.98100445068317,-0.234877229678068,
15.2922249591443));
#25173=CARTESIAN_POINT('Ctrl Pts',(-1.98399751581249,-0.206906205373042,
15.2903963344348));
#25174=CARTESIAN_POINT('Ctrl Pts',(-1.98454659748363,-0.201571636406673,
15.2900488737199));
#25175=CARTESIAN_POINT('Ctrl Pts',(-1.98537756917351,-0.193165685632635,
15.2895034625662));
#25176=CARTESIAN_POINT('Ctrl Pts',(-1.98567385550802,-0.190095802563266,
15.2893047173156));
#25177=CARTESIAN_POINT('Ctrl Pts',(-1.98621595254572,-0.184339441594563,
15.2889328904975));
#25178=CARTESIAN_POINT('Ctrl Pts',(-1.98646343059267,-0.181653183033562,
15.2887597195322));
#25179=CARTESIAN_POINT('Ctrl Pts',(-1.98701509900995,-0.175529112936757,
15.2883657069906));
#25180=CARTESIAN_POINT('Ctrl Pts',(-1.98731581682795,-0.172091016053264,
15.2881450628195));
#25181=CARTESIAN_POINT('Ctrl Pts',(-1.98820843730845,-0.161571259667954,
15.2874716013178));
#25182=CARTESIAN_POINT('Ctrl Pts',(-1.98877142973061,-0.15448710653519,
15.2870203788304));
#25183=CARTESIAN_POINT('Ctrl Pts',(-1.9929020221701,-0.0987410066511232,
15.2834866400716));
#25184=CARTESIAN_POINT('Ctrl Pts',(-1.99472128907784,-0.0499613959230888,
15.2804961767506));
#25185=CARTESIAN_POINT('Ctrl Pts',(-1.99480080939928,0.0868098812329685,
15.2722742076292));
#25186=CARTESIAN_POINT('Ctrl Pts',(-1.98903262433188,0.174692790294786,
15.2671769599265));
#25187=CARTESIAN_POINT('Ctrl Pts',(-1.9580319883537,0.408752153297152,15.2534837481734));
#25188=CARTESIAN_POINT('Ctrl Pts',(-1.9222926283037,0.552948031636237,15.2448875832467));
#25189=CARTESIAN_POINT('Ctrl Pts',(-1.86641799770841,0.704045754187782,
15.2349220473966));
#25190=CARTESIAN_POINT('Ctrl Pts',(-1.86179006631279,0.716194319169201,
15.2341141174458));
#25191=CARTESIAN_POINT('Ctrl Pts',(-1.85247175468876,0.739954575258685,
15.2325202680508));
#25192=CARTESIAN_POINT('Ctrl Pts',(-1.84779011653813,0.751569058163606,
15.2317346660948));
#25193=CARTESIAN_POINT('Ctrl Pts',(-1.84064671841057,0.768820552577513,
15.2305577431308));
#25194=CARTESIAN_POINT('Ctrl Pts',(-1.83826767770832,0.774491657655243,
15.230169222794));
#25195=CARTESIAN_POINT('Ctrl Pts',(-1.83397219844152,0.784599832766567,
15.2294737705707));
#25196=CARTESIAN_POINT('Ctrl Pts',(-1.83206577893743,0.789041128970013,
15.2291671815744));
#25197=CARTESIAN_POINT('Ctrl Pts',(-1.82800377910555,0.798410091612968,
15.2285182422574));
#25198=CARTESIAN_POINT('Ctrl Pts',(-1.82584437531591,0.803336048616278,
15.2281757632023));
#25199=CARTESIAN_POINT('Ctrl Pts',(-1.82005957604924,0.816388315963878,
15.2272648531099));
#25200=CARTESIAN_POINT('Ctrl Pts',(-1.81639971411059,0.824499131068781,
15.2266952436182));
#25201=CARTESIAN_POINT('Ctrl Pts',(-1.79907253452952,0.86222348185831,15.224029032601));
#25202=CARTESIAN_POINT('Ctrl Pts',(-1.78473517776987,0.891521986873294,
15.2219094195557));
#25203=CARTESIAN_POINT('Ctrl Pts',(-1.7438579943568,0.970113389341041,15.2160853490928));
#25204=CARTESIAN_POINT('Ctrl Pts',(-1.71595273161849,1.01865889723033,15.2123351915361));
#25205=CARTESIAN_POINT('Ctrl Pts',(-1.63022240228275,1.1542594522993,15.2014213903396));
#25206=CARTESIAN_POINT('Ctrl Pts',(-1.5675533622784,1.2380279510443,15.1941234151566));
#25207=CARTESIAN_POINT('Ctrl Pts',(-1.44751800232382,1.374668901293,15.1814421945112));
#25208=CARTESIAN_POINT('Ctrl Pts',(-1.39306822539288,1.42982011982667,15.1760658144811));
#25209=CARTESIAN_POINT('Ctrl Pts',(-1.30986335324619,1.50481929195788,15.1685122977678));
#25210=CARTESIAN_POINT('Ctrl Pts',(-1.28358081631915,1.52729949618003,15.1662131706301));
#25211=CARTESIAN_POINT('Ctrl Pts',(-1.25220267968629,1.55275559133462,15.1635805946313));
#25212=CARTESIAN_POINT('Ctrl Pts',(-1.24766402249621,1.55640482087588,15.163202477993));
#25213=CARTESIAN_POINT('Ctrl Pts',(-1.24036877857405,1.56221801798167,15.1625990595764));
#25214=CARTESIAN_POINT('Ctrl Pts',(-1.23762240050505,1.56439465506529,15.1623728756998));
#25215=CARTESIAN_POINT('Ctrl Pts',(-1.23274141573671,1.56824217279068,15.1619726476576));
#25216=CARTESIAN_POINT('Ctrl Pts',(-1.23060912428139,1.56991595131031,15.1617983972277));
#25217=CARTESIAN_POINT('Ctrl Pts',(-1.22609550621997,1.57344414625056,15.1614308010428));
#25218=CARTESIAN_POINT('Ctrl Pts',(-1.22371338743346,1.57529750125357,15.1612375305616));
#25219=CARTESIAN_POINT('Ctrl Pts',(-1.21732156993847,1.58024726640064,15.160720870029));
#25220=CARTESIAN_POINT('Ctrl Pts',(-1.21330423304413,1.58333384573065,15.160398171311));
#25221=CARTESIAN_POINT('Ctrl Pts',(-1.19401535039703,1.5980372563715,15.1588582124653));
#25222=CARTESIAN_POINT('Ctrl Pts',(-1.17858784541504,1.6094491251195,15.1576547644563));
#25223=CARTESIAN_POINT('Ctrl Pts',(-1.13510155823892,1.64065564156319,15.1543330275711));
#25224=CARTESIAN_POINT('Ctrl Pts',(-1.10669177363904,1.65995183301675,15.1522429472985));
#25225=CARTESIAN_POINT('Ctrl Pts',(-1.00124009921752,1.7276640850412,15.1447170002267));
#25226=CARTESIAN_POINT('Ctrl Pts',(-0.921405127454716,1.77153034581802,
15.1394544185937));
#25227=CARTESIAN_POINT('Ctrl Pts',(-0.696534339013358,1.87575914095947,
15.1250799494372));
#25228=CARTESIAN_POINT('Ctrl Pts',(-0.546959111374467,1.92469707869704,
15.1159464885486));
#25229=CARTESIAN_POINT('Ctrl Pts',(-0.380908247470206,1.95808422497812,
15.1053694082094));
#25230=CARTESIAN_POINT('Ctrl Pts',(-0.368587132168315,1.96044087889397,
15.1045824443923));
#25231=CARTESIAN_POINT('Ctrl Pts',(-0.350189480929749,1.96378022324521,
15.1034038752353));
#25232=CARTESIAN_POINT('Ctrl Pts',(-0.344129134898545,1.96485128569503,
15.103015082224));
#25233=CARTESIAN_POINT('Ctrl Pts',(-0.333300220069051,1.96671347438698,
15.1023193265262));
#25234=CARTESIAN_POINT('Ctrl Pts',(-0.328533528895954,1.96751534854255,
15.1020127078813));
#25235=CARTESIAN_POINT('Ctrl Pts',(-0.318459262704345,1.9691724561767,15.1013638982523));
#25236=CARTESIAN_POINT('Ctrl Pts',(-0.313151058556607,1.97002357289423,
15.1010215792733));
#25237=CARTESIAN_POINT('Ctrl Pts',(-0.299058785618285,1.97222473050573,
15.1001115443109));
#25238=CARTESIAN_POINT('Ctrl Pts',(-0.29026910264935,1.97353753161179,15.0995426538941));
#25239=CARTESIAN_POINT('Ctrl Pts',(-0.249299299617911,1.97937704102663,
15.0968848005136));
#25240=CARTESIAN_POINT('Ctrl Pts',(-0.217021984406268,1.98317544926241,
15.0947730011886));
#25241=CARTESIAN_POINT('Ctrl Pts',(-0.129216073968002,1.99133930929738,
15.0889759053021));
#25242=CARTESIAN_POINT('Ctrl Pts',(-0.0735774690030502,1.99417011351579,
15.0852454255007));
#25243=CARTESIAN_POINT('Ctrl Pts',(0.0863410709898142,1.99560499828671,
15.0743682201853));
#25244=CARTESIAN_POINT('Ctrl Pts',(0.190485317542087,1.9883677254945,15.067086962492));
#25245=CARTESIAN_POINT('Ctrl Pts',(0.368842389007298,1.96182901274293,15.0545134563551));
#25246=CARTESIAN_POINT('Ctrl Pts',(0.44341009782272,1.94633163668992,15.0492281869397));
#25247=CARTESIAN_POINT('Ctrl Pts',(0.552061654657239,1.91718015825094,15.0416306470847));
#25248=CARTESIAN_POINT('Ctrl Pts',(0.586947242990314,1.90678923212685,15.0392079963791));
#25249=CARTESIAN_POINT('Ctrl Pts',(0.627151514262558,1.89360595710644,15.0364507539518));
#25250=CARTESIAN_POINT('Ctrl Pts',(0.632763350600428,1.89173811266389,15.0360666884083));
#25251=CARTESIAN_POINT('Ctrl Pts',(0.641712149905379,1.88871531652209,15.0354556170125));
#25252=CARTESIAN_POINT('Ctrl Pts',(0.645054443832392,1.88757643425762,15.0352276938767));
#25253=CARTESIAN_POINT('Ctrl Pts',(0.650960803495403,1.88554633017055,15.0348254823307));
#25254=CARTESIAN_POINT('Ctrl Pts',(0.653526093965439,1.88465874252356,15.0346509805206));
#25255=CARTESIAN_POINT('Ctrl Pts',(0.658926436775886,1.8827778778209,15.0342840332829));
#25256=CARTESIAN_POINT('Ctrl Pts',(0.661761052539602,1.88178343491705,15.0340916586049));
#25257=CARTESIAN_POINT('Ctrl Pts',(0.66931016235145,1.87911588107262,15.0335799266968));
#25258=CARTESIAN_POINT('Ctrl Pts',(0.674020665720681,1.87743141856453,15.0332612379361));
#25259=CARTESIAN_POINT('Ctrl Pts',(0.696119985622988,1.86943487130393,15.0317688160012));
#25260=CARTESIAN_POINT('Ctrl Pts',(0.713427484007994,1.86289856322638,15.0306078837309));
#25261=CARTESIAN_POINT('Ctrl Pts',(0.890734578961677,1.79310355440872,15.0187717582043));
#25262=CARTESIAN_POINT('Ctrl Pts',(1.04202532815904,1.70962870249206,15.00910577681));
#25263=CARTESIAN_POINT('Ctrl Pts',(1.26972493122434,1.5424056940417,14.9925810546028));
#25264=CARTESIAN_POINT('Ctrl Pts',(1.35311867119392,1.46978957673048,14.9859976668641));
#25265=CARTESIAN_POINT('Ctrl Pts',(1.43908022240211,1.38139156267205,14.9783009980162));
#25266=CARTESIAN_POINT('Ctrl Pts',(1.44799836697333,1.3720405433729,14.9774906035349));
#25267=CARTESIAN_POINT('Ctrl Pts',(1.46107970562618,1.35805465789823,14.9762837463746));
#25268=CARTESIAN_POINT('Ctrl Pts',(1.46531317446124,1.35348574405218,14.9758903002234));
#25269=CARTESIAN_POINT('Ctrl Pts',(1.47279983858937,1.34532956893094,14.9751893352403));
#25270=CARTESIAN_POINT('Ctrl Pts',(1.47606151501364,1.34175013203158,14.9748821801282));
#25271=CARTESIAN_POINT('Ctrl Pts',(1.48288942211122,1.33420200594684,14.9742354355776));
#25272=CARTESIAN_POINT('Ctrl Pts',(1.48645282344283,1.33023081968834,14.9738957303736));
#25273=CARTESIAN_POINT('Ctrl Pts',(1.49578823918396,1.31974273705536,14.9729999823735));
#25274=CARTESIAN_POINT('Ctrl Pts',(1.50153354916492,1.31320232456329,14.9724428300073));
#25275=CARTESIAN_POINT('Ctrl Pts',(1.52729563045274,1.28348489009043,14.9699175734987));
#25276=CARTESIAN_POINT('Ctrl Pts',(1.5468189476705,1.25988744559841,14.967929316271));
#25277=CARTESIAN_POINT('Ctrl Pts',(1.59756783181815,1.19558995348401,14.9625528380557));
#25278=CARTESIAN_POINT('Ctrl Pts',(1.62777800869497,1.1541214463454,14.9591270637063));
#25279=CARTESIAN_POINT('Ctrl Pts',(1.71252213336685,1.02784024219568,14.9488194882605));
#25280=CARTESIAN_POINT('Ctrl Pts',(1.76226018648412,0.940012417867835,14.941800754716));
#25281=CARTESIAN_POINT('Ctrl Pts',(1.84139260246144,0.771723562317515,14.928826007052));
#25282=CARTESIAN_POINT('Ctrl Pts',(1.87266776147679,0.692388117021748,14.9228893921704));
#25283=CARTESIAN_POINT('Ctrl Pts',(1.9102041890702,0.575793566865182,14.9146106271431));
#25284=CARTESIAN_POINT('Ctrl Pts',(1.92063563320926,0.539979148710923,14.9121264681015));
#25285=CARTESIAN_POINT('Ctrl Pts',(1.93156257775568,0.49812555827962,14.909307317504));
#25286=CARTESIAN_POINT('Ctrl Pts',(1.93304187483262,0.492353710177109,14.9089203750672));
#25287=CARTESIAN_POINT('Ctrl Pts',(1.93535974414577,0.48313847064413,14.9083056063554));
#25288=CARTESIAN_POINT('Ctrl Pts',(1.93621502614915,0.479699378847779,14.9080768455621));
#25289=CARTESIAN_POINT('Ctrl Pts',(1.93770969084814,0.473620201269813,14.9076736745829));
#25290=CARTESIAN_POINT('Ctrl Pts',(1.93835285113517,0.470981067468106,14.9074990475611));
#25291=CARTESIAN_POINT('Ctrl Pts',(1.93969437176519,0.465426998435946,14.9071323933837));
#25292=CARTESIAN_POINT('Ctrl Pts',(1.94039155198076,0.462511807441816,14.9069404348515));
#25293=CARTESIAN_POINT('Ctrl Pts',(1.9422279643507,0.45475578954462,14.9064309918224));
#25294=CARTESIAN_POINT('Ctrl Pts',(1.94335567842903,0.449912215916506,14.9061141652831));
#25295=CARTESIAN_POINT('Ctrl Pts',(1.9485232235402,0.427335456758754,14.9046432912856));
#25296=CARTESIAN_POINT('Ctrl Pts',(1.95233868007559,0.40955107141852,14.9035015998676));
#25297=CARTESIAN_POINT('Ctrl Pts',(1.98663422462039,0.238307171274366,14.8926489748856));
#25298=CARTESIAN_POINT('Ctrl Pts',(1.99920750905528,0.0817929132677074,
14.8837790026025));
#25299=CARTESIAN_POINT('Ctrl Pts',(1.98863462462954,-0.200718385880195,
14.8673191846895));
#25300=CARTESIAN_POINT('Ctrl Pts',(1.9719578763923,-0.326084102407573,14.8598527150954));
#25301=CARTESIAN_POINT('Ctrl Pts',(1.94062593622361,-0.461700988290552,
14.8511652867954));
#25302=CARTESIAN_POINT('Ctrl Pts',(1.93757341671358,-0.474348046277771,
14.8503494086652));
#25303=CARTESIAN_POINT('Ctrl Pts',(1.93287265841588,-0.493021157499012,
14.849135940484));
#25304=CARTESIAN_POINT('Ctrl Pts',(1.9313194331916,-0.499070957808963,14.8487414157433));
#25305=CARTESIAN_POINT('Ctrl Pts',(1.92851102052709,-0.509800233966037,
14.8480392354362));
#25306=CARTESIAN_POINT('Ctrl Pts',(1.92726714461576,-0.514482640574314,
14.8477319481601));
#25307=CARTESIAN_POINT('Ctrl Pts',(1.92461989414998,-0.524303537053152,
14.8470856443031));
#25308=CARTESIAN_POINT('Ctrl Pts',(1.92321297258792,-0.529441023237143,
14.846746514691));
#25309=CARTESIAN_POINT('Ctrl Pts',(1.9194632355465,-0.542921302557391,14.8458539131069));
#25310=CARTESIAN_POINT('Ctrl Pts',(1.91708662422482,-0.551254500818922,
14.8452993456538));
#25311=CARTESIAN_POINT('Ctrl Pts',(1.90617667454421,-0.588584468351075,
14.8428023536974));
#25312=CARTESIAN_POINT('Ctrl Pts',(1.8970395997164,-0.61739920737807,14.8408403248901));
#25313=CARTESIAN_POINT('Ctrl Pts',(1.8709376268012,-0.69365532957347,14.8355517497883));
#25314=CARTESIAN_POINT('Ctrl Pts',(1.85282511125846,-0.740677871051671,
14.8321891437597));
#25315=CARTESIAN_POINT('Ctrl Pts',(1.79347697908041,-0.878908763841877,
14.822000968698));
#25316=CARTESIAN_POINT('Ctrl Pts',(1.74714085680376,-0.967747797229719,
14.8150381725344));
#25317=CARTESIAN_POINT('Ctrl Pts',(1.62933719241515,-1.15735008191424,14.7994637798773));
#25318=CARTESIAN_POINT('Ctrl Pts',(1.55477440098873,-1.25573998889278,14.7908723187804));
#25319=CARTESIAN_POINT('Ctrl Pts',(1.46650189535482,-1.35220443329619,14.7823355693203));
#25320=CARTESIAN_POINT('Ctrl Pts',(1.46136997719116,-1.35774903155914,14.7818445177215));
#25321=CARTESIAN_POINT('Ctrl Pts',(1.45381413645301,-1.36582000051582,14.7811293465781));
#25322=CARTESIAN_POINT('Ctrl Pts',(1.45141494420676,-1.36836927667659,14.7809033992405));
#25323=CARTESIAN_POINT('Ctrl Pts',(1.44714638968902,-1.37288099801883,14.7805034400217));
#25324=CARTESIAN_POINT('Ctrl Pts',(1.44527972616472,-1.37484596278961,14.7803292228468));
#25325=CARTESIAN_POINT('Ctrl Pts',(1.44132448642157,-1.37899253390432,14.7799615340296));
#25326=CARTESIAN_POINT('Ctrl Pts',(1.43923496454941,-1.38117319726308,14.7797681382884));
#25327=CARTESIAN_POINT('Ctrl Pts',(1.4336210208348,-1.38700543847324,14.779250788348));
#25328=CARTESIAN_POINT('Ctrl Pts',(1.43008757344184,-1.39064835648083,14.7789275287055));
#25329=CARTESIAN_POINT('Ctrl Pts',(1.41305977251629,-1.40807016641932,14.7773807929688));
#25330=CARTESIAN_POINT('Ctrl Pts',(1.39937940472645,-1.42166693105055,14.7761712765006));
#25331=CARTESIAN_POINT('Ctrl Pts',(1.36062312744969,-1.45908474841871,14.772828448244));
#25332=CARTESIAN_POINT('Ctrl Pts',(1.33512083489602,-1.48245615376489,14.7707237813228));
#25333=CARTESIAN_POINT('Ctrl Pts',(1.23980741855908,-1.56534958615536,14.7631401443741));
#25334=CARTESIAN_POINT('Ctrl Pts',(1.16651813537486,-1.62070338922514,14.7578365726643));
#25335=CARTESIAN_POINT('Ctrl Pts',(0.959271075542452,-1.75586578401537,
14.7434864113391));
#25336=CARTESIAN_POINT('Ctrl Pts',(0.819381425775328,-1.82534118989306,
14.7344156351421));
#25337=CARTESIAN_POINT('Ctrl Pts',(0.661003948046607,-1.88208916572404,
14.7239100001802));
#25338=CARTESIAN_POINT('Ctrl Pts',(0.649120498347943,-1.88622066952236,
14.7231207577561));
#25339=CARTESIAN_POINT('Ctrl Pts',(0.631360215353328,-1.89220765405401,
14.7219394347531));
#25340=CARTESIAN_POINT('Ctrl Pts',(0.62551242190712,-1.89414881576058,14.72155018606));
#25341=CARTESIAN_POINT('Ctrl Pts',(0.615060437903772,-1.89756464787097,
14.7208539227499));
#25342=CARTESIAN_POINT('Ctrl Pts',(0.610459683277312,-1.89904973856469,
14.7205472540992));
#25343=CARTESIAN_POINT('Ctrl Pts',(0.601170190040037,-1.90201107477083,
14.7199276547828));
#25344=CARTESIAN_POINT('Ctrl Pts',(0.59648130397468,-1.90348674259611,14.7196147076154));
#25345=CARTESIAN_POINT('Ctrl Pts',(0.583986723811788,-1.90736828798218,
14.7187802240287));
#25346=CARTESIAN_POINT('Ctrl Pts',(0.57617168964631,-1.90974355879213,14.7182576892593));
#25347=CARTESIAN_POINT('Ctrl Pts',(0.559099039307391,-1.91481821978313,
14.7171148022165));
#25348=CARTESIAN_POINT('Ctrl Pts',(0.549836032544862,-1.9174986003771,14.7164938431795));
#25349=CARTESIAN_POINT('Ctrl Pts',(0.522845912279533,-1.92509691877968,
14.7146818434446));
#25350=CARTESIAN_POINT('Ctrl Pts',(0.505070130984278,-1.92983681172478,
14.7134850998475));
#25351=CARTESIAN_POINT('Ctrl Pts',(0.443667653778369,-1.94530327288966,
14.7093388453182));
#25352=CARTESIAN_POINT('Ctrl Pts',(0.39974827929327,-1.9548009120681,14.7063514111754));
#25353=CARTESIAN_POINT('Ctrl Pts',(0.173425692977654,-1.99579761978097,
14.6908474355757));
#25354=CARTESIAN_POINT('Ctrl Pts',(-0.0123676467394637,-2.00327625017293,
14.6776477995529));
#25355=CARTESIAN_POINT('Ctrl Pts',(-0.205876688441953,-1.98411968517939,
14.6644020410063));
#25356=CARTESIAN_POINT('Ctrl Pts',(-0.215235721212382,-1.98312625056233,
14.6637629476002));
#25357=CARTESIAN_POINT('Ctrl Pts',(-0.263027584444043,-1.97771096549108,
14.660508349329));
#25358=CARTESIAN_POINT('Ctrl Pts',(-0.301336052990113,-1.97223762372811,
14.6579289971416));
#25359=CARTESIAN_POINT('Ctrl Pts',(-0.345973592532238,-1.96452881733855,
14.6549763543898));
#25360=CARTESIAN_POINT('Ctrl Pts',(-0.352477655690476,-1.96337227904,14.6545474549728));
#25361=CARTESIAN_POINT('Ctrl Pts',(-0.362315161909981,-1.96157253482772,
14.6539008685471));
#25362=CARTESIAN_POINT('Ctrl Pts',(-0.365652825840895,-1.9609531094126,
14.6536818671219));
#25363=CARTESIAN_POINT('Ctrl Pts',(-0.371635118917663,-1.95982707179363,
14.6532900253341));
#25364=CARTESIAN_POINT('Ctrl Pts',(-0.374280306503332,-1.95932362446945,
14.653117007348));
#25365=CARTESIAN_POINT('Ctrl Pts',(-0.379991175662831,-1.95822471170468,
14.652743994131));
#25366=CARTESIAN_POINT('Ctrl Pts',(-0.383056469736233,-1.95762740490456,
14.6525441058615));
#25367=CARTESIAN_POINT('Ctrl Pts',(-0.39155419293424,-1.95595080517453,
14.6519908397257));
#25368=CARTESIAN_POINT('Ctrl Pts',(-0.396983600992889,-1.95485607157423,
14.6516383330554));
#25369=CARTESIAN_POINT('Ctrl Pts',(-0.427107894392728,-1.94865141878452,
14.6496876405144));
#25370=CARTESIAN_POINT('Ctrl Pts',(-0.451710050428756,-1.94309590090232,
14.6481137347825));
#25371=CARTESIAN_POINT('Ctrl Pts',(-0.634194809744351,-1.89823468777809,
14.6365380993947));
#25372=CARTESIAN_POINT('Ctrl Pts',(-0.786863098619822,-1.84020620682486,
14.6273675226794));
#25373=CARTESIAN_POINT('Ctrl Pts',(-1.02985424164314,-1.7120077099945,14.6113061857728));
#25374=CARTESIAN_POINT('Ctrl Pts',(-1.12431648297316,-1.65150756914902,
14.6046332589389));
#25375=CARTESIAN_POINT('Ctrl Pts',(-1.22346629382407,-1.57553964285377,
14.596836584747));
#25376=CARTESIAN_POINT('Ctrl Pts',(-1.23365883797584,-1.56757162428156,
14.596025224356));
#25377=CARTESIAN_POINT('Ctrl Pts',(-1.24864502600964,-1.55561948978588,
14.5948172024474));
#25378=CARTESIAN_POINT('Ctrl Pts',(-1.25349880543022,-1.55171103667325,
14.5944235660231));
#25379=CARTESIAN_POINT('Ctrl Pts',(-1.26209197214017,-1.54472485289995,
14.5937223868507));
#25380=CARTESIAN_POINT('Ctrl Pts',(-1.26583863221877,-1.54165611399304,
14.5934152086284));
#25381=CARTESIAN_POINT('Ctrl Pts',(-1.26961833078248,-1.53853724684733,
14.5931038291399));
#25382=CARTESIAN_POINT('Ctrl Pts',(-1.26966260712151,-1.53850070844076,
14.5931001813545));
#25383=CARTESIAN_POINT('Ctrl Pts',(-1.26974953179697,-1.53842896880531,
14.5930930195013));
#25384=CARTESIAN_POINT('Ctrl Pts',(-1.26979218068056,-1.53839376735623,
14.5930895054035));
#25385=CARTESIAN_POINT('Ctrl Pts',(-1.26987592461901,-1.53832464109909,
14.5930826048583));
#25386=CARTESIAN_POINT('Ctrl Pts',(-1.26991701991006,-1.53829071630896,
14.5930792184052));
#25387=CARTESIAN_POINT('Ctrl Pts',(-1.26999772630241,-1.53822408651187,
14.5930725674516));
#25388=CARTESIAN_POINT('Ctrl Pts',(-1.27003733765258,-1.53819138149545,
14.5930693029432));
#25389=CARTESIAN_POINT('Ctrl Pts',(-1.27011514195353,-1.53812713750641,
14.5930628904947));
#25390=CARTESIAN_POINT('Ctrl Pts',(-1.27015333517176,-1.53809559849357,
14.5930597425441));
#25391=CARTESIAN_POINT('Ctrl Pts',(-1.2702283654229,-1.5380336356717,14.5930535581178));
#25392=CARTESIAN_POINT('Ctrl Pts',(-1.2702652027326,-1.53800321180065,14.5930505216301));
#25393=CARTESIAN_POINT('Ctrl Pts',(-1.27033758003062,-1.53794343114001,
14.5930445553093));
#25394=CARTESIAN_POINT('Ctrl Pts',(-1.27037312030605,-1.53791407426701,
14.5930416254625));
#25395=CARTESIAN_POINT('Ctrl Pts',(-1.27044295920464,-1.53785638207424,
14.5930358678639));
#25396=CARTESIAN_POINT('Ctrl Pts',(-1.27047725815306,-1.53782804662775,
14.5930330400944));
#25397=CARTESIAN_POINT('Ctrl Pts',(-1.2705446671855,-1.53777235409893,14.5930274823255));
#25398=CARTESIAN_POINT('Ctrl Pts',(-1.27057777759136,-1.53774499688193,
14.5930247523081));
#25399=CARTESIAN_POINT('Ctrl Pts',(-1.27064285953397,-1.53769121989276,
14.5930193859461));
#25400=CARTESIAN_POINT('Ctrl Pts',(-1.27067483141411,-1.53766479995823,
14.5930167495812));
#25401=CARTESIAN_POINT('Ctrl Pts',(-1.27073768369958,-1.53761285872956,
14.5930115666396));
#25402=CARTESIAN_POINT('Ctrl Pts',(-1.2707685644723,-1.53758733724417,14.5930090200398));
#25403=CARTESIAN_POINT('Ctrl Pts',(-1.27082927956527,-1.53753715603803,
14.5930040129373));
#25404=CARTESIAN_POINT('Ctrl Pts',(-1.27085911424879,-1.53751249612112,
14.5930015524113));
#25405=CARTESIAN_POINT('Ctrl Pts',(-1.2709177798195,-1.53746400310302,14.5929967139583));
#25406=CARTESIAN_POINT('Ctrl Pts',(-1.27094661112434,-1.53744016975308,
14.5929943360031));
#25407=CARTESIAN_POINT('Ctrl Pts',(-1.27100331047543,-1.53739329664454,
14.5929896593667));
#25408=CARTESIAN_POINT('Ctrl Pts',(-1.27103117896986,-1.53737025660492,
14.5929873606543));
#25409=CARTESIAN_POINT('Ctrl Pts',(-1.27108599125651,-1.53732493850628,
14.5929828393406));
#25410=CARTESIAN_POINT('Ctrl Pts',(-1.27111293550348,-1.53730266015431,
14.592980616707));
#25411=CARTESIAN_POINT('Ctrl Pts',(-1.27116593596108,-1.53725883536083,
14.5929762445421));
#25412=CARTESIAN_POINT('Ctrl Pts',(-1.27119199263413,-1.53723728861407,
14.5929740949777));
#25413=CARTESIAN_POINT('Ctrl Pts',(-1.27124325281111,-1.53719489842746,
14.5929698660895));
#25414=CARTESIAN_POINT('Ctrl Pts',(-1.27126845679979,-1.53717405465841,
14.5929677867305));
#25415=CARTESIAN_POINT('Ctrl Pts',(-1.27131804478319,-1.53713304320395,
14.5929636955298));
#25416=CARTESIAN_POINT('Ctrl Pts',(-1.27134242929451,-1.53711287515792,
14.5929616836499));
#25417=CARTESIAN_POINT('Ctrl Pts',(-1.27139040991838,-1.53707318921538,
14.5929577248135));
#25418=CARTESIAN_POINT('Ctrl Pts',(-1.27141400657607,-1.53705367092996,
14.5929557778161));
#25419=CARTESIAN_POINT('Ctrl Pts',(-1.2714604415981,-1.53701525979058,14.5929519462726));
#25420=CARTESIAN_POINT('Ctrl Pts',(-1.2714832805268,-1.53699636652747,14.5929500616837));
#25421=CARTESIAN_POINT('Ctrl Pts',(-1.27575141409662,-1.53346543777717,
14.5925978597812));
#25422=CARTESIAN_POINT('Ctrl Pts',(-1.27998210494452,-1.5299358579511,14.592246828577));
#25423=CARTESIAN_POINT('Ctrl Pts',(-1.29153930060784,-1.5202124321208,14.5912825839185));
#25424=CARTESIAN_POINT('Ctrl Pts',(-1.29883575475181,-1.51398324978483,
14.5906679235988));
#25425=CARTESIAN_POINT('Ctrl Pts',(-1.31496007599637,-1.50001512624289,
14.5892962620922));
#25426=CARTESIAN_POINT('Ctrl Pts',(-1.32376507517463,-1.49225044692981,
14.5885382042794));
#25427=CARTESIAN_POINT('Ctrl Pts',(-1.35046317354438,-1.46828451298885,
14.5862115641654));
#25428=CARTESIAN_POINT('Ctrl Pts',(-1.36813064579393,-1.45183630136658,
14.5846327087013));
#25429=CARTESIAN_POINT('Ctrl Pts',(-1.4331246173764,-1.38908767672252,14.5786737839427));
#25430=CARTESIAN_POINT('Ctrl Pts',(-1.47843105091569,-1.34076501709357,
14.5742097383838));
#25431=CARTESIAN_POINT('Ctrl Pts',(-1.64652228988481,-1.14258500881839,
14.5564034332814));
#25432=CARTESIAN_POINT('Ctrl Pts',(-1.74961210300578,-0.977440930746083,
14.542498689194));
#25433=CARTESIAN_POINT('Ctrl Pts',(-1.83204713369569,-0.789158946262437,
14.528982670265));
#25434=CARTESIAN_POINT('Ctrl Pts',(-1.83671218021921,-0.778239632900303,
14.5282069601541));
#25435=CARTESIAN_POINT('Ctrl Pts',(-1.84296713304245,-0.763229295130203,
14.5271523751145));
#25436=CARTESIAN_POINT('Ctrl Pts',(-1.84464133809237,-0.759173988697248,
14.5268686276136));
#25437=CARTESIAN_POINT('Ctrl Pts',(-1.84727939107534,-0.752723772621784,
14.526419199098));
#25438=CARTESIAN_POINT('Ctrl Pts',(-1.848251980349,-0.750332488890405,14.5262529940725));
#25439=CARTESIAN_POINT('Ctrl Pts',(-1.85024561867308,-0.745403378078806,
14.5259112550999));
#25440=CARTESIAN_POINT('Ctrl Pts',(-1.85126608798491,-0.742865342457778,
14.5257357594113));
#25441=CARTESIAN_POINT('Ctrl Pts',(-1.85366524738872,-0.736862685543493,
14.5253217883509));
#25442=CARTESIAN_POINT('Ctrl Pts',(-1.85503945815981,-0.733396261201187,
14.5250835834947));
#25443=CARTESIAN_POINT('Ctrl Pts',(-1.85954682786133,-0.721932771359423,
14.5242985978234));
#25444=CARTESIAN_POINT('Ctrl Pts',(-1.86263811161483,-0.713919185137957,
14.5237542781905));
#25445=CARTESIAN_POINT('Ctrl Pts',(-1.90307943843356,-0.607031516598376,
14.5165495530501));
#25446=CARTESIAN_POINT('Ctrl Pts',(-1.93257125688166,-0.505345141376698,
14.5103221302273));
#25447=CARTESIAN_POINT('Ctrl Pts',(-1.9809808172876,-0.269932199615473,
14.4963264032049));
#25448=CARTESIAN_POINT('Ctrl Pts',(-1.99467621243283,-0.135685087425805,
14.4886207563741));
#25449=CARTESIAN_POINT('Ctrl Pts',(-1.9947497026598,-0.00108914582907106,
14.4805293348879));
#25450=CARTESIAN_POINT('',(-1.99474935791997,0.0016004930108161,13.6790451185598));
#25451=CARTESIAN_POINT('Ctrl Pts',(-1.99474935792054,0.00160049230311827,
13.6790451186048));
#25452=CARTESIAN_POINT('Ctrl Pts',(-1.99480518364989,-0.0679770605314547,
13.6834740389305));
#25453=CARTESIAN_POINT('Ctrl Pts',(-1.99121636699624,-0.137603540603703,
13.6879029592563));
#25454=CARTESIAN_POINT('Ctrl Pts',(-1.98399420179308,-0.20686848419093,
13.692331879582));
#25455=CARTESIAN_POINT('Ctrl Pts',(-1.97677366562195,-0.276117804373161,
13.6967598009202));
#25456=CARTESIAN_POINT('Ctrl Pts',(-1.96592145888067,-0.345005261304889,
13.7011877222584));
#25457=CARTESIAN_POINT('Ctrl Pts',(-1.95150078725994,-0.413124968773165,
13.7056156435966));
#25458=CARTESIAN_POINT('Ctrl Pts',(-1.93707842336549,-0.481252670126485,
13.7100440845538));
#25459=CARTESIAN_POINT('Ctrl Pts',(-1.91908686764915,-0.548611962913746,
13.714472525511));
#25460=CARTESIAN_POINT('Ctrl Pts',(-1.8976401654057,-0.614808397095407,
13.7189009664682));
#25461=CARTESIAN_POINT('Ctrl Pts',(-1.87616885673531,-0.681080780376516,
13.7233344883049));
#25462=CARTESIAN_POINT('Ctrl Pts',(-1.85123464324678,-0.74618717445657,
13.7277680101415));
#25463=CARTESIAN_POINT('Ctrl Pts',(-1.82300076292189,-0.80975044358506,
13.7322015319782));
#25464=CARTESIAN_POINT('Ctrl Pts',(-1.79474856517079,-0.8733549509521,13.7366379301715));
#25465=CARTESIAN_POINT('Ctrl Pts',(-1.76319266460913,-0.9354139038495,13.7410743283648));
#25466=CARTESIAN_POINT('Ctrl Pts',(-1.72854227640487,-0.995574789345876,
13.7455107265581));
#25467=CARTESIAN_POINT('Ctrl Pts',(-1.6938298625014,-1.05584336543912,13.7499550660967));
#25468=CARTESIAN_POINT('Ctrl Pts',(-1.65601217440381,-1.11420668232168,
13.7543994056354));
#25469=CARTESIAN_POINT('Ctrl Pts',(-1.61534124467401,-1.17034192685515,
13.758843745174));
#25470=CARTESIAN_POINT('Ctrl Pts',(-1.5967195602771,-1.19604413760348,13.7608786405844));
#25471=CARTESIAN_POINT('Ctrl Pts',(-1.5775002754825,-1.22127973194823,13.7629135359947));
#25472=CARTESIAN_POINT('Ctrl Pts',(-1.55771020630618,-1.24602025491947,
13.7649484314051));
#25473=CARTESIAN_POINT('Ctrl Pts',(-1.51439312283603,-1.30017303675625,
13.7694024701231));
#25474=CARTESIAN_POINT('Ctrl Pts',(-1.46816300810093,-1.35217153646391,
13.773856508841));
#25475=CARTESIAN_POINT('Ctrl Pts',(-1.41926223182799,-1.40168551387486,
13.778310547559));
#25476=CARTESIAN_POINT('Ctrl Pts',(-1.37043496101952,-1.45112506408476,
13.7827578911648));
#25477=CARTESIAN_POINT('Ctrl Pts',(-1.31894533750337,-1.49808715881457,
13.7872052347706));
#25478=CARTESIAN_POINT('Ctrl Pts',(-1.2650762230469,-1.54227420142509,13.7916525783763));
#25479=CARTESIAN_POINT('Ctrl Pts',(-1.2112706147393,-1.58640915205424,13.7960946790211));
#25480=CARTESIAN_POINT('Ctrl Pts',(-1.15509146360779,-1.6277752391949,13.8005367796659));
#25481=CARTESIAN_POINT('Ctrl Pts',(-1.0968574485791,-1.66611263124572,13.8049788803107));
#25482=CARTESIAN_POINT('Ctrl Pts',(-1.03866016782506,-1.70442583989981,
13.8094181788587));
#25483=CARTESIAN_POINT('Ctrl Pts',(-0.978411002526847,-1.73971387491364,
13.8138574774067));
#25484=CARTESIAN_POINT('Ctrl Pts',(-0.916459356217322,-1.77175895959403,
13.8182967759548));
#25485=CARTESIAN_POINT('Ctrl Pts',(-0.854525737963603,-1.80379471908923,
13.8227347826578));
#25486=CARTESIAN_POINT('Ctrl Pts',(-0.790891056807318,-1.83258917684801,
13.8271727893609));
#25487=CARTESIAN_POINT('Ctrl Pts',(-0.725929612644464,-1.85797033345149,
13.831610796064));
#25488=CARTESIAN_POINT('Ctrl Pts',(-0.660964998985086,-1.88335272841242,
13.8360490192993));
#25489=CARTESIAN_POINT('Ctrl Pts',(-0.594673950661316,-1.90532131564903,
13.8404872425346));
#25490=CARTESIAN_POINT('Ctrl Pts',(-0.527449382701255,-1.92375276768821,
13.8449254657699));
#25491=CARTESIAN_POINT('Ctrl Pts',(-0.460153597730164,-1.94220374581679,
13.8493683908129));
#25492=CARTESIAN_POINT('Ctrl Pts',(-0.39192279228168,-1.95710997979983,
13.8538113158559));
#25493=CARTESIAN_POINT('Ctrl Pts',(-0.323162698535279,-1.96839869761575,
13.858254240899));
#25494=CARTESIAN_POINT('Ctrl Pts',(-0.254362466691924,-1.97969400512093,
13.8626997594602));
#25495=CARTESIAN_POINT('Ctrl Pts',(-0.185032818324061,-1.98736753950208,
13.8671452780215));
#25496=CARTESIAN_POINT('Ctrl Pts',(-0.115584490904185,-1.99139845032641,
13.8715907965827));
#25497=CARTESIAN_POINT('Ctrl Pts',(-0.0460149742143724,-1.99543639520265,
13.876044072698));
#25498=CARTESIAN_POINT('Ctrl Pts',(0.0236731454302083,-1.99581902516095,
13.8804973488132));
#25499=CARTESIAN_POINT('Ctrl Pts',(0.0930700454494838,-1.99257760931413,
13.8849506249284));
#25500=CARTESIAN_POINT('Ctrl Pts',(0.130230089777915,-1.99084192434087,
13.8873352262262));
#25501=CARTESIAN_POINT('Ctrl Pts',(0.167306729918206,-1.98806800686027,
13.889719827524));
#25502=CARTESIAN_POINT('Ctrl Pts',(0.204238144126611,-1.98426670157611,
13.8921044288218));
#25503=CARTESIAN_POINT('Ctrl Pts',(0.273219884993038,-1.97716649537802,
13.8965584675398));
#25504=CARTESIAN_POINT('Ctrl Pts',(0.341967546588619,-1.96645078236383,
13.9010125062578));
#25505=CARTESIAN_POINT('Ctrl Pts',(0.410072255166582,-1.95214454076602,
13.9054665449758));
#25506=CARTESIAN_POINT('Ctrl Pts',(0.478074591785962,-1.93785980367214,
13.9099138885815));
#25507=CARTESIAN_POINT('Ctrl Pts',(0.545435418367895,-1.91999534976437,
13.9143612321873));
#25508=CARTESIAN_POINT('Ctrl Pts',(0.611751383587362,-1.89862787485567,
13.918808575793));
#25509=CARTESIAN_POINT('Ctrl Pts',(0.677989169100425,-1.87728559000353,
13.9232506764378));
#25510=CARTESIAN_POINT('Ctrl Pts',(0.743184076008251,-1.85244863567209,
13.9276927770826));
#25511=CARTESIAN_POINT('Ctrl Pts',(0.806945112391134,-1.82424426765937,
13.9321348777274));
#25512=CARTESIAN_POINT('Ctrl Pts',(0.870665928029795,-1.79605769108694,
13.9365741762754));
#25513=CARTESIAN_POINT('Ctrl Pts',(0.932954220771736,-1.76450811230122,
13.9410134748235));
#25514=CARTESIAN_POINT('Ctrl Pts',(0.993437722011937,-1.72977138806946,
13.9454527733715));
#25515=CARTESIAN_POINT('Ctrl Pts',(1.05390362242961,-1.69504477229547,13.9498907800745));
#25516=CARTESIAN_POINT('Ctrl Pts',(1.11256534963501,-1.65713309593098,13.9543287867776));
#25517=CARTESIAN_POINT('Ctrl Pts',(1.16907564342495,-1.61625793190646,13.9587667934807));
#25518=CARTESIAN_POINT('Ctrl Pts',(1.22558869437612,-1.57538077356533,13.963205016716));
#25519=CARTESIAN_POINT('Ctrl Pts',(1.27994970824177,-1.53154012935786,13.9676432399513));
#25520=CARTESIAN_POINT('Ctrl Pts',(1.33184226767023,-1.48499957459489,13.9720814631866));
#25521=CARTESIAN_POINT('Ctrl Pts',(1.38378980153872,-1.43840971525021,13.9765243882296));
#25522=CARTESIAN_POINT('Ctrl Pts',(1.4332632962628,-1.38911456393194,13.9809673132726));
#25523=CARTESIAN_POINT('Ctrl Pts',(1.47998190000941,-1.33741584338774,13.9854102383157));
#25524=CARTESIAN_POINT('Ctrl Pts',(1.52672777532802,-1.28568694417237,13.9898557568769));
#25525=CARTESIAN_POINT('Ctrl Pts',(1.570715250024,-1.23155206315671,13.9943012754382));
#25526=CARTESIAN_POINT('Ctrl Pts',(1.61170441580573,-1.17534524228939,13.9987467939994));
#25527=CARTESIAN_POINT('Ctrl Pts',(1.65276510882595,-1.11904033895067,14.0032000701147));
#25528=CARTESIAN_POINT('Ctrl Pts',(1.69081678137464,-1.06065668848638,14.0076533462299));
#25529=CARTESIAN_POINT('Ctrl Pts',(1.72566384039382,-1.00055578178192,14.0121066223451));
#25530=CARTESIAN_POINT('Ctrl Pts',(1.7443234384093,-0.96837347455039,14.014491223643));
#25531=CARTESIAN_POINT('Ctrl Pts',(1.76206497861807,-0.935699178638638,
14.0168758249408));
#25532=CARTESIAN_POINT('Ctrl Pts',(1.77886410776198,-0.902590742593891,
14.0192604262386));
#25533=CARTESIAN_POINT('Ctrl Pts',(1.81024208767997,-0.840749689261355,
14.0237144649566));
#25534=CARTESIAN_POINT('Ctrl Pts',(1.83845356975254,-0.777147961615591,
14.0281685036746));
#25535=CARTESIAN_POINT('Ctrl Pts',(1.86329818552637,-0.712142846846149,
14.0326225423925));
#25536=CARTESIAN_POINT('Ctrl Pts',(1.88810545598251,-0.647235444864242,
14.0370698859983));
#25537=CARTESIAN_POINT('Ctrl Pts',(1.90955573146319,-0.580929296182433,
14.041517229604));
#25538=CARTESIAN_POINT('Ctrl Pts',(1.92749511536451,-0.513605045483351,
14.0459645732098));
#25539=CARTESIAN_POINT('Ctrl Pts',(1.94541335057622,-0.446360163155503,
14.0504066738546));
#25540=CARTESIAN_POINT('Ctrl Pts',(1.95982878930143,-0.378100033405074,
14.0548487744994));
#25541=CARTESIAN_POINT('Ctrl Pts',(1.97063673515249,-0.309222283426575,
14.0592908751442));
#25542=CARTESIAN_POINT('Ctrl Pts',(1.98143786330341,-0.240387981837958,
14.0637301736922));
#25543=CARTESIAN_POINT('Ctrl Pts',(1.98863593717698,-0.170937315413736,
14.0681694722402));
#25544=CARTESIAN_POINT('Ctrl Pts',(1.99217725904039,-0.101278482721227,
14.0726087707882));
#25545=CARTESIAN_POINT('Ctrl Pts',(1.9957175503719,-0.031639920891463,14.0770467774913));
#25546=CARTESIAN_POINT('Ctrl Pts',(1.99560317730049,0.0382061982726219,
14.0814847841943));
#25547=CARTESIAN_POINT('Ctrl Pts',(1.99183241814654,0.107847950933335,14.0859227908974));
#25548=CARTESIAN_POINT('Ctrl Pts',(1.98806147501563,0.177493101445062,14.0903610141327));
#25549=CARTESIAN_POINT('Ctrl Pts',(1.98063382047608,0.246933376942141,14.094799237368));
#25550=CARTESIAN_POINT('Ctrl Pts',(1.96959974535076,0.315760044360018,14.0992374606033));
#25551=CARTESIAN_POINT('Ctrl Pts',(1.95855398084057,0.384659626036245,14.1036803856464));
#25552=CARTESIAN_POINT('Ctrl Pts',(1.94389424765023,0.452943817812173,14.1081233106894));
#25553=CARTESIAN_POINT('Ctrl Pts',(1.9257221649402,0.520213135126373,14.1125662357324));
#25554=CARTESIAN_POINT('Ctrl Pts',(1.90753947443753,0.587521720309926,14.1170117542937));
#25555=CARTESIAN_POINT('Ctrl Pts',(1.88584050586163,0.653813786467538,14.1214572728549));
#25556=CARTESIAN_POINT('Ctrl Pts',(1.86077621830273,0.718706774629961,14.1259027914162));
#25557=CARTESIAN_POINT('Ctrl Pts',(1.83566819286234,0.783713002868256,14.1303560675314));
#25558=CARTESIAN_POINT('Ctrl Pts',(1.80718332580817,0.847314832827739,14.1348093436466));
#25559=CARTESIAN_POINT('Ctrl Pts',(1.77551964692295,0.909152102725731,14.1392626197619));
#25560=CARTESIAN_POINT('Ctrl Pts',(1.7585646574255,0.942264182515052,14.1416472210597));
#25561=CARTESIAN_POINT('Ctrl Pts',(1.74069897737165,0.974870766796611,14.1440318223575));
#25562=CARTESIAN_POINT('Ctrl Pts',(1.72195805822019,1.00692006049663,14.1464164236553));
#25563=CARTESIAN_POINT('Ctrl Pts',(1.68695313744456,1.06678281204141,14.1508704623733));
#25564=CARTESIAN_POINT('Ctrl Pts',(1.64875353704919,1.12493655663194,14.1553245010913));
#25565=CARTESIAN_POINT('Ctrl Pts',(1.60755116707231,1.1810193934667,14.1597785398093));
#25566=CARTESIAN_POINT('Ctrl Pts',(1.5664107306592,1.237017929084,14.164225883415));
#25567=CARTESIAN_POINT('Ctrl Pts',(1.52227677058713,1.29095134395445,14.1686732270208));
#25568=CARTESIAN_POINT('Ctrl Pts',(1.47538599529214,1.34248416281006,14.1731205706265));
#25569=CARTESIAN_POINT('Ctrl Pts',(1.42855049940136,1.39395622976926,14.1775626712713));
#25570=CARTESIAN_POINT('Ctrl Pts',(1.3789649710888,1.44303296121249,14.1820047719161));
#25571=CARTESIAN_POINT('Ctrl Pts',(1.32690703454506,1.48941105279061,14.1864468725609));
#25572=CARTESIAN_POINT('Ctrl Pts',(1.27488193637831,1.53575988886311,14.1908861711089));
#25573=CARTESIAN_POINT('Ctrl Pts',(1.22038788856991,1.57941313716979,14.1953254696569));
#25574=CARTESIAN_POINT('Ctrl Pts',(1.16373901454757,1.62010464739777,14.199764768205));
#25575=CARTESIAN_POINT('Ctrl Pts',(1.10710662546348,1.66078431631302,14.204202774908));
#25576=CARTESIAN_POINT('Ctrl Pts',(1.04832105238655,1.69850367263701,14.2086407816111));
#25577=CARTESIAN_POINT('Ctrl Pts',(0.987727691244489,1.73303824840909,14.2130787883141));
#25578=CARTESIAN_POINT('Ctrl Pts',(0.927131373726373,1.76757450913791,14.2175170115495));
#25579=CARTESIAN_POINT('Ctrl Pts',(0.864727519542407,1.79892544048044,14.2219552347848));
#25580=CARTESIAN_POINT('Ctrl Pts',(0.800887002138789,1.82691203190114,14.2263934580201));
#25581=CARTESIAN_POINT('Ctrl Pts',(0.736978852752398,1.85492827202685,14.2308363830631));
#25582=CARTESIAN_POINT('Ctrl Pts',(0.671631451598135,1.87957286141456,14.2352793081061));
#25583=CARTESIAN_POINT('Ctrl Pts',(0.605235686143643,1.90071495146385,14.2397222331492));
#25584=CARTESIAN_POINT('Ctrl Pts',(0.538801162747885,1.92186938302135,14.2441677517104));
#25585=CARTESIAN_POINT('Ctrl Pts',(0.471317530766223,1.93951712189295,14.2486132702717));
#25586=CARTESIAN_POINT('Ctrl Pts',(0.403188160569807,1.9535779661115,14.2530587888329));
#25587=CARTESIAN_POINT('Ctrl Pts',(0.334939902720654,1.96766334689569,14.2575120649482));
#25588=CARTESIAN_POINT('Ctrl Pts',(0.266044141236429,1.97814926482375,14.2619653410634));
#25589=CARTESIAN_POINT('Ctrl Pts',(0.196910900515753,1.98500721906951,14.2664186171786));
#25590=CARTESIAN_POINT('Ctrl Pts',(0.159892038159701,1.98867945635539,14.2688032184764));
#25591=CARTESIAN_POINT('Ctrl Pts',(0.122805116298964,1.99131234244859,14.2711878197742));
#25592=CARTESIAN_POINT('Ctrl Pts',(0.0857128758712415,1.99290764096329,
14.273572421072));
#25593=CARTESIAN_POINT('Ctrl Pts',(0.0164307383689842,1.99588739332601,
14.27802645979));
#25594=CARTESIAN_POINT('Ctrl Pts',(-0.0531441760713303,1.99525591815407,
14.282480498508));
#25595=CARTESIAN_POINT('Ctrl Pts',(-0.122603694260102,1.99097862787469,
14.286934537226));
#25596=CARTESIAN_POINT('Ctrl Pts',(-0.191958804001189,1.98670776702715,
14.2913818808318));
#25597=CARTESIAN_POINT('Ctrl Pts',(-0.261198377109999,1.97880199780628,
14.2958292244375));
#25598=CARTESIAN_POINT('Ctrl Pts',(-0.329912203479769,1.96727870432614,
14.3002765680433));
#25599=CARTESIAN_POINT('Ctrl Pts',(-0.398545023311044,1.95576899562458,
14.3047186686881));
#25600=CARTESIAN_POINT('Ctrl Pts',(-0.466652846918377,1.94065031345129,
14.3091607693329));
#25601=CARTESIAN_POINT('Ctrl Pts',(-0.533830359862819,1.92199185986537,
14.3136028699777));
#25602=CARTESIAN_POINT('Ctrl Pts',(-0.600965496934571,1.9033451761146,14.3180421685257));
#25603=CARTESIAN_POINT('Ctrl Pts',(-0.667171016897516,1.88116328122908,
14.3224814670737));
#25604=CARTESIAN_POINT('Ctrl Pts',(-0.732053081728854,1.85556617991148,
14.3269207656218));
#25605=CARTESIAN_POINT('Ctrl Pts',(-0.79691626574654,1.82997652740275,14.3313587723248));
#25606=CARTESIAN_POINT('Ctrl Pts',(-0.860456304003943,1.80097382094747,
14.3357967790279));
#25607=CARTESIAN_POINT('Ctrl Pts',(-0.922297471927478,1.76872692515724,
14.340234785731));
#25608=CARTESIAN_POINT('Ctrl Pts',(-0.984141657108056,1.73647845602717,
14.3446730089663));
#25609=CARTESIAN_POINT('Ctrl Pts',(-1.04428637440759,1.70098571178254,14.3491112322016));
#25610=CARTESIAN_POINT('Ctrl Pts',(-1.10238032409432,1.66246358863877,14.3535494554369));
#25611=CARTESIAN_POINT('Ctrl Pts',(-1.16053581790957,1.62390065555679,14.3579923804799));
#25612=CARTESIAN_POINT('Ctrl Pts',(-1.21663579895897,1.58230220907177,14.362435305523));
#25613=CARTESIAN_POINT('Ctrl Pts',(-1.27035862419177,1.53792604778045,14.366878230566));
#25614=CARTESIAN_POINT('Ctrl Pts',(-1.3241128096489,1.49352398229725,14.3713237491272));
#25615=CARTESIAN_POINT('Ctrl Pts',(-1.37548671666606,1.44634130591597,14.3757692676885));
#25616=CARTESIAN_POINT('Ctrl Pts',(-1.42419452533855,1.39667373301559,14.3802147862498));
#25617=CARTESIAN_POINT('Ctrl Pts',(-1.47298733049687,1.34691948881401,14.384668062365));
#25618=CARTESIAN_POINT('Ctrl Pts',(-1.51910442631869,1.29467205922888,14.3891213384802));
#25619=CARTESIAN_POINT('Ctrl Pts',(-1.56229985845326,1.24026074467304,14.3935746145955));
#25620=CARTESIAN_POINT('Ctrl Pts',(-1.58542977019919,1.21112505042334,14.3959592158932));
#25621=CARTESIAN_POINT('Ctrl Pts',(-1.60772268783294,1.18136941758474,14.398343817191));
#25622=CARTESIAN_POINT('Ctrl Pts',(-1.62914612543946,1.15104755091421,14.4007284184888));
#25623=CARTESIAN_POINT('Ctrl Pts',(-1.66957974506708,1.09381944187431,14.4052290062846));
#25624=CARTESIAN_POINT('Ctrl Pts',(-1.70707223248772,1.03434819745607,14.4097295940805));
#25625=CARTESIAN_POINT('Ctrl Pts',(-1.74136940073319,0.972964630749814,
14.4142301818764));
#25626=CARTESIAN_POINT('Ctrl Pts',(-1.77561242103956,0.911677975648865,
14.4187236642007));
#25627=CARTESIAN_POINT('Ctrl Pts',(-1.80666990660374,0.848485403704244,
14.423217146525));
#25628=CARTESIAN_POINT('Ctrl Pts',(-1.83433017896719,0.783747636060353,
14.4277106288492));
#25629=CARTESIAN_POINT('Ctrl Pts',(-1.8619505888703,0.719103164919873,14.4321976354144));
#25630=CARTESIAN_POINT('Ctrl Pts',(-1.88618333064802,0.652918359543348,
14.4366846419796));
#25631=CARTESIAN_POINT('Ctrl Pts',(-1.90686288451596,0.585577921506146,
14.4411716485448));
#25632=CARTESIAN_POINT('Ctrl Pts',(-1.92752471738716,0.51829518972756,14.445654810045));
#25633=CARTESIAN_POINT('Ctrl Pts',(-1.9446392685461,0.449859245091323,14.4501379715452));
#25634=CARTESIAN_POINT('Ctrl Pts',(-1.958089803987,0.380672933135736,14.4546211330453));
#25635=CARTESIAN_POINT('Ctrl Pts',(-1.97153482224691,0.311515000229131,
14.4591024556289));
#25636=CARTESIAN_POINT('Ctrl Pts',(-1.98131871235937,0.241607776836367,
14.4635837782125));
#25637=CARTESIAN_POINT('Ctrl Pts',(-1.98737547173003,0.171365973477396,
14.468065100796));
#25638=CARTESIAN_POINT('Ctrl Pts',(-1.99232217548495,0.113997771908761,
14.4717251067323));
#25639=CARTESIAN_POINT('Ctrl Pts',(-1.99478366955174,0.056406735287098,
14.4753851126685));
#25640=CARTESIAN_POINT('Ctrl Pts',(-1.99474965194692,-0.00117837076332067,
14.4790451186048));
#25641=CARTESIAN_POINT('',(-1.99502628289053,0.000403632376691979,12.8790451529297));
#25642=CARTESIAN_POINT('Ctrl Pts',(-1.99474995918462,0.000403525672960359,
12.879045156187));
#25643=CARTESIAN_POINT('Ctrl Pts',(-1.99476391393369,-0.0685790372895848,
12.8834750243028));
#25644=CARTESIAN_POINT('Ctrl Pts',(-1.99119525037218,-0.137704781892064,
12.8879048924186));
#25645=CARTESIAN_POINT('Ctrl Pts',(-1.98402549375135,-0.206568154962712,
12.8923347605343));
#25646=CARTESIAN_POINT('Ctrl Pts',(-1.97662908922472,-0.277608413542726,
12.8969046641331));
#25647=CARTESIAN_POINT('Ctrl Pts',(-1.96539997991584,-0.348368906523431,
12.9014745677318));
#25648=CARTESIAN_POINT('Ctrl Pts',(-1.95037610598785,-0.41840244704314,
12.9060444713306));
#25649=CARTESIAN_POINT('Ctrl Pts',(-1.93585123391419,-0.486109898649093,
12.9104625904841));
#25650=CARTESIAN_POINT('Ctrl Pts',(-1.91777983112837,-0.553137400773518,
12.9148807096376));
#25651=CARTESIAN_POINT('Ctrl Pts',(-1.89624871509232,-0.619086724951126,
12.9192988287911));
#25652=CARTESIAN_POINT('Ctrl Pts',(-1.87473021050309,-0.684997420550787,
12.9237143601143));
#25653=CARTESIAN_POINT('Ctrl Pts',(-1.84975616507364,-0.749830720662124,
12.9281298914375));
#25654=CARTESIAN_POINT('Ctrl Pts',(-1.82146361149838,-0.813202234679232,
12.9325454227606));
#25655=CARTESIAN_POINT('Ctrl Pts',(-1.79317774934347,-0.876558760814886,
12.9369599097746));
#25656=CARTESIAN_POINT('Ctrl Pts',(-1.76157513909554,-0.938453734973087,
12.9413743967885));
#25657=CARTESIAN_POINT('Ctrl Pts',(-1.7268407424001,-0.998523215998043,
12.9457888838024));
#25658=CARTESIAN_POINT('Ctrl Pts',(-1.69210243074373,-1.05859946753562,
12.9502038683791));
#25659=CARTESIAN_POINT('Ctrl Pts',(-1.65423188280755,-1.11684939032358,
12.9546188529558));
#25660=CARTESIAN_POINT('Ctrl Pts',(-1.61345881382973,-1.172935726532,12.9590338375325));
#25661=CARTESIAN_POINT('Ctrl Pts',(-1.57264128067329,-1.22908322646772,
12.9634536367741));
#25662=CARTESIAN_POINT('Ctrl Pts',(-1.52891520507429,-1.2830620325987,12.9678734360157));
#25663=CARTESIAN_POINT('Ctrl Pts',(-1.48255157511328,-1.33456674229097,
12.9722932352573));
#25664=CARTESIAN_POINT('Ctrl Pts',(-1.4361574262443,-1.38610535501234,12.9767159438364));
#25665=CARTESIAN_POINT('Ctrl Pts',(-1.38712262046823,-1.43516628284959,
12.9811386524155));
#25666=CARTESIAN_POINT('Ctrl Pts',(-1.33575408848825,-1.48148188567627,
12.9855613609945));
#25667=CARTESIAN_POINT('Ctrl Pts',(-1.2843006711123,-1.527874024042,12.9899913780045));
#25668=CARTESIAN_POINT('Ctrl Pts',(-1.23050622131947,-1.57151148022315,
12.9944213950146));
#25669=CARTESIAN_POINT('Ctrl Pts',(-1.17470881658145,-1.61216834069703,
12.9988514120246));
#25670=CARTESIAN_POINT('Ctrl Pts',(-1.16143741963982,-1.62183856346604,
12.9999050903179));
#25671=CARTESIAN_POINT('Ctrl Pts',(-1.14805282609176,-1.63134036776859,
13.0009587686113));
#25672=CARTESIAN_POINT('Ctrl Pts',(-1.13455979011492,-1.64067109597091,
13.0020124469047));
#25673=CARTESIAN_POINT('Ctrl Pts',(-1.07752292692536,-1.68011332890113,
13.0064664856227));
#25674=CARTESIAN_POINT('Ctrl Pts',(-1.01831387977906,-1.71665585503574,
13.0109205243406));
#25675=CARTESIAN_POINT('Ctrl Pts',(-0.957259602578503,-1.75005188945107,
13.0153745630586));
#25676=CARTESIAN_POINT('Ctrl Pts',(-0.896297099442749,-1.78339772443784,
13.0198219066644));
#25677=CARTESIAN_POINT('Ctrl Pts',(-0.833495297299515,-1.81360622189784,
13.0242692502701));
#25678=CARTESIAN_POINT('Ctrl Pts',(-0.769210569644161,-1.84047348854791,
13.0287165938759));
#25679=CARTESIAN_POINT('Ctrl Pts',(-0.705001627074957,-1.86730908145225,
13.0331586945207));
#25680=CARTESIAN_POINT('Ctrl Pts',(-0.639313680689665,-1.8908110789602,
13.0376007951655));
#25681=CARTESIAN_POINT('Ctrl Pts',(-0.572526575468782,-1.91082204375028,
13.0420428958103));
#25682=CARTESIAN_POINT('Ctrl Pts',(-0.505781599849651,-1.93082038553514,
13.0464821943583));
#25683=CARTESIAN_POINT('Ctrl Pts',(-0.437939308724834,-1.94733192299265,
13.0509214929063));
#25684=CARTESIAN_POINT('Ctrl Pts',(-0.369396909037524,-1.96024832255853,
13.0553607914543));
#25685=CARTESIAN_POINT('Ctrl Pts',(-0.300874455328736,-1.97316096342571,
13.0597987981574));
#25686=CARTESIAN_POINT('Ctrl Pts',(-0.231652778346969,-1.98248045264572,
13.0642368048605));
#25687=CARTESIAN_POINT('Ctrl Pts',(-0.162139795614553,-1.98814945343102,
13.0686748115635));
#25688=CARTESIAN_POINT('Ctrl Pts',(-0.0926234213143076,-1.99381873080927,
13.0731130347988));
#25689=CARTESIAN_POINT('Ctrl Pts',(-0.0228162011802754,-1.99583712873204,
13.0775512580341));
#25690=CARTESIAN_POINT('Ctrl Pts',(0.0468700844463606,-1.99419927732511,
13.0819894812694));
#25691=CARTESIAN_POINT('Ctrl Pts',(0.116630195002359,-1.99255969079536,
13.0864324063125));
#25692=CARTESIAN_POINT('Ctrl Pts',(0.186268624934378,-1.98725613535523,
13.0908753313555));
#25693=CARTESIAN_POINT('Ctrl Pts',(0.255375825712517,-1.97833534825157,
13.0953182563985));
#25694=CARTESIAN_POINT('Ctrl Pts',(0.324523367208244,-1.96940935371729,
13.0997637749598));
#25695=CARTESIAN_POINT('Ctrl Pts',(0.393138580608946,-1.95686201285637,
13.104209293521));
#25696=CARTESIAN_POINT('Ctrl Pts',(0.46082202448935,-1.94079123664693,13.1086548120823));
#25697=CARTESIAN_POINT('Ctrl Pts',(0.528623577868769,-1.92469241648439,
13.1131080881975));
#25698=CARTESIAN_POINT('Ctrl Pts',(0.595489646332659,-1.9050580253944,13.1175613643127));
#25699=CARTESIAN_POINT('Ctrl Pts',(0.661036623490899,-1.88203563858492,
13.122014640428));
#25700=CARTESIAN_POINT('Ctrl Pts',(0.696135144838806,-1.86970781249828,
13.1243992417258));
#25701=CARTESIAN_POINT('Ctrl Pts',(0.730855791739241,-1.85640937119444,
13.1267838430236));
#25702=CARTESIAN_POINT('Ctrl Pts',(0.765142455865676,-1.84216844635116,
13.1291684443214));
#25703=CARTESIAN_POINT('Ctrl Pts',(0.829184243341866,-1.81556876669395,
13.1336224830394));
#25704=CARTESIAN_POINT('Ctrl Pts',(0.891964126641946,-1.78557287142334,
13.1380765217574));
#25705=CARTESIAN_POINT('Ctrl Pts',(0.953097602768725,-1.75232203721134,
13.1425305604753));
#25706=CARTESIAN_POINT('Ctrl Pts',(1.01413918578238,-1.71912118416945,13.1469779040811));
#25707=CARTESIAN_POINT('Ctrl Pts',(1.07353884693997,-1.68267533494663,13.1514252476868));
#25708=CARTESIAN_POINT('Ctrl Pts',(1.13093221659763,-1.64317372300118,13.1558725912926));
#25709=CARTESIAN_POINT('Ctrl Pts',(1.188257925372,-1.6037186793958,13.1603146919374));
#25710=CARTESIAN_POINT('Ctrl Pts',(1.24358163892513,-1.56121530416657,13.1647567925822));
#25711=CARTESIAN_POINT('Ctrl Pts',(1.2965653380723,-1.5158977164075,13.1691988932269));
#25712=CARTESIAN_POINT('Ctrl Pts',(1.34951561486733,-1.47060871518354,13.173638191775));
#25713=CARTESIAN_POINT('Ctrl Pts',(1.40012843430692,-1.42250934052396,13.178077490323));
#25714=CARTESIAN_POINT('Ctrl Pts',(1.44809766158735,-1.37187489407936,13.182516788871));
#25715=CARTESIAN_POINT('Ctrl Pts',(1.49605292972452,-1.32125518236226,13.1869547955741));
#25716=CARTESIAN_POINT('Ctrl Pts',(1.54136579634628,-1.26810221855024,13.1913928022771));
#25717=CARTESIAN_POINT('Ctrl Pts',(1.58376720373819,-1.21272791955298,13.1958308089802));
#25718=CARTESIAN_POINT('Ctrl Pts',(1.62617067991297,-1.1573509188199,13.2002690322155));
#25719=CARTESIAN_POINT('Ctrl Pts',(1.66566211909979,-1.09975275787685,13.2047072554508));
#25720=CARTESIAN_POINT('Ctrl Pts',(1.70201406378162,-1.04027673682995,13.2091454786861));
#25721=CARTESIAN_POINT('Ctrl Pts',(1.73840451933701,-0.980737707502589,
13.2135884037292));
#25722=CARTESIAN_POINT('Ctrl Pts',(1.77164858613558,-0.919317265902124,
13.2180313287722));
#25723=CARTESIAN_POINT('Ctrl Pts',(1.80156382444342,-0.856385047135232,
13.2224742538152));
#25724=CARTESIAN_POINT('Ctrl Pts',(1.8314965255072,-0.793416092241892,13.2269197723765));
#25725=CARTESIAN_POINT('Ctrl Pts',(1.85809634366653,-0.728934056397803,
13.2313652909377));
#25726=CARTESIAN_POINT('Ctrl Pts',(1.88122933599327,-0.663327783149731,
13.235810809499));
#25727=CARTESIAN_POINT('Ctrl Pts',(1.90440269603738,-0.597607025123411,
13.2402640856142));
#25728=CARTESIAN_POINT('Ctrl Pts',(1.92409701561062,-0.5307585830934,13.2447173617295));
#25729=CARTESIAN_POINT('Ctrl Pts',(1.94022868063529,-0.463184875983908,
13.2491706378447));
#25730=CARTESIAN_POINT('Ctrl Pts',(1.94886672336118,-0.427001099029362,
13.2515552391425));
#25731=CARTESIAN_POINT('Ctrl Pts',(1.95648412833892,-0.390609520282348,
13.2539398404403));
#25732=CARTESIAN_POINT('Ctrl Pts',(1.96307416977555,-0.354072544064099,
13.2563244417381));
#25733=CARTESIAN_POINT('Ctrl Pts',(1.97538327140143,-0.285827547777349,
13.2607784804561));
#25734=CARTESIAN_POINT('Ctrl Pts',(1.98415376933049,-0.216804755553798,
13.2652325191741));
#25735=CARTESIAN_POINT('Ctrl Pts',(1.98929626850988,-0.147403930044804,
13.2696865578921));
#25736=CARTESIAN_POINT('Ctrl Pts',(1.99443103771401,-0.0781074247595321,
13.2741339014978));
#25737=CARTESIAN_POINT('Ctrl Pts',(1.995948596023,-0.00843449825290857,
13.2785812451036));
#25738=CARTESIAN_POINT('Ctrl Pts',(1.99381076884887,0.0612060497197463,
13.2830285887093));
#25739=CARTESIAN_POINT('Ctrl Pts',(1.99167546195322,0.130764498644711,13.2874706893541));
#25740=CARTESIAN_POINT('Ctrl Pts',(1.98589334338283,0.200290157879424,13.2919127899989));
#25741=CARTESIAN_POINT('Ctrl Pts',(1.97647824293634,0.269372080400441,13.2963548906437));
#25742=CARTESIAN_POINT('Ctrl Pts',(1.96706908157691,0.338410425738792,13.3007941891917));
#25743=CARTESIAN_POINT('Ctrl Pts',(1.95403155050615,0.407005105691801,13.3052334877398));
#25744=CARTESIAN_POINT('Ctrl Pts',(1.93743136664856,0.474749683545216,13.3096727862878));
#25745=CARTESIAN_POINT('Ctrl Pts',(1.92083601347846,0.542474547587803,13.3141107929909));
#25746=CARTESIAN_POINT('Ctrl Pts',(1.90068018206833,0.609349325371707,13.3185487996939));
#25747=CARTESIAN_POINT('Ctrl Pts',(1.87708044787254,0.674978929089375,13.322986806397));
#25748=CARTESIAN_POINT('Ctrl Pts',(1.85347956223567,0.740611734903338,13.3274250296323));
#25749=CARTESIAN_POINT('Ctrl Pts',(1.82643460811985,0.804998786162914,13.3318632528676));
#25750=CARTESIAN_POINT('Ctrl Pts',(1.79611106947771,0.867762979505146,13.3363014761029));
#25751=CARTESIAN_POINT('Ctrl Pts',(1.76575540639279,0.930593664583754,13.3407444011459));
#25752=CARTESIAN_POINT('Ctrl Pts',(1.73211443963886,0.991797618537426,13.3451873261889));
#25753=CARTESIAN_POINT('Ctrl Pts',(1.69540016767943,1.05102132896177,13.349630251232));
#25754=CARTESIAN_POINT('Ctrl Pts',(1.65866446408825,1.11027961070361,13.3540757697932));
#25755=CARTESIAN_POINT('Ctrl Pts',(1.61885216401748,1.16755494602156,13.3585212883545));
#25756=CARTESIAN_POINT('Ctrl Pts',(1.57621767231628,1.22252419688849,13.3629668069157));
#25757=CARTESIAN_POINT('Ctrl Pts',(1.53350878223693,1.27758937063264,13.367420083031));
#25758=CARTESIAN_POINT('Ctrl Pts',(1.48796818962266,1.33034005640665,13.3718733591462));
#25759=CARTESIAN_POINT('Ctrl Pts',(1.43988896155922,1.38048808067288,13.3763266352614));
#25760=CARTESIAN_POINT('Ctrl Pts',(1.4141439175352,1.40734090557158,13.3787112365593));
#25761=CARTESIAN_POINT('Ctrl Pts',(1.38767157722307,1.43344812795739,13.3810958378571));
#25762=CARTESIAN_POINT('Ctrl Pts',(1.3605207661014,1.45877030663051,13.3834804391549));
#25763=CARTESIAN_POINT('Ctrl Pts',(1.3098075655041,1.50606792587494,13.3879344778729));
#25764=CARTESIAN_POINT('Ctrl Pts',(1.2565245851602,1.55081154537459,13.3923885165908));
#25765=CARTESIAN_POINT('Ctrl Pts',(1.20095952898562,1.59270956933103,13.3968425553088));
#25766=CARTESIAN_POINT('Ctrl Pts',(1.14547799572374,1.63454461404768,13.4012898989146));
#25767=CARTESIAN_POINT('Ctrl Pts',(1.08772158265844,1.67354226040037,13.4057372425203));
#25768=CARTESIAN_POINT('Ctrl Pts',(1.02801332308524,1.70944908378672,13.4101845861261));
#25769=CARTESIAN_POINT('Ctrl Pts',(0.968375453412641,1.74531357671917,13.4146266867709));
#25770=CARTESIAN_POINT('Ctrl Pts',(0.906790724876314,1.77809423257428,13.4190687874157));
#25771=CARTESIAN_POINT('Ctrl Pts',(0.84361213189459,1.80758018727255,13.4235108880605));
#25772=CARTESIAN_POINT('Ctrl Pts',(0.780473392249227,1.83704754209996,13.4279501866085));
#25773=CARTESIAN_POINT('Ctrl Pts',(0.715743225269266,1.86322411210079,13.4323894851565));
#25774=CARTESIAN_POINT('Ctrl Pts',(0.649798925601301,1.88594509962178,13.4368287837045));
#25775=CARTESIAN_POINT('Ctrl Pts',(0.583873815859491,1.9086594752889,13.4412667904076));
#25776=CARTESIAN_POINT('Ctrl Pts',(0.51673573743669,1.9279201053192,13.4457047971106));
#25777=CARTESIAN_POINT('Ctrl Pts',(0.448779978711364,1.94361109618355,13.4501428038137));
#25778=CARTESIAN_POINT('Ctrl Pts',(0.38082090439542,1.95930285261808,13.454581027049));
#25779=CARTESIAN_POINT('Ctrl Pts',(0.312044548118415,1.97142451629559,13.4590192502843));
#25780=CARTESIAN_POINT('Ctrl Pts',(0.242857557342055,1.97991105086614,13.4634574735196));
#25781=CARTESIAN_POINT('Ctrl Pts',(0.173597270584371,1.9884065759835,13.4679003985627));
#25782=CARTESIAN_POINT('Ctrl Pts',(0.103925967932314,1.99325922582369,13.4723433236057));
#25783=CARTESIAN_POINT('Ctrl Pts',(0.0342556460789304,1.99445584388618,
13.4767862486487));
#25784=CARTESIAN_POINT('Ctrl Pts',(-0.0354553452089624,1.99565316046387,
13.48123176721));
#25785=CARTESIAN_POINT('Ctrl Pts',(-0.105164865154026,1.99319021472127,
13.4856772857712));
#25786=CARTESIAN_POINT('Ctrl Pts',(-0.174463495229841,1.98710594869327,
13.4901228043325));
#25787=CARTESIAN_POINT('Ctrl Pts',(-0.243883053349606,1.98101106545121,
13.4945760804477));
#25788=CARTESIAN_POINT('Ctrl Pts',(-0.312889805594576,1.97128231579446,
13.4990293565629));
#25789=CARTESIAN_POINT('Ctrl Pts',(-0.381082797903004,1.95801007751299,
13.5034826326782));
#25790=CARTESIAN_POINT('Ctrl Pts',(-0.417598184273228,1.95090317558011,
13.505867233976));
#25791=CARTESIAN_POINT('Ctrl Pts',(-0.453880466547818,1.94278111578831,
13.5082518352738));
#25792=CARTESIAN_POINT('Ctrl Pts',(-0.489870049548812,1.93366359459319,
13.5106364365716));
#25793=CARTESIAN_POINT('Ctrl Pts',(-0.557092606324624,1.91663358104241,
13.5150904752896));
#25794=CARTESIAN_POINT('Ctrl Pts',(-0.623559177798799,1.8960602401195,13.5195445140076));
#25795=CARTESIAN_POINT('Ctrl Pts',(-0.688868836301772,1.87202758763653,
13.5239985527256));
#25796=CARTESIAN_POINT('Ctrl Pts',(-0.754080324240724,1.84803105996424,
13.5284458963313));
#25797=CARTESIAN_POINT('Ctrl Pts',(-0.818137895034203,1.8205857088959,13.5328932399371));
#25798=CARTESIAN_POINT('Ctrl Pts',(-0.880653585988228,1.78982592002297,
13.5373405835429));
#25799=CARTESIAN_POINT('Ctrl Pts',(-0.943095577368579,1.75910239377934,
13.5417826841876));
#25800=CARTESIAN_POINT('Ctrl Pts',(-1.00399886197858,1.72507240537356,13.5462247848324));
#25801=CARTESIAN_POINT('Ctrl Pts',(-1.06299503889724,1.6879185732078,13.5506668854772));
#25802=CARTESIAN_POINT('Ctrl Pts',(-1.12195400076611,1.65078817784398,13.5551061840252));
#25803=CARTESIAN_POINT('Ctrl Pts',(-1.17900782814711,1.61053810808701,13.5595454825733));
#25804=CARTESIAN_POINT('Ctrl Pts',(-1.2338136943822,1.56739635384766,13.5639847811213));
#25805=CARTESIAN_POINT('Ctrl Pts',(-1.28860361199807,1.52426715394708,13.5684227878243));
#25806=CARTESIAN_POINT('Ctrl Pts',(-1.34114648260044,1.47824824270036,13.5728607945274));
#25807=CARTESIAN_POINT('Ctrl Pts',(-1.39113085402196,1.42960921565585,13.5772988012305));
#25808=CARTESIAN_POINT('Ctrl Pts',(-1.44111766420226,1.38096781549248,13.5817370244658));
#25809=CARTESIAN_POINT('Ctrl Pts',(-1.48854537817484,1.32970638886034,13.5861752477011));
#25810=CARTESIAN_POINT('Ctrl Pts',(-1.53313915238611,1.27613161622177,13.5906134709364));
#25811=CARTESIAN_POINT('Ctrl Pts',(-1.57778016877996,1.22250008702391,13.5950563959794));
#25812=CARTESIAN_POINT('Ctrl Pts',(-1.61958093925338,1.16655069729056,13.5994993210224));
#25813=CARTESIAN_POINT('Ctrl Pts',(-1.65830734248925,1.10862271325561,13.6039422460654));
#25814=CARTESIAN_POINT('Ctrl Pts',(-1.69705635192068,1.05066091427206,13.6083877646267));
#25815=CARTESIAN_POINT('Ctrl Pts',(-1.73272717166764,0.990718642949719,
13.6128332831879));
#25816=CARTESIAN_POINT('Ctrl Pts',(-1.76513087849859,0.929161204673771,
13.6172788017492));
#25817=CARTESIAN_POINT('Ctrl Pts',(-1.79759113070251,0.867496346949635,
13.6217320778644));
#25818=CARTESIAN_POINT('Ctrl Pts',(-1.82677268438971,0.804211140544934,
13.6261853539796));
#25819=CARTESIAN_POINT('Ctrl Pts',(-1.85253444408813,0.739691622209618,
13.6306386300949));
#25820=CARTESIAN_POINT('Ctrl Pts',(-1.86632912558135,0.70514327551471,13.6330232313927));
#25821=CARTESIAN_POINT('Ctrl Pts',(-1.87914410014879,0.670241294351013,
13.6354078326905));
#25822=CARTESIAN_POINT('Ctrl Pts',(-1.89096366219834,0.635046447707129,
13.6377924339883));
#25823=CARTESIAN_POINT('Ctrl Pts',(-1.91713820822316,0.557107085025591,
13.6430731589559));
#25824=CARTESIAN_POINT('Ctrl Pts',(-1.93851310398558,0.477479571807927,
13.6483538839235));
#25825=CARTESIAN_POINT('Ctrl Pts',(-1.95490359300059,0.396710857644933,
13.653634608891));
#25826=CARTESIAN_POINT('Ctrl Pts',(-1.97111438693516,0.316827641198072,
13.6588574392895));
#25827=CARTESIAN_POINT('Ctrl Pts',(-1.98244939795434,0.23582820185453,13.6640802696881));
#25828=CARTESIAN_POINT('Ctrl Pts',(-1.98877616824338,0.154262487751171,
13.6693031000866));
#25829=CARTESIAN_POINT('Ctrl Pts',(-1.99270989180756,0.103548307065135,
13.6725504395776));
#25830=CARTESIAN_POINT('Ctrl Pts',(-1.99470842578248,0.05261562048858,13.6757977790687));
#25831=CARTESIAN_POINT('Ctrl Pts',(-1.99474935791997,0.00160049301082166,
13.6790451185598));
#25832=CARTESIAN_POINT('',(-1.99423738866044,-0.00182902399065958,12.0790454206247));
#25833=CARTESIAN_POINT('Ctrl Pts',(-1.99423738866044,-0.00182902399065958,
12.0790454206247));
#25834=CARTESIAN_POINT('Ctrl Pts',(-1.99577709645304,-0.173571656520854,
12.0900037687456));
#25835=CARTESIAN_POINT('Ctrl Pts',(-1.89678413975083,-1.00784194773067,
12.1433474493388));
#25836=CARTESIAN_POINT('Ctrl Pts',(-0.728288010713249,-2.24331894452348,
12.2390764624042));
#25837=CARTESIAN_POINT('Ctrl Pts',(1.49178352251778,-1.82687307587338,12.366232459821));
#25838=CARTESIAN_POINT('Ctrl Pts',(2.34362655358403,0.265137494033562,12.4933884572377));
#25839=CARTESIAN_POINT('Ctrl Pts',(1.04595083702944,2.11397023629094,12.6205444546545));
#25840=CARTESIAN_POINT('Ctrl Pts',(-1.21104620563245,2.02391956392289,12.7477004520712));
#25841=CARTESIAN_POINT('Ctrl Pts',(-1.98780196605619,0.704986800798777,
12.8338673400546));
#25842=CARTESIAN_POINT('Ctrl Pts',(-1.99799837878425,0.0221817113925817,
12.8776488955658));
#25843=CARTESIAN_POINT('Ctrl Pts',(-1.99793808332185,0.000404756782470808,
12.8790451186048));
#25844=CARTESIAN_POINT('',(-1.99474936733483,0.00158871561359909,10.4790451186048));
#25845=CARTESIAN_POINT('Ctrl Pts',(-1.99474918095163,-0.00180764841896022,
12.0793396996528));
#25846=CARTESIAN_POINT('Ctrl Pts',(-1.99484885862249,0.108187165960091,
12.0729507633111));
#25847=CARTESIAN_POINT('Ctrl Pts',(-1.98585074754498,0.217993308813224,
12.0665054587627));
#25848=CARTESIAN_POINT('Ctrl Pts',(-1.96280285823564,0.3569073674302,12.0578927663831));
#25849=CARTESIAN_POINT('Ctrl Pts',(-1.95705291046282,0.387197204379771,
12.0559873421261));
#25850=CARTESIAN_POINT('Ctrl Pts',(-1.94891810280673,0.425218408213222,
12.0535559201257));
#25851=CARTESIAN_POINT('Ctrl Pts',(-1.94718488269249,0.433086014217266,
12.053050642673));
#25852=CARTESIAN_POINT('Ctrl Pts',(-1.94419256405425,0.44628788228874,12.0521990725554));
#25853=CARTESIAN_POINT('Ctrl Pts',(-1.94295904408368,0.451627891129366,
12.0518535979334));
#25854=CARTESIAN_POINT('Ctrl Pts',(-1.9404831389815,0.462148385791333,12.0511709161668));
#25855=CARTESIAN_POINT('Ctrl Pts',(-1.93924197591684,0.467329114334702,
12.0508337507229));
#25856=CARTESIAN_POINT('Ctrl Pts',(-1.9368325101669,0.477211547173679,12.0501886871813));
#25857=CARTESIAN_POINT('Ctrl Pts',(-1.93566780133287,0.481914095454843,
12.0498809070156));
#25858=CARTESIAN_POINT('Ctrl Pts',(-1.93296260807407,0.492668361670484,
12.0491751271378));
#25859=CARTESIAN_POINT('Ctrl Pts',(-1.93141081939197,0.498717158390616,
12.0487767645773));
#25860=CARTESIAN_POINT('Ctrl Pts',(-1.92654025131116,0.517338680208813,
12.0475460302998));
#25861=CARTESIAN_POINT('Ctrl Pts',(-1.92312696895886,0.529886117870888,
12.0467106076777));
#25862=CARTESIAN_POINT('Ctrl Pts',(-1.88441590732639,0.66688749837837,12.0375200092384));
#25863=CARTESIAN_POINT('Ctrl Pts',(-1.83722141552458,0.78763443173628,12.0287643231951));
#25864=CARTESIAN_POINT('Ctrl Pts',(-1.74787812498756,0.963629234417369,
12.015077962897));
#25865=CARTESIAN_POINT('Ctrl Pts',(-1.71398649726138,1.02269705494905,12.0103152752113));
#25866=CARTESIAN_POINT('Ctrl Pts',(-1.63085581147103,1.15180162108369,11.9996264039091));
#25867=CARTESIAN_POINT('Ctrl Pts',(-1.57998942645046,1.22064495557221,11.9937244327594));
#25868=CARTESIAN_POINT('Ctrl Pts',(-1.51342462071226,1.2995722040838,11.9868833827804));
#25869=CARTESIAN_POINT('Ctrl Pts',(-1.50181187290085,1.31297492286934,11.985719054412));
#25870=CARTESIAN_POINT('Ctrl Pts',(-1.48667898069485,1.32997685893993,11.9842406060038));
#25871=CARTESIAN_POINT('Ctrl Pts',(-1.48332227391515,1.33371956197636,11.983915057994));
#25872=CARTESIAN_POINT('Ctrl Pts',(-1.47793357859478,1.33968240897271,11.9833963081703));
#25873=CARTESIAN_POINT('Ctrl Pts',(-1.47591068107915,1.34191068310096,11.983202434957));
#25874=CARTESIAN_POINT('Ctrl Pts',(-1.4720546105342,1.34613897741245,11.982834524539));
#25875=CARTESIAN_POINT('Ctrl Pts',(-1.47022242289288,1.34813981107635,11.9826604207673));
#25876=CARTESIAN_POINT('Ctrl Pts',(-1.46600337344847,1.3527283779938,11.9822611130898));
#25877=CARTESIAN_POINT('Ctrl Pts',(-1.46361374126741,1.35531353288827,11.9820361232395));
#25878=CARTESIAN_POINT('Ctrl Pts',(-1.45618922870233,1.36330299221135,11.9813406641503));
#25879=CARTESIAN_POINT('Ctrl Pts',(-1.45113109457436,1.36868574509045,11.9808719337115));
#25880=CARTESIAN_POINT('Ctrl Pts',(-1.35911923888734,1.46551922219162,11.9724336906515));
#25881=CARTESIAN_POINT('Ctrl Pts',(-1.26369533533535,1.54855948118669,11.9650908535941));
#25882=CARTESIAN_POINT('Ctrl Pts',(-1.07027612907576,1.68700858150156,11.9512871450542));
#25883=CARTESIAN_POINT('Ctrl Pts',(-0.974215785000916,1.74424497553258,
11.9448441838547));
#25884=CARTESIAN_POINT('Ctrl Pts',(-0.818198653931384,1.82027873847391,
11.934436573094));
#25885=CARTESIAN_POINT('Ctrl Pts',(-0.761293234419289,1.84480219602976,
11.9306541643618));
#25886=CARTESIAN_POINT('Ctrl Pts',(-0.693291119944838,1.870425186837,11.9261076584501));
#25887=CARTESIAN_POINT('Ctrl Pts',(-0.683208600509569,1.87413152086904,
11.9254329366476));
#25888=CARTESIAN_POINT('Ctrl Pts',(-0.668587338317781,1.87937262979526,
11.9244533993587));
#25889=CARTESIAN_POINT('Ctrl Pts',(-0.664072108739256,1.88097281860383,
11.9241507576373));
#25890=CARTESIAN_POINT('Ctrl Pts',(-0.654941558998126,1.88417169431438,
11.9235384454758));
#25891=CARTESIAN_POINT('Ctrl Pts',(-0.650326045196499,1.88576972443685,
11.9232287557767));
#25892=CARTESIAN_POINT('Ctrl Pts',(-0.641373417822971,1.88883261768678,
11.9226277183401));
#25893=CARTESIAN_POINT('Ctrl Pts',(-0.637037035344169,1.89029953545775,
11.9223364408747));
#25894=CARTESIAN_POINT('Ctrl Pts',(-0.625517845486112,1.89415212473706,
11.9215622635058));
#25895=CARTESIAN_POINT('Ctrl Pts',(-0.618326498225142,1.89651184695599,
11.9210785111946));
#25896=CARTESIAN_POINT('Ctrl Pts',(-0.592670503133408,1.90476900416666,
11.9193509937921));
#25897=CARTESIAN_POINT('Ctrl Pts',(-0.574134017130108,1.91043800495356,
11.9180997712826));
#25898=CARTESIAN_POINT('Ctrl Pts',(-0.424621203735764,1.95379094618723,
11.9079796719291));
#25899=CARTESIAN_POINT('Ctrl Pts',(-0.290203918461033,1.97822417123613,
11.8986726693985));
#25900=CARTESIAN_POINT('Ctrl Pts',(-0.0168923781969079,1.99943906768614,
11.8795916941514));
#25901=CARTESIAN_POINT('Ctrl Pts',(0.121331746008538,1.99582718770227,11.8698700086057));
#25902=CARTESIAN_POINT('Ctrl Pts',(0.274380916292036,1.97585746830651,11.8596518898124));
#25903=CARTESIAN_POINT('Ctrl Pts',(0.29065003984629,1.97352988810661,11.8585731054541));
#25904=CARTESIAN_POINT('Ctrl Pts',(0.312062161289376,1.9701959746685,11.8571646959501));
#25905=CARTESIAN_POINT('Ctrl Pts',(0.317232035378616,1.969370155238,11.8568255201808));
#25906=CARTESIAN_POINT('Ctrl Pts',(0.325437880504499,1.96802622772115,11.8562886277261));
#25907=CARTESIAN_POINT('Ctrl Pts',(0.328475960789748,1.9675214333177,11.8560901707426));
#25908=CARTESIAN_POINT('Ctrl Pts',(0.334173703317038,1.966561155817,11.8557185899691));
#25909=CARTESIAN_POINT('Ctrl Pts',(0.336833579628456,1.9661073173413,11.8555453781047));
#25910=CARTESIAN_POINT('Ctrl Pts',(0.342900167127311,1.96505954004727,11.8551508892476));
#25911=CARTESIAN_POINT('Ctrl Pts',(0.346306253033582,1.9644621401539,11.8549298114993));
#25912=CARTESIAN_POINT('Ctrl Pts',(0.35674117106134,1.96260395719676,11.8542537189989));
#25913=CARTESIAN_POINT('Ctrl Pts',(0.363764897181355,1.9613142683493,11.8538003173172));
#25914=CARTESIAN_POINT('Ctrl Pts',(0.419662547128181,1.95073979738671,11.8502042266845));
#25915=CARTESIAN_POINT('Ctrl Pts',(0.468185222418544,1.93966645716922,11.8471572666069));
#25916=CARTESIAN_POINT('Ctrl Pts',(0.533914062706573,1.92205563153123,11.8430699621467));
#25917=CARTESIAN_POINT('Ctrl Pts',(0.551515154688451,1.91707932606761,11.8419794650533));
#25918=CARTESIAN_POINT('Ctrl Pts',(0.722686369746059,1.86613199322953,11.8313921624243));
#25919=CARTESIAN_POINT('Ctrl Pts',(0.870255180355367,1.80204996139328,11.8223554016313));
#25920=CARTESIAN_POINT('Ctrl Pts',(1.04955047029234,1.69697606776551,11.8099661025321));
#25921=CARTESIAN_POINT('Ctrl Pts',(1.08965952079484,1.67150399284907,11.807097049638));
#25922=CARTESIAN_POINT('Ctrl Pts',(1.15261526627158,1.62829316305592,11.8024037375847));
#25923=CARTESIAN_POINT('Ctrl Pts',(1.17605301515939,1.61144647708154,11.8006118901766));
#25924=CARTESIAN_POINT('Ctrl Pts',(1.20573611074448,1.58911818799078,11.7982804893771));
#25925=CARTESIAN_POINT('Ctrl Pts',(1.2123249315063,1.58409735851978,11.7977589498346));
#25926=CARTESIAN_POINT('Ctrl Pts',(1.223139054096,1.57574976912173,11.7968961788712));
#25927=CARTESIAN_POINT('Ctrl Pts',(1.22738256050131,1.57244666993689,11.7965558840395));
#25928=CARTESIAN_POINT('Ctrl Pts',(1.23541469885217,1.56614221766,11.7959084306857));
#25929=CARTESIAN_POINT('Ctrl Pts',(1.23920588588474,1.56314416986726,11.7956014053222));
#25930=CARTESIAN_POINT('Ctrl Pts',(1.24779739949618,1.55629915329115,11.7949023588638));
#25931=CARTESIAN_POINT('Ctrl Pts',(1.2525908840936,1.55244371247677,11.7945099994814));
#25932=CARTESIAN_POINT('Ctrl Pts',(1.26709444312639,1.54066747193688,11.7933156619083));
#25933=CARTESIAN_POINT('Ctrl Pts',(1.27674763709945,1.5326774109821,11.7925108884855));
#25934=CARTESIAN_POINT('Ctrl Pts',(1.40661048967167,1.42311023347928,11.7815480588068));
#25935=CARTESIAN_POINT('Ctrl Pts',(1.51443727901229,1.30776720970524,11.7707790256885));
#25936=CARTESIAN_POINT('Ctrl Pts',(1.66124710740046,1.10792779327813,11.7534928249695));
#25937=CARTESIAN_POINT('Ctrl Pts',(1.709878420532,1.03129191348939,11.7471429084596));
#25938=CARTESIAN_POINT('Ctrl Pts',(1.76945902784338,0.921528059331686,11.7386221069192));
#25939=CARTESIAN_POINT('Ctrl Pts',(1.7850124510975,0.891027528080388,11.7363122646895));
#25940=CARTESIAN_POINT('Ctrl Pts',(1.80802969927368,0.842865780320253,11.7327702042771));
#25941=CARTESIAN_POINT('Ctrl Pts',(1.81603658232634,0.825472783064892,11.7315119089266));
#25942=CARTESIAN_POINT('Ctrl Pts',(1.82584260359814,0.803338020924796,11.7299392476661));
#25943=CARTESIAN_POINT('Ctrl Pts',(1.8278754551799,0.798701765799615,11.7296114200392));
#25944=CARTESIAN_POINT('Ctrl Pts',(1.83109177052213,0.791289829664729,11.7290898941046));
#25945=CARTESIAN_POINT('Ctrl Pts',(1.83228660706276,0.788519154162068,11.7288955119525));
#25946=CARTESIAN_POINT('Ctrl Pts',(1.83454303716102,0.783253954178378,11.7285272190856));
#25947=CARTESIAN_POINT('Ctrl Pts',(1.83560581895316,0.780760007583391,11.7283532393672));
#25948=CARTESIAN_POINT('Ctrl Pts',(1.8380313631467,0.775035845378071,11.7279549782062));
#25949=CARTESIAN_POINT('Ctrl Pts',(1.8393906948618,0.771804201625543,11.7277309070036));
#25950=CARTESIAN_POINT('Ctrl Pts',(1.84366297158519,0.761571994084027,11.7270238276549));
#25951=CARTESIAN_POINT('Ctrl Pts',(1.84654456841583,0.754558292146722,11.7265426841799));
#25952=CARTESIAN_POINT('Ctrl Pts',(1.89503001638701,0.634605202873113,11.7183710696226));
#25953=CARTESIAN_POINT('Ctrl Pts',(1.93024327377328,0.517719228208718,11.7112636517435));
#25954=CARTESIAN_POINT('Ctrl Pts',(1.97464031991498,0.299868793151865,11.6983549000612));
#25955=CARTESIAN_POINT('Ctrl Pts',(1.98723742444042,0.20002991003316,11.6925606543961));
#25956=CARTESIAN_POINT('Ctrl Pts',(1.99480471555322,0.0487733192826281,
11.6835581582014));
#25957=CARTESIAN_POINT('Ctrl Pts',(1.99539952188995,-0.00220061530919844,
11.6804879050253));
#25958=CARTESIAN_POINT('Ctrl Pts',(1.99323007481769,-0.0836096056814195,
11.6754888512549));
#25959=CARTESIAN_POINT('Ctrl Pts',(1.99171977314159,-0.114056501075558,
11.6735979386913));
#25960=CARTESIAN_POINT('Ctrl Pts',(1.98888313599916,-0.153124040179684,
11.6711397086736));
#25961=CARTESIAN_POINT('Ctrl Pts',(1.98819709542604,-0.161788152317992,
11.6705925240673));
#25962=CARTESIAN_POINT('Ctrl Pts',(1.98699882125027,-0.175760295189872,
11.6697067482134));
#25963=CARTESIAN_POINT('Ctrl Pts',(1.98652187981424,-0.181071304003883,
11.6693692678851));
#25964=CARTESIAN_POINT('Ctrl Pts',(1.98557110693201,-0.191202511456369,
11.6687239714021));
#25965=CARTESIAN_POINT('Ctrl Pts',(1.98510100314457,-0.196023028506678,
11.6684162747333));
#25966=CARTESIAN_POINT('Ctrl Pts',(1.98398559089455,-0.207044950158387,
11.6677112089154));
#25967=CARTESIAN_POINT('Ctrl Pts',(1.98332875655866,-0.213245112984284,
11.6673134795132));
#25968=CARTESIAN_POINT('Ctrl Pts',(1.98121790476579,-0.232316505682064,
11.6660866130978));
#25969=CARTESIAN_POINT('Ctrl Pts',(1.97966759867766,-0.245176529389799,
11.6652544528902));
#25970=CARTESIAN_POINT('Ctrl Pts',(1.96337726564101,-0.370058765795065,
11.6571246703258));
#25971=CARTESIAN_POINT('Ctrl Pts',(1.93927252087176,-0.480632804230657,
11.6495261565314));
#25972=CARTESIAN_POINT('Ctrl Pts',(1.85816798075956,-0.743276750710874,
11.6305658696391));
#25973=CARTESIAN_POINT('Ctrl Pts',(1.79173053639902,-0.891600260354994,
11.6190425211045));
#25974=CARTESIAN_POINT('Ctrl Pts',(1.69517360110864,-1.05168433240267,11.6065568580152));
#25975=CARTESIAN_POINT('Ctrl Pts',(1.68184939079497,-1.07286357180088,11.6049052939087));
#25976=CARTESIAN_POINT('Ctrl Pts',(1.66509997765402,-1.09840800806227,11.6029189514031));
#25977=CARTESIAN_POINT('Ctrl Pts',(1.66205122821783,-1.10301577699605,11.6025608780701));
#25978=CARTESIAN_POINT('Ctrl Pts',(1.65725094942257,-1.1102056508084,11.6020025797066));
#25979=CARTESIAN_POINT('Ctrl Pts',(1.6555124691493,-1.11279637008216,11.6018014970358));
#25980=CARTESIAN_POINT('Ctrl Pts',(1.65226208322431,-1.11761568668576,11.6014276193161));
#25981=CARTESIAN_POINT('Ctrl Pts',(1.65075175860802,-1.11984527787244,11.6012547242442));
#25982=CARTESIAN_POINT('Ctrl Pts',(1.64732505077487,-1.12488190097569,11.6008643175221));
#25983=CARTESIAN_POINT('Ctrl Pts',(1.64540601097656,-1.12768709024932,11.6006469891924));
#25984=CARTESIAN_POINT('Ctrl Pts',(1.63972512704918,-1.13594584488514,11.6000074401708));
#25985=CARTESIAN_POINT('Ctrl Pts',(1.63594322667921,-1.14138565649322,11.5995865575342));
#25986=CARTESIAN_POINT('Ctrl Pts',(1.60968159344546,-1.17876119122882,11.5966965886775));
#25987=CARTESIAN_POINT('Ctrl Pts',(1.58629353090542,-1.21005210789473,11.5942862019571));
#25988=CARTESIAN_POINT('Ctrl Pts',(1.5565788281996,-1.2474637817082,11.5913883961672));
#25989=CARTESIAN_POINT('Ctrl Pts',(1.55111300363812,-1.2542535585753,11.5908618172267));
#25990=CARTESIAN_POINT('Ctrl Pts',(1.52933401218317,-1.28094782706485,11.5887879607823));
#25991=CARTESIAN_POINT('Ctrl Pts',(1.51268034270638,-1.30057222911857,11.587255377766));
#25992=CARTESIAN_POINT('Ctrl Pts',(1.46300240240858,-1.35686632934202,11.5828174953894));
#25993=CARTESIAN_POINT('Ctrl Pts',(1.42899115602662,-1.39264024437269,11.5799437707428));
#25994=CARTESIAN_POINT('Ctrl Pts',(1.32172972569539,-1.49738911145848,11.5712385953718));
#25995=CARTESIAN_POINT('Ctrl Pts',(1.24456184455973,-1.56211660966999,11.5654396830185));
#25996=CARTESIAN_POINT('Ctrl Pts',(1.121348002591,-1.65051953840637,11.5564260630053));
#25997=CARTESIAN_POINT('Ctrl Pts',(1.07872483074414,-1.6786864598584,11.5533493281785));
#25998=CARTESIAN_POINT('Ctrl Pts',(1.0089717614848,-1.72102749624539,11.5483406427772));
#25999=CARTESIAN_POINT('Ctrl Pts',(0.982514316992654,-1.73626758229258,
11.5464467686824));
#26000=CARTESIAN_POINT('Ctrl Pts',(0.948085605967691,-1.75506036042423,
11.5439852053992));
#26001=CARTESIAN_POINT('Ctrl Pts',(0.940425514347337,-1.75917680552066,
11.5434377172538));
#26002=CARTESIAN_POINT('Ctrl Pts',(0.928024356344151,-1.76573690073081,
11.5425515686164));
#26003=CARTESIAN_POINT('Ctrl Pts',(0.923299919687577,-1.76821188378936,
11.5422140207621));
#26004=CARTESIAN_POINT('Ctrl Pts',(0.914266569797192,-1.77289809573383,
11.5415686740953));
#26005=CARTESIAN_POINT('Ctrl Pts',(0.909959411952963,-1.77511264048898,
11.5412609951013));
#26006=CARTESIAN_POINT('Ctrl Pts',(0.900090879921511,-1.78014123542618,
11.5405560812922));
#26007=CARTESIAN_POINT('Ctrl Pts',(0.894524317425016,-1.78294493865071,
11.5401584867767));
#26008=CARTESIAN_POINT('Ctrl Pts',(0.877358585304075,-1.79149015648187,
11.538932443463));
#26009=CARTESIAN_POINT('Ctrl Pts',(0.865716787778558,-1.79714481837445,
11.5381009773507));
#26010=CARTESIAN_POINT('Ctrl Pts',(0.752071778063161,-1.85098405786124,
11.5299833723584));
#26011=CARTESIAN_POINT('Ctrl Pts',(0.646227564069054,-1.89053853113174,
11.5223973190649));
#26012=CARTESIAN_POINT('Ctrl Pts',(0.381544594245775,-1.96461714860328,
11.5034402644728));
#26013=CARTESIAN_POINT('Ctrl Pts',(0.220726094123614,-1.98911476078211,
11.4919058024667));
#26014=CARTESIAN_POINT('Ctrl Pts',(0.0336692489413088,-1.99462323167431,
11.4794070491161));
#26015=CARTESIAN_POINT('Ctrl Pts',(0.00860918121163235,-1.9948888393611,
11.4777528251775));
#26016=CARTESIAN_POINT('Ctrl Pts',(-0.0219781157949418,-1.99463657845007,
11.475763720997));
#26017=CARTESIAN_POINT('Ctrl Pts',(-0.0275054673085827,-1.99456801556112,
11.4754054707219));
#26018=CARTESIAN_POINT('Ctrl Pts',(-0.0361526363513712,-1.99442480105054,
11.4748469576618));
#26019=CARTESIAN_POINT('Ctrl Pts',(-0.0392726317413574,-1.99436580418058,
11.4746458361718));
#26020=CARTESIAN_POINT('Ctrl Pts',(-0.0450848360069074,-1.99424225509335,
11.4742719236012));
#26021=CARTESIAN_POINT('Ctrl Pts',(-0.047777024582177,-1.99417957328167,
11.4740990323226));
#26022=CARTESIAN_POINT('Ctrl Pts',(-0.0538659733519217,-1.99402546757891,
11.4737086818615));
#26023=CARTESIAN_POINT('Ctrl Pts',(-0.0572626227174797,-1.99393081647717,
11.4734914057772));
#26024=CARTESIAN_POINT('Ctrl Pts',(-0.0672772751470178,-1.9936261365331,
11.4728521519743));
#26025=CARTESIAN_POINT('Ctrl Pts',(-0.0738945744111544,-1.99339183274748,
11.4724315104659));
#26026=CARTESIAN_POINT('Ctrl Pts',(-0.119459882573349,-1.99155125804546,
11.4695463838337));
#26027=CARTESIAN_POINT('Ctrl Pts',(-0.158357764620448,-1.98883643987945,
11.46714037629));
#26028=CARTESIAN_POINT('Ctrl Pts',(-0.205693685456895,-1.98413490324016,
11.4642549602885));
#26029=CARTESIAN_POINT('Ctrl Pts',(-0.214227829298461,-1.98323161724602,
11.4637364464589));
#26030=CARTESIAN_POINT('Ctrl Pts',(-0.29674049139646,-1.97395933870372,
11.4587373372729));
#26031=CARTESIAN_POINT('Ctrl Pts',(-0.370206653177138,-1.9615093424676,
11.4543949416884));
#26032=CARTESIAN_POINT('Ctrl Pts',(-0.541163907989573,-1.92258791784375,
11.4442132612495));
#26033=CARTESIAN_POINT('Ctrl Pts',(-0.637676655607367,-1.89276782948434,
11.4383990057976));
#26034=CARTESIAN_POINT('Ctrl Pts',(-0.779373910791746,-1.83691321503152,
11.4293487666133));
#26035=CARTESIAN_POINT('Ctrl Pts',(-0.826481307962906,-1.81620535460337,
11.426250667406));
#26036=CARTESIAN_POINT('Ctrl Pts',(-0.900330014255933,-1.78027393962846,
11.4212102487798));
#26037=CARTESIAN_POINT('Ctrl Pts',(-0.927611932134093,-1.76621215535936,
11.4193066306862));
#26038=CARTESIAN_POINT('Ctrl Pts',(-0.962207310700516,-1.74735816423032,
11.4168341027166));
#26039=CARTESIAN_POINT('Ctrl Pts',(-0.969829621235627,-1.74313911228063,
11.4162856191016));
#26040=CARTESIAN_POINT('Ctrl Pts',(-0.982076374868853,-1.73625517721604,
11.4153982478786));
#26041=CARTESIAN_POINT('Ctrl Pts',(-0.986718245355617,-1.73362139749837,
11.4150604785516));
#26042=CARTESIAN_POINT('Ctrl Pts',(-0.995551402419267,-1.7285625286114,
11.4144149667268));
#26043=CARTESIAN_POINT('Ctrl Pts',(-0.999744543701183,-1.72614074073892,
11.4141073451367));
#26044=CARTESIAN_POINT('Ctrl Pts',(-1.00930877618424,-1.72057028901564,
11.4134029271462));
#26045=CARTESIAN_POINT('Ctrl Pts',(-1.01467400655014,-1.71741171071603,
11.4130057728487));
#26046=CARTESIAN_POINT('Ctrl Pts',(-1.03111664143485,-1.70762778092399,
11.4117824136283));
#26047=CARTESIAN_POINT('Ctrl Pts',(-1.04214442285568,-1.70092009080897,
11.4109532105261));
#26048=CARTESIAN_POINT('Ctrl Pts',(-1.17103287111351,-1.62079923931634,
11.4011570985037));
#26049=CARTESIAN_POINT('Ctrl Pts',(-1.28095890319296,-1.53539510147643,
11.3917242485488));
#26050=CARTESIAN_POINT('Ctrl Pts',(-1.45046430713703,-1.37274166259998,
11.3753962728556));
#26051=CARTESIAN_POINT('Ctrl Pts',(-1.51491738958601,-1.30126559770483,
11.3686448961182));
#26052=CARTESIAN_POINT('Ctrl Pts',(-1.61243467974873,-1.176011483173,11.357737462348));
#26053=CARTESIAN_POINT('Ctrl Pts',(-1.64855920119987,-1.12481240610626,
11.3535049234383));
#26054=CARTESIAN_POINT('Ctrl Pts',(-1.68593214343734,-1.06616514973489,
11.3489700326566));
#26055=CARTESIAN_POINT('Ctrl Pts',(-1.68961570199279,-1.06031792485678,
11.3485212377572));
#26056=CARTESIAN_POINT('Ctrl Pts',(-1.69507256614742,-1.05155513440061,
11.3478537763595));
#26057=CARTESIAN_POINT('Ctrl Pts',(-1.69686885012071,-1.04865404738951,
11.3476336324629));
#26058=CARTESIAN_POINT('Ctrl Pts',(-1.69993625787856,-1.0436715142072,11.3472569850947));
#26059=CARTESIAN_POINT('Ctrl Pts',(-1.70121101395357,-1.04159233708212,
11.3471002426869));
#26060=CARTESIAN_POINT('Ctrl Pts',(-1.70385671008482,-1.03725928926541,
11.3467744864204));
#26061=CARTESIAN_POINT('Ctrl Pts',(-1.70522698784058,-1.03500504433891,
11.3466055160234));
#26062=CARTESIAN_POINT('Ctrl Pts',(-1.70901135214203,-1.02875146803669,
11.3461381412386));
#26063=CARTESIAN_POINT('Ctrl Pts',(-1.71141588775784,-1.0247463319942,11.3458403589902));
#26064=CARTESIAN_POINT('Ctrl Pts',(-1.72089003532516,-1.00883927447145,
11.3446636473225));
#26065=CARTESIAN_POINT('Ctrl Pts',(-1.72784994749971,-0.996871997751052,
11.3437915981138));
#26066=CARTESIAN_POINT('Ctrl Pts',(-1.80206042138588,-0.866157640561091,
11.3343983272512));
#26067=CARTESIAN_POINT('Ctrl Pts',(-1.85709048237705,-0.740862511226564,
11.326551437279));
#26068=CARTESIAN_POINT('Ctrl Pts',(-1.94471219943039,-0.468508317244706,
11.3099556916309));
#26069=CARTESIAN_POINT('Ctrl Pts',(-1.97435629501184,-0.321425209948056,
11.3012230293888));
#26070=CARTESIAN_POINT('Ctrl Pts',(-1.98849628779947,-0.158450961733807,
11.291024449328));
#26071=CARTESIAN_POINT('Ctrl Pts',(-1.98956099172601,-0.14446881366375,
11.2901457708214));
#26072=CARTESIAN_POINT('Ctrl Pts',(-1.99089936334497,-0.124051407241659,
11.2888568439449));
#26073=CARTESIAN_POINT('Ctrl Pts',(-1.9912894367552,-0.11762399455444,11.2884502464913));
#26074=CARTESIAN_POINT('Ctrl Pts',(-1.99191996569431,-0.106330380202884,
11.2877342897963));
#26075=CARTESIAN_POINT('Ctrl Pts',(-1.99217372799311,-0.101464951042295,
11.2874253503271));
#26076=CARTESIAN_POINT('Ctrl Pts',(-1.99263245238927,-0.0920034661096103,
11.2868235911062));
#26077=CARTESIAN_POINT('Ctrl Pts',(-1.99283934400358,-0.0874075311297139,
11.286530833881));
#26078=CARTESIAN_POINT('Ctrl Pts',(-1.99334947391403,-0.0751301167560543,
11.2857475460491));
#26079=CARTESIAN_POINT('Ctrl Pts',(-1.9936242071673,-0.067447590412097,
11.2852561253582));
#26080=CARTESIAN_POINT('Ctrl Pts',(-1.99445806607978,-0.0396281648272461,
11.2834718654378));
#26081=CARTESIAN_POINT('Ctrl Pts',(-1.99475653780781,-0.0194852290356758,
11.2821709080192));
#26082=CARTESIAN_POINT('Ctrl Pts',(-1.99471414973372,0.10898149033513,11.2738132404301));
#26083=CARTESIAN_POINT('Ctrl Pts',(-1.98585511496646,0.217104032450646,
11.2664899925974));
#26084=CARTESIAN_POINT('Ctrl Pts',(-1.95017223943802,0.433901895587183,
11.2513024728591));
#26085=CARTESIAN_POINT('Ctrl Pts',(-1.92289727096811,0.542132887434468,
11.2434556380222));
#26086=CARTESIAN_POINT('Ctrl Pts',(-1.88156141372123,0.6625765128277,11.2346869576134));
#26087=CARTESIAN_POINT('Ctrl Pts',(-1.87621362607337,0.677571722353845,
11.233594879948));
#26088=CARTESIAN_POINT('Ctrl Pts',(-1.85310682343192,0.739991203550207,
11.2290514120307));
#26089=CARTESIAN_POINT('Ctrl Pts',(-1.83372302952571,0.786799050173972,
11.2256499073268));
#26090=CARTESIAN_POINT('Ctrl Pts',(-1.80958192734027,0.839340372631031,
11.2218775000677));
#26091=CARTESIAN_POINT('Ctrl Pts',(-1.80655200324658,0.845842110707983,
11.2214115069976));
#26092=CARTESIAN_POINT('Ctrl Pts',(-1.8020067567347,0.855459650030122,11.2207235776715));
#26093=CARTESIAN_POINT('Ctrl Pts',(-1.80051832436742,0.858587985130398,
11.2205000297473));
#26094=CARTESIAN_POINT('Ctrl Pts',(-1.79785581235016,0.864146587608158,
11.2201032257265));
#26095=CARTESIAN_POINT('Ctrl Pts',(-1.79668494584757,0.866578359158642,
11.2199297728655));
#26096=CARTESIAN_POINT('Ctrl Pts',(-1.79416920624207,0.871776279661413,
11.219559322282));
#26097=CARTESIAN_POINT('Ctrl Pts',(-1.79282287455694,0.874541687506327,
11.219362417559));
#26098=CARTESIAN_POINT('Ctrl Pts',(-1.78912833019076,0.882086011899745,
11.2188257114352));
#26099=CARTESIAN_POINT('Ctrl Pts',(-1.78676734926795,0.886858700943163,
11.2184866976372));
#26100=CARTESIAN_POINT('Ctrl Pts',(-1.7744326984453,0.911543819822088,11.2167356536189));
#26101=CARTESIAN_POINT('Ctrl Pts',(-1.76414470304014,0.931298612001251,
11.2153424252113));
#26102=CARTESIAN_POINT('Ctrl Pts',(-1.73327010004191,0.988234904828696,
11.2113385374838));
#26103=CARTESIAN_POINT('Ctrl Pts',(-1.71182265606783,1.02493763822833,11.2087720950914));
#26104=CARTESIAN_POINT('Ctrl Pts',(-1.66667147435011,1.09682758747717,11.2037183604904));
#26105=CARTESIAN_POINT('Ctrl Pts',(-1.64298589889468,1.13199918801789,11.2012321719789));
#26106=CARTESIAN_POINT('Ctrl Pts',(-1.51091864981972,1.31522324214131,11.1880656825469));
#26107=CARTESIAN_POINT('Ctrl Pts',(-1.38363604813714,1.44852782860564,11.1776153939314));
#26108=CARTESIAN_POINT('Ctrl Pts',(-1.22476888851582,1.5745931111486,11.1650457384017));
#26109=CARTESIAN_POINT('Ctrl Pts',(-1.20943111860765,1.58640430658461,11.1638376301024));
#26110=CARTESIAN_POINT('Ctrl Pts',(-1.18786436662905,1.60251771630324,11.1621451762499));
#26111=CARTESIAN_POINT('Ctrl Pts',(-1.18177880260236,1.60701077897569,11.1616682961255));
#26112=CARTESIAN_POINT('Ctrl Pts',(-1.17197033170511,1.61416667453005,11.1609007070685));
#26113=CARTESIAN_POINT('Ctrl Pts',(-1.16826351885159,1.61685152735509,11.1606108536295));
#26114=CARTESIAN_POINT('Ctrl Pts',(-1.16058158844212,1.62237535741303,11.1600106303612));
#26115=CARTESIAN_POINT('Ctrl Pts',(-1.15660522084007,1.62521253570094,11.1597001939598));
#26116=CARTESIAN_POINT('Ctrl Pts',(-1.14729659825684,1.63180286712385,11.1589740372681));
#26117=CARTESIAN_POINT('Ctrl Pts',(-1.14195630565864,1.63554451966978,11.1585578805209));
#26118=CARTESIAN_POINT('Ctrl Pts',(-1.12471266151726,1.64750057889092,11.1572154481452));
#26119=CARTESIAN_POINT('Ctrl Pts',(-1.11273850688099,1.65561158651543,11.1562852651877));
#26120=CARTESIAN_POINT('Ctrl Pts',(-1.08460455151432,1.6742257780697,11.1541039777264));
#26121=CARTESIAN_POINT('Ctrl Pts',(-1.06837884933993,1.68462624348337,11.1528491538563));
#26122=CARTESIAN_POINT('Ctrl Pts',(-1.01125892502959,1.72008224887004,11.1484418047274));
#26123=CARTESIAN_POINT('Ctrl Pts',(-0.969616550873315,1.7438952595526,11.1452458812956));
#26124=CARTESIAN_POINT('Ctrl Pts',(-0.746266333009698,1.86114313851902,
11.1281966848339));
#26125=CARTESIAN_POINT('Ctrl Pts',(-0.551892657704264,1.9277356069535,11.1135097981827));
#26126=CARTESIAN_POINT('Ctrl Pts',(-0.341177652899238,1.96538068168746,
11.0991978668756));
#26127=CARTESIAN_POINT('Ctrl Pts',(-0.331527084905448,1.96703157441143,
11.0985461644639));
#26128=CARTESIAN_POINT('Ctrl Pts',(-0.315736022130048,1.96961338586238,
11.0974863651123));
#26129=CARTESIAN_POINT('Ctrl Pts',(-0.309602755153813,1.9705867810459,11.0970763532846));
#26130=CARTESIAN_POINT('Ctrl Pts',(-0.291290409597636,1.97340548064566,
11.0958571767614));
#26131=CARTESIAN_POINT('Ctrl Pts',(-0.279098391181395,1.9751666765927,11.0950520762503));
#26132=CARTESIAN_POINT('Ctrl Pts',(-0.262474955543196,1.9774110125116,11.093964039578));
#26133=CARTESIAN_POINT('Ctrl Pts',(-0.258057399642526,1.97799236452394,
11.0936758319242));
#26134=CARTESIAN_POINT('Ctrl Pts',(-0.251063972197548,1.97888887465765,
11.0932210815517));
#26135=CARTESIAN_POINT('Ctrl Pts',(-0.248489403668808,1.97921381180342,
11.0930539929213));
#26136=CARTESIAN_POINT('Ctrl Pts',(-0.243206726917152,1.9798700699711,11.0927118230577));
#26137=CARTESIAN_POINT('Ctrl Pts',(-0.240498578913211,1.98020085839826,
11.0925367756152));
#26138=CARTESIAN_POINT('Ctrl Pts',(-0.234131735779365,1.98096528660171,
11.0921260828978));
#26139=CARTESIAN_POINT('Ctrl Pts',(-0.230472481476498,1.9813943505102,11.0918906960174));
#26140=CARTESIAN_POINT('Ctrl Pts',(-0.2185267537348,1.98276149983412,11.0911243385719));
#26141=CARTESIAN_POINT('Ctrl Pts',(-0.210235444758749,1.98365777566052,
11.0905956709455));
#26142=CARTESIAN_POINT('Ctrl Pts',(-0.109096762730718,1.99394942660463,
11.0841837881886));
#26143=CARTESIAN_POINT('Ctrl Pts',(-0.0156924274389661,1.99687133690277,
11.0786385887509));
#26144=CARTESIAN_POINT('Ctrl Pts',(0.20197861287314,1.98839871846358,11.0659008717482));
#26145=CARTESIAN_POINT('Ctrl Pts',(0.325642823904791,1.9719232850224,11.058791286622));
#26146=CARTESIAN_POINT('Ctrl Pts',(0.470385409641683,1.93864453764539,11.0499784270535));
#26147=CARTESIAN_POINT('Ctrl Pts',(0.493706062181091,1.93283712319577,11.0485436095578));
#26148=CARTESIAN_POINT('Ctrl Pts',(0.571294044103228,1.91202002185902,11.0437107036334));
#26149=CARTESIAN_POINT('Ctrl Pts',(0.625025987981041,1.89513562903186,11.0402651180139));
#26150=CARTESIAN_POINT('Ctrl Pts',(0.687427807448072,1.8725842402793,11.0361147830802));
#26151=CARTESIAN_POINT('Ctrl Pts',(0.696860994846514,1.86909429278878,11.0354833266871));
#26152=CARTESIAN_POINT('Ctrl Pts',(0.71210843460038,1.86332180516486,11.0344558982169));
#26153=CARTESIAN_POINT('Ctrl Pts',(0.717939146868416,1.86108300518392,11.0340613892884));
#26154=CARTESIAN_POINT('Ctrl Pts',(0.728273838849401,1.85705903249711,11.0333592268182));
#26155=CARTESIAN_POINT('Ctrl Pts',(0.732782030381808,1.85528475706629,11.0330519414998));
#26156=CARTESIAN_POINT('Ctrl Pts',(0.742233270264344,1.85152523877342,11.0324056312807));
#26157=CARTESIAN_POINT('Ctrl Pts',(0.747174913065369,1.84953658673747,11.0320664933089));
#26158=CARTESIAN_POINT('Ctrl Pts',(0.760134975801118,1.84426068711078,11.0311738460251));
#26159=CARTESIAN_POINT('Ctrl Pts',(0.76813997414649,1.84094096582307,11.0306192410278));
#26160=CARTESIAN_POINT('Ctrl Pts',(0.803972814082364,1.82580646631468,11.0281218408807));
#26161=CARTESIAN_POINT('Ctrl Pts',(0.83155027754727,1.81341266876545,11.0261594335594));
#26162=CARTESIAN_POINT('Ctrl Pts',(0.904314029014205,1.7787025557704,11.020869593305));
#26163=CARTESIAN_POINT('Ctrl Pts',(0.948951889413259,1.75529377540411,11.017506079385));
#26164=CARTESIAN_POINT('Ctrl Pts',(1.07945595432892,1.68042174971877,11.0073161832775));
#26165=CARTESIAN_POINT('Ctrl Pts',(1.16238131418147,1.6241640242548,11.0003525775965));
#26166=CARTESIAN_POINT('Ctrl Pts',(1.33715080289835,1.48533470045382,10.9847795593506));
#26167=CARTESIAN_POINT('Ctrl Pts',(1.42628573532158,1.3999671067408,10.976190332675));
#26168=CARTESIAN_POINT('Ctrl Pts',(1.511934732569,1.3012063628643,10.9676555821612));
#26169=CARTESIAN_POINT('Ctrl Pts',(1.51685195699323,1.29547087165352,10.9671645487956));
#26170=CARTESIAN_POINT('Ctrl Pts',(1.52399989745012,1.28703695726432,10.9664493991542));
#26171=CARTESIAN_POINT('Ctrl Pts',(1.52625620968471,1.28436046328533,10.9662234552391));
#26172=CARTESIAN_POINT('Ctrl Pts',(1.53024688085735,1.27960126269821,10.9658234999083));
#26173=CARTESIAN_POINT('Ctrl Pts',(1.53198405293116,1.27752094690757,10.9656492832129));
#26174=CARTESIAN_POINT('Ctrl Pts',(1.53564809435162,1.27311492576691,10.9652815930475));
#26175=CARTESIAN_POINT('Ctrl Pts',(1.53757391806136,1.27078838942245,10.9650881954876));
#26176=CARTESIAN_POINT('Ctrl Pts',(1.54272170582291,1.26454065076075,10.9645708355375));
#26177=CARTESIAN_POINT('Ctrl Pts',(1.54593402856096,1.26061147850669,10.9642475677505));
#26178=CARTESIAN_POINT('Ctrl Pts',(1.5612822600414,1.2416912957655,10.9627007333817));
#26179=CARTESIAN_POINT('Ctrl Pts',(1.57321581985781,1.22653643264868,10.9614911285787));
#26180=CARTESIAN_POINT('Ctrl Pts',(1.60592962879547,1.18372880164766,10.9581479929672));
#26181=CARTESIAN_POINT('Ctrl Pts',(1.62621404579863,1.15570412278028,10.9560431134106));
#26182=CARTESIAN_POINT('Ctrl Pts',(1.69760624878023,1.05146514246465,10.9484579299611));
#26183=CARTESIAN_POINT('Ctrl Pts',(1.74417085959855,0.972273731676528,10.9431531070067));
#26184=CARTESIAN_POINT('Ctrl Pts',(1.85458578864389,0.750846761892662,10.9288028019407));
#26185=CARTESIAN_POINT('Ctrl Pts',(1.90749604478679,0.603911316919937,10.9197330629681));
#26186=CARTESIAN_POINT('Ctrl Pts',(1.945639820445,0.440081144942404,10.9092289437504));
#26187=CARTESIAN_POINT('Ctrl Pts',(1.94837566380584,0.42780601465771,10.9084400025407));
#26188=CARTESIAN_POINT('Ctrl Pts',(1.95227845828373,0.409480569795257,10.9072590435396));
#26189=CARTESIAN_POINT('Ctrl Pts',(1.95353378138997,0.403449227664561,10.906869855045));
#26190=CARTESIAN_POINT('Ctrl Pts',(1.95572428910217,0.392674724251599,10.9061736588264));
#26191=CARTESIAN_POINT('Ctrl Pts',(1.95667021213585,0.387933775683647,10.9058669968145));
#26192=CARTESIAN_POINT('Ctrl Pts',(1.9586309279056,0.377917072951118,10.9052183735151));
#26193=CARTESIAN_POINT('Ctrl Pts',(1.95964165833786,0.372640571800645,10.9048762853009));
#26194=CARTESIAN_POINT('Ctrl Pts',(1.96226479608967,0.358640669761366,10.9039675118626));
#26195=CARTESIAN_POINT('Ctrl Pts',(1.96384033301381,0.34991056313041,10.9033996579913));
#26196=CARTESIAN_POINT('Ctrl Pts',(1.97088659520713,0.309319624980195,10.9007538031932));
#26197=CARTESIAN_POINT('Ctrl Pts',(1.97564026137116,0.277340864941067,10.8986532161165));
#26198=CARTESIAN_POINT('Ctrl Pts',(1.98641214249404,0.190396476743029,10.8928947489147));
#26199=CARTESIAN_POINT('Ctrl Pts',(1.99092525056377,0.135276499381504,10.8891924199297));
#26200=CARTESIAN_POINT('Ctrl Pts',(1.99731373093364,-0.0237999900573737,
10.8783675871078));
#26201=CARTESIAN_POINT('Ctrl Pts',(1.9933618471923,-0.127804115035621,10.8711102724036));
#26202=CARTESIAN_POINT('Ctrl Pts',(1.96840327881251,-0.341862118209449,
10.8560819114379));
#26203=CARTESIAN_POINT('Ctrl Pts',(1.94619830397782,-0.45144183950228,10.8483393833563));
#26204=CARTESIAN_POINT('Ctrl Pts',(1.91298558663952,-0.565298499776993,
10.8405935926979));
#26205=CARTESIAN_POINT('Ctrl Pts',(1.91099646315087,-0.571986686768454,
10.8401397531064));
#26206=CARTESIAN_POINT('Ctrl Pts',(1.9079600016913,-0.582003754515409,10.839461919585));
#26207=CARTESIAN_POINT('Ctrl Pts',(1.90693898253526,-0.58534046132441,10.8392364479633));
#26208=CARTESIAN_POINT('Ctrl Pts',(1.90515998825462,-0.591100183475566,
10.83884781316));
#26209=CARTESIAN_POINT('Ctrl Pts',(1.9044061375858,-0.593524448573728,10.8386844109206));
#26210=CARTESIAN_POINT('Ctrl Pts',(1.90282145889481,-0.59858642293466,10.8383435932321));
#26211=CARTESIAN_POINT('Ctrl Pts',(1.90198977273272,-0.601223847402193,
10.8381662315056));
#26212=CARTESIAN_POINT('Ctrl Pts',(1.8999729660485,-0.607573431998805,10.8377397304922));
#26213=CARTESIAN_POINT('Ctrl Pts',(1.89878243922579,-0.611283891576089,
10.8374909083308));
#26214=CARTESIAN_POINT('Ctrl Pts',(1.89462939570906,-0.624098287545705,
10.8366329175562));
#26215=CARTESIAN_POINT('Ctrl Pts',(1.89161215794336,-0.633184548359881,
10.8360268838645));
#26216=CARTESIAN_POINT('Ctrl Pts',(1.86591014906682,-0.708761165815411,
10.83100287727));
#26217=CARTESIAN_POINT('Ctrl Pts',(1.83978999220034,-0.774040176661591,
10.826771464365));
#26218=CARTESIAN_POINT('Ctrl Pts',(1.71995802878394,-1.0329635103083,10.8099169845858));
#26219=CARTESIAN_POINT('Ctrl Pts',(1.59868925052306,-1.21221524453463,10.7979075049042));
#26220=CARTESIAN_POINT('Ctrl Pts',(1.43841788903086,-1.38214516490472,10.7834184070685));
#26221=CARTESIAN_POINT('Ctrl Pts',(1.42551023265425,-1.39545398367508,10.7822607504544));
#26222=CARTESIAN_POINT('Ctrl Pts',(1.4071744588801,-1.4138397261316,10.7806279904034));
#26223=CARTESIAN_POINT('Ctrl Pts',(1.40190036466913,-1.41906944651749,10.7801596713481));
#26224=CARTESIAN_POINT('Ctrl Pts',(1.39334775204551,-1.4274558894862,10.7794022968901));
#26225=CARTESIAN_POINT('Ctrl Pts',(1.39008738814232,-1.43063109407207,10.779114054218));
#26226=CARTESIAN_POINT('Ctrl Pts',(1.38329341326811,-1.43720246157727,10.7785143835791));
#26227=CARTESIAN_POINT('Ctrl Pts',(1.3797580982615,-1.44059681116248,10.778202879712));
#26228=CARTESIAN_POINT('Ctrl Pts',(1.37141879070365,-1.44854474435454,10.7774693301549));
#26229=CARTESIAN_POINT('Ctrl Pts',(1.36660459362305,-1.4530874918027,10.7770468213284));
#26230=CARTESIAN_POINT('Ctrl Pts',(1.35080235057007,-1.46785073063549,10.7756630236307));
#26231=CARTESIAN_POINT('Ctrl Pts',(1.3397217800798,-1.47797100419504,10.7746974823524));
#26232=CARTESIAN_POINT('Ctrl Pts',(1.3134688300473,-1.50141092793196,10.7724204592106));
#26233=CARTESIAN_POINT('Ctrl Pts',(1.29820655542032,-1.51462696130548,10.7711048003558));
#26234=CARTESIAN_POINT('Ctrl Pts',(1.24352974053001,-1.56053957536424,10.7664186534991));
#26235=CARTESIAN_POINT('Ctrl Pts',(1.20306225242803,-1.59194549102781,10.7629984954555));
#26236=CARTESIAN_POINT('Ctrl Pts',(1.07961189172609,-1.68035540833415,10.7527077093552));
#26237=CARTESIAN_POINT('Ctrl Pts',(0.993478856661449,-1.73267209620089,
10.745700469698));
#26238=CARTESIAN_POINT('Ctrl Pts',(0.795663834775676,-1.83320858555724,
10.7302186708135));
#26239=CARTESIAN_POINT('Ctrl Pts',(0.68275319723829,-1.87818796353214,10.7217669820146));
#26240=CARTESIAN_POINT('Ctrl Pts',(0.559888341819996,-1.9145755016175,10.7134005982871));
#26241=CARTESIAN_POINT('Ctrl Pts',(0.55332276636768,-1.91648329661188,10.7129559924206));
#26242=CARTESIAN_POINT('Ctrl Pts',(0.543425704378367,-1.91930403954843,
10.7122896361611));
#26243=CARTESIAN_POINT('Ctrl Pts',(0.540101527074303,-1.92024212882044,
10.7120664755009));
#26244=CARTESIAN_POINT('Ctrl Pts',(0.534338602189818,-1.92185228870698,
10.7116807440751));
#26245=CARTESIAN_POINT('Ctrl Pts',(0.531900995442505,-1.92252835938038,
10.7115179424627));
#26246=CARTESIAN_POINT('Ctrl Pts',(0.526787963007332,-1.92393599100447,
10.7111772102434));
#26247=CARTESIAN_POINT('Ctrl Pts',(0.524112291688488,-1.92466661042395,
10.7109993370033));
#26248=CARTESIAN_POINT('Ctrl Pts',(0.517708900616808,-1.92640077854165,
10.7105746698735));
#26249=CARTESIAN_POINT('Ctrl Pts',(0.513979749351479,-1.92739909806181,
10.7103281792805));
#26250=CARTESIAN_POINT('Ctrl Pts',(0.501271270038886,-1.93076173922968,
10.7094908980206));
#26251=CARTESIAN_POINT('Ctrl Pts',(0.492278171765269,-1.93307423278164,
10.7089030301733));
#26252=CARTESIAN_POINT('Ctrl Pts',(0.470452452215516,-1.93852432549036,
10.7074867761515));
#26253=CARTESIAN_POINT('Ctrl Pts',(0.45760400021766,-1.94159745314368,10.7066617780542));
#26254=CARTESIAN_POINT('Ctrl Pts',(0.409409218789583,-1.95261981403455,
10.7035965335695));
#26255=CARTESIAN_POINT('Ctrl Pts',(0.373877085727865,-1.95973373268864,
10.7013954269203));
#26256=CARTESIAN_POINT('Ctrl Pts',(0.217022144433218,-1.986715817347,10.6918580652488));
#26257=CARTESIAN_POINT('Ctrl Pts',(0.094201094630038,-1.99631375931502,
10.6848434951022));
#26258=CARTESIAN_POINT('Ctrl Pts',(-0.150098987651191,-1.99279492673645,
10.6706009047127));
#26259=CARTESIAN_POINT('Ctrl Pts',(-0.271037755010063,-1.97997311258582,
10.6634023191527));
#26260=CARTESIAN_POINT('Ctrl Pts',(-0.40280551753441,-1.95370018279441,
10.6550161586736));
#26261=CARTESIAN_POINT('Ctrl Pts',(-0.415533921375953,-1.95103260778462,
10.6542006091297));
#26262=CARTESIAN_POINT('Ctrl Pts',(-0.43433448633204,-1.94690013007262,
10.6529875369877));
#26263=CARTESIAN_POINT('Ctrl Pts',(-0.440427490029545,-1.94553082398599,
10.6525930767661));
#26264=CARTESIAN_POINT('Ctrl Pts',(-0.451235666931748,-1.94304848278454,
10.6518909692361));
#26265=CARTESIAN_POINT('Ctrl Pts',(-0.455953425466466,-1.94194683415626,
10.6515836899444));
#26266=CARTESIAN_POINT('Ctrl Pts',(-0.465850284518916,-1.93959775571201,
10.6509373601097));
#26267=CARTESIAN_POINT('Ctrl Pts',(-0.471028487880685,-1.93834674510174,
10.6505981963727));
#26268=CARTESIAN_POINT('Ctrl Pts',(-0.484618831478258,-1.93500575779146,
10.6497054082381));
#26269=CARTESIAN_POINT('Ctrl Pts',(-0.493022396916671,-1.93288168461351,
10.6491506875261));
#26270=CARTESIAN_POINT('Ctrl Pts',(-0.530690230874716,-1.9230991883353,
10.6466520288688));
#26271=CARTESIAN_POINT('Ctrl Pts',(-0.559790539553972,-1.91483080034854,
10.6446884544847));
#26272=CARTESIAN_POINT('Ctrl Pts',(-0.636874061173812,-1.89102146065539,
10.6393947127876));
#26273=CARTESIAN_POINT('Ctrl Pts',(-0.684472333285816,-1.87431791305439,
10.636028398905));
#26274=CARTESIAN_POINT('Ctrl Pts',(-0.877401596119748,-1.79828440702858,
10.6219833888218));
#26275=CARTESIAN_POINT('Ctrl Pts',(-1.0161119061499,-1.723707522456,10.6108727852393));
#26276=CARTESIAN_POINT('Ctrl Pts',(-1.1581947589843,-1.62415731277163,10.59892463305));
#26277=CARTESIAN_POINT('Ctrl Pts',(-1.17164534681666,-1.61448111816995,
10.5977880160493));
#26278=CARTESIAN_POINT('Ctrl Pts',(-1.22544568058563,-1.5747512906306,10.5932236350435));
#26279=CARTESIAN_POINT('Ctrl Pts',(-1.26477623830486,-1.54334079418733,
10.5898448501145));
#26280=CARTESIAN_POINT('Ctrl Pts',(-1.30830296841903,-1.50579619735658,
10.5860947100608));
#26281=CARTESIAN_POINT('Ctrl Pts',(-1.3137004703893,-1.5010895786146,10.5856294844136));
#26282=CARTESIAN_POINT('Ctrl Pts',(-1.32166963728357,-1.494064562879,10.584942466842));
#26283=CARTESIAN_POINT('Ctrl Pts',(-1.32426072709766,-1.4917684388939,10.5847190693551));
#26284=CARTESIAN_POINT('Ctrl Pts',(-1.32886096642559,-1.48767045326297,
10.5843224312973));
#26285=CARTESIAN_POINT('Ctrl Pts',(-1.33087244476128,-1.48587125340549,
10.5841489945939));
#26286=CARTESIAN_POINT('Ctrl Pts',(-1.33476482285541,-1.48237540665768,
10.5838133751035));
#26287=CARTESIAN_POINT('Ctrl Pts',(-1.33664613006854,-1.48067927038371,
10.5836511557962));
#26288=CARTESIAN_POINT('Ctrl Pts',(-1.34196213486135,-1.47586811449661,
10.5831927444763));
#26289=CARTESIAN_POINT('Ctrl Pts',(-1.34538923787452,-1.47274466980684,
10.5828971835219));
#26290=CARTESIAN_POINT('Ctrl Pts',(-1.35975228755055,-1.45956228161801,
10.5816581807811));
#26291=CARTESIAN_POINT('Ctrl Pts',(-1.37058690733418,-1.44939294131666,
10.5807228128043));
#26292=CARTESIAN_POINT('Ctrl Pts',(-1.39888315082848,-1.42223310402637,
10.578274721014));
#26293=CARTESIAN_POINT('Ctrl Pts',(-1.41614936628058,-1.4050416929023,10.576775512938));
#26294=CARTESIAN_POINT('Ctrl Pts',(-1.48722382436947,-1.33163351269884,
10.5705584605321));
#26295=CARTESIAN_POINT('Ctrl Pts',(-1.53803771669201,-1.27260540314262,
10.5659986970419));
#26296=CARTESIAN_POINT('Ctrl Pts',(-1.69062725996627,-1.07281551577602,
10.551376716922));
#26297=CARTESIAN_POINT('Ctrl Pts',(-1.77751254700866,-0.921735378559279,
10.5414384016456));
#26298=CARTESIAN_POINT('Ctrl Pts',(-1.85148416868359,-0.742593142861553,
10.529436796406));
#26299=CARTESIAN_POINT('Ctrl Pts',(-1.85893220067566,-0.72374666056684,
10.5281728602616));
#26300=CARTESIAN_POINT('Ctrl Pts',(-1.8688144019601,-0.697581306868724,
10.5264149377355));
#26301=CARTESIAN_POINT('Ctrl Pts',(-1.87149536157609,-0.690356471377057,
10.5259292106535));
#26302=CARTESIAN_POINT('Ctrl Pts',(-1.87571111221322,-0.678790531014614,
10.5251510395536));
#26303=CARTESIAN_POINT('Ctrl Pts',(-1.87727287234161,-0.674459282436686,
10.5248594960355));
#26304=CARTESIAN_POINT('Ctrl Pts',(-1.88045574173863,-0.665535487599173,
10.5242585320391));
#26305=CARTESIAN_POINT('Ctrl Pts',(-1.88207505375224,-0.660942337306063,
10.5239490542189));
#26306=CARTESIAN_POINT('Ctrl Pts',(-1.88579234504433,-0.650273869073988,
10.523229847435));
#26307=CARTESIAN_POINT('Ctrl Pts',(-1.88787780509945,-0.644194275698024,
10.5228197070701));
#26308=CARTESIAN_POINT('Ctrl Pts',(-1.89439916021462,-0.624879375940557,
10.5215157094706));
#26309=CARTESIAN_POINT('Ctrl Pts',(-1.89872545071886,-0.611607765661261,
10.5206182519358));
#26310=CARTESIAN_POINT('Ctrl Pts',(-1.94370860280674,-0.468535547863655,
10.5109259451319));
#26311=CARTESIAN_POINT('Ctrl Pts',(-1.97111857903476,-0.334972842261761,
10.5016865325503));
#26312=CARTESIAN_POINT('Ctrl Pts',(-1.99145701881209,-0.132824304519319,
10.4875693700212));
#26313=CARTESIAN_POINT('Ctrl Pts',(-1.99480094163841,-0.0656668475864861,
10.4828651127876));
#26314=CARTESIAN_POINT('Ctrl Pts',(-1.99474941351911,0.00152962909411654,
10.478194963257));
#26315=CARTESIAN_POINT('',(-1.99474949650966,-0.00141727712825375,9.67904511860478));
#26316=CARTESIAN_POINT('Ctrl Pts',(-1.99474949650966,-0.00141727712825375,
9.67904511860478));
#26317=CARTESIAN_POINT('Ctrl Pts',(-1.99468698571738,-0.0893982153304589,
9.68468225042636));
#26318=CARTESIAN_POINT('Ctrl Pts',(-1.98880353854553,-0.177174871919355,
9.69031938224794));
#26319=CARTESIAN_POINT('Ctrl Pts',(-1.97718053383553,-0.264167937346383,
9.69595651406953));
#26320=CARTESIAN_POINT('Ctrl Pts',(-1.967996907368,-0.332903332201714,9.70041055278751));
#26321=CARTESIAN_POINT('Ctrl Pts',(-1.95520650942798,-0.401295387301663,
9.70486459150549));
#26322=CARTESIAN_POINT('Ctrl Pts',(-1.93884667508122,-0.468936171591067,
9.70931863022347));
#26323=CARTESIAN_POINT('Ctrl Pts',(-1.92251143210734,-0.536475281272242,
9.71376597382923));
#26324=CARTESIAN_POINT('Ctrl Pts',(-1.90261751589915,-0.603264889514319,
9.71821331743499));
#26325=CARTESIAN_POINT('Ctrl Pts',(-1.87925378838465,-0.668904149592394,
9.72266066104075));
#26326=CARTESIAN_POINT('Ctrl Pts',(-1.85591760430336,-0.734466027729838,
9.72710276168554));
#26327=CARTESIAN_POINT('Ctrl Pts',(-1.82911989663795,-0.798879792183266,
9.73154486233033));
#26328=CARTESIAN_POINT('Ctrl Pts',(-1.79899969029709,-0.861758479396032,
9.73598696297511));
#26329=CARTESIAN_POINT('Ctrl Pts',(-1.76889848391584,-0.924597502454316,
9.74042626152313));
#26330=CARTESIAN_POINT('Ctrl Pts',(-1.73547914754314,-0.985902928728562,
9.74486556007115));
#26331=CARTESIAN_POINT('Ctrl Pts',(-1.6989287184433,-1.04530797956804,9.74930485861917));
#26332=CARTESIAN_POINT('Ctrl Pts',(-1.66238892559304,-1.10469574341628,
9.75374286532223));
#26333=CARTESIAN_POINT('Ctrl Pts',(-1.62272010521412,-1.16218381290231,
9.7581808720253));
#26334=CARTESIAN_POINT('Ctrl Pts',(-1.58015423331931,-1.21743178922807,
9.76261887872837));
#26335=CARTESIAN_POINT('Ctrl Pts',(-1.53758628461752,-1.27268246112608,
9.76705710196367));
#26336=CARTESIAN_POINT('Ctrl Pts',(-1.4921213044535,-1.32569243652428,9.77149532519897));
#26337=CARTESIAN_POINT('Ctrl Pts',(-1.44403231901547,-1.37615341591655,
9.77593354843427));
#26338=CARTESIAN_POINT('Ctrl Pts',(-1.39589238860436,-1.42666785314775,
9.78037647347729));
#26339=CARTESIAN_POINT('Ctrl Pts',(-1.34512324289893,-1.47462754943579,
9.78481939852032));
#26340=CARTESIAN_POINT('Ctrl Pts',(-1.29203496222465,-1.51976090846197,
9.78926232356335));
#26341=CARTESIAN_POINT('Ctrl Pts',(-1.23891569173576,-1.56492061368756,
9.7937078421246));
#26342=CARTESIAN_POINT('Ctrl Pts',(-1.18347498097302,-1.60725040063283,
9.79815336068585));
#26343=CARTESIAN_POINT('Ctrl Pts',(-1.12605397614748,-1.64652057542639,
9.8025988792471));
#26344=CARTESIAN_POINT('Ctrl Pts',(-1.06853277006565,-1.68585927777117,
9.80705215536234));
#26345=CARTESIAN_POINT('Ctrl Pts',(-1.00902478978249,-1.72212745539155,
9.81150543147757));
#26346=CARTESIAN_POINT('Ctrl Pts',(-0.947897277366771,-1.75514053968925,
9.81595870759281));
#26347=CARTESIAN_POINT('Ctrl Pts',(-0.915165252298684,-1.77281809698061,
9.81834330889063));
#26348=CARTESIAN_POINT('Ctrl Pts',(-0.881969234569759,-1.78956313413351,
9.82072791018845));
#26349=CARTESIAN_POINT('Ctrl Pts',(-0.848367782930476,-1.80535305892937,
9.82311251148626));
#26350=CARTESIAN_POINT('Ctrl Pts',(-0.785605858444948,-1.83484601293351,
9.82756655020425));
#26351=CARTESIAN_POINT('Ctrl Pts',(-0.721179850639054,-1.86112065847741,
9.83202058892224));
#26352=CARTESIAN_POINT('Ctrl Pts',(-0.655452944263182,-1.88398752659266,
9.83647462764022));
#26353=CARTESIAN_POINT('Ctrl Pts',(-0.589824835639725,-1.90682002225226,
9.84092197124598));
#26354=CARTESIAN_POINT('Ctrl Pts',(-0.522900168142998,-1.92625474766008,
9.84536931485173));
#26355=CARTESIAN_POINT('Ctrl Pts',(-0.455064067573062,-1.94214939098512,
9.84981665845749));
#26356=CARTESIAN_POINT('Ctrl Pts',(-0.387307938792854,-1.95802529615948,
9.85425875910228));
#26357=CARTESIAN_POINT('Ctrl Pts',(-0.318642985354545,-1.97036929698977,
9.85870085974706));
#26358=CARTESIAN_POINT('Ctrl Pts',(-0.249469819512031,-1.97908877306013,
9.86314296039185));
#26359=CARTESIAN_POINT('Ctrl Pts',(-0.18034028840896,-1.98780274884635,
9.86758225893987));
#26360=CARTESIAN_POINT('Ctrl Pts',(-0.110703665453911,-1.99289667441333,
9.8720215574879));
#26361=CARTESIAN_POINT('Ctrl Pts',(-0.0409695867473876,-1.99432922444158,
9.87646085603592));
#26362=CARTESIAN_POINT('Ctrl Pts',(0.0287441991996099,-1.99576135759484,
9.88089886273898));
#26363=CARTESIAN_POINT('Ctrl Pts',(0.0985548953920414,-1.99353422028129,
9.88533686944205));
#26364=CARTESIAN_POINT('Ctrl Pts',(0.168050714418184,-1.98765855213705,
9.88977487614511));
#26365=CARTESIAN_POINT('Ctrl Pts',(0.237549924174972,-1.98178259731645,
9.89421309938042));
#26366=CARTESIAN_POINT('Ctrl Pts',(0.306733738645927,-1.97225780187023,
9.89865132261572));
#26367=CARTESIAN_POINT('Ctrl Pts',(0.375195133089241,-1.95914679761526,
9.90308954585102));
#26368=CARTESIAN_POINT('Ctrl Pts',(0.4437290548247,-1.9460219036982,9.90753247089405));
#26369=CARTESIAN_POINT('Ctrl Pts',(0.511538547200051,-1.92930331023155,
9.91197539593709));
#26370=CARTESIAN_POINT('Ctrl Pts',(0.57822738240554,-1.90910467411728,9.91641832098011));
#26371=CARTESIAN_POINT('Ctrl Pts',(0.644955146629108,-1.88889424722772,
9.92086383954137));
#26372=CARTESIAN_POINT('Ctrl Pts',(0.710560491034047,-1.86519990068222,
9.92530935810261));
#26373=CARTESIAN_POINT('Ctrl Pts',(0.774665598169962,-1.83818409674112,
9.92975487666387));
#26374=CARTESIAN_POINT('Ctrl Pts',(0.838882570507318,-1.81112114946801,
9.9342081527791));
#26375=CARTESIAN_POINT('Ctrl Pts',(0.901593639171837,-1.78072538837797,
9.93866142889434));
#26376=CARTESIAN_POINT('Ctrl Pts',(0.962444797519434,-1.74720564737749,
9.94311470500958));
#26377=CARTESIAN_POINT('Ctrl Pts',(0.995028842930854,-1.72925678999173,
9.94549930630738));
#26378=CARTESIAN_POINT('Ctrl Pts',(1.02708007614375,-1.71041294983575,9.94788390760518));
#26379=CARTESIAN_POINT('Ctrl Pts',(1.05854779817916,-1.69071112892476,9.95026850890298));
#26380=CARTESIAN_POINT('Ctrl Pts',(1.11732427055702,-1.6539114034389,9.95472254762097));
#26381=CARTESIAN_POINT('Ctrl Pts',(1.17429588030865,-1.61397015705659,9.95917658633896));
#26382=CARTESIAN_POINT('Ctrl Pts',(1.22910669744718,-1.57109015934493,9.96363062505694));
#26383=CARTESIAN_POINT('Ctrl Pts',(1.28383512541142,-1.52827461693224,9.96807796866269));
#26384=CARTESIAN_POINT('Ctrl Pts',(1.33640882480859,-1.48252938982695,9.97252531226844));
#26385=CARTESIAN_POINT('Ctrl Pts',(1.38649963422563,-1.43410122613161,9.9769726558742));
#26386=CARTESIAN_POINT('Ctrl Pts',(1.43653139172723,-1.38573015426331,9.98141475651899));
#26387=CARTESIAN_POINT('Ctrl Pts',(1.48408572251719,-1.33468276637419,9.98585685716378));
#26388=CARTESIAN_POINT('Ctrl Pts',(1.528867859064,-1.28124573444014,9.99029895780856));
#26389=CARTESIAN_POINT('Ctrl Pts',(1.5736217468407,-1.22784241082256,9.99473825635658));
#26390=CARTESIAN_POINT('Ctrl Pts',(1.61560659569774,-1.17205280784211,9.99917755490461));
#26391=CARTESIAN_POINT('Ctrl Pts',(1.65456587922435,-1.11419895611447,10.0036168534526));
#26392=CARTESIAN_POINT('Ctrl Pts',(1.69351382551975,-1.05636193997601,10.0080548601557));
#26393=CARTESIAN_POINT('Ctrl Pts',(1.72943768099633,-0.996462273439538,
10.0124928668588));
#26394=CARTESIAN_POINT('Ctrl Pts',(1.76212352850102,-0.934851984435565,
10.0169308735618));
#26395=CARTESIAN_POINT('Ctrl Pts',(1.79481097076216,-0.873238689439306,
10.0213690967971));
#26396=CARTESIAN_POINT('Ctrl Pts',(1.82425986407292,-0.809915039861802,
10.0258073200324));
#26397=CARTESIAN_POINT('Ctrl Pts',(1.85030249858752,-0.745257154424411,
10.0302455432677));
#26398=CARTESIAN_POINT('Ctrl Pts',(1.87637272239938,-0.680530771092921,
10.0346884683108));
#26399=CARTESIAN_POINT('Ctrl Pts',(1.89902930164196,-0.614467785687102,
10.0391313933538));
#26400=CARTESIAN_POINT('Ctrl Pts',(1.91815327178053,-0.54746286491199,10.0435743183968));
#26401=CARTESIAN_POINT('Ctrl Pts',(1.93728840536764,-0.480418830606623,
10.0480198369581));
#26402=CARTESIAN_POINT('Ctrl Pts',(1.95288671590791,-0.41243224383394,10.0524653555193));
#26403=CARTESIAN_POINT('Ctrl Pts',(1.9648802399255,-0.343908716450044,10.0569108740806));
#26404=CARTESIAN_POINT('Ctrl Pts',(1.97689469297729,-0.275265613598047,
10.0613641501958));
#26405=CARTESIAN_POINT('Ctrl Pts',(1.98529174365158,-0.206084185705428,
10.065817426311));
#26406=CARTESIAN_POINT('Ctrl Pts',(1.99005530723546,-0.136775131672311,
10.0702707024263));
#26407=CARTESIAN_POINT('Ctrl Pts',(1.99260605854986,-0.099662126343055,
10.0726553037241));
#26408=CARTESIAN_POINT('Ctrl Pts',(1.994115875531,-0.0625125326038895,10.0750399050219));
#26409=CARTESIAN_POINT('Ctrl Pts',(1.99458841887371,-0.0253890093321778,
10.0774245063197));
#26410=CARTESIAN_POINT('Ctrl Pts',(1.99547105126442,0.043951559320546,10.0818785450377));
#26411=CARTESIAN_POINT('Ctrl Pts',(1.99273525232063,0.113475532771467,10.0863325837557));
#26412=CARTESIAN_POINT('Ctrl Pts',(1.98635879736995,0.182773878360721,10.0907866224737));
#26413=CARTESIAN_POINT('Ctrl Pts',(1.97999192722178,0.251968057769495,10.0952339660794));
#26414=CARTESIAN_POINT('Ctrl Pts',(1.96999530705612,0.320936798924369,10.0996813096852));
#26415=CARTESIAN_POINT('Ctrl Pts',(1.95639872171989,0.389270605302754,10.104128653291));
#26416=CARTESIAN_POINT('Ctrl Pts',(1.94281816536018,0.457523853147437,10.1085707539357));
#26417=CARTESIAN_POINT('Ctrl Pts',(1.92564616800158,0.525143175045106,10.1130128545805));
#26418=CARTESIAN_POINT('Ctrl Pts',(1.90496416063095,0.591725535372297,10.1174549552253));
#26419=CARTESIAN_POINT('Ctrl Pts',(1.88429519956219,0.658265895251632,10.1218942537733));
#26420=CARTESIAN_POINT('Ctrl Pts',(1.86012076569267,0.723770124743734,10.1263335523214));
#26421=CARTESIAN_POINT('Ctrl Pts',(1.83257272224743,0.787848196148626,10.1307728508694));
#26422=CARTESIAN_POINT('Ctrl Pts',(1.80503269533918,0.851907620703676,10.1352108575725));
#26423=CARTESIAN_POINT('Ctrl Pts',(1.77412120099737,0.914541261513069,10.1396488642755));
#26424=CARTESIAN_POINT('Ctrl Pts',(1.74001839207206,0.975378674029203,10.1440868709786));
#26425=CARTESIAN_POINT('Ctrl Pts',(1.70591391925615,1.03621905482865,10.1485250942139));
#26426=CARTESIAN_POINT('Ctrl Pts',(1.66861806419197,1.09526260746632,10.1529633174492));
#26427=CARTESIAN_POINT('Ctrl Pts',(1.62835625142678,1.15216469349626,10.1574015406845));
#26428=CARTESIAN_POINT('Ctrl Pts',(1.58805178571418,1.20912706100673,10.1618444657275));
#26429=CARTESIAN_POINT('Ctrl Pts',(1.54477537414292,1.26394303336169,10.1662873907706));
#26430=CARTESIAN_POINT('Ctrl Pts',(1.49879442690592,1.31629891300409,10.1707303158136));
#26431=CARTESIAN_POINT('Ctrl Pts',(1.4527866386974,1.36868535492846,10.1751758343749));
#26432=CARTESIAN_POINT('Ctrl Pts',(1.40407151451476,1.41860849534032,10.1796213529361));
#26433=CARTESIAN_POINT('Ctrl Pts',(1.35295327934652,1.46579159037208,10.1840668714974));
#26434=CARTESIAN_POINT('Ctrl Pts',(1.30174584143096,1.51305702122177,10.1885201476126));
#26435=CARTESIAN_POINT('Ctrl Pts',(1.2481272981871,1.557572549363,10.1929734237278));
#26436=CARTESIAN_POINT('Ctrl Pts',(1.1924342393508,1.59910229420256,10.1974266998431));
#26437=CARTESIAN_POINT('Ctrl Pts',(1.16261220789733,1.62134027830216,10.1998113011409));
#26438=CARTESIAN_POINT('Ctrl Pts',(1.13219584028356,1.64272289842867,10.2021959024387));
#26439=CARTESIAN_POINT('Ctrl Pts',(1.10123979937559,1.66321930808033,10.2045805037365));
#26440=CARTESIAN_POINT('Ctrl Pts',(1.04341906226252,1.70150319321129,10.2090345424545));
#26441=CARTESIAN_POINT('Ctrl Pts',(0.983485064595533,1.73684415250669,10.2134885811725));
#26442=CARTESIAN_POINT('Ctrl Pts',(0.921769670959649,1.76900204527834,10.2179426198904));
#26443=CARTESIAN_POINT('Ctrl Pts',(0.860147045149284,1.8011115997407,10.2223899634962));
#26444=CARTESIAN_POINT('Ctrl Pts',(0.796748768587733,1.83004735962786,10.226837307102));
#26445=CARTESIAN_POINT('Ctrl Pts',(0.731935254425973,1.85561266050552,10.2312846507077));
#26446=CARTESIAN_POINT('Ctrl Pts',(0.667198148735234,1.88114782252131,10.2357267513525));
#26447=CARTESIAN_POINT('Ctrl Pts',(0.601049572350844,1.90332023848129,10.2401688519973));
#26448=CARTESIAN_POINT('Ctrl Pts',(0.533872468206237,1.92198016383921,10.2446109526421));
#26449=CARTESIAN_POINT('Ctrl Pts',(0.466737739676511,1.94062831843354,10.2490502511901));
#26450=CARTESIAN_POINT('Ctrl Pts',(0.398576241062933,1.95576824713277,10.2534895497381));
#26451=CARTESIAN_POINT('Ctrl Pts',(0.329787283400593,1.96729964931814,10.2579288482861));
#26452=CARTESIAN_POINT('Ctrl Pts',(0.261018343465655,1.97882769584188,10.2623668549892));
#26453=CARTESIAN_POINT('Ctrl Pts',(0.191622789532616,1.98674921954684,10.2668048616923));
#26454=CARTESIAN_POINT('Ctrl Pts',(0.122009612528938,1.9910151222305,10.2712428683953));
#26455=CARTESIAN_POINT('Ctrl Pts',(0.0523930390686258,1.99528123304937,
10.2756810916306));
#26456=CARTESIAN_POINT('Ctrl Pts',(-0.017440689752863,1.99589134118134,
10.2801193148659));
#26457=CARTESIAN_POINT('Ctrl Pts',(-0.0870797690490117,1.992848382673,10.2845575381012));
#26458=CARTESIAN_POINT('Ctrl Pts',(-0.156792623264412,1.98980220048593,
10.2890004631443));
#26459=CARTESIAN_POINT('Ctrl Pts',(-0.226309926300341,1.9830952486958,10.2934433881873));
#26460=CARTESIAN_POINT('Ctrl Pts',(-0.295223155529433,1.97278251486048,
10.2978863132303));
#26461=CARTESIAN_POINT('Ctrl Pts',(-0.364176612246978,1.96246376105793,
10.3023318317916));
#26462=CARTESIAN_POINT('Ctrl Pts',(-0.432524813455108,1.94853513354754,
10.3067773503528));
#26463=CARTESIAN_POINT('Ctrl Pts',(-0.499870373652458,1.93110257936873,
10.3112228689141));
#26464=CARTESIAN_POINT('Ctrl Pts',(-0.567333453732282,1.91363960489625,
10.3156761450293));
#26465=CARTESIAN_POINT('Ctrl Pts',(-0.633789933410183,1.89266064557725,
10.3201294211446));
#26466=CARTESIAN_POINT('Ctrl Pts',(-0.69885926063248,1.86832098321681,10.3245826972598));
#26467=CARTESIAN_POINT('Ctrl Pts',(-0.733702014175411,1.85528779395321,
10.3269672985576));
#26468=CARTESIAN_POINT('Ctrl Pts',(-0.768147394660999,1.84129180790358,
10.3293518998554));
#26469=CARTESIAN_POINT('Ctrl Pts',(-0.80213987253757,1.82636228262232,10.3317365011532));
#26470=CARTESIAN_POINT('Ctrl Pts',(-0.865632169015673,1.79847641184594,
10.3361905398712));
#26471=CARTESIAN_POINT('Ctrl Pts',(-0.927794322756352,1.76722046645013,
10.3406445785892));
#26472=CARTESIAN_POINT('Ctrl Pts',(-0.9882447582517,1.73274344906799,10.3450986173072));
#26473=CARTESIAN_POINT('Ctrl Pts',(-1.04860432735014,1.69831825599977,10.3495459609129));
#26474=CARTESIAN_POINT('Ctrl Pts',(-1.10725686313481,1.660681841223,10.3539933045187));
#26475=CARTESIAN_POINT('Ctrl Pts',(-1.16384188655351,1.62003074835127,10.3584406481244));
#26476=CARTESIAN_POINT('Ctrl Pts',(-1.22036020204599,1.57942757893949,10.3628827487692));
#26477=CARTESIAN_POINT('Ctrl Pts',(-1.27481545044851,1.53581707437227,10.367324849414));
#26478=CARTESIAN_POINT('Ctrl Pts',(-1.32687440306657,1.48944012333049,10.3717669500588));
#26479=CARTESIAN_POINT('Ctrl Pts',(-1.37890051666667,1.4430924270749,10.3762062486068));
#26480=CARTESIAN_POINT('Ctrl Pts',(-1.42853296843998,1.39398207108725,10.3806455471548));
#26481=CARTESIAN_POINT('Ctrl Pts',(-1.4754712381619,1.34239047518112,10.3850848457029));
#26482=CARTESIAN_POINT('Ctrl Pts',(-1.52239584875132,1.29081389253493,10.3895228524059));
#26483=CARTESIAN_POINT('Ctrl Pts',(-1.56662750439063,1.23675786527721,10.393960859109));
#26484=CARTESIAN_POINT('Ctrl Pts',(-1.60790349286346,1.18053967325859,10.3983988658121));
#26485=CARTESIAN_POINT('Ctrl Pts',(-1.64918149520935,1.12431873833043,10.4028370890474));
#26486=CARTESIAN_POINT('Ctrl Pts',(-1.6875032562771,1.06593582523333,10.4072753122827));
#26487=CARTESIAN_POINT('Ctrl Pts',(-1.72264828852599,1.00573875163408,10.411713535518));
#26488=CARTESIAN_POINT('Ctrl Pts',(-1.75783055305802,0.945477905878553,
10.416156460561));
#26489=CARTESIAN_POINT('Ctrl Pts',(-1.78982912428108,0.883399487218074,
10.420599385604));
#26490=CARTESIAN_POINT('Ctrl Pts',(-1.8184690544081,0.819876735040153,10.425042310647));
#26491=CARTESIAN_POINT('Ctrl Pts',(-1.8471257028412,0.756316902017108,10.4294878292083));
#26492=CARTESIAN_POINT('Ctrl Pts',(-1.87241963029432,0.691311513727324,
10.4339333477696));
#26493=CARTESIAN_POINT('Ctrl Pts',(-1.89422476331989,0.625252036002861,
10.4383788663308));
#26494=CARTESIAN_POINT('Ctrl Pts',(-1.91606794691126,0.55907728264574,10.442832142446));
#26495=CARTESIAN_POINT('Ctrl Pts',(-1.93441005440984,0.491845240301353,
10.4472854185613));
#26496=CARTESIAN_POINT('Ctrl Pts',(-1.94917560477138,0.423959932380545,
10.4517386946765));
#26497=CARTESIAN_POINT('Ctrl Pts',(-1.95708213238025,0.387609302152085,
10.4541232959743));
#26498=CARTESIAN_POINT('Ctrl Pts',(-1.9639640388674,0.351071496725345,10.4565078972722));
#26499=CARTESIAN_POINT('Ctrl Pts',(-1.96981585838471,0.314409043375201,
10.45889249857));
#26500=CARTESIAN_POINT('Ctrl Pts',(-1.98630072391942,0.211129095683448,
10.4656100385816));
#26501=CARTESIAN_POINT('Ctrl Pts',(-1.99466579522122,0.106519654372821,
10.4723275785932));
#26502=CARTESIAN_POINT('Ctrl Pts',(-1.99474936733483,0.00158871561359909,
10.4790451186048));
#26503=CARTESIAN_POINT('',(-1.99474901028124,0.00181008058995216,8.0796215781142));
#26504=CARTESIAN_POINT('Ctrl Pts',(-1.99474944855383,-0.00148323773318863,
9.67792750393623));
#26505=CARTESIAN_POINT('Ctrl Pts',(-1.99486336953519,0.151724713795801,
9.66888523581739));
#26506=CARTESIAN_POINT('Ctrl Pts',(-1.97732707703499,0.304441334498287,
9.6602202180674));
#26507=CARTESIAN_POINT('Ctrl Pts',(-1.93172749597254,0.499691205536763,
9.64826446450008));
#26508=CARTESIAN_POINT('Ctrl Pts',(-1.91934370848134,0.545327112525534,
9.64540865916488));
#26509=CARTESIAN_POINT('Ctrl Pts',(-1.89970424492805,0.608699655848255,
9.6413303975882));
#26510=CARTESIAN_POINT('Ctrl Pts',(-1.89379623677535,0.626839105852974,
9.64014992783809));
#26511=CARTESIAN_POINT('Ctrl Pts',(-1.88299127327452,0.658465810929409,
9.63806704965448));
#26512=CARTESIAN_POINT('Ctrl Pts',(-1.8782072115945,0.671990336719134,9.63716834279593));
#26513=CARTESIAN_POINT('Ctrl Pts',(-1.87104445499723,0.691565216930016,
9.6358554469013));
#26514=CARTESIAN_POINT('Ctrl Pts',(-1.86878132904338,0.697657612615147,
9.63544510599797));
#26515=CARTESIAN_POINT('Ctrl Pts',(-1.8647663648102,0.708306286143245,9.63472482129508));
#26516=CARTESIAN_POINT('Ctrl Pts',(-1.86302749063099,0.712867420196114,
9.63441531338033));
#26517=CARTESIAN_POINT('Ctrl Pts',(-1.85962358977727,0.72169846274358,9.63381411915987));
#26518=CARTESIAN_POINT('Ctrl Pts',(-1.8579605533933,0.725969109700604,9.63352250131237));
#26519=CARTESIAN_POINT('Ctrl Pts',(-1.85350206960992,0.737302747064408,
9.63274622118121));
#26520=CARTESIAN_POINT('Ctrl Pts',(-1.85068099148227,0.744355511834768,
9.6322606978397));
#26521=CARTESIAN_POINT('Ctrl Pts',(-1.84045298877569,0.769508171744016,
9.63052023989566));
#26522=CARTESIAN_POINT('Ctrl Pts',(-1.8328204523368,0.787514555075603,9.62925769992512));
#26523=CARTESIAN_POINT('Ctrl Pts',(-1.75158546050174,0.971580563808394,
9.61617593931634));
#26524=CARTESIAN_POINT('Ctrl Pts',(-1.65590593230408,1.12692811677535,9.60353424567096));
#26525=CARTESIAN_POINT('Ctrl Pts',(-1.49593765891223,1.32141400560299,9.58598725502769));
#26526=CARTESIAN_POINT('Ctrl Pts',(-1.44846449981781,1.37328670888208,9.58111673887083));
#26527=CARTESIAN_POINT('Ctrl Pts',(-1.38075488412061,1.4398445186779,9.57470467126326));
#26528=CARTESIAN_POINT('Ctrl Pts',(-1.36283960395149,1.45681317385472,9.57305451644416));
#26529=CARTESIAN_POINT('Ctrl Pts',(-1.33352065474393,1.48356858302032,9.57043377577451));
#26530=CARTESIAN_POINT('Ctrl Pts',(-1.32231369304064,1.49356607064646,9.56945008067372));
#26531=CARTESIAN_POINT('Ctrl Pts',(-1.30749423639179,1.50648861665987,9.56817394597322));
#26532=CARTESIAN_POINT('Ctrl Pts',(-1.30398328942877,1.50952863910247,9.56787339353341));
#26533=CARTESIAN_POINT('Ctrl Pts',(-1.29854068529335,1.51420806676782,9.56741027341006));
#26534=CARTESIAN_POINT('Ctrl Pts',(-1.29661649785109,1.51585607446859,9.56724707683529));
#26535=CARTESIAN_POINT('Ctrl Pts',(-1.29263640341932,1.51925178036044,9.56691062614857));
#26536=CARTESIAN_POINT('Ctrl Pts',(-1.29058011519985,1.52099895132617,9.56673741410326));
#26537=CARTESIAN_POINT('Ctrl Pts',(-1.28588044539942,1.52497573780478,9.56634292316337));
#26538=CARTESIAN_POINT('Ctrl Pts',(-1.28323481259262,1.52720265090973,9.56612184352126));
#26539=CARTESIAN_POINT('Ctrl Pts',(-1.27633252856082,1.532981923205,9.56554760550749));
#26540=CARTESIAN_POINT('Ctrl Pts',(-1.27206679865696,1.53652346608833,9.56519522332301));
#26541=CARTESIAN_POINT('Ctrl Pts',(-1.24502018350139,1.55878858073761,9.56297634307845));
#26542=CARTESIAN_POINT('Ctrl Pts',(-1.22183981665658,1.57702402741135,9.56114324914027));
#26543=CARTESIAN_POINT('Ctrl Pts',(-1.1122436033823,1.65937287633308,9.55274492284177));
#26544=CARTESIAN_POINT('Ctrl Pts',(-1.02112705945747,1.71694748922594,9.54651209429306));
#26545=CARTESIAN_POINT('Ctrl Pts',(-0.847640943653099,1.8078492242881,9.53515261173411));
#26546=CARTESIAN_POINT('Ctrl Pts',(-0.766850938651475,1.84357059554135,
9.53004181610148));
#26547=CARTESIAN_POINT('Ctrl Pts',(-0.636580822203791,1.89112052854411,
9.52179483033571));
#26548=CARTESIAN_POINT('Ctrl Pts',(-0.588560410152748,1.90661167015163,
9.51875473565148));
#26549=CARTESIAN_POINT('Ctrl Pts',(-0.510881436795937,1.92845614645175,
9.51380052290897));
#26550=CARTESIAN_POINT('Ctrl Pts',(-0.481574526245821,1.93598263761458,
9.51192342289343));
#26551=CARTESIAN_POINT('Ctrl Pts',(-0.443666096149035,1.94480412887344,
9.50948074370206));
#26552=CARTESIAN_POINT('Ctrl Pts',(-0.435210621159321,1.94671374782314,
9.50893498088891));
#26553=CARTESIAN_POINT('Ctrl Pts',(-0.421539082459801,1.9497078614206,9.50805095112077));
#26554=CARTESIAN_POINT('Ctrl Pts',(-0.416330587801435,1.95082669237658,
9.50771378704969));
#26555=CARTESIAN_POINT('Ctrl Pts',(-0.406377063005334,1.95292312084013,
9.50706872451976));
#26556=CARTESIAN_POINT('Ctrl Pts',(-0.40163282429066,1.95390432391677,9.50676094398615));
#26557=CARTESIAN_POINT('Ctrl Pts',(-0.390765200748853,1.95611071190383,
9.50605516097626));
#26558=CARTESIAN_POINT('Ctrl Pts',(-0.384639566684875,1.95732443953873,
9.50565679564035));
#26559=CARTESIAN_POINT('Ctrl Pts',(-0.365741056470827,1.96097683191608,
9.50442604439248));
#26560=CARTESIAN_POINT('Ctrl Pts',(-0.35295015794745,1.96331933938194,9.50359060745366));
#26561=CARTESIAN_POINT('Ctrl Pts',(-0.212729013835741,1.98758470919543,
9.49440389526563));
#26562=CARTESIAN_POINT('Ctrl Pts',(-0.0835038945242882,1.99718852518692,
9.48565250788074));
#26563=CARTESIAN_POINT('Ctrl Pts',(0.199241833779904,1.99070637977901,9.46604142701777));
#26564=CARTESIAN_POINT('Ctrl Pts',(0.351849080245797,1.9694709525747,9.45515173709032));
#26565=CARTESIAN_POINT('Ctrl Pts',(0.512109552224375,1.92793020432786,9.44418031865727));
#26566=CARTESIAN_POINT('Ctrl Pts',(0.523678643368025,1.92481992944447,9.44339126209958));
#26567=CARTESIAN_POINT('Ctrl Pts',(0.540984731063669,1.91999971399818,9.4422160844827));
#26568=CARTESIAN_POINT('Ctrl Pts',(0.546742962334904,1.91836793037592,9.44182593098086));
#26569=CARTESIAN_POINT('Ctrl Pts',(0.557069618074718,1.91539126041386,9.4411278976481));
#26570=CARTESIAN_POINT('Ctrl Pts',(0.561640707318694,1.91405589178286,9.44081949860981));
#26571=CARTESIAN_POINT('Ctrl Pts',(0.569101392256097,1.91184734727703,9.44031715321085));
#26572=CARTESIAN_POINT('Ctrl Pts',(0.57199383216599,1.91098396911628,9.44012264630375));
#26573=CARTESIAN_POINT('Ctrl Pts',(0.577468076498849,1.90933639351579,9.43975500622046));
#26574=CARTESIAN_POINT('Ctrl Pts',(0.580050219461494,1.90855353238875,9.439581800778));
#26575=CARTESIAN_POINT('Ctrl Pts',(0.585937042773836,1.90675569884789,9.43918738597544));
#26576=CARTESIAN_POINT('Ctrl Pts',(0.589240671398546,1.90573737560933,9.4389663755741));
#26577=CARTESIAN_POINT('Ctrl Pts',(0.599355158121452,1.90259083184598,9.43829069211669));
#26578=CARTESIAN_POINT('Ctrl Pts',(0.606157351188761,1.90043462089591,9.4378376292902));
#26579=CARTESIAN_POINT('Ctrl Pts',(0.660146832836769,1.88300125697074,9.43425128168266));
#26580=CARTESIAN_POINT('Ctrl Pts',(0.706765523435961,1.86600402430718,9.4312131466318));
#26581=CARTESIAN_POINT('Ctrl Pts',(0.779133320424617,1.83651658718984,9.42651872848952));
#26582=CARTESIAN_POINT('Ctrl Pts',(0.805327206027938,1.82518221225195,9.42482422109435));
#26583=CARTESIAN_POINT('Ctrl Pts',(0.95484966681138,1.75663634334875,9.41513065598344));
#26584=CARTESIAN_POINT('Ctrl Pts',(1.07231442600455,1.687498914872,9.40740715138574));
#26585=CARTESIAN_POINT('Ctrl Pts',(1.25047742352823,1.55646834964144,9.39432100124064));
#26586=CARTESIAN_POINT('Ctrl Pts',(1.31580481980559,1.50164655647361,9.38917315177025));
#26587=CARTESIAN_POINT('Ctrl Pts',(1.38581084034302,1.43481370363919,9.38312228310928));
#26588=CARTESIAN_POINT('Ctrl Pts',(1.39412881194766,1.42673294487213,9.38239419207877));
#26589=CARTESIAN_POINT('Ctrl Pts',(1.40661567089511,1.41438872416205,9.38128698759398));
#26590=CARTESIAN_POINT('Ctrl Pts',(1.41083677900199,1.41017824774195,9.38091020358462));
#26591=CARTESIAN_POINT('Ctrl Pts',(1.41840166453435,1.40256445251813,9.38023039137447));
#26592=CARTESIAN_POINT('Ctrl Pts',(1.42175224075325,1.39916792797931,9.379927666485));
#26593=CARTESIAN_POINT('Ctrl Pts',(1.42892689674726,1.39184250043757,9.37927590381884));
#26594=CARTESIAN_POINT('Ctrl Pts',(1.43274702059242,1.38790979399437,9.3789266966069));
#26595=CARTESIAN_POINT('Ctrl Pts',(1.44304976063602,1.37721555804097,9.37797893727992));
#26596=CARTESIAN_POINT('Ctrl Pts',(1.44950097864109,1.37042409966146,9.37737903229982));
#26597=CARTESIAN_POINT('Ctrl Pts',(1.47868666582193,1.33926250709052,9.37463514795554));
#26598=CARTESIAN_POINT('Ctrl Pts',(1.50085486365954,1.31437162691787,9.37246727035655));
#26599=CARTESIAN_POINT('Ctrl Pts',(1.52668728368815,1.28386049386743,9.36983604305288));
#26600=CARTESIAN_POINT('Ctrl Pts',(1.530960988755,1.27876122832517,9.36939714683275));
#26601=CARTESIAN_POINT('Ctrl Pts',(1.6667754524153,1.11505446950515,9.35533393798749));
#26602=CARTESIAN_POINT('Ctrl Pts',(1.77296149708675,0.937049072963789,9.34066303333356));
#26603=CARTESIAN_POINT('Ctrl Pts',(1.86475313706949,0.709422682285681,9.32384215273139));
#26604=CARTESIAN_POINT('Ctrl Pts',(1.87842333062044,0.672392009293282,9.32116778176887));
#26605=CARTESIAN_POINT('Ctrl Pts',(1.89544833692532,0.621690929561978,9.3176106430329));
#26606=CARTESIAN_POINT('Ctrl Pts',(1.89976994451975,0.608356961732152,9.3166847887765));
#26607=CARTESIAN_POINT('Ctrl Pts',(1.90688191491739,0.585598408311192,9.31512216619474));
#26608=CARTESIAN_POINT('Ctrl Pts',(1.90974376681167,0.576196917699078,9.3144817304523));
#26609=CARTESIAN_POINT('Ctrl Pts',(1.9136549941804,0.562998786128454,9.31359013646199));
#26610=CARTESIAN_POINT('Ctrl Pts',(1.91476272412859,0.559219796566307,9.31333570308313));
#26611=CARTESIAN_POINT('Ctrl Pts',(1.91663149301684,0.552773890202215,9.31290319515993));
#26612=CARTESIAN_POINT('Ctrl Pts',(1.91739817080719,0.550108633486317,9.31272479335456));
#26613=CARTESIAN_POINT('Ctrl Pts',(1.91885361076846,0.545008975550902,9.31238427857065));
#26614=CARTESIAN_POINT('Ctrl Pts',(1.91954330093344,0.542574860279767,9.31222211047175));
#26615=CARTESIAN_POINT('Ctrl Pts',(1.92116396323076,0.536813307652533,9.31183910197306));
#26616=CARTESIAN_POINT('Ctrl Pts',(1.92209092835677,0.533484736852513,9.31161849454324));
#26617=CARTESIAN_POINT('Ctrl Pts',(1.92482763183762,0.523557982274807,9.31096251287666));
#26618=CARTESIAN_POINT('Ctrl Pts',(1.92661210011941,0.516952794753302,9.31052856908641));
#26619=CARTESIAN_POINT('Ctrl Pts',(1.95931462873756,0.393383164968282,9.30245552124495));
#26620=CARTESIAN_POINT('Ctrl Pts',(1.97956778746662,0.273834093442378,9.29539201102278));
#26621=CARTESIAN_POINT('Ctrl Pts',(1.99659794082646,0.052703355300665,9.2825133151697));
#26622=CARTESIAN_POINT('Ctrl Pts',(1.99671137894172,-0.0482030712533112,
9.27670469174242));
#26623=CARTESIAN_POINT('Ctrl Pts',(1.98537697876301,-0.199845422790136,
9.26766790235005));
#26624=CARTESIAN_POINT('Ctrl Pts',(1.97958048428358,-0.250839473240393,
9.2645776546791));
#26625=CARTESIAN_POINT('Ctrl Pts',(1.96719463000029,-0.331829966342706,
9.25954889572562));
#26626=CARTESIAN_POINT('Ctrl Pts',(1.96186740813082,-0.36199717175393,9.25764885547487));
#26627=CARTESIAN_POINT('Ctrl Pts',(1.95413690913784,-0.400564977595431,
9.25518035314113));
#26628=CARTESIAN_POINT('Ctrl Pts',(1.95237002626808,-0.409090011598,9.25463223447236));
#26629=CARTESIAN_POINT('Ctrl Pts',(1.94943037190413,-0.422820597511132,
9.25374531146253));
#26630=CARTESIAN_POINT('Ctrl Pts',(1.9482924087709,-0.428033551961868,9.25340762333217));
#26631=CARTESIAN_POINT('Ctrl Pts',(1.94608178495891,-0.437968833899344,
9.25276217215791));
#26632=CARTESIAN_POINT('Ctrl Pts',(1.94501281473625,-0.442691950512122,
9.25245452962264));
#26633=CARTESIAN_POINT('Ctrl Pts',(1.94252965578907,-0.453480862444908,
9.25174993034045));
#26634=CARTESIAN_POINT('Ctrl Pts',(1.94110423975489,-0.45954399699574,9.25135261503699));
#26635=CARTESIAN_POINT('Ctrl Pts',(1.9366347083908,-0.478163676977603,9.25012827452099));
#26636=CARTESIAN_POINT('Ctrl Pts',(1.93349702260022,-0.490697204252851,
9.24929824414072));
#26637=CARTESIAN_POINT('Ctrl Pts',(1.9024132313487,-0.609932528231575,9.24134433307812));
#26638=CARTESIAN_POINT('Ctrl Pts',(1.86578895098847,-0.714155400904201,
9.23393437542665));
#26639=CARTESIAN_POINT('Ctrl Pts',(1.75049223543347,-0.971795668455693,
9.21448487254357));
#26640=CARTESIAN_POINT('Ctrl Pts',(1.66023016327808,-1.11903825025194,9.20221411777309));
#26641=CARTESIAN_POINT('Ctrl Pts',(1.54047957564099,-1.26739831390781,9.18956985716378));
#26642=CARTESIAN_POINT('Ctrl Pts',(1.52855488167458,-1.28175498627609,9.18834386125351));
#26643=CARTESIAN_POINT('Ctrl Pts',(1.51317003808025,-1.29975735275129,9.18680571452252));
#26644=CARTESIAN_POINT('Ctrl Pts',(1.50989570677115,-1.30355962509467,9.18648079599734));
#26645=CARTESIAN_POINT('Ctrl Pts',(1.50463601229805,-1.30962096699599,9.18596281283034));
#26646=CARTESIAN_POINT('Ctrl Pts',(1.50265985434682,-1.31188794076649,9.18576908020964));
#26647=CARTESIAN_POINT('Ctrl Pts',(1.49889083893141,-1.31619192331911,9.18540127419574));
#26648=CARTESIAN_POINT('Ctrl Pts',(1.49709897390799,-1.31822971763192,9.18522713491098));
#26649=CARTESIAN_POINT('Ctrl Pts',(1.49297019082687,-1.32290588994334,9.18482753253087));
#26650=CARTESIAN_POINT('Ctrl Pts',(1.4906304364177,-1.32554173334375,9.18460228456331));
#26651=CARTESIAN_POINT('Ctrl Pts',(1.48436043481582,-1.3325675894896,9.18400183547347));
#26652=CARTESIAN_POINT('Ctrl Pts',(1.48041766471036,-1.3369464540924,9.1836275539037));
#26653=CARTESIAN_POINT('Ctrl Pts',(1.45228802088711,-1.36791038759687,9.1809800082683));
#26654=CARTESIAN_POINT('Ctrl Pts',(1.42740413507433,-1.39385693296275,9.1787566260397));
#26655=CARTESIAN_POINT('Ctrl Pts',(1.34747306490184,-1.47281427228912,9.1719207254313));
#26656=CARTESIAN_POINT('Ctrl Pts',(1.29007038151825,-1.52334693184688,9.16744040352308));
#26657=CARTESIAN_POINT('Ctrl Pts',(1.14781660199042,-1.63475261993657,9.15692783015908));
#26658=CARTESIAN_POINT('Ctrl Pts',(1.06081636022466,-1.69250317833966,9.15093547937382));
#26659=CARTESIAN_POINT('Ctrl Pts',(0.920949581230171,-1.77030837267695,
9.14145738766702));
#26660=CARTESIAN_POINT('Ctrl Pts',(0.871084241938938,-1.79536942107091,
9.13810794791522));
#26661=CARTESIAN_POINT('Ctrl Pts',(0.79057738974391,-1.83168601482136,9.13269576415827));
#26662=CARTESIAN_POINT('Ctrl Pts',(0.760596270751748,-1.84433711367415,
9.13067950184846));
#26663=CARTESIAN_POINT('Ctrl Pts',(0.722046727561138,-1.85950400284161,
9.12808047227522));
#26664=CARTESIAN_POINT('Ctrl Pts',(0.713751442382475,-1.86270381106109,
9.12752082905616));
#26665=CARTESIAN_POINT('Ctrl Pts',(0.700405721877602,-1.86774952768151,
9.12661975012612));
#26666=CARTESIAN_POINT('Ctrl Pts',(0.695368667308701,-1.86963068251336,
9.12627949674023));
#26667=CARTESIAN_POINT('Ctrl Pts',(0.685789263783826,-1.87316417087338,
9.12563207607209));
#26668=CARTESIAN_POINT('Ctrl Pts',(0.681248387359192,-1.87482040724166,
9.12532504174964));
#26669=CARTESIAN_POINT('Ctrl Pts',(0.670913657572252,-1.87854738647071,
9.12462591112992));
#26670=CARTESIAN_POINT('Ctrl Pts',(0.665116174512405,-1.88060785176839,
9.12423347623666));
#26671=CARTESIAN_POINT('Ctrl Pts',(0.647477075305257,-1.88678514180739,
9.12303868461662));
#26672=CARTESIAN_POINT('Ctrl Pts',(0.635606275763195,-1.89081712089569,
9.12223352953804));
#26673=CARTESIAN_POINT('Ctrl Pts',(0.47442830436635,-1.94387274980272,9.11128508193633));
#26674=CARTESIAN_POINT('Ctrl Pts',(0.319907204669216,-1.97518669737377,
9.1005327593222));
#26675=CARTESIAN_POINT('Ctrl Pts',(0.072849997082817,-1.99548641573738,
9.08325253933275));
#26676=CARTESIAN_POINT('Ctrl Pts',(-0.0180556654180757,-1.99673444006547,
9.07689179547007));
#26677=CARTESIAN_POINT('Ctrl Pts',(-0.142959150029688,-1.98991586999494,
9.06835712747401));
#26678=CARTESIAN_POINT('Ctrl Pts',(-0.177133731720543,-1.98716542376212,
9.06604396697868));
#26679=CARTESIAN_POINT('Ctrl Pts',(-0.230279291309521,-1.98150606657555,
9.06249739820565));
#26680=CARTESIAN_POINT('Ctrl Pts',(-0.24930678216805,-1.97920212188548,
9.06123783706724));
#26681=CARTESIAN_POINT('Ctrl Pts',(-0.273316924148852,-1.97594308252605,
9.05966382509495));
#26682=CARTESIAN_POINT('Ctrl Pts',(-0.278332345629832,-1.9752428491579,
9.05933588499108));
#26683=CARTESIAN_POINT('Ctrl Pts',(-0.286332198725828,-1.97409486623535,
9.05881422209364));
#26684=CARTESIAN_POINT('Ctrl Pts',(-0.289318332913555,-1.97365943654459,
9.05861981483929));
#26685=CARTESIAN_POINT('Ctrl Pts',(-0.294985115165702,-1.9728199850055,
9.05825150292939));
#26686=CARTESIAN_POINT('Ctrl Pts',(-0.297665894506263,-1.97241728007503,
9.05807752915041));
#26687=CARTESIAN_POINT('Ctrl Pts',(-0.303811081637851,-1.97148134032565,
9.05767931879889));
#26688=CARTESIAN_POINT('Ctrl Pts',(-0.307274907112855,-1.97094443871356,
9.05745529228092));
#26689=CARTESIAN_POINT('Ctrl Pts',(-0.318223443835052,-1.96921782389349,
9.05674849518524));
#26690=CARTESIAN_POINT('Ctrl Pts',(-0.325702911167279,-1.96799456712226,
9.05626758716477));
#26691=CARTESIAN_POINT('Ctrl Pts',(-0.453220567830481,-1.94639232860153,
9.04809888668501));
#26692=CARTESIAN_POINT('Ctrl Pts',(-0.571172712391881,-1.91510403723221,
9.04099376209606));
#26693=CARTESIAN_POINT('Ctrl Pts',(-0.779933774678313,-1.83870399558062,
9.02808645854503));
#26694=CARTESIAN_POINT('Ctrl Pts',(-0.871570354730636,-1.79707903400079,
9.02229133038076));
#26695=CARTESIAN_POINT('Ctrl Pts',(-1.00437090827061,-1.72420008152258,
9.0132867311369));
#26696=CARTESIAN_POINT('Ctrl Pts',(-1.04810636664026,-1.69796916664244,
9.01021525285886));
#26697=CARTESIAN_POINT('Ctrl Pts',(-1.11631514555335,-1.65342001699696,
9.00521437845527));
#26698=CARTESIAN_POINT('Ctrl Pts',(-1.14145666655364,-1.63616434928798,
9.0033229059394));
#26699=CARTESIAN_POINT('Ctrl Pts',(-1.17324377663589,-1.61325824248199,
9.00086404565769));
#26700=CARTESIAN_POINT('Ctrl Pts',(-1.1802623499166,-1.60813055995689,9.00031680362441));
#26701=CARTESIAN_POINT('Ctrl Pts',(-1.19153231654802,-1.59978334090053,
8.9994309572435));
#26702=CARTESIAN_POINT('Ctrl Pts',(-1.19580475716871,-1.59659230269748,
8.9990934641401));
#26703=CARTESIAN_POINT('Ctrl Pts',(-1.20393313536772,-1.5904703788967,8.9984481581691));
#26704=CARTESIAN_POINT('Ctrl Pts',(-1.20779129986291,-1.58754250207034,
8.99814046485042));
#26705=CARTESIAN_POINT('Ctrl Pts',(-1.21659132142224,-1.58081371070847,
8.99743542782099));
#26706=CARTESIAN_POINT('Ctrl Pts',(-1.22152607962585,-1.57700363558835,
8.99703772396178));
#26707=CARTESIAN_POINT('Ctrl Pts',(-1.23665677514264,-1.56520775393851,
8.99581101343834));
#26708=CARTESIAN_POINT('Ctrl Pts',(-1.24679270414512,-1.55714586093694,
8.99497898469379));
#26709=CARTESIAN_POINT('Ctrl Pts',(-1.34444847600975,-1.47790784283936,
8.98686092462547));
#26710=CARTESIAN_POINT('Ctrl Pts',(-1.42584483262181,-1.39953987839287,
8.97927500335886));
#26711=CARTESIAN_POINT('Ctrl Pts',(-1.60699211115646,-1.19284135629211,
8.96031864009634));
#26712=CARTESIAN_POINT('Ctrl Pts',(-1.69855689737891,-1.05839469840758,
8.94878479315759));
#26713=CARTESIAN_POINT('Ctrl Pts',(-1.78433229483724,-0.892083856917428,
8.93628676229934));
#26714=CARTESIAN_POINT('Ctrl Pts',(-1.79539736412924,-0.86959979057228,
8.9346326838636));
#26715=CARTESIAN_POINT('Ctrl Pts',(-1.80838328685275,-0.841907360617288,
8.93264373074597));
#26716=CARTESIAN_POINT('Ctrl Pts',(-1.81070933271269,-0.836892962225977,
8.93228549014198));
#26717=CARTESIAN_POINT('Ctrl Pts',(-1.81431587354054,-0.829032695963559,
8.9317269888164));
#26718=CARTESIAN_POINT('Ctrl Pts',(-1.81561056280657,-0.826193430445362,
8.93152586944803));
#26719=CARTESIAN_POINT('Ctrl Pts',(-1.81801013270286,-0.820898271314013,
8.93115195878283));
#26720=CARTESIAN_POINT('Ctrl Pts',(-1.81911669125897,-0.818443204000036,
8.93097906729748));
#26721=CARTESIAN_POINT('Ctrl Pts',(-1.821608295118,-0.812885187404918,8.93058871376438));
#26722=CARTESIAN_POINT('Ctrl Pts',(-1.82299038184303,-0.809780943757151,
8.9303714348269));
#26723=CARTESIAN_POINT('Ctrl Pts',(-1.82704226519411,-0.800617241873368,
8.92973216490358));
#26724=CARTESIAN_POINT('Ctrl Pts',(-1.82968986340451,-0.794547930283797,
8.92931151022863));
#26725=CARTESIAN_POINT('Ctrl Pts',(-1.84771682724285,-0.752655243065184,
8.92642611871348));
#26726=CARTESIAN_POINT('Ctrl Pts',(-1.86207456535152,-0.716398067446356,
8.92401987158389));
#26727=CARTESIAN_POINT('Ctrl Pts',(-1.93366208434713,-0.518892600116926,
8.91127701331208));
#26728=CARTESIAN_POINT('Ctrl Pts',(-1.97103251553399,-0.351200055704026,
8.9016911687405));
#26729=CARTESIAN_POINT('Ctrl Pts',(-1.99199024446832,-0.12090296704569,
8.88803967058595));
#26730=CARTESIAN_POINT('Ctrl Pts',(-1.9947289275133,-0.0608133368123225,
8.88444065486108));
#26731=CARTESIAN_POINT('Ctrl Pts',(-1.99476161125608,0.0329699460048473,
8.87870197308211));
#26732=CARTESIAN_POINT('Ctrl Pts',(-1.99392110303576,0.0666282866475172,
8.87661823930357));
#26733=CARTESIAN_POINT('Ctrl Pts',(-1.99176245128306,0.109527292600944,
8.87392530536294));
#26734=CARTESIAN_POINT('Ctrl Pts',(-1.99123068921559,0.118803315593194,
8.8733408047614));
#26735=CARTESIAN_POINT('Ctrl Pts',(-1.99027977418863,0.133583105184661,
8.87240584832657));
#26736=CARTESIAN_POINT('Ctrl Pts',(-1.98990254356016,0.139089509561404,
8.87205670925127));
#26737=CARTESIAN_POINT('Ctrl Pts',(-1.98915357968622,0.149394661073251,
8.87140175749735));
#26738=CARTESIAN_POINT('Ctrl Pts',(-1.98878732072905,0.154193776062166,
8.87109611897631));
#26739=CARTESIAN_POINT('Ctrl Pts',(-1.98793081888436,0.164905490873897,
8.87041250649036));
#26740=CARTESIAN_POINT('Ctrl Pts',(-1.98743156075167,0.170817304926972,
8.87003425176789));
#26741=CARTESIAN_POINT('Ctrl Pts',(-1.98589097350591,0.188137840307838,
8.86892314950701));
#26742=CARTESIAN_POINT('Ctrl Pts',(-1.98477773979606,0.199539770771446,
8.86818804918902));
#26743=CARTESIAN_POINT('Ctrl Pts',(-1.97508248833094,0.290712470781469,
8.86227979049387));
#26744=CARTESIAN_POINT('Ctrl Pts',(-1.96179425111047,0.369898507814767,
8.85695840979102));
#26745=CARTESIAN_POINT('Ctrl Pts',(-1.9207610851264,0.547908397673107,8.84455584237897));
#26746=CARTESIAN_POINT('Ctrl Pts',(-1.89008778119344,0.645826338051234,
8.83740989865913));
#26747=CARTESIAN_POINT('Ctrl Pts',(-1.80895452013098,0.848623136024026,
8.82217341303137));
#26748=CARTESIAN_POINT('Ctrl Pts',(-1.75656177873735,0.952352465779989,
8.81411058645937));
#26749=CARTESIAN_POINT('Ctrl Pts',(-1.69139590018277,1.05748121009304,8.80603352311556));
#26750=CARTESIAN_POINT('Ctrl Pts',(-1.6873099296381,1.06398863098044,8.80553401987475));
#26751=CARTESIAN_POINT('Ctrl Pts',(-1.68129477589268,1.07344672143961,8.80480889054404));
#26752=CARTESIAN_POINT('Ctrl Pts',(-1.67939527370162,1.07641604519397,8.80458136472026));
#26753=CARTESIAN_POINT('Ctrl Pts',(-1.67601953023632,1.08166235972264,8.80417960732177));
#26754=CARTESIAN_POINT('Ctrl Pts',(-1.67454650238217,1.08394139043119,8.80400516397716));
#26755=CARTESIAN_POINT('Ctrl Pts',(-1.67143129852943,1.08873964734929,8.80363807338506));
#26756=CARTESIAN_POINT('Ctrl Pts',(-1.66978807940505,1.09125816174925,8.80344549790757));
#26757=CARTESIAN_POINT('Ctrl Pts',(-1.66538832820323,1.09796832689279,8.80293266143679));
#26758=CARTESIAN_POINT('Ctrl Pts',(-1.66262164532838,1.10215334521897,8.80261307400977));
#26759=CARTESIAN_POINT('Ctrl Pts',(-1.649494892678,1.12184759452823,8.80111013527543));
#26760=CARTESIAN_POINT('Ctrl Pts',(-1.63893300793373,1.13722209028045,8.79993980505107));
#26761=CARTESIAN_POINT('Ctrl Pts',(-1.52880177567023,1.29281355286047,8.78810141382086));
#26762=CARTESIAN_POINT('Ctrl Pts',(-1.41169775995678,1.41976397825655,8.77843980124234));
#26763=CARTESIAN_POINT('Ctrl Pts',(-1.19512894980028,1.60089393871845,8.76192491045458));
#26764=CARTESIAN_POINT('Ctrl Pts',(-1.10480549707487,1.66451021201874,8.75534717208111));
#26765=CARTESIAN_POINT('Ctrl Pts',(-0.998552948221976,1.72687188638907,
8.74765682610446));
#26766=CARTESIAN_POINT('Ctrl Pts',(-0.987346840240081,1.73330340880107,
8.7468465121535));
#26767=CARTESIAN_POINT('Ctrl Pts',(-0.970647350391145,1.74267325624923,
8.74563975210611));
#26768=CARTESIAN_POINT('Ctrl Pts',(-0.965201257934812,1.74569553104751,
8.74524632182401));
#26769=CARTESIAN_POINT('Ctrl Pts',(-0.955495897152954,1.75102215971219,
8.74454537470062));
#26770=CARTESIAN_POINT('Ctrl Pts',(-0.951242205081797,1.75333661339536,
8.74423822151205));
#26771=CARTESIAN_POINT('Ctrl Pts',(-0.942284050171711,1.75816859290734,
8.74359147037491));
#26772=CARTESIAN_POINT('Ctrl Pts',(-0.937577836024628,1.76068277460109,
8.7432517566204));
#26773=CARTESIAN_POINT('Ctrl Pts',(-0.925166217813102,1.76724950933876,
8.74235596188253));
#26774=CARTESIAN_POINT('Ctrl Pts',(-0.917444337608731,1.77127051639334,
8.74179877111921));
#26775=CARTESIAN_POINT('Ctrl Pts',(-0.882436955258173,1.78920954343265,
8.73927309228567));
#26776=CARTESIAN_POINT('Ctrl Pts',(-0.854860650210472,1.80254788160963,
8.73728444286876));
#26777=CARTESIAN_POINT('Ctrl Pts',(-0.780301653924716,1.83651546453293,
8.73190664659693));
#26778=CARTESIAN_POINT('Ctrl Pts',(-0.732814385000913,1.85597468827633,
8.72847992372128));
#26779=CARTESIAN_POINT('Ctrl Pts',(-0.589948609551209,1.90817988266176,
8.71817056031528));
#26780=CARTESIAN_POINT('Ctrl Pts',(-0.49278504584196,1.93554886662691,8.71115099238238));
#26781=CARTESIAN_POINT('Ctrl Pts',(-0.310560107016956,1.97226295060287,
8.69818173724003));
#26782=CARTESIAN_POINT('Ctrl Pts',(-0.226145848879563,1.98371586973232,
8.69225142046983));
#26783=CARTESIAN_POINT('Ctrl Pts',(-0.104001861381776,1.99238697340105,
8.68397475229841));
#26784=CARTESIAN_POINT('Ctrl Pts',(-0.0666802713103355,1.99398506090668,
8.6814869693489));
#26785=CARTESIAN_POINT('Ctrl Pts',(-0.0233728218016821,1.99462197052304,
8.67866417476682));
#26786=CARTESIAN_POINT('Ctrl Pts',(-0.0174121730664553,1.99468291026621,
8.67827706458009));
#26787=CARTESIAN_POINT('Ctrl Pts',(-0.00790675197565317,1.99473747888062,
8.67766208035376));
#26788=CARTESIAN_POINT('Ctrl Pts',(-0.00436217265854273,1.99474837969709,
8.67743327078668));
#26789=CARTESIAN_POINT('Ctrl Pts',(0.00189891029603759,1.99475094580639,
8.67703004386315));
#26790=CARTESIAN_POINT('Ctrl Pts',(0.00461538983852243,1.99474651025942,
8.6768554094708));
#26791=CARTESIAN_POINT('Ctrl Pts',(0.0103288690540395,1.99472550966838,
8.67648877198016));
#26792=CARTESIAN_POINT('Ctrl Pts',(0.0133258358558936,1.99470773970702,
8.67629683738261));
#26793=CARTESIAN_POINT('Ctrl Pts',(0.0212939527049333,1.99464253547758,
8.67578752598992));
#26794=CARTESIAN_POINT('Ctrl Pts',(0.0262650249644415,1.99458327138868,
8.67547080654992));
#26795=CARTESIAN_POINT('Ctrl Pts',(0.049403338615265,1.99422090297092,8.67400116187692));
#26796=CARTESIAN_POINT('Ctrl Pts',(0.0675668319085981,1.99368815999893,
8.67286056755772));
#26797=CARTESIAN_POINT('Ctrl Pts',(0.24167046082842,1.98619940962763,8.66203128675586));
#26798=CARTESIAN_POINT('Ctrl Pts',(0.396316964882176,1.96120890941292,8.65317990975153));
#26799=CARTESIAN_POINT('Ctrl Pts',(0.668225200603352,1.88375322562802,8.63672065419262));
#26800=CARTESIAN_POINT('Ctrl Pts',(0.786370314024065,1.83757067680839,8.62923327181646));
#26801=CARTESIAN_POINT('Ctrl Pts',(0.910950587665771,1.77464529714492,8.62052209064799));
#26802=CARTESIAN_POINT('Ctrl Pts',(0.922508174800024,1.76866490848215,8.61970602907216));
#26803=CARTESIAN_POINT('Ctrl Pts',(0.939525742298678,1.75964711296118,8.61849233979297));
#26804=CARTESIAN_POINT('Ctrl Pts',(0.945031456888975,1.7566963672311,8.61809777903834));
#26805=CARTESIAN_POINT('Ctrl Pts',(0.954782650850639,1.75141118107601,8.6173955581035));
#26806=CARTESIAN_POINT('Ctrl Pts',(0.959033675027193,1.74908703186797,8.61708826636628));
#26807=CARTESIAN_POINT('Ctrl Pts',(0.967940320115646,1.7441752978075,8.61644197698908));
#26808=CARTESIAN_POINT('Ctrl Pts',(0.972594122218522,1.74158450995239,8.61610286640846));
#26809=CARTESIAN_POINT('Ctrl Pts',(0.984790676098834,1.7347305135737,8.61521036886468));
#26810=CARTESIAN_POINT('Ctrl Pts',(0.99231606140882,1.73043678324184,8.61465588688509));
#26811=CARTESIAN_POINT('Ctrl Pts',(1.02595719426972,1.71095068204773,8.6121598239611));
#26812=CARTESIAN_POINT('Ctrl Pts',(1.05175254864138,1.69521585962313,8.61019865661296));
#26813=CARTESIAN_POINT('Ctrl Pts',(1.11955391700747,1.65171466421718,8.6049129604975));
#26814=CARTESIAN_POINT('Ctrl Pts',(1.16088057742308,1.62293495655182,8.6015524203319));
#26815=CARTESIAN_POINT('Ctrl Pts',(1.28094406655226,1.53238955643415,8.59136816200825));
#26816=CARTESIAN_POINT('Ctrl Pts',(1.35616534088264,1.46623589685976,8.58440720851115));
#26817=CARTESIAN_POINT('Ctrl Pts',(1.51227094783563,1.30661869258721,8.56882970224325));
#26818=CARTESIAN_POINT('Ctrl Pts',(1.59010087746871,1.21070330433734,8.56023316941198));
#26819=CARTESIAN_POINT('Ctrl Pts',(1.6627831072815,1.10192422069179,8.55169187303433));
#26820=CARTESIAN_POINT('Ctrl Pts',(1.66694507816974,1.0956179812349,8.55120077147977));
#26821=CARTESIAN_POINT('Ctrl Pts',(1.67298290993694,1.0863553751997,8.55048554142526));
#26822=CARTESIAN_POINT('Ctrl Pts',(1.67488691736652,1.08341757077333,8.55025958471084));
#26823=CARTESIAN_POINT('Ctrl Pts',(1.67825123673067,1.07819650084249,8.54985961483974));
#26824=CARTESIAN_POINT('Ctrl Pts',(1.67971463947711,1.07591525609307,8.54968539635086));
#26825=CARTESIAN_POINT('Ctrl Pts',(1.68279889422886,1.07108569443712,8.5493177112261));
#26826=CARTESIAN_POINT('Ctrl Pts',(1.68441860539452,1.06853668413568,8.54912432046628));
#26827=CARTESIAN_POINT('Ctrl Pts',(1.68874437851215,1.06169474812195,8.54860699794448));
#26828=CARTESIAN_POINT('Ctrl Pts',(1.69143988087485,1.05739512240872,8.54828376061073));
#26829=CARTESIAN_POINT('Ctrl Pts',(1.70429856525839,1.03670910262367,8.54673729501149));
#26830=CARTESIAN_POINT('Ctrl Pts',(1.71424062576099,1.02018552572916,8.54552802047596));
#26831=CARTESIAN_POINT('Ctrl Pts',(1.7413353765104,0.973639573314195,8.54218603395861));
#26832=CARTESIAN_POINT('Ctrl Pts',(1.75795009904916,0.943310476370931,8.54008194936214));
#26833=CARTESIAN_POINT('Ctrl Pts',(1.8157046992711,0.831051579067874,8.53250257829814));
#26834=CARTESIAN_POINT('Ctrl Pts',(1.85197481438699,0.746740811799411,8.52720246169032));
#26835=CARTESIAN_POINT('Ctrl Pts',(1.93387666849153,0.51323801473111,8.5128510081281));
#26836=CARTESIAN_POINT('Ctrl Pts',(1.96803229135681,0.360737933199634,8.50377564713194));
#26837=CARTESIAN_POINT('Ctrl Pts',(1.98540009027258,0.193318909351684,8.49326493829502));
#26838=CARTESIAN_POINT('Ctrl Pts',(1.98657939738878,0.18079824526646,8.49247601157161));
#26839=CARTESIAN_POINT('Ctrl Pts',(1.98815988852135,0.162128877200572,8.49129507007666));
#26840=CARTESIAN_POINT('Ctrl Pts',(1.98865111940251,0.155987945249319,8.49090588447729));
#26841=CARTESIAN_POINT('Ctrl Pts',(1.98947704983553,0.145024143425738,8.49020969148506));
#26842=CARTESIAN_POINT('Ctrl Pts',(1.98982267983578,0.140202126002045,8.48990302979203));
#26843=CARTESIAN_POINT('Ctrl Pts',(1.99051539237544,0.130018840068612,8.48925440513547));
#26844=CARTESIAN_POINT('Ctrl Pts',(1.99085835083834,0.12465733842149,8.4889123152375));
#26845=CARTESIAN_POINT('Ctrl Pts',(1.99171018317356,0.110439161075678,8.48800353259536));
#26846=CARTESIAN_POINT('Ctrl Pts',(1.99218163615962,0.101580442934999,8.48743567116195));
#26847=CARTESIAN_POINT('Ctrl Pts',(1.99409664364856,0.0604256341091231,
8.48478972903826));
#26848=CARTESIAN_POINT('Ctrl Pts',(1.99481396211781,0.0281022087461893,
8.48268906038251));
#26849=CARTESIAN_POINT('Ctrl Pts',(1.99462848562754,-0.0595109098138776,
8.4769303124561));
#26850=CARTESIAN_POINT('Ctrl Pts',(1.99221291203987,-0.114765515024974,
8.47322777901343));
#26851=CARTESIAN_POINT('Ctrl Pts',(1.97865686090083,-0.273397295996829,
8.46240256571958));
#26852=CARTESIAN_POINT('Ctrl Pts',(1.96172880981232,-0.376092937774062,
8.45514507698912));
#26853=CARTESIAN_POINT('Ctrl Pts',(1.91982084963911,-0.546264644558422,
8.44292368359057));
#26854=CARTESIAN_POINT('Ctrl Pts',(1.89905641030154,-0.614575560317481,
8.43796567661446));
#26855=CARTESIAN_POINT('Ctrl Pts',(1.87180631681041,-0.689520967815815,
8.43255693756747));
#26856=CARTESIAN_POINT('Ctrl Pts',(1.86888752402926,-0.697393346221799,
8.43198921226483));
#26857=CARTESIAN_POINT('Ctrl Pts',(1.85393830506228,-0.736945483102642,
8.42913973618636));
#26858=CARTESIAN_POINT('Ctrl Pts',(1.84115083480158,-0.768335750457242,
8.42688751182878));
#26859=CARTESIAN_POINT('Ctrl Pts',(1.82524927528295,-0.804690093931946,
8.42430240594606));
#26860=CARTESIAN_POINT('Ctrl Pts',(1.82290662936808,-0.809983016368391,
8.42392662198763));
#26861=CARTESIAN_POINT('Ctrl Pts',(1.81911300946868,-0.818454414053066,
8.42332620723367));
#26862=CARTESIAN_POINT('Ctrl Pts',(1.81767668725229,-0.821639355299856,
8.42310070797001));
#26863=CARTESIAN_POINT('Ctrl Pts',(1.81511170099361,-0.827287384048021,
8.4227012573476));
#26864=CARTESIAN_POINT('Ctrl Pts',(1.81398637935532,-0.829751962185732,
8.42252710253392));
#26865=CARTESIAN_POINT('Ctrl Pts',(1.81159442905761,-0.834962472968344,
8.42215923527944));
#26866=CARTESIAN_POINT('Ctrl Pts',(1.81032658033501,-0.837707812718036,
8.42196559993562));
#26867=CARTESIAN_POINT('Ctrl Pts',(1.806907079768,-0.845068219551413,8.42144693106417));
#26868=CARTESIAN_POINT('Ctrl Pts',(1.80474397342986,-0.849677987449023,
8.42112259827667));
#26869=CARTESIAN_POINT('Ctrl Pts',(1.79422248832292,-0.871878733638613,
8.4195628079825));
#26870=CARTESIAN_POINT('Ctrl Pts',(1.78562408911488,-0.889355690942119,
8.41834159660963));
#26871=CARTESIAN_POINT('Ctrl Pts',(1.76083223517264,-0.937937594563641,
8.41495799131184));
#26872=CARTESIAN_POINT('Ctrl Pts',(1.74407198214679,-0.968746776647528,
8.41282509621319));
#26873=CARTESIAN_POINT('Ctrl Pts',(1.67937658776836,-1.08054446994269,8.40507465326996));
#26874=CARTESIAN_POINT('Ctrl Pts',(1.62653889385068,-1.15855758517278,8.39964068520289));
#26875=CARTESIAN_POINT('Ctrl Pts',(1.47417826549765,-1.35243202908758,8.38533812765868));
#26876=CARTESIAN_POINT('Ctrl Pts',(1.36655174808003,-1.46109588468636,8.3764396728853));
#26877=CARTESIAN_POINT('Ctrl Pts',(1.23772448628793,-1.56436126146682,8.36613057473746));
#26878=CARTESIAN_POINT('Ctrl Pts',(1.22776438609564,-1.5721904021998,8.36533588962999));
#26879=CARTESIAN_POINT('Ctrl Pts',(1.21283657536215,-1.58369605148948,8.36414799128888));
#26880=CARTESIAN_POINT('Ctrl Pts',(1.20792513076438,-1.58744531216401,8.36375765691701));
#26881=CARTESIAN_POINT('Ctrl Pts',(1.1991383696673,-1.59408849350911,8.36306018192563));
#26882=CARTESIAN_POINT('Ctrl Pts',(1.19526978170201,-1.59699126579369,8.36275339186002));
#26883=CARTESIAN_POINT('Ctrl Pts',(1.18708993489509,-1.60308259384868,8.36210529679687));
#26884=CARTESIAN_POINT('Ctrl Pts',(1.18277630545501,-1.60626788754496,8.36176386793664));
#26885=CARTESIAN_POINT('Ctrl Pts',(1.17150393293358,-1.6145216663641,8.36087250536558));
#26886=CARTESIAN_POINT('Ctrl Pts',(1.16452518652817,-1.61956252183275,8.36032150811027));
#26887=CARTESIAN_POINT('Ctrl Pts',(1.14915316373773,-1.6305152447406,8.35910958069409));
#26888=CARTESIAN_POINT('Ctrl Pts',(1.14074647789215,-1.63640778037673,8.35844792822141));
#26889=CARTESIAN_POINT('Ctrl Pts',(1.11577752559575,-1.65362347355213,8.35648586631564));
#26890=CARTESIAN_POINT('Ctrl Pts',(1.09908988997372,-1.66476167784118,8.35517856503502));
#26891=CARTESIAN_POINT('Ctrl Pts',(1.03959916074087,-1.70318453369781,8.35053104701778));
#26892=CARTESIAN_POINT('Ctrl Pts',(0.995928506377608,-1.72908347034398,
8.34714205558288));
#26893=CARTESIAN_POINT('Ctrl Pts',(0.819951350029455,-1.82456737958286,
8.33357818182985));
#26894=CARTESIAN_POINT('Ctrl Pts',(0.680992712462007,-1.88085271223676,
8.32302151972718));
#26895=CARTESIAN_POINT('Ctrl Pts',(0.466750660034543,-1.94074825477413,
8.30765391027668));
#26896=CARTESIAN_POINT('Ctrl Pts',(0.3953883743506,-1.95653535277602,8.30268566346477));
#26897=CARTESIAN_POINT('Ctrl Pts',(0.315812298603969,-1.96960603556065,
8.29741940566992));
#26898=CARTESIAN_POINT('Ctrl Pts',(0.308304314995621,-1.97079521948055,
8.29692521328095));
#26899=CARTESIAN_POINT('Ctrl Pts',(0.297266882110772,-1.97247881138701,
8.29620281578304));
#26900=CARTESIAN_POINT('Ctrl Pts',(0.293742725015352,-1.97300670869494,
8.29597277504676));
#26901=CARTESIAN_POINT('Ctrl Pts',(0.287526788764371,-1.97392079444671,
8.2955681331199));
#26902=CARTESIAN_POINT('Ctrl Pts',(0.284835611458565,-1.97431092582046,
8.29539330984282));
#26903=CARTESIAN_POINT('Ctrl Pts',(0.279186049892442,-1.9751181325976,8.29502708018251));
#26904=CARTESIAN_POINT('Ctrl Pts',(0.276227530411742,-1.97553406447497,
8.29483573923658));
#26905=CARTESIAN_POINT('Ctrl Pts',(0.268385272949907,-1.97661862922778,
8.29432969271231));
#26906=CARTESIAN_POINT('Ctrl Pts',(0.263499933038235,-1.97727581451999,
8.29401562961622));
#26907=CARTESIAN_POINT('Ctrl Pts',(0.241393976438014,-1.98016616580136,
8.29259963257806));
#26908=CARTESIAN_POINT('Ctrl Pts',(0.224146437898077,-1.98219260412814,
8.29150889652619));
#26909=CARTESIAN_POINT('Ctrl Pts',(0.17702406174122,-1.98710612367152,8.28856177474792));
#26910=CARTESIAN_POINT('Ctrl Pts',(0.147106050608735,-1.98954474101159,
8.28672659729548));
#26911=CARTESIAN_POINT('Ctrl Pts',(0.0438186785867573,-1.99562083486986,
8.28047989771616));
#26912=CARTESIAN_POINT('Ctrl Pts',(-0.0296930805824241,-1.99588136608064,
8.27618697264572));
#26913=CARTESIAN_POINT('Ctrl Pts',(-0.231585628778115,-1.98543690349676,
8.26443880589486));
#26914=CARTESIAN_POINT('Ctrl Pts',(-0.359160631457635,-1.96636536369612,
8.2570428749965));
#26915=CARTESIAN_POINT('Ctrl Pts',(-0.489150578478365,-1.93385299103681,
8.24897111936738));
#26916=CARTESIAN_POINT('Ctrl Pts',(-0.494289470719627,-1.93254588504606,
8.24865116903215));
#26917=CARTESIAN_POINT('Ctrl Pts',(-0.547488380592045,-1.91878837140432,
8.24532988630469));
#26918=CARTESIAN_POINT('Ctrl Pts',(-0.595069395803439,-1.90456927310555,
8.24228172938183));
#26919=CARTESIAN_POINT('Ctrl Pts',(-0.651222371040707,-1.88547884652929,
8.23856989857006));
#26920=CARTESIAN_POINT('Ctrl Pts',(-0.66035416690302,-1.88230003618962,
8.23796260912844));
#26921=CARTESIAN_POINT('Ctrl Pts',(-0.675234450898315,-1.87699854683614,
8.23696688406439));
#26922=CARTESIAN_POINT('Ctrl Pts',(-0.6809969788628,-1.87491552394316,8.23657976593404));
#26923=CARTESIAN_POINT('Ctrl Pts',(-0.691285142901009,-1.87114289920849,
8.23588587099605));
#26924=CARTESIAN_POINT('Ctrl Pts',(-0.695814430400161,-1.86946333899012,
8.23557943115927));
#26925=CARTESIAN_POINT('Ctrl Pts',(-0.705385772902589,-1.86587447100627,
8.23492980894162));
#26926=CARTESIAN_POINT('Ctrl Pts',(-0.71042626958217,-1.86396114356299,
8.23458649397921));
#26927=CARTESIAN_POINT('Ctrl Pts',(-0.72338041391765,-1.8589836884265,8.23370102251431));
#26928=CARTESIAN_POINT('Ctrl Pts',(-0.731282313437865,-1.8558894771609,
8.23315785919395));
#26929=CARTESIAN_POINT('Ctrl Pts',(-0.767162417072151,-1.84157488672986,
8.23067747780603));
#26930=CARTESIAN_POINT('Ctrl Pts',(-0.794902547802253,-1.82977212014478,
8.22872069884412));
#26931=CARTESIAN_POINT('Ctrl Pts',(-0.868280492224898,-1.79656801944158,
8.22343593686068));
#26932=CARTESIAN_POINT('Ctrl Pts',(-0.913390069155155,-1.77405905319881,
8.22007172664467));
#26933=CARTESIAN_POINT('Ctrl Pts',(-1.03576364877011,-1.7070914519208,8.21062386344293));
#26934=CARTESIAN_POINT('Ctrl Pts',(-1.11097090444453,-1.65912890939449,
8.20444247386381));
#26935=CARTESIAN_POINT('Ctrl Pts',(-1.28321835246041,-1.53230394471539,
8.18952343736462));
#26936=CARTESIAN_POINT('Ctrl Pts',(-1.37656523210199,-1.44902690209786,
8.1807785162497));
#26937=CARTESIAN_POINT('Ctrl Pts',(-1.47114728672341,-1.34720199912272,
8.17161054949819));
#26938=CARTESIAN_POINT('Ctrl Pts',(-1.48066192470102,-1.33673776714208,
8.17068461922947));
#26939=CARTESIAN_POINT('Ctrl Pts',(-1.49319634116289,-1.32265431466557,
8.16946092396867));
#26940=CARTESIAN_POINT('Ctrl Pts',(-1.49631545968456,-1.31912463231378,
8.16915608689455));
#26941=CARTESIAN_POINT('Ctrl Pts',(-1.50116706651944,-1.31359506746867,
8.16868146333302));
#26942=CARTESIAN_POINT('Ctrl Pts',(-1.50290810217116,-1.31160275979795,
8.16851104631438));
#26943=CARTESIAN_POINT('Ctrl Pts',(-1.50624488345896,-1.3077690356633,8.16818426126638));
#26944=CARTESIAN_POINT('Ctrl Pts',(-1.50784120043325,-1.30592818100249,
8.16802785236674));
#26945=CARTESIAN_POINT('Ctrl Pts',(-1.51165353612885,-1.30151552959572,
8.16765412854783));
#26946=CARTESIAN_POINT('Ctrl Pts',(-1.51386636423064,-1.29894099894453,
8.1674370514186));
#26947=CARTESIAN_POINT('Ctrl Pts',(-1.52050779157342,-1.29117395897596,
8.16678502410681));
#26948=CARTESIAN_POINT('Ctrl Pts',(-1.52491638398229,-1.28596429253909,
8.16635152416989));
#26949=CARTESIAN_POINT('Ctrl Pts',(-1.55774099516945,-1.24676903601589,
8.16311781141746));
#26950=CARTESIAN_POINT('Ctrl Pts',(-1.58504705682597,-1.21186491114171,
8.16039348472467));
#26951=CARTESIAN_POINT('Ctrl Pts',(-1.65353669864764,-1.11803734452872,
8.15338136523548));
#26952=CARTESIAN_POINT('Ctrl Pts',(-1.69273901638744,-1.05774626794611,
8.14917900838138));
#26953=CARTESIAN_POINT('Ctrl Pts',(-1.76233778252968,-0.936889740923381,
8.14107225821186));
#26954=CARTESIAN_POINT('Ctrl Pts',(-1.79307195736845,-0.876635450618172,
8.13717013608704));
#26955=CARTESIAN_POINT('Ctrl Pts',(-1.86718057963606,-0.711066236539654,
8.12657180756088));
#26956=CARTESIAN_POINT('Ctrl Pts',(-1.90469293798104,-0.603421726607212,
8.11979724302245));
#26957=CARTESIAN_POINT('Ctrl Pts',(-1.9360277503575,-0.480616404137664,
8.11188639262492));
#26958=CARTESIAN_POINT('Ctrl Pts',(-1.93910989809191,-0.468026034075575,
8.11107349899703));
#26959=CARTESIAN_POINT('Ctrl Pts',(-1.94349290696159,-0.449334818143309,
8.1098636284517));
#26960=CARTESIAN_POINT('Ctrl Pts',(-1.94488825177285,-0.443256297063917,
8.10946969024776));
#26961=CARTESIAN_POINT('Ctrl Pts',(-1.94731658958484,-0.432445514673095,
8.10876817118136));
#26962=CARTESIAN_POINT('Ctrl Pts',(-1.94836089968368,-0.427715825214534,
8.10846095612334));
#26963=CARTESIAN_POINT('Ctrl Pts',(-1.95051849723119,-0.417772161922642,
8.10781441431247));
#26964=CARTESIAN_POINT('Ctrl Pts',(-1.95162812643588,-0.412557441470851,
8.10747497304597));
#26965=CARTESIAN_POINT('Ctrl Pts',(-1.95383722178578,-0.401967381924348,
8.10678484522419));
#26966=CARTESIAN_POINT('Ctrl Pts',(-1.95493544207345,-0.396591832612719,
8.10643412198102));
#26967=CARTESIAN_POINT('Ctrl Pts',(-1.95759428288649,-0.383297953845802,
8.10556572686589));
#26968=CARTESIAN_POINT('Ctrl Pts',(-1.95912904073472,-0.375374608062704,
8.10504723430336));
#26969=CARTESIAN_POINT('Ctrl Pts',(-1.96623800066139,-0.337442286318332,
8.10256045980665));
#26970=CARTESIAN_POINT('Ctrl Pts',(-1.97117077455213,-0.307318691573248,
8.10057196547371));
#26971=CARTESIAN_POINT('Ctrl Pts',(-1.98837368424034,-0.184679196643107,
8.09241690771572));
#26972=CARTESIAN_POINT('Ctrl Pts',(-1.99483390533887,-0.0914821070513714,
8.08607550797391));
#26973=CARTESIAN_POINT('Ctrl Pts',(-1.99474917736509,0.00181160185376153,
8.07962176510059));
#26974=CARTESIAN_POINT('Ctrl Pts',(-1.99474917872771,0.00181010085837489,
8.07962186893436));
#26975=CARTESIAN_POINT('Ctrl Pts',(-1.9946025293401,0.163419186970004,8.06844230140074));
#26976=CARTESIAN_POINT('Ctrl Pts',(-1.97481767100195,0.324419899408584,
8.05695069916315));
#26977=CARTESIAN_POINT('Ctrl Pts',(-1.93294149260101,0.492856029737398,
8.04544972196648));
#26978=CARTESIAN_POINT('Ctrl Pts',(-1.92995930451566,0.504407552142277,
8.04466399087229));
#26979=CARTESIAN_POINT('Ctrl Pts',(-1.92533025109995,0.521695880331543,
8.04349328407203));
#26980=CARTESIAN_POINT('Ctrl Pts',(-1.92376104353685,0.527452952278365,
8.04310431076097));
#26981=CARTESIAN_POINT('Ctrl Pts',(-1.92083256771947,0.538009938727879,
8.04239275368518));
#26982=CARTESIAN_POINT('Ctrl Pts',(-1.91948108787714,0.542811939781313,
8.04206974689217));
#26983=CARTESIAN_POINT('Ctrl Pts',(-1.91728779025176,0.550494411208243,
8.04155409221742));
#26984=CARTESIAN_POINT('Ctrl Pts',(-1.91645747300161,0.553378100297498,
8.04136078670241));
#26985=CARTESIAN_POINT('Ctrl Pts',(-1.91486342421142,0.558867607301989,
8.04099329444896));
#26986=CARTESIAN_POINT('Ctrl Pts',(-1.91410088865785,0.561473707303415,
8.04081904387778));
#26987=CARTESIAN_POINT('Ctrl Pts',(-1.91233280873882,0.567470970047757,
8.04041853087533));
#26988=CARTESIAN_POINT('Ctrl Pts',(-1.91132356510089,0.570861019151871,
8.04019248688016));
#26989=CARTESIAN_POINT('Ctrl Pts',(-1.90859668106549,0.579932321825721,
8.03958852422362));
#26990=CARTESIAN_POINT('Ctrl Pts',(-1.90686267654961,0.585608678036491,
8.03921154215899));
#26991=CARTESIAN_POINT('Ctrl Pts',(-1.89419058119865,0.626438338313878,
8.03650619561362));
#26992=CARTESIAN_POINT('Ctrl Pts',(-1.88230565389973,0.66129327250839,8.03423019557212));
#26993=CARTESIAN_POINT('Ctrl Pts',(-1.86528982749034,0.707010941722775,
8.03126481654285));
#26994=CARTESIAN_POINT('Ctrl Pts',(-1.86101705341103,0.718182532563603,
8.0305418025732));
#26995=CARTESIAN_POINT('Ctrl Pts',(-1.84774248716042,0.751976072845238,
8.02835770295901));
#26996=CARTESIAN_POINT('Ctrl Pts',(-1.83842659081066,0.7744727598571,8.02690780186416));
#26997=CARTESIAN_POINT('Ctrl Pts',(-1.79448605436488,0.875319537144692,
8.02040335955909));
#26998=CARTESIAN_POINT('Ctrl Pts',(-1.75524759950036,0.951562643050326,
8.01546884739643));
#26999=CARTESIAN_POINT('Ctrl Pts',(-1.68091433781392,1.07565534714707,8.00706789488677));
#27000=CARTESIAN_POINT('Ctrl Pts',(-1.64837179985535,1.12488995013763,8.00362780691618));
#27001=CARTESIAN_POINT('Ctrl Pts',(-1.56949188028581,1.23344132063484,7.99567643151273));
#27002=CARTESIAN_POINT('Ctrl Pts',(-1.52188725163734,1.2917195962136,7.99113573531167));
#27003=CARTESIAN_POINT('Ctrl Pts',(-1.46022150789559,1.35905874779749,7.98545699528291));
#27004=CARTESIAN_POINT('Ctrl Pts',(-1.44918883549138,1.37081699255257,7.98444836763508));
#27005=CARTESIAN_POINT('Ctrl Pts',(-1.43432196233404,1.38628152546335,7.98309825374717));
#27006=CARTESIAN_POINT('Ctrl Pts',(-1.43061348903908,1.39010827044605,7.98276220790587));
#27007=CARTESIAN_POINT('Ctrl Pts',(-1.42373137236618,1.39715316628911,7.98213990366135));
#27008=CARTESIAN_POINT('Ctrl Pts',(-1.42056203155644,1.40037548703302,7.98185383421981));
#27009=CARTESIAN_POINT('Ctrl Pts',(-1.41398765699366,1.40701447617827,7.98126146095665));
#27010=CARTESIAN_POINT('Ctrl Pts',(-1.41058112968504,1.41042961760265,7.98095509223284));
#27011=CARTESIAN_POINT('Ctrl Pts',(-1.40286737486535,1.41810698104987,7.9802626114396));
#27012=CARTESIAN_POINT('Ctrl Pts',(-1.39855306062161,1.42236198502735,7.97987618528826));
#27013=CARTESIAN_POINT('Ctrl Pts',(-1.38746237706074,1.43320095667876,7.97888500699063));
#27014=CARTESIAN_POINT('Ctrl Pts',(-1.38065855552888,1.43975649952544,7.97827902368101));
#27015=CARTESIAN_POINT('Ctrl Pts',(-1.34032739810685,1.47806714801907,7.97469873357842));
#27016=CARTESIAN_POINT('Ctrl Pts',(-1.30575454047324,1.50869629807674,7.97167672610601));
#27017=CARTESIAN_POINT('Ctrl Pts',(-1.26283585013824,1.54413834072007,7.96797671452249));
#27018=CARTESIAN_POINT('Ctrl Pts',(-1.25547638730432,1.55012794174535,7.96734402969188));
#27019=CARTESIAN_POINT('Ctrl Pts',(-1.22679009621421,1.57313638715877,7.96488475978215));
#27020=CARTESIAN_POINT('Ctrl Pts',(-1.20515839703623,1.58976890294754,7.96304477372632));
#27021=CARTESIAN_POINT('Ctrl Pts',(-1.10753266317454,1.66169515020721,7.95480713527513));
#27022=CARTESIAN_POINT('Ctrl Pts',(-1.02803304333606,1.71201776459951,7.94826585803189));
#27023=CARTESIAN_POINT('Ctrl Pts',(-0.876291992230998,1.79367760921354,
7.9362428620975));
#27024=CARTESIAN_POINT('Ctrl Pts',(-0.805162579032059,1.82671330701595,
7.93077786864641));
#27025=CARTESIAN_POINT('Ctrl Pts',(-0.702994978091094,1.86703406455688,
7.9233041551115));
#27026=CARTESIAN_POINT('Ctrl Pts',(-0.673447865357886,1.87789412473065,
7.92118540627067));
#27027=CARTESIAN_POINT('Ctrl Pts',(-0.6266526728255,1.89384704910893,7.91790909128924));
#27028=CARTESIAN_POINT('Ctrl Pts',(-0.609572626527827,1.89941345849472,
7.9167295592809));
#27029=CARTESIAN_POINT('Ctrl Pts',(-0.587650386738246,1.9062317605298,7.91523843614937));
#27030=CARTESIAN_POINT('Ctrl Pts',(-0.582876158117747,1.90769701144958,
7.91491507263978));
#27031=CARTESIAN_POINT('Ctrl Pts',(-0.575223208898215,1.91001435457658,
7.91439898346653));
#27032=CARTESIAN_POINT('Ctrl Pts',(-0.572348019207229,1.91087789247409,
7.91420559824399));
#27033=CARTESIAN_POINT('Ctrl Pts',(-0.566868807868184,1.91251004929935,
7.91383804783387));
#27034=CARTESIAN_POINT('Ctrl Pts',(-0.564265198602791,1.91327983309568,
7.91366381842855));
#27035=CARTESIAN_POINT('Ctrl Pts',(-0.558268311546124,1.91503956846406,
7.91326347715789));
#27036=CARTESIAN_POINT('Ctrl Pts',(-0.554873970463672,1.91602581763185,
7.91303758310535));
#27037=CARTESIAN_POINT('Ctrl Pts',(-0.545780922296382,1.91864167516669,
7.91243428278966));
#27038=CARTESIAN_POINT('Ctrl Pts',(-0.540077489353895,1.92025493110966,
7.91205780989862));
#27039=CARTESIAN_POINT('Ctrl Pts',(-0.499056828586545,1.93166069346229,
7.90936343277446));
#27040=CARTESIAN_POINT('Ctrl Pts',(-0.463480176268807,1.94050439091535,
7.90709741710329));
#27041=CARTESIAN_POINT('Ctrl Pts',(-0.357583343705635,1.96374937824469,
7.90050569743404));
#27042=CARTESIAN_POINT('Ctrl Pts',(-0.286704296100162,1.97534294145181,
7.8962899757783));
#27043=CARTESIAN_POINT('Ctrl Pts',(-0.0893911502836425,1.99676974638069,
7.88473122412065));
#27044=CARTESIAN_POINT('Ctrl Pts',(0.0375774038532549,1.99841604968019,
7.87747373598929));
#27045=CARTESIAN_POINT('Ctrl Pts',(0.207362399899169,1.98442314765283,7.86728265923098));
#27046=CARTESIAN_POINT('Ctrl Pts',(0.250750109838614,1.97940859373567,7.86463756706073));
#27047=CARTESIAN_POINT('Ctrl Pts',(0.311766672483799,1.97031827015229,7.86084012952415));
#27048=CARTESIAN_POINT('Ctrl Pts',(0.329559825385252,1.96742034981685,7.8597233972209));
#27049=CARTESIAN_POINT('Ctrl Pts',(0.360680664408105,1.96191777649685,7.85775243846465));
#27050=CARTESIAN_POINT('Ctrl Pts',(0.37402574833505,1.95941742069155,7.85690150559883));
#27051=CARTESIAN_POINT('Ctrl Pts',(0.393572800850712,1.95554808966998,7.85564625189801));
#27052=CARTESIAN_POINT('Ctrl Pts',(0.399795608883394,1.95428538094766,7.85524531920287));
#27053=CARTESIAN_POINT('Ctrl Pts',(0.410788306005286,1.95200008375483,7.85453468121337));
#27054=CARTESIAN_POINT('Ctrl Pts',(0.415560694392999,1.95098966371247,7.85422536725562));
#27055=CARTESIAN_POINT('Ctrl Pts',(0.424815090048621,1.9489948073615,7.85362399355915));
#27056=CARTESIAN_POINT('Ctrl Pts',(0.429297504977026,1.94801238997494,7.85333200030103));
#27057=CARTESIAN_POINT('Ctrl Pts',(0.44122022567228,1.94535612033029,7.85255340612052));
#27058=CARTESIAN_POINT('Ctrl Pts',(0.4486543330149,1.94365506436704,7.85206593458927));
#27059=CARTESIAN_POINT('Ctrl Pts',(0.475306606335467,1.93739549638792,7.85031098214982));
#27060=CARTESIAN_POINT('Ctrl Pts',(0.494466059297516,1.93259435706872,7.84903572782634));
#27061=CARTESIAN_POINT('Ctrl Pts',(0.518108170231655,1.9262953390674,7.8474445873111));
#27062=CARTESIAN_POINT('Ctrl Pts',(0.522661483108442,1.92506487756013,7.84713733540794));
#27063=CARTESIAN_POINT('Ctrl Pts',(0.532138269811713,1.92246782349646,7.84649615864681));
#27064=CARTESIAN_POINT('Ctrl Pts',(0.537060937400058,1.9210984408134,7.84616214695425));
#27065=CARTESIAN_POINT('Ctrl Pts',(0.746345873839542,1.86201249870024,7.83192089689819));
#27066=CARTESIAN_POINT('Ctrl Pts',(0.940164487803027,1.77205301469311,7.81685369619351));
#27067=CARTESIAN_POINT('Ctrl Pts',(1.1532751652314,1.6281882477511,7.79916118757827));
#27068=CARTESIAN_POINT('Ctrl Pts',(1.18960682236419,1.6018354348985,7.7961081150366));
#27069=CARTESIAN_POINT('Ctrl Pts',(1.24322178798088,1.56011505952547,7.79158010553127));
#27070=CARTESIAN_POINT('Ctrl Pts',(1.26117648862968,1.54563688869602,7.79005977236567));
#27071=CARTESIAN_POINT('Ctrl Pts',(1.28303408269369,1.5273769826986,7.78820814173184));
#27072=CARTESIAN_POINT('Ctrl Pts',(1.28717707353678,1.52388716368912,7.78785713867878));
#27073=CARTESIAN_POINT('Ctrl Pts',(1.29366567441279,1.51837619553806,7.7873074238131));
#27074=CARTESIAN_POINT('Ctrl Pts',(1.29602084360717,1.51636642062099,7.78710789644053));
#27075=CARTESIAN_POINT('Ctrl Pts',(1.30041801124789,1.51259638588108,7.78673539416489));
#27076=CARTESIAN_POINT('Ctrl Pts',(1.30246109770228,1.51083748949078,7.78656232628851));
#27077=CARTESIAN_POINT('Ctrl Pts',(1.30709781903029,1.50682933330186,7.78616956982153));
#27078=CARTESIAN_POINT('Ctrl Pts',(1.30968921108559,1.50457752176844,7.78595007376364));
#27079=CARTESIAN_POINT('Ctrl Pts',(1.31638831081193,1.49872586197163,7.78538263175004));
#27080=CARTESIAN_POINT('Ctrl Pts',(1.32048710376361,1.495115783026,7.78503543205357));
#27081=CARTESIAN_POINT('Ctrl Pts',(1.34561738247554,1.47279792261024,7.78290623279078));
#27082=CARTESIAN_POINT('Ctrl Pts',(1.36626702633225,1.45366243325787,7.78115462483105));
#27083=CARTESIAN_POINT('Ctrl Pts',(1.52841096151801,1.29689909791467,7.7673169105405));
#27084=CARTESIAN_POINT('Ctrl Pts',(1.64918321079767,1.13938744966882,7.75638668982092));
#27085=CARTESIAN_POINT('Ctrl Pts',(1.76937324823784,0.922444401457525,7.7416392628026));
#27086=CARTESIAN_POINT('Ctrl Pts',(1.79218957401354,0.877292033853806,7.73859148550451));
#27087=CARTESIAN_POINT('Ctrl Pts',(1.82589766243223,0.80376873190401,7.73362584582013));
#27088=CARTESIAN_POINT('Ctrl Pts',(1.83790051631615,0.775930399940775,7.73174522202751));
#27089=CARTESIAN_POINT('Ctrl Pts',(1.85251591493174,0.739788882466196,7.72929857487841));
#27090=CARTESIAN_POINT('Ctrl Pts',(1.85571536734314,0.731726231095351,7.72875244837687));
#27091=CARTESIAN_POINT('Ctrl Pts',(1.86079517630101,0.718677444068249,7.72786797196837));
#27092=CARTESIAN_POINT('Ctrl Pts',(1.86270834192547,0.713704132522616,7.72753072699844));
#27093=CARTESIAN_POINT('Ctrl Pts',(1.86632270786699,0.704194987350592,7.72688560477938));
#27094=CARTESIAN_POINT('Ctrl Pts',(1.86802735942135,0.699660499015529,7.72657784585518));
#27095=CARTESIAN_POINT('Ctrl Pts',(1.87189071716629,0.689268939315709,7.72587224707978));
#27096=CARTESIAN_POINT('Ctrl Pts',(1.87403847334495,0.683407877242711,7.72547404503841));
#27097=CARTESIAN_POINT('Ctrl Pts',(1.88057105385983,0.665318592664034,7.72424429204972));
#27098=CARTESIAN_POINT('Ctrl Pts',(1.88486389381281,0.653057736258307,7.72340969724007));
#27099=CARTESIAN_POINT('Ctrl Pts',(1.93000999235424,0.519960857251873,7.71433674047399));
#27100=CARTESIAN_POINT('Ctrl Pts',(1.9592948635304,0.395537911909164,7.70570965164376));
#27101=CARTESIAN_POINT('Ctrl Pts',(1.99745146459902,0.115380156957704,7.68611358089036));
#27102=CARTESIAN_POINT('Ctrl Pts',(2.00037508819516,-0.0403563045860061,
7.67509902156652));
#27103=CARTESIAN_POINT('Ctrl Pts',(1.98343883447003,-0.212900253517525,
7.66360846772554));
#27104=CARTESIAN_POINT('Ctrl Pts',(1.98142224128465,-0.230915757020227,
7.66241813209591));
#27105=CARTESIAN_POINT('Ctrl Pts',(1.97854046158315,-0.253830410825299,
7.6609182013289));
#27106=CARTESIAN_POINT('Ctrl Pts',(1.97790224697928,-0.258756523134797,
7.66059658440132));
#27107=CARTESIAN_POINT('Ctrl Pts',(1.97684958858511,-0.266650038477074,
7.66008262272875));
#27108=CARTESIAN_POINT('Ctrl Pts',(1.97644685378661,-0.269618941020809,
7.65988962783192));
#27109=CARTESIAN_POINT('Ctrl Pts',(1.97566617639554,-0.275278227902444,
7.65952236046447));
#27110=CARTESIAN_POINT('Ctrl Pts',(1.97528943124526,-0.277968714426434,
7.65934802566489));
#27111=CARTESIAN_POINT('Ctrl Pts',(1.97440821277893,-0.284169577311775,
7.65894683552531));
#27112=CARTESIAN_POINT('Ctrl Pts',(1.97389987403908,-0.287679382476234,
7.65872020107659));
#27113=CARTESIAN_POINT('Ctrl Pts',(1.97251111259077,-0.297091029008319,
7.65811362781496));
#27114=CARTESIAN_POINT('Ctrl Pts',(1.97161355511333,-0.302990363338583,
7.65773463836136));
#27115=CARTESIAN_POINT('Ctrl Pts',(1.96488643825788,-0.34590934590038,7.65498569517072));
#27116=CARTESIAN_POINT('Ctrl Pts',(1.95804068784878,-0.382765063830779,
7.65267001918923));
#27117=CARTESIAN_POINT('Ctrl Pts',(1.93229138985211,-0.502493724484299,
7.64523037877867));
#27118=CARTESIAN_POINT('Ctrl Pts',(1.90912983891965,-0.584359183644491,
7.64027244590276));
#27119=CARTESIAN_POINT('Ctrl Pts',(1.84724716953405,-0.7595123019111,7.62948548526538));
#27120=CARTESIAN_POINT('Ctrl Pts',(1.80652975264624,-0.851839292848211,
7.6236768459733));
#27121=CARTESIAN_POINT('Ctrl Pts',(1.73481795577841,-0.985934399525989,
7.61464001874356));
#27122=CARTESIAN_POINT('Ctrl Pts',(1.70888742779654,-1.03022479743342,7.61154974901048));
#27123=CARTESIAN_POINT('Ctrl Pts',(1.66479580844147,-1.09928193160132,7.60652095730684));
#27124=CARTESIAN_POINT('Ctrl Pts',(1.6477199030193,-1.12471543544125,7.60462090701549));
#27125=CARTESIAN_POINT('Ctrl Pts',(1.62504772493893,-1.15685921912941,7.60215239339524));
#27126=CARTESIAN_POINT('Ctrl Pts',(1.61998311364871,-1.16394074970994,7.60160427371356));
#27127=CARTESIAN_POINT('Ctrl Pts',(1.61174010199157,-1.17530841750219,7.60071734946718));
#27128=CARTESIAN_POINT('Ctrl Pts',(1.60859054000238,-1.17961540610982,7.600379661119));
#27129=CARTESIAN_POINT('Ctrl Pts',(1.60254961938989,-1.18780711001371,7.59973420979597));
#27130=CARTESIAN_POINT('Ctrl Pts',(1.59966131654855,-1.19169403995506,7.59942656733087));
#27131=CARTESIAN_POINT('Ctrl Pts',(1.593025832747,-1.20055614293285,7.59872196858692));
#27132=CARTESIAN_POINT('Ctrl Pts',(1.58926946065408,-1.20552434073758,7.59832465375341));
#27133=CARTESIAN_POINT('Ctrl Pts',(1.57764953090503,-1.2207442207174,7.59710031606074));
#27134=CARTESIAN_POINT('Ctrl Pts',(1.56970971372106,-1.2309369993507,7.59627028805374));
#27135=CARTESIAN_POINT('Ctrl Pts',(1.49304880361492,-1.32740289390338,7.58831656084079));
#27136=CARTESIAN_POINT('Ctrl Pts',(1.41739454947651,-1.40789858258302,7.58090679990818));
#27137=CARTESIAN_POINT('Ctrl Pts',(1.20773035090262,-1.59687097541437,7.5614575864931));
#27138=CARTESIAN_POINT('Ctrl Pts',(1.06561927147637,-1.69501209220942,7.54918691046629));
#27139=CARTESIAN_POINT('Ctrl Pts',(0.896085428783181,-1.78224769282635,
7.53654244970378));
#27140=CARTESIAN_POINT('Ctrl Pts',(0.879369189107662,-1.79055461397138,
7.53531623013543));
#27141=CARTESIAN_POINT('Ctrl Pts',(0.858013412657452,-1.80079585933755,
7.53377784409858));
#27142=CARTESIAN_POINT('Ctrl Pts',(0.853480507869025,-1.80294863136012,
7.53345290517926));
#27143=CARTESIAN_POINT('Ctrl Pts',(0.846217994505851,-1.80636422487075,
7.53293489718037));
#27144=CARTESIAN_POINT('Ctrl Pts',(0.843493607544295,-1.80763800066408,
7.53274116001116));
#27145=CARTESIAN_POINT('Ctrl Pts',(0.838305576563201,-1.81004936016725,
7.53237335064943));
#27146=CARTESIAN_POINT('Ctrl Pts',(0.835842522534803,-1.81118806410125,
7.53219921254341));
#27147=CARTESIAN_POINT('Ctrl Pts',(0.830175094530202,-1.81379417129579,
7.53179961980711));
#27148=CARTESIAN_POINT('Ctrl Pts',(0.826969152283247,-1.81525810975824,
7.53157438026967));
#27149=CARTESIAN_POINT('Ctrl Pts',(0.81676408767738,-1.81988543089769,7.53085989683099));
#27150=CARTESIAN_POINT('Ctrl Pts',(0.809750460589579,-1.82301693702622,
7.5303725734955));
#27151=CARTESIAN_POINT('Ctrl Pts',(0.696330574289468,-1.87287394304048,
7.52254897282997));
#27152=CARTESIAN_POINT('Ctrl Pts',(0.586040790476462,-1.91026122767459,
7.5157428035951));
#27153=CARTESIAN_POINT('Ctrl Pts',(0.373676905080303,-1.96210825393127,
7.50303926839564));
#27154=CARTESIAN_POINT('Ctrl Pts',(0.272529802133945,-1.97869395972625,
7.49714765933331));
#27155=CARTESIAN_POINT('Ctrl Pts',(0.11743306430779,-1.99200405124301,7.48791171169632));
#27156=CARTESIAN_POINT('Ctrl Pts',(0.0641497227846041,-1.99443094861027,
7.48470480224453));
#27157=CARTESIAN_POINT('Ctrl Pts',(-0.0206603140407525,-1.99489166703058,
7.47950309081823));
#27158=CARTESIAN_POINT('Ctrl Pts',(-0.0521548189967926,-1.99431675360186,
7.47755026087937));
#27159=CARTESIAN_POINT('Ctrl Pts',(-0.0924049868206681,-1.99262795614422,
7.47502241075901));
#27160=CARTESIAN_POINT('Ctrl Pts',(-0.101186123352513,-1.99220134967634,
7.4744689740873));
#27161=CARTESIAN_POINT('Ctrl Pts',(-0.115310620668992,-1.99142152652569,
7.47357551926709));
#27162=CARTESIAN_POINT('Ctrl Pts',(-0.120655946880693,-1.99110481319271,
7.47323664764734));
#27163=CARTESIAN_POINT('Ctrl Pts',(-0.130828425318791,-1.99046097519389,
7.4725903012896));
#27164=CARTESIAN_POINT('Ctrl Pts',(-0.135655796568988,-1.99013780297264,
7.47228295284327));
#27165=CARTESIAN_POINT('Ctrl Pts',(-0.146659270269622,-1.98936094536326,
7.47158094174434));
#27166=CARTESIAN_POINT('Ctrl Pts',(-0.152834508065125,-1.98889605666247,
7.47118592996382));
#27167=CARTESIAN_POINT('Ctrl Pts',(-0.171705395743079,-1.98738700034668,
7.46997558648977));
#27168=CARTESIAN_POINT('Ctrl Pts',(-0.184393097421516,-1.98624998557144,
7.46915734852765));
#27169=CARTESIAN_POINT('Ctrl Pts',(-0.209670990787775,-1.9837404111223,
7.46751797197997));
#27170=CARTESIAN_POINT('Ctrl Pts',(-0.222260734065426,-1.98236931395097,
7.46669691583978));
#27171=CARTESIAN_POINT('Ctrl Pts',(-0.38156347461975,-1.96348371749504,
7.45624877698675));
#27172=CARTESIAN_POINT('Ctrl Pts',(-0.52587553495734,-1.92984398222032,
7.44609659852811));
#27173=CARTESIAN_POINT('Ctrl Pts',(-0.748316912022514,-1.85117160980462,
7.42964325228764));
#27174=CARTESIAN_POINT('Ctrl Pts',(-0.829469929568279,-1.81625864781452,
7.42346728003289));
#27175=CARTESIAN_POINT('Ctrl Pts',(-0.937921367151235,-1.76081141297538,
7.41516244500048));
#27176=CARTESIAN_POINT('Ctrl Pts',(-0.967407481519828,-1.74478547793121,
7.41289960836647));
#27177=CARTESIAN_POINT('Ctrl Pts',(-1.01282854440652,-1.71859308378748,
7.40942150905995));
#27178=CARTESIAN_POINT('Ctrl Pts',(-1.02904621907731,-1.70893176901858,
7.40818123109543));
#27179=CARTESIAN_POINT('Ctrl Pts',(-1.04941579923842,-1.69640190399817,
7.40662781135966));
#27180=CARTESIAN_POINT('Ctrl Pts',(-1.05369662289857,-1.69374625248754,
7.40630159716159));
#27181=CARTESIAN_POINT('Ctrl Pts',(-1.06052067691524,-1.68947699812598,
7.40578203600991));
#27182=CARTESIAN_POINT('Ctrl Pts',(-1.06307035713122,-1.68787382509658,
7.40558801402943));
#27183=CARTESIAN_POINT('Ctrl Pts',(-1.06790935240903,-1.68481587560035,
7.40521999250112));
#27184=CARTESIAN_POINT('Ctrl Pts',(-1.07019930282471,-1.68336222244463,
7.40504592567276));
#27185=CARTESIAN_POINT('Ctrl Pts',(-1.07545097219631,-1.68001343204309,
7.40464692703962));
#27186=CARTESIAN_POINT('Ctrl Pts',(-1.07841064781337,-1.67811513329362,
7.40442220816449));
#27187=CARTESIAN_POINT('Ctrl Pts',(-1.08778261404218,-1.67206903807546,
7.40371103035528));
#27188=CARTESIAN_POINT('Ctrl Pts',(-1.09417620866053,-1.66789217649824,
7.40322646692585));
#27189=CARTESIAN_POINT('Ctrl Pts',(-1.199550715814,-1.59818552283159,7.39524751672005));
#27190=CARTESIAN_POINT('Ctrl Pts',(-1.29252888094534,-1.52397412721782,
7.38830656887432));
#27191=CARTESIAN_POINT('Ctrl Pts',(-1.45175047739315,-1.37177063494622,
7.37551168840027));
#27192=CARTESIAN_POINT('Ctrl Pts',(-1.51967208927657,-1.29612106912868,
7.3696634208893));
#27193=CARTESIAN_POINT('Ctrl Pts',(-1.61338804195452,-1.17419677909837,
7.36053179236581));
#27194=CARTESIAN_POINT('Ctrl Pts',(-1.64359545555285,-1.13152657637209,
7.35738607992213));
#27195=CARTESIAN_POINT('Ctrl Pts',(-1.68901933550856,-1.06169910861576,
7.35227501593395));
#27196=CARTESIAN_POINT('Ctrl Pts',(-1.7053369941738,-1.03528589456422,7.35034977868486));
#27197=CARTESIAN_POINT('Ctrl Pts',(-1.72545341794302,-1.00095683167633,
7.34785293604103));
#27198=CARTESIAN_POINT('Ctrl Pts',(-1.72982608226541,-0.99338099315371,
7.34730226121661));
#27199=CARTESIAN_POINT('Ctrl Pts',(-1.73679007586518,-0.981130145509479,
7.34641219867722));
#27200=CARTESIAN_POINT('Ctrl Pts',(-1.73941272233597,-0.976472995284484,
7.34607394170442));
#27201=CARTESIAN_POINT('Ctrl Pts',(-1.74437477011429,-0.967578241645158,
7.34542806312506));
#27202=CARTESIAN_POINT('Ctrl Pts',(-1.74671752959149,-0.963342547308899,
7.34512056481494));
#27203=CARTESIAN_POINT('Ctrl Pts',(-1.75203120730047,-0.953652341848402,
7.34441722356562));
#27204=CARTESIAN_POINT('Ctrl Pts',(-1.75499210152084,-0.948192418565323,
7.34402102664981));
#27205=CARTESIAN_POINT('Ctrl Pts',(-1.76399174693945,-0.931410401122638,
7.34280349353485));
#27206=CARTESIAN_POINT('Ctrl Pts',(-1.76994669419615,-0.920043969330585,
7.34197920047895));
#27207=CARTESIAN_POINT('Ctrl Pts',(-1.82317548411611,-0.816014654065569,
7.33443685126731));
#27208=CARTESIAN_POINT('Ctrl Pts',(-1.86323512525757,-0.71985924465018,
7.32746571093228));
#27209=CARTESIAN_POINT('Ctrl Pts',(-1.94773810326278,-0.461926290934635,
7.30881056135202));
#27210=CARTESIAN_POINT('Ctrl Pts',(-1.97962347072231,-0.296898718610514,
7.29687699468382));
#27211=CARTESIAN_POINT('Ctrl Pts',(-1.99236283329669,-0.101583539268264,
7.28376167222506));
#27212=CARTESIAN_POINT('Ctrl Pts',(-1.99360388469226,-0.0732982310438227,
7.28188860540407));
#27213=CARTESIAN_POINT('Ctrl Pts',(-1.99437183414486,-0.0392611292870622,
7.27967368621796));
#27214=CARTESIAN_POINT('Ctrl Pts',(-1.99447646566995,-0.033527286803309,
7.2793018961564));
#27215=CARTESIAN_POINT('Ctrl Pts',(-1.99460047899178,-0.0246275037247389,
7.27872697230926));
#27216=CARTESIAN_POINT('Ctrl Pts',(-1.99463705276389,-0.0214618922179287,
7.27852289669645));
#27217=CARTESIAN_POINT('Ctrl Pts',(-1.99469075502728,-0.0156072229377242,
7.2781462645416));
#27218=CARTESIAN_POINT('Ctrl Pts',(-1.99470998212934,-0.0129182411510024,
7.277973594608));
#27219=CARTESIAN_POINT('Ctrl Pts',(-1.99474089383202,-0.00689035509265752,
7.27758721691371));
#27220=CARTESIAN_POINT('Ctrl Pts',(-1.99474963291213,-0.00355146651014842,
7.27737367630814));
#27221=CARTESIAN_POINT('Ctrl Pts',(-1.99475068666648,0.00633823593360937,
7.27674254497808));
#27222=CARTESIAN_POINT('Ctrl Pts',(-1.99471911543883,0.0128890874863369,
7.27632627015099));
#27223=CARTESIAN_POINT('Ctrl Pts',(-1.99419126750845,0.0670499353735925,
7.27289846024733));
#27224=CARTESIAN_POINT('Ctrl Pts',(-1.99202276093881,0.114632811185366,
7.26997536760017));
#27225=CARTESIAN_POINT('Ctrl Pts',(-1.98147388664981,0.24401713358489,7.26215838591947));
#27226=CARTESIAN_POINT('Ctrl Pts',(-1.96973748999983,0.325452349299354,
7.25738005423522));
#27227=CARTESIAN_POINT('Ctrl Pts',(-1.92122301949776,0.558861592470391,
7.24354819242071));
#27228=CARTESIAN_POINT('Ctrl Pts',(-1.87159159017216,0.707503951896778,
7.23452215364744));
#27229=CARTESIAN_POINT('Ctrl Pts',(-1.79612706465119,0.86798809244787,7.22355013073217));
#27230=CARTESIAN_POINT('Ctrl Pts',(-1.78681411569341,0.887001140432456,
7.22223040976254));
#27231=CARTESIAN_POINT('Ctrl Pts',(-1.77363745262787,0.912852294724462,
7.22040713363302));
#27232=CARTESIAN_POINT('Ctrl Pts',(-1.77003314117497,0.919821614036633,
7.21991267046705));
#27233=CARTESIAN_POINT('Ctrl Pts',(-1.76423606591414,0.930870622779886,
7.21912402839341));
#27234=CARTESIAN_POINT('Ctrl Pts',(-1.76207002266776,0.934964302661715,
7.21883079525606));
#27235=CARTESIAN_POINT('Ctrl Pts',(-1.75760286108029,0.943336283696662,
7.21822895207724));
#27236=CARTESIAN_POINT('Ctrl Pts',(-1.75530033296402,0.947613793602898,
7.21792029344933));
#27237=CARTESIAN_POINT('Ctrl Pts',(-1.74995552530238,0.957456762304467,
7.21720734272551));
#27238=CARTESIAN_POINT('Ctrl Pts',(-1.7469022927326,0.963016183834959,7.21680266180658));
#27239=CARTESIAN_POINT('Ctrl Pts',(-1.73726225020492,0.980372371082721,
7.2155329401265));
#27240=CARTESIAN_POINT('Ctrl Pts',(-1.73058217739676,0.992116638460261,
7.21466456191485));
#27241=CARTESIAN_POINT('Ctrl Pts',(-1.66396023288622,1.10652461966725,7.20611292792303));
#27242=CARTESIAN_POINT('Ctrl Pts',(-1.59508437398908,1.20368477488011,7.19809532983916));
#27243=CARTESIAN_POINT('Ctrl Pts',(-1.43637289912589,1.38985052728461,7.18118149466509));
#27244=CARTESIAN_POINT('Ctrl Pts',(-1.34589232997853,1.47764178287968,7.17229882799095));
#27245=CARTESIAN_POINT('Ctrl Pts',(-1.20754913031707,1.58855506330613,7.16018793139051));
#27246=CARTESIAN_POINT('Ctrl Pts',(-1.16611324212138,1.61921680435236,7.15672526981292));
#27247=CARTESIAN_POINT('Ctrl Pts',(-1.11758002107271,1.65229971701209,7.15289299311178));
#27248=CARTESIAN_POINT('Ctrl Pts',(-1.11160548206492,1.65632506303091,7.15242496799704));
#27249=CARTESIAN_POINT('Ctrl Pts',(-1.10272055999878,1.66224155073488,7.15173462521528));
#27250=CARTESIAN_POINT('Ctrl Pts',(-1.0998269210096,1.66415754984446,7.15151067966071));
#27251=CARTESIAN_POINT('Ctrl Pts',(-1.09467350338531,1.66755053035037,7.15111343651087));
#27252=CARTESIAN_POINT('Ctrl Pts',(-1.0924157176492,1.66903048217886,7.15093994048077));
#27253=CARTESIAN_POINT('Ctrl Pts',(-1.08758235901016,1.6721846821442,7.15056969018291));
#27254=CARTESIAN_POINT('Ctrl Pts',(-1.08500592966238,1.67385756016979,7.15037302776044));
#27255=CARTESIAN_POINT('Ctrl Pts',(-1.07796762688584,1.67840445835585,7.1498376613282));
#27256=CARTESIAN_POINT('Ctrl Pts',(-1.07349809126748,1.68126665940922,7.14949973832222));
#27257=CARTESIAN_POINT('Ctrl Pts',(-1.05040169332083,1.69592747719877,7.14776376948652));
#27258=CARTESIAN_POINT('Ctrl Pts',(-1.0315906753481,1.70743506527776,7.14638414192533));
#27259=CARTESIAN_POINT('Ctrl Pts',(-0.976506181248834,1.73989006721012,
7.14243073808672));
#27260=CARTESIAN_POINT('Ctrl Pts',(-0.939757365411546,1.76001089346714,
7.13989985853828));
#27261=CARTESIAN_POINT('Ctrl Pts',(-0.785700343710376,1.83815821510842,
7.12961006741691));
#27262=CARTESIAN_POINT('Ctrl Pts',(-0.663454394023345,1.88573132329631,
7.12217070924366));
#27263=CARTESIAN_POINT('Ctrl Pts',(-0.435752793124694,1.94943407117073,
7.10831591615025));
#27264=CARTESIAN_POINT('Ctrl Pts',(-0.331998051581029,1.96975792856896,
7.10200553299235));
#27265=CARTESIAN_POINT('Ctrl Pts',(-0.214359720014107,1.98324046306529,
7.09461381602594));
#27266=CARTESIAN_POINT('Ctrl Pts',(-0.201574317927565,1.98458071287914,
7.09380754432778));
#27267=CARTESIAN_POINT('Ctrl Pts',(-0.182589241293978,1.9863855031038,7.09260565996354));
#27268=CARTESIAN_POINT('Ctrl Pts',(-0.176398736218186,1.98694481111507,
7.09221302739874));
#27269=CARTESIAN_POINT('Ctrl Pts',(-0.165382424496781,1.98788823918704,
7.09151297733458));
#27270=CARTESIAN_POINT('Ctrl Pts',(-0.1605576219764,1.98828374413182,7.09120592011053));
#27271=CARTESIAN_POINT('Ctrl Pts',(-0.150405362365629,1.9890787643456,7.09055883422007));
#27272=CARTESIAN_POINT('Ctrl Pts',(-0.145077651741275,1.98947444764908,
7.09021868770202));
#27273=CARTESIAN_POINT('Ctrl Pts',(-0.131033727629096,1.99046076219768,
7.08932052721176));
#27274=CARTESIAN_POINT('Ctrl Pts',(-0.122315187592673,1.99101553848319,
7.08876139281826));
#27275=CARTESIAN_POINT('Ctrl Pts',(-0.0827107702847989,1.99327452464209,
7.08621423956927));
#27276=CARTESIAN_POINT('Ctrl Pts',(-0.051792890060909,1.99431735687546,
7.08420563688783));
#27277=CARTESIAN_POINT('Ctrl Pts',(0.0311375349021303,1.99518483835903,
7.07876063889943));
#27278=CARTESIAN_POINT('Ctrl Pts',(0.0831369344897313,1.99369494899308,
7.07528550194827));
#27279=CARTESIAN_POINT('Ctrl Pts',(0.236146732048212,1.98331463699855,7.06488504609092));
#27280=CARTESIAN_POINT('Ctrl Pts',(0.336600332260701,1.96875573466987,7.05782308017482));
#27281=CARTESIAN_POINT('Ctrl Pts',(0.551908815801065,1.92058655224867,7.04243041712817));
#27282=CARTESIAN_POINT('Ctrl Pts',(0.66575901982097,1.88415182408532,7.03412492786596));
#27283=CARTESIAN_POINT('Ctrl Pts',(0.782012012049444,1.83508364595316,7.02588567682527));
#27284=CARTESIAN_POINT('Ctrl Pts',(0.788328602413289,1.83237899807135,7.02543882882449));
#27285=CARTESIAN_POINT('Ctrl Pts',(0.797807196215396,1.82826235255206,7.02476968361696));
#27286=CARTESIAN_POINT('Ctrl Pts',(0.80097962344079,1.82687470707954,7.0245459599067));
#27287=CARTESIAN_POINT('Ctrl Pts',(0.806465424282125,1.82445813655712,7.02415952189054));
#27288=CARTESIAN_POINT('Ctrl Pts',(0.8087804688011,1.82343306048631,7.02399657474294));
#27289=CARTESIAN_POINT('Ctrl Pts',(0.813625677936984,1.82127661279221,7.02365582594433));
#27290=CARTESIAN_POINT('Ctrl Pts',(0.816155441351031,1.82014437333398,7.02347808076424));
#27291=CARTESIAN_POINT('Ctrl Pts',(0.822265552123668,1.81739438761081,7.0230491562741));
#27292=CARTESIAN_POINT('Ctrl Pts',(0.825843520910581,1.81577131763351,7.02279830319067));
#27293=CARTESIAN_POINT('Ctrl Pts',(0.838302711073343,1.81007502420444,7.02192581134149));
#27294=CARTESIAN_POINT('Ctrl Pts',(0.847158961074161,1.80594704590415,7.02130745159122));
#27295=CARTESIAN_POINT('Ctrl Pts',(0.972007338894504,1.74663356459625,7.01261124055757));
#27296=CARTESIAN_POINT('Ctrl Pts',(1.08245438858042,1.68042562113706,7.00516380797185));
#27297=CARTESIAN_POINT('Ctrl Pts',(1.3085558397663,1.51328155150371,6.98885390347805));
#27298=CARTESIAN_POINT('Ctrl Pts',(1.42048995154919,1.40873720834088,6.98001442590273));
#27299=CARTESIAN_POINT('Ctrl Pts',(1.53269722152463,1.27682725685387,6.96930091877563));
#27300=CARTESIAN_POINT('Ctrl Pts',(1.54575010852392,1.26099372312026,6.96802219236812));
#27301=CARTESIAN_POINT('Ctrl Pts',(1.56368323574309,1.23854341395479,6.9662176781642));
#27302=CARTESIAN_POINT('Ctrl Pts',(1.56877066100798,1.23209320260194,6.96570019559267));
#27303=CARTESIAN_POINT('Ctrl Pts',(1.57670836275463,1.22190033573453,6.96488388698674));
#27304=CARTESIAN_POINT('Ctrl Pts',(1.57958553017727,1.21817865844236,6.96458613003455));
#27305=CARTESIAN_POINT('Ctrl Pts',(1.58509773155024,1.21099614557565,6.96401203939623));
#27306=CARTESIAN_POINT('Ctrl Pts',(1.58773466549602,1.20753679639785,6.96373578288426));
#27307=CARTESIAN_POINT('Ctrl Pts',(1.59392805115474,1.19935643847254,6.963083077779));
#27308=CARTESIAN_POINT('Ctrl Pts',(1.59747486087811,1.19462821261838,6.96270625426327));
#27309=CARTESIAN_POINT('Ctrl Pts',(1.60777069899071,1.18077506552362,6.96160343448227));
#27310=CARTESIAN_POINT('Ctrl Pts',(1.61446283901,1.17160834262333,6.96087523625416));
#27311=CARTESIAN_POINT('Ctrl Pts',(1.66581681700103,1.09998946973615,6.95519705379899));
#27312=CARTESIAN_POINT('Ctrl Pts',(1.70691196067171,1.03507073769376,6.95011169183221));
#27313=CARTESIAN_POINT('Ctrl Pts',(1.79296326601329,0.880014278648866,6.93809529956556));
#27314=CARTESIAN_POINT('Ctrl Pts',(1.83504170557687,0.788518249625135,6.93109369109041));
#27315=CARTESIAN_POINT('Ctrl Pts',(1.8820732772755,0.661833312060828,6.9216653500211));
#27316=CARTESIAN_POINT('Ctrl Pts',(1.89326276460418,0.629109938013492,6.91925381924777));
#27317=CARTESIAN_POINT('Ctrl Pts',(1.92949110039182,0.513420053017111,6.91083889901536));
#27318=CARTESIAN_POINT('Ctrl Pts',(1.9499738739975,0.429117469235799,6.90490062476081));
#27319=CARTESIAN_POINT('Ctrl Pts',(1.96625931665297,0.336025593520275,6.89872759464816));
#27320=CARTESIAN_POINT('Ctrl Pts',(1.96756349581628,0.328302900811625,6.89821836449237));
#27321=CARTESIAN_POINT('Ctrl Pts',(1.96939308725892,0.317066318167938,6.89748179541153));
#27322=CARTESIAN_POINT('Ctrl Pts',(1.96995462975499,0.313558510403451,6.89725247236131));
#27323=CARTESIAN_POINT('Ctrl Pts',(1.97092921167129,0.30736458901631,6.89684865593484));
#27324=CARTESIAN_POINT('Ctrl Pts',(1.97134613622403,0.304679109155858,6.89667394341581));
#27325=CARTESIAN_POINT('Ctrl Pts',(1.97221070370737,0.299034213570926,6.89630747940421));
#27326=CARTESIAN_POINT('Ctrl Pts',(1.97265717360171,0.296074646721272,6.89611579512523));
#27327=CARTESIAN_POINT('Ctrl Pts',(1.97382488240029,0.288214216243301,6.89560785931549));
#27328=CARTESIAN_POINT('Ctrl Pts',(1.97453453561625,0.283311612459413,6.89529225886045));
#27329=CARTESIAN_POINT('Ctrl Pts',(1.97773611920141,0.260597149070922,6.89383539031632));
#27330=CARTESIAN_POINT('Ctrl Pts',(1.98000544312203,0.242754055066817,6.89270619366479));
#27331=CARTESIAN_POINT('Ctrl Pts',(1.98556877822048,0.193720709666876,6.88963882631248));
#27332=CARTESIAN_POINT('Ctrl Pts',(1.98836918642222,0.162478587686997,6.88772389278685));
#27333=CARTESIAN_POINT('Ctrl Pts',(1.99563531842221,0.0522288974078525,
6.88106462330119));
#27334=CARTESIAN_POINT('Ctrl Pts',(1.99613691718685,-0.0269693157510462,
6.87645628370727));
#27335=CARTESIAN_POINT('Ctrl Pts',(1.9834004018424,-0.266328035117351,6.86254317604347));
#27336=CARTESIAN_POINT('Ctrl Pts',(1.95554448664742,-0.425025067664789,
6.85328606102782));
#27337=CARTESIAN_POINT('Ctrl Pts',(1.90489378778237,-0.592119051995601,
6.84248185364553));
#27338=CARTESIAN_POINT('Ctrl Pts',(1.90067227458819,-0.605532991200891,
6.84160730521256));
#27339=CARTESIAN_POINT('Ctrl Pts',(1.89306982741216,-0.628826852087737,
6.84007542127812));
#27340=CARTESIAN_POINT('Ctrl Pts',(1.88975245308941,-0.638727047173065,
6.83942016256767));
#27341=CARTESIAN_POINT('Ctrl Pts',(1.88431154579514,-0.654551110063635,
6.83836590224008));
#27342=CARTESIAN_POINT('Ctrl Pts',(1.88223740923146,-0.66049185545241,6.83796853414694));
#27343=CARTESIAN_POINT('Ctrl Pts',(1.87850946895029,-0.671009253072189,
6.83726220510875));
#27344=CARTESIAN_POINT('Ctrl Pts',(1.87686695384153,-0.675589875245848,
6.83695362122606));
#27345=CARTESIAN_POINT('Ctrl Pts',(1.87341622441068,-0.685103508038202,
6.83631069877948));
#27346=CARTESIAN_POINT('Ctrl Pts',(1.87160525065326,-0.690035471166528,
6.83597627017356));
#27347=CARTESIAN_POINT('Ctrl Pts',(1.86686985145359,-0.702775956782002,
6.83510939743517));
#27348=CARTESIAN_POINT('Ctrl Pts',(1.86391593557773,-0.710573338436012,
6.83457597042715));
#27349=CARTESIAN_POINT('Ctrl Pts',(1.85113523944515,-0.743682136118935,
6.83229847058753));
#27350=CARTESIAN_POINT('Ctrl Pts',(1.84084148645247,-0.76880901074337,6.83053878005297));
#27351=CARTESIAN_POINT('Ctrl Pts',(1.81271389500614,-0.833661568358566,
6.82591252252434));
#27352=CARTESIAN_POINT('Ctrl Pts',(1.79408729919948,-0.873025523795212,
6.82302005798224));
#27353=CARTESIAN_POINT('Ctrl Pts',(1.6945271571241,-1.06676199560036,6.808355877972));
#27354=CARTESIAN_POINT('Ctrl Pts',(1.5948941023617,-1.21066165863627,6.79597968835468));
#27355=CARTESIAN_POINT('Ctrl Pts',(1.43768831303722,-1.38407297265698,6.77991314323283));
#27356=CARTESIAN_POINT('Ctrl Pts',(1.39553477671232,-1.4265657836734,6.77587334301589));
#27357=CARTESIAN_POINT('Ctrl Pts',(1.34659752025626,-1.47164794256912,6.77153015647505));
#27358=CARTESIAN_POINT('Ctrl Pts',(1.34164155168241,-1.476167503477,6.77109407605614));
#27359=CARTESIAN_POINT('Ctrl Pts',(1.33412347058594,-1.48295442642768,6.77043833648228));
#27360=CARTESIAN_POINT('Ctrl Pts',(1.33157822835514,-1.48524027949247,6.77021732800031));
#27361=CARTESIAN_POINT('Ctrl Pts',(1.32714697978876,-1.48919938660804,6.76983429231993));
#27362=CARTESIAN_POINT('Ctrl Pts',(1.32526366855471,-1.4908756245977,6.76967204186657));
#27363=CARTESIAN_POINT('Ctrl Pts',(1.3212957029328,-1.49439384583382,6.76933134337173));
#27364=CARTESIAN_POINT('Ctrl Pts',(1.31921036722535,-1.49623504443829,6.7691529561751));
#27365=CARTESIAN_POINT('Ctrl Pts',(1.31413105912476,-1.50070082764237,6.768720046878));
#27366=CARTESIAN_POINT('Ctrl Pts',(1.31113304648571,-1.50332084058045,6.76846586606313));
#27367=CARTESIAN_POINT('Ctrl Pts',(1.30050239528803,-1.51255515181899,6.76756920815715));
#27368=CARTESIAN_POINT('Ctrl Pts',(1.29282722909961,-1.51912057894822,6.76693025792698));
#27369=CARTESIAN_POINT('Ctrl Pts',(1.24141590694143,-1.56242656697028,6.76270342425805));
#27370=CARTESIAN_POINT('Ctrl Pts',(1.1961644194305,-1.59733598396568,6.75923636779827));
#27371=CARTESIAN_POINT('Ctrl Pts',(1.02556110511555,-1.71762602727148,6.74680698745791));
#27372=CARTESIAN_POINT('Ctrl Pts',(0.892090093568565,-1.79058504929666,
6.73824555030284));
#27373=CARTESIAN_POINT('Ctrl Pts',(0.716234240689046,-1.86212156018101,
6.72701797584538));
#27374=CARTESIAN_POINT('Ctrl Pts',(0.680427989701769,-1.87550145784045,
6.72473694622258));
#27375=CARTESIAN_POINT('Ctrl Pts',(0.597422668638744,-1.9038285194621,6.71943515037275));
#27376=CARTESIAN_POINT('Ctrl Pts',(0.550009275411201,-1.91806309591593,
6.71639633892168));
#27377=CARTESIAN_POINT('Ctrl Pts',(0.492769956287579,-1.93295075998348,
6.71269482342136));
#27378=CARTESIAN_POINT('Ctrl Pts',(0.483403991971901,-1.93531430151124,
6.71208813518755));
#27379=CARTESIAN_POINT('Ctrl Pts',(0.468072283069895,-1.93906508658658,
6.71109319999435));
#27380=CARTESIAN_POINT('Ctrl Pts',(0.462116589323327,-1.94049306329855,
6.71070626699457));
#27381=CARTESIAN_POINT('Ctrl Pts',(0.451452101024465,-1.94299817173325,
6.71001257754239));
#27382=CARTESIAN_POINT('Ctrl Pts',(0.446745772305301,-1.94408567432939,
6.70970615728118));
#27383=CARTESIAN_POINT('Ctrl Pts',(0.436881860171351,-1.94632724257127,
6.70906331076621));
#27384=CARTESIAN_POINT('Ctrl Pts',(0.431723553822848,-1.94747792467844,
6.70872677852071));
#27385=CARTESIAN_POINT('Ctrl Pts',(0.41820087199882,-1.95043811236286,6.7078435812871));
#27386=CARTESIAN_POINT('Ctrl Pts',(0.409829387923799,-1.95221429881714,
6.70729585389748));
#27387=CARTESIAN_POINT('Ctrl Pts',(0.391412916538124,-1.95599806256989,
6.70608868774871));
#27388=CARTESIAN_POINT('Ctrl Pts',(0.381363421326324,-1.95798223341495,
6.70542851679255));
#27389=CARTESIAN_POINT('Ctrl Pts',(0.351647204436483,-1.96361194484257,
6.70347195743381));
#27390=CARTESIAN_POINT('Ctrl Pts',(0.331940898929404,-1.96703909918402,
6.7021687228488));
#27391=CARTESIAN_POINT('Ctrl Pts',(0.262270416187405,-1.97807886991449,
6.69753996073748));
#27392=CARTESIAN_POINT('Ctrl Pts',(0.21207519526325,-1.98408799545187,6.6941660901811));
#27393=CARTESIAN_POINT('Ctrl Pts',(0.043655013580932,-1.99778648180186,
6.68272047543573));
#27394=CARTESIAN_POINT('Ctrl Pts',(-0.0750107800357254,-1.99685377356109,
6.67443411863093));
#27395=CARTESIAN_POINT('Ctrl Pts',(-0.244166897664909,-1.98042050028122,
6.6625927489732));
#27396=CARTESIAN_POINT('Ctrl Pts',(-0.295244664471885,-1.97345227131158,
6.65901652919969));
#27397=CARTESIAN_POINT('Ctrl Pts',(-0.398610369668733,-1.95524713322919,
6.65183913742975));
#27398=CARTESIAN_POINT('Ctrl Pts',(-0.45083571632199,-1.94386982695586,
6.64824464390534));
#27399=CARTESIAN_POINT('Ctrl Pts',(-0.5095780399058,-1.92857734695514,6.64428377433788));
#27400=CARTESIAN_POINT('Ctrl Pts',(-0.51660005926903,-1.92670826661875,
6.6438116534999));
#27401=CARTESIAN_POINT('Ctrl Pts',(-0.526972403450067,-1.92388663326078,
6.64311644885455));
#27402=CARTESIAN_POINT('Ctrl Pts',(-0.530330599819436,-1.92296363641789,
6.64289170424983));
#27403=CARTESIAN_POINT('Ctrl Pts',(-0.536288848869815,-1.92130922238776,
6.64249357496844));
#27404=CARTESIAN_POINT('Ctrl Pts',(-0.53888984503603,-1.92058131634648,
6.64231998851144));
#27405=CARTESIAN_POINT('Ctrl Pts',(-0.544438688353919,-1.91901627595181,
6.64195012442986));
#27406=CARTESIAN_POINT('Ctrl Pts',(-0.547386077679175,-1.91817763385395,
6.64175393637243));
#27407=CARTESIAN_POINT('Ctrl Pts',(-0.555400255705559,-1.91587732564434,
6.64122120063175));
#27408=CARTESIAN_POINT('Ctrl Pts',(-0.560463244677572,-1.91440234116177,
6.64088542103152));
#27409=CARTESIAN_POINT('Ctrl Pts',(-0.586253432000998,-1.90677788540156,
6.6391786965708));
#27410=CARTESIAN_POINT('Ctrl Pts',(-0.606886485296367,-1.90031152123041,
6.6378254374689));
#27411=CARTESIAN_POINT('Ctrl Pts',(-0.66605306859671,-1.88070678072047,
6.6339691973003));
#27412=CARTESIAN_POINT('Ctrl Pts',(-0.704296488517449,-1.86672215136927,
6.63150663233279));
#27413=CARTESIAN_POINT('Ctrl Pts',(-0.884650774639296,-1.79443850019209,
6.61991914258434));
#27414=CARTESIAN_POINT('Ctrl Pts',(-1.02014269740057,-1.72102607436799,
6.61125317488648));
#27415=CARTESIAN_POINT('Ctrl Pts',(-1.17712688688369,-1.61085617140632,
6.59991259588884));
#27416=CARTESIAN_POINT('Ctrl Pts',(-1.20774180750381,-1.5880317425933,6.59763418900329));
#27417=CARTESIAN_POINT('Ctrl Pts',(-1.2767079609247,-1.53346690944367,6.59231920331009));
#27418=CARTESIAN_POINT('Ctrl Pts',(-1.31456215159463,-1.50114279331927,
6.5892640316761));
#27419=CARTESIAN_POINT('Ctrl Pts',(-1.35828461002956,-1.46088470342688,
6.58554445506575));
#27420=CARTESIAN_POINT('Ctrl Pts',(-1.36535529606649,-1.45427855267605,
6.58493671135866));
#27421=CARTESIAN_POINT('Ctrl Pts',(-1.37682599295557,-1.44340407420989,
6.58394038747499));
#27422=CARTESIAN_POINT('Ctrl Pts',(-1.38125494432265,-1.43916639543346,
6.5835531274377));
#27423=CARTESIAN_POINT('Ctrl Pts',(-1.38913938507402,-1.43155253823965,
6.58285907218617));
#27424=CARTESIAN_POINT('Ctrl Pts',(-1.39260228899916,-1.42818407948891,
6.58255261452684));
#27425=CARTESIAN_POINT('Ctrl Pts',(-1.39927757448958,-1.42164349036459,
6.58195869915859));
#27426=CARTESIAN_POINT('Ctrl Pts',(-1.40249149361131,-1.41847296553758,
6.58167131299408));
#27427=CARTESIAN_POINT('Ctrl Pts',(-1.40944639958939,-1.41156522021896,
6.58104626532935));
#27428=CARTESIAN_POINT('Ctrl Pts',(-1.41318333649937,-1.40782398786074,
6.58070842716295));
#27429=CARTESIAN_POINT('Ctrl Pts',(-1.4279587445258,-1.39291348870169,6.57936466420977));
#27430=CARTESIAN_POINT('Ctrl Pts',(-1.43887978834616,-1.3816291449958,6.57835360997683));
#27431=CARTESIAN_POINT('Ctrl Pts',(-1.49773550372064,-1.31936081581584,
6.57280511859302));
#27432=CARTESIAN_POINT('Ctrl Pts',(-1.54308986380432,-1.26601591592972,
6.56815940871857));
#27433=CARTESIAN_POINT('Ctrl Pts',(-1.62125493049575,-1.1636251635499,6.55943007336932));
#27434=CARTESIAN_POINT('Ctrl Pts',(-1.65487584720457,-1.11529197560446,
6.55537920419555));
#27435=CARTESIAN_POINT('Ctrl Pts',(-1.76854600651221,-0.935400164552377,
6.5406084665738));
#27436=CARTESIAN_POINT('Ctrl Pts',(-1.8354437169428,-0.796166047033757,
6.52969834963504));
#27437=CARTESIAN_POINT('Ctrl Pts',(-1.89030717688213,-0.637157031983151,
6.51860050737854));
#27438=CARTESIAN_POINT('Ctrl Pts',(-1.89480728673851,-0.623647080281074,
6.51766817237438));
#27439=CARTESIAN_POINT('Ctrl Pts',(-1.90060705794863,-0.605592834965986,
6.51643733635948));
#27440=CARTESIAN_POINT('Ctrl Pts',(-1.90203565951752,-0.601090859622062,
6.51613166090642));
#27441=CARTESIAN_POINT('Ctrl Pts',(-1.90424035390347,-0.594056606013305,
6.5156560340981));
#27442=CARTESIAN_POINT('Ctrl Pts',(-1.9050274046608,-0.591527822063384,
6.51548544782484));
#27443=CARTESIAN_POINT('Ctrl Pts',(-1.90652867546336,-0.586670184747108,
6.51515853882475));
#27444=CARTESIAN_POINT('Ctrl Pts',(-1.90724365771197,-0.584341617744951,
6.51500217448601));
#27445=CARTESIAN_POINT('Ctrl Pts',(-1.90894323872839,-0.578770040735878,
6.51462885408686));
#27446=CARTESIAN_POINT('Ctrl Pts',(-1.90992383860049,-0.575525829048528,
6.51441213436175));
#27447=CARTESIAN_POINT('Ctrl Pts',(-1.91284612196619,-0.56576803768594,
6.51376222326111));
#27448=CARTESIAN_POINT('Ctrl Pts',(-1.91476281268981,-0.559246933956545,
6.51333046828122));
#27449=CARTESIAN_POINT('Ctrl Pts',(-1.91907869260439,-0.544280813955333,
6.51234520752543));
#27450=CARTESIAN_POINT('Ctrl Pts',(-1.92145555607818,-0.535829436775219,
6.51179292195998));
#27451=CARTESIAN_POINT('Ctrl Pts',(-1.97072567241273,-0.356095946879005,
6.50012887838157));
#27452=CARTESIAN_POINT('Ctrl Pts',(-1.99459991883049,-0.179306569445352,
6.490166969518));
#27453=CARTESIAN_POINT('Ctrl Pts',(-1.99474929467261,-0.00167746926262795,
6.47978083014939));
#27454=CARTESIAN_POINT('Origin',(-6.93889390390723E-17,-2.77555756156289E-16,
5.));
#27455=CARTESIAN_POINT('',(4.,2.12302963502652E-16,5.));
#27456=CARTESIAN_POINT('Origin',(-6.93889390390723E-17,-2.77555756156289E-16,
5.));
#27457=CARTESIAN_POINT('',(4.,2.12302963502652E-16,5.5));
#27458=CARTESIAN_POINT('',(4.,2.12302963502652E-16,5.));
#27459=CARTESIAN_POINT('Origin',(-6.93889390390723E-17,-2.77555756156289E-16,
5.5));
#27460=CARTESIAN_POINT('Origin',(0.,0.,5.));
#27461=CARTESIAN_POINT('',(4.5,5.51091059616309E-16,5.5));
#27462=CARTESIAN_POINT('Origin',(0.,0.,5.5));
#27463=CARTESIAN_POINT('',(4.5,5.51091059616309E-16,5.));
#27464=CARTESIAN_POINT('',(4.5,5.51091059616309E-16,5.));
#27465=CARTESIAN_POINT('',(-4.5,5.51091059616309E-16,5.));
#27466=CARTESIAN_POINT('Origin',(0.,0.,5.));
#27467=CARTESIAN_POINT('Origin',(0.,0.,5.));
#27468=CARTESIAN_POINT('Origin',(0.,0.,5.5));
#27469=CARTESIAN_POINT('Ctrl Pts',(-0.873247375836237,1.78947949709258,
4.73478819788609));
#27470=CARTESIAN_POINT('Ctrl Pts',(-1.4690688679767,1.49873543257783,4.77718129246584));
#27471=CARTESIAN_POINT('Ctrl Pts',(-2.33695383301822,0.280390198345026,
4.86195971951784));
#27472=CARTESIAN_POINT('Ctrl Pts',(-1.4992907210582,-1.81727971168775,4.98912347904207));
#27473=CARTESIAN_POINT('Ctrl Pts',(0.715424845994203,-2.24230451559634,
5.11627947645882));
#27474=CARTESIAN_POINT('Ctrl Pts',(2.27294797015263,-0.613618701373298,
5.24343547387554));
#27475=CARTESIAN_POINT('Ctrl Pts',(1.74631047731586,1.57935716468537,5.37059147129228));
#27476=CARTESIAN_POINT('Ctrl Pts',(-0.382281089693881,2.32300256223768,
5.49774746870903));
#27477=CARTESIAN_POINT('Ctrl Pts',(-2.16010694979347,0.936454718196414,
5.62490346612576));
#27478=CARTESIAN_POINT('Ctrl Pts',(-1.95681075276908,-1.30920204522563,
5.75205946354249));
#27479=CARTESIAN_POINT('Ctrl Pts',(0.0412662141189832,-2.35397703574761,
5.87921546095925));
#27480=CARTESIAN_POINT('Ctrl Pts',(2.00147364547165,-1.23979915738411,6.00637145837596));
#27481=CARTESIAN_POINT('Ctrl Pts',(2.12598795827045,1.01152412810136,6.13352745579272));
#27482=CARTESIAN_POINT('Ctrl Pts',(0.300590670980986,2.33508519333647,6.26068345320944));
#27483=CARTESIAN_POINT('Ctrl Pts',(-1.80049820770884,1.51696997007267,6.38783945062618));
#27484=CARTESIAN_POINT('Ctrl Pts',(-2.25021438906683,-0.692478639950551,
6.51499544804292));
#27485=CARTESIAN_POINT('Ctrl Pts',(-0.636086407863099,-2.2667999029652,
6.64215144545965));
#27486=CARTESIAN_POINT('Ctrl Pts',(1.56144451584301,-1.76206723210801,6.76930744287639));
#27487=CARTESIAN_POINT('Ctrl Pts',(2.32685575557651,0.358792400677143,6.89646344029311));
#27488=CARTESIAN_POINT('Ctrl Pts',(0.958129905223776,2.15057580603736,7.02361943770987));
#27489=CARTESIAN_POINT('Ctrl Pts',(-1.28936992982972,1.9699022129551,7.15077543512658));
#27490=CARTESIAN_POINT('Ctrl Pts',(-2.35429024746335,-0.0175191102142973,
7.27793143254334));
#27491=CARTESIAN_POINT('Ctrl Pts',(-1.25991131263991,-1.98887227175793,
7.40508742996006));
#27492=CARTESIAN_POINT('Ctrl Pts',(0.990028418015555,-2.13607893341421,
7.5322434273768));
#27493=CARTESIAN_POINT('Ctrl Pts',(2.33193754512252,-0.324124593834741,
7.65939942479353));
#27494=CARTESIAN_POINT('Ctrl Pts',(1.53504880370339,1.78510913671325,7.78655542221029));
#27495=CARTESIAN_POINT('Ctrl Pts',(-0.669750329382192,2.25708306518675,
7.91371141962701));
#27496=CARTESIAN_POINT('Ctrl Pts',(-2.26027032938391,0.658913881193235,
8.04086741704374));
#27497=CARTESIAN_POINT('Ctrl Pts',(-1.77772393528634,-1.5435955020292,8.16802341446047));
#27498=CARTESIAN_POINT('Ctrl Pts',(0.335308732617007,-2.33035566358833,
8.29517941187722));
#27499=CARTESIAN_POINT('Ctrl Pts',(2.14080417550271,-0.9797688231252,8.42233540929394));
#27500=CARTESIAN_POINT('Ctrl Pts',(1.98280475043952,1.26943876818998,8.5494914067107));
#27501=CARTESIAN_POINT('Ctrl Pts',(0.00622378670963759,2.35434719809311,
8.67664740412742));
#27502=CARTESIAN_POINT('Ctrl Pts',(-1.97606548674515,1.27990415919458,8.80380340154417));
#27503=CARTESIAN_POINT('Ctrl Pts',(-2.1459543144859,-0.968436649845614,
8.93095939896089));
#27504=CARTESIAN_POINT('Ctrl Pts',(-0.347624688880569,-2.32855030873816,
9.05811539637764));
#27505=CARTESIAN_POINT('Ctrl Pts',(1.76953806512862,-1.55297279457662,9.18527139379437));
#27506=CARTESIAN_POINT('Ctrl Pts',(2.26372243130189,0.646954572327261,9.3124273912111));
#27507=CARTESIAN_POINT('Ctrl Pts',(0.681674217651123,2.25351053372882,9.43958338862785));
#27508=CARTESIAN_POINT('Ctrl Pts',(-1.52558943758558,1.7932000258094,9.56673938604457));
#27509=CARTESIAN_POINT('Ctrl Pts',(-2.33361860631759,-0.311791059660172,
9.69389538346132));
#27510=CARTESIAN_POINT('Ctrl Pts',(-1.00130807954425,-2.1308147724463,9.82105138087805));
#27511=CARTESIAN_POINT('Ctrl Pts',(1.24937849388772,-1.99550566114121,9.94820737829478));
#27512=CARTESIAN_POINT('Ctrl Pts',(2.35416471413455,-0.0299660367678983,
10.0753633757115));
#27513=CARTESIAN_POINT('Ctrl Pts',(1.29976683558327,1.96305772654644,10.2025193731283));
#27514=CARTESIAN_POINT('Ctrl Pts',(-0.946746389309996,2.15561145361688,
10.329675370545));
#27515=CARTESIAN_POINT('Ctrl Pts',(-2.32492625710246,0.371089428132024,
10.4568313679617));
#27516=CARTESIAN_POINT('Ctrl Pts',(-1.57073884614258,-1.75378702864814,
10.5839873653785));
#27517=CARTESIAN_POINT('Ctrl Pts',(0.624093019129565,-2.27013157506554,
10.7111433627952));
#27518=CARTESIAN_POINT('Ctrl Pts',(2.24652155383406,-0.704365226849547,
10.838299360212));
#27519=CARTESIAN_POINT('Ctrl Pts',(1.80849374598863,1.5074282189729,10.9654553576287));
#27520=CARTESIAN_POINT('Ctrl Pts',(-0.288241677203082,2.33664421771029,
11.0926113550454));
#27521=CARTESIAN_POINT('Ctrl Pts',(-2.12060866334743,1.02274550185841,11.2197673524622));
#27522=CARTESIAN_POINT('Ctrl Pts',(-2.00800362685378,-1.22919115648376,
11.3469233498789));
#27523=CARTESIAN_POINT('Ctrl Pts',(-0.0537052392534047,-2.35374280921101,
11.4740793472957));
#27524=CARTESIAN_POINT('Ctrl Pts',(1.94985032135694,-1.31949732433985,11.6012353447123));
#27525=CARTESIAN_POINT('Ctrl Pts',(2.1650493648414,0.924959843688164,11.7283913421291));
#27526=CARTESIAN_POINT('Ctrl Pts',(0.394516427207001,2.32106575807313,11.8555473395458));
#27527=CARTESIAN_POINT('Ctrl Pts',(-1.73785763022056,1.58834515194902,11.9827033369626));
#27528=CARTESIAN_POINT('Ctrl Pts',(-2.27630984410938,-0.601167995028458,
12.1098593343793));
#27529=CARTESIAN_POINT('Ctrl Pts',(-0.726984601378939,-2.23930410038336,
12.237015331796));
#27530=CARTESIAN_POINT('Ctrl Pts',(1.48911369335759,-1.82360354049086,12.3641713292128));
#27531=CARTESIAN_POINT('Ctrl Pts',(2.33943218997905,0.26466298027044,12.4913273266295));
#27532=CARTESIAN_POINT('Ctrl Pts',(1.04407890990149,2.1101868861631,12.6184833240463));
#27533=CARTESIAN_POINT('Ctrl Pts',(-1.20887880907301,2.02029737652902,12.745639321463));
#27534=CARTESIAN_POINT('Ctrl Pts',(-2.35308152621917,0.0774389798607678,
12.8727953188797));
#27535=CARTESIAN_POINT('Ctrl Pts',(-1.33909361885933,-1.93644461438122,
12.9999513162965));
#27536=CARTESIAN_POINT('Ctrl Pts',(0.903079228697448,-2.17426708831529,
13.1271073137132));
#27537=CARTESIAN_POINT('Ctrl Pts',(2.31696920426529,-0.417903303554905,
13.2542633111299));
#27538=CARTESIAN_POINT('Ctrl Pts',(1.60578992141732,1.72175148988184,13.3814193085467));
#27539=CARTESIAN_POINT('Ctrl Pts',(-0.578181831523024,2.28225661009723,
13.5085753059634));
#27540=CARTESIAN_POINT('Ctrl Pts',(-2.23185890739893,0.749530040825484,
13.6357313033802));
#27541=CARTESIAN_POINT('Ctrl Pts',(-1.83852787263449,-1.47064772334569,
13.7628873007969));
#27542=CARTESIAN_POINT('Ctrl Pts',(0.241057366840046,-2.34198223958423,
13.8900432982136));
#27543=CARTESIAN_POINT('Ctrl Pts',(2.09955050079873,-1.06530613404394,14.0171992956304));
#27544=CARTESIAN_POINT('Ctrl Pts',(2.03238565987995,1.18844351744209,14.1443552930471));
#27545=CARTESIAN_POINT('Ctrl Pts',(0.101164844844109,2.35218093241218,14.2715112904638));
#27546=CARTESIAN_POINT('Ctrl Pts',(-1.92284196899347,1.35855372617836,14.3986672878806));
#27547=CARTESIAN_POINT('Ctrl Pts',(-2.18326368658655,-0.881106769618909,
14.5258232852973));
#27548=CARTESIAN_POINT('Ctrl Pts',(-0.441247678706356,-2.31263701230264,
14.652979282714));
#27549=CARTESIAN_POINT('Ctrl Pts',(1.70547024564302,-1.62307138039649,14.7801352801308));
#27550=CARTESIAN_POINT('Ctrl Pts',(2.28797126823687,0.555136866329734,14.9072912775475));
#27551=CARTESIAN_POINT('Ctrl Pts',(0.77199925229478,2.22418673206457,15.0344472749642));
#27552=CARTESIAN_POINT('Ctrl Pts',(-1.45203218694544,1.85326522459962,15.161603272381));
#27553=CARTESIAN_POINT('Ctrl Pts',(-2.34429410718315,-0.217427237627146,
15.2887592697977));
#27554=CARTESIAN_POINT('Ctrl Pts',(-1.08642501545519,-2.08870058898564,
15.4159152672144));
#27555=CARTESIAN_POINT('Ctrl Pts',(1.16788735988121,-2.04426724751572,15.5430712646312));
#27556=CARTESIAN_POINT('Ctrl Pts',(2.35104111938139,-0.124880421258552,
15.6702272620479));
#27557=CARTESIAN_POINT('Ctrl Pts',(1.37787566718401,1.90904376859675,15.7973832594646));
#27558=CARTESIAN_POINT('Ctrl Pts',(-0.85904470107426,2.19203824469192,15.9245392568814));
#27559=CARTESIAN_POINT('Ctrl Pts',(-2.30806962277358,0.464547178514352,
16.0516952542981));
#27560=CARTESIAN_POINT('Ctrl Pts',(-1.64018777134433,-1.68901555332339,
16.1788512517149));
#27561=CARTESIAN_POINT('Ctrl Pts',(0.532035443145291,-2.29345323734167,
16.3060072491316));
#27562=CARTESIAN_POINT('Ctrl Pts',(2.21628835464842,-0.794389950644875,
16.4331632465483));
#27563=CARTESIAN_POINT('Ctrl Pts',(1.86781409758233,1.43326897737603,16.5603192439651));
#27564=CARTESIAN_POINT('Ctrl Pts',(-0.193774995840213,2.3463675576565,16.6874752413818));
#27565=CARTESIAN_POINT('Ctrl Pts',(-2.07763825417111,1.10743340632322,16.8146312387985));
#27566=CARTESIAN_POINT('Ctrl Pts',(-2.0559409310666,-1.1472124269728,16.9417872362153));
#27567=CARTESIAN_POINT('Ctrl Pts',(-0.148583297205478,-2.34966220304693,
17.068943233632));
#27568=CARTESIAN_POINT('Ctrl Pts',(1.89505141648223,-1.39705747681493,17.1960992310488));
#27569=CARTESIAN_POINT('Ctrl Pts',(2.20058987024978,0.836895266798587,17.3232552284655));
#27570=CARTESIAN_POINT('Ctrl Pts',(0.487799433395791,2.30326750018633,17.4504112258822));
#27571=CARTESIAN_POINT('Ctrl Pts',(-1.67238908638211,1.65713735350629,17.577567223299));
#27572=CARTESIAN_POINT('Ctrl Pts',(-2.29870195988975,-0.508879911408193,
17.7047232207157));
#27573=CARTESIAN_POINT('Ctrl Pts',(-0.816699858718716,-2.20816457842359,
17.8318792181324));
#27574=CARTESIAN_POINT('Ctrl Pts',(1.41436000287518,-1.88217301194729,17.9590352155492));
#27575=CARTESIAN_POINT('Ctrl Pts',(2.34820238013224,0.170103046936591,18.0861912129659));
#27576=CARTESIAN_POINT('Ctrl Pts',(1.12832917007305,2.06636462140593,18.2133472103826));
#27577=CARTESIAN_POINT('Ctrl Pts',(-1.12642082137883,2.06740552330695,18.3405032077994));
#27578=CARTESIAN_POINT('Ctrl Pts',(-2.34804432364603,0.17227106207802,18.4676592052161));
#27579=CARTESIAN_POINT('Ctrl Pts',(-1.41609720426133,-1.88086633568658,
18.5948152026329));
#27580=CARTESIAN_POINT('Ctrl Pts',(0.814660719412214,-2.20891769355098,
18.7219712000496));
#27581=CARTESIAN_POINT('Ctrl Pts',(2.2982311329217,-0.511002078572337,18.8491271974663));
#27582=CARTESIAN_POINT('Ctrl Pts',(1.67391840309234,1.65559253574803,18.976283194883));
#27583=CARTESIAN_POINT('Ctrl Pts',(-0.485672626059938,2.3037169020806,19.1034391922998));
#27584=CARTESIAN_POINT('Ctrl Pts',(-2.1998162295865,0.838926707575607,19.2305951897165));
#27585=CARTESIAN_POINT('Ctrl Pts',(-1.8963405073781,-1.39530718650511,19.3577511871333));
#27586=CARTESIAN_POINT('Ctrl Pts',(0.146413798377855,-2.34979838800702,
19.48490718455));
#27587=CARTESIAN_POINT('Ctrl Pts',(2.05488083723017,-1.14911018158402,19.6120631819667));
#27588=CARTESIAN_POINT('Ctrl Pts',(2.07865985827594,1.10551465762695,19.7392191793835));
#27589=CARTESIAN_POINT('Ctrl Pts',(0.19594130680613,2.34618764571867,19.8663751768002));
#27590=CARTESIAN_POINT('Ctrl Pts',(-1.86648996884708,1.43499291316336,19.9935311742169));
#27591=CARTESIAN_POINT('Ctrl Pts',(-2.21702086764734,-0.792343320191474,
20.1206871716337));
#27592=CARTESIAN_POINT('Ctrl Pts',(-0.534152754311119,-2.29296103318344,
20.2478431690504));
#27593=CARTESIAN_POINT('Ctrl Pts',(1.63862760964762,-1.6905292134525,20.3749991664672));
#27594=CARTESIAN_POINT('Ctrl Pts',(2.30849755388944,0.462415947305307,20.5021551638839));
#27595=CARTESIAN_POINT('Ctrl Pts',(0.861068236722175,2.19124415717281,20.6293111613006));
#27596=CARTESIAN_POINT('Ctrl Pts',(-1.37611246595686,1.91031514302587,20.7564671587174));
#27597=CARTESIAN_POINT('Ctrl Pts',(-2.3511554189652,-0.122709659385003,
20.8836231561341));
#27598=CARTESIAN_POINT('Ctrl Pts',(-1.1697743274058,-2.04318806955652,21.0107791535509));
#27599=CARTESIAN_POINT('Ctrl Pts',(1.08449606189562,-2.08970279139611,21.1379351509675));
#27600=CARTESIAN_POINT('Ctrl Pts',(2.34409235809092,-0.219591624101475,
21.2650911483843));
#27601=CARTESIAN_POINT('Ctrl Pts',(1.45374268180793,1.85192377805506,21.392247145801));
#27602=CARTESIAN_POINT('Ctrl Pts',(-0.769945338838868,2.2248985684377,21.5194031432178));
#27603=CARTESIAN_POINT('Ctrl Pts',(-2.2874577369461,0.557249106164581,21.6465591406345));
#27604=CARTESIAN_POINT('Ctrl Pts',(-1.70696809525024,-1.62149603343134,
21.7737151380513));
#27605=CARTESIAN_POINT('Ctrl Pts',(0.439112240372472,-2.31304342911907,
21.9008711354679));
#27606=CARTESIAN_POINT('Ctrl Pts',(2.18244923297112,-0.88312219434208,22.0280271328848));
#27607=CARTESIAN_POINT('Ctrl Pts',(1.92409549765578,1.35677779335326,22.1551831303014));
#27608=CARTESIAN_POINT('Ctrl Pts',(-0.0989930406933855,2.35227333499533,
22.2823391277182));
#27609=CARTESIAN_POINT('Ctrl Pts',(-2.0312875075515,1.19031950597351,22.4094951251349));
#27610=CARTESIAN_POINT('Ctrl Pts',(-2.10053319958978,-1.06336717179764,
22.5366511225517));
#27611=CARTESIAN_POINT('Ctrl Pts',(-0.243219608702475,-2.3417586738557,
22.6638071199684));
#27612=CARTESIAN_POINT('Ctrl Pts',(1.83716924470714,-1.47234460332425,22.7909631173852));
#27613=CARTESIAN_POINT('Ctrl Pts',(2.23254999475177,0.74746905325216,22.9181191148019));
#27614=CARTESIAN_POINT('Ctrl Pts',(0.580288785209907,2.2817218039006,23.0452751122186));
#27615=CARTESIAN_POINT('Ctrl Pts',(-1.60419954939816,1.72323337663434,23.1724311096353));
#27616=CARTESIAN_POINT('Ctrl Pts',(-2.31735406544925,-0.415763875272499,
23.2995871070521));
#27617=CARTESIAN_POINT('Ctrl Pts',(-0.905086337525095,-2.17343235143429,
23.4267431044688));
#27618=CARTESIAN_POINT('Ctrl Pts',(1.33730513505049,-1.93768016979155,23.5538991018855));
#27619=CARTESIAN_POINT('Ctrl Pts',(2.35315202240421,0.0752663543075803,
23.6810550993023));
#27620=CARTESIAN_POINT('Ctrl Pts',(1.21074362782129,2.01918036151453,23.808211096719));
#27621=CARTESIAN_POINT('Ctrl Pts',(-1.04213013616294,2.11114998139328,23.9353670941358));
#27622=CARTESIAN_POINT('Ctrl Pts',(-2.33918683035109,0.266822857618686,
24.0625230915525));
#27623=CARTESIAN_POINT('Ctrl Pts',(-1.49079678587771,-1.82222786935457,
24.1896790889692));
#27624=CARTESIAN_POINT('Ctrl Pts',(0.724916749292811,-2.2399743684316,24.316835086386));
#27625=CARTESIAN_POINT('Ctrl Pts',(2.27575381739723,-0.603269448287994,
24.4439910838027));
#27626=CARTESIAN_POINT('Ctrl Pts',(1.7393234034089,1.5867399166183,24.5711470812195));
#27627=CARTESIAN_POINT('Ctrl Pts',(-0.392373226558104,2.32142902448388,
24.6983030786362));
#27628=CARTESIAN_POINT('Ctrl Pts',(-2.16419442958846,0.926958432495279,
24.8254590760529));
#27629=CARTESIAN_POINT('Ctrl Pts',(-1.95106777785804,-1.31769647143789,
24.9526150734696));
#27630=CARTESIAN_POINT('Ctrl Pts',(0.0515320132559884,-2.35379139182843,
25.0797710708864));
#27631=CARTESIAN_POINT('Ctrl Pts',(2.00686786275484,-1.23104461579491,25.2069270683031));
#27632=CARTESIAN_POINT('Ctrl Pts',(2.12155205706895,1.02078711481988,25.3340830657199));
#27633=CARTESIAN_POINT('Ctrl Pts',(0.290398970375423,2.33637708913623,25.4612390631366));
#27634=CARTESIAN_POINT('Ctrl Pts',(-1.8071011715506,1.50909735286238,25.5883950605534));
#27635=CARTESIAN_POINT('Ctrl Pts',(-2.24717093441076,-0.702290720553313,
25.7155510579701));
#27636=CARTESIAN_POINT('Ctrl Pts',(-0.626188758241757,-2.26955438438638,
25.8427070553868));
#27637=CARTESIAN_POINT('Ctrl Pts',(1.56911891075444,-1.75523653920166,25.9698630528035));
#27638=CARTESIAN_POINT('Ctrl Pts',(2.3252678917954,0.368942673082406,26.0970190502203));
#27639=CARTESIAN_POINT('Ctrl Pts',(0.948736254837979,2.15473640693979,26.224175047637));
#27640=CARTESIAN_POINT('Ctrl Pts',(-1.2979537967368,1.96425696032171,26.3513310450538));
#27641=CARTESIAN_POINT('Ctrl Pts',(-2.35419137824343,-0.0277924313455661,
26.4784870424705));
#27642=CARTESIAN_POINT('Ctrl Pts',(-1.25122040526302,-1.9943512634662,26.6056430398872));
#27643=CARTESIAN_POINT('Ctrl Pts',(0.999340278375681,-2.13173836871502,
26.7327990373039));
#27644=CARTESIAN_POINT('Ctrl Pts',(2.33332973596469,-0.313945549257759,
26.8599550347207));
#27645=CARTESIAN_POINT('Ctrl Pts',(1.52724444309176,1.79179068969598,26.9871110321374));
#27646=CARTESIAN_POINT('Ctrl Pts',(-0.679593268124104,2.25413896079106,
27.1142670295542));
#27647=CARTESIAN_POINT('Ctrl Pts',(-2.26312413535676,0.649044384153771,
27.2414230269709));
#27648=CARTESIAN_POINT('Ctrl Pts',(-1.77097116563029,-1.55133832388099,
27.3685790243877));
#27649=CARTESIAN_POINT('Ctrl Pts',(0.345474597756808,-2.32887027696704,
27.4957350218043));
#27650=CARTESIAN_POINT('Ctrl Pts',(2.14505924537894,-0.970417589726265,
27.6228910192211));
#27651=CARTESIAN_POINT('Ctrl Pts',(1.97724637582914,1.27807911879756,27.7500470166378));
#27652=CARTESIAN_POINT('Ctrl Pts',(-0.00405002291626669,2.3543519409702,
27.8772030140546));
#27653=CARTESIAN_POINT('Ctrl Pts',(-1.9816318365997,1.27126894432701,28.0043590114713));
#27654=CARTESIAN_POINT('Ctrl Pts',(-2.14170788037307,-0.977791807995794,
28.131515008888));
#27655=CARTESIAN_POINT('Ctrl Pts',(-0.33746019955431,-2.33004508075543,
28.2586710063048));
#27656=CARTESIAN_POINT('Ctrl Pts',(1.77629798088247,-1.54523621098804,28.3858270037215));
#27657=CARTESIAN_POINT('Ctrl Pts',(2.26087773891706,0.65682670035945,28.5129830011383));
#27658=CARTESIAN_POINT('Ctrl Pts',(0.671834001583367,2.2564637242713,28.640138998555));
#27659=CARTESIAN_POINT('Ctrl Pts',(-1.53339996430195,1.78652568246711,28.7672949959717));
#27660=CARTESIAN_POINT('Ctrl Pts',(-2.33223581363256,-0.321971387308704,
28.8944509933885));
#27661=CARTESIAN_POINT('Ctrl Pts',(-0.992000232146069,-2.13516392908319,
29.0216069908052));
#27662=CARTESIAN_POINT('Ctrl Pts',(1.25807445889537,-1.99003470334338,29.148762988222));
#27663=CARTESIAN_POINT('Ctrl Pts',(2.35427306367935,-0.0196927974045315,
29.2759189856387));
#27664=CARTESIAN_POINT('Ctrl Pts',(1.29118819402983,1.96871087573412,29.4030749830554));
#27665=CARTESIAN_POINT('Ctrl Pts',(-0.956143895181802,2.1514595781335,29.5302309804722));
#27666=CARTESIAN_POINT('Ctrl Pts',(-2.32652345756126,0.360940529800938,
29.6573869778889));
#27667=CARTESIAN_POINT('Ctrl Pts',(-1.5630708267699,-1.76062462073453,29.7845429753057));
#27668=CARTESIAN_POINT('Ctrl Pts',(0.633993332642798,-2.2673865834481,29.9116989727223));
#27669=CARTESIAN_POINT('Ctrl Pts',(2.24957382850068,-0.694555292802842,
30.0388549701391));
#27670=CARTESIAN_POINT('Ctrl Pts',(1.80189850780172,1.51530565636686,30.1660109675558));
#27671=CARTESIAN_POINT('Ctrl Pts',(-0.298435432038931,2.33536415951361,
30.2931669649726));
#27672=CARTESIAN_POINT('Ctrl Pts',(-2.12505146441632,1.0134819871199,30.4203229623893));
#27673=CARTESIAN_POINT('Ctrl Pts',(-2.00262064227849,-1.23794185152384,
30.547478959806));
#27674=CARTESIAN_POINT('Ctrl Pts',(-0.0434336149472678,-2.35395475439451,
30.6746349572228));
#27675=CARTESIAN_POINT('Ctrl Pts',(1.95558969494388,-1.31097612855999,30.8017909546395));
#27676=CARTESIAN_POINT('Ctrl Pts',(2.16099247023974,0.934398741542428,30.9289469520563));
#27677=CARTESIAN_POINT('Ctrl Pts',(0.384384152021792,2.32276522454689,31.056102949473));
#27678=CARTESIAN_POINT('Ctrl Pts',(-1.74477220324497,1.58074647661569,31.1832589468898));
#27679=CARTESIAN_POINT('Ctrl Pts',(-2.2736648324357,-0.611095487107494,
31.3104149443064));
#27680=CARTESIAN_POINT('Ctrl Pts',(-0.717205947018836,-2.24245514883759,
31.4375709417232));
#27681=CARTESIAN_POINT('Ctrl Pts',(1.49705724025751,-1.81708807804335,31.5647269391399));
#27682=CARTESIAN_POINT('Ctrl Pts',(2.33825499650753,0.274869125275902,31.6918829365567));
#27683=CARTESIAN_POINT('Ctrl Pts',(1.03486066982954,2.11472288040308,31.8190389339733));
#27684=CARTESIAN_POINT('Ctrl Pts',(-1.21768334399615,2.01500291153206,31.9461949313902));
#27685=CARTESIAN_POINT('Ctrl Pts',(-2.35339704585751,0.0671700173426187,
32.0733509288068));
#27686=CARTESIAN_POINT('Ctrl Pts',(-1.33063073475968,-1.94226963266362,
32.2005069262237));
#27687=CARTESIAN_POINT('Ctrl Pts',(0.912558557239173,-2.17030557956596,
32.3276629236403));
#27688=CARTESIAN_POINT('Ctrl Pts',(2.31877076648926,-0.407788696506587,
32.4548189210572));
#27689=CARTESIAN_POINT('Ctrl Pts',(1.59826135801109,1.72874236832532,32.5819749184737));
#27690=CARTESIAN_POINT('Ctrl Pts',(-0.588135483178816,2.27971179455285,
32.7091309158906));
#27691=CARTESIAN_POINT('Ctrl Pts',(-2.23510842700854,0.739783761350988,
32.8362869133073));
#27692=CARTESIAN_POINT('Ctrl Pts',(-1.83209281455498,-1.47865676388438,
32.963442910724));
#27693=CARTESIAN_POINT('Ctrl Pts',(0.251274799212049,-2.34090766448235,
33.0905989081408));
#27694=CARTESIAN_POINT('Ctrl Pts',(2.10417935049844,-1.05613480412643,33.2177549055575));
#27695=CARTESIAN_POINT('Ctrl Pts',(2.02718001724375,1.19730232763188,33.3449109029743));
#27696=CARTESIAN_POINT('Ctrl Pts',(0.0909000378197398,2.35259745701308,
33.4720669003909));
#27697=CARTESIAN_POINT('Ctrl Pts',(-1.92875289630088,1.35015485239774,33.5992228978078));
#27698=CARTESIAN_POINT('Ctrl Pts',(-2.17939633307122,-0.890634789104744,
33.7263788952244));
#27699=CARTESIAN_POINT('Ctrl Pts',(-0.43115488299765,-2.31452289945943,
33.8535348926412));
#27700=CARTESIAN_POINT('Ctrl Pts',(1.71254265687404,-1.61564722812947,33.9806908900579));
#27701=CARTESIAN_POINT('Ctrl Pts',(2.28551558525492,0.56517960272398,34.1078468874747));
#27702=CARTESIAN_POINT('Ctrl Pts',(0.762307926725003,2.22741248100854,34.2350028848914));
#27703=CARTESIAN_POINT('Ctrl Pts',(-1.4601470665852,1.8471437087484,34.3621588823081));
#27704=CARTESIAN_POINT('Ctrl Pts',(-2.34324378646556,-0.228098537668562,
34.4893148797248));
#27705=CARTESIAN_POINT('Ctrl Pts',(-1.07745110930829,-2.09257290386258,
34.6164708771416));
#27706=CARTESIAN_POINT('Ctrl Pts',(1.17708439401579,-2.04079654697071,34.7436268745583));
#27707=CARTESIAN_POINT('Ctrl Pts',(2.35117936578161,-0.110982933612702,
34.8708003673951));
#27708=CARTESIAN_POINT('Ctrl Pts',(1.69716715890499,1.23460437476058,34.9555885277595));
#27709=CARTESIAN_POINT('Ctrl Pts',(1.15760455782972,1.6201078652314,34.9979913556517));
#27710=CARTESIAN_POINT('Ctrl Pts',(-0.940860907222522,1.92803476961866,
4.82379972005017));
#27711=CARTESIAN_POINT('Ctrl Pts',(-1.58281548406976,1.61477906238341,4.86619281462993));
#27712=CARTESIAN_POINT('Ctrl Pts',(-2.51789878139056,0.302100165074653,
4.95097124168192));
#27713=CARTESIAN_POINT('Ctrl Pts',(-1.6153773455708,-1.95798749074765,5.07813500120616));
#27714=CARTESIAN_POINT('Ctrl Pts',(0.770818542691949,-2.41592098549706,
5.2052909986229));
#27715=CARTESIAN_POINT('Ctrl Pts',(2.44893709210338,-0.661129782966532,
5.33244699603964));
#27716=CARTESIAN_POINT('Ctrl Pts',(1.88152327214964,1.70164314936676,5.45960299345635));
#27717=CARTESIAN_POINT('Ctrl Pts',(-0.41188023327182,2.50286729587259,5.58675899087311));
#27718=CARTESIAN_POINT('Ctrl Pts',(-2.32735905164794,1.00896224840214,5.71391498828984));
#27719=CARTESIAN_POINT('Ctrl Pts',(-2.10832209870648,-1.41057054174251,
5.84107098570658));
#27720=CARTESIAN_POINT('Ctrl Pts',(0.044461361955423,-2.53624005146705,
5.96822698312332));
#27721=CARTESIAN_POINT('Ctrl Pts',(2.15644313623853,-1.3357939482761,6.09538298054004));
#27722=CARTESIAN_POINT('Ctrl Pts',(2.29059830525902,1.08984410967345,6.2225389779568));
#27723=CARTESIAN_POINT('Ctrl Pts',(0.323864713742656,2.51588545724566,6.34969497537351));
#27724=CARTESIAN_POINT('Ctrl Pts',(-1.93990663359876,1.63442545808399,6.47685097279027));
#27725=CARTESIAN_POINT('Ctrl Pts',(-2.4244433022373,-0.746095664807696,
6.60400697020699));
#27726=CARTESIAN_POINT('Ctrl Pts',(-0.685337112179472,-2.44231299424555,
6.73116296762373));
#27727=CARTESIAN_POINT('Ctrl Pts',(1.68234356541504,-1.8985000361444,6.85831896504046));
#27728=CARTESIAN_POINT('Ctrl Pts',(2.50701883308963,0.386572869208354,6.98547496245721));
#27729=CARTESIAN_POINT('Ctrl Pts',(1.0323156951975,2.31708993340106,7.11263095987393));
#27730=CARTESIAN_POINT('Ctrl Pts',(-1.38920287136656,2.12242720047753,7.23978695729069));
#27731=CARTESIAN_POINT('Ctrl Pts',(-2.53657751444396,-0.0188755745349083,
7.36694295470739));
#27732=CARTESIAN_POINT('Ctrl Pts',(-1.35746334135277,-2.14286606720562,
7.49409895212416));
#27733=CARTESIAN_POINT('Ctrl Pts',(1.06668403630552,-2.30147060134743,7.62125494954088));
#27734=CARTESIAN_POINT('Ctrl Pts',(2.51249409388617,-0.349220813994871,
7.74841094695762));
#27735=CARTESIAN_POINT('Ctrl Pts',(1.65390409412917,1.92332602230935,7.87556694437436));
#27736=CARTESIAN_POINT('Ctrl Pts',(-0.721607553543116,2.43184380411619,
8.00272294179109));
#27737=CARTESIAN_POINT('Ctrl Pts',(-2.4352778508332,0.709932064149893,8.12987893920782));
#27738=CARTESIAN_POINT('Ctrl Pts',(-1.91536900175952,-1.66311254360542,
8.25703493662456));
#27739=CARTESIAN_POINT('Ctrl Pts',(0.361270914862585,-2.51078973091116,
8.3841909340413));
#27740=CARTESIAN_POINT('Ctrl Pts',(2.30656170803872,-1.05563006463211,8.51134693145805));
#27741=CARTESIAN_POINT('Ctrl Pts',(2.13632875169771,1.36772848582442,8.63850292887476));
#27742=CARTESIAN_POINT('Ctrl Pts',(0.00670568016803455,2.5366388746297,
8.76565892629152));
#27743=CARTESIAN_POINT('Ctrl Pts',(-2.12906768235024,1.3790041879306,8.89281492370824));
#27744=CARTESIAN_POINT('Ctrl Pts',(-2.31211061041173,-1.04342046729742,
9.01997092112498));
#27745=CARTESIAN_POINT('Ctrl Pts',(-0.374540467229969,-2.5088445915965,
9.14712691854171));
#27746=CARTESIAN_POINT('Ctrl Pts',(1.90654931854483,-1.67321589829907,9.27428291595846));
#27747=CARTESIAN_POINT('Ctrl Pts',(2.4389972410452,0.697046773565979,9.40143891337518));
#27748=CARTESIAN_POINT('Ctrl Pts',(0.734454680994803,2.42799465978255,9.52859491079192));
#27749=CARTESIAN_POINT('Ctrl Pts',(-1.64371231109775,1.9320433702978,9.65575090820866));
#27750=CARTESIAN_POINT('Ctrl Pts',(-2.51430531577452,-0.33593232269935,
9.7829069056254));
#27751=CARTESIAN_POINT('Ctrl Pts',(-1.07883705602549,-2.29579884853026,
9.91006290304212));
#27752=CARTESIAN_POINT('Ctrl Pts',(1.34611499072393,-2.15001306463813,10.0372189004589));
#27753=CARTESIAN_POINT('Ctrl Pts',(2.53644226135888,-0.0322862379199884,
10.1643748978756));
#27754=CARTESIAN_POINT('Ctrl Pts',(1.40040478556657,2.11505276126358,10.2915308952924));
#27755=CARTESIAN_POINT('Ctrl Pts',(-1.0200507798868,2.32251547956493,10.4186868927091));
#27756=CARTESIAN_POINT('Ctrl Pts',(-2.50493993799644,0.399822027153037,
10.5458428901259));
#27757=CARTESIAN_POINT('Ctrl Pts',(-1.69235753428521,-1.88957871561744,
10.6729988875426));
#27758=CARTESIAN_POINT('Ctrl Pts',(0.672415103002414,-2.44590263003674,
10.8001548849593));
#27759=CARTESIAN_POINT('Ctrl Pts',(2.42046453928486,-0.758902602730359,
10.927310882376));
#27760=CARTESIAN_POINT('Ctrl Pts',(1.94852124797693,1.62414491119137,11.0544668797928));
#27761=CARTESIAN_POINT('Ctrl Pts',(-0.31055956584235,2.51756519328303,11.1816228772095));
#27762=CARTESIAN_POINT('Ctrl Pts',(-2.28480250393,1.10193432853396,11.3087788746263));
#27763=CARTESIAN_POINT('Ctrl Pts',(-2.16347871902673,-1.32436459431867,
11.435934872043));
#27764=CARTESIAN_POINT('Ctrl Pts',(-0.0578635121326518,-2.53598768930965,
11.5630908694597));
#27765=CARTESIAN_POINT('Ctrl Pts',(2.10082273713468,-1.42166296058678,11.6902468668765));
#27766=CARTESIAN_POINT('Ctrl Pts',(2.33268414650022,0.996577352257691,11.8174028642932));
#27767=CARTESIAN_POINT('Ctrl Pts',(0.425062924764753,2.50078052942613,11.94455886171));
#27768=CARTESIAN_POINT('Ctrl Pts',(-1.87241594058851,1.71132705576591,12.0717148591266));
#27769=CARTESIAN_POINT('Ctrl Pts',(-2.4525592682111,-0.647715047129689,
12.1988708565434));
#27770=CARTESIAN_POINT('Ctrl Pts',(-0.783273343289587,-2.41268825505044,
12.3260268539601));
#27771=CARTESIAN_POINT('Ctrl Pts',(1.60441233407452,-1.96480095903783,12.4531828513769));
#27772=CARTESIAN_POINT('Ctrl Pts',(2.52056903181798,0.285155224757529,12.5803388487936));
#27773=CARTESIAN_POINT('Ctrl Pts',(1.12491953318614,2.27357379256154,12.7074948462104));
#27774=CARTESIAN_POINT('Ctrl Pts',(-1.30247950866994,2.17672434540097,12.8346508436271));
#27775=CARTESIAN_POINT('Ctrl Pts',(-2.53527520470006,0.083434901566532,
12.9618068410438));
#27776=CARTESIAN_POINT('Ctrl Pts',(-1.44277655101942,-2.08637905716934,
13.0889628384605));
#27777=CARTESIAN_POINT('Ctrl Pts',(0.973002571685308,-2.34261557705487,
13.2161188358773));
#27778=CARTESIAN_POINT('Ctrl Pts',(2.4963667888999,-0.450260593039129,13.343274833294));
#27779=CARTESIAN_POINT('Ctrl Pts',(1.73012253352216,1.85506273892967,13.4704308307108));
#27780=CARTESIAN_POINT('Ctrl Pts',(-0.622949117969492,2.45896647858148,
13.5975868281275));
#27781=CARTESIAN_POINT('Ctrl Pts',(-2.40466659793517,0.807564424142928,
13.7247428255442));
#27782=CARTESIAN_POINT('Ctrl Pts',(-1.98088084781725,-1.58451658657056,
13.851898822961));
#27783=CARTESIAN_POINT('Ctrl Pts',(0.259721883092581,-2.52331652588598,
13.9790548203777));
#27784=CARTESIAN_POINT('Ctrl Pts',(2.26211385639636,-1.14779033236301,14.1062108177944));
#27785=CARTESIAN_POINT('Ctrl Pts',(2.18974859666703,1.28046195951349,14.2333668152112));
#27786=CARTESIAN_POINT('Ctrl Pts',(0.108997805584984,2.53430487999057,14.3605228126279));
#27787=CARTESIAN_POINT('Ctrl Pts',(-2.07172319030473,1.46374340959063,14.4876788100447));
#27788=CARTESIAN_POINT('Ctrl Pts',(-2.35230876119222,-0.949328835749087,
14.6148348074614));
#27789=CARTESIAN_POINT('Ctrl Pts',(-0.475412469347375,-2.49169916529974,
14.7419908048781));
#27790=CARTESIAN_POINT('Ctrl Pts',(1.83752087547937,-1.74874205603454,14.8691468022949));
#27791=CARTESIAN_POINT('Ctrl Pts',(2.465123609528,0.598119834242293,14.9963027997116));
#27792=CARTESIAN_POINT('Ctrl Pts',(0.831773374862453,2.39640038374982,15.1234587971283));
#27793=CARTESIAN_POINT('Ctrl Pts',(-1.56445969209756,1.9967592789739,15.2506147945451));
#27794=CARTESIAN_POINT('Ctrl Pts',(-2.52580739606398,-0.234262127444595,
15.3777707919618));
#27795=CARTESIAN_POINT('Ctrl Pts',(-1.17054440008075,-2.25042386092176,
15.5049267893785));
#27796=CARTESIAN_POINT('Ctrl Pts',(1.25831418605672,-2.20255014824516,15.6320827867953));
#27797=CARTESIAN_POINT('Ctrl Pts',(2.53307681386418,-0.134549624414361,
15.759238784212));
#27798=CARTESIAN_POINT('Ctrl Pts',(1.48456140394928,2.05685662705754,15.8863947816287));
#27799=CARTESIAN_POINT('Ctrl Pts',(-0.925558552092357,2.36176271310543,
16.0135507790455));
#27800=CARTESIAN_POINT('Ctrl Pts',(-2.48677813332775,0.500515995717766,
16.1407067764622));
#27801=CARTESIAN_POINT('Ctrl Pts',(-1.76718372967845,-1.81979213426318,
16.267862773879));
#27802=CARTESIAN_POINT('Ctrl Pts',(0.573229721111829,-2.47103003486409,
16.3950187712957));
#27803=CARTESIAN_POINT('Ctrl Pts',(2.38789045317691,-0.855897733372941,
16.5221747687124));
#27804=CARTESIAN_POINT('Ctrl Pts',(2.01243463765503,1.54424369046231,16.6493307661292));
#27805=CARTESIAN_POINT('Ctrl Pts',(-0.208778547096946,2.52804138902797,
16.7764867635459));
#27806=CARTESIAN_POINT('Ctrl Pts',(-2.23850499502235,1.19317942222719,16.9036427609626));
#27807=CARTESIAN_POINT('Ctrl Pts',(-2.21512769820434,-1.23603844075105,
17.0307987583794));
#27808=CARTESIAN_POINT('Ctrl Pts',(-0.160087759408297,-2.53159113121649,
17.1579547557961));
#27809=CARTESIAN_POINT('Ctrl Pts',(2.04178087937262,-1.50522841688388,17.2851107532128));
#27810=CARTESIAN_POINT('Ctrl Pts',(2.37097647131784,0.901694138177437,17.4122667506296));
#27811=CARTESIAN_POINT('Ctrl Pts',(0.525568619095842,2.48160419345794,17.5394227480463));
#27812=CARTESIAN_POINT('Ctrl Pts',(-1.80187831831236,1.78544567891668,17.6665787454631));
#27813=CARTESIAN_POINT('Ctrl Pts',(-2.47668515390022,-0.548281309928203,
17.7937347428798));
#27814=CARTESIAN_POINT('Ctrl Pts',(-0.879935046202314,-2.37913767168513,
17.9208907402965));
#27815=CARTESIAN_POINT('Ctrl Pts',(1.52387063765299,-2.0279053296605,18.0480467377133));
#27816=CARTESIAN_POINT('Ctrl Pts',(2.53001827757856,0.183273733755983,18.17520273513));
#27817=CARTESIAN_POINT('Ctrl Pts',(1.21569309679729,2.22635847085903,18.3023587325467));
#27818=CARTESIAN_POINT('Ctrl Pts',(-1.21363698906272,2.2274799673948,18.4295147299635));
#27819=CARTESIAN_POINT('Ctrl Pts',(-2.52984798314295,0.185609613312194,
18.5566707273802));
#27820=CARTESIAN_POINT('Ctrl Pts',(-1.52574234653794,-2.02649748046901,
18.6838267247969));
#27821=CARTESIAN_POINT('Ctrl Pts',(0.877738021039851,-2.37994909878077,
18.8109827222137));
#27822=CARTESIAN_POINT('Ctrl Pts',(2.47617787188537,-0.550567791603931,
18.9381387196304));
#27823=CARTESIAN_POINT('Ctrl Pts',(1.80352604649014,1.78378124948045,19.0652947170472));
#27824=CARTESIAN_POINT('Ctrl Pts',(-0.523277137970608,2.48208839150496,
19.1924507144639));
#27825=CARTESIAN_POINT('Ctrl Pts',(-2.37014292944138,0.903882868731024,
19.3196067118806));
#27826=CARTESIAN_POINT('Ctrl Pts',(-2.04316978160497,-1.50334260563009,
19.4467627092973));
#27827=CARTESIAN_POINT('Ctrl Pts',(0.157750281287492,-2.53173786066411,
19.5739187067141));
#27828=CARTESIAN_POINT('Ctrl Pts',(2.21398552374585,-1.23808313412719,19.7010747041308));
#27829=CARTESIAN_POINT('Ctrl Pts',(2.23960569957805,1.1911121092424,19.8282307015476));
#27830=CARTESIAN_POINT('Ctrl Pts',(0.211112590527258,2.52784754692352,19.9553866989643));
#27831=CARTESIAN_POINT('Ctrl Pts',(-2.01100798468413,1.54610110662371,20.082542696381));
#27832=CARTESIAN_POINT('Ctrl Pts',(-2.38867968296877,-0.853692637041341,
20.2096986937978));
#27833=CARTESIAN_POINT('Ctrl Pts',(-0.575510970800485,-2.47049972047249,
20.3368546912145));
#27834=CARTESIAN_POINT('Ctrl Pts',(1.76550276825797,-1.82142299360686,20.4640106886313));
#27835=CARTESIAN_POINT('Ctrl Pts',(2.48723919816346,0.498219748189033,20.591166686048));
#27836=CARTESIAN_POINT('Ctrl Pts',(0.927738765440914,2.36090714122021,20.7183226834647));
#27837=CARTESIAN_POINT('Ctrl Pts',(-1.48266168211557,2.058226441078,20.8454786808814));
#27838=CARTESIAN_POINT('Ctrl Pts',(-2.5331999634013,-0.132210785452896,
20.9726346782982));
#27839=CARTESIAN_POINT('Ctrl Pts',(-1.26034725712697,-2.20138741202427,
21.0997906757149));
#27840=CARTESIAN_POINT('Ctrl Pts',(1.1684660920936,-2.25150366155463,21.2269466731317));
#27841=CARTESIAN_POINT('Ctrl Pts',(2.52559002600461,-0.236594097374377,
21.3541026705484));
#27842=CARTESIAN_POINT('Ctrl Pts',(1.56630262663429,1.99531396731565,21.4812586679652));
#27843=CARTESIAN_POINT('Ctrl Pts',(-0.829560431622247,2.39716733597241,
21.6084146653818));
#27844=CARTESIAN_POINT('Ctrl Pts',(-2.46457031669317,0.600395619938505,
21.7355706627986));
#27845=CARTESIAN_POINT('Ctrl Pts',(-1.8391347001289,-1.74704473358531,21.8627266602153));
#27846=CARTESIAN_POINT('Ctrl Pts',(0.473111688945822,-2.49213705003341,
21.9898826576321));
#27847=CARTESIAN_POINT('Ctrl Pts',(2.35143124631078,-0.9515003101627,22.1170386550488));
#27848=CARTESIAN_POINT('Ctrl Pts',(2.07307377680177,1.46182997038069,22.2441946524656));
#27849=CARTESIAN_POINT('Ctrl Pts',(-0.106657843645223,2.53440443709273,
22.3713506498822));
#27850=CARTESIAN_POINT('Ctrl Pts',(-2.18856541693521,1.28248320151244,22.4985066472991));
#27851=CARTESIAN_POINT('Ctrl Pts',(-2.26317264328954,-1.1457012407396,22.6256626447157));
#27852=CARTESIAN_POINT('Ctrl Pts',(-0.262051542358103,-2.52307564997844,
22.7528186421325));
#27853=CARTESIAN_POINT('Ctrl Pts',(1.97941702446132,-1.58634485205427,22.8799746395492));
#27854=CARTESIAN_POINT('Ctrl Pts',(2.40541119458867,0.805343859052706,23.007130636966));
#27855=CARTESIAN_POINT('Ctrl Pts',(0.625219208223486,2.45839026357387,23.1342866343827));
#27856=CARTESIAN_POINT('Ctrl Pts',(-1.72840902266361,1.85665936475742,23.2614426317994));
#27857=CARTESIAN_POINT('Ctrl Pts',(-2.49678144899819,-0.447955513756536,
23.3885986292162));
#27858=CARTESIAN_POINT('Ctrl Pts',(-0.975165086322767,-2.3417162084214,
23.5157546266329));
#27859=CARTESIAN_POINT('Ctrl Pts',(1.440849589032,-2.08771027878695,23.6429106240497));
#27860=CARTESIAN_POINT('Ctrl Pts',(2.53535115924222,0.0810940546250112,
23.7700666214663));
#27861=CARTESIAN_POINT('Ctrl Pts',(1.30448871603519,2.17552084248882,23.8972226188832));
#27862=CARTESIAN_POINT('Ctrl Pts',(-1.12281987038924,2.2746114580353,24.0243786162998));
#27863=CARTESIAN_POINT('Ctrl Pts',(-2.52030467455963,0.287482336429987,
24.1515346137166));
#27864=CARTESIAN_POINT('Ctrl Pts',(-1.60622574456868,-1.9633187728566,24.2786906111333));
#27865=CARTESIAN_POINT('Ctrl Pts',(0.781045382183157,-2.41341042040858,
24.4058466085501));
#27866=CARTESIAN_POINT('Ctrl Pts',(2.45196018963237,-0.649979211070922,
24.5330026059668));
#27867=CARTESIAN_POINT('Ctrl Pts',(1.87399520521599,1.70959753076386,24.6601586033835));
#27868=CARTESIAN_POINT('Ctrl Pts',(-0.42275378103003,2.50117192271767,24.7873146008003));
#27869=CARTESIAN_POINT('Ctrl Pts',(-2.33176301558138,0.998730687189076,
24.914470598217));
#27870=CARTESIAN_POINT('Ctrl Pts',(-2.10213445848623,-1.41972267179587,
25.0416265956337));
#27871=CARTESIAN_POINT('Ctrl Pts',(0.0555220182558873,-2.53604003356715,
25.1687825930505));
#27872=CARTESIAN_POINT('Ctrl Pts',(2.16225501533173,-1.32636156271175,25.2959385904672));
#27873=CARTESIAN_POINT('Ctrl Pts',(2.2858189424527,1.09982430810144,25.4230945878839));
#27874=CARTESIAN_POINT('Ctrl Pts',(0.312883893252119,2.51727738155925,25.5502505853007));
#27875=CARTESIAN_POINT('Ctrl Pts',(-1.94702084971026,1.6259432822703,25.6774065827174));
#27876=CARTESIAN_POINT('Ctrl Pts',(-2.42116419990269,-0.756667472193677,
25.8045625801342));
#27877=CARTESIAN_POINT('Ctrl Pts',(-0.674673110363047,-2.44528074881381,
25.9317185775509));
#27878=CARTESIAN_POINT('Ctrl Pts',(1.69061217103417,-1.89114045843176,26.0588745749677));
#27879=CARTESIAN_POINT('Ctrl Pts',(2.50530802467614,0.397509053808538,26.1860305723843));
#27880=CARTESIAN_POINT('Ctrl Pts',(1.02219471611566,2.32157268004076,26.3131865698011));
#27881=CARTESIAN_POINT('Ctrl Pts',(-1.39845136730157,2.11634484894564,26.4403425672178));
#27882=CARTESIAN_POINT('Ctrl Pts',(-2.53647099000825,-0.0299443352403086,
26.5674985646346));
#27883=CARTESIAN_POINT('Ctrl Pts',(-1.34809951705112,-2.14876928461222,
26.6946545620513));
#27884=CARTESIAN_POINT('Ctrl Pts',(1.07671689254853,-2.29679395672904,26.8218105594681));
#27885=CARTESIAN_POINT('Ctrl Pts',(2.5139940788561,-0.338253629460036,26.9489665568847));
#27886=CARTESIAN_POINT('Ctrl Pts',(1.64549545986523,1.93052491253787,27.0761225543016));
#27887=CARTESIAN_POINT('Ctrl Pts',(-0.732212608342833,2.4286717445036,27.2032785517182));
#27888=CARTESIAN_POINT('Ctrl Pts',(-2.4383526204242,0.699298394704866,27.330434549135));
#27889=CARTESIAN_POINT('Ctrl Pts',(-1.90809338071484,-1.6714548743052,27.4575905465517));
#27890=CARTESIAN_POINT('Ctrl Pts',(0.372223899506801,-2.50918933422776,
27.5847465439684));
#27891=CARTESIAN_POINT('Ctrl Pts',(2.31114623816709,-1.04555478678664,27.7119025413852));
#27892=CARTESIAN_POINT('Ctrl Pts',(2.13034000495386,1.37703783886266,27.8390585388019));
#27893=CARTESIAN_POINT('Ctrl Pts',(-0.00436360685501822,2.53664398473684,
27.9662145362187));
#27894=CARTESIAN_POINT('Ctrl Pts',(-2.13506502184302,1.3697003682809,28.0933705336354));
#27895=CARTESIAN_POINT('Ctrl Pts',(-2.30753538469401,-1.05349997377856,
28.2205265310522));
#27896=CARTESIAN_POINT('Ctrl Pts',(-0.363588964925368,-2.51045510036544,
28.3476825284689));
#27897=CARTESIAN_POINT('Ctrl Pts',(1.91383263899322,-1.66488028887685,28.4748385258856));
#27898=CARTESIAN_POINT('Ctrl Pts',(2.43593229068633,0.707683277715432,28.6019945233023));
#27899=CARTESIAN_POINT('Ctrl Pts',(0.723852559679631,2.43117650906132,28.7291505207191));
#27900=CARTESIAN_POINT('Ctrl Pts',(-1.65212758889371,1.92485224793558,28.8563065181358));
#27901=CARTESIAN_POINT('Ctrl Pts',(-2.51281545663937,-0.34690088965101,
28.9834625155526));
#27902=CARTESIAN_POINT('Ctrl Pts',(-1.06880852345881,-2.30048475034028,
29.1106185129693));
#27903=CARTESIAN_POINT('Ctrl Pts',(1.35548426425704,-2.14411850318913,29.2377745103861));
#27904=CARTESIAN_POINT('Ctrl Pts',(2.53655900015918,-0.0212175653135828,
29.3649305078028));
#27905=CARTESIAN_POINT('Ctrl Pts',(1.39116191957229,2.12114362076176,29.4920865052195));
#27906=CARTESIAN_POINT('Ctrl Pts',(-1.03017591297604,2.31804213393337,29.6192425026363));
#27907=CARTESIAN_POINT('Ctrl Pts',(-2.50666080600506,0.388887323018423,
29.746398500053));
#27908=CARTESIAN_POINT('Ctrl Pts',(-1.68409579784808,-1.89694572669772,
29.8735544974697));
#27909=CARTESIAN_POINT('Ctrl Pts',(0.683081974969736,-2.44294510004585,
30.0007104948864));
#27910=CARTESIAN_POINT('Ctrl Pts',(2.42375314454311,-0.74833310810332,30.1278664923032));
#27911=CARTESIAN_POINT('Ctrl Pts',(1.94141535569991,1.63263228040444,30.2550224897199));
#27912=CARTESIAN_POINT('Ctrl Pts',(-0.321542599617489,2.51618602313084,
30.3821784871367));
#27913=CARTESIAN_POINT('Ctrl Pts',(-2.28958930084453,1.09195356120261,30.5093344845534));
#27914=CARTESIAN_POINT('Ctrl Pts',(-2.15767894236412,-1.33379283550446,
30.6364904819702));
#27915=CARTESIAN_POINT('Ctrl Pts',(-0.0467965796336351,-2.53621604492014,
30.7636464793869));
#27916=CARTESIAN_POINT('Ctrl Pts',(2.1070064971886,-1.4124819882599,30.8908024768036));
#27917=CARTESIAN_POINT('Ctrl Pts',(2.3283131359011,1.00674708221518,31.0179584742203));
#27918=CARTESIAN_POINT('Ctrl Pts',(0.414146130867886,2.50261158167149,31.1451144716371));
#27919=CARTESIAN_POINT('Ctrl Pts',(-1.8798658930634,1.70314003251725,31.2722704690538));
#27920=CARTESIAN_POINT('Ctrl Pts',(-2.44970945938055,-0.658411202036514,
31.3994264664706));
#27921=CARTESIAN_POINT('Ctrl Pts',(-0.772737550263181,-2.416083281923,31.5265824638873));
#27922=CARTESIAN_POINT('Ctrl Pts',(1.61297093150021,-1.95778101935183,31.653738461304));
#27923=CARTESIAN_POINT('Ctrl Pts',(2.51930069096952,0.296151608044552,31.7808944587208));
#27924=CARTESIAN_POINT('Ctrl Pts',(1.11498754603441,2.27846099837959,31.9080504561375));
#27925=CARTESIAN_POINT('Ctrl Pts',(-1.31196575843683,2.17101994218358,32.0352064535542));
#27926=CARTESIAN_POINT('Ctrl Pts',(-2.5356151542967,0.0723708369516123,
32.1623624509709));
#27927=CARTESIAN_POINT('Ctrl Pts',(-1.43365840531175,-2.0926550931901,32.2895184483877));
#27928=CARTESIAN_POINT('Ctrl Pts',(0.983215862785192,-2.33834733781478,
32.4166744458044));
#27929=CARTESIAN_POINT('Ctrl Pts',(2.4983078419341,-0.439362835282259,32.5438304432212));
#27930=CARTESIAN_POINT('Ctrl Pts',(1.72201105080549,1.86259490497632,32.6709864406379));
#27931=CARTESIAN_POINT('Ctrl Pts',(-0.633673457928804,2.45622462383557,
32.7981424380546));
#27932=CARTESIAN_POINT('Ctrl Pts',(-2.40816772035767,0.797063512714892,
32.9252984354714));
#27933=CARTESIAN_POINT('Ctrl Pts',(-1.9739475380241,-1.5931457486565,33.0524544328881));
#27934=CARTESIAN_POINT('Ctrl Pts',(0.270730427700916,-2.52215874891095,
33.1796104303049));
#27935=CARTESIAN_POINT('Ctrl Pts',(2.26710110725835,-1.13790888751085,33.3067664277216));
#27936=CARTESIAN_POINT('Ctrl Pts',(2.18413989312104,1.29000668695582,33.4339224251383));
#27937=CARTESIAN_POINT('Ctrl Pts',(0.0979382182141485,2.53475365513117,
33.5610784225551));
#27938=CARTESIAN_POINT('Ctrl Pts',(-2.07809178708825,1.45469423037344,33.6882344199718));
#27939=CARTESIAN_POINT('Ctrl Pts',(-2.34814196740883,-0.959594587820653,
33.8153904173885));
#27940=CARTESIAN_POINT('Ctrl Pts',(-0.46453821173187,-2.49373107235192,
33.9425464148053));
#27941=CARTESIAN_POINT('Ctrl Pts',(1.84514088720937,-1.74074306877094,34.069702412222));
#27942=CARTESIAN_POINT('Ctrl Pts',(2.46247778867336,0.608940156566012,34.1968584096388));
#27943=CARTESIAN_POINT('Ctrl Pts',(0.821331672293306,2.39987589499884,34.3240144070555));
#27944=CARTESIAN_POINT('Ctrl Pts',(-1.5732028881622,1.99016378826106,34.4511704044722));
#27945=CARTESIAN_POINT('Ctrl Pts',(-2.52467575143432,-0.245759681649779,
34.5783264018889));
#27946=CARTESIAN_POINT('Ctrl Pts',(-1.16087566506667,-2.25459600021353,
34.7054823993057));
#27947=CARTESIAN_POINT('Ctrl Pts',(1.26822332534423,-2.19881071935727,34.8326383967224));
#27948=CARTESIAN_POINT('Ctrl Pts',(2.5332257643645,-0.119576086335227,34.9598118895592));
#27949=CARTESIAN_POINT('Ctrl Pts',(1.82857489987461,1.33019694560863,35.0446000499235));
#27950=CARTESIAN_POINT('Ctrl Pts',(1.24723521034521,1.7455490827215,35.0870028778158));
#27951=CARTESIAN_POINT('Ctrl Pts',(-1.00847443860881,2.06659004214475,4.91281124221424));
#27952=CARTESIAN_POINT('Ctrl Pts',(-1.69656210016283,1.73082269218899,4.955204336794));
#27953=CARTESIAN_POINT('Ctrl Pts',(-2.6988437297629,0.323810131804284,5.03998276384599));
#27954=CARTESIAN_POINT('Ctrl Pts',(-1.73146397008341,-2.09869526980756,
5.16714652337023));
#27955=CARTESIAN_POINT('Ctrl Pts',(0.826212239389695,-2.58953745539779,
5.29430252078697));
#27956=CARTESIAN_POINT('Ctrl Pts',(2.62492621405411,-0.708640864559765,
5.4214585182037));
#27957=CARTESIAN_POINT('Ctrl Pts',(2.01673606698341,1.82392913404815,5.54861451562044));
#27958=CARTESIAN_POINT('Ctrl Pts',(-0.441479376849763,2.68273202950749,
5.67577051303717));
#27959=CARTESIAN_POINT('Ctrl Pts',(-2.49461115350241,1.08146977860786,5.80292651045392));
#27960=CARTESIAN_POINT('Ctrl Pts',(-2.25983344464387,-1.51193903825939,
5.93008250787064));
#27961=CARTESIAN_POINT('Ctrl Pts',(0.0476565097918634,-2.71850306718649,
6.05723850528739));
#27962=CARTESIAN_POINT('Ctrl Pts',(2.3114126270054,-1.43178873916808,6.18439450270412));
#27963=CARTESIAN_POINT('Ctrl Pts',(2.45520865224759,1.16816409124554,6.31155050012086));
#27964=CARTESIAN_POINT('Ctrl Pts',(0.347138756504326,2.69668572115485,6.4387064975376));
#27965=CARTESIAN_POINT('Ctrl Pts',(-2.07931505948866,1.7518809460953,6.56586249495433));
#27966=CARTESIAN_POINT('Ctrl Pts',(-2.59867221540777,-0.799712689664839,
6.69301849237107));
#27967=CARTESIAN_POINT('Ctrl Pts',(-0.734587816495842,-2.61782608552589,
6.8201744897878));
#27968=CARTESIAN_POINT('Ctrl Pts',(1.80324261498706,-2.0349328401808,6.94733048720455));
#27969=CARTESIAN_POINT('Ctrl Pts',(2.68718191060275,0.414353337739565,7.07448648462127));
#27970=CARTESIAN_POINT('Ctrl Pts',(1.10650148517122,2.48360406076476,7.20164248203802));
#27971=CARTESIAN_POINT('Ctrl Pts',(-1.4890358129034,2.27495218799998,7.32879847945475));
#27972=CARTESIAN_POINT('Ctrl Pts',(-2.71886478142456,-0.0202320388555172,
7.45595447687148));
#27973=CARTESIAN_POINT('Ctrl Pts',(-1.45501537006563,-2.2968598626533,7.58311047428822));
#27974=CARTESIAN_POINT('Ctrl Pts',(1.14333965459547,-2.46686226928065,7.71026647170495));
#27975=CARTESIAN_POINT('Ctrl Pts',(2.69305064264981,-0.374317034155005,
7.8374224691217));
#27976=CARTESIAN_POINT('Ctrl Pts',(1.77275938455494,2.06154290790546,7.96457846653843));
#27977=CARTESIAN_POINT('Ctrl Pts',(-0.773464777704037,2.60660454304561,
8.09173446395516));
#27978=CARTESIAN_POINT('Ctrl Pts',(-2.61028537228249,0.760950247106553,
8.21889046137189));
#27979=CARTESIAN_POINT('Ctrl Pts',(-2.0530140682327,-1.78262958518165,8.34604645878863));
#27980=CARTESIAN_POINT('Ctrl Pts',(0.387233097108164,-2.69122379823399,
8.47320245620537));
#27981=CARTESIAN_POINT('Ctrl Pts',(2.47231924057473,-1.13149130613901,8.60035845362211));
#27982=CARTESIAN_POINT('Ctrl Pts',(2.2898527529559,1.46601820345888,8.72751445103884));
#27983=CARTESIAN_POINT('Ctrl Pts',(0.00718757362643308,2.7189305511663,
8.85467044845559));
#27984=CARTESIAN_POINT('Ctrl Pts',(-2.28206987795533,1.47810421666663,8.98182644587231));
#27985=CARTESIAN_POINT('Ctrl Pts',(-2.47826690633756,-1.11840428474922,
9.10898244328906));
#27986=CARTESIAN_POINT('Ctrl Pts',(-0.401456245579368,-2.68913887445482,
9.23613844070579));
#27987=CARTESIAN_POINT('Ctrl Pts',(2.04356057196105,-1.79345900202152,9.36329443812252));
#27988=CARTESIAN_POINT('Ctrl Pts',(2.61427205078852,0.747138974804695,9.49045043553926));
#27989=CARTESIAN_POINT('Ctrl Pts',(0.787235144338485,2.60247878583629,9.61760643295599));
#27990=CARTESIAN_POINT('Ctrl Pts',(-1.76183518460994,2.07088671478621,9.74476243037273));
#27991=CARTESIAN_POINT('Ctrl Pts',(-2.69499202523146,-0.360073585738528,
9.87191842778947));
#27992=CARTESIAN_POINT('Ctrl Pts',(-1.15636603250672,-2.4607829246142,9.9990744252062));
#27993=CARTESIAN_POINT('Ctrl Pts',(1.44285148756014,-2.30452046813505,10.126230422623));
#27994=CARTESIAN_POINT('Ctrl Pts',(2.71871980858321,-0.0346064390720735,
10.2533864200397));
#27995=CARTESIAN_POINT('Ctrl Pts',(1.50104273554987,2.2670477959807,10.3805424174564));
#27996=CARTESIAN_POINT('Ctrl Pts',(-1.0933551704636,2.48941950551298,10.5076984148732));
#27997=CARTESIAN_POINT('Ctrl Pts',(-2.68495361889042,0.428554626174045,
10.6348544122899));
#27998=CARTESIAN_POINT('Ctrl Pts',(-1.81397622242785,-2.02537040258673,
10.7620104097067));
#27999=CARTESIAN_POINT('Ctrl Pts',(0.720737186875261,-2.62167368500793,
10.8891664071234));
#28000=CARTESIAN_POINT('Ctrl Pts',(2.59440752473566,-0.813439978611172,
11.0163224045401));
#28001=CARTESIAN_POINT('Ctrl Pts',(2.08854874996522,1.74086160340985,11.1434784019569));
#28002=CARTESIAN_POINT('Ctrl Pts',(-0.332877454481621,2.69848616885575,
11.2706343993736));
#28003=CARTESIAN_POINT('Ctrl Pts',(-2.44899634451255,1.18112315520953,11.3977903967903));
#28004=CARTESIAN_POINT('Ctrl Pts',(-2.31895381119968,-1.41953803215357,
11.5249463942071));
#28005=CARTESIAN_POINT('Ctrl Pts',(-0.0620217850118915,-2.71823256940827,
11.6521023916238));
#28006=CARTESIAN_POINT('Ctrl Pts',(2.2517951529124,-1.5238285968337,11.7792583890405));
#28007=CARTESIAN_POINT('Ctrl Pts',(2.50031892815902,1.06819486082722,11.9064143864573));
#28008=CARTESIAN_POINT('Ctrl Pts',(0.455609422322499,2.68049530077911,12.033570383874));
#28009=CARTESIAN_POINT('Ctrl Pts',(-2.00697425095645,1.8343089595828,12.1607263812908));
#28010=CARTESIAN_POINT('Ctrl Pts',(-2.62880869231283,-0.694262099230915,
12.2878823787075));
#28011=CARTESIAN_POINT('Ctrl Pts',(-0.83956208520023,-2.58607240971753,
12.4150383761242));
#28012=CARTESIAN_POINT('Ctrl Pts',(1.71971097479146,-2.1059983775848,12.542194373541));
#28013=CARTESIAN_POINT('Ctrl Pts',(2.70170587365692,0.305647469244615,12.6693503709577));
#28014=CARTESIAN_POINT('Ctrl Pts',(1.20576015647079,2.43696069895998,12.7965063683744));
#28015=CARTESIAN_POINT('Ctrl Pts',(-1.39608020826688,2.33315131427293,12.9236623657912));
#28016=CARTESIAN_POINT('Ctrl Pts',(-2.71746888318096,0.0894308232722988,
13.0508183632079));
#28017=CARTESIAN_POINT('Ctrl Pts',(-1.54645948317952,-2.23631349995748,
13.1779743606246));
#28018=CARTESIAN_POINT('Ctrl Pts',(1.04292591467317,-2.51096406579447,13.3051303580414));
#28019=CARTESIAN_POINT('Ctrl Pts',(2.67576437353453,-0.482617882523345,
13.4322863554581));
#28020=CARTESIAN_POINT('Ctrl Pts',(1.854455145627,1.98837398797749,13.5594423528749));
#28021=CARTESIAN_POINT('Ctrl Pts',(-0.667716404415957,2.63567634706574,
13.6865983502916));
#28022=CARTESIAN_POINT('Ctrl Pts',(-2.5774742884714,0.865598807460369,13.8137543477083));
#28023=CARTESIAN_POINT('Ctrl Pts',(-2.12323382299999,-1.69838544979544,
13.9409103451251));
#28024=CARTESIAN_POINT('Ctrl Pts',(0.278386399345113,-2.70465081218771,
14.0680663425418));
#28025=CARTESIAN_POINT('Ctrl Pts',(2.424677211994,-1.23027453068208,14.1952223399585));
#28026=CARTESIAN_POINT('Ctrl Pts',(2.34711153345411,1.37248040158489,14.3223783373753));
#28027=CARTESIAN_POINT('Ctrl Pts',(0.116830766325856,2.71642882756896,14.449534334792));
#28028=CARTESIAN_POINT('Ctrl Pts',(-2.22060441161598,1.56893309300289,14.5766903322087));
#28029=CARTESIAN_POINT('Ctrl Pts',(-2.52135383579787,-1.01755090187926,
14.7038463296255));
#28030=CARTESIAN_POINT('Ctrl Pts',(-0.509577259988391,-2.67076131829684,
14.8310023270422));
#28031=CARTESIAN_POINT('Ctrl Pts',(1.96957150531571,-1.8744127316726,14.9581583244589));
#28032=CARTESIAN_POINT('Ctrl Pts',(2.64227595081914,0.641102802154851,15.0853143218757));
#28033=CARTESIAN_POINT('Ctrl Pts',(0.891547497430122,2.56861403543508,15.2124703192924));
#28034=CARTESIAN_POINT('Ctrl Pts',(-1.67688719724968,2.1402533333482,15.3396263167092));
#28035=CARTESIAN_POINT('Ctrl Pts',(-2.70732068494482,-0.251097017262045,
15.4667823141259));
#28036=CARTESIAN_POINT('Ctrl Pts',(-1.2546637847063,-2.41214713285786,15.5939383115426));
#28037=CARTESIAN_POINT('Ctrl Pts',(1.34874101223222,-2.36083304897461,15.7210943089594));
#28038=CARTESIAN_POINT('Ctrl Pts',(2.71511250834698,-0.144218827570166,
15.8482503063761));
#28039=CARTESIAN_POINT('Ctrl Pts',(1.59124714071456,2.20466948551834,15.9754063037928));
#28040=CARTESIAN_POINT('Ctrl Pts',(-0.992072403110452,2.53148718151893,
16.1025623012096));
#28041=CARTESIAN_POINT('Ctrl Pts',(-2.66548664388192,0.536484812921177,
16.2297182986263));
#28042=CARTESIAN_POINT('Ctrl Pts',(-1.89417968801256,-1.95056871520298,
16.356874296043));
#28043=CARTESIAN_POINT('Ctrl Pts',(0.614423999078366,-2.64860683238651,
16.4840302934598));
#28044=CARTESIAN_POINT('Ctrl Pts',(2.55949255170539,-0.917405516101003,
16.6111862908765));
#28045=CARTESIAN_POINT('Ctrl Pts',(2.15705517772773,1.6552184035486,16.7383422882933));
#28046=CARTESIAN_POINT('Ctrl Pts',(-0.223782098353677,2.70971522039944,
16.86549828571));
#28047=CARTESIAN_POINT('Ctrl Pts',(-2.39937173587358,1.27892543813116,16.9926542831267));
#28048=CARTESIAN_POINT('Ctrl Pts',(-2.3743144653421,-1.3248644545293,17.1198102805434));
#28049=CARTESIAN_POINT('Ctrl Pts',(-0.171592221611115,-2.71352005938606,
17.2469662779602));
#28050=CARTESIAN_POINT('Ctrl Pts',(2.18851034226299,-1.61339935695285,17.3741222753769));
#28051=CARTESIAN_POINT('Ctrl Pts',(2.54136307238592,0.966493009556284,17.5012782727937));
#28052=CARTESIAN_POINT('Ctrl Pts',(0.563337804795892,2.65994088672957,17.6284342702104));
#28053=CARTESIAN_POINT('Ctrl Pts',(-1.9313675502426,1.91375400432706,17.7555902676271));
#28054=CARTESIAN_POINT('Ctrl Pts',(-2.6546683479107,-0.587682708448213,
17.8827462650439));
#28055=CARTESIAN_POINT('Ctrl Pts',(-0.943170233685906,-2.55011076494666,
18.0099022624606));
#28056=CARTESIAN_POINT('Ctrl Pts',(1.6333812724308,-2.17363764737371,18.1370582598774));
#28057=CARTESIAN_POINT('Ctrl Pts',(2.71183417502487,0.196444420575375,18.2642142572941));
#28058=CARTESIAN_POINT('Ctrl Pts',(1.30305702352152,2.38635232031215,18.3913702547108));
#28059=CARTESIAN_POINT('Ctrl Pts',(-1.30085315674662,2.38755441148266,18.5185262521275));
#28060=CARTESIAN_POINT('Ctrl Pts',(-2.71165164263989,0.198948164546367,
18.6456822495443));
#28061=CARTESIAN_POINT('Ctrl Pts',(-1.63538748881455,-2.17212862525145,
18.772838246961));
#28062=CARTESIAN_POINT('Ctrl Pts',(0.940815322667484,-2.55098050401057,
18.8999942443778));
#28063=CARTESIAN_POINT('Ctrl Pts',(2.65412461084903,-0.590133504635526,
19.0271502417945));
#28064=CARTESIAN_POINT('Ctrl Pts',(1.93313368988793,1.91196996321286,19.1543062392113));
#28065=CARTESIAN_POINT('Ctrl Pts',(-0.560881649881273,2.66045988092931,
19.2814622366279));
#28066=CARTESIAN_POINT('Ctrl Pts',(-2.54046962929626,0.968839029886441,
19.4086182340448));
#28067=CARTESIAN_POINT('Ctrl Pts',(-2.18999905583186,-1.61137802475505,
19.5357742314614));
#28068=CARTESIAN_POINT('Ctrl Pts',(0.169086764197127,-2.71367733332121,
19.6629302288782));
#28069=CARTESIAN_POINT('Ctrl Pts',(2.37309021026153,-1.32705608667036,19.7900862262949));
#28070=CARTESIAN_POINT('Ctrl Pts',(2.40055154088017,1.27670956085784,19.9172422237117));
#28071=CARTESIAN_POINT('Ctrl Pts',(0.226283874248388,2.70950744812837,20.0443982211284));
#28072=CARTESIAN_POINT('Ctrl Pts',(-2.15552600052119,1.65720930008406,20.1715542185451));
#28073=CARTESIAN_POINT('Ctrl Pts',(-2.5603384982902,-0.91504195389121,20.2987102159619));
#28074=CARTESIAN_POINT('Ctrl Pts',(-0.616869187289855,-2.64803840776155,
20.4258662133786));
#28075=CARTESIAN_POINT('Ctrl Pts',(1.89237792686834,-1.95231677376124,20.5530222107954));
#28076=CARTESIAN_POINT('Ctrl Pts',(2.66598084243749,0.53402354907276,20.6801782082121));
#28077=CARTESIAN_POINT('Ctrl Pts',(0.994409294159658,2.5305701252676,20.8073342056288));
#28078=CARTESIAN_POINT('Ctrl Pts',(-1.5892108982743,2.20613773913011,20.9344902030455));
#28079=CARTESIAN_POINT('Ctrl Pts',(-2.71524450783739,-0.141711911520788,
21.0616462004623));
#28080=CARTESIAN_POINT('Ctrl Pts',(-1.35092018684815,-2.359586754492,21.188802197879));
#28081=CARTESIAN_POINT('Ctrl Pts',(1.25243612229158,-2.41330453171314,21.3159581952958));
#28082=CARTESIAN_POINT('Ctrl Pts',(2.7070876939183,-0.253596570647274,21.4431141927125));
#28083=CARTESIAN_POINT('Ctrl Pts',(1.67886257146065,2.13870415657625,21.5702701901293));
#28084=CARTESIAN_POINT('Ctrl Pts',(-0.889175524405625,2.56943610350714,
21.697426187546));
#28085=CARTESIAN_POINT('Ctrl Pts',(-2.64168289644022,0.643542133712422,
21.8245821849627));
#28086=CARTESIAN_POINT('Ctrl Pts',(-1.97130130500755,-1.87259343373928,
21.9517381823794));
#28087=CARTESIAN_POINT('Ctrl Pts',(0.507111137519175,-2.67123067094775,
22.0788941797962));
#28088=CARTESIAN_POINT('Ctrl Pts',(2.52041325965044,-1.01987842598331,22.2060501772129));
#28089=CARTESIAN_POINT('Ctrl Pts',(2.22205205594777,1.56688214740811,22.3332061746296));
#28090=CARTESIAN_POINT('Ctrl Pts',(-0.114322646597065,2.71653553919013,
22.4603621720464));
#28091=CARTESIAN_POINT('Ctrl Pts',(-2.34584332631891,1.37464689705138,22.5875181694631));
#28092=CARTESIAN_POINT('Ctrl Pts',(-2.42581208698928,-1.22803530968155,
22.7146741668798));
#28093=CARTESIAN_POINT('Ctrl Pts',(-0.28088347601373,-2.70439262610117,
22.8418301642966));
#28094=CARTESIAN_POINT('Ctrl Pts',(2.12166480421549,-1.7003451007843,22.9689861617133));
#28095=CARTESIAN_POINT('Ctrl Pts',(2.57827239442557,0.863218664853252,23.0961421591301));
#28096=CARTESIAN_POINT('Ctrl Pts',(0.670149631237062,2.63505872324713,23.2232981565468));
#28097=CARTESIAN_POINT('Ctrl Pts',(-1.85261849592907,1.99008535288051,23.3504541539635));
#28098=CARTESIAN_POINT('Ctrl Pts',(-2.67620883254712,-0.480147152240573,
23.4776101513803));
#28099=CARTESIAN_POINT('Ctrl Pts',(-1.04524383512044,-2.5100000654085,23.604766148797));
#28100=CARTESIAN_POINT('Ctrl Pts',(1.54439404301351,-2.23774038778235,23.7319221462137));
#28101=CARTESIAN_POINT('Ctrl Pts',(2.71755029608022,0.0869217549424415,
23.8590781436305));
#28102=CARTESIAN_POINT('Ctrl Pts',(1.3982338042491,2.33186132346309,23.9862341410472));
#28103=CARTESIAN_POINT('Ctrl Pts',(-1.20350960461554,2.43807293467732,24.113390138464));
#28104=CARTESIAN_POINT('Ctrl Pts',(-2.70142251876817,0.30814181524129,24.2405461358807));
#28105=CARTESIAN_POINT('Ctrl Pts',(-1.72165470325966,-2.10440967635864,
24.3677021332974));
#28106=CARTESIAN_POINT('Ctrl Pts',(0.837174015073502,-2.58684647238557,
24.4948581307141));
#28107=CARTESIAN_POINT('Ctrl Pts',(2.62816656186749,-0.696688973853852,
24.6220141281309));
#28108=CARTESIAN_POINT('Ctrl Pts',(2.00866700702307,1.83245514490942,24.7491701255476));
#28109=CARTESIAN_POINT('Ctrl Pts',(-0.453134335501955,2.68091482095145,
24.8763261229644));
#28110=CARTESIAN_POINT('Ctrl Pts',(-2.49933160157433,1.07050294188287,25.0034821203811));
#28111=CARTESIAN_POINT('Ctrl Pts',(-2.25320113911441,-1.52174887215384,
25.1306381177978));
#28112=CARTESIAN_POINT('Ctrl Pts',(0.0595120232557837,-2.71828867530585,
25.2577941152146));
#28113=CARTESIAN_POINT('Ctrl Pts',(2.31764216790862,-1.42167850962861,25.3849501126313));
#28114=CARTESIAN_POINT('Ctrl Pts',(2.45008582783643,1.17886150138301,25.512106110048));
#28115=CARTESIAN_POINT('Ctrl Pts',(0.335368816128816,2.69817767398226,25.6392621074648));
#28116=CARTESIAN_POINT('Ctrl Pts',(-2.08694052786993,1.7427892116782,25.7664181048815));
#28117=CARTESIAN_POINT('Ctrl Pts',(-2.59515746539462,-0.81104422383404,
25.8935741022983));
#28118=CARTESIAN_POINT('Ctrl Pts',(-0.723157462484335,-2.62100711324124,
26.020730099715));
#28119=CARTESIAN_POINT('Ctrl Pts',(1.81210543131392,-2.02704437766185,26.1478860971317));
#28120=CARTESIAN_POINT('Ctrl Pts',(2.68534815755687,0.426075434534669,26.2750420945485));
#28121=CARTESIAN_POINT('Ctrl Pts',(1.09565317739333,2.48840895314172,26.4021980919652));
#28122=CARTESIAN_POINT('Ctrl Pts',(-1.49894893786632,2.26843273756957,26.5293540893819));
#28123=CARTESIAN_POINT('Ctrl Pts',(-2.71875060177305,-0.0320962391350563,
26.6565100867987));
#28124=CARTESIAN_POINT('Ctrl Pts',(-1.44497862883923,-2.30318730575823,
26.7836660842154));
#28125=CARTESIAN_POINT('Ctrl Pts',(1.15409350672138,-2.46184954474304,26.9108220816321));
#28126=CARTESIAN_POINT('Ctrl Pts',(2.6946584217475,-0.36256170966231,27.0379780790489));
#28127=CARTESIAN_POINT('Ctrl Pts',(1.76374647663869,2.06925913537976,27.1651340764656));
#28128=CARTESIAN_POINT('Ctrl Pts',(-0.784831948561556,2.60320452821615,
27.2922900738823));
#28129=CARTESIAN_POINT('Ctrl Pts',(-2.61358110549165,0.749552405255957,
27.4194460712991));
#28130=CARTESIAN_POINT('Ctrl Pts',(-2.04521559579937,-1.79157142472941,
27.5466020687158));
#28131=CARTESIAN_POINT('Ctrl Pts',(0.398973201256793,-2.68950839148846,
27.6737580661326));
#28132=CARTESIAN_POINT('Ctrl Pts',(2.47723323095525,-1.12069198384702,27.8009140635493));
#28133=CARTESIAN_POINT('Ctrl Pts',(2.28343363407859,1.47599655892775,27.928070060966));
#28134=CARTESIAN_POINT('Ctrl Pts',(-0.00467719079377135,2.71893602850347,
28.0552260583828));
#28135=CARTESIAN_POINT('Ctrl Pts',(-2.28849820708635,1.46813179223479,28.1823820557995));
#28136=CARTESIAN_POINT('Ctrl Pts',(-2.47336288901496,-1.12920813956133,
28.3095380532162));
#28137=CARTESIAN_POINT('Ctrl Pts',(-0.389717730296424,-2.69086511997546,
28.436694050633));
#28138=CARTESIAN_POINT('Ctrl Pts',(2.05136729710396,-1.78452436676565,28.5638500480497));
#28139=CARTESIAN_POINT('Ctrl Pts',(2.61098684245559,0.758539855071413,28.6910060454665));
#28140=CARTESIAN_POINT('Ctrl Pts',(0.775871117775893,2.60588929385136,28.8181620428832));
#28141=CARTESIAN_POINT('Ctrl Pts',(-1.77085521348547,2.06317881340403,28.9453180403));
#28142=CARTESIAN_POINT('Ctrl Pts',(-2.69339509964618,-0.371830391993313,
29.0724740377166));
#28143=CARTESIAN_POINT('Ctrl Pts',(-1.14561681477155,-2.46580557159737,
29.1996300351334));
#28144=CARTESIAN_POINT('Ctrl Pts',(1.4528940696187,-2.29820230303488,29.3267860325501));
#28145=CARTESIAN_POINT('Ctrl Pts',(2.718844936639,-0.0227423332226366,29.4539420299669));
#28146=CARTESIAN_POINT('Ctrl Pts',(1.49113564511475,2.2735763657894,29.5810980273836));
#28147=CARTESIAN_POINT('Ctrl Pts',(-1.10420793077029,2.48462468973324,29.7082540248003));
#28148=CARTESIAN_POINT('Ctrl Pts',(-2.68679815444885,0.416834116235907,
29.8354100222171));
#28149=CARTESIAN_POINT('Ctrl Pts',(-1.80512076892626,-2.03326683266092,
29.9625660196338));
#28150=CARTESIAN_POINT('Ctrl Pts',(0.732170617296673,-2.6185036166436,30.0897220170505));
#28151=CARTESIAN_POINT('Ctrl Pts',(2.59793246058555,-0.802110923403799,
30.2168780144673));
#28152=CARTESIAN_POINT('Ctrl Pts',(2.08093220359809,1.74995890444202,30.344034011884));
#28153=CARTESIAN_POINT('Ctrl Pts',(-0.344649767196044,2.69700788674807,
30.4711900093008));
#28154=CARTESIAN_POINT('Ctrl Pts',(-2.45412713727274,1.17042513528533,30.5983460067174));
#28155=CARTESIAN_POINT('Ctrl Pts',(-2.31273724244973,-1.42964381948506,
30.7255020041343));
#28156=CARTESIAN_POINT('Ctrl Pts',(-0.0501595443200041,-2.71847733544578,
30.8526580015509));
#28157=CARTESIAN_POINT('Ctrl Pts',(2.25842329943333,-1.51398784795982,30.9798139989677));
#28158=CARTESIAN_POINT('Ctrl Pts',(2.49563380156246,1.07909542288794,31.1069699963845));
#28159=CARTESIAN_POINT('Ctrl Pts',(0.443908109713979,2.68245793879611,31.2341259938011));
#28160=CARTESIAN_POINT('Ctrl Pts',(-2.01495958288181,1.8255335884188,31.361281991218));
#28161=CARTESIAN_POINT('Ctrl Pts',(-2.6257540863254,-0.705726916965534,
31.4884379886346));
#28162=CARTESIAN_POINT('Ctrl Pts',(-0.828269153507524,-2.58971141500841,
31.6155939860514));
#28163=CARTESIAN_POINT('Ctrl Pts',(1.72888462274292,-2.09847396066029,31.7427499834681));
#28164=CARTESIAN_POINT('Ctrl Pts',(2.70034638543151,0.317434090813201,31.8699059808848));
#28165=CARTESIAN_POINT('Ctrl Pts',(1.19511442223928,2.4421991163561,31.9970619783016));
#28166=CARTESIAN_POINT('Ctrl Pts',(-1.40624817287752,2.3270369728351,32.1242179757183));
#28167=CARTESIAN_POINT('Ctrl Pts',(-2.71783326273588,0.0775716565606125,
32.251373973135));
#28168=CARTESIAN_POINT('Ctrl Pts',(-1.53668607586383,-2.24304055371657,
32.3785299705518));
#28169=CARTESIAN_POINT('Ctrl Pts',(1.05387316833121,-2.50638909606359,32.5056859679685));
#28170=CARTESIAN_POINT('Ctrl Pts',(2.67784491737894,-0.470936974057936,
32.6328419653853));
#28171=CARTESIAN_POINT('Ctrl Pts',(1.84576074359989,1.99644744162733,32.7599979628019));
#28172=CARTESIAN_POINT('Ctrl Pts',(-0.679211432678792,2.63273745311828,
32.8871539602188));
#28173=CARTESIAN_POINT('Ctrl Pts',(-2.5812270137068,0.854343264078797,33.0143099576354));
#28174=CARTESIAN_POINT('Ctrl Pts',(-2.11580226149321,-1.70763473342862,
33.1414659550522));
#28175=CARTESIAN_POINT('Ctrl Pts',(0.290186056189786,-2.70340983333955,
33.2686219524689));
#28176=CARTESIAN_POINT('Ctrl Pts',(2.43002286401826,-1.21968297089525,33.3957779498857));
#28177=CARTESIAN_POINT('Ctrl Pts',(2.34109976899834,1.38271104627974,33.5229339473025));
#28178=CARTESIAN_POINT('Ctrl Pts',(0.10497639860856,2.71690985324928,33.6500899447191));
#28179=CARTESIAN_POINT('Ctrl Pts',(-2.22743067787563,1.55923360834914,33.777245942136));
#28180=CARTESIAN_POINT('Ctrl Pts',(-2.51688760174644,-1.02855438653656,
33.9044019395525));
#28181=CARTESIAN_POINT('Ctrl Pts',(-0.497921540466094,-2.67293924524441,
34.0315579369694));
#28182=CARTESIAN_POINT('Ctrl Pts',(1.97773911754471,-1.86583890941239,34.158713934386));
#28183=CARTESIAN_POINT('Ctrl Pts',(2.6394399920918,0.652700710408037,34.2858699318029));
#28184=CARTESIAN_POINT('Ctrl Pts',(0.88035541786161,2.57233930898914,34.4130259292195));
#28185=CARTESIAN_POINT('Ctrl Pts',(-1.6862587097392,2.13318386777371,34.5401819266363));
#28186=CARTESIAN_POINT('Ctrl Pts',(-2.70610771640309,-0.263420825630993,
34.667337924053));
#28187=CARTESIAN_POINT('Ctrl Pts',(-1.24430022082504,-2.41661909656449,
34.7944939214698));
#28188=CARTESIAN_POINT('Ctrl Pts',(1.35936225667267,-2.35682489174383,34.9216499188865));
#28189=CARTESIAN_POINT('Ctrl Pts',(2.71527216294739,-0.128169239057751,
35.0488234117232));
#28190=CARTESIAN_POINT('Ctrl Pts',(1.95998264084422,1.42578951645669,35.1336115720876));
#28191=CARTESIAN_POINT('Ctrl Pts',(1.3368658628607,1.87099030021161,35.1760143999799));
#28192=CARTESIAN_POINT('Ctrl Pts',(-1.07608796999509,2.20514531467084,5.00182276437832));
#28193=CARTESIAN_POINT('Ctrl Pts',(-1.81030871625589,1.84686632199456,5.04421585895808));
#28194=CARTESIAN_POINT('Ctrl Pts',(-2.87978867813524,0.345520098533912,
5.12899428601007));
#28195=CARTESIAN_POINT('Ctrl Pts',(-1.84755059459602,-2.23940304886746,
5.25615804553432));
#28196=CARTESIAN_POINT('Ctrl Pts',(0.881605936087441,-2.76315392529851,
5.38331404295105));
#28197=CARTESIAN_POINT('Ctrl Pts',(2.80091533600486,-0.756151946153,5.51047004036779));
#28198=CARTESIAN_POINT('Ctrl Pts',(2.15194886181718,1.94621511872954,5.63762603778452));
#28199=CARTESIAN_POINT('Ctrl Pts',(-0.471078520427701,2.86259676314238,
5.76478203520127));
#28200=CARTESIAN_POINT('Ctrl Pts',(-2.66186325535688,1.15397730881358,5.89193803261799));
#28201=CARTESIAN_POINT('Ctrl Pts',(-2.41134479058127,-1.61330753477629,
6.01909403003473));
#28202=CARTESIAN_POINT('Ctrl Pts',(0.0508516576283012,-2.90076608290592,
6.14625002745147));
#28203=CARTESIAN_POINT('Ctrl Pts',(2.46638211777227,-1.52778353006007,6.2734060248682));
#28204=CARTESIAN_POINT('Ctrl Pts',(2.61981899923616,1.24648407281762,6.40056202228494));
#28205=CARTESIAN_POINT('Ctrl Pts',(0.370412799265996,2.87748598506404,6.52771801970167));
#28206=CARTESIAN_POINT('Ctrl Pts',(-2.21872348537856,1.86933643410663,6.65487401711841));
#28207=CARTESIAN_POINT('Ctrl Pts',(-2.77290112857825,-0.853329714521984,
6.78203001453515));
#28208=CARTESIAN_POINT('Ctrl Pts',(-0.783838520812214,-2.79333917680625,
6.90918601195188));
#28209=CARTESIAN_POINT('Ctrl Pts',(1.92414166455907,-2.17136564421719,7.03634200936862));
#28210=CARTESIAN_POINT('Ctrl Pts',(2.86734498811586,0.442133806270777,7.16349800678535));
#28211=CARTESIAN_POINT('Ctrl Pts',(1.18068727514493,2.65011818812846,7.29065400420209));
#28212=CARTESIAN_POINT('Ctrl Pts',(-1.58886875444023,2.42747717552242,7.41781000161883));
#28213=CARTESIAN_POINT('Ctrl Pts',(-2.90115204840517,-0.0215885031761271,
7.54496599903556));
#28214=CARTESIAN_POINT('Ctrl Pts',(-1.55256739877849,-2.45085365810098,
7.6721219964523));
#28215=CARTESIAN_POINT('Ctrl Pts',(1.21999527288542,-2.63225393721386,7.79927799386903));
#28216=CARTESIAN_POINT('Ctrl Pts',(2.87360719141344,-0.399413254315134,
7.92643399128578));
#28217=CARTESIAN_POINT('Ctrl Pts',(1.89161467498072,2.19975979350155,8.0535899887025));
#28218=CARTESIAN_POINT('Ctrl Pts',(-0.825322001864961,2.78136528197505,
8.18074598611925));
#28219=CARTESIAN_POINT('Ctrl Pts',(-2.78529289373178,0.811968430063206,
8.30790198353598));
#28220=CARTESIAN_POINT('Ctrl Pts',(-2.19065913470589,-1.90214662675786,
8.43505798095271));
#28221=CARTESIAN_POINT('Ctrl Pts',(0.413195279353741,-2.87165786555681,
8.56221397836945));
#28222=CARTESIAN_POINT('Ctrl Pts',(2.63807677311075,-1.20735254764592,8.6893699757862));
#28223=CARTESIAN_POINT('Ctrl Pts',(2.44337675421409,1.56430792109332,8.81652597320291));
#28224=CARTESIAN_POINT('Ctrl Pts',(0.0076694670848323,2.90122222770289,
8.94368197061967));
#28225=CARTESIAN_POINT('Ctrl Pts',(-2.43507207356043,1.57720424540266,9.07083796803638));
#28226=CARTESIAN_POINT('Ctrl Pts',(-2.64442320226339,-1.19338810220102,
9.19799396545314));
#28227=CARTESIAN_POINT('Ctrl Pts',(-0.428372023928768,-2.86943315731314,
9.32514996286987));
#28228=CARTESIAN_POINT('Ctrl Pts',(2.18057182537728,-1.91370210574398,9.4523059602866));
#28229=CARTESIAN_POINT('Ctrl Pts',(2.78954686053182,0.797231176043415,9.57946195770334));
#28230=CARTESIAN_POINT('Ctrl Pts',(0.840015607682165,2.77696291189002,9.70661795512008));
#28231=CARTESIAN_POINT('Ctrl Pts',(-1.87995805812211,2.20973005927462,9.83377395253681));
#28232=CARTESIAN_POINT('Ctrl Pts',(-2.87567873468839,-0.384214848777708,
9.96092994995354));
#28233=CARTESIAN_POINT('Ctrl Pts',(-1.23389500898796,-2.62576700069816,
10.0880859473702));
#28234=CARTESIAN_POINT('Ctrl Pts',(1.53958798439635,-2.45902787163197,10.2152419447871));
#28235=CARTESIAN_POINT('Ctrl Pts',(2.90099735580753,-0.0369266402241637,
10.3423979422037));
#28236=CARTESIAN_POINT('Ctrl Pts',(1.60168068553317,2.41904283069784,10.4695539396205));
#28237=CARTESIAN_POINT('Ctrl Pts',(-1.1666595610404,2.65632353146103,10.5967099370373));
#28238=CARTESIAN_POINT('Ctrl Pts',(-2.8649672997844,0.457287225195054,10.723865934454));
#28239=CARTESIAN_POINT('Ctrl Pts',(-1.93559491057049,-2.16116208955603,
10.8510219318708));
#28240=CARTESIAN_POINT('Ctrl Pts',(0.769059270748106,-2.79744473997913,
10.9781779292875));
#28241=CARTESIAN_POINT('Ctrl Pts',(2.76835051018645,-0.867977354491986,
11.1053339267041));
#28242=CARTESIAN_POINT('Ctrl Pts',(2.22857625195351,1.85757829562831,11.2324899241209));
#28243=CARTESIAN_POINT('Ctrl Pts',(-0.355195343120889,2.87940714442847,
11.3596459215376));
#28244=CARTESIAN_POINT('Ctrl Pts',(-2.61319018509511,1.26031198188509,11.4868019189544));
#28245=CARTESIAN_POINT('Ctrl Pts',(-2.47442890337263,-1.51471146998848,
11.6139579163712));
#28246=CARTESIAN_POINT('Ctrl Pts',(-0.0661800578911379,-2.9004774495069,
11.7411139137879));
#28247=CARTESIAN_POINT('Ctrl Pts',(2.40276756869014,-1.62599423308062,11.8682699112045));
#28248=CARTESIAN_POINT('Ctrl Pts',(2.66795370981783,1.13981236939675,11.9954259086213));
#28249=CARTESIAN_POINT('Ctrl Pts',(0.486155919880249,2.8602100721321,12.1225819060381));
#28250=CARTESIAN_POINT('Ctrl Pts',(-2.1415325613244,1.95729086339969,12.2497379034547));
#28251=CARTESIAN_POINT('Ctrl Pts',(-2.80505811641455,-0.740809151332146,
12.3768939008716));
#28252=CARTESIAN_POINT('Ctrl Pts',(-0.895850827110875,-2.75945656438461,
12.5040498982883));
#28253=CARTESIAN_POINT('Ctrl Pts',(1.83500961550839,-2.24719579613177,12.6312058957051));
#28254=CARTESIAN_POINT('Ctrl Pts',(2.88284271549586,0.326139713731703,12.7583618931217));
#28255=CARTESIAN_POINT('Ctrl Pts',(1.28660077975543,2.60034760535842,12.8855178905385));
#28256=CARTESIAN_POINT('Ctrl Pts',(-1.48968090786382,2.48957828314488,13.0126738879553));
#28257=CARTESIAN_POINT('Ctrl Pts',(-2.89966256166186,0.095426744978067,
13.139829885372));
#28258=CARTESIAN_POINT('Ctrl Pts',(-1.65014241533962,-2.38624794274561,
13.2669858827887));
#28259=CARTESIAN_POINT('Ctrl Pts',(1.11284925766102,-2.67931255453407,13.3941418802055));
#28260=CARTESIAN_POINT('Ctrl Pts',(2.85516195816916,-0.514975172007566,
13.5212978776221));
#28261=CARTESIAN_POINT('Ctrl Pts',(1.97878775773184,2.12168523702531,13.6484538750389));
#28262=CARTESIAN_POINT('Ctrl Pts',(-0.712483690862428,2.81238621554999,
13.7756098724557));
#28263=CARTESIAN_POINT('Ctrl Pts',(-2.75028197900763,0.923633190777811,
13.9027658698724));
#28264=CARTESIAN_POINT('Ctrl Pts',(-2.26558679818273,-1.81225431302031,
14.0299218672892));
#28265=CARTESIAN_POINT('Ctrl Pts',(0.297050915597647,-2.88598509848946,
14.1570778647059));
#28266=CARTESIAN_POINT('Ctrl Pts',(2.58724056759163,-1.31275872900115,14.2842338621225));
#28267=CARTESIAN_POINT('Ctrl Pts',(2.50447447024121,1.46449884365629,14.4113898595393));
#28268=CARTESIAN_POINT('Ctrl Pts',(0.124663727066729,2.89855277514735,14.538545856956));
#28269=CARTESIAN_POINT('Ctrl Pts',(-2.36948563292723,1.67412277641516,14.6657018543728));
#28270=CARTESIAN_POINT('Ctrl Pts',(-2.69039891040353,-1.08577296800945,
14.7928578517896));
#28271=CARTESIAN_POINT('Ctrl Pts',(-0.54374205062941,-2.84982347129394,
14.9200138492063));
#28272=CARTESIAN_POINT('Ctrl Pts',(2.10162213515206,-2.00008340731066,15.0471698466229));
#28273=CARTESIAN_POINT('Ctrl Pts',(2.81942829211027,0.684085770067413,15.1743258440397));
#28274=CARTESIAN_POINT('Ctrl Pts',(0.951321619997796,2.74082768712031,15.3014818414565));
#28275=CARTESIAN_POINT('Ctrl Pts',(-1.7893147024018,2.28374738772249,15.4286378388731));
#28276=CARTESIAN_POINT('Ctrl Pts',(-2.88883397382565,-0.267931907079493,
15.55579383629));
#28277=CARTESIAN_POINT('Ctrl Pts',(-1.33878316933185,-2.57387040479398,
15.6829498337066));
#28278=CARTESIAN_POINT('Ctrl Pts',(1.43916783840774,-2.51911594970405,15.8101058311235));
#28279=CARTESIAN_POINT('Ctrl Pts',(2.89714820282978,-0.153888030725978,
15.9372618285401));
#28280=CARTESIAN_POINT('Ctrl Pts',(1.69793287747983,2.35248234397915,16.0644178259569));
#28281=CARTESIAN_POINT('Ctrl Pts',(-1.05858625412856,2.70121164993243,16.1915738233737));
#28282=CARTESIAN_POINT('Ctrl Pts',(-2.84419515443609,0.572453630124593,
16.3187298207904));
#28283=CARTESIAN_POINT('Ctrl Pts',(-2.02117564634667,-2.08134529614278,
16.4458858182071));
#28284=CARTESIAN_POINT('Ctrl Pts',(0.655618277044906,-2.82618362990893,
16.5730418156239));
#28285=CARTESIAN_POINT('Ctrl Pts',(2.73109465023388,-0.978913298829069,
16.7001978130405));
#28286=CARTESIAN_POINT('Ctrl Pts',(2.30167571780043,1.76619311663488,16.8273538104573));
#28287=CARTESIAN_POINT('Ctrl Pts',(-0.23878564961041,2.89138905177091,16.9545098078741));
#28288=CARTESIAN_POINT('Ctrl Pts',(-2.56023847672482,1.36467145403512,17.0816658052908));
#28289=CARTESIAN_POINT('Ctrl Pts',(-2.53350123247984,-1.41369046830757,
17.2088218027076));
#28290=CARTESIAN_POINT('Ctrl Pts',(-0.183096683813934,-2.89544898755562,
17.3359778001242));
#28291=CARTESIAN_POINT('Ctrl Pts',(2.33523980515338,-1.72157029702181,17.4631337975409));
#28292=CARTESIAN_POINT('Ctrl Pts',(2.71174967345399,1.03129188093514,17.5902897949577));
#28293=CARTESIAN_POINT('Ctrl Pts',(0.601106990495946,2.8382775800012,17.7174457923745));
#28294=CARTESIAN_POINT('Ctrl Pts',(-2.06085678217284,2.04206232973746,17.8446017897912));
#28295=CARTESIAN_POINT('Ctrl Pts',(-2.83265154192117,-0.627084106968225,
17.971757787208));
#28296=CARTESIAN_POINT('Ctrl Pts',(-1.0064054211695,-2.72108385820819,18.0989137846246));
#28297=CARTESIAN_POINT('Ctrl Pts',(1.74289190720861,-2.31936996508692,18.2260697820413));
#28298=CARTESIAN_POINT('Ctrl Pts',(2.89365007247118,0.209615107394771,18.3532257794581));
#28299=CARTESIAN_POINT('Ctrl Pts',(1.39042095024577,2.54634616976526,18.4803817768749));
#28300=CARTESIAN_POINT('Ctrl Pts',(-1.38806932443051,2.54762885557052,18.6075377742917));
#28301=CARTESIAN_POINT('Ctrl Pts',(-2.89345530213681,0.212286715780541,
18.7346937717084));
#28302=CARTESIAN_POINT('Ctrl Pts',(-1.74503263109116,-2.31775977003389,
18.861849769125));
#28303=CARTESIAN_POINT('Ctrl Pts',(1.00389262429512,-2.72201190924037,18.9890057665418));
#28304=CARTESIAN_POINT('Ctrl Pts',(2.8320713498127,-0.629699217667123,19.1161617639586));
#28305=CARTESIAN_POINT('Ctrl Pts',(2.06274133328574,2.04015867694529,19.2433177613753));
#28306=CARTESIAN_POINT('Ctrl Pts',(-0.598486161791943,2.83883137035367,
19.370473758792));
#28307=CARTESIAN_POINT('Ctrl Pts',(-2.71079632915113,1.03379519104186,19.4976297562087));
#28308=CARTESIAN_POINT('Ctrl Pts',(-2.33682833005875,-1.71941344388002,
19.6247857536255));
#28309=CARTESIAN_POINT('Ctrl Pts',(0.180423247106767,-2.89561680597831,
19.7519417510422));
#28310=CARTESIAN_POINT('Ctrl Pts',(2.53219489677721,-1.41602903921353,19.8790977484589));
#28311=CARTESIAN_POINT('Ctrl Pts',(2.56149738218228,1.36230701247328,20.0062537458757));
#28312=CARTESIAN_POINT('Ctrl Pts',(0.241455157969516,2.89116734933321,20.1334097432925));
#28313=CARTESIAN_POINT('Ctrl Pts',(-2.30004401635826,1.76831749354441,20.2605657407091));
#28314=CARTESIAN_POINT('Ctrl Pts',(-2.73199731361163,-0.976391270741076,
20.387721738126));
#28315=CARTESIAN_POINT('Ctrl Pts',(-0.658227403779219,-2.82557709505061,
20.5148777355426));
#28316=CARTESIAN_POINT('Ctrl Pts',(2.01925308547869,-2.0832105539156,20.6420337329593));
#28317=CARTESIAN_POINT('Ctrl Pts',(2.84472248671151,0.569827349956488,20.769189730376));
#28318=CARTESIAN_POINT('Ctrl Pts',(1.06107982287839,2.70023310931498,20.8963457277929));
#28319=CARTESIAN_POINT('Ctrl Pts',(-1.69576011443302,2.35404903718225,21.0235017252096));
#28320=CARTESIAN_POINT('Ctrl Pts',(-2.89728905227348,-0.151213037588684,
21.1506577226264));
#28321=CARTESIAN_POINT('Ctrl Pts',(-1.44149311656933,-2.51778609695974,
21.2778137200429));
#28322=CARTESIAN_POINT('Ctrl Pts',(1.33640615248957,-2.57510540187165,21.4049697174598));
#28323=CARTESIAN_POINT('Ctrl Pts',(2.88858536183199,-0.270599043920174,
21.5321257148764));
#28324=CARTESIAN_POINT('Ctrl Pts',(1.791422516287,2.28209434583684,21.6592817122933));
#28325=CARTESIAN_POINT('Ctrl Pts',(-0.948790617189007,2.74170487104185,
21.7864377097099));
#28326=CARTESIAN_POINT('Ctrl Pts',(-2.81879547618728,0.686688647486343,
21.9135937071268));
#28327=CARTESIAN_POINT('Ctrl Pts',(-2.10346790988621,-1.99814213389326,
22.0407497045435));
#28328=CARTESIAN_POINT('Ctrl Pts',(0.541110586092526,-2.85032429186209,
22.1679057019603));
#28329=CARTESIAN_POINT('Ctrl Pts',(2.6893952729901,-1.08825654180393,22.2950616993769));
#28330=CARTESIAN_POINT('Ctrl Pts',(2.37103033509376,1.67193432443554,22.4222176967938));
#28331=CARTESIAN_POINT('Ctrl Pts',(-0.121987449548903,2.89866664128752,
22.5493736942105));
#28332=CARTESIAN_POINT('Ctrl Pts',(-2.50312123570262,1.46681059259031,22.6765296916271));
#28333=CARTESIAN_POINT('Ctrl Pts',(-2.58845153068903,-1.31036937862351,
22.8036856890438));
#28334=CARTESIAN_POINT('Ctrl Pts',(-0.299715409669359,-2.88570960222391,
22.9308416864606));
#28335=CARTESIAN_POINT('Ctrl Pts',(2.26391258396967,-1.81434534951434,23.0579976838774));
#28336=CARTESIAN_POINT('Ctrl Pts',(2.75113359426246,0.921093470653797,23.1851536812941));
#28337=CARTESIAN_POINT('Ctrl Pts',(0.715080054250639,2.81172718292039,23.3123096787109));
#28338=CARTESIAN_POINT('Ctrl Pts',(-1.97682796919452,2.12351134100359,23.4394656761275));
#28339=CARTESIAN_POINT('Ctrl Pts',(-2.85563621609605,-0.512338790724611,
23.5666216735442));
#28340=CARTESIAN_POINT('Ctrl Pts',(-1.11532258391811,-2.6782839223956,23.693777670961));
#28341=CARTESIAN_POINT('Ctrl Pts',(1.64793849699504,-2.38777049677775,23.8209336683777));
#28342=CARTESIAN_POINT('Ctrl Pts',(2.89974943291822,0.0927494552598746,
23.9480896657945));
#28343=CARTESIAN_POINT('Ctrl Pts',(1.49197889246301,2.48820180443737,24.0752456632113));
#28344=CARTESIAN_POINT('Ctrl Pts',(-1.28419933884185,2.60153441131934,24.202401660628));
#28345=CARTESIAN_POINT('Ctrl Pts',(-2.8825403629767,0.32880129405259,24.3295576580448));
#28346=CARTESIAN_POINT('Ctrl Pts',(-1.83708366195063,-2.24550057986067,
24.4567136554614));
#28347=CARTESIAN_POINT('Ctrl Pts',(0.893302647963849,-2.76028252436256,
24.5838696528783));
#28348=CARTESIAN_POINT('Ctrl Pts',(2.80437293410263,-0.74339873663678,24.7110256502948));
#28349=CARTESIAN_POINT('Ctrl Pts',(2.14333880883014,1.95531275905497,24.8381816477117));
#28350=CARTESIAN_POINT('Ctrl Pts',(-0.483514889973881,2.86065771918524,
24.9653376451283));
#28351=CARTESIAN_POINT('Ctrl Pts',(-2.66690018756726,1.14227519657666,25.0924936425451));
#28352=CARTESIAN_POINT('Ctrl Pts',(-2.40426781974259,-1.62377507251181,
25.2196496399619));
#28353=CARTESIAN_POINT('Ctrl Pts',(0.063502028255683,-2.90053731704456,
25.3468056373787));
#28354=CARTESIAN_POINT('Ctrl Pts',(2.47302932048551,-1.51699545654545,25.4739616347953));
#28355=CARTESIAN_POINT('Ctrl Pts',(2.61435271322018,1.25789869466457,25.6011176322122));
#28356=CARTESIAN_POINT('Ctrl Pts',(0.357853739005512,2.87907796640528,25.7282736296288));
#28357=CARTESIAN_POINT('Ctrl Pts',(-2.22686020602959,1.85963514108612,25.8554296270455));
#28358=CARTESIAN_POINT('Ctrl Pts',(-2.76915073088654,-0.865420975474404,
25.9825856244623));
#28359=CARTESIAN_POINT('Ctrl Pts',(-0.771641814605623,-2.79673347766867,
26.109741621879));
#28360=CARTESIAN_POINT('Ctrl Pts',(1.93359869159367,-2.16294829689196,26.2368976192958));
#28361=CARTESIAN_POINT('Ctrl Pts',(2.8653882904376,0.4546418152608,26.3640536167125));
#28362=CARTESIAN_POINT('Ctrl Pts',(1.169111638671,2.65524522624268,26.4912096141293));
#28363=CARTESIAN_POINT('Ctrl Pts',(-1.59944650843108,2.42052062619349,26.6183656115459));
#28364=CARTESIAN_POINT('Ctrl Pts',(-2.90103021353787,-0.0342481430297994,
26.7455216089627));
#28365=CARTESIAN_POINT('Ctrl Pts',(-1.54185774062733,-2.45760532690425,
26.8726776063794));
#28366=CARTESIAN_POINT('Ctrl Pts',(1.23147012089423,-2.62690513275704,26.9998336037961));
#28367=CARTESIAN_POINT('Ctrl Pts',(2.8753227646389,-0.386869789864589,27.1269896012129));
#28368=CARTESIAN_POINT('Ctrl Pts',(1.88199749341217,2.20799335822166,27.2541455986297));
#28369=CARTESIAN_POINT('Ctrl Pts',(-0.837451288780281,2.77773731192868,
27.3813015960464));
#28370=CARTESIAN_POINT('Ctrl Pts',(-2.7888095905591,0.799806415807056,27.5084575934632));
#28371=CARTESIAN_POINT('Ctrl Pts',(-2.18233781088392,-1.91168797515362,
27.6356135908798));
#28372=CARTESIAN_POINT('Ctrl Pts',(0.425722503006781,-2.86982744874917,
27.7627695882965));
#28373=CARTESIAN_POINT('Ctrl Pts',(2.64332022374341,-1.1958291809074,27.8899255857133));
#28374=CARTESIAN_POINT('Ctrl Pts',(2.43652726320332,1.57495527899285,28.0170815831301));
#28375=CARTESIAN_POINT('Ctrl Pts',(-0.00499077473252099,2.90122807227011,
28.1442375805469));
#28376=CARTESIAN_POINT('Ctrl Pts',(-2.44193139232967,1.56656321618868,28.2713935779634));
#28377=CARTESIAN_POINT('Ctrl Pts',(-2.63919039333589,-1.2049163053441,28.3985495753804));
#28378=CARTESIAN_POINT('Ctrl Pts',(-0.415846495667482,-2.87127513958548,
28.525705572797));
#28379=CARTESIAN_POINT('Ctrl Pts',(2.1889019552147,-1.90416844465447,28.6528615702139));
#28380=CARTESIAN_POINT('Ctrl Pts',(2.78604139422485,0.809396432427394,28.7800175676304));
#28381=CARTESIAN_POINT('Ctrl Pts',(0.827889675872156,2.7806020786414,28.9071735650473));
#28382=CARTESIAN_POINT('Ctrl Pts',(-1.88958283807723,2.2015053788725,29.0343295624639));
#28383=CARTESIAN_POINT('Ctrl Pts',(-2.87397474265299,-0.396759894335619,
29.1614855598808));
#28384=CARTESIAN_POINT('Ctrl Pts',(-1.22242510608428,-2.63112639285447,
29.2886415572974));
#28385=CARTESIAN_POINT('Ctrl Pts',(1.55030387498037,-2.45228610288064,29.4157975547142));
#28386=CARTESIAN_POINT('Ctrl Pts',(2.90113087311882,-0.0242671011316893,
29.5429535521309));
#28387=CARTESIAN_POINT('Ctrl Pts',(1.59110937065723,2.42600911081705,29.6701095495477));
#28388=CARTESIAN_POINT('Ctrl Pts',(-1.17823994856453,2.6512072455331,29.7972655469643));
#28389=CARTESIAN_POINT('Ctrl Pts',(-2.86693550289264,0.444780909453394,
29.924421544381));
#28390=CARTESIAN_POINT('Ctrl Pts',(-1.92614574000444,-2.16958793862411,
30.0515775417978));
#28391=CARTESIAN_POINT('Ctrl Pts',(0.781259259623611,-2.79406213324135,
30.1787335392145));
#28392=CARTESIAN_POINT('Ctrl Pts',(2.77211177662798,-0.855888738704282,
30.3058895366313));
#28393=CARTESIAN_POINT('Ctrl Pts',(2.22044905149627,1.86728552847961,30.433045534048));
#28394=CARTESIAN_POINT('Ctrl Pts',(-0.367756934774604,2.87782975036528,
30.5602015314649));
#28395=CARTESIAN_POINT('Ctrl Pts',(-2.61866497370095,1.24889670936804,30.6873575288816));
#28396=CARTESIAN_POINT('Ctrl Pts',(-2.46779554253535,-1.52549480346568,
30.8145135262982));
#28397=CARTESIAN_POINT('Ctrl Pts',(-0.0535225090063733,-2.90073862597142,
30.9416695237149));
#28398=CARTESIAN_POINT('Ctrl Pts',(2.40984010167806,-1.61549370765973,31.0688255211317));
#28399=CARTESIAN_POINT('Ctrl Pts',(2.66295446722381,1.15144376356069,31.1959815185485));
#28400=CARTESIAN_POINT('Ctrl Pts',(0.473670088560071,2.86230429592071,31.3231375159653));
#28401=CARTESIAN_POINT('Ctrl Pts',(-2.15005327270024,1.94792714432035,31.4502935133819));
#28402=CARTESIAN_POINT('Ctrl Pts',(-2.80179871327025,-0.753042631894556,
31.5774495107988));
#28403=CARTESIAN_POINT('Ctrl Pts',(-0.883800756751865,-2.76333954809381,
31.7046055082154));
#28404=CARTESIAN_POINT('Ctrl Pts',(1.84479831398562,-2.23916690196877,31.8317615056321));
#28405=CARTESIAN_POINT('Ctrl Pts',(2.8813920798935,0.338716573581852,31.9589175030488));
#28406=CARTESIAN_POINT('Ctrl Pts',(1.27524129844414,2.6059372343326,32.0860735004657));
#28407=CARTESIAN_POINT('Ctrl Pts',(-1.5005305873182,2.48305400348663,32.2132294978823));
#28408=CARTESIAN_POINT('Ctrl Pts',(-2.90005137117508,0.0827724761696081,
32.340385495299));
#28409=CARTESIAN_POINT('Ctrl Pts',(-1.6397137464159,-2.39342601424305,32.4675414927158));
#28410=CARTESIAN_POINT('Ctrl Pts',(1.12453047387723,-2.67443085431241,32.5946974901326));
#28411=CARTESIAN_POINT('Ctrl Pts',(2.85738199282378,-0.502511112833611,
32.7218534875494));
#28412=CARTESIAN_POINT('Ctrl Pts',(1.9695104363943,2.13029997827834,32.8490094849659));
#28413=CARTESIAN_POINT('Ctrl Pts',(-0.72474940742878,2.80925028240099,32.9761654823829));
#28414=CARTESIAN_POINT('Ctrl Pts',(-2.75428630705593,0.911623015442704,
33.1033214797994));
#28415=CARTESIAN_POINT('Ctrl Pts',(-2.25765698496233,-1.82212371820075,
33.2304774772162));
#28416=CARTESIAN_POINT('Ctrl Pts',(0.309641684678655,-2.88466091776816,
33.3576334746329));
#28417=CARTESIAN_POINT('Ctrl Pts',(2.59294462077817,-1.30145705427967,33.4847894720497));
#28418=CARTESIAN_POINT('Ctrl Pts',(2.49805964487565,1.47541540560368,33.6119454694664));
#28419=CARTESIAN_POINT('Ctrl Pts',(0.112014579002967,2.89906605136737,33.7391014668832));
#28420=CARTESIAN_POINT('Ctrl Pts',(-2.376769568663,1.66377298632484,33.8662574642999));
#28421=CARTESIAN_POINT('Ctrl Pts',(-2.68563323608405,-1.09751418525246,
33.9934134617166));
#28422=CARTESIAN_POINT('Ctrl Pts',(-0.531304869200315,-2.8521474181369,
34.1205694591334));
#28423=CARTESIAN_POINT('Ctrl Pts',(2.11033734788005,-1.99093475005384,34.2477254565501));
#28424=CARTESIAN_POINT('Ctrl Pts',(2.81640219551024,0.696461264250067,34.3748814539669));
#28425=CARTESIAN_POINT('Ctrl Pts',(0.939379163429915,2.74480272297943,34.5020374513837));
#28426=CARTESIAN_POINT('Ctrl Pts',(-1.79931453131619,2.27620394728637,34.6291934488004));
#28427=CARTESIAN_POINT('Ctrl Pts',(-2.88753968137186,-0.281081969612209,
34.7563494462171));
#28428=CARTESIAN_POINT('Ctrl Pts',(-1.32772477658342,-2.57864219291544,
34.8835054436339));
#28429=CARTESIAN_POINT('Ctrl Pts',(1.45050118800113,-2.5148390641304,35.0106614410506));
#28430=CARTESIAN_POINT('Ctrl Pts',(2.89731856153029,-0.136762391780276,
35.1378349338873));
#28431=CARTESIAN_POINT('Ctrl Pts',(2.09139038181383,1.52138208730474,35.2226230942517));
#28432=CARTESIAN_POINT('Ctrl Pts',(1.42649651537617,1.99643151770172,35.265025922144));
#28433=CARTESIAN_POINT('Ctrl Pts',(1.07765335145023,-2.20537355632018,35.));
#28434=CARTESIAN_POINT('Ctrl Pts',(1.12608568679243,-2.17636639516506,35.));
#28435=CARTESIAN_POINT('Ctrl Pts',(1.17334200114935,-2.14562777706368,35.));
#28436=CARTESIAN_POINT('Ctrl Pts',(1.21932057562345,-2.11315743459273,35.));
#28437=CARTESIAN_POINT('Ctrl Pts',(1.28817512261598,-2.06453194441387,35.));
#28438=CARTESIAN_POINT('Ctrl Pts',(1.35416618230553,-2.01202443036934,35.));
#28439=CARTESIAN_POINT('Ctrl Pts',(1.41715084111308,-1.95600074797492,35.));
#28440=CARTESIAN_POINT('Ctrl Pts',(1.48097822413899,-1.89922747806429,35.));
#28441=CARTESIAN_POINT('Ctrl Pts',(1.54171870905508,-1.8388423677737,35.));
#28442=CARTESIAN_POINT('Ctrl Pts',(1.59918018254526,-1.77519516634181,35.));
#28443=CARTESIAN_POINT('Ctrl Pts',(1.65050079776131,-1.71834988661151,35.));
#28444=CARTESIAN_POINT('Ctrl Pts',(1.69920540977255,-1.65890158684205,35.));
#28445=CARTESIAN_POINT('Ctrl Pts',(1.74512376077102,-1.5970884092347,35.));
#28446=CARTESIAN_POINT('Ctrl Pts',(1.75529127963222,-1.58340136177924,35.));
#28447=CARTESIAN_POINT('Ctrl Pts',(1.76532422531884,-1.56959511326082,35.));
#28448=CARTESIAN_POINT('Ctrl Pts',(1.77520514651304,-1.5556944105563,35.));
#28449=CARTESIAN_POINT('Ctrl Pts',(1.82386234832705,-1.48724236205229,35.));
#28450=CARTESIAN_POINT('Ctrl Pts',(1.86891170266444,-1.41640445602353,35.));
#28451=CARTESIAN_POINT('Ctrl Pts',(1.91020321093418,-1.34352891022868,35.));
#28452=CARTESIAN_POINT('Ctrl Pts',(1.95133765088607,-1.27093057492749,35.));
#28453=CARTESIAN_POINT('Ctrl Pts',(1.98874309755711,-1.19630906999412,35.));
#28454=CARTESIAN_POINT('Ctrl Pts',(2.02222286790158,-1.11999139492036,35.));
#28455=CARTESIAN_POINT('Ctrl Pts',(2.05486283066187,-1.04558807474436,35.));
#28456=CARTESIAN_POINT('Ctrl Pts',(2.08377169731716,-0.969571724964817,
35.0000000000001));
#28457=CARTESIAN_POINT('Ctrl Pts',(2.10871830317936,-0.892242812277137,
35.));
#28458=CARTESIAN_POINT('Ctrl Pts',(2.12038288024076,-0.856085225705955,
35.));
#28459=CARTESIAN_POINT('Ctrl Pts',(2.13118046130615,-0.819640713985427,
35.0000000000001));
#28460=CARTESIAN_POINT('Ctrl Pts',(2.14108350125101,-0.782940603525681,
35.0000000000001));
#28461=CARTESIAN_POINT('Ctrl Pts',(2.14499434205243,-0.768447246919899,
35.0000000000001));
#28462=CARTESIAN_POINT('Ctrl Pts',(2.14876589141593,-0.753912606988428,
35.));
#28463=CARTESIAN_POINT('Ctrl Pts',(2.15239164739826,-0.739358800620033,
35.));
#28464=CARTESIAN_POINT('Ctrl Pts',(2.1717999226392,-0.661453866813646,35.));
#28465=CARTESIAN_POINT('Ctrl Pts',(2.18707152189339,-0.582868815048147,
35.0000000000001));
#28466=CARTESIAN_POINT('Ctrl Pts',(2.19803328046829,-0.503902432658308,
35.));
#28467=CARTESIAN_POINT('Ctrl Pts',(2.20867776994429,-0.427221595312448,
35.));
#28468=CARTESIAN_POINT('Ctrl Pts',(2.21525829954634,-0.350180402115567,
35.));
#28469=CARTESIAN_POINT('Ctrl Pts',(2.21756806762709,-0.273055178946711,
35.));
#28470=CARTESIAN_POINT('Ctrl Pts',(2.21922188933148,-0.217832592273324,
35.));
#28471=CARTESIAN_POINT('Ctrl Pts',(2.21868522452938,-0.16256695838533,35.));
#28472=CARTESIAN_POINT('Ctrl Pts',(2.21586615289966,-0.107363829501902,
35.));
#28473=CARTESIAN_POINT('Ctrl Pts',(2.21363495647111,-0.0636724870361094,
35.));
#28474=CARTESIAN_POINT('Ctrl Pts',(2.20997361758447,-0.0200203449622079,
35.));
#28475=CARTESIAN_POINT('Ctrl Pts',(2.20490714034605,0.02353692277755,35.));
#28476=CARTESIAN_POINT('Ctrl Pts',(2.20288214372725,0.0409461236377381,
35.));
#28477=CARTESIAN_POINT('Ctrl Pts',(2.20063263637465,0.0583401394397984,
35.));
#28478=CARTESIAN_POINT('Ctrl Pts',(2.19816005299519,0.0757152900358326,
35.));
#28479=CARTESIAN_POINT('Ctrl Pts',(2.19629318131952,0.0888340292369028,
35.));
#28480=CARTESIAN_POINT('Ctrl Pts',(2.19429889864556,0.101942946564588,35.));
#28481=CARTESIAN_POINT('Ctrl Pts',(2.19218072060339,0.115023983495219,35.));
#28482=CARTESIAN_POINT('Ctrl Pts',(2.17977000031993,0.191667725018257,35.));
#28483=CARTESIAN_POINT('Ctrl Pts',(2.16309238897283,0.267488609930578,35.));
#28484=CARTESIAN_POINT('Ctrl Pts',(2.1423663045745,0.342201061127123,35.));
#28485=CARTESIAN_POINT('Ctrl Pts',(2.12141046041582,0.417741739911314,35.));
#28486=CARTESIAN_POINT('Ctrl Pts',(2.09631530446764,0.492150169822511,35.));
#28487=CARTESIAN_POINT('Ctrl Pts',(2.06725864745812,0.565108591848321,35.));
#28488=CARTESIAN_POINT('Ctrl Pts',(2.04123920834817,0.630440856975602,35.));
#28489=CARTESIAN_POINT('Ctrl Pts',(2.01204219851591,0.69461051592541,35.));
#28490=CARTESIAN_POINT('Ctrl Pts',(1.9797690575023,0.757365501062226,35.));
#28491=CARTESIAN_POINT('Ctrl Pts',(1.9659229546567,0.78428918902653,35.));
#28492=CARTESIAN_POINT('Ctrl Pts',(1.95151036732749,0.81095215532431,35.));
#28493=CARTESIAN_POINT('Ctrl Pts',(1.93653818053308,0.837332865669673,35.));
#28494=CARTESIAN_POINT('Ctrl Pts',(1.92952503385073,0.84968989766354,35.));
#28495=CARTESIAN_POINT('Ctrl Pts',(1.92238807723357,0.861986698760252,35.));
#28496=CARTESIAN_POINT('Ctrl Pts',(1.91513122016409,0.874215517168203,35.));
#28497=CARTESIAN_POINT('Ctrl Pts',(1.87607319733047,0.940033744540321,35.));
#28498=CARTESIAN_POINT('Ctrl Pts',(1.83365076636555,1.0037092427996,35.));
#28499=CARTESIAN_POINT('Ctrl Pts',(1.78802404629311,1.06493571288568,35.));
#28500=CARTESIAN_POINT('Ctrl Pts',(1.74567631435256,1.12176211063583,35.));
#28501=CARTESIAN_POINT('Ctrl Pts',(1.70056750903953,1.17647899830786,35.));
#28502=CARTESIAN_POINT('Ctrl Pts',(1.65280195923282,1.22880897718462,35.));
#28503=CARTESIAN_POINT('Ctrl Pts',(1.63720809247316,1.24589297855049,35.));
#28504=CARTESIAN_POINT('Ctrl Pts',(1.62133091608016,1.26272229886012,35.));
#28505=CARTESIAN_POINT('Ctrl Pts',(1.60517365571296,1.27928641683785,35.));
#28506=CARTESIAN_POINT('Ctrl Pts',(1.59049326620989,1.29433647471657,35.));
#28507=CARTESIAN_POINT('Ctrl Pts',(1.57557759509512,1.30917128746184,35.));
#28508=CARTESIAN_POINT('Ctrl Pts',(1.56045218899025,1.32376086026856,35.));
#28509=CARTESIAN_POINT('Ctrl Pts',(1.50795809437859,1.37439529678875,35.));
#28510=CARTESIAN_POINT('Ctrl Pts',(1.45289725142259,1.42212540384556,35.));
#28511=CARTESIAN_POINT('Ctrl Pts',(1.39539290098519,1.46665275041003,35.));
#28512=CARTESIAN_POINT('Ctrl Pts',(1.33835522673797,1.5108187355767,35.));
#28513=CARTESIAN_POINT('Ctrl Pts',(1.27891299211275,1.55183426341562,35.));
#28514=CARTESIAN_POINT('Ctrl Pts',(1.2171680440423,1.58936089781169,35.));
#28515=CARTESIAN_POINT('Ctrl Pts',(1.19843944143164,1.60074355250463,35.));
#28516=CARTESIAN_POINT('Ctrl Pts',(1.17949888147004,1.61180485329072,35.));
#28517=CARTESIAN_POINT('Ctrl Pts',(1.16034898466929,1.62253437445157,35.));
#28518=CARTESIAN_POINT('',(-1.16151515828124,-1.62372562119785,4.99906051802604));
#28519=CARTESIAN_POINT('Ctrl Pts',(-1.16285328700336,-1.62483580526419,
5.));
#28520=CARTESIAN_POINT('Ctrl Pts',(-1.20343768958331,-1.60238320695503,
5.));
#28521=CARTESIAN_POINT('Ctrl Pts',(-1.24311218157518,-1.57845987066057,
5.));
#28522=CARTESIAN_POINT('Ctrl Pts',(-1.28178686802123,-1.55308297299673,
5.));
#28523=CARTESIAN_POINT('Ctrl Pts',(-1.34195170533604,-1.51360503381216,
5.));
#28524=CARTESIAN_POINT('Ctrl Pts',(-1.39969830932625,-1.470612093931,5.));
#28525=CARTESIAN_POINT('Ctrl Pts',(-1.45494355975133,-1.42445336940955,
5.));
#28526=CARTESIAN_POINT('Ctrl Pts',(-1.48514962863777,-1.39921547833516,
5.));
#28527=CARTESIAN_POINT('Ctrl Pts',(-1.51460761679082,-1.3730302650096,5.));
#28528=CARTESIAN_POINT('Ctrl Pts',(-1.54330127771845,-1.34594885488638,
5.));
#28529=CARTESIAN_POINT('Ctrl Pts',(-1.5566354423299,-1.33336391560645,5.));
#28530=CARTESIAN_POINT('Ctrl Pts',(-1.56980451805764,-1.32058538486767,
5.));
#28531=CARTESIAN_POINT('Ctrl Pts',(-1.58280670788321,-1.30761812162911,
5.));
#28532=CARTESIAN_POINT('Ctrl Pts',(-1.59329282042784,-1.29716017696445,
5.));
#28533=CARTESIAN_POINT('Ctrl Pts',(-1.60366420748321,-1.28658560363462,
5.));
#28534=CARTESIAN_POINT('Ctrl Pts',(-1.61391823577837,-1.27589950014936,
5.));
#28535=CARTESIAN_POINT('Ctrl Pts',(-1.66537461857496,-1.22227489372994,
5.));
#28536=CARTESIAN_POINT('Ctrl Pts',(-1.71389395975769,-1.16582913622441,
5.));
#28537=CARTESIAN_POINT('Ctrl Pts',(-1.75938584450093,-1.10692270980611,
5.));
#28538=CARTESIAN_POINT('Ctrl Pts',(-1.80604256162394,-1.04650796793208,
5.));
#28539=CARTESIAN_POINT('Ctrl Pts',(-1.8495154674723,-0.983504341078151,
5.));
#28540=CARTESIAN_POINT('Ctrl Pts',(-1.88967804425422,-0.918255072861017,
5.));
#28541=CARTESIAN_POINT('Ctrl Pts',(-1.89492548324527,-0.909729933748583,
5.));
#28542=CARTESIAN_POINT('Ctrl Pts',(-1.90011636451144,-0.901166405302841,
5.));
#28543=CARTESIAN_POINT('Ctrl Pts',(-1.90525036092304,-0.89256520611988,
5.));
#28544=CARTESIAN_POINT('Ctrl Pts',(-1.91542554647779,-0.875518291657261,
5.));
#28545=CARTESIAN_POINT('Ctrl Pts',(-1.92537820160518,-0.858321342061171,
5.));
#28546=CARTESIAN_POINT('Ctrl Pts',(-1.93509056212758,-0.841008120409997,
5.));
#28547=CARTESIAN_POINT('Ctrl Pts',(-1.97336409133439,-0.772781854199896,
5.));
#28548=CARTESIAN_POINT('Ctrl Pts',(-2.00796690665968,-0.702658135348163,
5.));
#28549=CARTESIAN_POINT('Ctrl Pts',(-2.03880011439901,-0.631020466449058,
5.));
#28550=CARTESIAN_POINT('Ctrl Pts',(-2.07000444132555,-0.558520541709422,
5.));
#28551=CARTESIAN_POINT('Ctrl Pts',(-2.09734851848856,-0.484469191405541,
5.));
#28552=CARTESIAN_POINT('Ctrl Pts',(-2.12069441174469,-0.409223850782309,
5.));
#28553=CARTESIAN_POINT('Ctrl Pts',(-2.14389726846613,-0.334439526263928,
5.));
#28554=CARTESIAN_POINT('Ctrl Pts',(-2.16315133497366,-0.258474862586811,
5.));
#28555=CARTESIAN_POINT('Ctrl Pts',(-2.17827758432059,-0.181654682439834,
5.));
#28556=CARTESIAN_POINT('Ctrl Pts',(-2.1821185547538,-0.162147927404194,
5.));
#28557=CARTESIAN_POINT('Ctrl Pts',(-2.18569312293337,-0.142585917374366,
5.));
#28558=CARTESIAN_POINT('Ctrl Pts',(-2.18899783935687,-0.122973812778064,
5.));
#28559=CARTESIAN_POINT('Ctrl Pts',(-2.19117568691587,-0.110049201813536,
5.));
#28560=CARTESIAN_POINT('Ctrl Pts',(-2.19323666341748,-0.0971006168957883,
5.));
#28561=CARTESIAN_POINT('Ctrl Pts',(-2.19517866938162,-0.0841366491538629,
5.));
#28562=CARTESIAN_POINT('Ctrl Pts',(-2.20719266907519,-0.00393653269949183,
5.));
#28563=CARTESIAN_POINT('Ctrl Pts',(-2.21462073981273,0.07659741124565,5.));
#28564=CARTESIAN_POINT('Ctrl Pts',(-2.21733626437033,0.157086393268394,
5.));
#28565=CARTESIAN_POINT('Ctrl Pts',(-2.21853337584323,0.192569145045132,
5.));
#28566=CARTESIAN_POINT('Ctrl Pts',(-2.21881410288858,0.228043565217086,
5.));
#28567=CARTESIAN_POINT('Ctrl Pts',(-2.21816479719429,0.26347878735506,5.));
#28568=CARTESIAN_POINT('Ctrl Pts',(-2.21672815511135,0.341882121545975,
5.));
#28569=CARTESIAN_POINT('Ctrl Pts',(-2.21074233778476,0.42009311079211,5.));
#28570=CARTESIAN_POINT('Ctrl Pts',(-2.20044788110181,0.497853177799087,
5.));
#28571=CARTESIAN_POINT('Ctrl Pts',(-2.19015342441887,0.575613244806064,
5.));
#28572=CARTESIAN_POINT('Ctrl Pts',(-2.17555003407646,0.652923153155624,
5.));
#28573=CARTESIAN_POINT('Ctrl Pts',(-2.15682597556414,0.729526478768245,
5.));
#28574=CARTESIAN_POINT('Ctrl Pts',(-2.15351333591367,0.743079054114864,
5.));
#28575=CARTESIAN_POINT('Ctrl Pts',(-2.15007106234521,0.756611497694574,
5.));
#28576=CARTESIAN_POINT('Ctrl Pts',(-2.14650173555311,0.770115975691647,
5.));
#28577=CARTESIAN_POINT('Ctrl Pts',(-2.14362734645692,0.780991170529645,
5.));
#28578=CARTESIAN_POINT('Ctrl Pts',(-2.14067167855265,0.791844072988402,
5.));
#28579=CARTESIAN_POINT('Ctrl Pts',(-2.13763596071444,0.802672401844663,
5.));
#28580=CARTESIAN_POINT('Ctrl Pts',(-2.11580129108532,0.880556116936863,
5.));
#28581=CARTESIAN_POINT('Ctrl Pts',(-2.089821911864,0.957197613250287,5.));
#28582=CARTESIAN_POINT('Ctrl Pts',(-2.05997091461799,1.03232750463359,5.));
#28583=CARTESIAN_POINT('Ctrl Pts',(-2.02958681930464,1.10879911333258,5.));
#28584=CARTESIAN_POINT('Ctrl Pts',(-1.99519138342501,1.18370546487653,5.));
#28585=CARTESIAN_POINT('Ctrl Pts',(-1.95701797710563,1.25676376200865,5.));
#28586=CARTESIAN_POINT('Ctrl Pts',(-1.91845318815751,1.33057110805044,5.));
#28587=CARTESIAN_POINT('Ctrl Pts',(-1.87603226072822,1.40249322828441,5.));
#28588=CARTESIAN_POINT('Ctrl Pts',(-1.82994451627638,1.47222660890071,5.));
#28589=CARTESIAN_POINT('Ctrl Pts',(-1.81136251787481,1.50034223014795,5.));
#28590=CARTESIAN_POINT('Ctrl Pts',(-1.79218388918198,1.52810183780879,5.));
#28591=CARTESIAN_POINT('Ctrl Pts',(-1.77241889109871,1.55548446600544,5.));
#28592=CARTESIAN_POINT('Ctrl Pts',(-1.7626765455579,1.56898161002658,5.));
#28593=CARTESIAN_POINT('Ctrl Pts',(-1.75278959954955,1.58238978774029,5.));
#28594=CARTESIAN_POINT('Ctrl Pts',(-1.74277497729945,1.59568597132499,5.));
#28595=CARTESIAN_POINT('Ctrl Pts',(-1.69111299121085,1.66427640182051,5.));
#28596=CARTESIAN_POINT('Ctrl Pts',(-1.63598077918668,1.72999683047024,5.));
#28597=CARTESIAN_POINT('Ctrl Pts',(-1.57763490532952,1.79255088797377,5.));
#28598=CARTESIAN_POINT('Ctrl Pts',(-1.51919867470482,1.85520181920732,5.));
#28599=CARTESIAN_POINT('Ctrl Pts',(-1.45753838720462,1.91467750037871,5.));
#28600=CARTESIAN_POINT('Ctrl Pts',(-1.39286260070177,1.97066278379734,5.));
#28601=CARTESIAN_POINT('Ctrl Pts',(-1.32955699149425,2.02546200101775,5.));
#28602=CARTESIAN_POINT('Ctrl Pts',(-1.2633617398569,2.0769179289258,5.));
#28603=CARTESIAN_POINT('Ctrl Pts',(-1.19443292968338,2.12470580679072,5.));
#28604=CARTESIAN_POINT('Ctrl Pts',(-1.15551571854606,2.15168684603965,5.));
#28605=CARTESIAN_POINT('Ctrl Pts',(-1.11572644903728,2.17749801406487,5.));
#28606=CARTESIAN_POINT('Ctrl Pts',(-1.07508846035129,2.20207516956608,5.));
#28607=CARTESIAN_POINT('Ctrl Pts',(-1.16055672420885,-1.62238579024646,
4.99906051802604));
#28608=CARTESIAN_POINT('Ctrl Pts',(-1.15296330661381,-1.6278176621863,4.99937367868403));
#28609=CARTESIAN_POINT('Ctrl Pts',(-1.14533175338124,-1.63319622287715,
4.99968683934202));
#28610=CARTESIAN_POINT('Ctrl Pts',(-1.13766281679009,-1.63852094212837,
5.));
#28611=CARTESIAN_POINT('Ctrl Pts',(1.42649653067546,-1.99643148636002,4.73497408903594));
#28612=CARTESIAN_POINT('Ctrl Pts',(2.09139037751359,-1.52138205586238,4.77737691639768));
#28613=CARTESIAN_POINT('Ctrl Pts',(2.89731909148689,0.136761439869381,4.86216507623168));
#28614=CARTESIAN_POINT('Ctrl Pts',(1.450500801584,2.51483958866074,4.98933856853792));
#28615=CARTESIAN_POINT('Ctrl Pts',(-1.32772456687247,2.57864173676513,5.11649456595466));
#28616=CARTESIAN_POINT('Ctrl Pts',(-2.88753967722034,0.281082199765186,
5.24365056337139));
#28617=CARTESIAN_POINT('Ctrl Pts',(-1.79931443848377,-2.27620402637004,
5.37080656078811));
#28618=CARTESIAN_POINT('Ctrl Pts',(0.939379116963788,-2.74480255219456,
5.49796255820487));
#28619=CARTESIAN_POINT('Ctrl Pts',(2.81640211996325,-0.696461296195236,
5.6251185556216));
#28620=CARTESIAN_POINT('Ctrl Pts',(2.11033728095063,1.99093472149687,5.75227455303834));
#28621=CARTESIAN_POINT('Ctrl Pts',(-0.5313048515864,2.85214731506389,5.87943055045507));
#28622=CARTESIAN_POINT('Ctrl Pts',(-2.68563315664284,1.09751416275767,6.00658654787181));
#28623=CARTESIAN_POINT('Ctrl Pts',(-2.37676949737353,-1.66377294249894,
6.13374254528854));
#28624=CARTESIAN_POINT('Ctrl Pts',(0.112014575536817,-2.89906596147756,
6.26089854270528));
#28625=CARTESIAN_POINT('Ctrl Pts',(2.49805957031855,-1.47541536341306,6.38805454012201));
#28626=CARTESIAN_POINT('Ctrl Pts',(2.59294454333804,1.30145701646242,6.51521053753876));
#28627=CARTESIAN_POINT('Ctrl Pts',(0.309641675430814,2.88466083104124,6.64236653495548));
#28628=CARTESIAN_POINT('Ctrl Pts',(-2.25765691753952,1.82212366411349,6.76952253237223));
#28629=CARTESIAN_POINT('Ctrl Pts',(-2.75428622481087,-0.911622988399715,
6.89667852978896));
#28630=CARTESIAN_POINT('Ctrl Pts',(-0.724749385783444,-2.80925019841095,
7.0238345272057));
#28631=CARTESIAN_POINT('Ctrl Pts',(1.96951037757824,-2.13029991471801,7.15099052462243));
#28632=CARTESIAN_POINT('Ctrl Pts',(2.85738190749746,0.502511097857537,7.27814652203917));
#28633=CARTESIAN_POINT('Ctrl Pts',(1.12453044029566,2.6744307744314,7.4053025194559));
#28634=CARTESIAN_POINT('Ctrl Pts',(-1.6397136974498,2.39342594277931,7.53245851687264));
#28635=CARTESIAN_POINT('Ctrl Pts',(-2.90005128457351,-0.082772473702611,
7.65961451428937));
#28636=CARTESIAN_POINT('Ctrl Pts',(-1.50053054250907,-2.48305392933439,
7.78677051170611));
#28637=CARTESIAN_POINT('Ctrl Pts',(1.27524126036236,-2.60593715651519,7.91392650912285));
#28638=CARTESIAN_POINT('Ctrl Pts',(2.88139199384887,-0.338716563466436,
8.04108250653958));
#28639=CARTESIAN_POINT('Ctrl Pts',(1.84479825889604,2.2391668351018,8.16823850395633));
#28640=CARTESIAN_POINT('Ctrl Pts',(-0.88380073035943,2.76333946557476,8.29539450137305));
#28641=CARTESIAN_POINT('Ctrl Pts',(-2.80179862960237,0.75304260940714,8.42255049878981));
#28642=CARTESIAN_POINT('Ctrl Pts',(-2.15005320849511,-1.94792708615075,
8.54970649620651));
#28643=CARTESIAN_POINT('Ctrl Pts',(0.473670074415001,-2.86230421044614,
8.67686249362328));
#28644=CARTESIAN_POINT('Ctrl Pts',(2.66295438770209,-1.15144372917626,8.80401849103999));
#28645=CARTESIAN_POINT('Ctrl Pts',(2.4098400297151,1.61549365941736,8.93117448845674));
#28646=CARTESIAN_POINT('Ctrl Pts',(-0.0535225074078562,2.90073853934904,
9.05833048587348));
#28647=CARTESIAN_POINT('Ctrl Pts',(-2.46779546884147,1.52549475791126,9.1854864832902));
#28648=CARTESIAN_POINT('Ctrl Pts',(-2.61866489550199,-1.24889667207306,
9.31264248070695));
#28649=CARTESIAN_POINT('Ctrl Pts',(-0.367756923792801,-2.87782966442698,
9.43979847812368));
#28650=CARTESIAN_POINT('Ctrl Pts',(2.22044898518867,-1.86728547271856,9.56695447554042));
#28651=CARTESIAN_POINT('Ctrl Pts',(2.77211169384673,0.85588871314536,9.69411047295715));
#28652=CARTESIAN_POINT('Ctrl Pts',(0.781259236293708,2.79406204980448,9.82126647037389));
#28653=CARTESIAN_POINT('Ctrl Pts',(-1.92614568248534,2.16958787383562,9.94842246779061));
#28654=CARTESIAN_POINT('Ctrl Pts',(-2.86693541727973,-0.444780896171051,
10.0755784652073));
#28655=CARTESIAN_POINT('Ctrl Pts',(-1.17823991337992,-2.65120716636218,
10.2027344626241));
#28656=CARTESIAN_POINT('Ctrl Pts',(1.59110932314304,-2.42600903837123,10.3298904600408));
#28657=CARTESIAN_POINT('Ctrl Pts',(2.90113078648473,0.0242671004068106,
10.4570464574575));
#28658=CARTESIAN_POINT('Ctrl Pts',(1.55030382868508,2.45228602964989,10.5842024548743));
#28659=CARTESIAN_POINT('Ctrl Pts',(-1.22242506957978,2.63112631428339,10.711358452291));
#28660=CARTESIAN_POINT('Ctrl Pts',(-2.8739746568298,0.396759882487747,10.8385144497078));
#28661=CARTESIAN_POINT('Ctrl Pts',(-1.88958278165034,-2.20150531313058,
10.9656704471245));
#28662=CARTESIAN_POINT('Ctrl Pts',(0.827889651149327,-2.78060199560661,
11.0928264445412));
#28663=CARTESIAN_POINT('Ctrl Pts',(2.78604131102751,-0.809396408257279,
11.219982441958));
#28664=CARTESIAN_POINT('Ctrl Pts',(2.18890188984948,1.90416838779164,11.3471384393747));
#28665=CARTESIAN_POINT('Ctrl Pts',(-0.415846483249164,2.87127505384296,
11.4742944367915));
#28666=CARTESIAN_POINT('Ctrl Pts',(-2.6391903145238,1.2049162693629,11.6014504342082));
#28667=CARTESIAN_POINT('Ctrl Pts',(-2.44193131940839,-1.56656316940748,
11.7286064316249));
#28668=CARTESIAN_POINT('Ctrl Pts',(-0.00499077458373336,-2.9012279856331,
11.8557624290416));
#28669=CARTESIAN_POINT('Ctrl Pts',(2.43652719044317,-1.57495523196144,11.9829184264584));
#28670=CARTESIAN_POINT('Ctrl Pts',(2.64332014480819,1.19582914519711,12.1100744238751));
#28671=CARTESIAN_POINT('Ctrl Pts',(0.425722490293999,2.86982736304983,12.2372304212918));
#28672=CARTESIAN_POINT('Ctrl Pts',(-2.1823377457144,1.9116879180666,12.3643864187086));
#28673=CARTESIAN_POINT('Ctrl Pts',(-2.78880950727922,-0.799806391922873,
12.4915424161253));
#28674=CARTESIAN_POINT('Ctrl Pts',(-0.837451263772367,-2.77773722897932,
12.6186984135421));
#28675=CARTESIAN_POINT('Ctrl Pts',(1.88199743721141,-2.2079932922863,12.7458544109588));
#28676=CARTESIAN_POINT('Ctrl Pts',(2.87532267877552,0.386869778311558,12.8730104083755));
#28677=CARTESIAN_POINT('Ctrl Pts',(1.23147008412008,2.62690505431182,13.0001664057923));
#28678=CARTESIAN_POINT('Ctrl Pts',(-1.54185769458389,2.45760525351491,13.127322403209));
#28679=CARTESIAN_POINT('Ctrl Pts',(-2.90103012690677,0.034248142007324,
13.2544784006258));
#28680=CARTESIAN_POINT('Ctrl Pts',(-1.59944646066832,-2.42052055391133,
13.3816343980425));
#28681=CARTESIAN_POINT('Ctrl Pts',(1.16911160375855,-2.65524514695135,13.5087903954592));
#28682=CARTESIAN_POINT('Ctrl Pts',(2.86538820487081,-0.454641801684438,
13.6359463928759));
#28683=CARTESIAN_POINT('Ctrl Pts',(1.93359863385237,2.16294823230143,13.7631023902927));
#28684=CARTESIAN_POINT('Ctrl Pts',(-0.771641791562487,2.79673339415216,
13.8902583877094));
#28685=CARTESIAN_POINT('Ctrl Pts',(-2.76915064819359,0.865420949631279,
14.0174143851262));
#28686=CARTESIAN_POINT('Ctrl Pts',(-2.22686013953083,-1.85963508555317,
14.1445703825429));
#28687=CARTESIAN_POINT('Ctrl Pts',(0.357853728318975,-2.87907788042974,
14.2717263799596));
#28688=CARTESIAN_POINT('Ctrl Pts',(2.6143526351498,-1.25789865710119,14.3988823773764));
#28689=CARTESIAN_POINT('Ctrl Pts',(2.47302924663558,1.51699541124444,14.5260383747931));
#28690=CARTESIAN_POINT('Ctrl Pts',(0.0635020263596358,2.90053723042815,
14.6531943722098));
#28691=CARTESIAN_POINT('Ctrl Pts',(-2.40426774794574,1.62377502402257,14.7803503696266));
#28692=CARTESIAN_POINT('Ctrl Pts',(-2.66690010792791,-1.14227516246556,
14.9075063670433));
#28693=CARTESIAN_POINT('Ctrl Pts',(-0.483514875535344,-2.86065763375971,
15.0346623644601));
#28694=CARTESIAN_POINT('Ctrl Pts',(2.14333874482516,-1.95531270066527,15.1618183618768));
#28695=CARTESIAN_POINT('Ctrl Pts',(2.80437285035799,0.743398714437,15.2889743592935));
#28696=CARTESIAN_POINT('Ctrl Pts',(0.893302621288155,2.7602824419344,15.4161303567102));
#28697=CARTESIAN_POINT('Ctrl Pts',(-1.83708360709109,2.2455005128053,15.543286354127));
#28698=CARTESIAN_POINT('Ctrl Pts',(-2.88254027689778,-0.328801284233579,
15.6704423515437));
#28699=CARTESIAN_POINT('Ctrl Pts',(-1.2841993004931,-2.60153433363172,15.7975983489605));
#28700=CARTESIAN_POINT('Ctrl Pts',(1.49197884790902,-2.48820173013437,15.9247543463772));
#28701=CARTESIAN_POINT('Ctrl Pts',(2.89974934632536,-0.0927494524904423,
16.0519103437939));
#28702=CARTESIAN_POINT('Ctrl Pts',(1.64793844778422,2.38777042547358,16.1790663412107));
#28703=CARTESIAN_POINT('Ctrl Pts',(-1.11532255061193,2.67828384241628,16.3062223386274));
#28704=CARTESIAN_POINT('Ctrl Pts',(-2.85563613082048,0.512338775425298,
16.4333783360441));
#28705=CARTESIAN_POINT('Ctrl Pts',(-1.97682791016231,-2.12351127759072,
16.5605343334609));
#28706=CARTESIAN_POINT('Ctrl Pts',(0.715080032896517,-2.81172709895614,
16.6876903308776));
#28707=CARTESIAN_POINT('Ctrl Pts',(2.75113351210751,-0.92109344314821,16.8148463282943));
#28708=CARTESIAN_POINT('Ctrl Pts',(2.26391251636448,1.8143452953338,16.9420023257111));
#28709=CARTESIAN_POINT('Ctrl Pts',(-0.299715400718915,2.88570951605034,
17.0691583231278));
#28710=CARTESIAN_POINT('Ctrl Pts',(-2.58845145339209,1.31036933949326,17.1963143205446));
#28711=CARTESIAN_POINT('Ctrl Pts',(-2.5031211609541,-1.46681054878789,17.3234703179612));
#28712=CARTESIAN_POINT('Ctrl Pts',(-0.121987445906368,-2.898666554727,17.4506263153781));
#28713=CARTESIAN_POINT('Ctrl Pts',(2.37103026428945,-1.67193427450816,17.5777823127947));
#28714=CARTESIAN_POINT('Ctrl Pts',(2.68939519267899,1.08825650930596,17.7049383102115));
#28715=CARTESIAN_POINT('Ctrl Pts',(0.541110569934063,2.85032420674513,17.8320943076282));
#28716=CARTESIAN_POINT('Ctrl Pts',(-2.10346784707187,1.99814207422457,17.959250305045));
#28717=CARTESIAN_POINT('Ctrl Pts',(-2.81879539201196,-0.686688626980042,
18.0864063024617));
#28718=CARTESIAN_POINT('Ctrl Pts',(-0.948790588856309,-2.74170478916847,
18.2135622998784));
#28719=CARTESIAN_POINT('Ctrl Pts',(1.79142246279098,-2.2820942776887,18.3407182972952));
#28720=CARTESIAN_POINT('Ctrl Pts',(2.88858527557254,0.270599035839221,18.4678742947119));
#28721=CARTESIAN_POINT('Ctrl Pts',(1.33640611258182,2.57510532497325,18.5950302921287));
#28722=CARTESIAN_POINT('Ctrl Pts',(-1.44149307352296,2.51778602177329,18.7221862895454));
#28723=CARTESIAN_POINT('Ctrl Pts',(-2.89728896575409,0.151213033073416,
18.8493422869621));
#28724=CARTESIAN_POINT('Ctrl Pts',(-1.69576006379414,-2.35404896688503,
18.9764982843789));
#28725=CARTESIAN_POINT('Ctrl Pts',(1.06107979119196,-2.70023302868023,19.1036542817956));
#28726=CARTESIAN_POINT('Ctrl Pts',(2.84472240176183,-0.569827332940471,
19.2308102792123));
#28727=CARTESIAN_POINT('Ctrl Pts',(2.01925302517959,2.08321049170619,19.3579662766291));
#28728=CARTESIAN_POINT('Ctrl Pts',(-0.658227384122869,2.82557701067276,
19.4851222740458));
#28729=CARTESIAN_POINT('Ctrl Pts',(-2.73199723202815,0.976391241584123,
19.6122782714625));
#28730=CARTESIAN_POINT('Ctrl Pts',(-2.30004394767405,-1.7683174407384,19.7394342688793));
#28731=CARTESIAN_POINT('Ctrl Pts',(0.241455150758871,-2.89116726299665,
19.866590266296));
#28732=CARTESIAN_POINT('Ctrl Pts',(2.56149730569025,-1.36230697179206,19.9937462637128));
#28733=CARTESIAN_POINT('Ctrl Pts',(2.53219482116047,1.41602899692759,20.1209022611294));
#28734=CARTESIAN_POINT('Ctrl Pts',(0.180423241719181,2.89561671950885,20.2480582585463));
#28735=CARTESIAN_POINT('Ctrl Pts',(-2.3368282602758,1.71941339253478,20.375214255963));
#28736=CARTESIAN_POINT('Ctrl Pts',(-2.71079624820093,-1.03379516017022,
20.5023702533797));
#28737=CARTESIAN_POINT('Ctrl Pts',(-0.598486143920099,-2.83883128557993,
20.6295262507964));
#28738=CARTESIAN_POINT('Ctrl Pts',(2.0627412716876,-2.04015861602187,20.7566822482131));
#28739=CARTESIAN_POINT('Ctrl Pts',(2.83207126524092,0.629699198862666,20.8838382456299));
#28740=CARTESIAN_POINT('Ctrl Pts',(1.00389259431695,2.72201182795505,21.0109942430466));
#28741=CARTESIAN_POINT('Ctrl Pts',(-1.74503257898048,2.31775970082069,21.1381502404634));
#28742=CARTESIAN_POINT('Ctrl Pts',(-2.89345521573194,-0.212286709440951,
21.2653062378801));
#28743=CARTESIAN_POINT('Ctrl Pts',(-1.38806928297995,-2.54762877949265,
21.3924622352968));
#28744=CARTESIAN_POINT('Ctrl Pts',(1.39042090872455,-2.54634609372591,21.5196182327136));
#28745=CARTESIAN_POINT('Ctrl Pts',(2.89364998606044,-0.209615101135453,
21.6467742301303));
#28746=CARTESIAN_POINT('Ctrl Pts',(1.74289185516227,2.3193698958253,21.773930227547));
#28747=CARTESIAN_POINT('Ctrl Pts',(-1.00640539111578,2.72108377695078,21.9010862249638));
#28748=CARTESIAN_POINT('Ctrl Pts',(-2.83265145733194,0.627084088242402,
22.0282422223805));
#28749=CARTESIAN_POINT('Ctrl Pts',(-2.06085672063136,-2.04206226875681,
22.1553982197973));
#28750=CARTESIAN_POINT('Ctrl Pts',(0.601106972545297,-2.83827749524409,
22.282554217214));
#28751=CARTESIAN_POINT('Ctrl Pts',(2.71174959247513,-1.03129185013877,22.4097102146307));
#28752=CARTESIAN_POINT('Ctrl Pts',(2.33523973541819,1.72157024561173,22.5368662120475));
#28753=CARTESIAN_POINT('Ctrl Pts',(-0.18309667834599,2.89544890109121,22.6640222094642));
#28754=CARTESIAN_POINT('Ctrl Pts',(-2.53350115682382,1.41369042609194,22.7911782068809));
#28755=CARTESIAN_POINT('Ctrl Pts',(-2.56023840027064,-1.36467141328281,
22.9183342042977));
#28756=CARTESIAN_POINT('Ctrl Pts',(-0.238785642480034,-2.8913889654277,
23.0454902017144));
#28757=CARTESIAN_POINT('Ctrl Pts',(2.3016756490672,-1.76619306389272,23.1726461991311));
#28758=CARTESIAN_POINT('Ctrl Pts',(2.73109456867753,0.978913269596307,23.2998021965479));
#28759=CARTESIAN_POINT('Ctrl Pts',(0.655618257466982,2.82618354551285,23.4269581939646));
#28760=CARTESIAN_POINT('Ctrl Pts',(-2.02117558598974,2.08134523398946,23.5541141913814));
#28761=CARTESIAN_POINT('Ctrl Pts',(-2.84419506950227,-0.572453613029604,
23.6812701887981));
#28762=CARTESIAN_POINT('Ctrl Pts',(-1.05858622251712,-2.70121156926823,
23.8084261862149));
#28763=CARTESIAN_POINT('Ctrl Pts',(1.6979328267756,-2.35248227372907,23.9355821836315));
#28764=CARTESIAN_POINT('Ctrl Pts',(2.89714811631462,0.153888026130212,24.0627381810483));
#28765=CARTESIAN_POINT('Ctrl Pts',(1.43916779543132,2.51911587447759,24.189894178465));
#28766=CARTESIAN_POINT('Ctrl Pts',(-1.33878312935259,2.57387032793273,24.3170501758818));
#28767=CARTESIAN_POINT('Ctrl Pts',(-2.88883388755873,0.26793189907875,24.4442061732985));
#28768=CARTESIAN_POINT('Ctrl Pts',(-1.78931464896918,-2.28374731952464,
24.5713621707153));
#28769=CARTESIAN_POINT('Ctrl Pts',(0.951321591588982,-2.74082760527331,
24.698518168132));
#28770=CARTESIAN_POINT('Ctrl Pts',(2.81942820791591,-0.684085749639387,
24.8256741655487));
#28771=CARTESIAN_POINT('Ctrl Pts',(2.10162207239324,2.00008334758359,24.9528301629654));
#28772=CARTESIAN_POINT('Ctrl Pts',(-0.543742034391811,2.84982338619205,
25.0799861603822));
#28773=CARTESIAN_POINT('Ctrl Pts',(-2.69039883006224,1.08577293558616,25.2071421577989));
#28774=CARTESIAN_POINT('Ctrl Pts',(-2.36948556216938,-1.67412272642197,
25.3342981552157));
#28775=CARTESIAN_POINT('Ctrl Pts',(0.12466372334371,-2.89855268859024,25.4614541526324));
#28776=CARTESIAN_POINT('Ctrl Pts',(2.50447439545198,-1.46449879992339,25.5886101500491));
#28777=CARTESIAN_POINT('Ctrl Pts',(2.58724049033111,1.31275868979903,25.7157661474659));
#28778=CARTESIAN_POINT('Ctrl Pts',(0.297050906727364,2.8859850123076,25.8429221448826));
#28779=CARTESIAN_POINT('Ctrl Pts',(-2.26558673052715,1.81225425890269,25.9700781422993));
#28780=CARTESIAN_POINT('Ctrl Pts',(-2.75028189687831,-0.923633163195802,
26.0972341397161));
#28781=CARTESIAN_POINT('Ctrl Pts',(-0.712483669586427,-2.81238613156592,
26.2243901371328));
#28782=CARTESIAN_POINT('Ctrl Pts',(1.97878769864067,-2.12168517366737,26.3515461345495));
#28783=CARTESIAN_POINT('Ctrl Pts',(2.85516187290784,0.514975156628957,26.4787021319663));
#28784=CARTESIAN_POINT('Ctrl Pts',(1.11284922442921,2.67931247452382,26.605858129383));
#28785=CARTESIAN_POINT('Ctrl Pts',(-1.6501423660625,2.38624787148722,26.7330141267998));
#28786=CARTESIAN_POINT('Ctrl Pts',(-2.89966247507162,-0.0954267421280935,
26.8601701242165));
#28787=CARTESIAN_POINT('Ctrl Pts',(-1.48968086337897,-2.48957820880047,
26.9873261216332));
#28788=CARTESIAN_POINT('Ctrl Pts',(1.28660074133443,-2.60034752770651,27.11448211905));
#28789=CARTESIAN_POINT('Ctrl Pts',(2.88284262940784,-0.326139703992787,
27.2416381164667));
#28790=CARTESIAN_POINT('Ctrl Pts',(1.83500956071125,2.24719572902539,27.3687941138834));
#28791=CARTESIAN_POINT('Ctrl Pts',(-0.895850800358501,2.75945648198132,
27.4959501113002));
#28792=CARTESIAN_POINT('Ctrl Pts',(-2.80505803264929,0.740809129210285,
27.6231061087169));
#28793=CARTESIAN_POINT('Ctrl Pts',(-2.14153249737378,-1.95729080495048,
27.7502621061337));
#28794=CARTESIAN_POINT('Ctrl Pts',(0.486155905362252,-2.86020998672004,
27.8774181035504));
#28795=CARTESIAN_POINT('Ctrl Pts',(2.66795363014677,-1.13981233535976,28.0045741009671));
#28796=CARTESIAN_POINT('Ctrl Pts',(2.40276749693843,1.62599418452461,28.1317300983839));
#28797=CARTESIAN_POINT('Ctrl Pts',(-0.0661800559145379,2.90047736289232,
28.2588860958006));
#28798=CARTESIAN_POINT('Ctrl Pts',(-2.4744288294806,1.51471142475617,28.3860420932174));
#28799=CARTESIAN_POINT('Ctrl Pts',(-2.61319010705968,-1.26031194424914,
28.5131980906341));
#28800=CARTESIAN_POINT('Ctrl Pts',(-0.355195332514304,-2.87940705844306,
28.6403540880508));
#28801=CARTESIAN_POINT('Ctrl Pts',(2.22857618540315,-1.85757824015722,28.7675100854675));
#28802=CARTESIAN_POINT('Ctrl Pts',(2.76835042751757,0.867977328571968,28.8946660828843));
#28803=CARTESIAN_POINT('Ctrl Pts',(0.769059247782621,2.79744465644124,29.021822080301));
#28804=CARTESIAN_POINT('Ctrl Pts',(-1.93559485276915,2.16116202501923,29.1489780777177));
#28805=CARTESIAN_POINT('Ctrl Pts',(-2.86496721423027,-0.457287211539142,
29.2761340751345));
#28806=CARTESIAN_POINT('Ctrl Pts',(-1.16665952620171,-2.65632345213726,
29.4032900725512));
#28807=CARTESIAN_POINT('Ctrl Pts',(1.60168063770319,-2.41904275846012,29.5304460699679));
#28808=CARTESIAN_POINT('Ctrl Pts',(2.90099726917742,0.0369266391210829,
29.6576020673847));
#28809=CARTESIAN_POINT('Ctrl Pts',(1.53958793842119,2.45902779819983,29.7847580648014));
#28810=CARTESIAN_POINT('Ctrl Pts',(-1.23389497214082,2.62576692228718,29.9119140622182));
#28811=CARTESIAN_POINT('Ctrl Pts',(-2.8756786488143,0.38421483730457,30.0390700596349));
#28812=CARTESIAN_POINT('Ctrl Pts',(-1.87995800198274,-2.20972999328701,
30.1662260570517));
#28813=CARTESIAN_POINT('Ctrl Pts',(0.840015582597118,-2.77696282896395,
30.2933820544683));
#28814=CARTESIAN_POINT('Ctrl Pts',(2.78954677722976,-0.797231152236704,
30.4205380518851));
#28815=CARTESIAN_POINT('Ctrl Pts',(2.18057176026088,1.91370204859638,30.5476940493018));
#28816=CARTESIAN_POINT('Ctrl Pts',(-0.428372011136305,2.86943307162567,
30.6748500467186));
#28817=CARTESIAN_POINT('Ctrl Pts',(-2.644423123295,1.19338806656412,30.8020060441353));
#28818=CARTESIAN_POINT('Ctrl Pts',(-2.43507200084404,-1.5772041983036,30.929162041552));
#28819=CARTESIAN_POINT('Ctrl Pts',(0.00766946685548332,-2.9012221410661,
31.0563180389688));
#28820=CARTESIAN_POINT('Ctrl Pts',(2.44337668124933,-1.56430787437987,31.1834740363855));
#28821=CARTESIAN_POINT('Ctrl Pts',(2.63807669433218,1.20735251159128,31.3106300338023));
#28822=CARTESIAN_POINT('Ctrl Pts',(0.413195267015108,2.87165777980301,31.437786031219));
#28823=CARTESIAN_POINT('Ctrl Pts',(-2.19065906928768,1.90214656995545,31.5649420286357));
#28824=CARTESIAN_POINT('Ctrl Pts',(-2.78529281055713,-0.81196840581493,
31.6920980260525));
#28825=CARTESIAN_POINT('Ctrl Pts',(-0.825321977219055,-2.78136519891875,
31.8192540234692));
#28826=CARTESIAN_POINT('Ctrl Pts',(1.89161461849208,-2.19975972780952,31.946410020886));
#28827=CARTESIAN_POINT('Ctrl Pts',(2.87360710560243,0.399413242382576,32.0735660183027));
#28828=CARTESIAN_POINT('Ctrl Pts',(1.21999523645203,2.63225385861773,32.2007220157194));
#28829=CARTESIAN_POINT('Ctrl Pts',(-1.55256735241157,2.45085358489712,32.3278780131362));
#28830=CARTESIAN_POINT('Ctrl Pts',(-2.90115196177673,0.0215885025613874,
32.4550340105528));
#28831=CARTESIAN_POINT('Ctrl Pts',(-1.58886870698235,-2.42747710308629,
32.5821900079697));
#28832=CARTESIAN_POINT('Ctrl Pts',(1.18068723986726,-2.65011810889251,32.7093460053863));
#28833=CARTESIAN_POINT('Ctrl Pts',(2.86734490252435,-0.442133793245194,
32.8365020028031));
#28834=CARTESIAN_POINT('Ctrl Pts',(1.92414160704232,2.1713655796952,32.9636580002198));
#28835=CARTESIAN_POINT('Ctrl Pts',(-0.783838497306285,2.79333909281486,
33.0908139976365));
#28836=CARTESIAN_POINT('Ctrl Pts',(-2.77290104593788,0.853329690074369,
33.2179699950533));
#28837=CARTESIAN_POINT('Ctrl Pts',(-2.21872341885293,-1.86933638013305,
33.34512599247));
#28838=CARTESIAN_POINT('Ctrl Pts',(0.370412787773323,-2.87748589584457,
33.4722819898868));
#28839=CARTESIAN_POINT('Ctrl Pts',(2.61981892166448,-1.24648404142433,33.5994379873035));
#28840=CARTESIAN_POINT('Ctrl Pts',(2.46638204316312,1.5277834946993,33.7265939847202));
#28841=CARTESIAN_POINT('Ctrl Pts',(0.0508516573559641,2.90076597833909,
33.853749982137));
#28842=CARTESIAN_POINT('Ctrl Pts',(-2.41134471984188,1.61330751771713,33.9809059795537));
#28843=CARTESIAN_POINT('Ctrl Pts',(-2.66186317555782,-1.15397732778452,
34.1080619769705));
#28844=CARTESIAN_POINT('Ctrl Pts',(-0.471078502934338,-2.86259658701582,
34.2352179743872));
#28845=CARTESIAN_POINT('Ctrl Pts',(2.15194878338818,-1.94621521211644,34.3623739718039));
#28846=CARTESIAN_POINT('Ctrl Pts',(2.80091529373492,0.756152172428542,34.4895299692206));
#28847=CARTESIAN_POINT('Ctrl Pts',(0.881605804944954,2.76315344068171,34.6166859666374));
#28848=CARTESIAN_POINT('Ctrl Pts',(-1.84755030053663,2.23940363022795,34.7438419640541));
#28849=CARTESIAN_POINT('Ctrl Pts',(-2.87978905100241,-0.345521145569797,
34.8710057240579));
#28850=CARTESIAN_POINT('Ctrl Pts',(-1.81030869183372,-1.84686632628722,
34.9557841515895));
#28851=CARTESIAN_POINT('Ctrl Pts',(-1.07608793779701,-2.20514531190313,
34.9981772466487));
#28852=CARTESIAN_POINT('Ctrl Pts',(1.33686590078714,-1.87099030385222,4.82398558717196));
#28853=CARTESIAN_POINT('Ctrl Pts',(1.95998267139732,-1.42578951214757,4.8663884145337));
#28854=CARTESIAN_POINT('Ctrl Pts',(2.71527270751542,0.128168349219389,4.9511765743677));
#28855=CARTESIAN_POINT('Ctrl Pts',(1.35936191852075,2.35682542490182,5.07835006667395));
#28856=CARTESIAN_POINT('Ctrl Pts',(-1.24430004624595,2.41661871171578,5.20550606409067));
#28857=CARTESIAN_POINT('Ctrl Pts',(-2.70610776026073,0.263421045970905,
5.33266206150741));
#28858=CARTESIAN_POINT('Ctrl Pts',(-1.68625865249321,-2.13318397952756,
5.45981805892415));
#28859=CARTESIAN_POINT('Ctrl Pts',(0.880355389848543,-2.5723391943232,5.58697405634089));
#28860=CARTESIAN_POINT('Ctrl Pts',(2.63943996786359,-0.65270075186278,5.71413005375762));
#28861=CARTESIAN_POINT('Ctrl Pts',(1.97773908971723,1.86583891557173,5.84128605117436));
#28862=CARTESIAN_POINT('Ctrl Pts',(-0.497921532744458,2.67293919581084,
5.96844204859109));
#28863=CARTESIAN_POINT('Ctrl Pts',(-2.5168875717063,1.02855438360375,6.09559804600783));
#28864=CARTESIAN_POINT('Ctrl Pts',(-2.22743065036776,-1.55923359478898,
6.22275404342456));
#28865=CARTESIAN_POINT('Ctrl Pts',(0.104976397212366,-2.7169098169464,6.3499100408413));
#28866=CARTESIAN_POINT('Ctrl Pts',(2.3410997404337,-1.38271103113762,6.47706603825804));
#28867=CARTESIAN_POINT('Ctrl Pts',(2.43002283432085,1.21968295697496,6.60422203567477));
#28868=CARTESIAN_POINT('Ctrl Pts',(0.290186052643345,2.70340979976262,6.73137803309151));
#28869=CARTESIAN_POINT('Ctrl Pts',(-2.11580223563929,1.70763471287051,6.85853403050825));
#28870=CARTESIAN_POINT('Ctrl Pts',(-2.58122698217429,-0.854343253809485,
6.98569002792498));
#28871=CARTESIAN_POINT('Ctrl Pts',(-0.679211424378038,-2.63273742085926,
7.11284602534172));
#28872=CARTESIAN_POINT('Ctrl Pts',(1.84576072104714,-1.99644741728735,7.24000202275845));
#28873=CARTESIAN_POINT('Ctrl Pts',(2.67784488466356,0.470936968332268,7.36715802017519));
#28874=CARTESIAN_POINT('Ctrl Pts',(1.05387315545497,2.50638906542604,7.49431401759193));
#28875=CARTESIAN_POINT('Ctrl Pts',(-1.5366860570886,2.24304052632082,7.62147001500866));
#28876=CARTESIAN_POINT('Ctrl Pts',(-2.71783322953095,-0.077571655617246,
7.7486260124254));
#28877=CARTESIAN_POINT('Ctrl Pts',(-1.40624815569671,-2.32703694440175,
7.87578200984213));
#28878=CARTESIAN_POINT('Ctrl Pts',(1.19511440763756,-2.44219908651995,8.00293800725887));
#28879=CARTESIAN_POINT('Ctrl Pts',(2.70034635243996,-0.317434086934477,
8.1300940046756));
#28880=CARTESIAN_POINT('Ctrl Pts',(1.72888460162041,2.09847393502153,8.25725000209234));
#28881=CARTESIAN_POINT('Ctrl Pts',(-0.82826914338782,2.58971138336883,8.38440599950907));
#28882=CARTESIAN_POINT('Ctrl Pts',(-2.62575405424508,0.705726908343466,
8.51156199692582));
#28883=CARTESIAN_POINT('Ctrl Pts',(-2.01495955826419,-1.82553356611497,
8.63871799434254));
#28884=CARTESIAN_POINT('Ctrl Pts',(0.443908104290186,-2.68245790602317,
8.76587399175929));
#28885=CARTESIAN_POINT('Ctrl Pts',(2.49563377107184,-1.07909540970433,8.89302998917602));
#28886=CARTESIAN_POINT('Ctrl Pts',(2.25842327184115,1.51398782946234,9.02018598659275));
#28887=CARTESIAN_POINT('Ctrl Pts',(-0.0501595437068742,2.7184773022327,
9.14734198400951));
#28888=CARTESIAN_POINT('Ctrl Pts',(-2.31273721419361,1.42964380201861,9.27449798142622));
#28889=CARTESIAN_POINT('Ctrl Pts',(-2.45412710728949,-1.17042512098534,
9.40165397884297));
#28890=CARTESIAN_POINT('Ctrl Pts',(-0.344649762985586,-2.69700785379723,
9.5288099762597));
#28891=CARTESIAN_POINT('Ctrl Pts',(2.08093217817404,-1.74995888306207,9.65596597367644));
#28892=CARTESIAN_POINT('Ctrl Pts',(2.5979324288453,0.802110913603682,9.78312197109316));
#28893=CARTESIAN_POINT('Ctrl Pts',(0.732170608351645,2.61850358465186,9.91027796850992));
#28894=CARTESIAN_POINT('Ctrl Pts',(-1.8051207468719,2.03326680781961,10.0374339659267));
#28895=CARTESIAN_POINT('Ctrl Pts',(-2.68679812162284,-0.416834111142922,
10.1645899633433));
#28896=CARTESIAN_POINT('Ctrl Pts',(-1.10420791727987,-2.48462465937712,
10.2917459607601));
#28897=CARTESIAN_POINT('Ctrl Pts',(1.49113562689651,-2.27357633801207,10.4189019581768));
#28898=CARTESIAN_POINT('Ctrl Pts',(2.71884490342142,0.0227423329444836,
10.5460579555935));
#28899=CARTESIAN_POINT('Ctrl Pts',(1.45289405186817,2.29820227495634,10.6732139530104));
#28900=CARTESIAN_POINT('Ctrl Pts',(-1.14561680077464,2.46580554147145,10.800369950427));
#28901=CARTESIAN_POINT('Ctrl Pts',(-2.69339506673948,0.371830387450793,
10.9275259478437));
#28902=CARTESIAN_POINT('Ctrl Pts',(-1.77085519185023,-2.06317878819687,
11.0546819452605));
#28903=CARTESIAN_POINT('Ctrl Pts',(0.775871108296341,-2.60588926201391,
11.1818379426773));
#28904=CARTESIAN_POINT('Ctrl Pts',(2.61098681055567,-0.758539845804237,
11.308993940094));
#28905=CARTESIAN_POINT('Ctrl Pts',(2.05136727204152,1.78452434496292,11.4361499375107));
#28906=CARTESIAN_POINT('Ctrl Pts',(-0.389717725534715,2.69086508709977,
11.5633059349274));
#28907=CARTESIAN_POINT('Ctrl Pts',(-2.47336285879642,1.12920812576549,11.6904619323442));
#28908=CARTESIAN_POINT('Ctrl Pts',(-2.28849817912672,-1.46813177429756,
11.817617929761));
#28909=CARTESIAN_POINT('Ctrl Pts',(-0.00467719073695795,-2.71893599528478,
11.9447739271776));
#28910=CARTESIAN_POINT('Ctrl Pts',(2.28343360618049,-1.47599654089498,12.0719299245944));
#28911=CARTESIAN_POINT('Ctrl Pts',(2.4772332006897,1.12069197015463,12.1990859220111));
#28912=CARTESIAN_POINT('Ctrl Pts',(0.398973196382628,2.68950835862925,12.326241919428));
#28913=CARTESIAN_POINT('Ctrl Pts',(-2.04521557081167,1.79157140284105,12.4533979168447));
#28914=CARTESIAN_POINT('Ctrl Pts',(-2.61358107356021,-0.749552396097977,
12.5805539142613));
#28915=CARTESIAN_POINT('Ctrl Pts',(-0.784831938973139,-2.60320449641131,
12.707709911678));
#28916=CARTESIAN_POINT('Ctrl Pts',(1.7637464550898,-2.06925911009872,12.8348659090948));
#28917=CARTESIAN_POINT('Ctrl Pts',(2.69465838882545,0.362561705232363,12.9620219065116));
#28918=CARTESIAN_POINT('Ctrl Pts',(1.15409349262152,2.46184951466517,13.0891779039284));
#28919=CARTESIAN_POINT('Ctrl Pts',(-1.44497861118487,2.30318727761913,13.216333901345));
#28920=CARTESIAN_POINT('Ctrl Pts',(-2.71875056855662,0.0320962387432519,
13.3434898987617));
#28921=CARTESIAN_POINT('Ctrl Pts',(-1.49894891955313,-2.26843270985474,
13.4706458961785));
#28922=CARTESIAN_POINT('Ctrl Pts',(1.09565316400684,-2.48840892273963,13.5978018935953));
#28923=CARTESIAN_POINT('Ctrl Pts',(2.68534812474848,-0.426075429329398,
13.724957891012));
#28924=CARTESIAN_POINT('Ctrl Pts',(1.81210540917471,2.02704435289614,13.8521138884288));
#28925=CARTESIAN_POINT('Ctrl Pts',(-0.723157453648822,2.62100708121908,
13.9792698858454));
#28926=CARTESIAN_POINT('Ctrl Pts',(-2.59515743368809,0.811044213925397,
14.1064258832623));
#28927=CARTESIAN_POINT('Ctrl Pts',(-2.08694050237286,-1.74278919038536,
14.233581880679));
#28928=CARTESIAN_POINT('Ctrl Pts',(0.335368812031106,-2.69817764101722,
14.3607378780956));
#28929=CARTESIAN_POINT('Ctrl Pts',(2.45008579790229,-1.17886148698052,14.4878938755124));
#28930=CARTESIAN_POINT('Ctrl Pts',(2.31764213959291,1.42167849225891,14.6150498729291));
#28931=CARTESIAN_POINT('Ctrl Pts',(0.0595120225290418,2.71828864209504,
14.7422058703459));
#28932=CARTESIAN_POINT('Ctrl Pts',(-2.25320111158564,1.52174885356211,14.8693618677626));
#28933=CARTESIAN_POINT('Ctrl Pts',(-2.49933157103879,-1.07050292880361,
14.9965178651794));
#28934=CARTESIAN_POINT('Ctrl Pts',(-0.453134329966127,-2.68091478819722,
15.1236738625962));
#28935=CARTESIAN_POINT('Ctrl Pts',(2.00866698248185,-1.8324551225216,15.2508298600128));
#28936=CARTESIAN_POINT('Ctrl Pts',(2.62816652975788,0.696688965341679,15.3779858574296));
#28937=CARTESIAN_POINT('Ctrl Pts',(0.837174004845652,2.58684644078056,15.5051418548462));
#28938=CARTESIAN_POINT('Ctrl Pts',(-1.721654682225,2.10440965064816,15.632297852263));
#28939=CARTESIAN_POINT('Ctrl Pts',(-2.70142248576348,-0.308141811476186,
15.7594538496798));
#28940=CARTESIAN_POINT('Ctrl Pts',(-1.20350958991195,-2.43807290488992,
15.8866098470964));
#28941=CARTESIAN_POINT('Ctrl Pts',(1.39823378716581,-2.33186129497368,16.0137658445133));
#28942=CARTESIAN_POINT('Ctrl Pts',(2.71755026287845,-0.0869217538808249,
16.14092184193));
#28943=CARTESIAN_POINT('Ctrl Pts',(1.54439402414511,2.23774036044249,16.2680778393468));
#28944=CARTESIAN_POINT('Ctrl Pts',(-1.04524382234984,2.51000003474261,16.3952338367634));
#28945=CARTESIAN_POINT('Ctrl Pts',(-2.67620879985039,0.480147146374683,
16.5223898341802));
#28946=CARTESIAN_POINT('Ctrl Pts',(-1.85261847329488,-1.99008532856633,
16.6495458315969));
#28947=CARTESIAN_POINT('Ctrl Pts',(0.670149623049134,-2.63505869105329,
16.7767018290136));
#28948=CARTESIAN_POINT('Ctrl Pts',(2.57827236292531,-0.863218654307199,
16.9038578264304));
#28949=CARTESIAN_POINT('Ctrl Pts',(2.12166477829421,1.70034508000999,17.0310138238472));
#28950=CARTESIAN_POINT('Ctrl Pts',(-0.280883472581658,2.70439259306019,
17.1581698212639));
#28951=CARTESIAN_POINT('Ctrl Pts',(-2.42581205735167,1.22803529467831,17.2853258186807));
#28952=CARTESIAN_POINT('Ctrl Pts',(-2.34584329765868,-1.37464688025626,
17.4124818160974));
#28953=CARTESIAN_POINT('Ctrl Pts',(-0.114322645200683,-2.71653550600074,
17.5396378135142));
#28954=CARTESIAN_POINT('Ctrl Pts',(2.22205202879955,-1.56688212826498,17.6667938109308));
#28955=CARTESIAN_POINT('Ctrl Pts',(2.52041322885733,1.01987841352257,17.7939498083476));
#28956=CARTESIAN_POINT('Ctrl Pts',(0.507111131323891,2.67123063831182,17.9211058057642));
#28957=CARTESIAN_POINT('Ctrl Pts',(-1.97130128092286,1.87259341086107,18.048261803181));
#28958=CARTESIAN_POINT('Ctrl Pts',(-2.64168286416546,-0.643542125849563,
18.1754178005977));
#28959=CARTESIAN_POINT('Ctrl Pts',(-0.889175513542436,-2.56943607211484,
18.3025737980144));
#28960=CARTESIAN_POINT('Ctrl Pts',(1.67886255094878,-2.13870413044678,18.4297297954312));
#28961=CARTESIAN_POINT('Ctrl Pts',(2.7070876608444,0.25359656754859,18.5568857928479));
#28962=CARTESIAN_POINT('Ctrl Pts',(1.25243610699023,2.41330450222833,18.6840417902647));
#28963=CARTESIAN_POINT('Ctrl Pts',(-1.35092017034292,2.35958672566386,18.8111977876814));
#28964=CARTESIAN_POINT('Ctrl Pts',(-2.71524447466377,0.141711909789787,
18.9383537850982));
#28965=CARTESIAN_POINT('Ctrl Pts',(-1.58921087885835,-2.20613771217634,
19.0655097825149));
#28966=CARTESIAN_POINT('Ctrl Pts',(0.994409282010079,-2.5305700943504,19.1926657799316));
#28967=CARTESIAN_POINT('Ctrl Pts',(2.66598080986571,-0.534023542548665,
19.3198217773484));
#28968=CARTESIAN_POINT('Ctrl Pts',(1.8923779037484,1.95231674990849,19.446977774765));
#28969=CARTESIAN_POINT('Ctrl Pts',(-0.616869179752904,2.64803837540913,
19.5741337721818));
#28970=CARTESIAN_POINT('Ctrl Pts',(-2.56033846700907,0.915041942711955,
19.7012897695985));
#28971=CARTESIAN_POINT('Ctrl Pts',(-2.15552597418617,-1.65720927983679,
19.8284457670153));
#28972=CARTESIAN_POINT('Ctrl Pts',(0.226283871483405,-2.70950741502488,
19.955601764432));
#28973=CARTESIAN_POINT('Ctrl Pts',(2.40055151155118,-1.27670954525991,20.0827577618488));
#28974=CARTESIAN_POINT('Ctrl Pts',(2.3730901812684,1.32705607045671,20.2099137592656));
#28975=CARTESIAN_POINT('Ctrl Pts',(0.169086762131636,2.71367730016675,20.3370697566822));
#28976=CARTESIAN_POINT('Ctrl Pts',(-2.18999902907526,1.61137800506825,20.4642257540991));
#28977=CARTESIAN_POINT('Ctrl Pts',(-2.54046959825811,-0.968839018049278,
20.5913817515157));
#28978=CARTESIAN_POINT('Ctrl Pts',(-0.560881643029023,-2.660459848425,20.7185377489324));
#28979=CARTESIAN_POINT('Ctrl Pts',(1.93313366626957,-1.91196993985354,20.8456937463493));
#28980=CARTESIAN_POINT('Ctrl Pts',(2.65412457842224,0.590133497425207,20.9728497437659));
#28981=CARTESIAN_POINT('Ctrl Pts',(0.940815311173381,2.55098047284375,21.1000057411826));
#28982=CARTESIAN_POINT('Ctrl Pts',(-1.63538746883388,2.17212859871361,21.2271617385995));
#28983=CARTESIAN_POINT('Ctrl Pts',(-2.71165160951022,-0.19894816211538,
21.3543177360161));
#28984=CARTESIAN_POINT('Ctrl Pts',(-1.30085314085368,-2.38755438231248,
21.4814737334328));
#28985=CARTESIAN_POINT('Ctrl Pts',(1.3030570076011,-2.38635229115696,21.6086297308496));
#28986=CARTESIAN_POINT('Ctrl Pts',(2.71183414189291,-0.196444418175644,
21.7357857282663));
#28987=CARTESIAN_POINT('Ctrl Pts',(1.63338125247519,2.17363762081699,21.8629417256831));
#28988=CARTESIAN_POINT('Ctrl Pts',(-0.94317022216235,2.55011073379072,21.9900977230998));
#28989=CARTESIAN_POINT('Ctrl Pts',(-2.65466831547712,0.58768270126854,22.1172537205165));
#28990=CARTESIAN_POINT('Ctrl Pts',(-1.9313675266463,-1.91375398094545,22.2444097179333));
#28991=CARTESIAN_POINT('Ctrl Pts',(0.56333779791293,-2.65994085423172,22.3715657153501));
#28992=CARTESIAN_POINT('Ctrl Pts',(2.5413630413366,-0.966492997748461,22.4987217127668));
#28993=CARTESIAN_POINT('Ctrl Pts',(2.18851031552501,1.61339933724078,22.6258777101835));
#28994=CARTESIAN_POINT('Ctrl Pts',(-0.171592219514319,2.71352002623355,
22.7530337076002));
#28995=CARTESIAN_POINT('Ctrl Pts',(-2.37431443633364,1.32486443834305,22.8801897050169));
#28996=CARTESIAN_POINT('Ctrl Pts',(-2.39937170655933,-1.27892542250552,
23.0073457024337));
#28997=CARTESIAN_POINT('Ctrl Pts',(-0.223782095619982,-2.70971518729337,
23.1345016998504));
#28998=CARTESIAN_POINT('Ctrl Pts',(2.15705515137361,-1.6552183833262,23.2616576972671));
#28999=CARTESIAN_POINT('Ctrl Pts',(2.55949252043483,0.91740550489222,23.3888136946838));
#29000=CARTESIAN_POINT('Ctrl Pts',(0.614423991571972,2.64860680002698,23.5159696921006));
#29001=CARTESIAN_POINT('Ctrl Pts',(-1.89417966487008,1.95056869137211,23.6431256895173));
#29002=CARTESIAN_POINT('Ctrl Pts',(-2.66548661131631,-0.536484806366303,
23.7702816869341));
#29003=CARTESIAN_POINT('Ctrl Pts',(-0.992072390990129,-2.53148715059024,
23.8974376843508));
#29004=CARTESIAN_POINT('Ctrl Pts',(1.59124712127312,-2.20466945858295,24.0245936817677));
#29005=CARTESIAN_POINT('Ctrl Pts',(2.71511247517501,0.14421882580776,24.1517496791844));
#29006=CARTESIAN_POINT('Ctrl Pts',(1.34874099575428,2.36083302013085,24.278905676601));
#29007=CARTESIAN_POINT('Ctrl Pts',(-1.25466376937707,2.41214710338757,24.4060616740178));
#29008=CARTESIAN_POINT('Ctrl Pts',(-2.70732065186799,0.251097014194625,
24.5332176714345));
#29009=CARTESIAN_POINT('Ctrl Pts',(-1.67688717676254,-2.14025330719935,
24.6603736688514));
#29010=CARTESIAN_POINT('Ctrl Pts',(0.89154748653726,-2.56861400405307,24.787529666268));
#29011=CARTESIAN_POINT('Ctrl Pts',(2.64227591853694,-0.641102794322506,
24.9146856636847));
#29012=CARTESIAN_POINT('Ctrl Pts',(1.96957148125265,1.87441270877163,25.0418416611014));
#29013=CARTESIAN_POINT('Ctrl Pts',(-0.509577253762257,2.67076128566679,
25.1689976585183));
#29014=CARTESIAN_POINT('Ctrl Pts',(-2.52135380499301,1.01755088944764,25.2961536559349));
#29015=CARTESIAN_POINT('Ctrl Pts',(-2.22060438448587,-1.5689330738341,25.4233096533516));
#29016=CARTESIAN_POINT('Ctrl Pts',(0.1168307648981,-2.71642879438091,25.5504656507684));
#29017=CARTESIAN_POINT('Ctrl Pts',(2.34711150477801,-1.37248038481687,25.6776216481851));
#29018=CARTESIAN_POINT('Ctrl Pts',(2.42467718237059,1.23027451565081,25.8047776456018));
#29019=CARTESIAN_POINT('Ctrl Pts',(0.278386395944303,2.7046507791435,25.9319336430186));
#29020=CARTESIAN_POINT('Ctrl Pts',(-2.12323379705904,1.69838542904567,26.0590896404354));
#29021=CARTESIAN_POINT('Ctrl Pts',(-2.57747425698115,-0.865598796884507,
26.1862456378521));
#29022=CARTESIAN_POINT('Ctrl Pts',(-0.667716396258505,-2.63567631486417,
26.3134016352688));
#29023=CARTESIAN_POINT('Ctrl Pts',(1.85445512296983,-1.98837396368473,26.4405576326856));
#29024=CARTESIAN_POINT('Ctrl Pts',(2.67576434084336,0.482617876626542,26.5677136301024));
#29025=CARTESIAN_POINT('Ctrl Pts',(1.04292590193155,2.51096403511652,26.694869627519));
#29026=CARTESIAN_POINT('Ctrl Pts',(-1.54645946428526,2.23631347263548,26.8220256249357));
#29027=CARTESIAN_POINT('Ctrl Pts',(-2.71746884998021,-0.0894308221792745,
26.9491816223525));
#29028=CARTESIAN_POINT('Ctrl Pts',(-1.39608019121057,-2.33315128576736,
27.0763376197693));
#29029=CARTESIAN_POINT('Ctrl Pts',(1.20576014173901,-2.4369606691865,27.2034936171861));
#29030=CARTESIAN_POINT('Ctrl Pts',(2.70170584064869,-0.305647465510764,
27.3306496146028));
#29031=CARTESIAN_POINT('Ctrl Pts',(1.71971095378114,2.10599835185442,27.4578056120194));
#29032=CARTESIAN_POINT('Ctrl Pts',(-0.839562074942459,2.58607237812223,
27.5849616094363));
#29033=CARTESIAN_POINT('Ctrl Pts',(-2.62880866019516,0.694262090749141,
27.7121176068529));
#29034=CARTESIAN_POINT('Ctrl Pts',(-2.00697422643644,-1.83430893717177,
27.8392736042696));
#29035=CARTESIAN_POINT('Ctrl Pts',(0.455609416755672,-2.68049526803014,
27.9664296016865));
#29036=CARTESIAN_POINT('Ctrl Pts',(2.50031889761113,-1.06819484777688,28.0935855991032));
#29037=CARTESIAN_POINT('Ctrl Pts',(2.25179512540124,1.52382857821593,28.22074159652));
#29038=CARTESIAN_POINT('Ctrl Pts',(-0.0620217842537382,2.71823253619818,
28.3478975939367));
#29039=CARTESIAN_POINT('Ctrl Pts',(-2.31895378286757,1.41953801481067,28.4750535913533));
#29040=CARTESIAN_POINT('Ctrl Pts',(-2.44899631459202,-1.18112314077876,
28.60220958877));
#29041=CARTESIAN_POINT('Ctrl Pts',(-0.332877450415083,-2.69848613588685,
28.7293655861868));
#29042=CARTESIAN_POINT('Ctrl Pts',(2.08854872444804,-1.74086158214111,28.8565215836035));
#29043=CARTESIAN_POINT('Ctrl Pts',(2.59440749303851,0.813439968672548,28.9836775810204));
#29044=CARTESIAN_POINT('Ctrl Pts',(0.720737178070014,2.62167365297744,29.110833578437));
#29045=CARTESIAN_POINT('Ctrl Pts',(-1.81397620026522,2.02537037784197,29.2379895758538));
#29046=CARTESIAN_POINT('Ctrl Pts',(-2.68495358608697,-0.428554620937766,
29.3651455732704));
#29047=CARTESIAN_POINT('Ctrl Pts',(-1.09335515710588,-2.48941947509823,
29.4923015706873));
#29048=CARTESIAN_POINT('Ctrl Pts',(1.50104271721046,-2.2670477682832,29.6194575681039));
#29049=CARTESIAN_POINT('Ctrl Pts',(2.71871977536715,0.0346064386488195,
29.7466135655207));
#29050=CARTESIAN_POINT('Ctrl Pts',(1.44285146993242,2.30452043997926,29.8737695629374));
#29051=CARTESIAN_POINT('Ctrl Pts',(-1.15636601837838,2.46078289454969,30.0009255603543));
#29052=CARTESIAN_POINT('Ctrl Pts',(-2.69499199230524,0.360073581339755,
30.1280815577708));
#29053=CARTESIAN_POINT('Ctrl Pts',(-1.76183516308499,-2.07088668948479,
30.2552375551877));
#29054=CARTESIAN_POINT('Ctrl Pts',(0.78723513471999,-2.60247875404054,30.3823935526044));
#29055=CARTESIAN_POINT('Ctrl Pts',(2.61427201884843,-0.747138965676931,
30.5095495500212));
#29056=CARTESIAN_POINT('Ctrl Pts',(2.04356054699407,1.79345898010954,30.6367055474379));
#29057=CARTESIAN_POINT('Ctrl Pts',(-0.401456240674143,2.68913884160025,
30.7638615448547));
#29058=CARTESIAN_POINT('Ctrl Pts',(-2.47826687605908,1.11840427108543,30.8910175422714));
#29059=CARTESIAN_POINT('Ctrl Pts',(-2.28206985007429,-1.47810419860748,
31.018173539688));
#29060=CARTESIAN_POINT('Ctrl Pts',(0.00718757353821803,-2.7189305179477,
31.1453295371049));
#29061=CARTESIAN_POINT('Ctrl Pts',(2.2898527249793,-1.46601818554802,31.2724855345215));
#29062=CARTESIAN_POINT('Ctrl Pts',(2.47231921036929,1.13149129231446,31.3996415319384));
#29063=CARTESIAN_POINT('Ctrl Pts',(0.38723309237749,2.69122376535401,31.5267975293551));
#29064=CARTESIAN_POINT('Ctrl Pts',(-2.05301404314954,1.78262956340224,31.6539535267717));
#29065=CARTESIAN_POINT('Ctrl Pts',(-2.61028534039153,-0.760950237808461,
31.7811095241884));
#29066=CARTESIAN_POINT('Ctrl Pts',(-0.77346476825431,-2.60660451120056,
31.9082655216052));
#29067=CARTESIAN_POINT('Ctrl Pts',(1.77275936289528,-2.06154288271629,32.035421519022));
#29068=CARTESIAN_POINT('Ctrl Pts',(2.69305060974847,0.374317029576794,32.1625775164387));
#29069=CARTESIAN_POINT('Ctrl Pts',(1.14333964062519,2.4668622391498,32.2897335138555));
#29070=CARTESIAN_POINT('Ctrl Pts',(-1.45501535228521,2.29685983457637,32.4168895112722));
#29071=CARTESIAN_POINT('Ctrl Pts',(-2.71886474821264,0.0202320386364921,
32.544045508689));
#29072=CARTESIAN_POINT('Ctrl Pts',(-1.48903579470102,-2.27495216025588,
32.6712015061057));
#29073=CARTESIAN_POINT('Ctrl Pts',(1.10650147163388,-2.48360403032979,32.7983575035225));
#29074=CARTESIAN_POINT('Ctrl Pts',(2.68718187780354,-0.414353332843636,
32.925513500939));
#29075=CARTESIAN_POINT('Ctrl Pts',(1.80324259290189,2.0349328156185,33.0526694983558));
#29076=CARTESIAN_POINT('Ctrl Pts',(-0.734587807428301,2.61782605300257,
33.1798254957725));
#29077=CARTESIAN_POINT('Ctrl Pts',(-2.59867218381255,0.799712680864083,
33.3069814931893));
#29078=CARTESIAN_POINT('Ctrl Pts',(-2.07931503383186,-1.75188092642428,
33.434137490606));
#29079=CARTESIAN_POINT('Ctrl Pts',(0.347138751858806,-2.69668568512338,
33.5612934880228));
#29080=CARTESIAN_POINT('Ctrl Pts',(2.4552086228712,-1.16816408243671,33.6884494854395));
#29081=CARTESIAN_POINT('Ctrl Pts',(2.31141259786826,1.43178873129245,33.8156054828562));
#29082=CARTESIAN_POINT('Ctrl Pts',(0.0476565103776217,2.71850301715689,
33.9427614802729));
#29083=CARTESIAN_POINT('Ctrl Pts',(-2.25983341822314,1.51193904894985,34.0699174776897));
#29084=CARTESIAN_POINT('Ctrl Pts',(-2.49461112273393,-1.08146981546886,
34.1970734751064));
#29085=CARTESIAN_POINT('Ctrl Pts',(-0.441479368245401,-2.68273191178327,
34.3242294725231));
#29086=CARTESIAN_POINT('Ctrl Pts',(2.01673602906685,-1.82392925374997,34.4513854699399));
#29087=CARTESIAN_POINT('Ctrl Pts',(2.62492622075604,0.708641089121424,34.5785414673567));
#29088=CARTESIAN_POINT('Ctrl Pts',(0.826212131065567,2.58953704692221,34.7056974647735));
#29089=CARTESIAN_POINT('Ctrl Pts',(-1.73146372505156,2.09869585167041,34.8328534621901));
#29090=CARTESIAN_POINT('Ctrl Pts',(-2.69884412682198,-0.323811118765491,
34.9600172221939));
#29091=CARTESIAN_POINT('Ctrl Pts',(-1.69656210721047,-1.73082272675162,
35.0447956497254));
#29092=CARTESIAN_POINT('Ctrl Pts',(-1.00847442622808,-2.06659007601517,
35.0871887447847));
#29093=CARTESIAN_POINT('Ctrl Pts',(1.24723527089883,-1.74554912134441,4.91299708530798));
#29094=CARTESIAN_POINT('Ctrl Pts',(1.82857496528105,-1.33019696843275,4.95539991266972));
#29095=CARTESIAN_POINT('Ctrl Pts',(2.53322632354395,0.119575258569398,5.04018807250373));
#29096=CARTESIAN_POINT('Ctrl Pts',(1.26822303545749,2.19881126114289,5.16736156480996));
#29097=CARTESIAN_POINT('Ctrl Pts',(-1.16087552561943,2.25459568666643,5.2945175622267));
#29098=CARTESIAN_POINT('Ctrl Pts',(-2.52467584330113,0.245759892176623,
5.42167355964344));
#29099=CARTESIAN_POINT('Ctrl Pts',(-1.57320286650264,-1.99016393268508,
5.54882955706016));
#29100=CARTESIAN_POINT('Ctrl Pts',(0.821331662733299,-2.39987583645184,
5.67598555447692));
#29101=CARTESIAN_POINT('Ctrl Pts',(2.46247781576393,-0.608940207530322,
5.80314155189363));
#29102=CARTESIAN_POINT('Ctrl Pts',(1.84514089848384,1.74074310964657,5.93029754931038));
#29103=CARTESIAN_POINT('Ctrl Pts',(-0.46453821390252,2.49373107655781,6.05745354672711));
#29104=CARTESIAN_POINT('Ctrl Pts',(-2.34814198676975,0.95959460444983,6.18460954414384));
#29105=CARTESIAN_POINT('Ctrl Pts',(-2.07809180336199,-1.45469424707903,
6.31176554156058));
#29106=CARTESIAN_POINT('Ctrl Pts',(0.0979382188879125,-2.53475367241525,
6.43892153897732));
#29107=CARTESIAN_POINT('Ctrl Pts',(2.18413991054886,-1.29000669886218,6.56607753639405));
#29108=CARTESIAN_POINT('Ctrl Pts',(2.26710112530366,1.13790889748749,6.69323353381079));
#29109=CARTESIAN_POINT('Ctrl Pts',(0.270730429855875,2.522158768484,6.82038953122753));
#29110=CARTESIAN_POINT('Ctrl Pts',(-1.97394755373906,1.59314576162754,6.94754552864427));
#29111=CARTESIAN_POINT('Ctrl Pts',(-2.40816773953772,-0.797063519219258,
7.074701526061));
#29112=CARTESIAN_POINT('Ctrl Pts',(-0.633673462972628,-2.45622464330757,
7.20185752347775));
#29113=CARTESIAN_POINT('Ctrl Pts',(1.72201106451603,-1.86259491985669,7.32901352089446));
#29114=CARTESIAN_POINT('Ctrl Pts',(2.49830786182965,0.439362838806997,7.45616951831122));
#29115=CARTESIAN_POINT('Ctrl Pts',(0.983215870614292,2.33834735642068,7.58332551572794));
#29116=CARTESIAN_POINT('Ctrl Pts',(-1.43365841672741,2.09265510986232,7.71048151314468));
#29117=CARTESIAN_POINT('Ctrl Pts',(-2.53561517448838,-0.0723708375318783,
7.83763751056142));
#29118=CARTESIAN_POINT('Ctrl Pts',(-1.31196576888435,-2.17101995946912,
7.96479350797814));
#29119=CARTESIAN_POINT('Ctrl Pts',(1.11498755491276,-2.27846101652471,8.09194950539489));
#29120=CARTESIAN_POINT('Ctrl Pts',(2.51930071103104,-0.296151610402521,
8.21910550281162));
#29121=CARTESIAN_POINT('Ctrl Pts',(1.61297094434476,1.95778103494126,8.34626150022837));
#29122=CARTESIAN_POINT('Ctrl Pts',(-0.772737556416206,2.41608330116289,
8.47341749764509));
#29123=CARTESIAN_POINT('Ctrl Pts',(-2.44970947888779,0.658411207279792,
8.60057349506184));
#29124=CARTESIAN_POINT('Ctrl Pts',(-1.87986590803327,-1.70314004607919,
8.72772949247856));
#29125=CARTESIAN_POINT('Ctrl Pts',(0.414146134165366,-2.50261160160021,
8.85488548989531));
#29126=CARTESIAN_POINT('Ctrl Pts',(2.32831315444159,-1.00674709023239,8.98204148731205));
#29127=CARTESIAN_POINT('Ctrl Pts',(2.1070065139672,1.41248199950732,9.10919748472876));
#29128=CARTESIAN_POINT('Ctrl Pts',(-0.0467965800058906,2.53621606511637,
9.23635348214553));
#29129=CARTESIAN_POINT('Ctrl Pts',(-2.15767895954577,1.33379284612595,9.36350947956224));
#29130=CARTESIAN_POINT('Ctrl Pts',(-2.28958931907699,-1.09195356989761,
9.49066547697899));
#29131=CARTESIAN_POINT('Ctrl Pts',(-0.321542602178368,-2.51618604316749,
9.61782147439571));
#29132=CARTESIAN_POINT('Ctrl Pts',(1.94141537115939,-1.6326322934056,9.74497747181245));
#29133=CARTESIAN_POINT('Ctrl Pts',(2.42375316384388,0.748333114062007,9.8721334692292));
#29134=CARTESIAN_POINT('Ctrl Pts',(0.68308198040958,2.44294511949922,9.99928946664592));
#29135=CARTESIAN_POINT('Ctrl Pts',(-1.68409581125844,1.8969457418036,10.1264454640627));
#29136=CARTESIAN_POINT('Ctrl Pts',(-2.50666082596597,-0.388887326114794,
10.2536014614794));
#29137=CARTESIAN_POINT('Ctrl Pts',(-1.03017592117983,-2.31804215239206,
10.3807574588962));
#29138=CARTESIAN_POINT('Ctrl Pts',(1.39116193064996,-2.1211436376529,10.5079134563129));
#29139=CARTESIAN_POINT('Ctrl Pts',(2.53655902035812,0.021217565482156,10.6350694537296));
#29140=CARTESIAN_POINT('Ctrl Pts',(1.35548427505125,2.14411852026279,10.7622254511464));
#29141=CARTESIAN_POINT('Ctrl Pts',(-1.06880853196949,2.3004847686595,10.8893814485631));
#29142=CARTESIAN_POINT('Ctrl Pts',(-2.51281547664917,0.346900892413839,
11.0165374459798));
#29143=CARTESIAN_POINT('Ctrl Pts',(-1.65212760205011,-1.92485226326314,
11.1436934433966));
#29144=CARTESIAN_POINT('Ctrl Pts',(0.723852565443357,-2.4311765284212,11.2708494408133));
#29145=CARTESIAN_POINT('Ctrl Pts',(2.43593231008385,-0.707683283351195,
11.39800543823));
#29146=CARTESIAN_POINT('Ctrl Pts',(1.91383265423357,1.66488030213418,11.5251614356468));
#29147=CARTESIAN_POINT('Ctrl Pts',(-0.363588967820266,2.51045512035657,
11.6523174330635));
#29148=CARTESIAN_POINT('Ctrl Pts',(-2.30753540306903,1.05349998216809,11.7794734304802));
#29149=CARTESIAN_POINT('Ctrl Pts',(-2.13506503884503,-1.36970037918765,
11.906629427897));
#29150=CARTESIAN_POINT('Ctrl Pts',(-0.00436360689018303,-2.53664400493645,
12.0337854253137));
#29151=CARTESIAN_POINT('Ctrl Pts',(2.1303400219178,-1.37703784982852,12.1609414227305));
#29152=CARTESIAN_POINT('Ctrl Pts',(2.31114625657121,1.04555479511216,12.2880974201472));
#29153=CARTESIAN_POINT('Ctrl Pts',(0.372223902471257,2.50918935420869,12.4152534175639));
#29154=CARTESIAN_POINT('Ctrl Pts',(-1.90809339590896,1.6714548876155,12.5424094149807));
#29155=CARTESIAN_POINT('Ctrl Pts',(-2.43835263984122,-0.699298400273082,
12.6695654123974));
#29156=CARTESIAN_POINT('Ctrl Pts',(-0.732212614173908,-2.42867176384331,
12.7967214098141));
#29157=CARTESIAN_POINT('Ctrl Pts',(1.64549547296818,-1.93052492791114,12.9238774072309));
#29158=CARTESIAN_POINT('Ctrl Pts',(2.51399409887539,0.338253632153168,13.0510334046476));
#29159=CARTESIAN_POINT('Ctrl Pts',(1.07671690112295,2.29679397501851,13.1781894020643));
#29160=CARTESIAN_POINT('Ctrl Pts',(-1.34809952778586,2.14876930172335,13.3053453994811));
#29161=CARTESIAN_POINT('Ctrl Pts',(-2.53647101020647,0.02994433547918,13.4325013968978));
#29162=CARTESIAN_POINT('Ctrl Pts',(-1.39845137843795,-2.11634486579813,
13.5596573943146));
#29163=CARTESIAN_POINT('Ctrl Pts',(1.02219472425514,-2.3215726985279,13.6868133917313));
#29164=CARTESIAN_POINT('Ctrl Pts',(2.50530804462615,-0.397509056974356,
13.813969389148));
#29165=CARTESIAN_POINT('Ctrl Pts',(1.69061218449704,1.89114047349086,13.9411253865648));
#29166=CARTESIAN_POINT('Ctrl Pts',(-0.674673115735156,2.44528076828599,
14.0682813839815));
#29167=CARTESIAN_POINT('Ctrl Pts',(-2.4211642191826,0.756667478219514,14.1954373813982));
#29168=CARTESIAN_POINT('Ctrl Pts',(-1.9470208652149,-1.62594329521757,14.322593378815));
#29169=CARTESIAN_POINT('Ctrl Pts',(0.312883895743237,-2.51727740160469,
14.4497493762317));
#29170=CARTESIAN_POINT('Ctrl Pts',(2.28581896065478,-1.09982431685984,14.5769053736484));
#29171=CARTESIAN_POINT('Ctrl Pts',(2.16225503255025,1.32636157327338,14.7040613710652));
#29172=CARTESIAN_POINT('Ctrl Pts',(0.0555220186984494,2.53604005376192,
14.8312173684819));
#29173=CARTESIAN_POINT('Ctrl Pts',(-2.10213447522553,1.41972268310166,14.9583733658987));
#29174=CARTESIAN_POINT('Ctrl Pts',(-2.33176303414969,-0.998730695141672,
15.0855293633154));
#29175=CARTESIAN_POINT('Ctrl Pts',(-0.42275378439691,-2.50117194263474,
15.2126853607321));
#29176=CARTESIAN_POINT('Ctrl Pts',(1.87399522013853,-1.70959754437793,15.3398413581488));
#29177=CARTESIAN_POINT('Ctrl Pts',(2.45196020915775,0.649979216246355,15.4669973555656));
#29178=CARTESIAN_POINT('Ctrl Pts',(0.781045388403149,2.41341043962673,15.5941533529823));
#29179=CARTESIAN_POINT('Ctrl Pts',(-1.60622575735892,1.96331878849104,15.7213093503991));
#29180=CARTESIAN_POINT('Ctrl Pts',(-2.52030469462918,-0.287482338718793,
15.8484653478158));
#29181=CARTESIAN_POINT('Ctrl Pts',(-1.12281987933079,-2.27461147614811,
15.9756213452325));
#29182=CARTESIAN_POINT('Ctrl Pts',(1.30448872642261,-2.17552085981299,16.1027773426493));
#29183=CARTESIAN_POINT('Ctrl Pts',(2.53535117943153,-0.0810940552712092,
16.229933340066));
#29184=CARTESIAN_POINT('Ctrl Pts',(1.44084960050602,2.08771029541141,16.3570893374828));
#29185=CARTESIAN_POINT('Ctrl Pts',(-0.975165094087748,2.34171622706894,
16.4842453348995));
#29186=CARTESIAN_POINT('Ctrl Pts',(-2.4967814688803,0.447955517324072,16.6114013323162));
#29187=CARTESIAN_POINT('Ctrl Pts',(-1.72840903642746,-1.85665937954192,
16.738557329733));
#29188=CARTESIAN_POINT('Ctrl Pts',(0.625219213201751,-2.45839028315044,
16.8657133271497));
#29189=CARTESIAN_POINT('Ctrl Pts',(2.4054112137431,-0.805343865466191,16.9928693245664));
#29190=CARTESIAN_POINT('Ctrl Pts',(1.97941704022394,1.58634486468619,17.1200253219832));
#29191=CARTESIAN_POINT('Ctrl Pts',(-0.2620515444444,2.52307567007005,17.2471813193999));
#29192=CARTESIAN_POINT('Ctrl Pts',(-2.26317266131126,1.14570124986335,17.3743373168166));
#29193=CARTESIAN_POINT('Ctrl Pts',(-2.18856543436326,-1.28248321172463,
17.5014933142334));
#29194=CARTESIAN_POINT('Ctrl Pts',(-0.106657844494999,-2.53440445727449,
17.6286493116501));
#29195=CARTESIAN_POINT('Ctrl Pts',(2.07307379330966,-1.46182998202179,17.7558053090668));
#29196=CARTESIAN_POINT('Ctrl Pts',(2.35143126503568,0.9515003177392,17.8829613064836));
#29197=CARTESIAN_POINT('Ctrl Pts',(0.473111692713715,2.49213706987852,18.0101173039003));
#29198=CARTESIAN_POINT('Ctrl Pts',(-1.83913471477385,1.74704474749757,18.137273301317));
#29199=CARTESIAN_POINT('Ctrl Pts',(-2.46457033631895,-0.600395624719085,
18.2644292987338));
#29200=CARTESIAN_POINT('Ctrl Pts',(-0.829560438228563,-2.39716735506121,
18.3915852961505));
#29201=CARTESIAN_POINT('Ctrl Pts',(1.56630263910659,-1.99531398320486,18.5187412935673));
#29202=CARTESIAN_POINT('Ctrl Pts',(2.52559004611624,0.236594099257959,18.645897290984));
#29203=CARTESIAN_POINT('Ctrl Pts',(1.16846610139864,2.25150367948342,18.7730532884007));
#29204=CARTESIAN_POINT('Ctrl Pts',(-1.26034726716289,2.20138742955441,18.9002092858175));
#29205=CARTESIAN_POINT('Ctrl Pts',(-2.53319998357345,0.132210786506162,
19.0273652832342));
#29206=CARTESIAN_POINT('Ctrl Pts',(-1.48266169392256,-2.05822645746765,
19.1545212806509));
#29207=CARTESIAN_POINT('Ctrl Pts',(0.927738772828189,-2.36090716002057,
19.2816772780677));
#29208=CARTESIAN_POINT('Ctrl Pts',(2.48723921796958,-0.498219752156858,
19.4088332754844));
#29209=CARTESIAN_POINT('Ctrl Pts',(1.76550278231721,1.82142300811078,19.5359892729011));
#29210=CARTESIAN_POINT('Ctrl Pts',(-0.57551097538294,2.47049974014549,19.6631452703179));
#29211=CARTESIAN_POINT('Ctrl Pts',(-2.38867970198999,0.853692643839789,
19.7903012677346));
#29212=CARTESIAN_POINT('Ctrl Pts',(-2.01100800069828,-1.54610111893518,
19.9174572651514));
#29213=CARTESIAN_POINT('Ctrl Pts',(0.211112592207941,-2.52784756705311,
20.0446132625681));
#29214=CARTESIAN_POINT('Ctrl Pts',(2.2396057174121,-1.19111211872777,20.1717692599848));
#29215=CARTESIAN_POINT('Ctrl Pts',(2.21398554137631,1.23808314398582,20.2989252574016));
#29216=CARTESIAN_POINT('Ctrl Pts',(0.157750282544093,2.53173788082463,20.4260812548183));
#29217=CARTESIAN_POINT('Ctrl Pts',(-2.04316979787472,1.50334261760173,20.553237252235));
#29218=CARTESIAN_POINT('Ctrl Pts',(-2.37014294831528,-0.903882875928337,
20.6803932496518));
#29219=CARTESIAN_POINT('Ctrl Pts',(-0.523277142137953,-2.48208841127005,
20.8075492470685));
#29220=CARTESIAN_POINT('Ctrl Pts',(1.80352606085155,-1.78378126368521,20.9347052444853));
#29221=CARTESIAN_POINT('Ctrl Pts',(2.47617789160356,0.550567795987747,21.061861241902));
#29222=CARTESIAN_POINT('Ctrl Pts',(0.877738028029808,2.37994911773245,21.1890172393187));
#29223=CARTESIAN_POINT('Ctrl Pts',(-1.52574235868728,2.02649749660654,21.3161732367354));
#29224=CARTESIAN_POINT('Ctrl Pts',(-2.52984800328848,-0.185609614789812,
21.4433292341522));
#29225=CARTESIAN_POINT('Ctrl Pts',(-1.21363699872742,-2.2274799851323,21.5704852315689));
#29226=CARTESIAN_POINT('Ctrl Pts',(1.21569310647764,-2.22635848858801,21.6976412289857));
#29227=CARTESIAN_POINT('Ctrl Pts',(2.53001829772536,-0.183273735215835,
21.8247972264024));
#29228=CARTESIAN_POINT('Ctrl Pts',(1.52387064978812,2.0279053458087,21.9519532238192));
#29229=CARTESIAN_POINT('Ctrl Pts',(-0.879935053208925,2.37913769063065,
22.0791092212358));
#29230=CARTESIAN_POINT('Ctrl Pts',(-2.47668517362228,0.548281314294679,
22.2062652186526));
#29231=CARTESIAN_POINT('Ctrl Pts',(-1.80187833266125,-1.78544569313408,
22.3334212160693));
#29232=CARTESIAN_POINT('Ctrl Pts',(0.525568623280569,-2.48160421321936,
22.4605772134861));
#29233=CARTESIAN_POINT('Ctrl Pts',(2.37097649019807,-0.901694145358155,
22.5877332109028));
#29234=CARTESIAN_POINT('Ctrl Pts',(2.04178089563184,1.50522842886984,22.7148892083196));
#29235=CARTESIAN_POINT('Ctrl Pts',(-0.16008776068265,2.5315911513759,22.8420452057363));
#29236=CARTESIAN_POINT('Ctrl Pts',(-2.21512771584346,1.23603845059418,22.969201203153));
#29237=CARTESIAN_POINT('Ctrl Pts',(-2.23850501284805,-1.19317943172823,
23.0963572005698));
#29238=CARTESIAN_POINT('Ctrl Pts',(-0.208778548759929,-2.52804140915904,
23.2235131979865));
#29239=CARTESIAN_POINT('Ctrl Pts',(2.01243465368002,-1.54424370275967,23.3506691954032));
#29240=CARTESIAN_POINT('Ctrl Pts',(2.38789047219213,0.855897740188131,23.47782519282));
#29241=CARTESIAN_POINT('Ctrl Pts',(0.57322972567696,2.47103005454111,23.6049811902367));
#29242=CARTESIAN_POINT('Ctrl Pts',(-1.76718374375042,1.81979214875473,23.7321371876534));
#29243=CARTESIAN_POINT('Ctrl Pts',(-2.48677815313036,-0.500515999702998,
23.8592931850702));
#29244=CARTESIAN_POINT('Ctrl Pts',(-0.925558559463123,-2.36176273191226,
23.9864491824869));
#29245=CARTESIAN_POINT('Ctrl Pts',(1.48456141577064,-2.05685664343682,24.1136051799036));
#29246=CARTESIAN_POINT('Ctrl Pts',(2.53307683403542,0.134549625485303,24.2407611773204));
#29247=CARTESIAN_POINT('Ctrl Pts',(1.25831419607725,2.20255016578411,24.3679171747371));
#29248=CARTESIAN_POINT('Ctrl Pts',(-1.17054440940153,2.25042387884239,24.4950731721539));
#29249=CARTESIAN_POINT('Ctrl Pts',(-2.52580741617726,0.234262129310505,
24.6222291695706));
#29250=CARTESIAN_POINT('Ctrl Pts',(-1.5644597045559,-1.99675929487407,24.7493851669873));
#29251=CARTESIAN_POINT('Ctrl Pts',(0.83177338148554,-2.39640040283281,24.8765411644041));
#29252=CARTESIAN_POINT('Ctrl Pts',(2.46512362915797,-0.598119839005628,
25.0036971618208));
#29253=CARTESIAN_POINT('Ctrl Pts',(1.83752089011209,1.74874206995966,25.1308531592375));
#29254=CARTESIAN_POINT('Ctrl Pts',(-0.475412473132706,2.49169918514153,
25.2580091566543));
#29255=CARTESIAN_POINT('Ctrl Pts',(-2.35230877992377,0.949328843309133,
25.385165154071));
#29256=CARTESIAN_POINT('Ctrl Pts',(-2.07172320680237,-1.46374342124623,
25.5123211514877));
#29257=CARTESIAN_POINT('Ctrl Pts',(0.108997806452491,-2.53430490017158,
25.6394771489045));
#29258=CARTESIAN_POINT('Ctrl Pts',(2.18974861410406,-1.28046196971035,25.7666331463212));
#29259=CARTESIAN_POINT('Ctrl Pts',(2.26211387441007,1.14779034150259,25.893789143738));
#29260=CARTESIAN_POINT('Ctrl Pts',(0.259721885161245,2.5233165459794,26.0209451411547));
#29261=CARTESIAN_POINT('Ctrl Pts',(-1.98088086359093,1.58451659918865,26.1481011385715));
#29262=CARTESIAN_POINT('Ctrl Pts',(-2.40466661708398,-0.807564430573208,
26.2752571359881));
#29263=CARTESIAN_POINT('Ctrl Pts',(-0.622949122930586,-2.45896649816241,
26.4024131334049));
#29264=CARTESIAN_POINT('Ctrl Pts',(1.73012254729899,-1.85506275370209,26.5295691308216));
#29265=CARTESIAN_POINT('Ctrl Pts',(2.49636680877887,0.450260596624125,26.6567251282384));
#29266=CARTESIAN_POINT('Ctrl Pts',(0.973002579433895,2.34261559570924,26.7838811256551));
#29267=CARTESIAN_POINT('Ctrl Pts',(-1.44277656250804,2.08637907378373,26.9110371230718));
#29268=CARTESIAN_POINT('Ctrl Pts',(-2.53527522488879,-0.0834349022304562,
27.0381931204886));
#29269=CARTESIAN_POINT('Ctrl Pts',(-1.30247951904217,-2.17672436273424,
27.1653491179053));
#29270=CARTESIAN_POINT('Ctrl Pts',(1.12491954214358,-2.27357381066651,27.2925051153221));
#29271=CARTESIAN_POINT('Ctrl Pts',(2.52056905188954,-0.285155227028738,
27.4196611127388));
#29272=CARTESIAN_POINT('Ctrl Pts',(1.60441234685104,1.96480097468346,27.5468171101555));
#29273=CARTESIAN_POINT('Ctrl Pts',(-0.783273349526421,2.41268827426315,
27.6739731075723));
#29274=CARTESIAN_POINT('Ctrl Pts',(-2.45255928774101,0.647715052287995,
27.801129104989));
#29275=CARTESIAN_POINT('Ctrl Pts',(-1.87241595549912,-1.71132706939307,
27.9282851024057));
#29276=CARTESIAN_POINT('Ctrl Pts',(0.425062928149098,-2.50078054934024,
28.0554410998225));
#29277=CARTESIAN_POINT('Ctrl Pts',(2.33268416507548,-0.996577360194006,
28.1825970972391));
#29278=CARTESIAN_POINT('Ctrl Pts',(2.10082275386406,1.42166297190725,28.309753094656));
#29279=CARTESIAN_POINT('Ctrl Pts',(-0.0578635125929414,2.53598770950404,
28.4369090920726));
#29280=CARTESIAN_POINT('Ctrl Pts',(-2.16347873625452,1.32436460486516,28.5640650894894));
#29281=CARTESIAN_POINT('Ctrl Pts',(-2.28480252212436,-1.10193433730837,
28.6912210869062));
#29282=CARTESIAN_POINT('Ctrl Pts',(-0.310559568315866,-2.51756521333065,
28.8183770843229));
#29283=CARTESIAN_POINT('Ctrl Pts',(1.94852126349294,-1.62414492412501,28.9455330817396));
#29284=CARTESIAN_POINT('Ctrl Pts',(2.42046455855946,0.758902608773127,29.0726890791563));
#29285=CARTESIAN_POINT('Ctrl Pts',(0.672415108357407,2.44590264951363,29.1998450765731));
#29286=CARTESIAN_POINT('Ctrl Pts',(-1.6923575477613,1.88957873066472,29.3270010739898));
#29287=CARTESIAN_POINT('Ctrl Pts',(-2.50493995794367,-0.39982203033639,
29.4541570714066));
#29288=CARTESIAN_POINT('Ctrl Pts',(-1.02005078801005,-2.32251549805921,
29.5813130688233));
#29289=CARTESIAN_POINT('Ctrl Pts',(1.40040479671775,-2.11505277810627,29.70846906624));
#29290=CARTESIAN_POINT('Ctrl Pts',(2.53644228155689,0.0322862381765574,
29.8356250636568));
#29291=CARTESIAN_POINT('Ctrl Pts',(1.34611500144365,2.15001308175867,29.9627810610735));
#29292=CARTESIAN_POINT('Ctrl Pts',(-1.07883706461593,2.29579886681221,30.0899370584902));
#29293=CARTESIAN_POINT('Ctrl Pts',(-2.51430533579618,0.335932325374936,
30.217093055907));
#29294=CARTESIAN_POINT('Ctrl Pts',(-1.64371232418725,-1.93204338568256,
30.3442490533237));
#29295=CARTESIAN_POINT('Ctrl Pts',(0.734454686842863,-2.42799467911713,
30.4714050507405));
#29296=CARTESIAN_POINT('Ctrl Pts',(2.43899726046709,-0.697046779117154,
30.5985610481571));
#29297=CARTESIAN_POINT('Ctrl Pts',(1.90654933372726,1.6732159116227,30.725717045574));
#29298=CARTESIAN_POINT('Ctrl Pts',(-0.374540470211985,2.50884461157482,
30.8528730429906));
#29299=CARTESIAN_POINT('Ctrl Pts',(-2.31211062882314,1.04342047560674,30.9800290404074));
#29300=CARTESIAN_POINT('Ctrl Pts',(-2.12906769930454,-1.37900419891136,
31.1071850378241));
#29301=CARTESIAN_POINT('Ctrl Pts',(0.0067056802209494,-2.53663889482931,
31.2343410352408));
#29302=CARTESIAN_POINT('Ctrl Pts',(2.13632876870929,-1.36772849671617,31.3614970326576));
#29303=CARTESIAN_POINT('Ctrl Pts',(2.30656172640638,1.05563007303765,31.4886530300743));
#29304=CARTESIAN_POINT('Ctrl Pts',(0.361270917739877,2.51078975090502,31.6158090274911));
#29305=CARTESIAN_POINT('Ctrl Pts',(-1.91536901701141,1.66311255684901,31.7429650249078));
#29306=CARTESIAN_POINT('Ctrl Pts',(-2.43527787022593,-0.709932069801992,
31.8701210223245));
#29307=CARTESIAN_POINT('Ctrl Pts',(-0.721607559289571,-2.43184382348237,
31.9972770197413));
#29308=CARTESIAN_POINT('Ctrl Pts',(1.65390410729847,-1.92332603762306,32.124433017158));
#29309=CARTESIAN_POINT('Ctrl Pts',(2.51249411389452,0.349220816771008,32.2515890145748));
#29310=CARTESIAN_POINT('Ctrl Pts',(1.06668404479837,2.30147061968187,32.3787450119915));
#29311=CARTESIAN_POINT('Ctrl Pts',(-1.35746335215886,2.14286608425562,32.5059010094083));
#29312=CARTESIAN_POINT('Ctrl Pts',(-2.53657753464855,0.0188755747115968,
32.6330570068249));
#29313=CARTESIAN_POINT('Ctrl Pts',(-1.38920288241969,-2.12242721742547,
32.7602130042417));
#29314=CARTESIAN_POINT('Ctrl Pts',(1.03231570340048,-2.31708995176706,32.8873690016584));
#29315=CARTESIAN_POINT('Ctrl Pts',(2.50701885308274,-0.386572872442074,
33.0145249990751));
#29316=CARTESIAN_POINT('Ctrl Pts',(1.68234357876146,1.89850005154182,33.1416809964919));
#29317=CARTESIAN_POINT('Ctrl Pts',(-0.685337117550317,2.44231301319027,
33.2688369939086));
#29318=CARTESIAN_POINT('Ctrl Pts',(-2.42444332168722,0.746095671653793,
33.3959929913254));
#29319=CARTESIAN_POINT('Ctrl Pts',(-1.93990664881079,-1.63442547271552,
33.5231489887421));
#29320=CARTESIAN_POINT('Ctrl Pts',(0.323864715944294,-2.51588547440217,
33.6503049861589));
#29321=CARTESIAN_POINT('Ctrl Pts',(2.29059832407793,-1.08984412344908,33.7774609835755));
#29322=CARTESIAN_POINT('Ctrl Pts',(2.1564431525734,1.3357939678856,33.9046169809924));
#29323=CARTESIAN_POINT('Ctrl Pts',(0.0444613633992766,2.5362400559747,34.031772978409));
#29324=CARTESIAN_POINT('Ctrl Pts',(-2.1083221166044,1.41057058018255,34.1589289758258));
#29325=CARTESIAN_POINT('Ctrl Pts',(-2.32735906991002,-1.00896230315321,
34.2860849732425));
#29326=CARTESIAN_POINT('Ctrl Pts',(-0.411880233556468,-2.50286723655074,
34.4132409706593));
#29327=CARTESIAN_POINT('Ctrl Pts',(1.88152327474552,-1.70164329538349,34.540396968076));
#29328=CARTESIAN_POINT('Ctrl Pts',(2.44893714777715,0.661130005814309,34.6675529654928));
#29329=CARTESIAN_POINT('Ctrl Pts',(0.77081845718618,2.41592065316272,34.7947089629094));
#29330=CARTESIAN_POINT('Ctrl Pts',(-1.6153771495665,1.95798807311286,34.9218649603262));
#29331=CARTESIAN_POINT('Ctrl Pts',(-2.51789920264154,-0.302101091961186,
35.0490287203299));
#29332=CARTESIAN_POINT('Ctrl Pts',(-1.58281552258723,-1.61477912721602,
35.1338071478614));
#29333=CARTESIAN_POINT('Ctrl Pts',(-0.940860914659138,-1.9280348401272,
35.1762002429208));
#29334=CARTESIAN_POINT('Ctrl Pts',(1.1576046410105,-1.62010793883659,5.002008583444));
#29335=CARTESIAN_POINT('Ctrl Pts',(1.69716725916479,-1.23460442471794,5.04441141080575));
#29336=CARTESIAN_POINT('Ctrl Pts',(2.35117993957248,0.110982167919405,5.12919957063975));
#29337=CARTESIAN_POINT('Ctrl Pts',(1.17708415239424,2.04079709738398,5.25637306294598));
#29338=CARTESIAN_POINT('Ctrl Pts',(-1.07745100499292,2.09257266161708,5.38352906036272));
#29339=CARTESIAN_POINT('Ctrl Pts',(-2.34324392634153,0.228098738382345,
5.51068505777945));
#29340=CARTESIAN_POINT('Ctrl Pts',(-1.46014708051209,-1.8471438858426,5.63784105519619));
#29341=CARTESIAN_POINT('Ctrl Pts',(0.762307935618055,-2.22741247858047,
5.76499705261293));
#29342=CARTESIAN_POINT('Ctrl Pts',(2.28551566366429,-0.565179663197865,
5.89215305002966));
#29343=CARTESIAN_POINT('Ctrl Pts',(1.71254270725044,1.61564730372143,6.0193090474464));
#29344=CARTESIAN_POINT('Ctrl Pts',(-0.431154895060577,2.31452295730476,
6.14646504486313));
#29345=CARTESIAN_POINT('Ctrl Pts',(-2.1793964018332,0.89063482529591,6.27362104227988));
#29346=CARTESIAN_POINT('Ctrl Pts',(-1.92875295635622,-1.35015489936908,
6.4007770396966));
#29347=CARTESIAN_POINT('Ctrl Pts',(0.0909000405634622,-2.35259752788409,
6.52793303711335));
#29348=CARTESIAN_POINT('Ctrl Pts',(2.02718008066401,-1.19730236658674,6.65508903453007));
#29349=CARTESIAN_POINT('Ctrl Pts',(2.10417941628647,1.05613483800003,6.78224503194682));
#29350=CARTESIAN_POINT('Ctrl Pts',(0.251274807068405,2.3409077372054,6.90940102936354));
#29351=CARTESIAN_POINT('Ctrl Pts',(-1.83209287183882,1.47865681038455,7.0365570267803));
#29352=CARTESIAN_POINT('Ctrl Pts',(-2.23510849690114,-0.739783784629025,
7.16371302419701));
#29353=CARTESIAN_POINT('Ctrl Pts',(-0.58813550156722,-2.27971186575587,
7.29086902161376));
#29354=CARTESIAN_POINT('Ctrl Pts',(1.59826140798492,-1.72874242242604,7.41802501903049));
#29355=CARTESIAN_POINT('Ctrl Pts',(2.31877083899574,0.407788709281728,7.54518101644724));
#29356=CARTESIAN_POINT('Ctrl Pts',(0.912558585773612,2.17030564741532,7.67233701386396));
#29357=CARTESIAN_POINT('Ctrl Pts',(-1.3306307763662,1.94226969340383,7.79949301128071));
#29358=CARTESIAN_POINT('Ctrl Pts',(-2.35339711944582,-0.067170019446514,
7.92664900869743));
#29359=CARTESIAN_POINT('Ctrl Pts',(-1.21768338207199,-2.01500297453647,
8.05380500611418));
#29360=CARTESIAN_POINT('Ctrl Pts',(1.03486070218796,-2.11472294652947,8.1809610035309));
#29361=CARTESIAN_POINT('Ctrl Pts',(2.33825506962212,-0.274869133870564,
8.30811700094765));
#29362=CARTESIAN_POINT('Ctrl Pts',(1.49705728706912,1.81708813486099,8.43527299836438));
#29363=CARTESIAN_POINT('Ctrl Pts',(-0.717205969444591,2.24245521895696,
8.56242899578111));
#29364=CARTESIAN_POINT('Ctrl Pts',(-2.2736649035305,0.611095506216118,8.68958499319786));
#29365=CARTESIAN_POINT('Ctrl Pts',(-1.74477225780235,-1.58074652604342,
8.81674099061458));
#29366=CARTESIAN_POINT('Ctrl Pts',(0.384384164040551,-2.32276529717725,
8.94389698803133));
#29367=CARTESIAN_POINT('Ctrl Pts',(2.16099253781133,-0.934398770760454,
9.07105298544807));
#29368=CARTESIAN_POINT('Ctrl Pts',(1.95558975609324,1.31097616955231,9.19820898286478));
#29369=CARTESIAN_POINT('Ctrl Pts',(-0.0434336163049105,2.35395482800003,
9.32536498028155));
#29370=CARTESIAN_POINT('Ctrl Pts',(-2.00262070489792,1.2379418902333,9.45252097769825));
#29371=CARTESIAN_POINT('Ctrl Pts',(-2.12505153086449,-1.0134820188099,9.57967697511502));
#29372=CARTESIAN_POINT('Ctrl Pts',(-0.298435441371154,-2.33536423253774,
9.70683297253173));
#29373=CARTESIAN_POINT('Ctrl Pts',(1.80189856414474,-1.51530570374911,9.83398896994848));
#29374=CARTESIAN_POINT('Ctrl Pts',(2.24957389884245,0.694555314520332,9.96114496736521));
#29375=CARTESIAN_POINT('Ctrl Pts',(0.633993352467514,2.26738665434658,10.088300964782));
#29376=CARTESIAN_POINT('Ctrl Pts',(-1.56307087564499,1.76062467578759,10.2154569621987));
#29377=CARTESIAN_POINT('Ctrl Pts',(-2.32652353030908,-0.360940541086664,
10.3426129596154));
#29378=CARTESIAN_POINT('Ctrl Pts',(-0.956143925079784,-2.15145964540702,
10.4697689570321));
#29379=CARTESIAN_POINT('Ctrl Pts',(1.29118823440342,-1.96871093729374,10.5969249544489));
#29380=CARTESIAN_POINT('Ctrl Pts',(2.35427313729481,0.0196927980198272,
10.7240809518656));
#29381=CARTESIAN_POINT('Ctrl Pts',(1.25807449823434,1.99003476556925,10.8512369492824));
#29382=CARTESIAN_POINT('Ctrl Pts',(-0.992000263164342,2.13516399584755,
10.9783929466991));
#29383=CARTESIAN_POINT('Ctrl Pts',(-2.33223588655886,0.321971397376884,
11.1055489441158));
#29384=CARTESIAN_POINT('Ctrl Pts',(-1.53340001225001,-1.78652573832943,
11.2327049415326));
#29385=CARTESIAN_POINT('Ctrl Pts',(0.671834022590375,-2.2564637948285,11.3598609389493));
#29386=CARTESIAN_POINT('Ctrl Pts',(2.26087780961201,-0.656826720898154,
11.4870169363661));
#29387=CARTESIAN_POINT('Ctrl Pts',(1.77629803642563,1.54523625930544,11.6141729337828));
#29388=CARTESIAN_POINT('Ctrl Pts',(-0.337460210105816,2.33004515361337,
11.7413289311995));
#29389=CARTESIAN_POINT('Ctrl Pts',(-2.14170794734164,0.977791838570695,
11.8684849286162));
#29390=CARTESIAN_POINT('Ctrl Pts',(-1.98163189856334,-1.27126898407774,
11.995640926033));
#29391=CARTESIAN_POINT('Ctrl Pts',(-0.0040500230434116,-2.35435201458813,
12.1227969234497));
#29392=CARTESIAN_POINT('Ctrl Pts',(1.97724643765512,-1.27807915876207,12.2499529208664));
#29393=CARTESIAN_POINT('Ctrl Pts',(2.14505931245273,0.970417620069677,12.3771089182832));
#29394=CARTESIAN_POINT('Ctrl Pts',(0.345474608559887,2.32887034978811,12.5042649156999));
#29395=CARTESIAN_POINT('Ctrl Pts',(-1.77097122100624,1.55133837238995,12.6314209131167));
#29396=CARTESIAN_POINT('Ctrl Pts',(-2.26312420612221,-0.649044404448188,
12.7585769105334));
#29397=CARTESIAN_POINT('Ctrl Pts',(-0.679593289374679,-2.25413903127529,
12.8857329079501));
#29398=CARTESIAN_POINT('Ctrl Pts',(1.52724449084658,-1.79179074572356,13.0128889053669));
#29399=CARTESIAN_POINT('Ctrl Pts',(2.33332980892533,0.313945559073971,13.1400449027836));
#29400=CARTESIAN_POINT('Ctrl Pts',(0.999340309624393,2.13173843537186,13.2672009002004));
#29401=CARTESIAN_POINT('Ctrl Pts',(-1.25122044438684,1.99435132582757,13.3943568976171));
#29402=CARTESIAN_POINT('Ctrl Pts',(-2.35419145185632,0.0277924322151094,
13.5215128950338));
#29403=CARTESIAN_POINT('Ctrl Pts',(-1.29795383732276,-1.96425702174153,
13.6486688924505));
#29404=CARTESIAN_POINT('Ctrl Pts',(0.948736284503426,-2.15473647431616,
13.7758248898673));
#29405=CARTESIAN_POINT('Ctrl Pts',(2.32526796450381,-0.368942684619317,
13.902980887284));
#29406=CARTESIAN_POINT('Ctrl Pts',(1.56911895981938,1.75523659408559,14.0301368847008));
#29407=CARTESIAN_POINT('Ctrl Pts',(-0.626188777821492,2.26955445535291,
14.1572928821175));
#29408=CARTESIAN_POINT('Ctrl Pts',(-2.2471710046771,0.702290742513631,14.2844488795342));
#29409=CARTESIAN_POINT('Ctrl Pts',(-1.80710122805693,-1.50909740004977,
14.411604876951));
#29410=CARTESIAN_POINT('Ctrl Pts',(0.29039897945537,-2.33637716219216,14.5387608743677));
#29411=CARTESIAN_POINT('Ctrl Pts',(2.12155212340728,-1.02078714673918,14.6659168717844));
#29412=CARTESIAN_POINT('Ctrl Pts',(2.00686792550758,1.23104465428785,14.7930728692012));
#29413=CARTESIAN_POINT('Ctrl Pts',(0.0515320148678548,2.3537914654288,14.9202288666179));
#29414=CARTESIAN_POINT('Ctrl Pts',(-1.95106783886543,1.3176965126412,15.0473848640346));
#29415=CARTESIAN_POINT('Ctrl Pts',(-2.16419449726058,-0.926958461479726,
15.1745408614514));
#29416=CARTESIAN_POINT('Ctrl Pts',(-0.392373238827692,-2.32142909707225,
15.3016968588681));
#29417=CARTESIAN_POINT('Ctrl Pts',(1.73932345779521,-1.58673996623426,15.4288528562848));
#29418=CARTESIAN_POINT('Ctrl Pts',(2.27575388855762,0.603269467151035,15.5560088537016));
#29419=CARTESIAN_POINT('Ctrl Pts',(0.724916771960646,2.23997443847289,15.6831648511183));
#29420=CARTESIAN_POINT('Ctrl Pts',(-1.49079683249283,1.8222279263339,15.8103208485351));
#29421=CARTESIAN_POINT('Ctrl Pts',(-2.33918690349488,-0.266822865961399,
15.9374768459518));
#29422=CARTESIAN_POINT('Ctrl Pts',(-1.04213016874964,-2.11115004740632,
16.0646328433685));
#29423=CARTESIAN_POINT('Ctrl Pts',(1.2107436656794,-2.0191804246523,16.1917888407853));
#29424=CARTESIAN_POINT('Ctrl Pts',(2.3531520959846,-0.0752663566615951,
16.318944838202));
#29425=CARTESIAN_POINT('Ctrl Pts',(1.33730517686693,1.93768023038033,16.4461008356188));
#29426=CARTESIAN_POINT('Ctrl Pts',(-0.905086365825657,2.17343241939525,
16.5732568330355));
#29427=CARTESIAN_POINT('Ctrl Pts',(-2.31735413791021,0.415763888273461,
16.7004128304522));
#29428=CARTESIAN_POINT('Ctrl Pts',(-1.60419959956003,-1.72323343051753,
16.8275688278689));
#29429=CARTESIAN_POINT('Ctrl Pts',(0.580288803354365,-2.28172187524759,
16.9547248252857));
#29430=CARTESIAN_POINT('Ctrl Pts',(2.23255006456091,-0.747469076625183,
17.0818808227024));
#29431=CARTESIAN_POINT('Ctrl Pts',(1.83716930215367,1.47234464936238,17.2090368201192));
#29432=CARTESIAN_POINT('Ctrl Pts',(-0.243219616307141,2.3417587470799,17.3361928175359));
#29433=CARTESIAN_POINT('Ctrl Pts',(-2.10053326527084,1.0633672050484,17.4633488149526));
#29434=CARTESIAN_POINT('Ctrl Pts',(-2.03128757106783,-1.19031954319298,
17.5905048123694));
#29435=CARTESIAN_POINT('Ctrl Pts',(-0.0989930437893146,-2.35227340854824,
17.7176608097861));
#29436=CARTESIAN_POINT('Ctrl Pts',(1.92409555781977,-1.3567778357786,17.8448168072028));
#29437=CARTESIAN_POINT('Ctrl Pts',(2.18244930121404,0.88312222195582,17.9719728046196));
#29438=CARTESIAN_POINT('Ctrl Pts',(0.439112254103542,2.31304350144521,18.0991288020363));
#29439=CARTESIAN_POINT('Ctrl Pts',(-1.70696814862484,1.62149608413407,18.2262847994531));
#29440=CARTESIAN_POINT('Ctrl Pts',(-2.28745780847244,-0.557249123588607,
18.3534407968698));
#29441=CARTESIAN_POINT('Ctrl Pts',(-0.769945362914689,-2.22489863800758,
18.4805967942865));
#29442=CARTESIAN_POINT('Ctrl Pts',(1.45374272726439,-1.85192383596294,18.6077527917033));
#29443=CARTESIAN_POINT('Ctrl Pts',(2.34409243138809,0.219591630967329,18.73490878912));
#29444=CARTESIAN_POINT('Ctrl Pts',(1.08449609580706,2.0897028567385,18.8620647865367));
#29445=CARTESIAN_POINT('Ctrl Pts',(-1.16977436398285,2.04318813344496,18.9892207839534));
#29446=CARTESIAN_POINT('Ctrl Pts',(-2.35115549248314,0.122709663222533,
19.1163767813702));
#29447=CARTESIAN_POINT('Ctrl Pts',(-1.37611250898677,-1.91031520275895,
19.2435327787869));
#29448=CARTESIAN_POINT('Ctrl Pts',(0.8610682636463,-2.19124422569073,19.3706887762036));
#29449=CARTESIAN_POINT('Ctrl Pts',(2.30849762607345,-0.462415961765052,
19.4978447736204));
#29450=CARTESIAN_POINT('Ctrl Pts',(1.63862766088603,1.69052926631307,19.6250007710371));
#29451=CARTESIAN_POINT('Ctrl Pts',(-0.534152771012978,2.29296110488185,
19.7521567684539));
#29452=CARTESIAN_POINT('Ctrl Pts',(-2.21702093697091,0.79234334496762,19.8793127658706));
#29453=CARTESIAN_POINT('Ctrl Pts',(-1.8664900272104,-1.43499295803357,20.0064687632874));
#29454=CARTESIAN_POINT('Ctrl Pts',(0.195941312932475,-2.34618771908133,
20.1336247607041));
#29455=CARTESIAN_POINT('Ctrl Pts',(2.07865992327303,-1.10551469219562,20.2607807581208));
#29456=CARTESIAN_POINT('Ctrl Pts',(2.05488090148423,1.14911021751495,20.3879367555375));
#29457=CARTESIAN_POINT('Ctrl Pts',(0.146413802956549,2.34979846148252,20.5150927529543));
#29458=CARTESIAN_POINT('Ctrl Pts',(-1.8963405666742,1.3953072301352,20.642248750371));
#29459=CARTESIAN_POINT('Ctrl Pts',(-2.19981629837245,-0.838926733807399,
20.7694047477878));
#29460=CARTESIAN_POINT('Ctrl Pts',(-0.485672641246882,-2.30371697411512,
20.8965607452045));
#29461=CARTESIAN_POINT('Ctrl Pts',(1.67391845543353,-1.65559258751689,21.0237167426212));
#29462=CARTESIAN_POINT('Ctrl Pts',(2.29823120478489,0.511002094550286,21.150872740038));
#29463=CARTESIAN_POINT('Ctrl Pts',(0.814660744886235,2.20891776262115,21.2780287374547));
#29464=CARTESIAN_POINT('Ctrl Pts',(-1.41609724854068,1.88086639449945,21.4051847348714));
#29465=CARTESIAN_POINT('Ctrl Pts',(-2.34804439706675,-0.172271067464243,
21.5323407322882));
#29466=CARTESIAN_POINT('Ctrl Pts',(-1.12642085660117,-2.06740558795213,
21.6594967297049));
#29467=CARTESIAN_POINT('Ctrl Pts',(1.12832920535418,-2.06636468601906,21.7866527271216));
#29468=CARTESIAN_POINT('Ctrl Pts',(2.34820245355783,-0.170103052256023,
21.9138087245384));
#29469=CARTESIAN_POINT('Ctrl Pts',(1.41436004710103,1.88217307080039,22.0409647219551));
#29470=CARTESIAN_POINT('Ctrl Pts',(-0.816699884255499,2.20816464747058,
22.1681207193719));
#29471=CARTESIAN_POINT('Ctrl Pts',(-2.29870203176745,0.508879927320817,
22.2952767167886));
#29472=CARTESIAN_POINT('Ctrl Pts',(-1.6723891386762,-1.65713740532272,22.4224327142054));
#29473=CARTESIAN_POINT('Ctrl Pts',(0.487799448648201,-2.303267572207,22.549588711622));
#29474=CARTESIAN_POINT('Ctrl Pts',(2.20058993905954,-0.836895292967851,
22.6767447090389));
#29475=CARTESIAN_POINT('Ctrl Pts',(1.89505147573867,1.3970575204989,22.8039007064555));
#29476=CARTESIAN_POINT('Ctrl Pts',(-0.148583301850979,2.34966227651824,
22.9310567038723));
#29477=CARTESIAN_POINT('Ctrl Pts',(-2.05594099535328,1.1472124628453,23.058212701289));
#29478=CARTESIAN_POINT('Ctrl Pts',(-2.07763831913675,-1.10743344095094,
23.1853686987058));
#29479=CARTESIAN_POINT('Ctrl Pts',(-0.193775001899879,-2.34636763102471,
23.3125246961225));
#29480=CARTESIAN_POINT('Ctrl Pts',(1.86781415598644,-1.43326902219314,23.4396806935392));
#29481=CARTESIAN_POINT('Ctrl Pts',(2.21628842394943,0.794389975484045,23.566836690956));
#29482=CARTESIAN_POINT('Ctrl Pts',(0.532035459781954,2.29345330905524,23.6939926883727));
#29483=CARTESIAN_POINT('Ctrl Pts',(-1.64018782263076,1.68901560613737,23.8211486857894));
#29484=CARTESIAN_POINT('Ctrl Pts',(-2.3080696949444,-0.464547193039696,
23.9483046832062));
#29485=CARTESIAN_POINT('Ctrl Pts',(-0.859044727936122,-2.19203831323428,
24.0754606806229));
#29486=CARTESIAN_POINT('Ctrl Pts',(1.37787571026816,-1.9090438282907,24.2026166780396));
#29487=CARTESIAN_POINT('Ctrl Pts',(2.35104119289581,0.124880425162849,24.3297726754563));
#29488=CARTESIAN_POINT('Ctrl Pts',(1.16788739640021,2.04426731143737,24.4569286728731));
#29489=CARTESIAN_POINT('Ctrl Pts',(-1.08642504942599,2.08870065429722,24.5840846702898));
#29490=CARTESIAN_POINT('Ctrl Pts',(-2.34429418048653,0.217427244426385,
24.7112406677066));
#29491=CARTESIAN_POINT('Ctrl Pts',(-1.45203223234926,-1.85326528254879,
24.8383966651233));
#29492=CARTESIAN_POINT('Ctrl Pts',(0.771999276433814,-2.22418680161256,
24.9655526625401));
#29493=CARTESIAN_POINT('Ctrl Pts',(2.28797133977901,-0.555136883688751,
25.0927086599568));
#29494=CARTESIAN_POINT('Ctrl Pts',(1.70547029897151,1.6230714311477,25.2198646573735));
#29495=CARTESIAN_POINT('Ctrl Pts',(-0.44124769250315,2.31263708461627,25.3470206547902));
#29496=CARTESIAN_POINT('Ctrl Pts',(-2.18326375485454,0.881106797170618,
25.474176652207));
#29497=CARTESIAN_POINT('Ctrl Pts',(-1.92284202911887,-1.35855376865836,
25.6013326496237));
#29498=CARTESIAN_POINT('Ctrl Pts',(0.101164848006878,-2.35218100596224,
25.7284886470405));
#29499=CARTESIAN_POINT('Ctrl Pts',(2.03238572343009,-1.18844355460383,25.8556446444572));
#29500=CARTESIAN_POINT('Ctrl Pts',(2.09955056644954,1.06530616735437,25.982800641874));
#29501=CARTESIAN_POINT('Ctrl Pts',(0.241057374378188,2.3419823128153,26.1099566392906));
#29502=CARTESIAN_POINT('Ctrl Pts',(-1.83852793012283,1.47064776933163,26.2371126367074));
#29503=CARTESIAN_POINT('Ctrl Pts',(-2.23185897718681,-0.74953006426191,
26.3642686341241));
#29504=CARTESIAN_POINT('Ctrl Pts',(-0.578181849602668,-2.28225668146067,
26.4914246315409));
#29505=CARTESIAN_POINT('Ctrl Pts',(1.60578997162814,-1.72175154371944,26.6185806289576));
#29506=CARTESIAN_POINT('Ctrl Pts',(2.31696927671439,0.417903316621709,26.7457366263743));
#29507=CARTESIAN_POINT('Ctrl Pts',(0.903079256936234,2.17426715630194,26.8728926237911));
#29508=CARTESIAN_POINT('Ctrl Pts',(-1.3390936607308,1.93644467493197,27.0000486212078));
#29509=CARTESIAN_POINT('Ctrl Pts',(-2.35308159979739,-0.0774389822816324,
27.1272046186246));
#29510=CARTESIAN_POINT('Ctrl Pts',(-1.20887884687377,-2.02029743970114,
27.2543606160413));
#29511=CARTESIAN_POINT('Ctrl Pts',(1.04407894254815,-2.1101869521465,27.381516613458));
#29512=CARTESIAN_POINT('Ctrl Pts',(2.33943226313038,-0.264662988546719,
27.5086726108748));
#29513=CARTESIAN_POINT('Ctrl Pts',(1.48911373992093,1.82360359751251,27.6358286082915));
#29514=CARTESIAN_POINT('Ctrl Pts',(-0.726984624110384,2.23930417040404,
27.7629846057082));
#29515=CARTESIAN_POINT('Ctrl Pts',(-2.27630991528687,0.601168013826854,
27.890140603125));
#29516=CARTESIAN_POINT('Ctrl Pts',(-1.73785768456178,-1.58834520161436,
28.0172966005417));
#29517=CARTESIAN_POINT('Ctrl Pts',(0.394516439542522,-2.32106583065033,
28.1444525979584));
#29518=CARTESIAN_POINT('Ctrl Pts',(2.16504943253982,-0.924959872611133,
28.2716085953752));
#29519=CARTESIAN_POINT('Ctrl Pts',(1.94985038232687,1.31949736559857,28.3987645927919));
#29520=CARTESIAN_POINT('Ctrl Pts',(-0.0537052409321449,2.35374288280989,
28.5259205902087));
#29521=CARTESIAN_POINT('Ctrl Pts',(-2.00800368964148,1.22919119491966,28.6530765876254));
#29522=CARTESIAN_POINT('Ctrl Pts',(-2.12060872965672,-1.02274553383799,
28.7802325850421));
#29523=CARTESIAN_POINT('Ctrl Pts',(-0.28824168621664,-2.33664429077444,
28.9073885824589));
#29524=CARTESIAN_POINT('Ctrl Pts',(1.80849380253782,-1.5074282661089,29.0345445798756));
#29525=CARTESIAN_POINT('Ctrl Pts',(2.24652162408042,0.704365248873706,29.1617005772923));
#29526=CARTESIAN_POINT('Ctrl Pts',(0.624093038644794,2.27013164604984,29.2888565747091));
#29527=CARTESIAN_POINT('Ctrl Pts',(-1.57073889525738,1.75378708348746,29.4160125721258));
#29528=CARTESIAN_POINT('Ctrl Pts',(-2.32492632980036,-0.371089439735015,
29.5431685695426));
#29529=CARTESIAN_POINT('Ctrl Pts',(-0.946746418914216,-2.15561152102017,
29.6703245669592));
#29530=CARTESIAN_POINT('Ctrl Pts',(1.29976687622502,-1.96305778792936,29.797480564376));
#29531=CARTESIAN_POINT('Ctrl Pts',(2.35416478774663,0.0299660377042993,
29.9246365617928));
#29532=CARTESIAN_POINT('Ctrl Pts',(1.24937853295487,1.99550572353809,30.0517925592095));
#29533=CARTESIAN_POINT('Ctrl Pts',(-1.00130811085348,2.13081483907472,30.1789485566262));
#29534=CARTESIAN_POINT('Ctrl Pts',(-2.33361867928712,0.311791069410117,
30.306104554043));
#29535=CARTESIAN_POINT('Ctrl Pts',(-1.5255894852895,-1.79320008188034,30.4332605514597));
#29536=CARTESIAN_POINT('Ctrl Pts',(0.681674238965734,-2.25351060419371,
30.5604165488764));
#29537=CARTESIAN_POINT('Ctrl Pts',(2.26372250208576,-0.646954592557379,
30.6875725462932));
#29538=CARTESIAN_POINT('Ctrl Pts',(1.76953812046046,1.55297284313587,30.8147285437099));
#29539=CARTESIAN_POINT('Ctrl Pts',(-0.347624699749826,2.3285503815494,30.9418845411267));
#29540=CARTESIAN_POINT('Ctrl Pts',(-2.14595438158722,0.968436680128043,
31.0690405385433));
#29541=CARTESIAN_POINT('Ctrl Pts',(-1.97606554853479,-1.27990419921524,
31.1961965359601));
#29542=CARTESIAN_POINT('Ctrl Pts',(0.00622378690368324,-2.35434727171091,
31.3233525333769));
#29543=CARTESIAN_POINT('Ctrl Pts',(1.98280481243926,-1.26943880788431,31.4505085307936));
#29544=CARTESIAN_POINT('Ctrl Pts',(2.14080424244349,0.979768853760829,31.5776645282103));
#29545=CARTESIAN_POINT('Ctrl Pts',(0.335308743102262,2.33035573645602,31.704820525627));
#29546=CARTESIAN_POINT('Ctrl Pts',(-1.77772399087328,1.54359555029578,31.8319765230438));
#29547=CARTESIAN_POINT('Ctrl Pts',(-2.26027040006032,-0.658913901795522,
31.9591325204605));
#29548=CARTESIAN_POINT('Ctrl Pts',(-0.669750350324828,-2.25708313576418,
32.0862885178773));
#29549=CARTESIAN_POINT('Ctrl Pts',(1.53504885170168,-1.78510919252983,32.213444515294));
#29550=CARTESIAN_POINT('Ctrl Pts',(2.33193761804057,0.324124603965224,32.3406005127108));
#29551=CARTESIAN_POINT('Ctrl Pts',(0.990028448971534,2.13607900021394,32.4677565101275));
#29552=CARTESIAN_POINT('Ctrl Pts',(-1.25991135203251,1.98887233393488,32.5949125075442));
#29553=CARTESIAN_POINT('Ctrl Pts',(-2.35429032108445,0.0175191107867025,
32.7220685049609));
#29554=CARTESIAN_POINT('Ctrl Pts',(-1.28936997013835,-1.96990227459506,
32.8492245023777));
#29555=CARTESIAN_POINT('Ctrl Pts',(0.958129935167091,-2.15057587320433,
32.9763804997944));
#29556=CARTESIAN_POINT('Ctrl Pts',(2.32685582836193,-0.358792412040517,
33.1035364972112));
#29557=CARTESIAN_POINT('Ctrl Pts',(1.56144456462104,1.76206728746512,33.2306924946279));
#29558=CARTESIAN_POINT('Ctrl Pts',(-0.636086427672334,2.26679997337798,
33.3578484920446));
#29559=CARTESIAN_POINT('Ctrl Pts',(-2.2502144595619,0.692478662443505,33.4850044894614));
#29560=CARTESIAN_POINT('Ctrl Pts',(-1.80049826378972,-1.51697001900675,
33.612160486878));
#29561=CARTESIAN_POINT('Ctrl Pts',(0.300590680029782,-2.33508526368096,
33.7393164842949));
#29562=CARTESIAN_POINT('Ctrl Pts',(2.12598802528465,-1.01152416446146,33.8664724817115));
#29563=CARTESIAN_POINT('Ctrl Pts',(2.00147370727853,1.23979920447876,33.9936284791284));
#29564=CARTESIAN_POINT('Ctrl Pts',(0.0412662164209308,2.35397709479251,
34.120784476545));
#29565=CARTESIAN_POINT('Ctrl Pts',(-1.95681081498566,1.30920211141525,34.2479404739618));
#29566=CARTESIAN_POINT('Ctrl Pts',(-2.16010701708612,-0.936454790837551,
34.3750964713785));
#29567=CARTESIAN_POINT('Ctrl Pts',(-0.382281098867528,-2.32300256131819,
34.5022524687953));
#29568=CARTESIAN_POINT('Ctrl Pts',(1.74631052042418,-1.57935733701702,34.629408466212));
#29569=CARTESIAN_POINT('Ctrl Pts',(2.27294807479828,0.613618922507192,34.7565644636287));
#29570=CARTESIAN_POINT('Ctrl Pts',(0.715424783306792,2.24230425940323,34.8837204610454));
#29571=CARTESIAN_POINT('Ctrl Pts',(-1.49929057408143,1.81728029455531,35.0108764584622));
#29572=CARTESIAN_POINT('Ctrl Pts',(-2.33695427846112,-0.280391065156878,
35.138040218466));
#29573=CARTESIAN_POINT('Ctrl Pts',(-1.46906893796398,-1.49873552768042,
35.2228186459975));
#29574=CARTESIAN_POINT('Ctrl Pts',(-0.873247403090202,-1.78947960423924,
35.2652117410568));
#29575=CARTESIAN_POINT('Ctrl Pts',(-1.16285319861171,1.62483593567698,35.));
#29576=CARTESIAN_POINT('Ctrl Pts',(-1.2034571535085,1.60237251915514,35.));
#29577=CARTESIAN_POINT('Ctrl Pts',(-1.24313101615398,1.5784475810686,35.));
#29578=CARTESIAN_POINT('Ctrl Pts',(-1.28178678438056,1.55308309322909,35.));
#29579=CARTESIAN_POINT('Ctrl Pts',(-1.34124439891837,1.51406920189803,35.));
#29580=CARTESIAN_POINT('Ctrl Pts',(-1.39829464397926,1.4716523739051,35.));
#29581=CARTESIAN_POINT('Ctrl Pts',(-1.45286647428986,1.42618637516297,35.));
#29582=CARTESIAN_POINT('Ctrl Pts',(-1.50919953362205,1.37925302529803,35.));
#29583=CARTESIAN_POINT('Ctrl Pts',(-1.56289222325683,1.3290701152209,35.));
#29584=CARTESIAN_POINT('Ctrl Pts',(-1.61384568307356,1.27597508797261,35.));
#29585=CARTESIAN_POINT('Ctrl Pts',(-1.63889408811983,1.24987390165,35.));
#29586=CARTESIAN_POINT('Ctrl Pts',(-1.66328015009881,1.22306822207441,35.));
#29587=CARTESIAN_POINT('Ctrl Pts',(-1.68698967741847,1.19559427323466,35.));
#29588=CARTESIAN_POINT('Ctrl Pts',(-1.7056134239364,1.17401358745636,35.));
#29589=CARTESIAN_POINT('Ctrl Pts',(-1.72381971498931,1.15202052478812,35.));
#29590=CARTESIAN_POINT('Ctrl Pts',(-1.74160084989885,1.12963170748219,35.));
#29591=CARTESIAN_POINT('Ctrl Pts',(-1.75105180158785,1.1177317004349,35.));
#29592=CARTESIAN_POINT('Ctrl Pts',(-1.76038424143082,1.10571756791684,35.));
#29593=CARTESIAN_POINT('Ctrl Pts',(-1.76958246640894,1.09361130996028,35.));
#29594=CARTESIAN_POINT('Ctrl Pts',(-1.81578754020787,1.03279843099259,35.));
#29595=CARTESIAN_POINT('Ctrl Pts',(-1.85868694579373,0.969568012909778,
35.));
#29596=CARTESIAN_POINT('Ctrl Pts',(-1.89819404295453,0.904303946702904,
35.));
#29597=CARTESIAN_POINT('Ctrl Pts',(-1.9383827536208,0.837913883595611,35.));
#29598=CARTESIAN_POINT('Ctrl Pts',(-1.97506173048199,0.769418694780337,
35.));
#29599=CARTESIAN_POINT('Ctrl Pts',(-2.00810989179612,0.699176647445272,
35.));
#29600=CARTESIAN_POINT('Ctrl Pts',(-2.03387549323432,0.644413280169376,
35.));
#29601=CARTESIAN_POINT('Ctrl Pts',(-2.05743364892923,0.588587058078158,
35.));
#29602=CARTESIAN_POINT('Ctrl Pts',(-2.07871088918223,0.531853309281494,
35.));
#29603=CARTESIAN_POINT('Ctrl Pts',(-2.08934950930873,0.503486434883161,
35.));
#29604=CARTESIAN_POINT('Ctrl Pts',(-2.09941766122464,0.474892509303888,
35.));
#29605=CARTESIAN_POINT('Ctrl Pts',(-2.10890461491907,0.446090093541291,
35.));
#29606=CARTESIAN_POINT('Ctrl Pts',(-2.11515647320623,0.427109435737392,
35.));
#29607=CARTESIAN_POINT('Ctrl Pts',(-2.12115622262752,0.40803718097923,35.));
#29608=CARTESIAN_POINT('Ctrl Pts',(-2.12689957333395,0.388881715849516,
35.));
#29609=CARTESIAN_POINT('Ctrl Pts',(-2.12987153569128,0.378969501845442,
35.));
#29610=CARTESIAN_POINT('Ctrl Pts',(-2.13277431889566,0.36903665131058,35.));
#29611=CARTESIAN_POINT('Ctrl Pts',(-2.13560562780928,0.359090962659784,
35.));
#29612=CARTESIAN_POINT('Ctrl Pts',(-2.15761496010993,0.281777616376262,
35.));
#29613=CARTESIAN_POINT('Ctrl Pts',(-2.17534799254665,0.203559623333045,
35.));
#29614=CARTESIAN_POINT('Ctrl Pts',(-2.18868635601065,0.124817877959984,
35.));
#29615=CARTESIAN_POINT('Ctrl Pts',(-2.20197077284454,0.0463946013273144,
35.));
#29616=CARTESIAN_POINT('Ctrl Pts',(-2.21089654715116,-0.0325491535936027,
35.));
#29617=CARTESIAN_POINT('Ctrl Pts',(-2.2153044627471,-0.111665411483039,
35.));
#29618=CARTESIAN_POINT('Ctrl Pts',(-2.21812153834263,-0.162228194380512,
35.));
#29619=CARTESIAN_POINT('Ctrl Pts',(-2.21909245699586,-0.212861963887261,
35.));
#29620=CARTESIAN_POINT('Ctrl Pts',(-2.21816496049036,-0.263479248160428,
35.));
#29621=CARTESIAN_POINT('Ctrl Pts',(-2.21727633251441,-0.311975317532206,
35.));
#29622=CARTESIAN_POINT('Ctrl Pts',(-2.21464503552917,-0.360456344076136,
35.));
#29623=CARTESIAN_POINT('Ctrl Pts',(-2.21031794958881,-0.408861980263073,
35.));
#29624=CARTESIAN_POINT('Ctrl Pts',(-2.20896704755131,-0.423974061107329,
35.));
#29625=CARTESIAN_POINT('Ctrl Pts',(-2.20745080465866,-0.439078794635521,
35.));
#29626=CARTESIAN_POINT('Ctrl Pts',(-2.20577049210996,-0.454174341115026,
35.));
#29627=CARTESIAN_POINT('Ctrl Pts',(-2.20425945721676,-0.467749135566183,
35.));
#29628=CARTESIAN_POINT('Ctrl Pts',(-2.20261652682881,-0.481309054795014,
35.));
#29629=CARTESIAN_POINT('Ctrl Pts',(-2.2008440773238,-0.494845688706287,
35.));
#29630=CARTESIAN_POINT('Ctrl Pts',(-2.1906273199638,-0.572873583860459,
35.));
#29631=CARTESIAN_POINT('Ctrl Pts',(-2.17610342800899,-0.650199777639862,
35.));
#29632=CARTESIAN_POINT('Ctrl Pts',(-2.15754788660862,-0.726565307611558,
35.));
#29633=CARTESIAN_POINT('Ctrl Pts',(-2.13861027143035,-0.804503266320675,
35.));
#29634=CARTESIAN_POINT('Ctrl Pts',(-2.11547312842759,-0.881441324263912,
35.));
#29635=CARTESIAN_POINT('Ctrl Pts',(-2.08837491381414,-0.957111475263221,
35.));
#29636=CARTESIAN_POINT('Ctrl Pts',(-2.06075709345851,-1.03423259436255,
35.));
#29637=CARTESIAN_POINT('Ctrl Pts',(-2.0290246498135,-1.11003758370528,35.));
#29638=CARTESIAN_POINT('Ctrl Pts',(-1.99337661763573,-1.18423795994886,
35.));
#29639=CARTESIAN_POINT('Ctrl Pts',(-1.98369777462059,-1.20438419943115,
35.));
#29640=CARTESIAN_POINT('Ctrl Pts',(-1.97372999136114,-1.22441208038623,
35.));
#29641=CARTESIAN_POINT('Ctrl Pts',(-1.9634766200881,-1.24431563610298,35.));
#29642=CARTESIAN_POINT('Ctrl Pts',(-1.95462855428264,-1.26149125240076,
35.));
#29643=CARTESIAN_POINT('Ctrl Pts',(-1.94556781553865,-1.27857428649159,
35.));
#29644=CARTESIAN_POINT('Ctrl Pts',(-1.93629640525643,-1.29556083361615,
35.));
#29645=CARTESIAN_POINT('Ctrl Pts',(-1.92954927376081,-1.30792254166459,
35.));
#29646=CARTESIAN_POINT('Ctrl Pts',(-1.92269527151118,-1.32022451322101,
35.));
#29647=CARTESIAN_POINT('Ctrl Pts',(-1.9157363590997,-1.33246413569888,35.));
#29648=CARTESIAN_POINT('Ctrl Pts',(-1.87408701044033,-1.40571872979299,
35.));
#29649=CARTESIAN_POINT('Ctrl Pts',(-1.82867588507373,-1.47675530540997,
35.));
#29650=CARTESIAN_POINT('Ctrl Pts',(-1.77974591339315,-1.54527892431103,
35.));
#29651=CARTESIAN_POINT('Ctrl Pts',(-1.73048679382613,-1.61426349594838,
35.));
#29652=CARTESIAN_POINT('Ctrl Pts',(-1.67766096404848,-1.68070212529753,
35.));
#29653=CARTESIAN_POINT('Ctrl Pts',(-1.62146650439762,-1.74427821650641,
35.));
#29654=CARTESIAN_POINT('Ctrl Pts',(-1.60491685000561,-1.76300181209999,
35.));
#29655=CARTESIAN_POINT('Ctrl Pts',(-1.58807471310564,-1.78147697299719,
35.));
#29656=CARTESIAN_POINT('Ctrl Pts',(-1.57094441010341,-1.79969516910559,
35.));
#29657=CARTESIAN_POINT('Ctrl Pts',(-1.55994931079185,-1.81138853351738,
35.));
#29658=CARTESIAN_POINT('Ctrl Pts',(-1.54884194222482,-1.82296914707541,
35.));
#29659=CARTESIAN_POINT('Ctrl Pts',(-1.53762523100423,-1.83443366707108,
35.));
#29660=CARTESIAN_POINT('Ctrl Pts',(-1.47735309480073,-1.89603738469371,
35.));
#29661=CARTESIAN_POINT('Ctrl Pts',(-1.41391520823538,-1.95430395747543,
35.));
#29662=CARTESIAN_POINT('Ctrl Pts',(-1.34753369268451,-2.00892008903311,
35.));
#29663=CARTESIAN_POINT('Ctrl Pts',(-1.28175657869132,-2.06303894247482,
35.));
#29664=CARTESIAN_POINT('Ctrl Pts',(-1.21308869306104,-2.11357440098649,
35.));
#29665=CARTESIAN_POINT('Ctrl Pts',(-1.14170435717708,-2.1601933216293,35.));
#29666=CARTESIAN_POINT('Ctrl Pts',(-1.11975470438348,-2.17452796674509,
35.));
#29667=CARTESIAN_POINT('Ctrl Pts',(-1.09754794696018,-2.18849205896657,
35.));
#29668=CARTESIAN_POINT('Ctrl Pts',(-1.07508846035141,-2.20207516956602,
35.));
#29669=CARTESIAN_POINT('Ctrl Pts',(1.07765321779378,2.20537369629785,5.));
#29670=CARTESIAN_POINT('Ctrl Pts',(1.12605534704973,2.17638462489288,5.));
#29671=CARTESIAN_POINT('Ctrl Pts',(1.1733135262994,2.14564792857991,5.));
#29672=CARTESIAN_POINT('Ctrl Pts',(1.21932045153113,2.11315756143298,5.));
#29673=CARTESIAN_POINT('Ctrl Pts',(1.28915280522501,2.06384153349108,5.));
#29674=CARTESIAN_POINT('Ctrl Pts',(1.35610447303115,2.01048641170541,5.));
#29675=CARTESIAN_POINT('Ctrl Pts',(1.42000521897292,1.95345758415458,5.));
#29676=CARTESIAN_POINT('Ctrl Pts',(1.45203025925604,1.92487653282728,5.));
#29677=CARTESIAN_POINT('Ctrl Pts',(1.48328834939632,1.89537222664871,5.));
#29678=CARTESIAN_POINT('Ctrl Pts',(1.51375388140517,1.86498810835876,5.));
#29679=CARTESIAN_POINT('Ctrl Pts',(1.52811363799061,1.85066672567029,5.));
#29680=CARTESIAN_POINT('Ctrl Pts',(1.54229727331263,1.83614985958058,5.));
#29681=CARTESIAN_POINT('Ctrl Pts',(1.55630187408297,1.82144196987146,5.));
#29682=CARTESIAN_POINT('Ctrl Pts',(1.56790736208478,1.80925367258614,5.));
#29683=CARTESIAN_POINT('Ctrl Pts',(1.57939111667914,1.79693273685352,5.));
#29684=CARTESIAN_POINT('Ctrl Pts',(1.59073993809508,1.78449460478855,5.));
#29685=CARTESIAN_POINT('Ctrl Pts',(1.6478349293045,1.72191938090552,5.));
#29686=CARTESIAN_POINT('Ctrl Pts',(1.70158263478878,1.65631424483516,5.));
#29687=CARTESIAN_POINT('Ctrl Pts',(1.75181663638728,1.58803510705647,5.));
#29688=CARTESIAN_POINT('Ctrl Pts',(1.80202321464289,1.51979324367655,5.));
#29689=CARTESIAN_POINT('Ctrl Pts',(1.84872029427685,1.44887929457968,5.));
#29690=CARTESIAN_POINT('Ctrl Pts',(1.89169373885761,1.37563015276107,5.));
#29691=CARTESIAN_POINT('Ctrl Pts',(1.89767700253961,1.36543155373656,5.));
#29692=CARTESIAN_POINT('Ctrl Pts',(1.90358800061462,1.35518767071414,5.));
#29693=CARTESIAN_POINT('Ctrl Pts',(1.90942607495413,1.34489940162725,5.));
#29694=CARTESIAN_POINT('Ctrl Pts',(1.91766729738792,1.33037613435231,5.));
#29695=CARTESIAN_POINT('Ctrl Pts',(1.92576320743067,1.31576441843905,5.));
#29696=CARTESIAN_POINT('Ctrl Pts',(1.93371188435635,1.30106677809768,5.));
#29697=CARTESIAN_POINT('Ctrl Pts',(1.94061116483423,1.28830954264504,5.));
#29698=CARTESIAN_POINT('Ctrl Pts',(1.94739530897506,1.27549531421591,5.));
#29699=CARTESIAN_POINT('Ctrl Pts',(1.95406177942983,1.26262928097317,5.));
#29700=CARTESIAN_POINT('Ctrl Pts',(1.99226151800852,1.18890524518061,5.));
#29701=CARTESIAN_POINT('Ctrl Pts',(2.02662081955031,1.11344588745721,5.));
#29702=CARTESIAN_POINT('Ctrl Pts',(2.05697787439092,1.03658084236829,5.));
#29703=CARTESIAN_POINT('Ctrl Pts',(2.08698381426429,0.960604831737085,5.));
#29704=CARTESIAN_POINT('Ctrl Pts',(2.11307977329731,0.883254514836898,5.));
#29705=CARTESIAN_POINT('Ctrl Pts',(2.13505987244827,0.804839634021934,5.));
#29706=CARTESIAN_POINT('Ctrl Pts',(2.15637299228847,0.728804228513231,5.));
#29707=CARTESIAN_POINT('Ctrl Pts',(2.17381627703144,0.651767110791863,5.));
#29708=CARTESIAN_POINT('Ctrl Pts',(2.18715357665171,0.574015077520465,5.));
#29709=CARTESIAN_POINT('Ctrl Pts',(2.19288012175061,0.540631218888172,5.));
#29710=CARTESIAN_POINT('Ctrl Pts',(2.19784909558329,0.507115686650812,5.));
#29711=CARTESIAN_POINT('Ctrl Pts',(2.20203891829051,0.473491966359662,5.));
#29712=CARTESIAN_POINT('Ctrl Pts',(2.203880446088,0.458713533023023,5.));
#29713=CARTESIAN_POINT('Ctrl Pts',(2.20557146498055,0.443912805281082,5.));
#29714=CARTESIAN_POINT('Ctrl Pts',(2.20710823476353,0.429112420088137,5.));
#29715=CARTESIAN_POINT('Ctrl Pts',(2.21517716213172,0.351401864827779,5.));
#29716=CARTESIAN_POINT('Ctrl Pts',(2.21901524210411,0.273570144957761,5.));
#29717=CARTESIAN_POINT('Ctrl Pts',(2.21844424195061,0.195896659425403,5.));
#29718=CARTESIAN_POINT('Ctrl Pts',(2.21822709066427,0.166357442676425,5.));
#29719=CARTESIAN_POINT('Ctrl Pts',(2.21737173543002,0.136841145695996,5.));
#29720=CARTESIAN_POINT('Ctrl Pts',(2.21586638874295,0.107363405091233,5.));
#29721=CARTESIAN_POINT('Ctrl Pts',(2.21181137114425,0.0279579379327235,
5.));
#29722=CARTESIAN_POINT('Ctrl Pts',(2.20304328499261,-0.0511693321485583,
5.));
#29723=CARTESIAN_POINT('Ctrl Pts',(2.18975147681156,-0.129695492434029,
5.));
#29724=CARTESIAN_POINT('Ctrl Pts',(2.17683622913987,-0.20599698542724,5.));
#29725=CARTESIAN_POINT('Ctrl Pts',(2.15964916296706,-0.281731621075645,
5.));
#29726=CARTESIAN_POINT('Ctrl Pts',(2.13832461156907,-0.356577243192453,
5.));
#29727=CARTESIAN_POINT('Ctrl Pts',(2.13318601839716,-0.374612848986876,
5.));
#29728=CARTESIAN_POINT('Ctrl Pts',(2.1278049053625,-0.392602968217722,5.));
#29729=CARTESIAN_POINT('Ctrl Pts',(2.12219400142581,-0.41050867268925,5.));
#29730=CARTESIAN_POINT('Ctrl Pts',(2.09893248463381,-0.484741603770714,
5.));
#29731=CARTESIAN_POINT('Ctrl Pts',(2.07170317080282,-0.557614084834952,
5.));
#29732=CARTESIAN_POINT('Ctrl Pts',(2.04071024615788,-0.628834903151848,
5.));
#29733=CARTESIAN_POINT('Ctrl Pts',(2.00970031783733,-0.7000947954092,5.));
#29734=CARTESIAN_POINT('Ctrl Pts',(1.97492198177241,-0.769702049232439,
5.));
#29735=CARTESIAN_POINT('Ctrl Pts',(1.93653689050298,-0.837335602906435,
5.));
#29736=CARTESIAN_POINT('Ctrl Pts',(1.89892488427954,-0.903607000409294,
5.));
#29737=CARTESIAN_POINT('Ctrl Pts',(1.8578492344502,-0.967984023593398,5.));
#29738=CARTESIAN_POINT('Ctrl Pts',(1.81343121203445,-1.03012582810539,5.));
#29739=CARTESIAN_POINT('Ctrl Pts',(1.79641142470554,-1.05393689036138,5.));
#29740=CARTESIAN_POINT('Ctrl Pts',(1.77890063322063,-1.07741931484657,5.));
#29741=CARTESIAN_POINT('Ctrl Pts',(1.76090475095969,-1.10055208232734,5.));
#29742=CARTESIAN_POINT('Ctrl Pts',(1.75328563734958,-1.11034605524828,5.));
#29743=CARTESIAN_POINT('Ctrl Pts',(1.7455793850169,-1.12007743144322,5.00000000000001));
#29744=CARTESIAN_POINT('Ctrl Pts',(1.7377958257542,-1.12973327713713,5.00000000000001));
#29745=CARTESIAN_POINT('Ctrl Pts',(1.69072775812267,-1.18812327364407,5.));
#29746=CARTESIAN_POINT('Ctrl Pts',(1.64075413084026,-1.24386031821466,5.));
#29747=CARTESIAN_POINT('Ctrl Pts',(1.58802770749618,-1.29665904591518,5.));
#29748=CARTESIAN_POINT('Ctrl Pts',(1.53615683351676,-1.34860105102627,5.));
#29749=CARTESIAN_POINT('Ctrl Pts',(1.48162111426943,-1.39769987612691,5.));
#29750=CARTESIAN_POINT('Ctrl Pts',(1.42453922398786,-1.44364191562489,5.));
#29751=CARTESIAN_POINT('Ctrl Pts',(1.36928567044666,-1.48811242854364,5.));
#29752=CARTESIAN_POINT('Ctrl Pts',(1.31164585798449,-1.52962545660389,5.));
#29753=CARTESIAN_POINT('Ctrl Pts',(1.25171120792614,-1.56785089596259,5.));
#29754=CARTESIAN_POINT('Ctrl Pts',(1.22182449225738,-1.58691220417603,5.00000000000001));
#29755=CARTESIAN_POINT('Ctrl Pts',(1.19136694642474,-1.60515527938473,5.));
#29756=CARTESIAN_POINT('Ctrl Pts',(1.16034898466907,-1.62253437445174,5.));
#29757=CARTESIAN_POINT('Origin',(-0.860389557721271,-5.43228587327326,0.));
#29758=CARTESIAN_POINT('',(-1.10635903124561,-5.38757549311203,4.));
#29759=CARTESIAN_POINT('',(-0.61264241982148,-5.46577252229136,4.));
#29760=CARTESIAN_POINT('Ctrl Pts',(-1.1063590312456,-5.38757549311203,4.));
#29761=CARTESIAN_POINT('Ctrl Pts',(-1.1063590312456,-5.38757549311203,4.02673063961774));
#29762=CARTESIAN_POINT('Ctrl Pts',(-1.10617564982983,-5.38651975223822,
4.05414638576014));
#29763=CARTESIAN_POINT('Ctrl Pts',(-1.10402140302146,-5.37551658340327,
4.19012241323847));
#29764=CARTESIAN_POINT('Ctrl Pts',(-1.09908519447304,-5.35042611089804,
4.2868635932903));
#29765=CARTESIAN_POINT('Ctrl Pts',(-1.0731593931695,-5.29897209514011,4.42646405387435));
#29766=CARTESIAN_POINT('Ctrl Pts',(-1.05808598501925,-5.27637155422115,
4.47482705790044));
#29767=CARTESIAN_POINT('Ctrl Pts',(-1.02277290612915,-5.24115473829855,
4.54353143773206));
#29768=CARTESIAN_POINT('Ctrl Pts',(-1.00509927187885,-5.22683772617801,
4.56934838942209));
#29769=CARTESIAN_POINT('Ctrl Pts',(-0.967491407182819,-5.2057010863751,
4.60714056402289));
#29770=CARTESIAN_POINT('Ctrl Pts',(-0.949946965001191,-5.19797165415639,
4.62089194101728));
#29771=CARTESIAN_POINT('Ctrl Pts',(-0.909396227292148,-5.18618243478151,
4.6438839467319));
#29772=CARTESIAN_POINT('Ctrl Pts',(-0.88662313686,-5.182496726827,4.65258978726599));
#29773=CARTESIAN_POINT('Ctrl Pts',(-0.854886118918664,-5.18223104137204,
4.65886310574997));
#29774=CARTESIAN_POINT('Ctrl Pts',(-0.84722203253019,-5.1825134084958,4.65995935047192));
#29775=CARTESIAN_POINT('Ctrl Pts',(-0.834941493334292,-5.18354193434975,
4.661036848069));
#29776=CARTESIAN_POINT('Ctrl Pts',(-0.830357414107847,-5.18405325452173,
4.66128876278954));
#29777=CARTESIAN_POINT('Ctrl Pts',(-0.821749396602631,-5.18525652141284,
4.6614766362689));
#29778=CARTESIAN_POINT('Ctrl Pts',(-0.81773045401176,-5.18591867583012,
4.66144660123003));
#29779=CARTESIAN_POINT('Ctrl Pts',(-0.808785506788643,-5.18761806734741,
4.66111486035927));
#29780=CARTESIAN_POINT('Ctrl Pts',(-0.803879954994015,-5.1887046972058,
4.6607514048391));
#29781=CARTESIAN_POINT('Ctrl Pts',(-0.789765163415022,-5.19227888074625,
4.65917598249655));
#29782=CARTESIAN_POINT('Ctrl Pts',(-0.780742800229034,-5.19512838427145,
4.65750148702093));
#29783=CARTESIAN_POINT('Ctrl Pts',(-0.750108423554742,-5.20670671111326,
4.64948528566701));
#29784=CARTESIAN_POINT('Ctrl Pts',(-0.730633160772477,-5.21757743244348,
4.64009844156317));
#29785=CARTESIAN_POINT('Ctrl Pts',(-0.696424921417121,-5.24236094114524,
4.61539308723158));
#29786=CARTESIAN_POINT('Ctrl Pts',(-0.682131617948138,-5.25606733420563,
4.60019195379195));
#29787=CARTESIAN_POINT('Ctrl Pts',(-0.654795226139854,-5.28804986143137,
4.56080656181527));
#29788=CARTESIAN_POINT('Ctrl Pts',(-0.643602532663009,-5.30634185619752,
4.53533737515853));
#29789=CARTESIAN_POINT('Ctrl Pts',(-0.623508365378195,-5.34786498829097,
4.46952174021342));
#29790=CARTESIAN_POINT('Ctrl Pts',(-0.616850747770232,-5.37181868573423,
4.42457618200303));
#29791=CARTESIAN_POINT('Ctrl Pts',(-0.606819121617709,-5.43514820992187,
4.27073174534983));
#29792=CARTESIAN_POINT('Ctrl Pts',(-0.6126424198215,-5.46577252229136,4.14407324412986));
#29793=CARTESIAN_POINT('Ctrl Pts',(-0.6126424198215,-5.46577252229136,4.));
#29794=CARTESIAN_POINT('',(-1.10635903124561,-5.38757549311203,0.));
#29795=CARTESIAN_POINT('',(-1.10635903124561,-5.38757549311203,0.));
#29796=CARTESIAN_POINT('',(-0.61264241982148,-5.46577252229136,0.));
#29797=CARTESIAN_POINT('Origin',(-0.860389557721271,-5.43228587327326,0.));
#29798=CARTESIAN_POINT('',(-0.61264241982148,-5.46577252229136,0.));
#29799=CARTESIAN_POINT('Origin',(-1.69959346906221,-5.23081083962335,0.));
#29800=CARTESIAN_POINT('',(-1.93554040580225,-5.14817281542751,4.));
#29801=CARTESIAN_POINT('',(-1.46013497556791,-5.30264140340673,4.));
#29802=CARTESIAN_POINT('Ctrl Pts',(-1.93554040580225,-5.14817281542751,
4.));
#29803=CARTESIAN_POINT('Ctrl Pts',(-1.93554040580225,-5.14817281542751,
4.02673063961772));
#29804=CARTESIAN_POINT('Ctrl Pts',(-1.93519412785719,-5.14715875964944,
4.05414638576009));
#29805=CARTESIAN_POINT('Ctrl Pts',(-1.93134512857136,-5.1366280565286,4.19012241323843));
#29806=CARTESIAN_POINT('Ctrl Pts',(-1.92254467829738,-5.11261868251876,
4.28686359329027));
#29807=CARTESIAN_POINT('Ctrl Pts',(-1.88888888520001,-5.0658538399355,4.42646405387438));
#29808=CARTESIAN_POINT('Ctrl Pts',(-1.87046555218869,-5.04588954971901,
4.47482705790046));
#29809=CARTESIAN_POINT('Ctrl Pts',(-1.83007811213918,-5.01663049384449,
4.54353143773204));
#29810=CARTESIAN_POINT('Ctrl Pts',(-1.81038239552216,-5.00525451342013,
4.56934838942208));
#29811=CARTESIAN_POINT('Ctrl Pts',(-1.76993104710689,-4.99026126692246,
4.6071405640229));
#29812=CARTESIAN_POINT('Ctrl Pts',(-1.75139345652765,-4.98537155226774,
4.62089194101727));
#29813=CARTESIAN_POINT('Ctrl Pts',(-1.70949772546375,-4.98007101070696,
4.64388394673189));
#29814=CARTESIAN_POINT('Ctrl Pts',(-1.68642843781244,-4.97999317615251,
4.65258978726598));
#29815=CARTESIAN_POINT('Ctrl Pts',(-1.65504059286453,-4.98469552515,4.65886310574996));
#29816=CARTESIAN_POINT('Ctrl Pts',(-1.64751503604726,-4.98617334312011,
4.65995935047191));
#29817=CARTESIAN_POINT('Ctrl Pts',(-1.63554658755897,-4.98911030569358,
4.66103684806899));
#29818=CARTESIAN_POINT('Ctrl Pts',(-1.63109893405222,-4.99033243864725,
4.66128876278954));
#29819=CARTESIAN_POINT('Ctrl Pts',(-1.6227851279391,-4.9928674819397,4.66147663626889));
#29820=CARTESIAN_POINT('Ctrl Pts',(-1.61891924897263,-4.99415018527155,
4.66144660123003));
#29821=CARTESIAN_POINT('Ctrl Pts',(-1.610350272296,-4.99722795249295,4.66111486035926));
#29822=CARTESIAN_POINT('Ctrl Pts',(-1.60567510234486,-4.99906860150534,
4.6607514048391));
#29823=CARTESIAN_POINT('Ctrl Pts',(-1.59229321276246,-5.00480682078521,
4.65917598249655));
#29824=CARTESIAN_POINT('Ctrl Pts',(-1.58382769039864,-5.00903265075193,
4.65750148702093));
#29825=CARTESIAN_POINT('Ctrl Pts',(-1.5553817231016,-5.02526070150406,4.64948528566701));
#29826=CARTESIAN_POINT('Ctrl Pts',(-1.53784678859742,-5.03904418853065,
4.64009844156316));
#29827=CARTESIAN_POINT('Ctrl Pts',(-1.50793670435943,-5.06887391873794,
4.61539308723157));
#29828=CARTESIAN_POINT('Ctrl Pts',(-1.49596352744056,-5.08464752863713,
4.60019195379194));
#29829=CARTESIAN_POINT('Ctrl Pts',(-1.47396686151477,-5.12051265170942,
4.56080656181526));
#29830=CARTESIAN_POINT('Ctrl Pts',(-1.4657734670836,-5.14033036468258,4.53533737515852));
#29831=CARTESIAN_POINT('Ctrl Pts',(-1.45242234129827,-5.18448569842586,
4.46952174021348));
#29832=CARTESIAN_POINT('Ctrl Pts',(-1.449593873856,-5.20918596695366,4.42457618200312));
#29833=CARTESIAN_POINT('Ctrl Pts',(-1.44959267390549,-5.27330509167993,
4.2707317453498));
#29834=CARTESIAN_POINT('Ctrl Pts',(-1.46013497556793,-5.30264140340673,
4.14407324412983));
#29835=CARTESIAN_POINT('Ctrl Pts',(-1.46013497556793,-5.30264140340673,
4.));
#29836=CARTESIAN_POINT('',(-1.93554040580225,-5.14817281542751,0.));
#29837=CARTESIAN_POINT('',(-1.93554040580225,-5.14817281542751,0.));
#29838=CARTESIAN_POINT('',(-1.46013497556791,-5.30264140340673,0.));
#29839=CARTESIAN_POINT('Origin',(-1.69959346906221,-5.23081083962335,0.));
#29840=CARTESIAN_POINT('',(-1.46013497556791,-5.30264140340673,0.));
#29841=CARTESIAN_POINT('Origin',(-2.49694774856751,-4.90053588303602,0.));
#29842=CARTESIAN_POINT('',(-2.71706235187773,-4.78200503722117,4.));
#29843=CARTESIAN_POINT('',(-2.2716741623057,-5.00894165471237,4.));
#29844=CARTESIAN_POINT('Ctrl Pts',(-2.71706235187773,-4.78200503722117,
4.));
#29845=CARTESIAN_POINT('Ctrl Pts',(-2.71706235187773,-4.78200503722117,
4.02673063961772));
#29846=CARTESIAN_POINT('Ctrl Pts',(-2.71656170391563,-4.78105763595755,
4.0541463857601));
#29847=CARTESIAN_POINT('Ctrl Pts',(-2.71111272728885,-4.77125869941104,
4.19012241323842));
#29848=CARTESIAN_POINT('Ctrl Pts',(-2.69866473158208,-4.74892161436726,
4.28686359329027));
#29849=CARTESIAN_POINT('Ctrl Pts',(-2.65810766401411,-4.70799745058668,
4.4264640538744));
#29850=CARTESIAN_POINT('Ctrl Pts',(-2.636788049744,-4.69116099815549,4.47482705790047));
#29851=CARTESIAN_POINT('Ctrl Pts',(-2.59232072134732,-4.6685801573899,4.54353143773204));
#29852=CARTESIAN_POINT('Ctrl Pts',(-2.57108789627303,-4.66042532305449,
4.56934838942208));
#29853=CARTESIAN_POINT('Ctrl Pts',(-2.52878911058682,-4.65194465335057,
4.60714056402291));
#29854=CARTESIAN_POINT('Ctrl Pts',(-2.50971482861277,-4.65001505726266,
4.62089194101728));
#29855=CARTESIAN_POINT('Ctrl Pts',(-2.46750571613677,-4.65133371044068,
4.64388394673189));
#29856=CARTESIAN_POINT('Ctrl Pts',(-2.44470827369085,-4.65486566583135,
4.65258978726599));
#29857=CARTESIAN_POINT('Ctrl Pts',(-2.4144424746492,-4.66442026184278,4.65886310574998));
#29858=CARTESIAN_POINT('Ctrl Pts',(-2.4072407515879,-4.66705714187622,4.65995935047192));
#29859=CARTESIAN_POINT('Ctrl Pts',(-2.39587909673009,-4.67183022340341,
4.661036848069));
#29860=CARTESIAN_POINT('Ctrl Pts',(-2.39167738493325,-4.67373307616942,
4.66128876278955));
#29861=CARTESIAN_POINT('Ctrl Pts',(-2.38386250371065,-4.67753747468404,
4.6614766362689));
#29862=CARTESIAN_POINT('Ctrl Pts',(-2.38024487913883,-4.67940914251738,
4.66144660123004));
#29863=CARTESIAN_POINT('Ctrl Pts',(-2.37226286965329,-4.68378950059938,
4.66111486035927));
#29864=CARTESIAN_POINT('Ctrl Pts',(-2.36793319974582,-4.68633884587832,
4.66075140483911));
#29865=CARTESIAN_POINT('Ctrl Pts',(-2.35561371869349,-4.69409980689487,
4.65917598249656));
#29866=CARTESIAN_POINT('Ctrl Pts',(-2.34791348640789,-4.69959790934462,
4.65750148702093));
#29867=CARTESIAN_POINT('Ctrl Pts',(-2.32235636260971,-4.72007609553974,
4.64948528566702));
#29868=CARTESIAN_POINT('Ctrl Pts',(-2.30719352466623,-4.73643295306732,
4.64009844156317));
#29869=CARTESIAN_POINT('Ctrl Pts',(-2.28231808108542,-4.77057439782324,
4.61539308723158));
#29870=CARTESIAN_POINT('Ctrl Pts',(-2.2729598500691,-4.7880268259359,4.60019195379196));
#29871=CARTESIAN_POINT('Ctrl Pts',(-2.25684454094365,-4.82689142649518,
4.56080656181528));
#29872=CARTESIAN_POINT('Ctrl Pts',(-2.25185219412135,-4.84774687981073,
4.53533737515855));
#29873=CARTESIAN_POINT('Ctrl Pts',(-2.24557285886215,-4.89344716434407,
4.46952174021337));
#29874=CARTESIAN_POINT('Ctrl Pts',(-2.2466431878412,-4.91828580136974,4.42457618200295));
#29875=CARTESIAN_POINT('Ctrl Pts',(-2.25667244363945,-4.98161570098457,
4.27073174534984));
#29876=CARTESIAN_POINT('Ctrl Pts',(-2.27167416230572,-5.00894165471236,
4.14407324412988));
#29877=CARTESIAN_POINT('Ctrl Pts',(-2.27167416230572,-5.00894165471236,
4.));
#29878=CARTESIAN_POINT('',(-2.71706235187773,-4.78200503722117,0.));
#29879=CARTESIAN_POINT('',(-2.71706235187773,-4.78200503722117,0.));
#29880=CARTESIAN_POINT('',(-2.2716741623057,-5.00894165471237,0.));
#29881=CARTESIAN_POINT('Origin',(-2.49694774856751,-4.90053588303602,0.));
#29882=CARTESIAN_POINT('',(-2.2716741623057,-5.00894165471237,0.));
#29883=CARTESIAN_POINT('Origin',(-3.2328188876086,-4.44959346906221,0.));
#29884=CARTESIAN_POINT('',(-3.43168120543702,-4.29808842443363,4.));
#29885=CARTESIAN_POINT('',(-3.02727719191323,-4.59190513875472,4.));
#29886=CARTESIAN_POINT('Ctrl Pts',(-3.43168120543702,-4.29808842443363,
4.));
#29887=CARTESIAN_POINT('Ctrl Pts',(-3.43168120543702,-4.29808842443363,
4.02673063961774));
#29888=CARTESIAN_POINT('Ctrl Pts',(-3.43103851507225,-4.2972310058478,4.05414638576013));
#29889=CARTESIAN_POINT('Ctrl Pts',(-3.42412373299319,-4.28840511821421,
4.19012241323849));
#29890=CARTESIAN_POINT('Ctrl Pts',(-3.40833470282043,-4.26829033530279,
4.28686359329032));
#29891=CARTESIAN_POINT('Ctrl Pts',(-3.36187501038667,-4.23421453905677,
4.4264640538742));
#29892=CARTESIAN_POINT('Ctrl Pts',(-3.33818407451688,-4.22092049374668,
4.47482705790034));
#29893=CARTESIAN_POINT('Ctrl Pts',(-3.29073179097662,-4.20557388333114,
4.54353143773207));
#29894=CARTESIAN_POINT('Ctrl Pts',(-3.2684846800661,-4.20084099417036,4.5693483894221));
#29895=CARTESIAN_POINT('Ctrl Pts',(-3.2253799935942,-4.19908172349404,4.60714056402291));
#29896=CARTESIAN_POINT('Ctrl Pts',(-3.20623869235145,-4.20015975903259,
4.62089194101729));
#29897=CARTESIAN_POINT('Ctrl Pts',(-3.16475552689651,-4.20806513733182,
4.6438839467319));
#29898=CARTESIAN_POINT('Ctrl Pts',(-3.14279127834937,-4.215119914204,4.65258978726599));
#29899=CARTESIAN_POINT('Ctrl Pts',(-3.11439276963288,-4.22929149136568,
4.65886310574998));
#29900=CARTESIAN_POINT('Ctrl Pts',(-3.10769221065044,-4.23302250472472,
4.65995935047192));
#29901=CARTESIAN_POINT('Ctrl Pts',(-3.09721711107279,-4.23951417609749,
4.661036848069));
#29902=CARTESIAN_POINT('Ctrl Pts',(-3.09336480107502,-4.24205089412554,
4.66128876278955));
#29903=CARTESIAN_POINT('Ctrl Pts',(-3.08624127305476,-4.24703097094482,
4.6614766362689));
#29904=CARTESIAN_POINT('Ctrl Pts',(-3.08296098080076,-4.24944551660589,
4.66144660123004));
#29905=CARTESIAN_POINT('Ctrl Pts',(-3.07576248207062,-4.25502060659492,
4.66111486035927));
#29906=CARTESIAN_POINT('Ctrl Pts',(-3.0718849230493,-4.25821587479886,4.66075140483911));
#29907=CARTESIAN_POINT('Ctrl Pts',(-3.06093119703656,-4.26780847693471,
4.65917598249656));
#29908=CARTESIAN_POINT('Ctrl Pts',(-3.05418586010366,-4.274443470338,4.65750148702094));
#29909=CARTESIAN_POINT('Ctrl Pts',(-3.03214688101148,-4.2986675510688,4.64948528566701));
#29910=CARTESIAN_POINT('Ctrl Pts',(-3.01972949902144,-4.31719501897975,
4.64009844156317));
#29911=CARTESIAN_POINT('Ctrl Pts',(-3.00050121207563,-4.35480750260545,
4.61539308723158));
#29912=CARTESIAN_POINT('Ctrl Pts',(-2.99398835766767,-4.37350901223015,
4.60019195379196));
#29913=CARTESIAN_POINT('Ctrl Pts',(-2.98415121773687,-4.41441611482645,
4.56080656181527));
#29914=CARTESIAN_POINT('Ctrl Pts',(-2.98248284667088,-4.43579577800849,
4.53533737515853));
#29915=CARTESIAN_POINT('Ctrl Pts',(-2.98342992001184,-4.48191572065595,
4.46952174021345));
#29916=CARTESIAN_POINT('Ctrl Pts',(-2.98837269036046,-4.50628111650125,
4.42457618200307));
#29917=CARTESIAN_POINT('Ctrl Pts',(-3.00818544834456,-4.56726239869638,
4.27073174534983));
#29918=CARTESIAN_POINT('Ctrl Pts',(-3.02727719191324,-4.59190513875471,
4.14407324412986));
#29919=CARTESIAN_POINT('Ctrl Pts',(-3.02727719191324,-4.59190513875471,
4.));
#29920=CARTESIAN_POINT('',(-3.43168120543702,-4.29808842443363,0.));
#29921=CARTESIAN_POINT('',(-3.43168120543702,-4.29808842443363,0.));
#29922=CARTESIAN_POINT('',(-3.02727719191323,-4.59190513875472,0.));
#29923=CARTESIAN_POINT('Origin',(-3.2328188876086,-4.44959346906221,0.));
#29924=CARTESIAN_POINT('',(-3.02727719191323,-4.59190513875472,0.));
#29925=CARTESIAN_POINT('Origin',(-3.88908729652601,-3.88908729652601,0.));
#29926=CARTESIAN_POINT('',(-4.0618006786215,-3.70833861009886,4.));
#29927=CARTESIAN_POINT('',(-3.70833861009886,-4.06180067862149,4.));
#29928=CARTESIAN_POINT('Ctrl Pts',(-4.06180067862149,-3.70833861009886,
4.));
#29929=CARTESIAN_POINT('Ctrl Pts',(-4.06180067862149,-3.70833861009886,
4.02673063961774));
#29930=CARTESIAN_POINT('Ctrl Pts',(-4.06103177102382,-3.70759228668204,
4.05414638576013));
#29931=CARTESIAN_POINT('Ctrl Pts',(-4.0528214483761,-3.69995677060634,4.1901224132385));
#29932=CARTESIAN_POINT('Ctrl Pts',(-4.03408016206102,-3.68255958253971,
4.28686359329032));
#29933=CARTESIAN_POINT('Ctrl Pts',(-3.98286183657994,-3.6561712130228,4.42646405387434));
#29934=CARTESIAN_POINT('Ctrl Pts',(-3.95738292857724,-3.64674691834979,
4.47482705790044));
#29935=CARTESIAN_POINT('Ctrl Pts',(-3.90811412259944,-3.63901242276528,
4.54353143773206));
#29936=CARTESIAN_POINT('Ctrl Pts',(-3.88540052355723,-3.63781801821782,
4.5693483894221));
#29937=CARTESIAN_POINT('Ctrl Pts',(-3.84255131673681,-3.64282346565183,
4.60714056402291));
#29938=CARTESIAN_POINT('Ctrl Pts',(-3.8238143185883,-3.64688258800408,4.62089194101729));
#29939=CARTESIAN_POINT('Ctrl Pts',(-3.78407855336265,-3.66118003477435,
4.6438839467319));
#29940=CARTESIAN_POINT('Ctrl Pts',(-3.76348833140868,-3.67158392110798,
4.65258978726599));
#29941=CARTESIAN_POINT('Ctrl Pts',(-3.73765637855118,-3.69002352815742,
4.65886310574998));
#29942=CARTESIAN_POINT('Ctrl Pts',(-3.73162197364763,-3.69475680491064,
4.65995935047192));
#29943=CARTESIAN_POINT('Ctrl Pts',(-3.72229136106663,-3.70280721963518,
4.661036848069));
#29944=CARTESIAN_POINT('Ctrl Pts',(-3.71888330952516,-3.70591534050852,
4.66128876278955));
#29945=CARTESIAN_POINT('Ctrl Pts',(-3.71262653960873,-3.71194846961323,
4.6614766362689));
#29946=CARTESIAN_POINT('Ctrl Pts',(-3.70976435135453,-3.71484643897442,
4.66144660123004));
#29947=CARTESIAN_POINT('Ctrl Pts',(-3.70352661430895,-3.72147898365232,
4.66111486035927));
#29948=CARTESIAN_POINT('Ctrl Pts',(-3.70019664454577,-3.72524149667359,
4.66075140483911));
#29949=CARTESIAN_POINT('Ctrl Pts',(-3.69087839066037,-3.73642953822814,
4.65917598249656));
#29950=CARTESIAN_POINT('Ctrl Pts',(-3.68525404166195,-3.74403804702711,
4.65750148702093));
#29951=CARTESIAN_POINT('Ctrl Pts',(-3.6672758800842,-3.77141154503088,4.64948528566701));
#29952=CARTESIAN_POINT('Ctrl Pts',(-3.65790971120312,-3.79165341557609,
4.64009844156317));
#29953=CARTESIAN_POINT('Ctrl Pts',(-3.64480204513195,-3.83181079389602,
4.61539308723158));
#29954=CARTESIAN_POINT('Ctrl Pts',(-3.6412949354228,-3.85130089179906,4.60019195379196));
#29955=CARTESIAN_POINT('Ctrl Pts',(-3.63797818771934,-3.89324322780355,
4.56080656181527));
#29956=CARTESIAN_POINT('Ctrl Pts',(-3.6396748732423,-3.9146206625895,4.53533737515852));
#29957=CARTESIAN_POINT('Ctrl Pts',(-3.64782503509459,-3.96002463729987,
4.46952174021346));
#29958=CARTESIAN_POINT('Ctrl Pts',(-3.65651853940272,-3.98331683505495,
4.42457618200308));
#29959=CARTESIAN_POINT('Ctrl Pts',(-3.68562694371632,-4.04044793827742,
4.27073174534979));
#29960=CARTESIAN_POINT('Ctrl Pts',(-3.70833861009888,-4.06180067862148,
4.14407324412981));
#29961=CARTESIAN_POINT('Ctrl Pts',(-3.70833861009888,-4.06180067862148,
4.));
#29962=CARTESIAN_POINT('',(-4.0618006786215,-3.70833861009886,0.));
#29963=CARTESIAN_POINT('',(-4.0618006786215,-3.70833861009886,0.));
#29964=CARTESIAN_POINT('',(-3.70833861009886,-4.06180067862149,0.));
#29965=CARTESIAN_POINT('Origin',(-3.88908729652601,-3.88908729652601,0.));
#29966=CARTESIAN_POINT('',(-3.70833861009886,-4.06180067862149,0.));
#29967=CARTESIAN_POINT('Origin',(-4.44959346906221,-3.2328188876086,0.));
#29968=CARTESIAN_POINT('',(-4.59190513875472,-3.02727719191322,4.));
#29969=CARTESIAN_POINT('',(-4.29808842443363,-3.43168120543702,4.));
#29970=CARTESIAN_POINT('Ctrl Pts',(-4.59190513875472,-3.02727719191322,
4.));
#29971=CARTESIAN_POINT('Ctrl Pts',(-4.59190513875472,-3.02727719191322,
4.02673063961772));
#29972=CARTESIAN_POINT('Ctrl Pts',(-4.59102894698104,-3.02666034062482,
4.05414638576009));
#29973=CARTESIAN_POINT('Ctrl Pts',(-4.58172524915676,-3.02040320785364,
4.1901224132384));
#29974=CARTESIAN_POINT('Ctrl Pts',(-4.56049317936721,-3.00615199113995,
4.28686359329025));
#29975=CARTESIAN_POINT('Ctrl Pts',(-4.50577738599604,-2.98810081758766,
4.42646405387439));
#29976=CARTESIAN_POINT('Ctrl Pts',(-4.47913788113512,-2.98277833096402,
4.47482705790046));
#29977=CARTESIAN_POINT('Ctrl Pts',(-4.42926571423673,-2.98284639916111,
4.54353143773203));
#29978=CARTESIAN_POINT('Ctrl Pts',(-4.40664491125336,-2.98521988943094,
4.56934838942208));
#29979=CARTESIAN_POINT('Ctrl Pts',(-4.3651062737647,-2.99686680424732,4.6071405640229));
#29980=CARTESIAN_POINT('Ctrl Pts',(-4.34723494578937,-3.00380706434951,
4.62089194101728));
#29981=CARTESIAN_POINT('Ctrl Pts',(-4.31022500720832,-3.02414452900082,
4.64388394673189));
#29982=CARTESIAN_POINT('Ctrl Pts',(-4.29151581144706,-3.03764134658585,
4.65258978726599));
#29983=CARTESIAN_POINT('Ctrl Pts',(-4.26888648285923,-3.05989493919994,
4.65886310574997));
#29984=CARTESIAN_POINT('Ctrl Pts',(-4.26366681911034,-3.06551393036483,
4.65995935047192));
#29985=CARTESIAN_POINT('Ctrl Pts',(-4.25571044417423,-3.07492486051285,
4.66103684806901));
#29986=CARTESIAN_POINT('Ctrl Pts',(-4.25283056862868,-3.07852785198032,
4.66128876278955));
#29987=CARTESIAN_POINT('Ctrl Pts',(-4.24759461925647,-3.08546547770909,
4.6614766362689));
#29988=CARTESIAN_POINT('Ctrl Pts',(-4.24522101157593,-3.08877551314693,
4.66144660123004));
#29989=CARTESIAN_POINT('Ctrl Pts',(-4.24009763000285,-3.09630219725155,
4.66111486035927));
#29990=CARTESIAN_POINT('Ctrl Pts',(-4.23739724440491,-3.1005393095325,4.66075140483911));
#29991=CARTESIAN_POINT('Ctrl Pts',(-4.22994390898303,-3.1130473037917,4.65917598249656));
#29992=CARTESIAN_POINT('Ctrl Pts',(-4.22557903805758,-3.12144198124853,
4.65750148702094));
#29993=CARTESIAN_POINT('Ctrl Pts',(-4.2121043759984,-3.15129087015696,4.64948528566702));
#29994=CARTESIAN_POINT('Ctrl Pts',(-4.20602004638866,-3.17274872130469,
4.64009844156318));
#29995=CARTESIAN_POINT('Ctrl Pts',(-4.19935575543264,-3.21446218638993,
4.61539308723159));
#29996=CARTESIAN_POINT('Ctrl Pts',(-4.19894074710277,-3.23426096167702,
4.60019195379196));
#29997=CARTESIAN_POINT('Ctrl Pts',(-4.20222606096277,-3.27620577157863,
4.56080656181528));
#29998=CARTESIAN_POINT('Ctrl Pts',(-4.20724602504612,-3.29705459457642,
4.53533737515853));
#29999=CARTESIAN_POINT('Ctrl Pts',(-4.22239859137612,-3.34062460480519,
4.46952174021345));
#30000=CARTESIAN_POINT('Ctrl Pts',(-4.2346287667156,-3.36227007325895,4.42457618200306));
#30001=CARTESIAN_POINT('Ctrl Pts',(-4.27231607183921,-3.41414424014012,
4.27073174534987));
#30002=CARTESIAN_POINT('Ctrl Pts',(-4.29808842443364,-3.431681205437,4.14407324412991));
#30003=CARTESIAN_POINT('Ctrl Pts',(-4.29808842443364,-3.431681205437,4.));
#30004=CARTESIAN_POINT('',(-4.59190513875472,-3.02727719191322,0.));
#30005=CARTESIAN_POINT('',(-4.59190513875472,-3.02727719191322,0.));
#30006=CARTESIAN_POINT('',(-4.29808842443363,-3.43168120543702,0.));
#30007=CARTESIAN_POINT('Origin',(-4.44959346906221,-3.2328188876086,0.));
#30008=CARTESIAN_POINT('',(-4.29808842443363,-3.43168120543702,0.));
#30009=CARTESIAN_POINT('Origin',(-4.90053588303603,-2.49694774856751,0.));
#30010=CARTESIAN_POINT('',(-5.00894165471237,-2.2716741623057,4.));
#30011=CARTESIAN_POINT('',(-4.78200503722117,-2.71706235187773,4.));
#30012=CARTESIAN_POINT('Ctrl Pts',(-5.00894165471237,-2.2716741623057,4.));
#30013=CARTESIAN_POINT('Ctrl Pts',(-5.00894165471237,-2.2716741623057,4.02673063961771));
#30014=CARTESIAN_POINT('Ctrl Pts',(-5.00797975351207,-2.27120197207165,
4.05414638576009));
#30015=CARTESIAN_POINT('Ctrl Pts',(-4.99781176842887,-2.26647729398004,
4.19012241323838));
#30016=CARTESIAN_POINT('Ctrl Pts',(-4.97461171918825,-2.25572296087186,
4.28686359329023));
#30017=CARTESIAN_POINT('Ctrl Pts',(-4.91774574235115,-2.24645346308547,
4.42646405387434));
#30018=CARTESIAN_POINT('Ctrl Pts',(-4.89060159365313,-2.24536384179618,
4.47482705790043));
#30019=CARTESIAN_POINT('Ctrl Pts',(-4.84135408409937,-2.25323279770997,
4.54353143773201));
#30020=CARTESIAN_POINT('Ctrl Pts',(-4.81938307641843,-2.25911573958947,
4.56934838942206));
#30021=CARTESIAN_POINT('Ctrl Pts',(-4.78017782737534,-2.27711733609156,
4.60714056402289));
#30022=CARTESIAN_POINT('Ctrl Pts',(-4.76361222097949,-2.28676784170657,
4.62089194101727));
#30023=CARTESIAN_POINT('Ctrl Pts',(-4.73023941655985,-2.31264454836302,
4.64388394673188));
#30024=CARTESIAN_POINT('Ctrl Pts',(-4.7138719294832,-2.32890196075715,4.65258978726598));
#30025=CARTESIAN_POINT('Ctrl Pts',(-4.69500243433731,-2.3544215816303,4.65886310574996));
#30026=CARTESIAN_POINT('Ctrl Pts',(-4.69072603718765,-2.36078792899601,
4.65995935047191));
#30027=CARTESIAN_POINT('Ctrl Pts',(-4.6843398122531,-2.37132764623413,4.66103684806899));
#30028=CARTESIAN_POINT('Ctrl Pts',(-4.68205902479715,-2.37533679068818,
4.66128876278954));
#30029=CARTESIAN_POINT('Ctrl Pts',(-4.67797282241978,-2.38300808567095,
4.66147663626889));
#30030=CARTESIAN_POINT('Ctrl Pts',(-4.67614624141154,-2.38664868312759,
4.66144660123003));
#30031=CARTESIAN_POINT('Ctrl Pts',(-4.67226336996884,-2.39488417471662,
4.66111486035926));
#30032=CARTESIAN_POINT('Ctrl Pts',(-4.67025906099163,-2.39949155449073,
4.6607514048391));
#30033=CARTESIAN_POINT('Ctrl Pts',(-4.66485416988756,-2.41301151312426,
4.65917598249655));
#30034=CARTESIAN_POINT('Ctrl Pts',(-4.66185625464343,-2.42198565441961,
4.65750148702092));
#30035=CARTESIAN_POINT('Ctrl Pts',(-4.65321688300255,-2.45357495552502,
4.64948528566701));
#30036=CARTESIAN_POINT('Ctrl Pts',(-4.65056420905188,-2.47572042376548,
4.64009844156316));
#30037=CARTESIAN_POINT('Ctrl Pts',(-4.65050739017188,-2.51796285166656,
4.61539308723158));
#30038=CARTESIAN_POINT('Ctrl Pts',(-4.6531947021037,-2.53758279278175,4.60019195379196));
#30039=CARTESIAN_POINT('Ctrl Pts',(-4.66300118219659,-2.57849725615388,
4.56080656181527));
#30040=CARTESIAN_POINT('Ctrl Pts',(-4.6712208166643,-2.59830410014803,4.53533737515853));
#30041=CARTESIAN_POINT('Ctrl Pts',(-4.69300268100046,-2.63896730764278,
4.46952174021343));
#30042=CARTESIAN_POINT('Ctrl Pts',(-4.70846837986481,-2.6584330635247,4.42457618200304));
#30043=CARTESIAN_POINT('Ctrl Pts',(-4.75380659926932,-2.70377297991549,
4.27073174534987));
#30044=CARTESIAN_POINT('Ctrl Pts',(-4.78200503722118,-2.71706235187771,
4.14407324412992));
#30045=CARTESIAN_POINT('Ctrl Pts',(-4.78200503722118,-2.71706235187771,
4.));
#30046=CARTESIAN_POINT('',(-5.00894165471237,-2.2716741623057,0.));
#30047=CARTESIAN_POINT('',(-5.00894165471237,-2.2716741623057,0.));
#30048=CARTESIAN_POINT('',(-4.78200503722117,-2.71706235187773,0.));
#30049=CARTESIAN_POINT('Origin',(-4.90053588303603,-2.49694774856751,0.));
#30050=CARTESIAN_POINT('',(-4.78200503722117,-2.71706235187773,0.));
#30051=CARTESIAN_POINT('Origin',(-5.23081083962335,-1.69959346906221,0.));
#30052=CARTESIAN_POINT('',(-5.30264140340673,-1.46013497556791,4.));
#30053=CARTESIAN_POINT('',(-5.14817281542751,-1.93554040580225,4.));
#30054=CARTESIAN_POINT('Ctrl Pts',(-5.30264140340673,-1.46013497556791,
4.));
#30055=CARTESIAN_POINT('Ctrl Pts',(-5.30264140340673,-1.46013497556791,
4.02673063961772));
#30056=CARTESIAN_POINT('Ctrl Pts',(-5.30161747797973,-1.45981907327888,
4.05414638576009));
#30057=CARTESIAN_POINT('Ctrl Pts',(-5.29083557517596,-1.45674318712176,
4.19012241323843));
#30058=CARTESIAN_POINT('Ctrl Pts',(-5.26623880869311,-1.4497505449918,4.28686359329027));
#30059=CARTESIAN_POINT('Ctrl Pts',(-5.20862287746719,-1.44949096877052,
4.42646405387427));
#30060=CARTESIAN_POINT('Ctrl Pts',(-5.1816424639593,-1.45266104290795,4.47482705790038));
#30061=CARTESIAN_POINT('Ctrl Pts',(-5.13423224887844,-1.46813712672828,
4.54353143773205));
#30062=CARTESIAN_POINT('Ctrl Pts',(-5.11345203562664,-1.47738466266403,
4.56934838942208));
#30063=CARTESIAN_POINT('Ctrl Pts',(-5.07754553837534,-1.50129768180205,
4.60714056402289));
#30064=CARTESIAN_POINT('Ctrl Pts',(-5.06269355376651,-1.51342080545345,
4.62089194101727));
#30065=CARTESIAN_POINT('Ctrl Pts',(-5.03377963271108,-1.54419958371732,
4.64388394673188));
#30066=CARTESIAN_POINT('Ctrl Pts',(-5.02015687617144,-1.56281727947213,
4.65258978726598));
#30067=CARTESIAN_POINT('Ctrl Pts',(-5.00551184406225,-1.59097455084368,
4.65886310574997));
#30068=CARTESIAN_POINT('Ctrl Pts',(-5.0022840126022,-1.59793149380938,4.65995935047191));
#30069=CARTESIAN_POINT('Ctrl Pts',(-4.99762518772176,-1.60934047531987,
4.66103684806899));
#30070=CARTESIAN_POINT('Ctrl Pts',(-4.99599964891207,-1.61365705431845,
4.66128876278954));
#30071=CARTESIAN_POINT('Ctrl Pts',(-4.99316380939342,-1.62187312581316,
4.6614766362689));
#30072=CARTESIAN_POINT('Ctrl Pts',(-4.99192923154399,-1.62575464169678,
4.66144660123003));
#30073=CARTESIAN_POINT('Ctrl Pts',(-4.98938247941308,-1.63449615563528,
4.66111486035926));
#30074=CARTESIAN_POINT('Ctrl Pts',(-4.98812359979553,-1.63936035392148,
4.6607514048391));
#30075=CARTESIAN_POINT('Ctrl Pts',(-4.98490023936606,-1.6535593706776,4.65917598249655));
#30076=CARTESIAN_POINT('Ctrl Pts',(-4.98334309842607,-1.66289200266933,
4.65750148702093));
#30077=CARTESIAN_POINT('Ctrl Pts',(-4.97975174720573,-1.69544388253963,
4.64948528566701));
#30078=CARTESIAN_POINT('Ctrl Pts',(-4.98059604655052,-1.71773167294815,
4.64009844156316));
#30079=CARTESIAN_POINT('Ctrl Pts',(-4.98714809881592,-1.75946291489558,
4.61539308723157));
#30080=CARTESIAN_POINT('Ctrl Pts',(-4.992871560471,-1.77842091377376,4.60019195379195));
#30081=CARTESIAN_POINT('Ctrl Pts',(-5.00895773871105,-1.81729758074086,
4.56080656181526));
#30082=CARTESIAN_POINT('Ctrl Pts',(-5.02017464888312,-1.83557473549708,
4.53533737515853));
#30083=CARTESIAN_POINT('Ctrl Pts',(-5.04804946943568,-1.87232987713589,
4.46952174021334));
#30084=CARTESIAN_POINT('Ctrl Pts',(-5.06636987499114,-1.88913660893299,
4.42457618200292));
#30085=CARTESIAN_POINT('Ctrl Pts',(-5.11824263124585,-1.9268258556173,4.27073174534982));
#30086=CARTESIAN_POINT('Ctrl Pts',(-5.14817281542752,-1.93554040580223,
4.14407324412985));
#30087=CARTESIAN_POINT('Ctrl Pts',(-5.14817281542752,-1.93554040580223,
4.));
#30088=CARTESIAN_POINT('',(-5.30264140340673,-1.46013497556791,0.));
#30089=CARTESIAN_POINT('',(-5.30264140340673,-1.46013497556791,0.));
#30090=CARTESIAN_POINT('',(-5.14817281542751,-1.93554040580225,0.));
#30091=CARTESIAN_POINT('Origin',(-5.23081083962335,-1.69959346906221,0.));
#30092=CARTESIAN_POINT('',(-5.14817281542751,-1.93554040580225,0.));
#30093=CARTESIAN_POINT('Origin',(-5.43228587327326,-0.860389557721269,0.));
#30094=CARTESIAN_POINT('',(-5.46577252229136,-0.612642419821477,4.));
#30095=CARTESIAN_POINT('',(-5.38757549311203,-1.1063590312456,4.));
#30096=CARTESIAN_POINT('Ctrl Pts',(-5.46577252229136,-0.612642419821477,
4.));
#30097=CARTESIAN_POINT('Ctrl Pts',(-5.46577252229136,-0.612642419821477,
4.02673063961772));
#30098=CARTESIAN_POINT('Ctrl Pts',(-5.46471178507989,-0.612490584040255,
4.0541463857601));
#30099=CARTESIAN_POINT('Ctrl Pts',(-5.45358145078565,-0.611139228343087,
4.19012241323848));
#30100=CARTESIAN_POINT('Ctrl Pts',(-5.42819362108337,-0.608080459247839,
4.28686359329031));
#30101=CARTESIAN_POINT('Ctrl Pts',(-5.37124643091165,-0.61683719621971,
4.42646405387439));
#30102=CARTESIAN_POINT('Ctrl Pts',(-5.34509409991729,-0.624188908037767,
4.47482705790046));
#30103=CARTESIAN_POINT('Ctrl Pts',(-5.30068857615023,-0.646891047218764,
4.54353143773204));
#30104=CARTESIAN_POINT('Ctrl Pts',(-5.2816108351434,-0.659275472185209,
4.56934838942208));
#30105=CARTESIAN_POINT('Ctrl Pts',(-5.24988722681302,-0.688511096065241,
4.6071405640229));
#30106=CARTESIAN_POINT('Ctrl Pts',(-5.23711456914321,-0.702808326214393,
4.62089194101728));
#30107=CARTESIAN_POINT('Ctrl Pts',(-5.21337148814816,-0.737731300415899,
4.64388394673189));
#30108=CARTESIAN_POINT('Ctrl Pts',(-5.20282889962289,-0.758250850073326,
4.65258978726599));
#30109=CARTESIAN_POINT('Ctrl Pts',(-5.19276893984501,-0.788352446473459,
4.65886310574997));
#30110=CARTESIAN_POINT('Ctrl Pts',(-5.19066915399765,-0.795728682014567,
4.65995935047192));
#30111=CARTESIAN_POINT('Ctrl Pts',(-5.1878524449016,-0.807726000808509,
4.661036848069));
#30112=CARTESIAN_POINT('Ctrl Pts',(-5.18692218089855,-0.812243725850724,
4.66128876278954));
#30113=CARTESIAN_POINT('Ctrl Pts',(-5.1854065320192,-0.82080226690951,4.6614766362689));
#30114=CARTESIAN_POINT('Ctrl Pts',(-5.18479435673256,-0.824829125416977,
4.66144660123004));
#30115=CARTESIAN_POINT('Ctrl Pts',(-5.18364643340307,-0.833861416620456,
4.66111486035927));
#30116=CARTESIAN_POINT('Ctrl Pts',(-5.18316398093936,-0.8388626607136,4.6607514048391));
#30117=CARTESIAN_POINT('Ctrl Pts',(-5.18220152101598,-0.853391108675958,
4.65917598249656));
#30118=CARTESIAN_POINT('Ctrl Pts',(-5.18212349635793,-0.86285243099119,
4.65750148702093));
#30119=CARTESIAN_POINT('Ctrl Pts',(-5.18366859654418,-0.895565354310466,
4.64948528566701));
#30120=CARTESIAN_POINT('Ctrl Pts',(-5.18798907973249,-0.917446667518258,
4.64009844156316));
#30121=CARTESIAN_POINT('Ctrl Pts',(-5.2009886698715,-0.957639161837225,
4.61539308723158));
#30122=CARTESIAN_POINT('Ctrl Pts',(-5.20960735062881,-0.975468409628027,
4.60019195379196));
#30123=CARTESIAN_POINT('Ctrl Pts',(-5.23157713192079,-1.01135000762512,
4.56080656181526));
#30124=CARTESIAN_POINT('Ctrl Pts',(-5.245515120242,-1.02764742893492,4.53533737515851));
#30125=CARTESIAN_POINT('Ctrl Pts',(-5.27879652641764,-1.05958947114722,
4.46952174021343));
#30126=CARTESIAN_POINT('Ctrl Pts',(-5.2995205294775,-1.07332334134435,4.42457618200303));
#30127=CARTESIAN_POINT('Ctrl Pts',(-5.35665054316768,-1.10243388398541,
4.27073174534983));
#30128=CARTESIAN_POINT('Ctrl Pts',(-5.38757549311203,-1.10635903124558,
4.14407324412986));
#30129=CARTESIAN_POINT('Ctrl Pts',(-5.38757549311203,-1.10635903124558,
4.));
#30130=CARTESIAN_POINT('',(-5.46577252229136,-0.612642419821477,0.));
#30131=CARTESIAN_POINT('',(-5.46577252229136,-0.612642419821477,0.));
#30132=CARTESIAN_POINT('',(-5.38757549311203,-1.1063590312456,0.));
#30133=CARTESIAN_POINT('Origin',(-5.43228587327326,-0.860389557721269,0.));
#30134=CARTESIAN_POINT('',(-5.38757549311203,-1.1063590312456,0.));
#30135=CARTESIAN_POINT('Origin',(-5.5,1.11022302462516E-15,0.));
#30136=CARTESIAN_POINT('',(-5.49431818181818,0.249935425544578,4.));
#30137=CARTESIAN_POINT('',(-5.25,-6.78278558411441E-16,4.66143782776615));
#30138=CARTESIAN_POINT('Ctrl Pts',(-5.49431818181818,0.249935425544578,
4.));
#30139=CARTESIAN_POINT('Ctrl Pts',(-5.49431818181818,0.249935425544578,
4.1114335267762));
#30140=CARTESIAN_POINT('Ctrl Pts',(-5.4756767400248,0.250197727297926,4.21120478468484));
#30141=CARTESIAN_POINT('Ctrl Pts',(-5.42857544323548,0.240569456691875,
4.36489144191036));
#30142=CARTESIAN_POINT('Ctrl Pts',(-5.4017694101364,0.232168981737913,4.425924297522));
#30143=CARTESIAN_POINT('Ctrl Pts',(-5.354112808079,0.204293630300537,4.51536926219335));
#30144=CARTESIAN_POINT('Ctrl Pts',(-5.33487327574923,0.189393579953126,
4.54624819863964));
#30145=CARTESIAN_POINT('Ctrl Pts',(-5.30503927476288,0.157570272463533,
4.59049297273665));
#30146=CARTESIAN_POINT('Ctrl Pts',(-5.29273012882291,0.141503389631088,
4.6074172319051));
#30147=CARTESIAN_POINT('Ctrl Pts',(-5.27400968904813,0.108133425552988,
4.63197965561651));
#30148=CARTESIAN_POINT('Ctrl Pts',(-5.26698529556665,0.0923722545750434,
4.64078922803164));
#30149=CARTESIAN_POINT('Ctrl Pts',(-5.25718642825102,0.0612525257750982,
4.65284375994342));
#30150=CARTESIAN_POINT('Ctrl Pts',(-5.25391607094643,0.0466559930935807,
4.65676521233374));
#30151=CARTESIAN_POINT('Ctrl Pts',(-5.25122338487753,0.0254407476598933,
4.65998297001336));
#30152=CARTESIAN_POINT('Ctrl Pts',(-5.25067352981899,0.0193427404519049,
4.66063713008572));
#30153=CARTESIAN_POINT('Ctrl Pts',(-5.25012437329208,0.00895709567438105,
4.66129014831286));
#30154=CARTESIAN_POINT('Ctrl Pts',(-5.25000782702704,0.00470041714920988,
4.66142853012161));
#30155=CARTESIAN_POINT('Ctrl Pts',(-5.25000012706038,0.00029104482780982,
4.66143767683269));
#30156=CARTESIAN_POINT('Ctrl Pts',(-5.25,0.000145522242130993,4.66143782776615));
#30157=CARTESIAN_POINT('Ctrl Pts',(-5.25,-7.13617547270521E-16,4.66143782776615));
#30158=CARTESIAN_POINT('',(-5.49431818181818,0.249935425544578,0.));
#30159=CARTESIAN_POINT('',(-5.49431818181818,0.249935425544578,0.));
#30160=CARTESIAN_POINT('',(-5.49431818181818,-0.249935425544576,0.));
#30161=CARTESIAN_POINT('Origin',(-5.5,1.11022302462516E-15,0.));
#30162=CARTESIAN_POINT('',(-5.49431818181818,-0.249935425544576,4.));
#30163=CARTESIAN_POINT('',(-5.49431818181818,-0.249935425544576,0.));
#30164=CARTESIAN_POINT('Ctrl Pts',(-5.25,-7.13617547270521E-16,4.66143782776615));
#30165=CARTESIAN_POINT('Ctrl Pts',(-5.25,-0.00401273696638705,4.66143782776615));
#30166=CARTESIAN_POINT('Ctrl Pts',(-5.25009663683444,-0.00802521271127695,
4.6613230837511));
#30167=CARTESIAN_POINT('Ctrl Pts',(-5.25057191524974,-0.0178887267944777,
4.66075801609034));
#30168=CARTESIAN_POINT('Ctrl Pts',(-5.25105929530591,-0.0237157972436869,
4.66017835073772));
#30169=CARTESIAN_POINT('Ctrl Pts',(-5.25327427371658,-0.0423565274659345,
4.65753338733037));
#30170=CARTESIAN_POINT('Ctrl Pts',(-5.25577300860231,-0.0548474302584322,
4.65454084811324));
#30171=CARTESIAN_POINT('Ctrl Pts',(-5.26513174003141,-0.0885738625581881,
4.64311349551522));
#30172=CARTESIAN_POINT('Ctrl Pts',(-5.27370766679928,-0.108104477794349,
4.63244216484639));
#30173=CARTESIAN_POINT('Ctrl Pts',(-5.29504707030263,-0.144948043057416,
4.60428833810774));
#30174=CARTESIAN_POINT('Ctrl Pts',(-5.30802661494925,-0.161251465092565,
4.58628814678021));
#30175=CARTESIAN_POINT('Ctrl Pts',(-5.33877014255047,-0.192707055001167,
4.54008611674082));
#30176=CARTESIAN_POINT('Ctrl Pts',(-5.35671971365448,-0.205776251869831,
4.51041431850453));
#30177=CARTESIAN_POINT('Ctrl Pts',(-5.40048917407278,-0.231487544890781,
4.42842633637123));
#30178=CARTESIAN_POINT('Ctrl Pts',(-5.42658774433484,-0.239954791804268,
4.36954193373565));
#30179=CARTESIAN_POINT('Ctrl Pts',(-5.47416618476358,-0.250126227193806,
4.21822112899257));
#30180=CARTESIAN_POINT('Ctrl Pts',(-5.49431818181814,-0.249935425544575,
4.11550482956185));
#30181=CARTESIAN_POINT('Ctrl Pts',(-5.49431818181818,-0.249935425544576,
4.00000000000038));
#30182=CARTESIAN_POINT('Origin',(-5.43228587327326,0.860389557721271,0.));
#30183=CARTESIAN_POINT('',(-5.38757549311203,1.10635903124561,4.));
#30184=CARTESIAN_POINT('',(-5.46577252229136,0.61264241982148,4.));
#30185=CARTESIAN_POINT('Ctrl Pts',(-5.38757549311203,1.1063590312456,4.));
#30186=CARTESIAN_POINT('Ctrl Pts',(-5.38757549311203,1.1063590312456,4.02673063961772));
#30187=CARTESIAN_POINT('Ctrl Pts',(-5.38651975223822,1.10617564982983,4.05414638576011));
#30188=CARTESIAN_POINT('Ctrl Pts',(-5.37551658340328,1.10402140302146,4.19012241323843));
#30189=CARTESIAN_POINT('Ctrl Pts',(-5.35042611089805,1.09908519447304,4.28686359329027));
#30190=CARTESIAN_POINT('Ctrl Pts',(-5.29897209514017,1.07315939316953,4.42646405387417));
#30191=CARTESIAN_POINT('Ctrl Pts',(-5.27637155422121,1.05808598501931,4.47482705790032));
#30192=CARTESIAN_POINT('Ctrl Pts',(-5.24115473829857,1.02277290612916,4.54353143773204));
#30193=CARTESIAN_POINT('Ctrl Pts',(-5.22683772617802,1.00509927187887,4.56934838942207));
#30194=CARTESIAN_POINT('Ctrl Pts',(-5.2057010863751,0.967491407182816,4.6071405640229));
#30195=CARTESIAN_POINT('Ctrl Pts',(-5.1979716541564,0.949946965001195,4.62089194101727));
#30196=CARTESIAN_POINT('Ctrl Pts',(-5.18618243478152,0.909396227292173,
4.64388394673188));
#30197=CARTESIAN_POINT('Ctrl Pts',(-5.182496726827,0.886623136860021,4.65258978726598));
#30198=CARTESIAN_POINT('Ctrl Pts',(-5.18223104137204,0.854886118918676,
4.65886310574997));
#30199=CARTESIAN_POINT('Ctrl Pts',(-5.1825134084958,0.8472220325302,4.65995935047192));
#30200=CARTESIAN_POINT('Ctrl Pts',(-5.18354193434975,0.834941493334305,
4.661036848069));
#30201=CARTESIAN_POINT('Ctrl Pts',(-5.18405325452173,0.830357414107855,
4.66128876278954));
#30202=CARTESIAN_POINT('Ctrl Pts',(-5.18525652141284,0.821749396602635,
4.6614766362689));
#30203=CARTESIAN_POINT('Ctrl Pts',(-5.18591867583012,0.817730454011764,
4.66144660123003));
#30204=CARTESIAN_POINT('Ctrl Pts',(-5.18761806734741,0.808785506788655,
4.66111486035927));
#30205=CARTESIAN_POINT('Ctrl Pts',(-5.18870469720579,0.803879954994031,
4.6607514048391));
#30206=CARTESIAN_POINT('Ctrl Pts',(-5.19227888074625,0.789765163415027,
4.65917598249656));
#30207=CARTESIAN_POINT('Ctrl Pts',(-5.19512838427145,0.780742800229034,
4.65750148702093));
#30208=CARTESIAN_POINT('Ctrl Pts',(-5.20670671111325,0.750108423554761,
4.64948528566701));
#30209=CARTESIAN_POINT('Ctrl Pts',(-5.21757743244347,0.730633160772493,
4.64009844156318));
#30210=CARTESIAN_POINT('Ctrl Pts',(-5.24236094114524,0.696424921417127,
4.61539308723158));
#30211=CARTESIAN_POINT('Ctrl Pts',(-5.25606733420563,0.682131617948139,
4.60019195379195));
#30212=CARTESIAN_POINT('Ctrl Pts',(-5.28804986143135,0.654795226139872,
4.56080656181529));
#30213=CARTESIAN_POINT('Ctrl Pts',(-5.30634185619748,0.643602532663021,
4.53533737515858));
#30214=CARTESIAN_POINT('Ctrl Pts',(-5.34786498829106,0.623508365378145,
4.46952174021328));
#30215=CARTESIAN_POINT('Ctrl Pts',(-5.37181868573432,0.616850747770218,
4.42457618200282));
#30216=CARTESIAN_POINT('Ctrl Pts',(-5.43514820992185,0.606819121617711,
4.27073174534987));
#30217=CARTESIAN_POINT('Ctrl Pts',(-5.46577252229136,0.612642419821501,
4.14407324412992));
#30218=CARTESIAN_POINT('Ctrl Pts',(-5.46577252229136,0.612642419821501,
4.));
#30219=CARTESIAN_POINT('',(-5.38757549311203,1.10635903124561,0.));
#30220=CARTESIAN_POINT('',(-5.38757549311203,1.10635903124561,0.));
#30221=CARTESIAN_POINT('',(-5.46577252229136,0.61264241982148,0.));
#30222=CARTESIAN_POINT('Origin',(-5.43228587327326,0.860389557721271,0.));
#30223=CARTESIAN_POINT('',(-5.46577252229136,0.61264241982148,0.));
#30224=CARTESIAN_POINT('Origin',(-5.23081083962335,1.69959346906221,0.));
#30225=CARTESIAN_POINT('',(-5.14817281542751,1.93554040580225,4.));
#30226=CARTESIAN_POINT('',(-5.30264140340673,1.46013497556791,4.));
#30227=CARTESIAN_POINT('Ctrl Pts',(-5.14817281542751,1.93554040580225,4.));
#30228=CARTESIAN_POINT('Ctrl Pts',(-5.14817281542751,1.93554040580225,4.02673063961775));
#30229=CARTESIAN_POINT('Ctrl Pts',(-5.14715875964944,1.9351941278572,4.05414638576016));
#30230=CARTESIAN_POINT('Ctrl Pts',(-5.13662805652858,1.93134512857136,4.19012241323852));
#30231=CARTESIAN_POINT('Ctrl Pts',(-5.11261868251874,1.92254467829737,4.28686359329035));
#30232=CARTESIAN_POINT('Ctrl Pts',(-5.06585383993555,1.88888888520005,4.42646405387421));
#30233=CARTESIAN_POINT('Ctrl Pts',(-5.04588954971906,1.87046555218876,4.47482705790035));
#30234=CARTESIAN_POINT('Ctrl Pts',(-5.01663049384449,1.83007811213917,4.54353143773205));
#30235=CARTESIAN_POINT('Ctrl Pts',(-5.00525451342013,1.81038239552216,4.56934838942209));
#30236=CARTESIAN_POINT('Ctrl Pts',(-4.99026126692246,1.76993104710686,4.60714056402292));
#30237=CARTESIAN_POINT('Ctrl Pts',(-4.98537155226774,1.75139345652763,4.62089194101728));
#30238=CARTESIAN_POINT('Ctrl Pts',(-4.98007101070696,1.70949772546375,4.64388394673188));
#30239=CARTESIAN_POINT('Ctrl Pts',(-4.97999317615251,1.68642843781244,4.65258978726598));
#30240=CARTESIAN_POINT('Ctrl Pts',(-4.98469552515,1.6550405928645,4.65886310574997));
#30241=CARTESIAN_POINT('Ctrl Pts',(-4.98617334312012,1.64751503604724,4.65995935047191));
#30242=CARTESIAN_POINT('Ctrl Pts',(-4.98911030569358,1.635546587559,4.66103684806899));
#30243=CARTESIAN_POINT('Ctrl Pts',(-4.99033243864724,1.63109893405223,4.66128876278954));
#30244=CARTESIAN_POINT('Ctrl Pts',(-4.9928674819397,1.6227851279391,4.6614766362689));
#30245=CARTESIAN_POINT('Ctrl Pts',(-4.99415018527155,1.61891924897262,4.66144660123003));
#30246=CARTESIAN_POINT('Ctrl Pts',(-4.99722795249295,1.610350272296,4.66111486035926));
#30247=CARTESIAN_POINT('Ctrl Pts',(-4.99906860150534,1.60567510234486,4.6607514048391));
#30248=CARTESIAN_POINT('Ctrl Pts',(-5.0048068207852,1.59229321276247,4.65917598249655));
#30249=CARTESIAN_POINT('Ctrl Pts',(-5.00903265075192,1.58382769039865,4.65750148702093));
#30250=CARTESIAN_POINT('Ctrl Pts',(-5.02526070150406,1.5553817231016,4.64948528566701));
#30251=CARTESIAN_POINT('Ctrl Pts',(-5.03904418853066,1.53784678859742,4.64009844156316));
#30252=CARTESIAN_POINT('Ctrl Pts',(-5.06887391873792,1.50793670435945,4.61539308723159));
#30253=CARTESIAN_POINT('Ctrl Pts',(-5.08464752863709,1.49596352744058,4.60019195379199));
#30254=CARTESIAN_POINT('Ctrl Pts',(-5.12051265170942,1.47396686151477,4.56080656181526));
#30255=CARTESIAN_POINT('Ctrl Pts',(-5.14033036468259,1.46577346708359,4.53533737515849));
#30256=CARTESIAN_POINT('Ctrl Pts',(-5.18448569842593,1.45242234129825,4.46952174021338));
#30257=CARTESIAN_POINT('Ctrl Pts',(-5.20918596695372,1.449593873856,4.42457618200296));
#30258=CARTESIAN_POINT('Ctrl Pts',(-5.2733050916799,1.44959267390549,4.27073174534986));
#30259=CARTESIAN_POINT('Ctrl Pts',(-5.30264140340673,1.46013497556793,4.14407324412991));
#30260=CARTESIAN_POINT('Ctrl Pts',(-5.30264140340673,1.46013497556793,4.));
#30261=CARTESIAN_POINT('',(-5.14817281542751,1.93554040580225,0.));
#30262=CARTESIAN_POINT('',(-5.14817281542751,1.93554040580225,0.));
#30263=CARTESIAN_POINT('',(-5.30264140340673,1.46013497556791,0.));
#30264=CARTESIAN_POINT('Origin',(-5.23081083962335,1.69959346906221,0.));
#30265=CARTESIAN_POINT('',(-5.30264140340673,1.46013497556791,0.));
#30266=CARTESIAN_POINT('Origin',(-4.90053588303602,2.49694774856751,0.));
#30267=CARTESIAN_POINT('',(-4.78200503722117,2.71706235187773,4.));
#30268=CARTESIAN_POINT('',(-5.00894165471237,2.2716741623057,4.));
#30269=CARTESIAN_POINT('Ctrl Pts',(-4.78200503722117,2.71706235187773,4.));
#30270=CARTESIAN_POINT('Ctrl Pts',(-4.78200503722117,2.71706235187773,4.02673063961767));
#30271=CARTESIAN_POINT('Ctrl Pts',(-4.78105763595755,2.71656170391563,4.05414638575999));
#30272=CARTESIAN_POINT('Ctrl Pts',(-4.77125869941107,2.71111272728886,4.19012241323822));
#30273=CARTESIAN_POINT('Ctrl Pts',(-4.7489216143673,2.69866473158211,4.2868635932901));
#30274=CARTESIAN_POINT('Ctrl Pts',(-4.7079974505867,2.65810766401414,4.42646405387435));
#30275=CARTESIAN_POINT('Ctrl Pts',(-4.69116099815551,2.63678804974402,4.47482705790043));
#30276=CARTESIAN_POINT('Ctrl Pts',(-4.66858015738992,2.59232072134735,4.54353143773199));
#30277=CARTESIAN_POINT('Ctrl Pts',(-4.6604253230545,2.57108789627306,4.56934838942204));
#30278=CARTESIAN_POINT('Ctrl Pts',(-4.65194465335057,2.52878911058685,4.60714056402288));
#30279=CARTESIAN_POINT('Ctrl Pts',(-4.65001505726266,2.5097148286128,4.62089194101726));
#30280=CARTESIAN_POINT('Ctrl Pts',(-4.65133371044068,2.46750571613681,4.64388394673187));
#30281=CARTESIAN_POINT('Ctrl Pts',(-4.65486566583134,2.44470827369088,4.65258978726598));
#30282=CARTESIAN_POINT('Ctrl Pts',(-4.66442026184277,2.41444247464924,4.65886310574997));
#30283=CARTESIAN_POINT('Ctrl Pts',(-4.66705714187621,2.40724075158792,4.65995935047192));
#30284=CARTESIAN_POINT('Ctrl Pts',(-4.67183022340342,2.39587909673004,4.661036848069));
#30285=CARTESIAN_POINT('Ctrl Pts',(-4.67373307616942,2.39167738493323,4.66128876278955));
#30286=CARTESIAN_POINT('Ctrl Pts',(-4.67753747468403,2.38386250371066,4.6614766362689));
#30287=CARTESIAN_POINT('Ctrl Pts',(-4.67940914251737,2.38024487913886,4.66144660123004));
#30288=CARTESIAN_POINT('Ctrl Pts',(-4.68378950059938,2.37226286965328,4.66111486035927));
#30289=CARTESIAN_POINT('Ctrl Pts',(-4.68633884587834,2.3679331997458,4.66075140483911));
#30290=CARTESIAN_POINT('Ctrl Pts',(-4.69409980689487,2.3556137186935,4.65917598249656));
#30291=CARTESIAN_POINT('Ctrl Pts',(-4.6995979093446,2.34791348640791,4.65750148702094));
#30292=CARTESIAN_POINT('Ctrl Pts',(-4.72007609553974,2.32235636260972,4.64948528566702));
#30293=CARTESIAN_POINT('Ctrl Pts',(-4.73643295306733,2.30719352466623,4.64009844156317));
#30294=CARTESIAN_POINT('Ctrl Pts',(-4.77057439782323,2.28231808108543,4.61539308723159));
#30295=CARTESIAN_POINT('Ctrl Pts',(-4.78802682593589,2.2729598500691,4.60019195379197));
#30296=CARTESIAN_POINT('Ctrl Pts',(-4.82689142649517,2.25684454094365,4.56080656181529));
#30297=CARTESIAN_POINT('Ctrl Pts',(-4.84774687981072,2.25185219412136,4.53533737515855));
#30298=CARTESIAN_POINT('Ctrl Pts',(-4.89344716434411,2.24557285886215,4.46952174021331));
#30299=CARTESIAN_POINT('Ctrl Pts',(-4.91828580136978,2.2466431878412,4.42457618200287));
#30300=CARTESIAN_POINT('Ctrl Pts',(-4.98161570098456,2.25667244363945,4.27073174534989));
#30301=CARTESIAN_POINT('Ctrl Pts',(-5.00894165471236,2.27167416230572,4.14407324412994));
#30302=CARTESIAN_POINT('Ctrl Pts',(-5.00894165471236,2.27167416230572,4.));
#30303=CARTESIAN_POINT('',(-4.78200503722117,2.71706235187773,0.));
#30304=CARTESIAN_POINT('',(-4.78200503722117,2.71706235187773,0.));
#30305=CARTESIAN_POINT('',(-5.00894165471237,2.2716741623057,0.));
#30306=CARTESIAN_POINT('Origin',(-4.90053588303602,2.49694774856751,0.));
#30307=CARTESIAN_POINT('',(-5.00894165471237,2.2716741623057,0.));
#30308=CARTESIAN_POINT('Origin',(-4.44959346906221,3.2328188876086,0.));
#30309=CARTESIAN_POINT('',(-4.29808842443363,3.43168120543702,4.));
#30310=CARTESIAN_POINT('',(-4.59190513875472,3.02727719191323,4.));
#30311=CARTESIAN_POINT('Ctrl Pts',(-4.29808842443363,3.43168120543702,4.));
#30312=CARTESIAN_POINT('Ctrl Pts',(-4.29808842443363,3.43168120543702,4.02673063961775));
#30313=CARTESIAN_POINT('Ctrl Pts',(-4.29723100584781,3.43103851507225,4.05414638576015));
#30314=CARTESIAN_POINT('Ctrl Pts',(-4.28840511821421,3.42412373299318,4.19012241323848));
#30315=CARTESIAN_POINT('Ctrl Pts',(-4.26829033530279,3.40833470282044,4.2868635932903));
#30316=CARTESIAN_POINT('Ctrl Pts',(-4.23421453905669,3.36187501038656,4.42646405387453));
#30317=CARTESIAN_POINT('Ctrl Pts',(-4.22092049374663,3.33818407451672,4.47482705790057));
#30318=CARTESIAN_POINT('Ctrl Pts',(-4.20557388333115,3.29073179097664,4.54353143773204));
#30319=CARTESIAN_POINT('Ctrl Pts',(-4.20084099417036,3.26848468006611,4.56934838942209));
#30320=CARTESIAN_POINT('Ctrl Pts',(-4.19908172349404,3.22537999359419,4.60714056402292));
#30321=CARTESIAN_POINT('Ctrl Pts',(-4.20015975903259,3.20623869235145,4.62089194101729));
#30322=CARTESIAN_POINT('Ctrl Pts',(-4.20806513733182,3.16475552689651,4.6438839467319));
#30323=CARTESIAN_POINT('Ctrl Pts',(-4.215119914204,3.14279127834937,4.652589787266));
#30324=CARTESIAN_POINT('Ctrl Pts',(-4.22929149136569,3.11439276963285,4.65886310574998));
#30325=CARTESIAN_POINT('Ctrl Pts',(-4.23302250472473,3.10769221065042,4.65995935047192));
#30326=CARTESIAN_POINT('Ctrl Pts',(-4.2395141760975,3.09721711107278,4.661036848069));
#30327=CARTESIAN_POINT('Ctrl Pts',(-4.24205089412554,3.09336480107502,4.66128876278955));
#30328=CARTESIAN_POINT('Ctrl Pts',(-4.24703097094481,3.08624127305477,4.6614766362689));
#30329=CARTESIAN_POINT('Ctrl Pts',(-4.24944551660587,3.08296098080079,4.66144660123004));
#30330=CARTESIAN_POINT('Ctrl Pts',(-4.25502060659492,3.07576248207062,4.66111486035927));
#30331=CARTESIAN_POINT('Ctrl Pts',(-4.25821587479887,3.07188492304929,4.66075140483911));
#30332=CARTESIAN_POINT('Ctrl Pts',(-4.26780847693471,3.06093119703656,4.65917598249656));
#30333=CARTESIAN_POINT('Ctrl Pts',(-4.274443470338,3.05418586010366,4.65750148702094));
#30334=CARTESIAN_POINT('Ctrl Pts',(-4.29866755106879,3.03214688101149,4.64948528566702));
#30335=CARTESIAN_POINT('Ctrl Pts',(-4.31719501897974,3.01972949902145,4.64009844156318));
#30336=CARTESIAN_POINT('Ctrl Pts',(-4.35480750260545,3.00050121207563,4.61539308723159));
#30337=CARTESIAN_POINT('Ctrl Pts',(-4.37350901223016,2.99398835766767,4.60019195379195));
#30338=CARTESIAN_POINT('Ctrl Pts',(-4.41441611482645,2.98415121773687,4.56080656181527));
#30339=CARTESIAN_POINT('Ctrl Pts',(-4.4357957780085,2.98248284667088,4.53533737515851));
#30340=CARTESIAN_POINT('Ctrl Pts',(-4.48191572065581,2.98342992001184,4.46952174021366));
#30341=CARTESIAN_POINT('Ctrl Pts',(-4.50628111650113,2.98837269036042,4.42457618200336));
#30342=CARTESIAN_POINT('Ctrl Pts',(-4.56726239869638,3.00818544834456,4.27073174534982));
#30343=CARTESIAN_POINT('Ctrl Pts',(-4.59190513875471,3.02727719191324,4.14407324412986));
#30344=CARTESIAN_POINT('Ctrl Pts',(-4.59190513875471,3.02727719191324,4.));
#30345=CARTESIAN_POINT('',(-4.29808842443363,3.43168120543702,0.));
#30346=CARTESIAN_POINT('',(-4.29808842443363,3.43168120543702,0.));
#30347=CARTESIAN_POINT('',(-4.59190513875472,3.02727719191323,0.));
#30348=CARTESIAN_POINT('Origin',(-4.44959346906221,3.2328188876086,0.));
#30349=CARTESIAN_POINT('',(-4.59190513875472,3.02727719191323,0.));
#30350=CARTESIAN_POINT('Origin',(-3.88908729652601,3.88908729652601,0.));
#30351=CARTESIAN_POINT('',(-3.70833861009886,4.0618006786215,4.));
#30352=CARTESIAN_POINT('',(-4.0618006786215,3.70833861009886,4.));
#30353=CARTESIAN_POINT('Ctrl Pts',(-3.70833861009886,4.06180067862149,4.));
#30354=CARTESIAN_POINT('Ctrl Pts',(-3.70833861009886,4.06180067862149,4.02673063961768));
#30355=CARTESIAN_POINT('Ctrl Pts',(-3.70759228668204,4.06103177102382,4.05414638576001));
#30356=CARTESIAN_POINT('Ctrl Pts',(-3.69995677060637,4.05282144837612,4.19012241323826));
#30357=CARTESIAN_POINT('Ctrl Pts',(-3.68255958253974,4.03408016206108,4.28686359329013));
#30358=CARTESIAN_POINT('Ctrl Pts',(-3.65617121302277,3.9828618365799,4.42646405387448));
#30359=CARTESIAN_POINT('Ctrl Pts',(-3.64674691834979,3.95738292857717,4.47482705790052));
#30360=CARTESIAN_POINT('Ctrl Pts',(-3.63901242276529,3.90811412259949,4.543531437732));
#30361=CARTESIAN_POINT('Ctrl Pts',(-3.63781801821782,3.88540052355728,4.56934838942205));
#30362=CARTESIAN_POINT('Ctrl Pts',(-3.64282346565182,3.84255131673685,4.60714056402287));
#30363=CARTESIAN_POINT('Ctrl Pts',(-3.64688258800407,3.82381431858834,4.62089194101726));
#30364=CARTESIAN_POINT('Ctrl Pts',(-3.66118003477433,3.78407855336268,4.64388394673188));
#30365=CARTESIAN_POINT('Ctrl Pts',(-3.67158392110796,3.76348833140871,4.65258978726598));
#30366=CARTESIAN_POINT('Ctrl Pts',(-3.69002352815739,3.73765637855122,4.65886310574997));
#30367=CARTESIAN_POINT('Ctrl Pts',(-3.69475680491062,3.73162197364765,4.65995935047192));
#30368=CARTESIAN_POINT('Ctrl Pts',(-3.70280721963517,3.72229136106664,4.661036848069));
#30369=CARTESIAN_POINT('Ctrl Pts',(-3.70591534050851,3.71888330952516,4.66128876278955));
#30370=CARTESIAN_POINT('Ctrl Pts',(-3.71194846961323,3.71262653960874,4.6614766362689));
#30371=CARTESIAN_POINT('Ctrl Pts',(-3.71484643897442,3.70976435135453,4.66144660123004));
#30372=CARTESIAN_POINT('Ctrl Pts',(-3.72147898365232,3.70352661430895,4.66111486035927));
#30373=CARTESIAN_POINT('Ctrl Pts',(-3.7252414966736,3.70019664454576,4.66075140483911));
#30374=CARTESIAN_POINT('Ctrl Pts',(-3.73642953822813,3.69087839066038,4.65917598249656));
#30375=CARTESIAN_POINT('Ctrl Pts',(-3.74403804702709,3.68525404166196,4.65750148702094));
#30376=CARTESIAN_POINT('Ctrl Pts',(-3.77141154503086,3.66727588008421,4.64948528566702));
#30377=CARTESIAN_POINT('Ctrl Pts',(-3.79165341557607,3.65790971120312,4.64009844156318));
#30378=CARTESIAN_POINT('Ctrl Pts',(-3.831810793896,3.64480204513195,4.61539308723159));
#30379=CARTESIAN_POINT('Ctrl Pts',(-3.85130089179906,3.6412949354228,4.60019195379196));
#30380=CARTESIAN_POINT('Ctrl Pts',(-3.89324322780352,3.63797818771934,4.56080656181529));
#30381=CARTESIAN_POINT('Ctrl Pts',(-3.91462066258947,3.63967487324229,4.53533737515857));
#30382=CARTESIAN_POINT('Ctrl Pts',(-3.96002463729984,3.64782503509458,4.46952174021349));
#30383=CARTESIAN_POINT('Ctrl Pts',(-3.98331683505493,3.65651853940271,4.42457618200313));
#30384=CARTESIAN_POINT('Ctrl Pts',(-4.0404479382774,3.68562694371631,4.27073174534985));
#30385=CARTESIAN_POINT('Ctrl Pts',(-4.06180067862148,3.70833861009888,4.1440732441299));
#30386=CARTESIAN_POINT('Ctrl Pts',(-4.06180067862148,3.70833861009888,4.));
#30387=CARTESIAN_POINT('',(-3.70833861009886,4.0618006786215,0.));
#30388=CARTESIAN_POINT('',(-3.70833861009886,4.0618006786215,0.));
#30389=CARTESIAN_POINT('',(-4.0618006786215,3.70833861009886,0.));
#30390=CARTESIAN_POINT('Origin',(-3.88908729652601,3.88908729652601,0.));
#30391=CARTESIAN_POINT('',(-4.06180067862149,3.70833861009886,0.));
#30392=CARTESIAN_POINT('Origin',(-3.2328188876086,4.44959346906221,0.));
#30393=CARTESIAN_POINT('',(-3.02727719191323,4.59190513875472,4.));
#30394=CARTESIAN_POINT('',(-3.43168120543702,4.29808842443363,4.));
#30395=CARTESIAN_POINT('Ctrl Pts',(-3.02727719191322,4.59190513875472,4.));
#30396=CARTESIAN_POINT('Ctrl Pts',(-3.02727719191322,4.59190513875472,4.02673063961773));
#30397=CARTESIAN_POINT('Ctrl Pts',(-3.02666034062482,4.59102894698104,4.05414638576012));
#30398=CARTESIAN_POINT('Ctrl Pts',(-3.02040320785364,4.58172524915676,4.19012241323842));
#30399=CARTESIAN_POINT('Ctrl Pts',(-3.00615199113995,4.5604931793672,4.28686359329027));
#30400=CARTESIAN_POINT('Ctrl Pts',(-2.98810081758769,4.50577738599611,4.4264640538742));
#30401=CARTESIAN_POINT('Ctrl Pts',(-2.98277833096402,4.47913788113521,4.47482705790034));
#30402=CARTESIAN_POINT('Ctrl Pts',(-2.98284639916111,4.42926571423672,4.54353143773204));
#30403=CARTESIAN_POINT('Ctrl Pts',(-2.98521988943094,4.40664491125336,4.56934838942208));
#30404=CARTESIAN_POINT('Ctrl Pts',(-2.99686680424732,4.36510627376469,4.60714056402291));
#30405=CARTESIAN_POINT('Ctrl Pts',(-3.00380706434952,4.34723494578936,4.62089194101728));
#30406=CARTESIAN_POINT('Ctrl Pts',(-3.02414452900081,4.31022500720833,4.64388394673188));
#30407=CARTESIAN_POINT('Ctrl Pts',(-3.03764134658585,4.29151581144707,4.65258978726599));
#30408=CARTESIAN_POINT('Ctrl Pts',(-3.05989493919994,4.26888648285924,4.65886310574997));
#30409=CARTESIAN_POINT('Ctrl Pts',(-3.06551393036483,4.26366681911034,4.65995935047192));
#30410=CARTESIAN_POINT('Ctrl Pts',(-3.07492486051283,4.25571044417425,4.661036848069));
#30411=CARTESIAN_POINT('Ctrl Pts',(-3.07852785198031,4.25283056862869,4.66128876278955));
#30412=CARTESIAN_POINT('Ctrl Pts',(-3.08546547770911,4.24759461925646,4.6614766362689));
#30413=CARTESIAN_POINT('Ctrl Pts',(-3.08877551314696,4.24522101157591,4.66144660123004));
#30414=CARTESIAN_POINT('Ctrl Pts',(-3.09630219725155,4.24009763000285,4.66111486035927));
#30415=CARTESIAN_POINT('Ctrl Pts',(-3.10053930953249,4.23739724440492,4.66075140483911));
#30416=CARTESIAN_POINT('Ctrl Pts',(-3.11304730379171,4.22994390898303,4.65917598249656));
#30417=CARTESIAN_POINT('Ctrl Pts',(-3.12144198124854,4.22557903805757,4.65750148702093));
#30418=CARTESIAN_POINT('Ctrl Pts',(-3.15129087015696,4.2121043759984,4.64948528566702));
#30419=CARTESIAN_POINT('Ctrl Pts',(-3.17274872130468,4.20602004638866,4.64009844156319));
#30420=CARTESIAN_POINT('Ctrl Pts',(-3.21446218638992,4.19935575543265,4.61539308723159));
#30421=CARTESIAN_POINT('Ctrl Pts',(-3.23426096167701,4.19894074710277,4.60019195379197));
#30422=CARTESIAN_POINT('Ctrl Pts',(-3.27620577157862,4.20222606096277,4.56080656181529));
#30423=CARTESIAN_POINT('Ctrl Pts',(-3.29705459457641,4.20724602504611,4.53533737515856));
#30424=CARTESIAN_POINT('Ctrl Pts',(-3.34062460480529,4.22239859137615,4.46952174021329));
#30425=CARTESIAN_POINT('Ctrl Pts',(-3.36227007325902,4.23462876671565,4.42457618200284));
#30426=CARTESIAN_POINT('Ctrl Pts',(-3.41414424014011,4.27231607183921,4.27073174534989));
#30427=CARTESIAN_POINT('Ctrl Pts',(-3.431681205437,4.29808842443364,4.14407324412994));
#30428=CARTESIAN_POINT('Ctrl Pts',(-3.431681205437,4.29808842443364,4.));
#30429=CARTESIAN_POINT('',(-3.02727719191323,4.59190513875472,0.));
#30430=CARTESIAN_POINT('',(-3.02727719191322,4.59190513875472,0.));
#30431=CARTESIAN_POINT('',(-3.43168120543702,4.29808842443363,0.));
#30432=CARTESIAN_POINT('Origin',(-3.2328188876086,4.44959346906221,0.));
#30433=CARTESIAN_POINT('',(-3.43168120543702,4.29808842443363,0.));
#30434=CARTESIAN_POINT('Origin',(-2.49694774856751,4.90053588303602,0.));
#30435=CARTESIAN_POINT('',(-2.2716741623057,5.00894165471237,4.));
#30436=CARTESIAN_POINT('',(-2.71706235187773,4.78200503722117,4.));
#30437=CARTESIAN_POINT('Ctrl Pts',(-2.2716741623057,5.00894165471237,4.));
#30438=CARTESIAN_POINT('Ctrl Pts',(-2.2716741623057,5.00894165471237,4.02673063961772));
#30439=CARTESIAN_POINT('Ctrl Pts',(-2.27120197207165,5.00797975351207,4.05414638576009));
#30440=CARTESIAN_POINT('Ctrl Pts',(-2.26647729398003,4.99781176842887,4.19012241323845));
#30441=CARTESIAN_POINT('Ctrl Pts',(-2.25572296087186,4.97461171918823,4.28686359329029));
#30442=CARTESIAN_POINT('Ctrl Pts',(-2.24645346308548,4.91774574235115,4.42646405387434));
#30443=CARTESIAN_POINT('Ctrl Pts',(-2.24536384179618,4.89060159365313,4.47482705790043));
#30444=CARTESIAN_POINT('Ctrl Pts',(-2.25323279770997,4.84135408409937,4.54353143773202));
#30445=CARTESIAN_POINT('Ctrl Pts',(-2.25911573958947,4.81938307641843,4.56934838942208));
#30446=CARTESIAN_POINT('Ctrl Pts',(-2.27711733609156,4.78017782737532,4.60714056402291));
#30447=CARTESIAN_POINT('Ctrl Pts',(-2.28676784170657,4.76361222097947,4.62089194101728));
#30448=CARTESIAN_POINT('Ctrl Pts',(-2.31264454836303,4.73023941655983,4.6438839467319));
#30449=CARTESIAN_POINT('Ctrl Pts',(-2.32890196075715,4.71387192948318,4.65258978726599));
#30450=CARTESIAN_POINT('Ctrl Pts',(-2.35442158163031,4.69500243433729,4.65886310574998));
#30451=CARTESIAN_POINT('Ctrl Pts',(-2.36078792899602,4.69072603718763,4.65995935047192));
#30452=CARTESIAN_POINT('Ctrl Pts',(-2.37132764623411,4.68433981225311,4.661036848069));
#30453=CARTESIAN_POINT('Ctrl Pts',(-2.37533679068817,4.68205902479715,4.66128876278955));
#30454=CARTESIAN_POINT('Ctrl Pts',(-2.38300808567094,4.67797282241978,4.6614766362689));
#30455=CARTESIAN_POINT('Ctrl Pts',(-2.38664868312757,4.67614624141154,4.66144660123004));
#30456=CARTESIAN_POINT('Ctrl Pts',(-2.39488417471663,4.67226336996882,4.66111486035927));
#30457=CARTESIAN_POINT('Ctrl Pts',(-2.39949155449074,4.67025906099161,4.66075140483911));
#30458=CARTESIAN_POINT('Ctrl Pts',(-2.41301151312427,4.66485416988754,4.65917598249656));
#30459=CARTESIAN_POINT('Ctrl Pts',(-2.42198565441963,4.66185625464341,4.65750148702093));
#30460=CARTESIAN_POINT('Ctrl Pts',(-2.45357495552502,4.65321688300254,4.64948528566701));
#30461=CARTESIAN_POINT('Ctrl Pts',(-2.47572042376548,4.65056420905187,4.64009844156318));
#30462=CARTESIAN_POINT('Ctrl Pts',(-2.51796285166657,4.65050739017187,4.61539308723158));
#30463=CARTESIAN_POINT('Ctrl Pts',(-2.53758279278176,4.65319470210369,4.60019195379196));
#30464=CARTESIAN_POINT('Ctrl Pts',(-2.5784972561539,4.66300118219658,4.56080656181527));
#30465=CARTESIAN_POINT('Ctrl Pts',(-2.59830410014805,4.6712208166643,4.53533737515851));
#30466=CARTESIAN_POINT('Ctrl Pts',(-2.63896730764275,4.69300268100044,4.46952174021349));
#30467=CARTESIAN_POINT('Ctrl Pts',(-2.65843306352468,4.70846837986478,4.42457618200312));
#30468=CARTESIAN_POINT('Ctrl Pts',(-2.70377297991551,4.75380659926932,4.27073174534983));
#30469=CARTESIAN_POINT('Ctrl Pts',(-2.71706235187771,4.78200503722118,4.14407324412986));
#30470=CARTESIAN_POINT('Ctrl Pts',(-2.71706235187771,4.78200503722118,4.));
#30471=CARTESIAN_POINT('',(-2.2716741623057,5.00894165471237,0.));
#30472=CARTESIAN_POINT('',(-2.2716741623057,5.00894165471237,0.));
#30473=CARTESIAN_POINT('',(-2.71706235187773,4.78200503722117,0.));
#30474=CARTESIAN_POINT('Origin',(-2.49694774856751,4.90053588303602,0.));
#30475=CARTESIAN_POINT('',(-2.71706235187773,4.78200503722117,0.));
#30476=CARTESIAN_POINT('Origin',(-1.69959346906221,5.23081083962335,0.));
#30477=CARTESIAN_POINT('',(-1.46013497556791,5.30264140340673,4.));
#30478=CARTESIAN_POINT('',(-1.93554040580225,5.14817281542751,4.));
#30479=CARTESIAN_POINT('Ctrl Pts',(-1.46013497556791,5.30264140340673,4.));
#30480=CARTESIAN_POINT('Ctrl Pts',(-1.46013497556791,5.30264140340673,4.02673063961775));
#30481=CARTESIAN_POINT('Ctrl Pts',(-1.45981907327888,5.30161747797973,4.05414638576016));
#30482=CARTESIAN_POINT('Ctrl Pts',(-1.45674318712176,5.29083557517594,4.19012241323845));
#30483=CARTESIAN_POINT('Ctrl Pts',(-1.44975054499179,5.26623880869311,4.28686359329028));
#30484=CARTESIAN_POINT('Ctrl Pts',(-1.44949096877052,5.20862287746718,4.42646405387428));
#30485=CARTESIAN_POINT('Ctrl Pts',(-1.45266104290795,5.18164246395929,4.4748270579004));
#30486=CARTESIAN_POINT('Ctrl Pts',(-1.46813712672828,5.13423224887844,4.54353143773205));
#30487=CARTESIAN_POINT('Ctrl Pts',(-1.47738466266403,5.11345203562664,4.56934838942209));
#30488=CARTESIAN_POINT('Ctrl Pts',(-1.50129768180207,5.07754553837531,4.60714056402292));
#30489=CARTESIAN_POINT('Ctrl Pts',(-1.51342080545347,5.0626935537665,4.62089194101728));
#30490=CARTESIAN_POINT('Ctrl Pts',(-1.54419958371733,5.03377963271106,4.6438839467319));
#30491=CARTESIAN_POINT('Ctrl Pts',(-1.56281727947214,5.02015687617144,4.65258978726599));
#30492=CARTESIAN_POINT('Ctrl Pts',(-1.59097455084368,5.00551184406225,4.65886310574997));
#30493=CARTESIAN_POINT('Ctrl Pts',(-1.59793149380938,5.00228401260219,4.65995935047191));
#30494=CARTESIAN_POINT('Ctrl Pts',(-1.60934047531988,4.99762518772176,4.66103684806899));
#30495=CARTESIAN_POINT('Ctrl Pts',(-1.61365705431846,4.99599964891207,4.66128876278954));
#30496=CARTESIAN_POINT('Ctrl Pts',(-1.62187312581316,4.99316380939343,4.6614766362689));
#30497=CARTESIAN_POINT('Ctrl Pts',(-1.62575464169676,4.99192923154399,4.66144660123003));
#30498=CARTESIAN_POINT('Ctrl Pts',(-1.63449615563526,4.98938247941308,4.66111486035926));
#30499=CARTESIAN_POINT('Ctrl Pts',(-1.63936035392143,4.98812359979554,4.66075140483911));
#30500=CARTESIAN_POINT('Ctrl Pts',(-1.65355937067761,4.98490023936606,4.65917598249655));
#30501=CARTESIAN_POINT('Ctrl Pts',(-1.66289200266934,4.98334309842607,4.65750148702093));
#30502=CARTESIAN_POINT('Ctrl Pts',(-1.69544388253963,4.97975174720573,4.64948528566701));
#30503=CARTESIAN_POINT('Ctrl Pts',(-1.71773167294816,4.98059604655052,4.64009844156316));
#30504=CARTESIAN_POINT('Ctrl Pts',(-1.75946291489557,4.98714809881592,4.61539308723158));
#30505=CARTESIAN_POINT('Ctrl Pts',(-1.77842091377375,4.992871560471,4.60019195379196));
#30506=CARTESIAN_POINT('Ctrl Pts',(-1.81729758074085,5.00895773871105,4.56080656181527));
#30507=CARTESIAN_POINT('Ctrl Pts',(-1.83557473549708,5.02017464888311,4.53533737515854));
#30508=CARTESIAN_POINT('Ctrl Pts',(-1.87232987713593,5.0480494694357,4.46952174021328));
#30509=CARTESIAN_POINT('Ctrl Pts',(-1.88913660893301,5.06636987499118,4.42457618200282));
#30510=CARTESIAN_POINT('Ctrl Pts',(-1.92682585561729,5.11824263124584,4.27073174534986));
#30511=CARTESIAN_POINT('Ctrl Pts',(-1.93554040580223,5.14817281542752,4.1440732441299));
#30512=CARTESIAN_POINT('Ctrl Pts',(-1.93554040580223,5.14817281542752,4.));
#30513=CARTESIAN_POINT('',(-1.46013497556791,5.30264140340673,0.));
#30514=CARTESIAN_POINT('',(-1.46013497556791,5.30264140340673,0.));
#30515=CARTESIAN_POINT('',(-1.93554040580225,5.14817281542751,0.));
#30516=CARTESIAN_POINT('Origin',(-1.69959346906221,5.23081083962335,0.));
#30517=CARTESIAN_POINT('',(-1.93554040580225,5.14817281542751,0.));
#30518=CARTESIAN_POINT('Origin',(-0.860389557721269,5.43228587327326,0.));
#30519=CARTESIAN_POINT('',(-0.612642419821478,5.46577252229136,4.));
#30520=CARTESIAN_POINT('',(-1.1063590312456,5.38757549311203,4.));
#30521=CARTESIAN_POINT('Ctrl Pts',(-0.612642419821477,5.46577252229136,
4.));
#30522=CARTESIAN_POINT('Ctrl Pts',(-0.612642419821477,5.46577252229136,
4.02673063961771));
#30523=CARTESIAN_POINT('Ctrl Pts',(-0.612490584040256,5.46471178507989,
4.05414638576007));
#30524=CARTESIAN_POINT('Ctrl Pts',(-0.61113922834309,5.45358145078566,4.19012241323841));
#30525=CARTESIAN_POINT('Ctrl Pts',(-0.608080459247833,5.42819362108339,
4.28686359329025));
#30526=CARTESIAN_POINT('Ctrl Pts',(-0.616837196219717,5.37124643091157,
4.42646405387458));
#30527=CARTESIAN_POINT('Ctrl Pts',(-0.624188908037812,5.34509409991721,
4.47482705790059));
#30528=CARTESIAN_POINT('Ctrl Pts',(-0.646891047218759,5.30068857615024,
4.54353143773202));
#30529=CARTESIAN_POINT('Ctrl Pts',(-0.659275472185204,5.2816108351434,4.56934838942207));
#30530=CARTESIAN_POINT('Ctrl Pts',(-0.688511096065249,5.24988722681301,
4.60714056402291));
#30531=CARTESIAN_POINT('Ctrl Pts',(-0.702808326214398,5.23711456914321,
4.62089194101728));
#30532=CARTESIAN_POINT('Ctrl Pts',(-0.737731300415893,5.21337148814817,
4.64388394673189));
#30533=CARTESIAN_POINT('Ctrl Pts',(-0.758250850073323,5.20282889962289,
4.65258978726598));
#30534=CARTESIAN_POINT('Ctrl Pts',(-0.788352446473459,5.19276893984501,
4.65886310574997));
#30535=CARTESIAN_POINT('Ctrl Pts',(-0.795728682014567,5.19066915399765,
4.65995935047192));
#30536=CARTESIAN_POINT('Ctrl Pts',(-0.807726000808486,5.18785244490161,
4.661036848069));
#30537=CARTESIAN_POINT('Ctrl Pts',(-0.812243725850714,5.18692218089855,
4.66128876278954));
#30538=CARTESIAN_POINT('Ctrl Pts',(-0.820802266909525,5.1854065320192,4.6614766362689));
#30539=CARTESIAN_POINT('Ctrl Pts',(-0.824829125417006,5.18479435673255,
4.66144660123004));
#30540=CARTESIAN_POINT('Ctrl Pts',(-0.833861416620445,5.18364643340307,
4.66111486035927));
#30541=CARTESIAN_POINT('Ctrl Pts',(-0.838862660713575,5.18316398093936,
4.66075140483911));
#30542=CARTESIAN_POINT('Ctrl Pts',(-0.853391108675981,5.18220152101598,
4.65917598249655));
#30543=CARTESIAN_POINT('Ctrl Pts',(-0.862852430991235,5.18212349635794,
4.65750148702092));
#30544=CARTESIAN_POINT('Ctrl Pts',(-0.895565354310451,5.18366859654418,
4.64948528566701));
#30545=CARTESIAN_POINT('Ctrl Pts',(-0.917446667518231,5.18798907973248,
4.64009844156318));
#30546=CARTESIAN_POINT('Ctrl Pts',(-0.957639161837241,5.20098866987151,
4.61539308723157));
#30547=CARTESIAN_POINT('Ctrl Pts',(-0.975468409628044,5.20960735062882,
4.60019195379194));
#30548=CARTESIAN_POINT('Ctrl Pts',(-1.01135000762512,5.2315771319208,4.56080656181526));
#30549=CARTESIAN_POINT('Ctrl Pts',(-1.02764742893493,5.24551512024201,4.53533737515851));
#30550=CARTESIAN_POINT('Ctrl Pts',(-1.05958947114721,5.27879652641763,4.46952174021344));
#30551=CARTESIAN_POINT('Ctrl Pts',(-1.07332334134435,5.29952052947749,4.42457618200306));
#30552=CARTESIAN_POINT('Ctrl Pts',(-1.10243388398541,5.35665054316769,4.2707317453498));
#30553=CARTESIAN_POINT('Ctrl Pts',(-1.10635903124558,5.38757549311203,4.14407324412982));
#30554=CARTESIAN_POINT('Ctrl Pts',(-1.10635903124558,5.38757549311203,4.));
#30555=CARTESIAN_POINT('',(-0.612642419821478,5.46577252229136,0.));
#30556=CARTESIAN_POINT('',(-0.612642419821478,5.46577252229136,0.));
#30557=CARTESIAN_POINT('',(-1.1063590312456,5.38757549311203,0.));
#30558=CARTESIAN_POINT('Origin',(-0.860389557721269,5.43228587327326,0.));
#30559=CARTESIAN_POINT('',(-1.1063590312456,5.38757549311203,0.));
#30560=CARTESIAN_POINT('Origin',(5.55111512312578E-16,5.5,0.));
#30561=CARTESIAN_POINT('',(0.249935425544578,5.49431818181818,4.));
#30562=CARTESIAN_POINT('',(-0.249935425544576,5.49431818181818,4.));
#30563=CARTESIAN_POINT('Ctrl Pts',(0.249935425544578,5.49431818181818,4.));
#30564=CARTESIAN_POINT('Ctrl Pts',(0.249935425544578,5.49431818181818,4.02673063961771));
#30565=CARTESIAN_POINT('Ctrl Pts',(0.249919456117149,5.49324675169276,4.05414638576008));
#30566=CARTESIAN_POINT('Ctrl Pts',(0.249513006492202,5.48204205167786,4.19012241323844));
#30567=CARTESIAN_POINT('Ctrl Pts',(0.248562585506145,5.45648829138081,4.28686359329028));
#30568=CARTESIAN_POINT('Ctrl Pts',(0.231005155267317,5.40161207108225,4.42646405387434));
#30569=CARTESIAN_POINT('Ctrl Pts',(0.219652829312556,5.37693177978513,4.47482705790043));
#30570=CARTESIAN_POINT('Ctrl Pts',(0.190283636781579,5.33662435870042,4.54353143773203));
#30571=CARTESIAN_POINT('Ctrl Pts',(0.175067268428665,5.31971884723752,4.56934838942208));
#30572=CARTESIAN_POINT('Ctrl Pts',(0.141228917894012,5.29295926834978,4.60714056402291));
#30573=CARTESIAN_POINT('Ctrl Pts',(0.125109626503174,5.28258044284084,4.62089194101728));
#30574=CARTESIAN_POINT('Ctrl Pts',(0.0869023758915849,5.26459283535906,
4.64388394673189));
#30575=CARTESIAN_POINT('Ctrl Pts',(0.064986231744588,5.25739000836648,4.65258978726599));
#30576=CARTESIAN_POINT('Ctrl Pts',(0.0336815115206837,5.25216283051672,
4.65886310574997));
#30577=CARTESIAN_POINT('Ctrl Pts',(0.0260676108035225,5.25124279397842,
4.65995935047192));
#30578=CARTESIAN_POINT('Ctrl Pts',(0.0137773685317983,5.25033755739286,
4.661036848069));
#30579=CARTESIAN_POINT('Ctrl Pts',(0.00916973882989,5.25012547438354,4.66128876278955));
#30580=CARTESIAN_POINT('Ctrl Pts',(0.000479467891945075,5.24996733644903,
4.6614766362689));
#30581=CARTESIAN_POINT('Ctrl Pts',(-0.00359357861859843,5.24999263751242,
4.66144660123004));
#30582=CARTESIAN_POINT('Ctrl Pts',(-0.0126942421010641,5.25027180866649,
4.66111486035927));
#30583=CARTESIAN_POINT('Ctrl Pts',(-0.0177093847734033,5.25057766293744,
4.66075140483911));
#30584=CARTESIAN_POINT('Ctrl Pts',(-0.0322095253360055,5.25189980247768,
4.65917598249656));
#30585=CARTESIAN_POINT('Ctrl Pts',(-0.0415665688190214,5.25330281532761,
4.65750148702093));
#30586=CARTESIAN_POINT('Ctrl Pts',(-0.0736350348471669,5.25994632142597,
4.64948528566701));
#30587=CARTESIAN_POINT('Ctrl Pts',(-0.0945710803031294,5.26763660382283,
4.64009844156317));
#30588=CARTESIAN_POINT('Ctrl Pts',(-0.13223515439229,5.28676363878308,4.61539308723158));
#30589=CARTESIAN_POINT('Ctrl Pts',(-0.148496635843228,5.29806531811862,
4.60019195379194));
#30590=CARTESIAN_POINT('Ctrl Pts',(-0.180499640843389,5.32537773353358,
4.56080656181527));
#30591=CARTESIAN_POINT('Ctrl Pts',(-0.194416032106083,5.34169360047391,
4.53533737515855));
#30592=CARTESIAN_POINT('Ctrl Pts',(-0.220758455803101,5.37956209359798,
4.46952174021344));
#30593=CARTESIAN_POINT('Ctrl Pts',(-0.231081290935902,5.40217940042789,
4.42457618200305));
#30594=CARTESIAN_POINT('Ctrl Pts',(-0.250896331361511,5.46315994101283,
4.27073174534979));
#30595=CARTESIAN_POINT('Ctrl Pts',(-0.249935425544556,5.49431818181818,
4.14407324412982));
#30596=CARTESIAN_POINT('Ctrl Pts',(-0.249935425544556,5.49431818181818,
4.));
#30597=CARTESIAN_POINT('',(0.249935425544578,5.49431818181818,0.));
#30598=CARTESIAN_POINT('',(0.249935425544578,5.49431818181818,0.));
#30599=CARTESIAN_POINT('',(-0.249935425544576,5.49431818181818,0.));
#30600=CARTESIAN_POINT('Origin',(5.55111512312578E-16,5.5,0.));
#30601=CARTESIAN_POINT('',(-0.249935425544576,5.49431818181818,0.));
#30602=CARTESIAN_POINT('Origin',(0.860389557721271,5.43228587327326,0.));
#30603=CARTESIAN_POINT('',(1.1063590312456,5.38757549311203,4.));
#30604=CARTESIAN_POINT('',(0.612642419821479,5.46577252229136,4.));
#30605=CARTESIAN_POINT('Ctrl Pts',(1.1063590312456,5.38757549311203,4.));
#30606=CARTESIAN_POINT('Ctrl Pts',(1.1063590312456,5.38757549311203,4.02673063961778));
#30607=CARTESIAN_POINT('Ctrl Pts',(1.10617564982983,5.38651975223822,4.05414638576023));
#30608=CARTESIAN_POINT('Ctrl Pts',(1.10402140302145,5.37551658340324,4.19012241323862));
#30609=CARTESIAN_POINT('Ctrl Pts',(1.09908519447303,5.350426110898,4.28686359329042));
#30610=CARTESIAN_POINT('Ctrl Pts',(1.0731593931695,5.29897209514011,4.42646405387433));
#30611=CARTESIAN_POINT('Ctrl Pts',(1.05808598501926,5.27637155422115,4.47482705790043));
#30612=CARTESIAN_POINT('Ctrl Pts',(1.02277290612914,5.24115473829854,4.54353143773207));
#30613=CARTESIAN_POINT('Ctrl Pts',(1.00509927187884,5.22683772617799,4.56934838942211));
#30614=CARTESIAN_POINT('Ctrl Pts',(0.96749140718278,5.20570108637508,4.60714056402294));
#30615=CARTESIAN_POINT('Ctrl Pts',(0.949946965001159,5.19797165415638,4.6208919410173));
#30616=CARTESIAN_POINT('Ctrl Pts',(0.909396227292128,5.18618243478151,4.6438839467319));
#30617=CARTESIAN_POINT('Ctrl Pts',(0.886623136859981,5.182496726827,4.65258978726599));
#30618=CARTESIAN_POINT('Ctrl Pts',(0.854886118918656,5.18223104137204,4.65886310574997));
#30619=CARTESIAN_POINT('Ctrl Pts',(0.847222032530184,5.1825134084958,4.65995935047192));
#30620=CARTESIAN_POINT('Ctrl Pts',(0.834941493334322,5.18354193434975,4.66103684806899));
#30621=CARTESIAN_POINT('Ctrl Pts',(0.830357414107859,5.18405325452173,4.66128876278954));
#30622=CARTESIAN_POINT('Ctrl Pts',(0.821749396602616,5.18525652141284,4.6614766362689));
#30623=CARTESIAN_POINT('Ctrl Pts',(0.817730454011735,5.18591867583013,4.66144660123003));
#30624=CARTESIAN_POINT('Ctrl Pts',(0.808785506788659,5.18761806734741,4.66111486035927));
#30625=CARTESIAN_POINT('Ctrl Pts',(0.803879954994051,5.18870469720579,4.66075140483911));
#30626=CARTESIAN_POINT('Ctrl Pts',(0.78976516341501,5.19227888074625,4.65917598249655));
#30627=CARTESIAN_POINT('Ctrl Pts',(0.780742800229017,5.19512838427146,4.65750148702093));
#30628=CARTESIAN_POINT('Ctrl Pts',(0.750108423554737,5.20670671111326,4.64948528566701));
#30629=CARTESIAN_POINT('Ctrl Pts',(0.730633160772473,5.21757743244348,4.64009844156316));
#30630=CARTESIAN_POINT('Ctrl Pts',(0.696424921417117,5.24236094114525,4.61539308723157));
#30631=CARTESIAN_POINT('Ctrl Pts',(0.682131617948134,5.25606733420563,4.60019195379195));
#30632=CARTESIAN_POINT('Ctrl Pts',(0.654795226139856,5.28804986143137,4.56080656181527));
#30633=CARTESIAN_POINT('Ctrl Pts',(0.64360253266301,5.30634185619751,4.53533737515854));
#30634=CARTESIAN_POINT('Ctrl Pts',(0.623508365378152,5.34786498829105,4.4695217402133));
#30635=CARTESIAN_POINT('Ctrl Pts',(0.61685074777022,5.3718186857343,4.42457618200285));
#30636=CARTESIAN_POINT('Ctrl Pts',(0.606819121617707,5.43514820992188,4.27073174534981));
#30637=CARTESIAN_POINT('Ctrl Pts',(0.6126424198215,5.46577252229136,4.14407324412984));
#30638=CARTESIAN_POINT('Ctrl Pts',(0.6126424198215,5.46577252229136,4.));
#30639=CARTESIAN_POINT('',(1.1063590312456,5.38757549311203,0.));
#30640=CARTESIAN_POINT('',(1.1063590312456,5.38757549311203,0.));
#30641=CARTESIAN_POINT('',(0.612642419821479,5.46577252229136,0.));
#30642=CARTESIAN_POINT('Origin',(0.860389557721271,5.43228587327326,0.));
#30643=CARTESIAN_POINT('',(0.612642419821479,5.46577252229136,0.));
#30644=CARTESIAN_POINT('Origin',(1.69959346906221,5.23081083962335,0.));
#30645=CARTESIAN_POINT('',(1.93554040580225,5.14817281542751,4.));
#30646=CARTESIAN_POINT('',(1.46013497556791,5.30264140340673,4.));
#30647=CARTESIAN_POINT('Ctrl Pts',(1.93554040580225,5.14817281542752,4.));
#30648=CARTESIAN_POINT('Ctrl Pts',(1.93554040580225,5.14817281542752,4.02673063961771));
#30649=CARTESIAN_POINT('Ctrl Pts',(1.9351941278572,5.14715875964944,4.05414638576008));
#30650=CARTESIAN_POINT('Ctrl Pts',(1.93134512857137,5.1366280565286,4.19012241323841));
#30651=CARTESIAN_POINT('Ctrl Pts',(1.92254467829738,5.11261868251876,4.28686359329026));
#30652=CARTESIAN_POINT('Ctrl Pts',(1.88888888520004,5.06585383993554,4.42646405387427));
#30653=CARTESIAN_POINT('Ctrl Pts',(1.87046555218873,5.04588954971905,4.47482705790038));
#30654=CARTESIAN_POINT('Ctrl Pts',(1.8300781121392,5.01663049384451,4.54353143773201));
#30655=CARTESIAN_POINT('Ctrl Pts',(1.81038239552218,5.00525451342014,4.56934838942206));
#30656=CARTESIAN_POINT('Ctrl Pts',(1.76993104710689,4.99026126692246,4.6071405640229));
#30657=CARTESIAN_POINT('Ctrl Pts',(1.75139345652766,4.98537155226774,4.62089194101727));
#30658=CARTESIAN_POINT('Ctrl Pts',(1.70949772546377,4.98007101070696,4.64388394673188));
#30659=CARTESIAN_POINT('Ctrl Pts',(1.68642843781245,4.97999317615251,4.65258978726598));
#30660=CARTESIAN_POINT('Ctrl Pts',(1.65504059286449,4.98469552515,4.65886310574997));
#30661=CARTESIAN_POINT('Ctrl Pts',(1.64751503604724,4.98617334312012,4.65995935047191));
#30662=CARTESIAN_POINT('Ctrl Pts',(1.63554658755904,4.98911030569357,4.66103684806899));
#30663=CARTESIAN_POINT('Ctrl Pts',(1.63109893405225,4.99033243864724,4.66128876278954));
#30664=CARTESIAN_POINT('Ctrl Pts',(1.62278512793909,4.9928674819397,4.6614766362689));
#30665=CARTESIAN_POINT('Ctrl Pts',(1.61891924897259,4.99415018527156,4.66144660123003));
#30666=CARTESIAN_POINT('Ctrl Pts',(1.61035027229599,4.99722795249295,4.66111486035926));
#30667=CARTESIAN_POINT('Ctrl Pts',(1.60567510234484,4.99906860150535,4.6607514048391));
#30668=CARTESIAN_POINT('Ctrl Pts',(1.59229321276247,5.0048068207852,4.65917598249655));
#30669=CARTESIAN_POINT('Ctrl Pts',(1.58382769039865,5.00903265075193,4.65750148702093));
#30670=CARTESIAN_POINT('Ctrl Pts',(1.55538172310161,5.02526070150406,4.64948528566701));
#30671=CARTESIAN_POINT('Ctrl Pts',(1.53784678859743,5.03904418853064,4.64009844156317));
#30672=CARTESIAN_POINT('Ctrl Pts',(1.50793670435945,5.06887391873793,4.61539308723159));
#30673=CARTESIAN_POINT('Ctrl Pts',(1.49596352744057,5.0846475286371,4.60019195379198));
#30674=CARTESIAN_POINT('Ctrl Pts',(1.47396686151476,5.12051265170942,4.56080656181526));
#30675=CARTESIAN_POINT('Ctrl Pts',(1.46577346708359,5.14033036468259,4.53533737515849));
#30676=CARTESIAN_POINT('Ctrl Pts',(1.45242234129825,5.18448569842591,4.4695217402134));
#30677=CARTESIAN_POINT('Ctrl Pts',(1.449593873856,5.20918596695371,4.424576182003));
#30678=CARTESIAN_POINT('Ctrl Pts',(1.44959267390549,5.2733050916799,4.27073174534986));
#30679=CARTESIAN_POINT('Ctrl Pts',(1.46013497556793,5.30264140340673,4.14407324412991));
#30680=CARTESIAN_POINT('Ctrl Pts',(1.46013497556793,5.30264140340673,4.));
#30681=CARTESIAN_POINT('',(1.93554040580225,5.14817281542751,0.));
#30682=CARTESIAN_POINT('',(1.93554040580225,5.14817281542751,0.));
#30683=CARTESIAN_POINT('',(1.46013497556791,5.30264140340673,0.));
#30684=CARTESIAN_POINT('Origin',(1.69959346906221,5.23081083962335,0.));
#30685=CARTESIAN_POINT('',(1.46013497556791,5.30264140340673,0.));
#30686=CARTESIAN_POINT('Origin',(2.49694774856751,4.90053588303602,0.));
#30687=CARTESIAN_POINT('',(2.71706235187773,4.78200503722117,4.));
#30688=CARTESIAN_POINT('',(2.2716741623057,5.00894165471237,4.));
#30689=CARTESIAN_POINT('Ctrl Pts',(2.71706235187773,4.78200503722117,4.));
#30690=CARTESIAN_POINT('Ctrl Pts',(2.71706235187773,4.78200503722117,4.02673063961773));
#30691=CARTESIAN_POINT('Ctrl Pts',(2.71656170391563,4.78105763595755,4.05414638576012));
#30692=CARTESIAN_POINT('Ctrl Pts',(2.71111272728885,4.77125869941104,4.19012241323842));
#30693=CARTESIAN_POINT('Ctrl Pts',(2.69866473158208,4.74892161436726,4.28686359329027));
#30694=CARTESIAN_POINT('Ctrl Pts',(2.65810766401412,4.70799745058669,4.42646405387437));
#30695=CARTESIAN_POINT('Ctrl Pts',(2.63678804974402,4.6911609981555,4.47482705790045));
#30696=CARTESIAN_POINT('Ctrl Pts',(2.59232072134733,4.66858015738991,4.54353143773201));
#30697=CARTESIAN_POINT('Ctrl Pts',(2.57108789627304,4.66042532305449,4.56934838942207));
#30698=CARTESIAN_POINT('Ctrl Pts',(2.52878911058682,4.65194465335057,4.60714056402291));
#30699=CARTESIAN_POINT('Ctrl Pts',(2.50971482861278,4.65001505726266,4.62089194101728));
#30700=CARTESIAN_POINT('Ctrl Pts',(2.46750571613677,4.65133371044068,4.64388394673189));
#30701=CARTESIAN_POINT('Ctrl Pts',(2.44470827369085,4.65486566583135,4.65258978726599));
#30702=CARTESIAN_POINT('Ctrl Pts',(2.41444247464919,4.66442026184278,4.65886310574998));
#30703=CARTESIAN_POINT('Ctrl Pts',(2.40724075158789,4.66705714187622,4.65995935047192));
#30704=CARTESIAN_POINT('Ctrl Pts',(2.3958790967301,4.6718302234034,4.661036848069));
#30705=CARTESIAN_POINT('Ctrl Pts',(2.39167738493326,4.67373307616941,4.66128876278955));
#30706=CARTESIAN_POINT('Ctrl Pts',(2.38386250371063,4.67753747468405,4.6614766362689));
#30707=CARTESIAN_POINT('Ctrl Pts',(2.3802448791388,4.67940914251739,4.66144660123004));
#30708=CARTESIAN_POINT('Ctrl Pts',(2.37226286965328,4.68378950059938,4.66111486035927));
#30709=CARTESIAN_POINT('Ctrl Pts',(2.36793319974581,4.68633884587833,4.66075140483911));
#30710=CARTESIAN_POINT('Ctrl Pts',(2.35561371869349,4.69409980689487,4.65917598249656));
#30711=CARTESIAN_POINT('Ctrl Pts',(2.3479134864079,4.69959790934461,4.65750148702094));
#30712=CARTESIAN_POINT('Ctrl Pts',(2.32235636260971,4.72007609553974,4.64948528566702));
#30713=CARTESIAN_POINT('Ctrl Pts',(2.30719352466623,4.73643295306733,4.64009844156317));
#30714=CARTESIAN_POINT('Ctrl Pts',(2.28231808108543,4.77057439782323,4.61539308723159));
#30715=CARTESIAN_POINT('Ctrl Pts',(2.27295985006911,4.78802682593589,4.60019195379197));
#30716=CARTESIAN_POINT('Ctrl Pts',(2.25684454094365,4.82689142649517,4.56080656181529));
#30717=CARTESIAN_POINT('Ctrl Pts',(2.25185219412136,4.84774687981072,4.53533737515856));
#30718=CARTESIAN_POINT('Ctrl Pts',(2.24557285886215,4.89344716434413,4.46952174021327));
#30719=CARTESIAN_POINT('Ctrl Pts',(2.24664318784121,4.9182858013698,4.42457618200281));
#30720=CARTESIAN_POINT('Ctrl Pts',(2.25667244363945,4.98161570098455,4.2707317453499));
#30721=CARTESIAN_POINT('Ctrl Pts',(2.27167416230572,5.00894165471236,4.14407324412995));
#30722=CARTESIAN_POINT('Ctrl Pts',(2.27167416230572,5.00894165471236,4.));
#30723=CARTESIAN_POINT('',(2.71706235187773,4.78200503722117,0.));
#30724=CARTESIAN_POINT('',(2.71706235187773,4.78200503722117,0.));
#30725=CARTESIAN_POINT('',(2.2716741623057,5.00894165471237,0.));
#30726=CARTESIAN_POINT('Origin',(2.49694774856751,4.90053588303602,0.));
#30727=CARTESIAN_POINT('',(2.2716741623057,5.00894165471237,0.));
#30728=CARTESIAN_POINT('Origin',(3.2328188876086,4.44959346906221,0.));
#30729=CARTESIAN_POINT('',(3.43168120543702,4.29808842443363,4.));
#30730=CARTESIAN_POINT('',(3.02727719191323,4.59190513875472,4.));
#30731=CARTESIAN_POINT('Ctrl Pts',(3.43168120543702,4.29808842443363,4.));
#30732=CARTESIAN_POINT('Ctrl Pts',(3.43168120543702,4.29808842443363,4.02673063961771));
#30733=CARTESIAN_POINT('Ctrl Pts',(3.43103851507226,4.29723100584781,4.05414638576007));
#30734=CARTESIAN_POINT('Ctrl Pts',(3.4241237329932,4.28840511821422,4.19012241323845));
#30735=CARTESIAN_POINT('Ctrl Pts',(3.40833470282044,4.26829033530279,4.28686359329029));
#30736=CARTESIAN_POINT('Ctrl Pts',(3.36187501038662,4.23421453905672,4.4264640538744));
#30737=CARTESIAN_POINT('Ctrl Pts',(3.33818407451679,4.22092049374665,4.47482705790047));
#30738=CARTESIAN_POINT('Ctrl Pts',(3.29073179097663,4.20557388333114,4.54353143773206));
#30739=CARTESIAN_POINT('Ctrl Pts',(3.26848468006611,4.20084099417036,4.56934838942209));
#30740=CARTESIAN_POINT('Ctrl Pts',(3.22537999359419,4.19908172349404,4.60714056402291));
#30741=CARTESIAN_POINT('Ctrl Pts',(3.20623869235145,4.20015975903259,4.62089194101728));
#30742=CARTESIAN_POINT('Ctrl Pts',(3.16475552689653,4.20806513733182,4.64388394673189));
#30743=CARTESIAN_POINT('Ctrl Pts',(3.14279127834938,4.215119914204,4.65258978726599));
#30744=CARTESIAN_POINT('Ctrl Pts',(3.11439276963289,4.22929149136567,4.65886310574998));
#30745=CARTESIAN_POINT('Ctrl Pts',(3.10769221065044,4.23302250472471,4.65995935047192));
#30746=CARTESIAN_POINT('Ctrl Pts',(3.0972171110728,4.23951417609748,4.661036848069));
#30747=CARTESIAN_POINT('Ctrl Pts',(3.09336480107503,4.24205089412553,4.66128876278955));
#30748=CARTESIAN_POINT('Ctrl Pts',(3.08624127305476,4.24703097094481,4.6614766362689));
#30749=CARTESIAN_POINT('Ctrl Pts',(3.08296098080077,4.24944551660588,4.66144660123004));
#30750=CARTESIAN_POINT('Ctrl Pts',(3.07576248207062,4.25502060659492,4.66111486035927));
#30751=CARTESIAN_POINT('Ctrl Pts',(3.07188492304929,4.25821587479887,4.66075140483911));
#30752=CARTESIAN_POINT('Ctrl Pts',(3.06093119703656,4.26780847693471,4.65917598249656));
#30753=CARTESIAN_POINT('Ctrl Pts',(3.05418586010366,4.27444347033801,4.65750148702093));
#30754=CARTESIAN_POINT('Ctrl Pts',(3.03214688101148,4.2986675510688,4.64948528566702));
#30755=CARTESIAN_POINT('Ctrl Pts',(3.01972949902144,4.31719501897974,4.64009844156318));
#30756=CARTESIAN_POINT('Ctrl Pts',(3.00050121207562,4.35480750260546,4.61539308723158));
#30757=CARTESIAN_POINT('Ctrl Pts',(2.99398835766767,4.37350901223017,4.60019195379194));
#30758=CARTESIAN_POINT('Ctrl Pts',(2.98415121773687,4.41441611482646,4.56080656181526));
#30759=CARTESIAN_POINT('Ctrl Pts',(2.98248284667088,4.43579577800851,4.53533737515849));
#30760=CARTESIAN_POINT('Ctrl Pts',(2.98342992001184,4.48191572065583,4.46952174021363));
#30761=CARTESIAN_POINT('Ctrl Pts',(2.98837269036043,4.50628111650115,4.42457618200332));
#30762=CARTESIAN_POINT('Ctrl Pts',(3.00818544834457,4.56726239869641,4.27073174534976));
#30763=CARTESIAN_POINT('Ctrl Pts',(3.02727719191324,4.59190513875471,4.14407324412977));
#30764=CARTESIAN_POINT('Ctrl Pts',(3.02727719191324,4.59190513875471,4.));
#30765=CARTESIAN_POINT('',(3.43168120543702,4.29808842443363,0.));
#30766=CARTESIAN_POINT('',(3.43168120543702,4.29808842443363,0.));
#30767=CARTESIAN_POINT('',(3.02727719191323,4.59190513875472,0.));
#30768=CARTESIAN_POINT('Origin',(3.2328188876086,4.44959346906221,0.));
#30769=CARTESIAN_POINT('',(3.02727719191323,4.59190513875472,0.));
#30770=CARTESIAN_POINT('Origin',(3.88908729652601,3.88908729652601,0.));
#30771=CARTESIAN_POINT('',(4.06180067862149,3.70833861009886,4.));
#30772=CARTESIAN_POINT('',(3.70833861009886,4.0618006786215,4.));
#30773=CARTESIAN_POINT('Ctrl Pts',(4.06180067862149,3.70833861009886,4.));
#30774=CARTESIAN_POINT('Ctrl Pts',(4.06180067862149,3.70833861009886,4.02673063961773));
#30775=CARTESIAN_POINT('Ctrl Pts',(4.06103177102382,3.70759228668204,4.05414638576012));
#30776=CARTESIAN_POINT('Ctrl Pts',(4.0528214483761,3.69995677060634,4.19012241323843));
#30777=CARTESIAN_POINT('Ctrl Pts',(4.03408016206104,3.68255958253971,4.28686359329027));
#30778=CARTESIAN_POINT('Ctrl Pts',(3.98286183657991,3.65617121302278,4.42646405387441));
#30779=CARTESIAN_POINT('Ctrl Pts',(3.9573829285772,3.64674691834979,4.47482705790048));
#30780=CARTESIAN_POINT('Ctrl Pts',(3.90811412259945,3.63901242276528,4.54353143773204));
#30781=CARTESIAN_POINT('Ctrl Pts',(3.88540052355725,3.63781801821782,4.56934838942208));
#30782=CARTESIAN_POINT('Ctrl Pts',(3.84255131673683,3.64282346565182,4.60714056402289));
#30783=CARTESIAN_POINT('Ctrl Pts',(3.82381431858832,3.64688258800408,4.62089194101728));
#30784=CARTESIAN_POINT('Ctrl Pts',(3.78407855336266,3.66118003477434,4.64388394673189));
#30785=CARTESIAN_POINT('Ctrl Pts',(3.7634883314087,3.67158392110797,4.65258978726599));
#30786=CARTESIAN_POINT('Ctrl Pts',(3.73765637855118,3.69002352815742,4.65886310574998));
#30787=CARTESIAN_POINT('Ctrl Pts',(3.73162197364763,3.69475680491063,4.65995935047192));
#30788=CARTESIAN_POINT('Ctrl Pts',(3.72229136106665,3.70280721963516,4.661036848069));
#30789=CARTESIAN_POINT('Ctrl Pts',(3.71888330952516,3.70591534050851,4.66128876278955));
#30790=CARTESIAN_POINT('Ctrl Pts',(3.71262653960873,3.71194846961323,4.6614766362689));
#30791=CARTESIAN_POINT('Ctrl Pts',(3.70976435135452,3.71484643897443,4.66144660123004));
#30792=CARTESIAN_POINT('Ctrl Pts',(3.70352661430894,3.72147898365233,4.66111486035927));
#30793=CARTESIAN_POINT('Ctrl Pts',(3.70019664454575,3.72524149667361,4.6607514048391));
#30794=CARTESIAN_POINT('Ctrl Pts',(3.69087839066038,3.73642953822813,4.65917598249656));
#30795=CARTESIAN_POINT('Ctrl Pts',(3.68525404166196,3.7440380470271,4.65750148702094));
#30796=CARTESIAN_POINT('Ctrl Pts',(3.66727588008421,3.77141154503087,4.64948528566702));
#30797=CARTESIAN_POINT('Ctrl Pts',(3.65790971120312,3.79165341557608,4.64009844156317));
#30798=CARTESIAN_POINT('Ctrl Pts',(3.64480204513195,3.831810793896,4.61539308723159));
#30799=CARTESIAN_POINT('Ctrl Pts',(3.6412949354228,3.85130089179904,4.60019195379197));
#30800=CARTESIAN_POINT('Ctrl Pts',(3.63797818771934,3.89324322780353,4.56080656181529));
#30801=CARTESIAN_POINT('Ctrl Pts',(3.63967487324229,3.91462066258948,4.53533737515856));
#30802=CARTESIAN_POINT('Ctrl Pts',(3.6478250350946,3.96002463729993,4.46952174021337));
#30803=CARTESIAN_POINT('Ctrl Pts',(3.65651853940274,3.98331683505499,4.42457618200295));
#30804=CARTESIAN_POINT('Ctrl Pts',(3.6856269437163,4.04044793827739,4.27073174534987));
#30805=CARTESIAN_POINT('Ctrl Pts',(3.70833861009888,4.06180067862148,4.14407324412992));
#30806=CARTESIAN_POINT('Ctrl Pts',(3.70833861009888,4.06180067862148,4.));
#30807=CARTESIAN_POINT('',(4.06180067862149,3.70833861009886,0.));
#30808=CARTESIAN_POINT('',(4.0618006786215,3.70833861009886,0.));
#30809=CARTESIAN_POINT('',(3.70833861009886,4.0618006786215,0.));
#30810=CARTESIAN_POINT('Origin',(3.88908729652601,3.88908729652601,0.));
#30811=CARTESIAN_POINT('',(3.70833861009886,4.06180067862149,0.));
#30812=CARTESIAN_POINT('Origin',(4.44959346906221,3.2328188876086,0.));
#30813=CARTESIAN_POINT('',(4.59190513875472,3.02727719191323,4.));
#30814=CARTESIAN_POINT('',(4.29808842443363,3.43168120543702,4.));
#30815=CARTESIAN_POINT('Ctrl Pts',(4.59190513875472,3.02727719191322,4.));
#30816=CARTESIAN_POINT('Ctrl Pts',(4.59190513875472,3.02727719191322,4.02673063961771));
#30817=CARTESIAN_POINT('Ctrl Pts',(4.59102894698104,3.02666034062482,4.05414638576008));
#30818=CARTESIAN_POINT('Ctrl Pts',(4.58172524915676,3.02040320785364,4.19012241323846));
#30819=CARTESIAN_POINT('Ctrl Pts',(4.56049317936719,3.00615199113995,4.28686359329029));
#30820=CARTESIAN_POINT('Ctrl Pts',(4.5057773859961,2.98810081758768,4.42646405387423));
#30821=CARTESIAN_POINT('Ctrl Pts',(4.47913788113519,2.98277833096402,4.47482705790036));
#30822=CARTESIAN_POINT('Ctrl Pts',(4.42926571423672,2.98284639916111,4.54353143773204));
#30823=CARTESIAN_POINT('Ctrl Pts',(4.40664491125335,2.98521988943094,4.56934838942208));
#30824=CARTESIAN_POINT('Ctrl Pts',(4.3651062737647,2.99686680424732,4.60714056402289));
#30825=CARTESIAN_POINT('Ctrl Pts',(4.34723494578937,3.00380706434951,4.62089194101728));
#30826=CARTESIAN_POINT('Ctrl Pts',(4.3102250072083,3.02414452900082,4.6438839467319));
#30827=CARTESIAN_POINT('Ctrl Pts',(4.29151581144705,3.03764134658586,4.65258978726599));
#30828=CARTESIAN_POINT('Ctrl Pts',(4.26888648285923,3.05989493919995,4.65886310574998));
#30829=CARTESIAN_POINT('Ctrl Pts',(4.26366681911034,3.06551393036484,4.65995935047192));
#30830=CARTESIAN_POINT('Ctrl Pts',(4.25571044417427,3.07492486051281,4.661036848069));
#30831=CARTESIAN_POINT('Ctrl Pts',(4.2528305686287,3.0785278519803,4.66128876278955));
#30832=CARTESIAN_POINT('Ctrl Pts',(4.24759461925646,3.08546547770911,4.6614766362689));
#30833=CARTESIAN_POINT('Ctrl Pts',(4.24522101157591,3.08877551314697,4.66144660123004));
#30834=CARTESIAN_POINT('Ctrl Pts',(4.24009763000285,3.09630219725156,4.66111486035927));
#30835=CARTESIAN_POINT('Ctrl Pts',(4.2373972444049,3.10053930953252,4.66075140483911));
#30836=CARTESIAN_POINT('Ctrl Pts',(4.22994390898303,3.11304730379171,4.65917598249656));
#30837=CARTESIAN_POINT('Ctrl Pts',(4.22557903805757,3.12144198124854,4.65750148702093));
#30838=CARTESIAN_POINT('Ctrl Pts',(4.21210437599839,3.15129087015698,4.64948528566701));
#30839=CARTESIAN_POINT('Ctrl Pts',(4.20602004638866,3.1727487213047,4.64009844156317));
#30840=CARTESIAN_POINT('Ctrl Pts',(4.19935575543264,3.21446218638994,4.61539308723158));
#30841=CARTESIAN_POINT('Ctrl Pts',(4.19894074710277,3.23426096167702,4.60019195379196));
#30842=CARTESIAN_POINT('Ctrl Pts',(4.20222606096277,3.27620577157864,4.56080656181527));
#30843=CARTESIAN_POINT('Ctrl Pts',(4.20724602504612,3.29705459457643,4.53533737515852));
#30844=CARTESIAN_POINT('Ctrl Pts',(4.22239859137616,3.3406246048053,4.46952174021328));
#30845=CARTESIAN_POINT('Ctrl Pts',(4.23462876671566,3.36227007325903,4.42457618200282));
#30846=CARTESIAN_POINT('Ctrl Pts',(4.27231607183923,3.41414424014013,4.27073174534982));
#30847=CARTESIAN_POINT('Ctrl Pts',(4.29808842443364,3.431681205437,4.14407324412984));
#30848=CARTESIAN_POINT('Ctrl Pts',(4.29808842443364,3.431681205437,4.));
#30849=CARTESIAN_POINT('',(4.59190513875472,3.02727719191323,0.));
#30850=CARTESIAN_POINT('',(4.59190513875472,3.02727719191322,0.));
#30851=CARTESIAN_POINT('',(4.29808842443363,3.43168120543702,0.));
#30852=CARTESIAN_POINT('Origin',(4.44959346906221,3.2328188876086,0.));
#30853=CARTESIAN_POINT('',(4.29808842443363,3.43168120543702,0.));
#30854=CARTESIAN_POINT('Origin',(4.90053588303602,2.49694774856751,0.));
#30855=CARTESIAN_POINT('',(5.00894165471237,2.2716741623057,4.));
#30856=CARTESIAN_POINT('',(4.78200503722117,2.71706235187773,4.));
#30857=CARTESIAN_POINT('Ctrl Pts',(5.00894165471237,2.2716741623057,4.));
#30858=CARTESIAN_POINT('Ctrl Pts',(5.00894165471237,2.2716741623057,4.02673063961773));
#30859=CARTESIAN_POINT('Ctrl Pts',(5.00797975351207,2.27120197207165,4.05414638576012));
#30860=CARTESIAN_POINT('Ctrl Pts',(4.99781176842886,2.26647729398004,4.19012241323845));
#30861=CARTESIAN_POINT('Ctrl Pts',(4.97461171918823,2.25572296087186,4.28686359329029));
#30862=CARTESIAN_POINT('Ctrl Pts',(4.91774574235111,2.24645346308547,4.42646405387443));
#30863=CARTESIAN_POINT('Ctrl Pts',(4.89060159365309,2.24536384179619,4.47482705790049));
#30864=CARTESIAN_POINT('Ctrl Pts',(4.84135408409934,2.25323279770997,4.54353143773205));
#30865=CARTESIAN_POINT('Ctrl Pts',(4.81938307641841,2.25911573958948,4.56934838942209));
#30866=CARTESIAN_POINT('Ctrl Pts',(4.78017782737534,2.27711733609155,4.60714056402289));
#30867=CARTESIAN_POINT('Ctrl Pts',(4.76361222097947,2.28676784170657,4.62089194101728));
#30868=CARTESIAN_POINT('Ctrl Pts',(4.73023941655983,2.31264454836303,4.6438839467319));
#30869=CARTESIAN_POINT('Ctrl Pts',(4.71387192948318,2.32890196075716,4.65258978726599));
#30870=CARTESIAN_POINT('Ctrl Pts',(4.6950024343373,2.3544215816303,4.65886310574997));
#30871=CARTESIAN_POINT('Ctrl Pts',(4.69072603718763,2.36078792899602,4.65995935047192));
#30872=CARTESIAN_POINT('Ctrl Pts',(4.68433981225311,2.37132764623411,4.661036848069));
#30873=CARTESIAN_POINT('Ctrl Pts',(4.68205902479715,2.37533679068817,4.66128876278955));
#30874=CARTESIAN_POINT('Ctrl Pts',(4.67797282241977,2.38300808567095,4.6614766362689));
#30875=CARTESIAN_POINT('Ctrl Pts',(4.67614624141153,2.38664868312759,4.66144660123004));
#30876=CARTESIAN_POINT('Ctrl Pts',(4.67226336996882,2.39488417471663,4.66111486035927));
#30877=CARTESIAN_POINT('Ctrl Pts',(4.67025906099161,2.39949155449074,4.66075140483911));
#30878=CARTESIAN_POINT('Ctrl Pts',(4.66485416988754,2.41301151312426,4.65917598249656));
#30879=CARTESIAN_POINT('Ctrl Pts',(4.66185625464341,2.42198565441962,4.65750148702093));
#30880=CARTESIAN_POINT('Ctrl Pts',(4.65321688300254,2.45357495552503,4.64948528566701));
#30881=CARTESIAN_POINT('Ctrl Pts',(4.65056420905187,2.47572042376549,4.64009844156317));
#30882=CARTESIAN_POINT('Ctrl Pts',(4.65050739017187,2.51796285166657,4.61539308723158));
#30883=CARTESIAN_POINT('Ctrl Pts',(4.65319470210369,2.53758279278176,4.60019195379196));
#30884=CARTESIAN_POINT('Ctrl Pts',(4.66300118219658,2.57849725615389,4.56080656181528));
#30885=CARTESIAN_POINT('Ctrl Pts',(4.67122081666429,2.59830410014804,4.53533737515854));
#30886=CARTESIAN_POINT('Ctrl Pts',(4.69300268100047,2.63896730764281,4.4695217402134));
#30887=CARTESIAN_POINT('Ctrl Pts',(4.70846837986482,2.65843306352472,4.424576182003));
#30888=CARTESIAN_POINT('Ctrl Pts',(4.75380659926932,2.70377297991551,4.27073174534984));
#30889=CARTESIAN_POINT('Ctrl Pts',(4.78200503722118,2.71706235187771,4.14407324412987));
#30890=CARTESIAN_POINT('Ctrl Pts',(4.78200503722118,2.71706235187771,4.));
#30891=CARTESIAN_POINT('',(5.00894165471237,2.2716741623057,0.));
#30892=CARTESIAN_POINT('',(5.00894165471237,2.2716741623057,0.));
#30893=CARTESIAN_POINT('',(4.78200503722117,2.71706235187773,0.));
#30894=CARTESIAN_POINT('Origin',(4.90053588303602,2.49694774856751,0.));
#30895=CARTESIAN_POINT('',(4.78200503722117,2.71706235187773,0.));
#30896=CARTESIAN_POINT('Origin',(5.23081083962335,1.69959346906221,0.));
#30897=CARTESIAN_POINT('',(5.30264140340673,1.46013497556791,4.));
#30898=CARTESIAN_POINT('',(5.14817281542751,1.93554040580225,4.));
#30899=CARTESIAN_POINT('Ctrl Pts',(5.30264140340673,1.46013497556791,4.));
#30900=CARTESIAN_POINT('Ctrl Pts',(5.30264140340673,1.46013497556791,4.02673063961776));
#30901=CARTESIAN_POINT('Ctrl Pts',(5.30161747797973,1.45981907327888,4.05414638576018));
#30902=CARTESIAN_POINT('Ctrl Pts',(5.29083557517593,1.45674318712175,4.19012241323858));
#30903=CARTESIAN_POINT('Ctrl Pts',(5.26623880869307,1.4497505449918,4.28686359329039));
#30904=CARTESIAN_POINT('Ctrl Pts',(5.2086228774672,1.44949096877052,4.42646405387422));
#30905=CARTESIAN_POINT('Ctrl Pts',(5.18164246395932,1.45266104290794,4.47482705790035));
#30906=CARTESIAN_POINT('Ctrl Pts',(5.13423224887842,1.46813712672829,4.54353143773208));
#30907=CARTESIAN_POINT('Ctrl Pts',(5.11345203562662,1.47738466266404,4.5693483894221));
#30908=CARTESIAN_POINT('Ctrl Pts',(5.07754553837533,1.50129768180206,4.6071405640229));
#30909=CARTESIAN_POINT('Ctrl Pts',(5.0626935537665,1.51342080545347,4.62089194101728));
#30910=CARTESIAN_POINT('Ctrl Pts',(5.03377963271106,1.54419958371734,4.6438839467319));
#30911=CARTESIAN_POINT('Ctrl Pts',(5.02015687617143,1.56281727947215,4.65258978726599));
#30912=CARTESIAN_POINT('Ctrl Pts',(5.00551184406225,1.59097455084369,4.65886310574997));
#30913=CARTESIAN_POINT('Ctrl Pts',(5.00228401260219,1.59793149380939,4.65995935047191));
#30914=CARTESIAN_POINT('Ctrl Pts',(4.99762518772177,1.60934047531985,4.66103684806899));
#30915=CARTESIAN_POINT('Ctrl Pts',(4.99599964891208,1.61365705431844,4.66128876278954));
#30916=CARTESIAN_POINT('Ctrl Pts',(4.99316380939342,1.62187312581317,4.6614766362689));
#30917=CARTESIAN_POINT('Ctrl Pts',(4.99192923154398,1.62575464169678,4.66144660123003));
#30918=CARTESIAN_POINT('Ctrl Pts',(4.98938247941308,1.63449615563528,4.66111486035926));
#30919=CARTESIAN_POINT('Ctrl Pts',(4.98812359979553,1.63936035392149,4.6607514048391));
#30920=CARTESIAN_POINT('Ctrl Pts',(4.98490023936606,1.6535593706776,4.65917598249655));
#30921=CARTESIAN_POINT('Ctrl Pts',(4.98334309842607,1.66289200266933,4.65750148702093));
#30922=CARTESIAN_POINT('Ctrl Pts',(4.97975174720573,1.69544388253964,4.649485285667));
#30923=CARTESIAN_POINT('Ctrl Pts',(4.98059604655052,1.71773167294816,4.64009844156315));
#30924=CARTESIAN_POINT('Ctrl Pts',(4.98714809881592,1.75946291489558,4.61539308723157));
#30925=CARTESIAN_POINT('Ctrl Pts',(4.992871560471,1.77842091377375,4.60019195379196));
#30926=CARTESIAN_POINT('Ctrl Pts',(5.00895773871105,1.81729758074086,4.56080656181526));
#30927=CARTESIAN_POINT('Ctrl Pts',(5.02017464888312,1.83557473549709,4.53533737515852));
#30928=CARTESIAN_POINT('Ctrl Pts',(5.04804946943565,1.87232987713585,4.46952174021341));
#30929=CARTESIAN_POINT('Ctrl Pts',(5.06636987499111,1.88913660893297,4.42457618200302));
#30930=CARTESIAN_POINT('Ctrl Pts',(5.11824263124586,1.9268258556173,4.27073174534981));
#30931=CARTESIAN_POINT('Ctrl Pts',(5.14817281542752,1.93554040580223,4.14407324412983));
#30932=CARTESIAN_POINT('Ctrl Pts',(5.14817281542752,1.93554040580223,4.));
#30933=CARTESIAN_POINT('',(5.30264140340673,1.46013497556791,0.));
#30934=CARTESIAN_POINT('',(5.30264140340673,1.46013497556791,0.));
#30935=CARTESIAN_POINT('',(5.14817281542751,1.93554040580225,0.));
#30936=CARTESIAN_POINT('Origin',(5.23081083962335,1.69959346906221,0.));
#30937=CARTESIAN_POINT('',(5.14817281542751,1.93554040580225,0.));
#30938=CARTESIAN_POINT('Origin',(5.43228587327326,0.86038955772127,0.));
#30939=CARTESIAN_POINT('',(5.46577252229136,0.612642419821478,4.));
#30940=CARTESIAN_POINT('',(5.38757549311203,1.1063590312456,4.));
#30941=CARTESIAN_POINT('Ctrl Pts',(5.46577252229136,0.612642419821478,4.));
#30942=CARTESIAN_POINT('Ctrl Pts',(5.46577252229136,0.612642419821478,4.02673063961772));
#30943=CARTESIAN_POINT('Ctrl Pts',(5.46471178507988,0.612490584040257,4.0541463857601));
#30944=CARTESIAN_POINT('Ctrl Pts',(5.45358145078565,0.611139228343089,4.19012241323844));
#30945=CARTESIAN_POINT('Ctrl Pts',(5.42819362108338,0.608080459247841,4.28686359329029));
#30946=CARTESIAN_POINT('Ctrl Pts',(5.37124643091175,0.616837196219698,4.42646405387413));
#30947=CARTESIAN_POINT('Ctrl Pts',(5.34509409991741,0.624188908037709,4.47482705790029));
#30948=CARTESIAN_POINT('Ctrl Pts',(5.30068857615022,0.646891047218769,4.54353143773206));
#30949=CARTESIAN_POINT('Ctrl Pts',(5.2816108351434,0.659275472185214,4.56934838942208));
#30950=CARTESIAN_POINT('Ctrl Pts',(5.24988722681303,0.688511096065236,4.60714056402288));
#30951=CARTESIAN_POINT('Ctrl Pts',(5.23711456914321,0.702808326214387,4.62089194101727));
#30952=CARTESIAN_POINT('Ctrl Pts',(5.21337148814817,0.737731300415894,4.64388394673189));
#30953=CARTESIAN_POINT('Ctrl Pts',(5.20282889962289,0.758250850073321,4.65258978726599));
#30954=CARTESIAN_POINT('Ctrl Pts',(5.19276893984501,0.788352446473467,4.65886310574997));
#30955=CARTESIAN_POINT('Ctrl Pts',(5.19066915399765,0.795728682014571,4.65995935047192));
#30956=CARTESIAN_POINT('Ctrl Pts',(5.18785244490161,0.8077260008085,4.661036848069));
#30957=CARTESIAN_POINT('Ctrl Pts',(5.18692218089855,0.812243725850719,4.66128876278954));
#30958=CARTESIAN_POINT('Ctrl Pts',(5.1854065320192,0.820802266909536,4.6614766362689));
#30959=CARTESIAN_POINT('Ctrl Pts',(5.18479435673255,0.824829125417031,4.66144660123003));
#30960=CARTESIAN_POINT('Ctrl Pts',(5.18364643340307,0.833861416620435,4.66111486035927));
#30961=CARTESIAN_POINT('Ctrl Pts',(5.18316398093936,0.838862660713559,4.66075140483911));
#30962=CARTESIAN_POINT('Ctrl Pts',(5.18220152101598,0.853391108675971,4.65917598249655));
#30963=CARTESIAN_POINT('Ctrl Pts',(5.18212349635794,0.862852430991219,4.65750148702092));
#30964=CARTESIAN_POINT('Ctrl Pts',(5.18366859654418,0.895565354310452,4.64948528566701));
#30965=CARTESIAN_POINT('Ctrl Pts',(5.18798907973248,0.917446667518238,4.64009844156317));
#30966=CARTESIAN_POINT('Ctrl Pts',(5.2009886698715,0.957639161837228,4.61539308723158));
#30967=CARTESIAN_POINT('Ctrl Pts',(5.20960735062881,0.975468409628032,4.60019195379195));
#30968=CARTESIAN_POINT('Ctrl Pts',(5.23157713192079,1.01135000762511,4.56080656181527));
#30969=CARTESIAN_POINT('Ctrl Pts',(5.245515120242,1.02764742893492,4.53533737515852));
#30970=CARTESIAN_POINT('Ctrl Pts',(5.27879652641762,1.0595894711472,4.46952174021347));
#30971=CARTESIAN_POINT('Ctrl Pts',(5.29952052947748,1.07332334134434,4.42457618200309));
#30972=CARTESIAN_POINT('Ctrl Pts',(5.35665054316768,1.10243388398541,4.27073174534985));
#30973=CARTESIAN_POINT('Ctrl Pts',(5.38757549311203,1.10635903124558,4.14407324412988));
#30974=CARTESIAN_POINT('Ctrl Pts',(5.38757549311203,1.10635903124558,4.));
#30975=CARTESIAN_POINT('',(5.46577252229136,0.612642419821478,0.));
#30976=CARTESIAN_POINT('',(5.46577252229136,0.612642419821478,0.));
#30977=CARTESIAN_POINT('',(5.38757549311203,1.1063590312456,0.));
#30978=CARTESIAN_POINT('Origin',(5.43228587327326,0.86038955772127,0.));
#30979=CARTESIAN_POINT('',(5.38757549311203,1.1063590312456,0.));
#30980=CARTESIAN_POINT('Origin',(5.5,-2.77555756156289E-16,0.));
#30981=CARTESIAN_POINT('',(5.49431818181818,-0.249935425544577,4.));
#30982=CARTESIAN_POINT('',(5.49431818181818,0.249935425544577,4.));
#30983=CARTESIAN_POINT('Ctrl Pts',(5.49431818181818,-0.249935425544577,
4.));
#30984=CARTESIAN_POINT('Ctrl Pts',(5.49431818181818,-0.249935425544577,
4.02673063961774));
#30985=CARTESIAN_POINT('Ctrl Pts',(5.49324675169276,-0.249919456117149,
4.05414638576014));
#30986=CARTESIAN_POINT('Ctrl Pts',(5.48204205167785,-0.2495130064922,4.19012241323845));
#30987=CARTESIAN_POINT('Ctrl Pts',(5.45648829138081,-0.248562585506152,
4.28686359329028));
#30988=CARTESIAN_POINT('Ctrl Pts',(5.4016120710822,-0.231005155267301,4.42646405387446));
#30989=CARTESIAN_POINT('Ctrl Pts',(5.37693177978508,-0.219652829312523,
4.47482705790052));
#30990=CARTESIAN_POINT('Ctrl Pts',(5.3366243587004,-0.190283636781565,4.54353143773205));
#30991=CARTESIAN_POINT('Ctrl Pts',(5.31971884723751,-0.175067268428654,
4.56934838942209));
#30992=CARTESIAN_POINT('Ctrl Pts',(5.29295926834979,-0.14122891789402,4.60714056402289));
#30993=CARTESIAN_POINT('Ctrl Pts',(5.28258044284084,-0.125109626503179,
4.62089194101728));
#30994=CARTESIAN_POINT('Ctrl Pts',(5.26459283535906,-0.086902375891581,
4.64388394673189));
#30995=CARTESIAN_POINT('Ctrl Pts',(5.25739000836648,-0.0649862317445868,
4.65258978726599));
#30996=CARTESIAN_POINT('Ctrl Pts',(5.25216283051672,-0.0336815115206723,
4.65886310574998));
#30997=CARTESIAN_POINT('Ctrl Pts',(5.25124279397842,-0.0260676108035159,
4.65995935047192));
#30998=CARTESIAN_POINT('Ctrl Pts',(5.25033755739286,-0.0137773685317611,
4.661036848069));
#30999=CARTESIAN_POINT('Ctrl Pts',(5.25012547438354,-0.00916973882987097,
4.66128876278955));
#31000=CARTESIAN_POINT('Ctrl Pts',(5.24996733644903,-0.00047946789193707,
4.6614766362689));
#31001=CARTESIAN_POINT('Ctrl Pts',(5.24999263751242,0.00359357861861347,
4.66144660123004));
#31002=CARTESIAN_POINT('Ctrl Pts',(5.25027180866649,0.0126942421010739,
4.66111486035927));
#31003=CARTESIAN_POINT('Ctrl Pts',(5.25057766293744,0.0177093847734224,
4.6607514048391));
#31004=CARTESIAN_POINT('Ctrl Pts',(5.25189980247768,0.0322095253359952,
4.65917598249656));
#31005=CARTESIAN_POINT('Ctrl Pts',(5.25330281532761,0.0415665688190047,
4.65750148702093));
#31006=CARTESIAN_POINT('Ctrl Pts',(5.25994632142597,0.0736350348471544,
4.64948528566701));
#31007=CARTESIAN_POINT('Ctrl Pts',(5.26763660382283,0.0945710803031198,
4.64009844156318));
#31008=CARTESIAN_POINT('Ctrl Pts',(5.28676363878308,0.132235154392277,4.61539308723158));
#31009=CARTESIAN_POINT('Ctrl Pts',(5.29806531811861,0.148496635843216,4.60019195379196));
#31010=CARTESIAN_POINT('Ctrl Pts',(5.32537773353357,0.180499640843384,4.56080656181528));
#31011=CARTESIAN_POINT('Ctrl Pts',(5.3416936004739,0.194416032106081,4.53533737515856));
#31012=CARTESIAN_POINT('Ctrl Pts',(5.37956209359802,0.220758455803131,4.46952174021337));
#31013=CARTESIAN_POINT('Ctrl Pts',(5.40217940042793,0.231081290935914,4.42457618200295));
#31014=CARTESIAN_POINT('Ctrl Pts',(5.4631599410128,0.250896331361503,4.27073174534984));
#31015=CARTESIAN_POINT('Ctrl Pts',(5.49431818181818,0.249935425544556,4.14407324412989));
#31016=CARTESIAN_POINT('Ctrl Pts',(5.49431818181818,0.249935425544556,4.));
#31017=CARTESIAN_POINT('',(5.49431818181818,-0.249935425544577,0.));
#31018=CARTESIAN_POINT('',(5.49431818181818,-0.249935425544577,0.));
#31019=CARTESIAN_POINT('',(5.49431818181818,0.249935425544577,0.));
#31020=CARTESIAN_POINT('Origin',(5.5,-2.77555756156289E-16,0.));
#31021=CARTESIAN_POINT('',(5.49431818181818,0.249935425544577,0.));
#31022=CARTESIAN_POINT('Origin',(5.43228587327326,-0.86038955772127,0.));
#31023=CARTESIAN_POINT('',(5.38757549311203,-1.1063590312456,4.));
#31024=CARTESIAN_POINT('',(5.46577252229136,-0.612642419821479,4.));
#31025=CARTESIAN_POINT('Ctrl Pts',(5.38757549311203,-1.1063590312456,4.));
#31026=CARTESIAN_POINT('Ctrl Pts',(5.38757549311203,-1.1063590312456,4.02673063961776));
#31027=CARTESIAN_POINT('Ctrl Pts',(5.38651975223822,-1.10617564982983,4.05414638576019));
#31028=CARTESIAN_POINT('Ctrl Pts',(5.37551658340325,-1.10402140302146,4.19012241323857));
#31029=CARTESIAN_POINT('Ctrl Pts',(5.35042611089801,-1.09908519447303,4.28686359329038));
#31030=CARTESIAN_POINT('Ctrl Pts',(5.29897209514011,-1.0731593931695,4.42646405387435));
#31031=CARTESIAN_POINT('Ctrl Pts',(5.27637155422115,-1.05808598501925,4.47482705790044));
#31032=CARTESIAN_POINT('Ctrl Pts',(5.24115473829854,-1.02277290612914,4.54353143773208));
#31033=CARTESIAN_POINT('Ctrl Pts',(5.226837726178,-1.00509927187884,4.56934838942211));
#31034=CARTESIAN_POINT('Ctrl Pts',(5.20570108637508,-0.967491407182789,
4.60714056402292));
#31035=CARTESIAN_POINT('Ctrl Pts',(5.19797165415638,-0.949946965001165,
4.62089194101729));
#31036=CARTESIAN_POINT('Ctrl Pts',(5.18618243478152,-0.909396227292144,
4.64388394673189));
#31037=CARTESIAN_POINT('Ctrl Pts',(5.182496726827,-0.88662313685999,4.65258978726599));
#31038=CARTESIAN_POINT('Ctrl Pts',(5.18223104137204,-0.854886118918637,
4.65886310574998));
#31039=CARTESIAN_POINT('Ctrl Pts',(5.1825134084958,-0.847222032530173,4.65995935047192));
#31040=CARTESIAN_POINT('Ctrl Pts',(5.18354193434976,-0.834941493334267,
4.661036848069));
#31041=CARTESIAN_POINT('Ctrl Pts',(5.18405325452173,-0.830357414107832,
4.66128876278954));
#31042=CARTESIAN_POINT('Ctrl Pts',(5.18525652141284,-0.821749396602635,
4.6614766362689));
#31043=CARTESIAN_POINT('Ctrl Pts',(5.18591867583012,-0.817730454011772,
4.66144660123003));
#31044=CARTESIAN_POINT('Ctrl Pts',(5.18761806734741,-0.808785506788643,
4.66111486035927));
#31045=CARTESIAN_POINT('Ctrl Pts',(5.1887046972058,-0.803879954994019,4.6607514048391));
#31046=CARTESIAN_POINT('Ctrl Pts',(5.19227888074625,-0.789765163415024,
4.65917598249656));
#31047=CARTESIAN_POINT('Ctrl Pts',(5.19512838427145,-0.780742800229044,
4.65750148702093));
#31048=CARTESIAN_POINT('Ctrl Pts',(5.20670671111326,-0.750108423554733,
4.64948528566701));
#31049=CARTESIAN_POINT('Ctrl Pts',(5.21757743244349,-0.730633160772468,
4.64009844156316));
#31050=CARTESIAN_POINT('Ctrl Pts',(5.24236094114524,-0.696424921417119,
4.61539308723158));
#31051=CARTESIAN_POINT('Ctrl Pts',(5.25606733420563,-0.682131617948136,
4.60019195379195));
#31052=CARTESIAN_POINT('Ctrl Pts',(5.28804986143138,-0.654795226139849,
4.56080656181526));
#31053=CARTESIAN_POINT('Ctrl Pts',(5.30634185619752,-0.643602532663006,
4.53533737515852));
#31054=CARTESIAN_POINT('Ctrl Pts',(5.34786498829094,-0.623508365378209,
4.46952174021347));
#31055=CARTESIAN_POINT('Ctrl Pts',(5.3718186857342,-0.616850747770234,4.42457618200311));
#31056=CARTESIAN_POINT('Ctrl Pts',(5.43514820992188,-0.606819121617703,
4.27073174534979));
#31057=CARTESIAN_POINT('Ctrl Pts',(5.46577252229136,-0.612642419821499,
4.14407324412982));
#31058=CARTESIAN_POINT('Ctrl Pts',(5.46577252229136,-0.612642419821499,
4.));
#31059=CARTESIAN_POINT('',(5.38757549311203,-1.1063590312456,0.));
#31060=CARTESIAN_POINT('',(5.38757549311203,-1.1063590312456,0.));
#31061=CARTESIAN_POINT('',(5.46577252229136,-0.612642419821479,0.));
#31062=CARTESIAN_POINT('Origin',(5.43228587327326,-0.86038955772127,0.));
#31063=CARTESIAN_POINT('',(5.46577252229136,-0.612642419821479,0.));
#31064=CARTESIAN_POINT('Origin',(5.23081083962335,-1.69959346906221,0.));
#31065=CARTESIAN_POINT('',(5.14817281542751,-1.93554040580225,4.));
#31066=CARTESIAN_POINT('',(5.30264140340673,-1.46013497556791,4.));
#31067=CARTESIAN_POINT('Ctrl Pts',(5.14817281542752,-1.93554040580225,4.));
#31068=CARTESIAN_POINT('Ctrl Pts',(5.14817281542752,-1.93554040580225,4.02673063961775));
#31069=CARTESIAN_POINT('Ctrl Pts',(5.14715875964944,-1.93519412785719,4.05414638576015));
#31070=CARTESIAN_POINT('Ctrl Pts',(5.13662805652859,-1.93134512857135,4.19012241323851));
#31071=CARTESIAN_POINT('Ctrl Pts',(5.11261868251874,-1.92254467829737,4.28686359329034));
#31072=CARTESIAN_POINT('Ctrl Pts',(5.06585383993552,-1.88888888520002,4.42646405387432));
#31073=CARTESIAN_POINT('Ctrl Pts',(5.04588954971903,-1.87046555218872,4.47482705790042));
#31074=CARTESIAN_POINT('Ctrl Pts',(5.01663049384449,-1.83007811213917,4.54353143773206));
#31075=CARTESIAN_POINT('Ctrl Pts',(5.00525451342013,-1.81038239552215,4.56934838942209));
#31076=CARTESIAN_POINT('Ctrl Pts',(4.99026126692246,-1.76993104710687,4.60714056402291));
#31077=CARTESIAN_POINT('Ctrl Pts',(4.98537155226774,-1.75139345652764,4.62089194101728));
#31078=CARTESIAN_POINT('Ctrl Pts',(4.98007101070696,-1.70949772546375,4.64388394673189));
#31079=CARTESIAN_POINT('Ctrl Pts',(4.97999317615251,-1.68642843781244,4.65258978726599));
#31080=CARTESIAN_POINT('Ctrl Pts',(4.98469552515001,-1.65504059286449,4.65886310574997));
#31081=CARTESIAN_POINT('Ctrl Pts',(4.98617334312012,-1.64751503604723,4.65995935047191));
#31082=CARTESIAN_POINT('Ctrl Pts',(4.98911030569358,-1.63554658755898,4.66103684806899));
#31083=CARTESIAN_POINT('Ctrl Pts',(4.99033243864725,-1.63109893405222,4.66128876278954));
#31084=CARTESIAN_POINT('Ctrl Pts',(4.9928674819397,-1.6227851279391,4.66147663626889));
#31085=CARTESIAN_POINT('Ctrl Pts',(4.99415018527155,-1.61891924897263,4.66144660123003));
#31086=CARTESIAN_POINT('Ctrl Pts',(4.99722795249295,-1.610350272296,4.66111486035926));
#31087=CARTESIAN_POINT('Ctrl Pts',(4.99906860150534,-1.60567510234485,4.6607514048391));
#31088=CARTESIAN_POINT('Ctrl Pts',(5.00480682078521,-1.59229321276246,4.65917598249655));
#31089=CARTESIAN_POINT('Ctrl Pts',(5.00903265075193,-1.58382769039864,4.65750148702093));
#31090=CARTESIAN_POINT('Ctrl Pts',(5.02526070150406,-1.5553817231016,4.64948528566701));
#31091=CARTESIAN_POINT('Ctrl Pts',(5.03904418853065,-1.53784678859743,4.64009844156316));
#31092=CARTESIAN_POINT('Ctrl Pts',(5.06887391873794,-1.50793670435944,4.61539308723158));
#31093=CARTESIAN_POINT('Ctrl Pts',(5.08464752863712,-1.49596352744056,4.60019195379196));
#31094=CARTESIAN_POINT('Ctrl Pts',(5.12051265170942,-1.47396686151477,4.56080656181526));
#31095=CARTESIAN_POINT('Ctrl Pts',(5.14033036468258,-1.4657734670836,4.53533737515852));
#31096=CARTESIAN_POINT('Ctrl Pts',(5.18448569842586,-1.45242234129827,4.46952174021348));
#31097=CARTESIAN_POINT('Ctrl Pts',(5.20918596695366,-1.449593873856,4.42457618200312));
#31098=CARTESIAN_POINT('Ctrl Pts',(5.27330509167992,-1.44959267390549,4.27073174534981));
#31099=CARTESIAN_POINT('Ctrl Pts',(5.30264140340673,-1.46013497556793,4.14407324412984));
#31100=CARTESIAN_POINT('Ctrl Pts',(5.30264140340673,-1.46013497556793,4.));
#31101=CARTESIAN_POINT('',(5.14817281542751,-1.93554040580225,0.));
#31102=CARTESIAN_POINT('',(5.14817281542751,-1.93554040580225,0.));
#31103=CARTESIAN_POINT('',(5.30264140340673,-1.46013497556791,0.));
#31104=CARTESIAN_POINT('Origin',(5.23081083962335,-1.69959346906221,0.));
#31105=CARTESIAN_POINT('',(5.30264140340673,-1.46013497556791,0.));
#31106=CARTESIAN_POINT('Origin',(4.90053588303602,-2.49694774856751,0.));
#31107=CARTESIAN_POINT('',(4.78200503722117,-2.71706235187773,4.));
#31108=CARTESIAN_POINT('',(5.00894165471237,-2.2716741623057,4.));
#31109=CARTESIAN_POINT('Ctrl Pts',(4.78200503722117,-2.71706235187773,4.));
#31110=CARTESIAN_POINT('Ctrl Pts',(4.78200503722117,-2.71706235187773,4.02673063961772));
#31111=CARTESIAN_POINT('Ctrl Pts',(4.78105763595755,-2.71656170391563,4.0541463857601));
#31112=CARTESIAN_POINT('Ctrl Pts',(4.77125869941104,-2.71111272728885,4.19012241323846));
#31113=CARTESIAN_POINT('Ctrl Pts',(4.74892161436725,-2.69866473158207,4.28686359329029));
#31114=CARTESIAN_POINT('Ctrl Pts',(4.70799745058672,-2.65810766401414,4.42646405387428));
#31115=CARTESIAN_POINT('Ctrl Pts',(4.69116099815552,-2.63678804974405,4.47482705790039));
#31116=CARTESIAN_POINT('Ctrl Pts',(4.6685801573899,-2.5923207213473,4.54353143773206));
#31117=CARTESIAN_POINT('Ctrl Pts',(4.66042532305449,-2.57108789627302,4.56934838942209));
#31118=CARTESIAN_POINT('Ctrl Pts',(4.65194465335057,-2.52878911058683,4.60714056402289));
#31119=CARTESIAN_POINT('Ctrl Pts',(4.65001505726266,-2.50971482861278,4.62089194101728));
#31120=CARTESIAN_POINT('Ctrl Pts',(4.65133371044068,-2.46750571613676,4.6438839467319));
#31121=CARTESIAN_POINT('Ctrl Pts',(4.65486566583135,-2.44470827369084,4.65258978726599));
#31122=CARTESIAN_POINT('Ctrl Pts',(4.66442026184278,-2.41444247464922,4.65886310574997));
#31123=CARTESIAN_POINT('Ctrl Pts',(4.66705714187622,-2.40724075158791,4.65995935047192));
#31124=CARTESIAN_POINT('Ctrl Pts',(4.67183022340342,-2.39587909673005,4.661036848069));
#31125=CARTESIAN_POINT('Ctrl Pts',(4.67373307616942,-2.39167738493324,4.66128876278955));
#31126=CARTESIAN_POINT('Ctrl Pts',(4.67753747468404,-2.38386250371066,4.6614766362689));
#31127=CARTESIAN_POINT('Ctrl Pts',(4.67940914251737,-2.38024487913885,4.66144660123004));
#31128=CARTESIAN_POINT('Ctrl Pts',(4.68378950059938,-2.37226286965329,4.66111486035927));
#31129=CARTESIAN_POINT('Ctrl Pts',(4.68633884587832,-2.36793319974582,4.66075140483911));
#31130=CARTESIAN_POINT('Ctrl Pts',(4.69409980689487,-2.35561371869349,4.65917598249656));
#31131=CARTESIAN_POINT('Ctrl Pts',(4.69959790934461,-2.34791348640789,4.65750148702094));
#31132=CARTESIAN_POINT('Ctrl Pts',(4.72007609553975,-2.32235636260971,4.64948528566701));
#31133=CARTESIAN_POINT('Ctrl Pts',(4.73643295306733,-2.30719352466623,4.64009844156317));
#31134=CARTESIAN_POINT('Ctrl Pts',(4.77057439782324,-2.28231808108542,4.61539308723158));
#31135=CARTESIAN_POINT('Ctrl Pts',(4.7880268259359,-2.2729598500691,4.60019195379196));
#31136=CARTESIAN_POINT('Ctrl Pts',(4.82689142649519,-2.25684454094364,4.56080656181527));
#31137=CARTESIAN_POINT('Ctrl Pts',(4.84774687981075,-2.25185219412135,4.53533737515851));
#31138=CARTESIAN_POINT('Ctrl Pts',(4.893447164344,-2.24557285886217,4.46952174021346));
#31139=CARTESIAN_POINT('Ctrl Pts',(4.91828580136969,-2.24664318784119,4.42457618200308));
#31140=CARTESIAN_POINT('Ctrl Pts',(4.98161570098458,-2.25667244363946,4.27073174534982));
#31141=CARTESIAN_POINT('Ctrl Pts',(5.00894165471236,-2.27167416230572,4.14407324412985));
#31142=CARTESIAN_POINT('Ctrl Pts',(5.00894165471236,-2.27167416230572,4.));
#31143=CARTESIAN_POINT('',(4.78200503722117,-2.71706235187773,0.));
#31144=CARTESIAN_POINT('',(4.78200503722117,-2.71706235187773,0.));
#31145=CARTESIAN_POINT('',(5.00894165471237,-2.2716741623057,0.));
#31146=CARTESIAN_POINT('Origin',(4.90053588303602,-2.49694774856751,0.));
#31147=CARTESIAN_POINT('',(5.00894165471237,-2.2716741623057,0.));
#31148=CARTESIAN_POINT('Origin',(4.44959346906221,-3.2328188876086,0.));
#31149=CARTESIAN_POINT('',(4.29808842443363,-3.43168120543702,4.));
#31150=CARTESIAN_POINT('',(4.59190513875472,-3.02727719191323,4.));
#31151=CARTESIAN_POINT('Ctrl Pts',(4.29808842443363,-3.43168120543702,4.));
#31152=CARTESIAN_POINT('Ctrl Pts',(4.29808842443363,-3.43168120543702,4.02673063961769));
#31153=CARTESIAN_POINT('Ctrl Pts',(4.29723100584781,-3.43103851507226,4.05414638576003));
#31154=CARTESIAN_POINT('Ctrl Pts',(4.28840511821423,-3.4241237329932,4.19012241323837));
#31155=CARTESIAN_POINT('Ctrl Pts',(4.26829033530281,-3.40833470282046,4.28686359329022));
#31156=CARTESIAN_POINT('Ctrl Pts',(4.23421453905673,-3.36187501038663,4.42646405387436));
#31157=CARTESIAN_POINT('Ctrl Pts',(4.22092049374666,-3.3381840745168,4.47482705790044));
#31158=CARTESIAN_POINT('Ctrl Pts',(4.20557388333116,-3.29073179097666,4.54353143773201));
#31159=CARTESIAN_POINT('Ctrl Pts',(4.20084099417037,-3.26848468006614,4.56934838942206));
#31160=CARTESIAN_POINT('Ctrl Pts',(4.19908172349404,-3.22537999359422,4.6071405640229));
#31161=CARTESIAN_POINT('Ctrl Pts',(4.20015975903259,-3.20623869235147,4.62089194101727));
#31162=CARTESIAN_POINT('Ctrl Pts',(4.20806513733181,-3.16475552689654,4.64388394673188));
#31163=CARTESIAN_POINT('Ctrl Pts',(4.21511991420399,-3.14279127834939,4.65258978726599));
#31164=CARTESIAN_POINT('Ctrl Pts',(4.22929149136567,-3.1143927696329,4.65886310574997));
#31165=CARTESIAN_POINT('Ctrl Pts',(4.23302250472471,-3.10769221065045,4.65995935047192));
#31166=CARTESIAN_POINT('Ctrl Pts',(4.23951417609748,-3.0972171110728,4.661036848069));
#31167=CARTESIAN_POINT('Ctrl Pts',(4.24205089412553,-3.09336480107503,4.66128876278955));
#31168=CARTESIAN_POINT('Ctrl Pts',(4.24703097094481,-3.08624127305476,4.6614766362689));
#31169=CARTESIAN_POINT('Ctrl Pts',(4.24944551660588,-3.08296098080077,4.66144660123004));
#31170=CARTESIAN_POINT('Ctrl Pts',(4.25502060659492,-3.07576248207062,4.66111486035927));
#31171=CARTESIAN_POINT('Ctrl Pts',(4.25821587479886,-3.0718849230493,4.66075140483911));
#31172=CARTESIAN_POINT('Ctrl Pts',(4.26780847693471,-3.06093119703656,4.65917598249656));
#31173=CARTESIAN_POINT('Ctrl Pts',(4.27444347033799,-3.05418586010367,4.65750148702094));
#31174=CARTESIAN_POINT('Ctrl Pts',(4.2986675510688,-3.03214688101148,4.64948528566702));
#31175=CARTESIAN_POINT('Ctrl Pts',(4.31719501897975,-3.01972949902144,4.64009844156317));
#31176=CARTESIAN_POINT('Ctrl Pts',(4.35480750260544,-3.00050121207564,4.61539308723159));
#31177=CARTESIAN_POINT('Ctrl Pts',(4.37350901223014,-2.99398835766768,4.60019195379197));
#31178=CARTESIAN_POINT('Ctrl Pts',(4.41441611482644,-2.98415121773687,4.56080656181528));
#31179=CARTESIAN_POINT('Ctrl Pts',(4.43579577800848,-2.98248284667088,4.53533737515853));
#31180=CARTESIAN_POINT('Ctrl Pts',(4.48191572065602,-2.98342992001184,4.46952174021336));
#31181=CARTESIAN_POINT('Ctrl Pts',(4.5062811165013,-2.98837269036048,4.42457618200294));
#31182=CARTESIAN_POINT('Ctrl Pts',(4.56726239869637,-3.00818544834456,4.27073174534984));
#31183=CARTESIAN_POINT('Ctrl Pts',(4.59190513875471,-3.02727719191324,4.14407324412988));
#31184=CARTESIAN_POINT('Ctrl Pts',(4.59190513875471,-3.02727719191324,4.));
#31185=CARTESIAN_POINT('',(4.29808842443363,-3.43168120543702,0.));
#31186=CARTESIAN_POINT('',(4.29808842443363,-3.43168120543702,0.));
#31187=CARTESIAN_POINT('',(4.59190513875472,-3.02727719191323,0.));
#31188=CARTESIAN_POINT('Origin',(4.44959346906221,-3.2328188876086,0.));
#31189=CARTESIAN_POINT('',(4.59190513875472,-3.02727719191322,0.));
#31190=CARTESIAN_POINT('Origin',(3.88908729652601,-3.88908729652601,0.));
#31191=CARTESIAN_POINT('',(3.70833861009886,-4.06180067862149,4.));
#31192=CARTESIAN_POINT('',(4.0618006786215,-3.70833861009886,4.));
#31193=CARTESIAN_POINT('Ctrl Pts',(3.70833861009886,-4.06180067862149,4.));
#31194=CARTESIAN_POINT('Ctrl Pts',(3.70833861009886,-4.06180067862149,4.02673063961773));
#31195=CARTESIAN_POINT('Ctrl Pts',(3.70759228668204,-4.06103177102382,4.05414638576013));
#31196=CARTESIAN_POINT('Ctrl Pts',(3.69995677060634,-4.0528214483761,4.19012241323846));
#31197=CARTESIAN_POINT('Ctrl Pts',(3.68255958253971,-4.03408016206103,4.2868635932903));
#31198=CARTESIAN_POINT('Ctrl Pts',(3.6561712130228,-3.98286183657994,4.42646405387435));
#31199=CARTESIAN_POINT('Ctrl Pts',(3.64674691834979,-3.95738292857724,4.47482705790044));
#31200=CARTESIAN_POINT('Ctrl Pts',(3.63901242276528,-3.90811412259946,4.54353143773204));
#31201=CARTESIAN_POINT('Ctrl Pts',(3.63781801821782,-3.88540052355725,4.56934838942208));
#31202=CARTESIAN_POINT('Ctrl Pts',(3.64282346565182,-3.84255131673681,4.60714056402291));
#31203=CARTESIAN_POINT('Ctrl Pts',(3.64688258800408,-3.8238143185883,4.62089194101728));
#31204=CARTESIAN_POINT('Ctrl Pts',(3.66118003477434,-3.78407855336266,4.6438839467319));
#31205=CARTESIAN_POINT('Ctrl Pts',(3.67158392110798,-3.76348833140869,4.65258978726599));
#31206=CARTESIAN_POINT('Ctrl Pts',(3.69002352815741,-3.73765637855119,4.65886310574997));
#31207=CARTESIAN_POINT('Ctrl Pts',(3.69475680491063,-3.73162197364764,4.65995935047192));
#31208=CARTESIAN_POINT('Ctrl Pts',(3.70280721963516,-3.72229136106665,4.661036848069));
#31209=CARTESIAN_POINT('Ctrl Pts',(3.70591534050851,-3.71888330952516,4.66128876278955));
#31210=CARTESIAN_POINT('Ctrl Pts',(3.71194846961324,-3.71262653960872,4.6614766362689));
#31211=CARTESIAN_POINT('Ctrl Pts',(3.71484643897445,-3.70976435135451,4.66144660123004));
#31212=CARTESIAN_POINT('Ctrl Pts',(3.72147898365232,-3.70352661430895,4.66111486035927));
#31213=CARTESIAN_POINT('Ctrl Pts',(3.72524149667359,-3.70019664454577,4.66075140483911));
#31214=CARTESIAN_POINT('Ctrl Pts',(3.73642953822814,-3.69087839066037,4.65917598249656));
#31215=CARTESIAN_POINT('Ctrl Pts',(3.74403804702711,-3.68525404166196,4.65750148702094));
#31216=CARTESIAN_POINT('Ctrl Pts',(3.77141154503086,-3.66727588008421,4.64948528566702));
#31217=CARTESIAN_POINT('Ctrl Pts',(3.79165341557607,-3.65790971120312,4.64009844156318));
#31218=CARTESIAN_POINT('Ctrl Pts',(3.83181079389601,-3.64480204513195,4.61539308723159));
#31219=CARTESIAN_POINT('Ctrl Pts',(3.85130089179905,-3.6412949354228,4.60019195379196));
#31220=CARTESIAN_POINT('Ctrl Pts',(3.89324322780354,-3.63797818771934,4.56080656181528));
#31221=CARTESIAN_POINT('Ctrl Pts',(3.91462066258949,-3.63967487324229,4.53533737515854));
#31222=CARTESIAN_POINT('Ctrl Pts',(3.96002463729994,-3.6478250350946,4.46952174021335));
#31223=CARTESIAN_POINT('Ctrl Pts',(3.983316835055,-3.65651853940275,4.42457618200292));
#31224=CARTESIAN_POINT('Ctrl Pts',(4.04044793827739,-3.68562694371631,4.27073174534986));
#31225=CARTESIAN_POINT('Ctrl Pts',(4.06180067862148,-3.70833861009888,4.1440732441299));
#31226=CARTESIAN_POINT('Ctrl Pts',(4.06180067862148,-3.70833861009888,4.));
#31227=CARTESIAN_POINT('',(3.70833861009886,-4.06180067862149,0.));
#31228=CARTESIAN_POINT('',(3.70833861009886,-4.06180067862149,0.));
#31229=CARTESIAN_POINT('',(4.0618006786215,-3.70833861009886,0.));
#31230=CARTESIAN_POINT('Origin',(3.88908729652601,-3.88908729652601,0.));
#31231=CARTESIAN_POINT('',(4.06180067862149,-3.70833861009886,0.));
#31232=CARTESIAN_POINT('Origin',(3.2328188876086,-4.44959346906221,0.));
#31233=CARTESIAN_POINT('',(3.02727719191323,-4.59190513875472,4.));
#31234=CARTESIAN_POINT('',(3.43168120543702,-4.29808842443363,4.));
#31235=CARTESIAN_POINT('Ctrl Pts',(3.02727719191322,-4.59190513875472,4.));
#31236=CARTESIAN_POINT('Ctrl Pts',(3.02727719191322,-4.59190513875472,4.02673063961775));
#31237=CARTESIAN_POINT('Ctrl Pts',(3.02666034062482,-4.59102894698104,4.05414638576016));
#31238=CARTESIAN_POINT('Ctrl Pts',(3.02040320785363,-4.58172524915675,4.19012241323852));
#31239=CARTESIAN_POINT('Ctrl Pts',(3.00615199113994,-4.56049317936718,4.28686359329035));
#31240=CARTESIAN_POINT('Ctrl Pts',(2.98810081758767,-4.50577738599606,4.42646405387433));
#31241=CARTESIAN_POINT('Ctrl Pts',(2.98277833096401,-4.47913788113514,4.47482705790043));
#31242=CARTESIAN_POINT('Ctrl Pts',(2.98284639916111,-4.4292657142367,4.54353143773207));
#31243=CARTESIAN_POINT('Ctrl Pts',(2.98521988943094,-4.40664491125333,4.5693483894221));
#31244=CARTESIAN_POINT('Ctrl Pts',(2.99686680424733,-4.36510627376467,4.60714056402292));
#31245=CARTESIAN_POINT('Ctrl Pts',(3.00380706434952,-4.34723494578935,4.62089194101729));
#31246=CARTESIAN_POINT('Ctrl Pts',(3.02414452900082,-4.31022500720831,4.6438839467319));
#31247=CARTESIAN_POINT('Ctrl Pts',(3.03764134658586,-4.29151581144705,4.65258978726599));
#31248=CARTESIAN_POINT('Ctrl Pts',(3.05989493919995,-4.26888648285923,4.65886310574998));
#31249=CARTESIAN_POINT('Ctrl Pts',(3.06551393036484,-4.26366681911033,4.65995935047192));
#31250=CARTESIAN_POINT('Ctrl Pts',(3.07492486051284,-4.25571044417424,4.661036848069));
#31251=CARTESIAN_POINT('Ctrl Pts',(3.07852785198032,-4.25283056862869,4.66128876278955));
#31252=CARTESIAN_POINT('Ctrl Pts',(3.08546547770909,-4.24759461925647,4.6614766362689));
#31253=CARTESIAN_POINT('Ctrl Pts',(3.08877551314693,-4.24522101157593,4.66144660123004));
#31254=CARTESIAN_POINT('Ctrl Pts',(3.09630219725157,-4.24009763000284,4.66111486035927));
#31255=CARTESIAN_POINT('Ctrl Pts',(3.10053930953254,-4.23739724440489,4.66075140483911));
#31256=CARTESIAN_POINT('Ctrl Pts',(3.11304730379171,-4.22994390898303,4.65917598249656));
#31257=CARTESIAN_POINT('Ctrl Pts',(3.12144198124853,-4.22557903805758,4.65750148702094));
#31258=CARTESIAN_POINT('Ctrl Pts',(3.15129087015698,-4.21210437599839,4.64948528566701));
#31259=CARTESIAN_POINT('Ctrl Pts',(3.17274872130471,-4.20602004638866,4.64009844156317));
#31260=CARTESIAN_POINT('Ctrl Pts',(3.21446218638993,-4.19935575543265,4.61539308723158));
#31261=CARTESIAN_POINT('Ctrl Pts',(3.23426096167702,-4.19894074710278,4.60019195379196));
#31262=CARTESIAN_POINT('Ctrl Pts',(3.27620577157864,-4.20222606096277,4.56080656181527));
#31263=CARTESIAN_POINT('Ctrl Pts',(3.29705459457642,-4.20724602504612,4.53533737515854));
#31264=CARTESIAN_POINT('Ctrl Pts',(3.34062460480514,-4.2223985913761,4.46952174021351));
#31265=CARTESIAN_POINT('Ctrl Pts',(3.36227007325892,-4.23462876671557,4.42457618200316));
#31266=CARTESIAN_POINT('Ctrl Pts',(3.41414424014014,-4.27231607183923,4.27073174534981));
#31267=CARTESIAN_POINT('Ctrl Pts',(3.431681205437,-4.29808842443364,4.14407324412984));
#31268=CARTESIAN_POINT('Ctrl Pts',(3.431681205437,-4.29808842443364,4.));
#31269=CARTESIAN_POINT('',(3.02727719191323,-4.59190513875472,0.));
#31270=CARTESIAN_POINT('',(3.02727719191322,-4.59190513875472,0.));
#31271=CARTESIAN_POINT('',(3.43168120543702,-4.29808842443363,0.));
#31272=CARTESIAN_POINT('Origin',(3.2328188876086,-4.44959346906221,0.));
#31273=CARTESIAN_POINT('',(3.43168120543702,-4.29808842443363,0.));
#31274=CARTESIAN_POINT('Origin',(2.49694774856751,-4.90053588303602,0.));
#31275=CARTESIAN_POINT('',(2.2716741623057,-5.00894165471237,4.));
#31276=CARTESIAN_POINT('',(2.71706235187773,-4.78200503722117,4.));
#31277=CARTESIAN_POINT('Ctrl Pts',(2.2716741623057,-5.00894165471237,4.));
#31278=CARTESIAN_POINT('Ctrl Pts',(2.2716741623057,-5.00894165471237,4.02673063961774));
#31279=CARTESIAN_POINT('Ctrl Pts',(2.27120197207165,-5.00797975351207,4.05414638576013));
#31280=CARTESIAN_POINT('Ctrl Pts',(2.26647729398003,-4.99781176842886,4.19012241323847));
#31281=CARTESIAN_POINT('Ctrl Pts',(2.25572296087185,-4.97461171918823,4.2868635932903));
#31282=CARTESIAN_POINT('Ctrl Pts',(2.24645346308548,-4.91774574235116,4.42646405387431));
#31283=CARTESIAN_POINT('Ctrl Pts',(2.24536384179618,-4.89060159365315,4.47482705790041));
#31284=CARTESIAN_POINT('Ctrl Pts',(2.25323279770997,-4.84135408409934,4.54353143773206));
#31285=CARTESIAN_POINT('Ctrl Pts',(2.25911573958948,-4.81938307641841,4.56934838942209));
#31286=CARTESIAN_POINT('Ctrl Pts',(2.27711733609156,-4.78017782737533,4.60714056402291));
#31287=CARTESIAN_POINT('Ctrl Pts',(2.28676784170657,-4.76361222097947,4.62089194101728));
#31288=CARTESIAN_POINT('Ctrl Pts',(2.31264454836303,-4.73023941655982,4.6438839467319));
#31289=CARTESIAN_POINT('Ctrl Pts',(2.32890196075716,-4.71387192948318,4.65258978726599));
#31290=CARTESIAN_POINT('Ctrl Pts',(2.35442158163029,-4.69500243433731,4.65886310574997));
#31291=CARTESIAN_POINT('Ctrl Pts',(2.36078792899601,-4.69072603718764,4.65995935047192));
#31292=CARTESIAN_POINT('Ctrl Pts',(2.37132764623416,-4.68433981225308,4.661036848069));
#31293=CARTESIAN_POINT('Ctrl Pts',(2.3753367906882,-4.68205902479713,4.66128876278955));
#31294=CARTESIAN_POINT('Ctrl Pts',(2.38300808567094,-4.67797282241977,4.6614766362689));
#31295=CARTESIAN_POINT('Ctrl Pts',(2.38664868312759,-4.67614624141154,4.66144660123004));
#31296=CARTESIAN_POINT('Ctrl Pts',(2.39488417471663,-4.67226336996883,4.66111486035927));
#31297=CARTESIAN_POINT('Ctrl Pts',(2.39949155449074,-4.67025906099161,4.66075140483911));
#31298=CARTESIAN_POINT('Ctrl Pts',(2.41301151312425,-4.66485416988755,4.65917598249656));
#31299=CARTESIAN_POINT('Ctrl Pts',(2.4219856544196,-4.66185625464342,4.65750148702094));
#31300=CARTESIAN_POINT('Ctrl Pts',(2.45357495552503,-4.65321688300254,4.64948528566701));
#31301=CARTESIAN_POINT('Ctrl Pts',(2.4757204237655,-4.65056420905187,4.64009844156317));
#31302=CARTESIAN_POINT('Ctrl Pts',(2.51796285166657,-4.65050739017187,4.61539308723158));
#31303=CARTESIAN_POINT('Ctrl Pts',(2.53758279278176,-4.65319470210369,4.60019195379196));
#31304=CARTESIAN_POINT('Ctrl Pts',(2.57849725615389,-4.66300118219658,4.56080656181528));
#31305=CARTESIAN_POINT('Ctrl Pts',(2.59830410014803,-4.67122081666428,4.53533737515855));
#31306=CARTESIAN_POINT('Ctrl Pts',(2.63896730764288,-4.69300268100051,4.46952174021329));
#31307=CARTESIAN_POINT('Ctrl Pts',(2.65843306352477,-4.70846837986487,4.42457618200283));
#31308=CARTESIAN_POINT('Ctrl Pts',(2.7037729799155,-4.75380659926932,4.27073174534984));
#31309=CARTESIAN_POINT('Ctrl Pts',(2.71706235187771,-4.78200503722118,4.14407324412987));
#31310=CARTESIAN_POINT('Ctrl Pts',(2.71706235187771,-4.78200503722118,4.));
#31311=CARTESIAN_POINT('',(2.2716741623057,-5.00894165471237,0.));
#31312=CARTESIAN_POINT('',(2.2716741623057,-5.00894165471237,0.));
#31313=CARTESIAN_POINT('',(2.71706235187773,-4.78200503722117,0.));
#31314=CARTESIAN_POINT('Origin',(2.49694774856751,-4.90053588303602,0.));
#31315=CARTESIAN_POINT('',(2.71706235187773,-4.78200503722117,0.));
#31316=CARTESIAN_POINT('Origin',(1.69959346906221,-5.23081083962335,0.));
#31317=CARTESIAN_POINT('',(1.46013497556791,-5.30264140340673,4.));
#31318=CARTESIAN_POINT('',(1.93554040580225,-5.14817281542751,4.));
#31319=CARTESIAN_POINT('Ctrl Pts',(1.46013497556791,-5.30264140340673,4.));
#31320=CARTESIAN_POINT('Ctrl Pts',(1.46013497556791,-5.30264140340673,4.0267306396177));
#31321=CARTESIAN_POINT('Ctrl Pts',(1.45981907327888,-5.30161747797973,4.05414638576006));
#31322=CARTESIAN_POINT('Ctrl Pts',(1.45674318712176,-5.29083557517596,4.19012241323839));
#31323=CARTESIAN_POINT('Ctrl Pts',(1.4497505449918,-5.26623880869312,4.28686359329023));
#31324=CARTESIAN_POINT('Ctrl Pts',(1.44949096877051,-5.20862287746716,4.42646405387434));
#31325=CARTESIAN_POINT('Ctrl Pts',(1.45266104290796,-5.18164246395926,4.47482705790043));
#31326=CARTESIAN_POINT('Ctrl Pts',(1.46813712672827,-5.13423224887846,4.54353143773201));
#31327=CARTESIAN_POINT('Ctrl Pts',(1.47738466266402,-5.11345203562666,4.56934838942206));
#31328=CARTESIAN_POINT('Ctrl Pts',(1.50129768180205,-5.07754553837534,4.6071405640229));
#31329=CARTESIAN_POINT('Ctrl Pts',(1.51342080545345,-5.06269355376651,4.62089194101727));
#31330=CARTESIAN_POINT('Ctrl Pts',(1.54419958371731,-5.03377963271108,4.64388394673188));
#31331=CARTESIAN_POINT('Ctrl Pts',(1.56281727947213,-5.02015687617145,4.65258978726598));
#31332=CARTESIAN_POINT('Ctrl Pts',(1.59097455084368,-5.00551184406225,4.65886310574997));
#31333=CARTESIAN_POINT('Ctrl Pts',(1.59793149380938,-5.0022840126022,4.65995935047191));
#31334=CARTESIAN_POINT('Ctrl Pts',(1.6093404753199,-4.99762518772175,4.66103684806899));
#31335=CARTESIAN_POINT('Ctrl Pts',(1.61365705431846,-4.99599964891207,4.66128876278954));
#31336=CARTESIAN_POINT('Ctrl Pts',(1.62187312581315,-4.99316380939343,4.66147663626889));
#31337=CARTESIAN_POINT('Ctrl Pts',(1.62575464169675,-4.991929231544,4.66144660123003));
#31338=CARTESIAN_POINT('Ctrl Pts',(1.63449615563527,-4.98938247941308,4.66111486035926));
#31339=CARTESIAN_POINT('Ctrl Pts',(1.63936035392147,-4.98812359979554,4.6607514048391));
#31340=CARTESIAN_POINT('Ctrl Pts',(1.6535593706776,-4.98490023936606,4.65917598249655));
#31341=CARTESIAN_POINT('Ctrl Pts',(1.66289200266933,-4.98334309842607,4.65750148702093));
#31342=CARTESIAN_POINT('Ctrl Pts',(1.69544388253963,-4.97975174720573,4.64948528566701));
#31343=CARTESIAN_POINT('Ctrl Pts',(1.71773167294815,-4.98059604655052,4.64009844156316));
#31344=CARTESIAN_POINT('Ctrl Pts',(1.75946291489558,-4.98714809881592,4.61539308723158));
#31345=CARTESIAN_POINT('Ctrl Pts',(1.77842091377376,-4.992871560471,4.60019195379195));
#31346=CARTESIAN_POINT('Ctrl Pts',(1.81729758074086,-5.00895773871105,4.56080656181527));
#31347=CARTESIAN_POINT('Ctrl Pts',(1.83557473549708,-5.02017464888312,4.53533737515853));
#31348=CARTESIAN_POINT('Ctrl Pts',(1.87232987713586,-5.04804946943565,4.4695217402134));
#31349=CARTESIAN_POINT('Ctrl Pts',(1.88913660893297,-5.06636987499112,4.424576182003));
#31350=CARTESIAN_POINT('Ctrl Pts',(1.92682585561729,-5.11824263124585,4.27073174534984));
#31351=CARTESIAN_POINT('Ctrl Pts',(1.93554040580223,-5.14817281542752,4.14407324412987));
#31352=CARTESIAN_POINT('Ctrl Pts',(1.93554040580223,-5.14817281542752,4.));
#31353=CARTESIAN_POINT('',(1.46013497556791,-5.30264140340673,0.));
#31354=CARTESIAN_POINT('',(1.46013497556791,-5.30264140340673,0.));
#31355=CARTESIAN_POINT('',(1.93554040580225,-5.14817281542751,0.));
#31356=CARTESIAN_POINT('Origin',(1.69959346906221,-5.23081083962335,0.));
#31357=CARTESIAN_POINT('',(1.93554040580225,-5.14817281542751,0.));
#31358=CARTESIAN_POINT('Origin',(0.86038955772127,-5.43228587327326,0.));
#31359=CARTESIAN_POINT('',(0.612642419821478,-5.46577252229136,4.));
#31360=CARTESIAN_POINT('',(1.1063590312456,-5.38757549311203,4.));
#31361=CARTESIAN_POINT('Ctrl Pts',(0.612642419821478,-5.46577252229136,
4.));
#31362=CARTESIAN_POINT('Ctrl Pts',(0.612642419821478,-5.46577252229136,
4.02673063961775));
#31363=CARTESIAN_POINT('Ctrl Pts',(0.612490584040258,-5.46471178507988,
4.05414638576016));
#31364=CARTESIAN_POINT('Ctrl Pts',(0.611139228343089,-5.45358145078564,
4.19012241323849));
#31365=CARTESIAN_POINT('Ctrl Pts',(0.608080459247835,-5.42819362108337,
4.28686359329032));
#31366=CARTESIAN_POINT('Ctrl Pts',(0.616837196219715,-5.37124643091163,
4.42646405387443));
#31367=CARTESIAN_POINT('Ctrl Pts',(0.624188908037774,-5.34509409991728,
4.47482705790049));
#31368=CARTESIAN_POINT('Ctrl Pts',(0.646891047218772,-5.30068857615022,
4.54353143773205));
#31369=CARTESIAN_POINT('Ctrl Pts',(0.659275472185216,-5.28161083514339,
4.56934838942209));
#31370=CARTESIAN_POINT('Ctrl Pts',(0.688511096065256,-5.24988722681301,
4.60714056402291));
#31371=CARTESIAN_POINT('Ctrl Pts',(0.702808326214403,-5.2371145691432,4.62089194101728));
#31372=CARTESIAN_POINT('Ctrl Pts',(0.737731300415902,-5.21337148814816,
4.64388394673189));
#31373=CARTESIAN_POINT('Ctrl Pts',(0.758250850073328,-5.20282889962289,
4.65258978726599));
#31374=CARTESIAN_POINT('Ctrl Pts',(0.788352446473466,-5.19276893984501,
4.65886310574997));
#31375=CARTESIAN_POINT('Ctrl Pts',(0.795728682014572,-5.19066915399765,
4.65995935047192));
#31376=CARTESIAN_POINT('Ctrl Pts',(0.80772600080848,-5.18785244490161,4.661036848069));
#31377=CARTESIAN_POINT('Ctrl Pts',(0.812243725850711,-5.18692218089855,
4.66128876278954));
#31378=CARTESIAN_POINT('Ctrl Pts',(0.820802266909534,-5.1854065320192,4.6614766362689));
#31379=CARTESIAN_POINT('Ctrl Pts',(0.824829125417023,-5.18479435673255,
4.66144660123003));
#31380=CARTESIAN_POINT('Ctrl Pts',(0.833861416620451,-5.18364643340307,
4.66111486035927));
#31381=CARTESIAN_POINT('Ctrl Pts',(0.838862660713588,-5.18316398093936,
4.6607514048391));
#31382=CARTESIAN_POINT('Ctrl Pts',(0.85339110867596,-5.18220152101598,4.65917598249656));
#31383=CARTESIAN_POINT('Ctrl Pts',(0.862852430991196,-5.18212349635793,
4.65750148702093));
#31384=CARTESIAN_POINT('Ctrl Pts',(0.895565354310455,-5.18366859654418,
4.64948528566701));
#31385=CARTESIAN_POINT('Ctrl Pts',(0.917446667518246,-5.18798907973249,
4.64009844156317));
#31386=CARTESIAN_POINT('Ctrl Pts',(0.957639161837223,-5.2009886698715,4.61539308723158));
#31387=CARTESIAN_POINT('Ctrl Pts',(0.975468409628028,-5.20960735062881,
4.60019195379196));
#31388=CARTESIAN_POINT('Ctrl Pts',(1.01135000762511,-5.23157713192079,4.56080656181527));
#31389=CARTESIAN_POINT('Ctrl Pts',(1.02764742893491,-5.24551512024199,4.53533737515854));
#31390=CARTESIAN_POINT('Ctrl Pts',(1.05958947114721,-5.27879652641763,4.46952174021344));
#31391=CARTESIAN_POINT('Ctrl Pts',(1.07332334134435,-5.29952052947749,4.42457618200306));
#31392=CARTESIAN_POINT('Ctrl Pts',(1.1024338839854,-5.35665054316767,4.27073174534985));
#31393=CARTESIAN_POINT('Ctrl Pts',(1.10635903124558,-5.38757549311203,4.1440732441299));
#31394=CARTESIAN_POINT('Ctrl Pts',(1.10635903124558,-5.38757549311203,4.));
#31395=CARTESIAN_POINT('',(0.612642419821478,-5.46577252229136,0.));
#31396=CARTESIAN_POINT('',(0.612642419821478,-5.46577252229136,0.));
#31397=CARTESIAN_POINT('',(1.1063590312456,-5.38757549311203,0.));
#31398=CARTESIAN_POINT('Origin',(0.86038955772127,-5.43228587327326,0.));
#31399=CARTESIAN_POINT('',(1.1063590312456,-5.38757549311203,0.));
#31400=CARTESIAN_POINT('Origin',(0.,0.,0.));
#31401=CARTESIAN_POINT('Origin',(0.,0.,0.));
#31402=CARTESIAN_POINT('Origin',(0.,0.,0.));
#31403=CARTESIAN_POINT('Origin',(0.,0.,0.));
#31404=CARTESIAN_POINT('Origin',(0.,0.,0.));
#31405=CARTESIAN_POINT('Origin',(0.,0.,0.));
#31406=CARTESIAN_POINT('Origin',(0.,0.,0.));
#31407=CARTESIAN_POINT('Origin',(0.,0.,0.));
#31408=CARTESIAN_POINT('Origin',(0.,0.,0.));
#31409=CARTESIAN_POINT('Origin',(0.,0.,0.));
#31410=CARTESIAN_POINT('Origin',(0.,0.,0.));
#31411=CARTESIAN_POINT('Origin',(0.,0.,0.));
#31412=CARTESIAN_POINT('Origin',(0.,0.,0.));
#31413=CARTESIAN_POINT('Origin',(0.,0.,0.));
#31414=CARTESIAN_POINT('Origin',(0.,0.,0.));
#31415=CARTESIAN_POINT('Origin',(0.,0.,0.));
#31416=CARTESIAN_POINT('Origin',(0.,0.,0.));
#31417=CARTESIAN_POINT('Origin',(0.,0.,0.));
#31418=CARTESIAN_POINT('Origin',(0.,0.,0.));
#31419=CARTESIAN_POINT('Origin',(0.,0.,0.));
#31420=CARTESIAN_POINT('Origin',(0.,0.,0.));
#31421=CARTESIAN_POINT('Origin',(0.,0.,0.));
#31422=CARTESIAN_POINT('Origin',(0.,0.,0.));
#31423=CARTESIAN_POINT('Origin',(0.,0.,0.));
#31424=CARTESIAN_POINT('Origin',(0.,0.,0.));
#31425=CARTESIAN_POINT('Origin',(0.,0.,0.));
#31426=CARTESIAN_POINT('Origin',(0.,0.,0.));
#31427=CARTESIAN_POINT('Origin',(0.,0.,0.));
#31428=CARTESIAN_POINT('Origin',(0.,0.,0.));
#31429=CARTESIAN_POINT('Origin',(0.,0.,0.));
#31430=CARTESIAN_POINT('Origin',(0.,0.,0.));
#31431=CARTESIAN_POINT('Origin',(0.,0.,0.));
#31432=CARTESIAN_POINT('Origin',(0.,0.,0.));
#31433=CARTESIAN_POINT('Origin',(0.,0.,0.));
#31434=CARTESIAN_POINT('Origin',(0.,0.,0.));
#31435=CARTESIAN_POINT('Origin',(0.,0.,0.));
#31436=CARTESIAN_POINT('Origin',(0.,0.,0.));
#31437=CARTESIAN_POINT('Origin',(0.,0.,0.));
#31438=CARTESIAN_POINT('Origin',(0.,0.,0.));
#31439=CARTESIAN_POINT('',(0.249935425544577,-5.49431818181818,0.));
#31440=CARTESIAN_POINT('Origin',(0.,0.,0.));
#31441=CARTESIAN_POINT('',(-0.249935425544577,-5.49431818181818,0.));
#31442=CARTESIAN_POINT('Origin',(0.,-5.5,0.));
#31443=CARTESIAN_POINT('Origin',(0.,0.,0.));
#31444=CARTESIAN_POINT('Origin',(0.,0.,0.));
#31445=CARTESIAN_POINT('',(0.249935425544577,-5.49431818181818,4.));
#31446=CARTESIAN_POINT('Origin',(0.,0.,4.));
#31447=CARTESIAN_POINT('',(0.249935425544577,-5.49431818181818,0.));
#31448=CARTESIAN_POINT('Origin',(0.,0.,0.));
#31449=CARTESIAN_POINT('Origin',(0.,0.,4.));
#31450=CARTESIAN_POINT('Origin',(0.,0.,0.));
#31451=CARTESIAN_POINT('Origin',(0.,0.,4.));
#31452=CARTESIAN_POINT('Origin',(0.,0.,0.));
#31453=CARTESIAN_POINT('Origin',(0.,0.,4.));
#31454=CARTESIAN_POINT('Origin',(0.,0.,0.));
#31455=CARTESIAN_POINT('Origin',(0.,0.,4.));
#31456=CARTESIAN_POINT('Origin',(0.,0.,0.));
#31457=CARTESIAN_POINT('Origin',(0.,0.,4.));
#31458=CARTESIAN_POINT('Origin',(0.,0.,0.));
#31459=CARTESIAN_POINT('Origin',(0.,0.,4.));
#31460=CARTESIAN_POINT('Origin',(0.,0.,0.));
#31461=CARTESIAN_POINT('Origin',(0.,0.,4.));
#31462=CARTESIAN_POINT('Origin',(0.,0.,0.));
#31463=CARTESIAN_POINT('Origin',(0.,0.,4.));
#31464=CARTESIAN_POINT('Origin',(0.,0.,0.));
#31465=CARTESIAN_POINT('Origin',(0.,0.,4.));
#31466=CARTESIAN_POINT('Origin',(0.,0.,0.));
#31467=CARTESIAN_POINT('Origin',(0.,0.,4.));
#31468=CARTESIAN_POINT('Origin',(0.,0.,0.));
#31469=CARTESIAN_POINT('Origin',(0.,0.,4.));
#31470=CARTESIAN_POINT('Origin',(0.,0.,0.));
#31471=CARTESIAN_POINT('Origin',(0.,0.,4.));
#31472=CARTESIAN_POINT('Origin',(0.,0.,0.));
#31473=CARTESIAN_POINT('Origin',(0.,0.,4.));
#31474=CARTESIAN_POINT('Origin',(0.,0.,0.));
#31475=CARTESIAN_POINT('Origin',(0.,0.,4.));
#31476=CARTESIAN_POINT('Origin',(0.,0.,0.));
#31477=CARTESIAN_POINT('Origin',(0.,0.,4.));
#31478=CARTESIAN_POINT('Origin',(0.,0.,0.));
#31479=CARTESIAN_POINT('Origin',(0.,0.,4.));
#31480=CARTESIAN_POINT('Origin',(0.,0.,0.));
#31481=CARTESIAN_POINT('Origin',(0.,0.,4.));
#31482=CARTESIAN_POINT('Origin',(0.,0.,0.));
#31483=CARTESIAN_POINT('Origin',(0.,0.,4.));
#31484=CARTESIAN_POINT('Origin',(0.,0.,0.));
#31485=CARTESIAN_POINT('Origin',(0.,0.,4.));
#31486=CARTESIAN_POINT('Origin',(0.,0.,0.));
#31487=CARTESIAN_POINT('Origin',(0.,0.,4.));
#31488=CARTESIAN_POINT('Origin',(0.,0.,0.));
#31489=CARTESIAN_POINT('Origin',(0.,0.,4.));
#31490=CARTESIAN_POINT('Origin',(0.,0.,0.));
#31491=CARTESIAN_POINT('Origin',(0.,0.,4.));
#31492=CARTESIAN_POINT('Origin',(0.,0.,0.));
#31493=CARTESIAN_POINT('Origin',(0.,0.,4.));
#31494=CARTESIAN_POINT('Origin',(0.,0.,0.));
#31495=CARTESIAN_POINT('Origin',(0.,0.,4.));
#31496=CARTESIAN_POINT('Origin',(0.,0.,0.));
#31497=CARTESIAN_POINT('Origin',(0.,0.,4.));
#31498=CARTESIAN_POINT('Origin',(0.,0.,0.));
#31499=CARTESIAN_POINT('Origin',(0.,0.,4.));
#31500=CARTESIAN_POINT('Origin',(0.,0.,0.));
#31501=CARTESIAN_POINT('Origin',(0.,0.,4.));
#31502=CARTESIAN_POINT('Origin',(0.,0.,0.));
#31503=CARTESIAN_POINT('Origin',(0.,0.,4.));
#31504=CARTESIAN_POINT('Origin',(0.,0.,0.));
#31505=CARTESIAN_POINT('Origin',(0.,0.,4.));
#31506=CARTESIAN_POINT('Origin',(0.,0.,0.));
#31507=CARTESIAN_POINT('Origin',(0.,0.,4.));
#31508=CARTESIAN_POINT('Origin',(0.,0.,0.));
#31509=CARTESIAN_POINT('Origin',(0.,0.,4.));
#31510=CARTESIAN_POINT('Origin',(0.,0.,0.));
#31511=CARTESIAN_POINT('Origin',(0.,0.,4.));
#31512=CARTESIAN_POINT('Origin',(0.,0.,0.));
#31513=CARTESIAN_POINT('Origin',(0.,0.,4.));
#31514=CARTESIAN_POINT('Origin',(0.,0.,0.));
#31515=CARTESIAN_POINT('Origin',(0.,0.,4.));
#31516=CARTESIAN_POINT('Origin',(0.,0.,0.));
#31517=CARTESIAN_POINT('Origin',(0.,0.,4.));
#31518=CARTESIAN_POINT('Origin',(0.,0.,0.));
#31519=CARTESIAN_POINT('Origin',(0.,0.,4.));
#31520=CARTESIAN_POINT('Origin',(0.,0.,0.));
#31521=CARTESIAN_POINT('Origin',(0.,0.,4.));
#31522=CARTESIAN_POINT('Origin',(0.,0.,0.));
#31523=CARTESIAN_POINT('Origin',(0.,0.,4.));
#31524=CARTESIAN_POINT('Origin',(0.,0.,4.));
#31525=CARTESIAN_POINT('Origin',(-4.5,-5.51091059616309E-16,4.));
#31526=CARTESIAN_POINT('',(-0.249935425544577,-5.49431818181818,4.));
#31527=CARTESIAN_POINT('Origin',(0.,0.,4.));
#31528=CARTESIAN_POINT('Ctrl Pts',(-0.249935425544577,-5.49431818181818,
4.));
#31529=CARTESIAN_POINT('Ctrl Pts',(-0.249935425544577,-5.49431818181818,
4.02673063961773));
#31530=CARTESIAN_POINT('Ctrl Pts',(-0.249919456117148,-5.49324675169276,
4.05414638576012));
#31531=CARTESIAN_POINT('Ctrl Pts',(-0.249513006492199,-5.48204205167785,
4.19012241323843));
#31532=CARTESIAN_POINT('Ctrl Pts',(-0.24856258550615,-5.45648829138082,
4.28686359329027));
#31533=CARTESIAN_POINT('Ctrl Pts',(-0.231005155267322,-5.40161207108227,
4.42646405387428));
#31534=CARTESIAN_POINT('Ctrl Pts',(-0.219652829312575,-5.37693177978515,
4.4748270579004));
#31535=CARTESIAN_POINT('Ctrl Pts',(-0.190283636781574,-5.33662435870041,
4.54353143773204));
#31536=CARTESIAN_POINT('Ctrl Pts',(-0.175067268428665,-5.31971884723752,
4.56934838942208));
#31537=CARTESIAN_POINT('Ctrl Pts',(-0.141228917894015,-5.29295926834979,
4.6071405640229));
#31538=CARTESIAN_POINT('Ctrl Pts',(-0.125109626503179,-5.28258044284084,
4.62089194101728));
#31539=CARTESIAN_POINT('Ctrl Pts',(-0.0869023758915853,-5.26459283535906,
4.64388394673189));
#31540=CARTESIAN_POINT('Ctrl Pts',(-0.0649862317445936,-5.25739000836648,
4.65258978726599));
#31541=CARTESIAN_POINT('Ctrl Pts',(-0.0336815115207147,-5.25216283051672,
4.65886310574997));
#31542=CARTESIAN_POINT('Ctrl Pts',(-0.026067610803539,-5.25124279397843,
4.65995935047192));
#31543=CARTESIAN_POINT('Ctrl Pts',(-0.0137773685317613,-5.25033755739286,
4.661036848069));
#31544=CARTESIAN_POINT('Ctrl Pts',(-0.0091697388298722,-5.25012547438354,
4.66128876278955));
#31545=CARTESIAN_POINT('Ctrl Pts',(-0.000479467891947508,-5.24996733644903,
4.6614766362689));
#31546=CARTESIAN_POINT('Ctrl Pts',(0.00359357861859472,-5.24999263751242,
4.66144660123004));
#31547=CARTESIAN_POINT('Ctrl Pts',(0.0126942421010939,-5.25027180866649,
4.66111486035927));
#31548=CARTESIAN_POINT('Ctrl Pts',(0.0177093847734648,-5.25057766293745,
4.6607514048391));
#31549=CARTESIAN_POINT('Ctrl Pts',(0.0322095253359853,-5.25189980247768,
4.65917598249656));
#31550=CARTESIAN_POINT('Ctrl Pts',(0.0415665688189868,-5.2533028153276,
4.65750148702094));
#31551=CARTESIAN_POINT('Ctrl Pts',(0.0736350348471512,-5.25994632142597,
4.64948528566701));
#31552=CARTESIAN_POINT('Ctrl Pts',(0.0945710803031181,-5.26763660382283,
4.64009844156318));
#31553=CARTESIAN_POINT('Ctrl Pts',(0.132235154392271,-5.28676363878307,
4.61539308723159));
#31554=CARTESIAN_POINT('Ctrl Pts',(0.14849663584321,-5.2980653181186,4.60019195379196));
#31555=CARTESIAN_POINT('Ctrl Pts',(0.180499640843384,-5.32537773353357,
4.56080656181528));
#31556=CARTESIAN_POINT('Ctrl Pts',(0.194416032106083,-5.34169360047391,
4.53533737515855));
#31557=CARTESIAN_POINT('Ctrl Pts',(0.220758455803108,-5.379562093598,4.46952174021342));
#31558=CARTESIAN_POINT('Ctrl Pts',(0.231081290935903,-5.4021794004279,4.42457618200302));
#31559=CARTESIAN_POINT('Ctrl Pts',(0.250896331361498,-5.46315994101279,
4.27073174534988));
#31560=CARTESIAN_POINT('Ctrl Pts',(0.249935425544557,-5.49431818181818,
4.14407324412993));
#31561=CARTESIAN_POINT('Ctrl Pts',(0.249935425544557,-5.49431818181818,
4.));
#31562=CARTESIAN_POINT('Origin',(0.,-5.5,0.));
#31563=CARTESIAN_POINT('',(-0.249935425544577,-5.49431818181818,0.));
#31564=CARTESIAN_POINT('Origin',(0.,0.,0.));
#31565=CARTESIAN_POINT('Origin',(0.,0.,5.));
#31566=CARTESIAN_POINT('Origin',(0.,0.,35.));
#33462=UNCERTAINTY_MEASURE_WITH_UNIT(LENGTH_MEASURE(0.01),#33475,
'DISTANCE_ACCURACY_VALUE',
'Maximum model space distance between geometric entities at asserted c
onnectivities');
#33467=UNCERTAINTY_MEASURE_WITH_UNIT(LENGTH_MEASURE(0.01),#33475,
'DISTANCE_ACCURACY_VALUE',
'Maximum model space distance between geometric entities at asserted c
onnectivities');
#33469=(
GEOMETRIC_REPRESENTATION_CONTEXT(3)
GLOBAL_UNCERTAINTY_ASSIGNED_CONTEXT((#33462))
GLOBAL_UNIT_ASSIGNED_CONTEXT((#33475,#33477,#33478))
REPRESENTATION_CONTEXT('','3D')
);
#33474=(
GEOMETRIC_REPRESENTATION_CONTEXT(3)
GLOBAL_UNCERTAINTY_ASSIGNED_CONTEXT((#33467))
GLOBAL_UNIT_ASSIGNED_CONTEXT((#33475,#33477,#33478))
REPRESENTATION_CONTEXT('','3D')
);
#33475=(
LENGTH_UNIT()
NAMED_UNIT(*)
SI_UNIT(.MILLI.,.METRE.)
);
#33477=(
NAMED_UNIT(*)
PLANE_ANGLE_UNIT()
SI_UNIT($,.RADIAN.)
);
#33478=(
NAMED_UNIT(*)
SI_UNIT($,.STERADIAN.)
SOLID_ANGLE_UNIT()
);
#33480=SHAPE_DEFINITION_REPRESENTATION(#33486,#33497);
#33486=PRODUCT_DEFINITION_SHAPE('',$,#33504);
#33497=SHAPE_REPRESENTATION('',(#2869),#33469);
#33502=PRODUCT_DEFINITION_CONTEXT('part definition',#33522,'design');
#33504=PRODUCT_DEFINITION('Screw','Screw',#33510,#33502);
#33510=PRODUCT_DEFINITION_FORMATION('',$,#33525);
#33522=APPLICATION_CONTEXT(
'Core Data for Automotive Mechanical Design Process');
#33523=PRODUCT_CONTEXT('part definition',#33522,'mechanical');
#33525=PRODUCT('Screw','Screw',$,(#33523));
#33531=PRESENTATION_STYLE_ASSIGNMENT((#33533));
#33533=SURFACE_STYLE_USAGE(.BOTH.,#33535);
#33535=SURFACE_SIDE_STYLE('',(#33537));
#33537=SURFACE_STYLE_FILL_AREA(#33539);
#33539=FILL_AREA_STYLE('Opaque(203,203,203)',(#33541));
#33541=FILL_AREA_STYLE_COLOUR('Opaque(203,203,203)',#33543);
#33543=COLOUR_RGB('Opaque(203,203,203)', 0.09019608, 0.27058824, 0.51372549);
ENDSEC;
END-ISO-10303-21;
